ISO-10303-21;
HEADER;
FILE_DESCRIPTION (('STEP AP214'),
    '1' );
FILE_NAME ( 'U-Bolt.step', '2026-10-04T02:08:54', ( '' ), ( '' ), 'STEP AP214', 'Unspecified', '' );
FILE_SCHEMA (( 'AUTOMOTIVE_DESIGN' ));
ENDSEC;
DATA;
#1=ORIENTED_EDGE ( 'NONE', *, *, #31259, .T. ) ;
#3=CARTESIAN_POINT ( 'NONE',  ( -0.7646288533564489232, -0.1113553986120547346, 1.136811023622047223 ) ) ;
#8=FACE_OUTER_BOUND ( 'NONE', #9994, .T. ) ;
#9=CARTESIAN_POINT ( 'NONE',  ( 0.8019270111902717657, 0.1787899950787401604, 1.727362204670645385 ) ) ;
#10=CARTESIAN_POINT ( 'NONE',  ( 0.7495606340400177148, 0.1264236179284866091, 0.3518700786863940833 ) ) ;
#11=CARTESIAN_POINT ( 'NONE',  ( 0.7185039370078746268, -0.06523048226347956391, 0.3075787401574804347 ) ) ;
#17=CARTESIAN_POINT ( 'NONE',  ( 0.8019270111902717657, -0.1787899950787401604, 0.6791338582139527791 ) ) ;
#19=DIRECTION ( 'NONE',  ( 0.000000000000000000, 0.000000000000000000, -1.000000000000000000 ) ) ;
#22=EDGE_CURVE ( 'NONE', #36685, #42555, #8791, .T. ) ;
#23=CARTESIAN_POINT ( 'NONE',  ( -0.8759842519685039353, 0.1574803149606299191, 1.309055118002708573 ) ) ;
#24=CARTESIAN_POINT ( 'NONE',  ( 0.6971942568897637749, 2.189545951927499583E-17, 1.739665354276945131 ) ) ;
#27=CARTESIAN_POINT ( 'NONE',  ( 0.8759842519685039353, 0.1787899950787401882, 0.5044291338045039375 ) ) ;
#32=CARTESIAN_POINT ( 'NONE',  ( -0.8759842519685039353, 0.1787899950787401882, 0.4699803149068661479 ) ) ;
#35=FACE_OUTER_BOUND ( 'NONE', #16706, .T. ) ;
#36=ADVANCED_FACE ( 'NONE', ( #44420 ), #33931, .T. ) ;
#38=CARTESIAN_POINT ( 'NONE',  ( -0.8759842519685039353, -0.1787899950787401882, 1.587106299158834721 ) ) ;
#40=CARTESIAN_POINT ( 'NONE',  ( -0.6971942568897648851, 0.07405724077823318263, 1.186023621993481658 ) ) ;
#41=CYLINDRICAL_SURFACE ( 'NONE', #813, 0.1574803149606299191 ) ;
#42=CARTESIAN_POINT ( 'NONE',  ( 0.6971942568897648851, -0.07405724077823297447, 1.112204724355684959 ) ) ;
#44=CARTESIAN_POINT ( 'NONE',  ( 0.6971942568897637749, 2.189545951927499583E-17, 1.813484251914740053 ) ) ;
#45=CARTESIAN_POINT ( 'NONE',  ( -1.033464566929133799, 0.000000000000000000, 0.5610236220472440971 ) ) ;
#46=CARTESIAN_POINT ( 'NONE',  ( -0.8019270111902717657, -0.1787899950787401604, 0.9940944881352130613 ) ) ;
#47=EDGE_CURVE ( 'NONE', #46518, #3252, #13426, .T. ) ;
#49=DIRECTION ( 'NONE',  ( 1.822029033848725028E-16, 0.000000000000000000, 1.000000000000000000 ) ) ;
#50=CARTESIAN_POINT ( 'NONE',  ( 1.002407869896990045, 0.1264236179284866091, 0.3469488188438744070 ) ) ;
#51=CARTESIAN_POINT ( 'NONE',  ( -0.6971942568897637749, 2.189545951927499583E-17, 0.2780511810485988278 ) ) ;
#52=CARTESIAN_POINT ( 'NONE',  ( 0.7646288533564489232, -0.1113553986120547346, 1.678149606191684962 ) ) ;
#53=ORIENTED_EDGE ( 'NONE', *, *, #45978, .F. ) ;
#54=VECTOR ( 'NONE', #41568, 39.37007874015748143 ) ;
#56=CARTESIAN_POINT ( 'NONE',  ( 0.7495606340400177148, 0.1264236179284866091, 0.7898622046706456068 ) ) ;
#57=CARTESIAN_POINT ( 'NONE',  ( 0.8759842519685039353, -0.1787899950787401882, 1.040846456639149764 ) ) ;
#58=CARTESIAN_POINT ( 'NONE',  ( -0.9500414927467377701, -0.1787899950787401604, 1.825787401521040243 ) ) ;
#59=ORIENTED_EDGE ( 'NONE', *, *, #22403, .F. ) ;
#61=AXIS2_PLACEMENT_3D ( 'NONE', #5298, #38366, #19916 ) ;
#62=( BOUNDED_CURVE ( )  B_SPLINE_CURVE ( 2, ( #7459, #22081, #47251, #3868, #22310, #18713, #36940, #14196, #13878 ),
 .UNSPECIFIED., .F., .F. ) 
 B_SPLINE_CURVE_WITH_KNOTS ( ( 3, 2, 2, 2, 3 ),
 ( 0.05000000000000000278, 0.05249999999999999806, 0.05500000000000000028, 0.05750000000000000250, 0.05999999999999999778 ),
 .UNSPECIFIED. ) 
 CURVE ( )  GEOMETRIC_REPRESENTATION_ITEM ( )  RATIONAL_B_SPLINE_CURVE ( ( 1.000000000000000000, 0.9238795325112869605, 1.000000000000000000, 0.9238795325112869605, 1.000000000000000000, 0.9238795325112869605, 1.000000000000000000, 0.9238795325112869605, 1.000000000000000000 ) ) 
 REPRESENTATION_ITEM ( '' )  ) ;
#63=DIRECTION ( 'NONE',  ( 1.822029033848725028E-16, 0.000000000000000000, 1.000000000000000000 ) ) ;
#68=CARTESIAN_POINT ( 'NONE',  ( 1.002407869896990045, 0.1264236179284866091, 1.208169291284818980 ) ) ;
#71=CARTESIAN_POINT ( 'NONE',  ( -0.7646288533564489232, 0.1113553986120547346, 0.9990157479239685223 ) ) ;
#72=CARTESIAN_POINT ( 'NONE',  ( 0.8759842519685039353, 0.1787899950787401882, 1.488681102308440751 ) ) ;
#73=CARTESIAN_POINT ( 'NONE',  ( 0.7646288533564489232, 0.1113553986120547346, 1.914370078740157632 ) ) ;
#75=CIRCLE ( 'NONE', #20007, 0.1787899950787401049 ) ;
#76=CARTESIAN_POINT ( 'NONE',  ( -0.6971942568897637749, 2.189545951927499583E-17, 0.4404527558517480901 ) ) ;
#79=CARTESIAN_POINT ( 'NONE',  ( -0.7240989362502219251, -0.07281704346119359517, 1.984672674023657102 ) ) ;
#81=CARTESIAN_POINT ( 'NONE',  ( 1.054774247047244540, 0.07405724077823318263, 1.249999999946235896 ) ) ;
#82=CARTESIAN_POINT ( 'NONE',  ( 1.054774247047244540, -0.07405724077823318263, 1.712598425143087466 ) ) ;
#84=CARTESIAN_POINT ( 'NONE',  ( 0.7646288533564489232, 0.1113553986120547346, 1.510826771546015523 ) ) ;
#90=CARTESIAN_POINT ( 'NONE',  ( 0.7646288533564489232, 0.1113553986120547346, 0.7627952754830236159 ) ) ;
#91=CARTESIAN_POINT ( 'NONE',  ( 0.7013496418058506876, 0.02137559083948704225, 0.03937007727944009938 ) ) ;
#93=CARTESIAN_POINT ( 'NONE',  ( 0.8019270111902716547, -0.1787899950787401604, 1.269685039316314601 ) ) ;
#97=CARTESIAN_POINT ( 'NONE',  ( 0.9412147342319837628, -0.1574803149606297803, 0.5831692912310553201 ) ) ;
#99=DIRECTION ( 'NONE',  ( 1.822029033848725028E-16, 0.000000000000000000, 1.000000000000000000 ) ) ;
#100=CARTESIAN_POINT ( 'NONE',  ( 0.9656857656210602325, 0.1425117190157106917, 0.03937007042889534292 ) ) ;
#101=CARTESIAN_POINT ( 'NONE',  ( -1.033464566929134687, -0.06523048226347956391, 0.3124999998924728462 ) ) ;
#102=CARTESIAN_POINT ( 'NONE',  ( -0.7185039370078746268, -0.06523048226347956391, 0.4158464565853862704 ) ) ;
#104=CARTESIAN_POINT ( 'NONE',  ( 0.9500414927467378812, -0.1787899950787401604, 1.432086614119464141 ) ) ;
#105=CARTESIAN_POINT ( 'NONE',  ( -0.8107537697050253289, 0.1574803149606300301, 1.163877952755904666 ) ) ;
#107=CARTESIAN_POINT ( 'NONE',  ( -1.033464566929133355, 0.06523048226348168721, 1.626476377952755570 ) ) ;
#108=CARTESIAN_POINT ( 'NONE',  ( 0.7185039370078739607, 1.928577636452523993E-17, 1.683070866141732402 ) ) ;
#110=VERTEX_POINT ( 'NONE', #36790 ) ;
#111=CARTESIAN_POINT ( 'NONE',  ( 0.7185039370078746268, -0.06523048226347956391, 0.6520669290263312323 ) ) ;
#112=DIRECTION ( 'NONE',  ( 1.822029033848725028E-16, 0.000000000000000000, 1.000000000000000000 ) ) ;
#114=CARTESIAN_POINT ( 'NONE',  ( 0.6971942568897626646, 0.07405724077823318263, 0.5954724408911187261 ) ) ;
#115=ORIENTED_EDGE ( 'NONE', *, *, #9426, .T. ) ;
#116=CARTESIAN_POINT ( 'NONE',  ( -0.8019270111902716547, 0.1787899950787401604, 1.451771653489543290 ) ) ;
#118=CARTESIAN_POINT ( 'NONE',  ( -1.002407869896990045, -0.1264236179284866091, 1.163877952702141672 ) ) ;
#121=CARTESIAN_POINT ( 'NONE',  ( -0.8019270111902717657, 0.1787899950787401604, 0.8661417322297003674 ) ) ;
#123=CARTESIAN_POINT ( 'NONE',  ( 0.8107537697050254399, -0.1574803149606297803, 0.6668307086614162493 ) ) ;
#128=VECTOR ( 'NONE', #18538, 39.37007874015748143 ) ;
#129=CARTESIAN_POINT ( 'NONE',  ( 0.7185039370078739607, 1.928577636452523993E-17, 0.9645669290263307882 ) ) ;
#131=CARTESIAN_POINT ( 'NONE',  ( -0.9500414927467378812, -0.1787899950787401604, 0.8021653542769460188 ) ) ;
#134=CARTESIAN_POINT ( 'NONE',  ( -0.8019270111902716547, -0.1787899950787401604, 1.865157480261198097 ) ) ;
#137=CARTESIAN_POINT ( 'NONE',  ( 0.7185039370078746268, -0.06523048226347956391, 0.6225393700787401619 ) ) ;
#139=FACE_OUTER_BOUND ( 'NONE', #32124, .T. ) ;
#140=CARTESIAN_POINT ( 'NONE',  ( -0.8759842519685039353, 0.1574803149606299191, 1.466535432963338437 ) ) ;
#141=EDGE_CURVE ( 'NONE', #480, #43073, #20129, .T. ) ;
#142=CARTESIAN_POINT ( 'NONE',  ( 0.9500414927467378812, -0.1787899950787401604, 0.7283464566391493200 ) ) ;
#144=CARTESIAN_POINT ( 'NONE',  ( 0.9873396505805591694, -0.1113553986120547346, 1.343503937007874072 ) ) ;
#146=CARTESIAN_POINT ( 'NONE',  ( 0.9356431618536311667, -0.1660064224309732994, 1.989266148032244885 ) ) ;
#151=CIRCLE ( 'NONE', #10128, 0.1787899950787401049 ) ;
#153=CARTESIAN_POINT ( 'NONE',  ( 0.7495606340400177148, -0.1264236179284866091, 0.8341535432533228045 ) ) ;
#158=CARTESIAN_POINT ( 'NONE',  ( -0.7646288533564489232, 0.1113553986120547346, 1.166338582677165281 ) ) ;
#161=CARTESIAN_POINT ( 'NONE',  ( 0.6971942568897637749, 2.189545951927499583E-17, 0.9867125983714331028 ) ) ;
#162=EDGE_CURVE ( 'NONE', #28497, #15222, #36387, .T. ) ;
#165=CARTESIAN_POINT ( 'NONE',  ( -0.8107537697050254399, -0.1574803149606297803, 0.5093503937007877180 ) ) ;
#166=ORIENTED_EDGE ( 'NONE', *, *, #15392, .T. ) ;
#168=CARTESIAN_POINT ( 'NONE',  ( -0.8019270111902717657, 0.1787899950787401604, 0.1131889763241894359 ) ) ;
#169=ORIENTED_EDGE ( 'NONE', *, *, #21607, .F. ) ;
#170=CARTESIAN_POINT ( 'NONE',  ( -0.9873396505805591694, -0.1113553986120547346, 0.7135826771653542844 ) ) ;
#172=CARTESIAN_POINT ( 'NONE',  ( -0.9873396505805591694, -0.1113553986120547346, 1.855314960629921295 ) ) ;
#173=CARTESIAN_POINT ( 'NONE',  ( -1.002407869896990045, -0.1264236179284866091, 1.631397637741511808 ) ) ;
#174=CARTESIAN_POINT ( 'NONE',  ( -1.033464566929133799, 0.000000000000000000, 0.1181102361129454797 ) ) ;
#176=CARTESIAN_POINT ( 'NONE',  ( 0.9500414927467378812, 0.1787899950787401604, 0.02952755900135462311 ) ) ;
#179=CARTESIAN_POINT ( 'NONE',  ( 0.8759842519685039353, 0.000000000000000000, 4.498031496062992574 ) ) ;
#180=DIRECTION ( 'NONE',  ( 1.822029033848725028E-16, 0.000000000000000000, 1.000000000000000000 ) ) ;
#181=CARTESIAN_POINT ( 'NONE',  ( -0.9500414927467378812, 0.1787899950787401604, 0.3051181101824569919 ) ) ;
#184=ORIENTED_EDGE ( 'NONE', *, *, #3239, .T. ) ;
#185=CARTESIAN_POINT ( 'NONE',  ( -0.8019270111902716547, -0.1787899950787401604, 1.313976377898992132 ) ) ;
#194=CARTESIAN_POINT ( 'NONE',  ( 0.8759842519685039353, 0.1574803149606299191, 0.3346456692913385988 ) ) ;
#196=CARTESIAN_POINT ( 'NONE',  ( -0.8107537697050253289, -0.1574803149606297803, 1.011318897530268712 ) ) ;
#197=VECTOR ( 'NONE', #24397, 39.37007874015748143 ) ;
#198=ADVANCED_FACE ( 'NONE', ( #20458 ), #16639, .T. ) ;
#199=CARTESIAN_POINT ( 'NONE',  ( 0.6971942568897637749, 2.189545951927499583E-17, 0.4010826771115905687 ) ) ;
#201=CARTESIAN_POINT ( 'NONE',  ( 0.7185039370078746268, 0.06523048226347956391, 1.906988188868851797 ) ) ;
#202=EDGE_LOOP ( 'NONE', ( #15956, #3484, #38224, #16323 ) ) ;
#203=DIRECTION ( 'NONE',  ( 0.000000000000000000, 0.000000000000000000, -1.000000000000000000 ) ) ;
#204=CARTESIAN_POINT ( 'NONE',  ( 0.7185039370078746268, -0.06523048226347956391, 0.9374999999999991118 ) ) ;
#205=CARTESIAN_POINT ( 'NONE',  ( -1.033464566929133799, 0.000000000000000000, 0.6692913384751496553 ) ) ;
#207=CARTESIAN_POINT ( 'NONE',  ( 0.8759842519685039353, 0.000000000000000000, 4.498031496062992574 ) ) ;
#208=CARTESIAN_POINT ( 'NONE',  ( 0.7185039370078746268, -0.06523048226347956391, 0.7406496062992133922 ) ) ;
#209=CARTESIAN_POINT ( 'NONE',  ( -0.7185039370078739607, 1.928577636452523993E-17, 0.7677165353255432922 ) ) ;
#217=CARTESIAN_POINT ( 'NONE',  ( 1.033464566929134687, -0.06523048226347956391, 0.9424212597349932441 ) ) ;
#218=CARTESIAN_POINT ( 'NONE',  ( 0.7185039370078746268, 0.06523048226347956391, 0.5388779527559055538 ) ) ;
#219=VECTOR ( 'NONE', #41742, 39.37007874015748143 ) ;
#220=EDGE_CURVE ( 'NONE', #8537, #45765, #3616, .T. ) ;
#221=ORIENTED_EDGE ( 'NONE', *, *, #44499, .F. ) ;
#224=CARTESIAN_POINT ( 'NONE',  ( -1.054774247047244096, 0.000000000000000000, 1.562499999946236118 ) ) ;
#225=CARTESIAN_POINT ( 'NONE',  ( 0.6971942568897648851, 0.07405724077823318263, 1.697834645615527771 ) ) ;
#227=CARTESIAN_POINT ( 'NONE',  ( -0.9500414927467378812, -0.1787899950787401604, 0.7283464566391493200 ) ) ;
#231=CARTESIAN_POINT ( 'NONE',  ( 1.054774247047244096, 0.000000000000000000, 0.3420275590013546751 ) ) ;
#233=CARTESIAN_POINT ( 'NONE',  ( -0.6971942568897648851, 0.07405724077823318263, 1.220472440891118504 ) ) ;
#234=CARTESIAN_POINT ( 'NONE',  ( -0.7495606340400177148, -0.1264236179284866091, 0.6373031495525354195 ) ) ;
#235=DIRECTION ( 'NONE',  ( 1.000000000000000000, 0.000000000000000000, -1.822029033848725275E-16 ) ) ;
#236=( BOUNDED_CURVE ( )  B_SPLINE_CURVE ( 2, ( #18764, #29842, #25754, #33895, #32949, #1015, #4363, #41246, #25970 ),
 .UNSPECIFIED., .F., .T. ) 
 B_SPLINE_CURVE_WITH_KNOTS ( ( 3, 2, 2, 2, 3 ),
 ( 0.4000000000000000222, 0.4025000000000000244, 0.4050000000000000266, 0.4074999999999999734, 0.4099999999999999756 ),
 .UNSPECIFIED. ) 
 CURVE ( )  GEOMETRIC_REPRESENTATION_ITEM ( )  RATIONAL_B_SPLINE_CURVE ( ( 1.000000000000000000, 0.9238795325112869605, 1.000000000000000000, 0.9238795325112869605, 1.000000000000000000, 0.9238795325112869605, 1.000000000000000000, 0.9238795325112849621, 1.000000000000000000 ) ) 
 REPRESENTATION_ITEM ( '' )  ) ;
#238=DIRECTION ( 'NONE',  ( -1.000000000000000000, 0.000000000000000000, 0.000000000000000000 ) ) ;
#239=CARTESIAN_POINT ( 'NONE',  ( -0.8759842519685039353, 0.1787899950787401882, 1.572342519631275692 ) ) ;
#240=CARTESIAN_POINT ( 'NONE',  ( -0.7185039370078739607, 1.928577636452523993E-17, 1.948818897530267602 ) ) ;
#242=CARTESIAN_POINT ( 'NONE',  ( -0.9412147342319837628, -0.1574803149606297803, 1.656003937007873406 ) ) ;
#243=( BOUNDED_CURVE ( )  B_SPLINE_CURVE ( 2, ( #38368, #35271, #35028, #17505, #31910, #27861, #39299, #28309, #42180 ),
 .UNSPECIFIED., .F., .F. ) 
 B_SPLINE_CURVE_WITH_KNOTS ( ( 3, 2, 2, 2, 3 ),
 ( 0.4500000000000000111, 0.4525000000000000133, 0.4550000000000000155, 0.4575000000000000178, 0.4600000000000000200 ),
 .UNSPECIFIED. ) 
 CURVE ( )  GEOMETRIC_REPRESENTATION_ITEM ( )  RATIONAL_B_SPLINE_CURVE ( ( 1.000000000000000000, 0.9238795325112869605, 1.000000000000000000, 0.9238795325112869605, 1.000000000000000000, 0.9238795325112869605, 1.000000000000000000, 0.9238795325112869605, 1.000000000000000000 ) ) 
 REPRESENTATION_ITEM ( '' )  ) ;
#245=CARTESIAN_POINT ( 'NONE',  ( 0.8019270111902716547, -0.1787899950787401604, 1.471456692859622217 ) ) ;
#247=ORIENTED_EDGE ( 'NONE', *, *, #10180, .F. ) ;
#249=ORIENTED_EDGE ( 'NONE', *, *, #21041, .T. ) ;
#251=EDGE_CURVE ( 'NONE', #13767, #23712, #510, .T. ) ;
#256=CARTESIAN_POINT ( 'NONE',  ( 0.7185039370078739607, 0.000000000000000000, 4.498031496062992574 ) ) ;
#257=CARTESIAN_POINT ( 'NONE',  ( 0.7495606340400177148, 0.1264236179284866091, 1.729822834591905556 ) ) ;
#265=CARTESIAN_POINT ( 'NONE',  ( 1.054774247047244540, -0.07405724077823318263, 0.7283464566391493200 ) ) ;
#270=CARTESIAN_POINT ( 'NONE',  ( 0.8019270111902717657, -0.1787899950787401604, 1.786417322780882388 ) ) ;
#271=CYLINDRICAL_SURFACE ( 'NONE', #38342, 0.1574803149606299191 ) ;
#272=CARTESIAN_POINT ( 'NONE',  ( 0.6971942568897637749, 2.189545951927499583E-17, 0.5142716534895434011 ) ) ;
#274=CARTESIAN_POINT ( 'NONE',  ( 1.033464566929134687, -0.06523048226347956391, 0.08612204724409450174 ) ) ;
#277=CARTESIAN_POINT ( 'NONE',  ( -0.8759842519685039353, -0.1787899950787401882, 0.4502952755367874427 ) ) ;
#280=CARTESIAN_POINT ( 'NONE',  ( 0.6971942568897626646, -0.07405724077823297447, 0.2460629920722207375 ) ) ;
#282=CARTESIAN_POINT ( 'NONE',  ( -0.6971942568897648851, 0.07405724077823318263, 1.535433070812378675 ) ) ;
#283=ORIENTED_EDGE ( 'NONE', *, *, #46313, .T. ) ;
#284=CARTESIAN_POINT ( 'NONE',  ( -0.8759842519685039353, 0.1787899950787401882, 1.218011810969858111 ) ) ;
#285=CARTESIAN_POINT ( 'NONE',  ( -0.8107537697050254399, 0.1574803149606300301, 0.3371062992125987146 ) ) ;
#286=CARTESIAN_POINT ( 'NONE',  ( 0.9500414927467378812, 0.1787899950787401604, 1.254921259788757348 ) ) ;
#288=CARTESIAN_POINT ( 'NONE',  ( 1.054774247047244096, 0.000000000000000000, 1.951279527505291433 ) ) ;
#289=CARTESIAN_POINT ( 'NONE',  ( -0.8759842519685039353, 0.1574803149606299191, 0.6496062992125984925 ) ) ;
#290=CARTESIAN_POINT ( 'NONE',  ( -0.6971942568897648851, -0.07405724077823297447, 1.028543307032851795 ) ) ;
#291=CARTESIAN_POINT ( 'NONE',  ( -0.7185039370078739607, 1.928577636452523993E-17, 1.604330708661417360 ) ) ;
#293=CARTESIAN_POINT ( 'NONE',  ( 0.8759842519685039353, -0.1787899950787401882, 0.3715551180564728440 ) ) ;
#294=CARTESIAN_POINT ( 'NONE',  ( -1.002407869896990045, -0.1264236179284866091, 0.1747047243556852092 ) ) ;
#295=CARTESIAN_POINT ( 'NONE',  ( 0.7185039370078746268, 0.06523048226347956391, 1.670767716427906002 ) ) ;
#296=ORIENTED_EDGE ( 'NONE', *, *, #20298, .F. ) ;
#298=ORIENTED_EDGE ( 'NONE', *, *, #27985, .F. ) ;
#299=CARTESIAN_POINT ( 'NONE',  ( 1.002407869896990045, 0.1264236179284866091, 0.8981299212060788184 ) ) ;
#300=CARTESIAN_POINT ( 'NONE',  ( 0.9500414927467377701, -0.1787899950787401604, 1.082677165300567346 ) ) ;
#301=CARTESIAN_POINT ( 'NONE',  ( -0.8759842519685039353, -0.1787899950787401882, 1.823326771599779406 ) ) ;
#304=CARTESIAN_POINT ( 'NONE',  ( 1.054774247047244540, 0.07405724077823318263, 1.953740157426552715 ) ) ;
#311=ORIENTED_EDGE ( 'NONE', *, *, #11167, .T. ) ;
#312=CARTESIAN_POINT ( 'NONE',  ( 0.8019270111902717657, 0.1787899950787401604, 1.136811023568283119 ) ) ;
#314=CARTESIAN_POINT ( 'NONE',  ( -0.8759842519685039353, 0.1574803149606299191, 0.9940944880814488460 ) ) ;
#316=CARTESIAN_POINT ( 'NONE',  ( 0.9500414927467378812, 0.1787899950787401604, 0.1870078739619845387 ) ) ;
#321=EDGE_CURVE ( 'NONE', #8150, #39441, #13683, .T. ) ;
#322=CARTESIAN_POINT ( 'NONE',  ( -0.8759842519685039353, -0.1787899950787401882, 0.5290354330171024300 ) ) ;
#325=CARTESIAN_POINT ( 'NONE',  ( 1.033464566929134687, 0.06523048226347956391, 1.429625984251967852 ) ) ;
#327=CARTESIAN_POINT ( 'NONE',  ( 1.002407869896990045, 0.1264236179284866091, 1.409940944828126153 ) ) ;
#328=CARTESIAN_POINT ( 'NONE',  ( 0.6971942568897648851, 0.07405724077823318263, 1.732283464513166615 ) ) ;
#332=CARTESIAN_POINT ( 'NONE',  ( 0.7185039370078714072, 0.06523048226347728795, 1.513287401467276583 ) ) ;
#334=CARTESIAN_POINT ( 'NONE',  ( 0.7185039370078746268, -0.06523048226347956391, 0.8095472439869610959 ) ) ;
#337=CARTESIAN_POINT ( 'NONE',  ( 0.7185039370078739607, 1.928577636452523993E-17, 0.7677165353255432922 ) ) ;
#338=CARTESIAN_POINT ( 'NONE',  ( 1.002407869896990045, 0.1264236179284866091, 1.286909448765133801 ) ) ;
#341=CARTESIAN_POINT ( 'NONE',  ( 0.7185039370078739607, 0.000000000000000000, 4.498031496062992574 ) ) ;
#342=CARTESIAN_POINT ( 'NONE',  ( -0.7495606340400177148, -0.1264236179284866091, 1.267224409395055096 ) ) ;
#343=CARTESIAN_POINT ( 'NONE',  ( 0.7646288533564489232, -0.1113553986120547346, 0.6545275589475906264 ) ) ;
#344=ORIENTED_EDGE ( 'NONE', *, *, #39545, .F. ) ;
#345=CARTESIAN_POINT ( 'NONE',  ( -0.7185039370078739607, 1.928577636452523993E-17, 1.761811023622047223 ) ) ;
#348=CARTESIAN_POINT ( 'NONE',  ( 0.9412147342319837628, -0.1574803149606297803, 0.2780511811023620439 ) ) ;
#352=CARTESIAN_POINT ( 'NONE',  ( 0.9500414927467378812, 0.1787899950787401604, 1.643700787347811998 ) ) ;
#353=CARTESIAN_POINT ( 'NONE',  ( -0.8759842519685039353, 0.1574803149606299191, 0.9251968503937008093 ) ) ;
#354=CARTESIAN_POINT ( 'NONE',  ( -0.7185039370078732945, -0.06523048226347920309, 0.1107283464566930498 ) ) ;
#355=CARTESIAN_POINT ( 'NONE',  ( 0.7646288533564489232, -0.1113553986120547346, 1.176181102362204633 ) ) ;
#358=( BOUNDED_CURVE ( )  B_SPLINE_CURVE ( 2, ( #11263, #3350, #25876, #28789, #17960, #43354, #17490, #32615, #32121 ),
 .UNSPECIFIED., .F., .T. ) 
 B_SPLINE_CURVE_WITH_KNOTS ( ( 3, 2, 2, 2, 3 ),
 ( 0.2300000000000000100, 0.2325000000000000122, 0.2349999999999999867, 0.2374999999999999889, 0.2399999999999999911 ),
 .UNSPECIFIED. ) 
 CURVE ( )  GEOMETRIC_REPRESENTATION_ITEM ( )  RATIONAL_B_SPLINE_CURVE ( ( 1.000000000000000000, 0.9238795325112869605, 1.000000000000000000, 0.9238795325112869605, 1.000000000000000000, 0.9238795325112869605, 1.000000000000000000, 0.9238795325112869605, 1.000000000000000000 ) ) 
 REPRESENTATION_ITEM ( '' )  ) ;
#359=DIRECTION ( 'NONE',  ( 1.822029033848725028E-16, 0.000000000000000000, 1.000000000000000000 ) ) ;
#361=CARTESIAN_POINT ( 'NONE',  ( 1.054774247047244540, -0.07405724077823318263, 0.6545275590013545086 ) ) ;
#363=CARTESIAN_POINT ( 'NONE',  ( 0.8759842519685039353, 0.1787899950787401882, 0.8243110235682834519 ) ) ;
#365=CARTESIAN_POINT ( 'NONE',  ( -0.8759842519685039353, -0.1787899950787401882, 1.277066929080094448 ) ) ;
#366=CARTESIAN_POINT ( 'NONE',  ( -0.7495606340400177148, 0.1264236179284866091, 0.1599409448281264023 ) ) ;
#367=LINE ( 'NONE', #8269, #13455 ) ;
#374=CARTESIAN_POINT ( 'NONE',  ( 1.054774247047244096, 0.000000000000000000, 1.006397637741511808 ) ) ;
#376=( BOUNDED_CURVE ( )  B_SPLINE_CURVE ( 2, ( #44031, #36857, #22706, #4461, #11233, #44728, #15066, #25618, #15540 ),
 .UNSPECIFIED., .F., .T. ) 
 B_SPLINE_CURVE_WITH_KNOTS ( ( 3, 2, 2, 2, 3 ),
 ( 0.07000000000000000666, 0.07249999999999999500, 0.07499999999999999722, 0.07749999999999999944, 0.08000000000000000167 ),
 .UNSPECIFIED. ) 
 CURVE ( )  GEOMETRIC_REPRESENTATION_ITEM ( )  RATIONAL_B_SPLINE_CURVE ( ( 1.000000000000000000, 0.9238795325112859613, 1.000000000000000000, 0.9238795325112869605, 1.000000000000000000, 0.9238795325112869605, 1.000000000000000000, 0.9238795325112869605, 1.000000000000000000 ) ) 
 REPRESENTATION_ITEM ( '' )  ) ;
#377=CARTESIAN_POINT ( 'NONE',  ( -1.054774247047244540, -0.07405724077823318263, 0.7283464566391493200 ) ) ;
#381=CARTESIAN_POINT ( 'NONE',  ( -1.002407869896990045, 0.1264236179284866091, 0.07135826766277185429 ) ) ;
#382=CARTESIAN_POINT ( 'NONE',  ( -0.8759842519685039353, 0.1574803149606299191, 0.9251968503937008093 ) ) ;
#385=CARTESIAN_POINT ( 'NONE',  ( -0.7185039370078739607, 1.928577636452523993E-17, 1.594488188868850242 ) ) ;
#386=CARTESIAN_POINT ( 'NONE',  ( 0.8019270111902717657, -0.1787899950787401604, 0.7234251967966300878 ) ) ;
#387=CARTESIAN_POINT ( 'NONE',  ( 0.7495606340400177148, -0.1264236179284866091, 1.345964566875370139 ) ) ;
#390=CARTESIAN_POINT ( 'NONE',  ( 0.7125413026092556334, -0.03488858553940781676, 1.983914878791770864 ) ) ;
#393=CARTESIAN_POINT ( 'NONE',  ( 1.054774247047244096, 0.000000000000000000, 0.8095472440407244230 ) ) ;
#398=VERTEX_POINT ( 'NONE', #6064 ) ;
#401=DIRECTION ( 'NONE',  ( 1.822029033848725028E-16, 0.000000000000000000, 1.000000000000000000 ) ) ;
#402=CARTESIAN_POINT ( 'NONE',  ( 0.8019270111902717657, 0.1787899950787401604, 0.9399606298674970661 ) ) ;
#403=DIRECTION ( 'NONE',  ( 1.000000000000000000, 0.000000000000000000, -1.822029033848725275E-16 ) ) ;
#409=CARTESIAN_POINT ( 'NONE',  ( -0.8019270111902717657, 0.1787899950787401604, 0.2706692912848194243 ) ) ;
#410=CARTESIAN_POINT ( 'NONE',  ( 0.9873396505805591694, 0.1113553986120547346, 0.3297244094488189226 ) ) ;
#411=CARTESIAN_POINT ( 'NONE',  ( -0.7495606340400177148, 0.1264236179284866091, 1.611712598371433103 ) ) ;
#412=CARTESIAN_POINT ( 'NONE',  ( -0.6971942568897648851, 0.07405724077823318263, 0.9055118109698584439 ) ) ;
#413=CARTESIAN_POINT ( 'NONE',  ( -0.9500414927467378812, -0.1787899950787401604, 0.3346456692375748831 ) ) ;
#416=CARTESIAN_POINT ( 'NONE',  ( 0.6971942568897626646, 0.07405724077823318263, 0.03937007868639404856 ) ) ;
#420=CARTESIAN_POINT ( 'NONE',  ( -0.8107537697050254399, 0.1574803149606300301, 1.902066929026330566 ) ) ;
#423=CARTESIAN_POINT ( 'NONE',  ( -0.8019270111902717657, 0.1787899950787401604, 0.3100393700249766682 ) ) ;
#425=CARTESIAN_POINT ( 'NONE',  ( -1.054774247047244540, -0.07405724077823318263, 1.323818897584032594 ) ) ;
#426=VERTEX_POINT ( 'NONE', #25002 ) ;
#429=EDGE_CURVE ( 'NONE', #8074, #10105, #18584, .T. ) ;
#434=CARTESIAN_POINT ( 'NONE',  ( 0.9412147342319837628, -0.1574803149606297803, 0.3567913385826772532 ) ) ;
#436=CARTESIAN_POINT ( 'NONE',  ( -0.7646288533564489232, -0.1113553986120547346, 1.048228346349165507 ) ) ;
#437=CARTESIAN_POINT ( 'NONE',  ( 0.7495606340400177148, -0.1264236179284866091, 0.4453740156942677664 ) ) ;
#439=DIRECTION ( 'NONE',  ( 0.000000000000000000, 0.000000000000000000, -1.000000000000000000 ) ) ;
#443=CARTESIAN_POINT ( 'NONE',  ( 0.8759842519685039353, 0.1574803149606299191, 0.9645669291338583307 ) ) ;
#444=CARTESIAN_POINT ( 'NONE',  ( 1.033464566929133799, 0.000000000000000000, 1.348425196850393748 ) ) ;
#445=LINE ( 'NONE', #14857, #29310 ) ;
#450=ORIENTED_EDGE ( 'NONE', *, *, #1798, .T. ) ;
#456=CARTESIAN_POINT ( 'NONE',  ( 0.7646288533564489232, -0.1113553986120547346, 0.9301181101286929431 ) ) ;
#460=VERTEX_POINT ( 'NONE', #6542 ) ;
#461=VERTEX_POINT ( 'NONE', #43426 ) ;
#462=CARTESIAN_POINT ( 'NONE',  ( -1.002407869896990045, -0.1264236179284866091, 1.557578740103716441 ) ) ;
#463=CARTESIAN_POINT ( 'NONE',  ( 1.054774247047244540, -0.07405724077823318263, 1.638779527505292988 ) ) ;
#464=CARTESIAN_POINT ( 'NONE',  ( -1.002407869896990045, -0.1264236179284866091, 0.8095472440407244230 ) ) ;
#466=CARTESIAN_POINT ( 'NONE',  ( 0.8759842519685039353, 0.1787899950787401882, 0.2731299212060791515 ) ) ;
#468=CARTESIAN_POINT ( 'NONE',  ( -0.7495606340400177148, 0.1264236179284866091, 1.296751968450173154 ) ) ;
#469=DIRECTION ( 'NONE',  ( 1.822029033848725028E-16, 0.000000000000000000, 1.000000000000000000 ) ) ;
#471=CARTESIAN_POINT ( 'NONE',  ( -0.7495606340400177148, -0.1264236179284866091, 1.626476377898992132 ) ) ;
#472=CARTESIAN_POINT ( 'NONE',  ( -0.9873396505805591694, -0.1113553986120547346, 1.884842519577511810 ) ) ;
#473=ORIENTED_EDGE ( 'NONE', *, *, #10794, .F. ) ;
#474=CARTESIAN_POINT ( 'NONE',  ( -1.033464566929133799, 0.000000000000000000, 1.663385826771653697 ) ) ;
#477=CARTESIAN_POINT ( 'NONE',  ( 0.7495606340400177148, -0.1264236179284866091, 1.468996062938362046 ) ) ;
#479=CARTESIAN_POINT ( 'NONE',  ( 1.033464566929133799, 1.928577636452524610E-17, 4.498031496062992574 ) ) ;
#480=VERTEX_POINT ( 'NONE', #32205 ) ;
#482=EDGE_LOOP ( 'NONE', ( #14896, #4355, #6135, #13847 ) ) ;
#487=CARTESIAN_POINT ( 'NONE',  ( 0.6971942568897648851, 0.07405724077823318263, 1.732283464513166615 ) ) ;
#491=CARTESIAN_POINT ( 'NONE',  ( -0.9873396505805591694, -0.1113553986120547346, 0.9005905510735748853 ) ) ;
#492=CARTESIAN_POINT ( 'NONE',  ( 0.6971942568897626646, -0.07405724077823297447, 0.7923228345919055560 ) ) ;
#494=LINE ( 'NONE', #33851, #14264 ) ;
#497=CARTESIAN_POINT ( 'NONE',  ( 1.054774247047244540, -0.07405724077823318263, 1.874999999946236784 ) ) ;
#499=CARTESIAN_POINT ( 'NONE',  ( 1.033464566929134687, 0.06523048226347956391, 0.05167322834645668439 ) ) ;
#505=( BOUNDED_CURVE ( )  B_SPLINE_CURVE ( 2, ( #37995, #45404, #8993, #34647, #17355, #14004, #10901, #46347, #35584 ),
 .UNSPECIFIED., .F., .F. ) 
 B_SPLINE_CURVE_WITH_KNOTS ( ( 3, 2, 2, 2, 3 ),
 ( 0.5899999999999999689, 0.5925000000000000266, 0.5949999999999999734, 0.5975000000000000311, 0.5999999999999999778 ),
 .UNSPECIFIED. ) 
 CURVE ( )  GEOMETRIC_REPRESENTATION_ITEM ( )  RATIONAL_B_SPLINE_CURVE ( ( 1.000000000000000000, 0.9238795325112869605, 1.000000000000000000, 0.9238795325112869605, 1.000000000000000000, 0.9238795325112869605, 1.000000000000000000, 0.9238795325112869605, 1.000000000000000000 ) ) 
 REPRESENTATION_ITEM ( '' )  ) ;
#506=CARTESIAN_POINT ( 'NONE',  ( 0.6971942568897626646, 0.07405724077823318263, 0.2017716534895435399 ) ) ;
#508=CARTESIAN_POINT ( 'NONE',  ( -0.6971942568897637749, 2.189545951927499583E-17, 1.577263779473795369 ) ) ;
#510=( BOUNDED_CURVE ( )  B_SPLINE_CURVE ( 2, ( #44895, #41286, #45377, #26733, #8969, #4890, #8486, #9205, #45132 ),
 .UNSPECIFIED., .F., .T. ) 
 B_SPLINE_CURVE_WITH_KNOTS ( ( 3, 2, 2, 2, 3 ),
 ( 0.6099999999999999867, 0.6125000000000000444, 0.6149999999999999911, 0.6175000000000000488, 0.6199999999999999956 ),
 .UNSPECIFIED. ) 
 CURVE ( )  GEOMETRIC_REPRESENTATION_ITEM ( )  RATIONAL_B_SPLINE_CURVE ( ( 1.000000000000000000, 0.9238795325112869605, 1.000000000000000000, 0.9238795325112869605, 1.000000000000000000, 0.9238795325112869605, 1.000000000000000000, 0.9238795325112869605, 1.000000000000000000 ) ) 
 REPRESENTATION_ITEM ( '' )  ) ;
#511=CARTESIAN_POINT ( 'NONE',  ( -0.9500414927467378812, 0.1787899950787401604, 1.176181102308441417 ) ) ;
#513=CARTESIAN_POINT ( 'NONE',  ( 0.6971942568897648851, 0.07405724077823318263, 1.304133858213953667 ) ) ;
#514=CARTESIAN_POINT ( 'NONE',  ( 0.8759842519685039353, -0.1787899950787401882, 1.980807086560409491 ) ) ;
#515=CARTESIAN_POINT ( 'NONE',  ( -0.6971942568897648851, 0.07405724077823318263, 1.102362204670646495 ) ) ;
#516=ADVANCED_FACE ( 'NONE', ( #27279 ), #1832, .T. ) ;
#519=CARTESIAN_POINT ( 'NONE',  ( 1.054774247047244540, -0.07405724077823318263, 0.4183070865604096578 ) ) ;
#520=CARTESIAN_POINT ( 'NONE',  ( -0.7495606340400177148, 0.1264236179284866091, 0.1550196849856066983 ) ) ;
#521=CARTESIAN_POINT ( 'NONE',  ( -0.9500414927467378812, -0.1787899950787401604, 0.7234251967966300878 ) ) ;
#525=ORIENTED_EDGE ( 'NONE', *, *, #11840, .F. ) ;
#526=CARTESIAN_POINT ( 'NONE',  ( -0.9412147342319837628, -0.1574803149606297803, 0.1205708661417322497 ) ) ;
#527=ADVANCED_FACE ( 'NONE', ( #9030 ), #27517, .T. ) ;
#530=CARTESIAN_POINT ( 'NONE',  ( 0.8759842519685039353, 0.1787899950787401882, 1.921751968450173376 ) ) ;
#531=CARTESIAN_POINT ( 'NONE',  ( -1.002407869896990045, -0.1264236179284866091, 0.05659448813521283234 ) ) ;
#536=ORIENTED_EDGE ( 'NONE', *, *, #44389, .T. ) ;
#537=CARTESIAN_POINT ( 'NONE',  ( 0.8759842519685039353, -0.1787899950787401882, 1.232775590497417362 ) ) ;
#540=CARTESIAN_POINT ( 'NONE',  ( -0.9873396505805591694, 0.1113553986120547346, 1.432086614173228245 ) ) ;
#541=CARTESIAN_POINT ( 'NONE',  ( 1.002407869896990045, 0.1264236179284866091, 0.2239173227808822775 ) ) ;
#546=ORIENTED_EDGE ( 'NONE', *, *, #8764, .F. ) ;
#547=CARTESIAN_POINT ( 'NONE',  ( -0.6971942568897648851, 0.07405724077823318263, 0.7135826771115916234 ) ) ;
#550=CARTESIAN_POINT ( 'NONE',  ( 1.054774247047244540, -0.07405724077823318263, 1.323818897584032817 ) ) ;
#551=CARTESIAN_POINT ( 'NONE',  ( 1.054774247047244540, -0.07405724077823318263, 1.633858267662771091 ) ) ;
#552=CARTESIAN_POINT ( 'NONE',  ( 0.8759842519685039353, -0.1787899950787401882, 0.2485236219934806867 ) ) ;
#553=DIRECTION ( 'NONE',  ( 1.000000000000000000, 0.000000000000000000, -1.822029033848725275E-16 ) ) ;
#559=CARTESIAN_POINT ( 'NONE',  ( 0.6971942568897637749, 2.189545951927499583E-17, 0.2780511810485988278 ) ) ;
#560=CARTESIAN_POINT ( 'NONE',  ( -0.9412147342319837628, 0.1574803149606300301, 1.710137795275591843 ) ) ;
#564=CARTESIAN_POINT ( 'NONE',  ( -0.8019270111902717657, 0.1787899950787401604, 1.215551181048599272 ) ) ;
#565=CARTESIAN_POINT ( 'NONE',  ( 0.8107537697050253289, -0.1574803149606297803, 0.6963582676090082080 ) ) ;
#566=ORIENTED_EDGE ( 'NONE', *, *, #42957, .T. ) ;
#567=CARTESIAN_POINT ( 'NONE',  ( 0.7185039370078746268, 0.06523048226347956391, 1.405019685039369914 ) ) ;
#571=CARTESIAN_POINT ( 'NONE',  ( -0.7185039370078746268, -0.06523048226347956391, 0.2977362203649139283 ) ) ;
#574=CARTESIAN_POINT ( 'NONE',  ( 0.8759842519685039353, -0.1787899950787401882, 1.626476377898992132 ) ) ;
#575=EDGE_CURVE ( 'NONE', #3281, #35903, #38693, .T. ) ;
#577=CARTESIAN_POINT ( 'NONE',  ( -1.033464566929134687, 0.06523048226347956391, 0.9178149606299221830 ) ) ;
#578=CARTESIAN_POINT ( 'NONE',  ( 0.7646288533564489232, -0.1113553986120547346, 1.914370078632629868 ) ) ;
#587=CARTESIAN_POINT ( 'NONE',  ( -0.7495606340400177148, -0.1264236179284866091, 1.464074803095842370 ) ) ;
#589=CARTESIAN_POINT ( 'NONE',  ( -0.7495606340400177148, -0.1264236179284866091, 1.311515747977732405 ) ) ;
#590=ADVANCED_FACE ( 'NONE', ( #4944 ), #41819, .T. ) ;
#591=CARTESIAN_POINT ( 'NONE',  ( -0.8019270111902717657, -0.1787899950787401604, 0.3690944881352128393 ) ) ;
#595=ORIENTED_EDGE ( 'NONE', *, *, #3073, .T. ) ;
#597=EDGE_LOOP ( 'NONE', ( #36228, #9549, #2235, #27768 ) ) ;
#598=CARTESIAN_POINT ( 'NONE',  ( 0.6971942568897648851, -0.07405724077823297447, 1.028543307032851795 ) ) ;
#599=CARTESIAN_POINT ( 'NONE',  ( 0.7185039370078739607, 1.928577636452523993E-17, 1.200787401467275695 ) ) ;
#600=CARTESIAN_POINT ( 'NONE',  ( -0.8759842519685039353, -0.1574803149606299191, 0.5807086613097960370 ) ) ;
#601=VECTOR ( 'NONE', #24176, 39.37007874015748143 ) ;
#602=AXIS2_PLACEMENT_3D ( 'NONE', #9099, #23721, #38801 ) ;
#603=CARTESIAN_POINT ( 'NONE',  ( -0.7646288533564489232, 0.1113553986120547346, 0.8907480314960629642 ) ) ;
#604=CYLINDRICAL_SURFACE ( 'NONE', #44721, 0.1574803149606299191 ) ;
#607=CARTESIAN_POINT ( 'NONE',  ( -0.7185039370078746268, -0.06523048226347956391, 1.518208661309795149 ) ) ;
#608=CARTESIAN_POINT ( 'NONE',  ( 1.054774247047244540, 0.07405724077823318263, 0.9350393700249758355 ) ) ;
#609=CARTESIAN_POINT ( 'NONE',  ( 0.7495606340400177148, 0.1264236179284866091, 1.375492125930488196 ) ) ;
#610=CARTESIAN_POINT ( 'NONE',  ( -0.9412147342319837628, 0.1574803149606300301, 0.4502952755905510474 ) ) ;
#611=CARTESIAN_POINT ( 'NONE',  ( 0.8759842519685039353, -0.1574803149606299191, 1.456692913385826849 ) ) ;
#613=( BOUNDED_CURVE ( )  B_SPLINE_CURVE ( 2, ( #7881, #44290, #26361, #32849, #7413, #29979, #15326, #47443, #39990 ),
 .UNSPECIFIED., .F., .T. ) 
 B_SPLINE_CURVE_WITH_KNOTS ( ( 3, 2, 2, 2, 3 ),
 ( 0.4099999999999999756, 0.4124999999999999778, 0.4149999999999999800, 0.4174999999999999822, 0.4199999999999999845 ),
 .UNSPECIFIED. ) 
 CURVE ( )  GEOMETRIC_REPRESENTATION_ITEM ( )  RATIONAL_B_SPLINE_CURVE ( ( 1.000000000000000000, 0.9238795325112879597, 1.000000000000000000, 0.9238795325112869605, 1.000000000000000000, 0.9238795325112869605, 1.000000000000000000, 0.9238795325112869605, 1.000000000000000000 ) ) 
 REPRESENTATION_ITEM ( '' )  ) ;
#614=CARTESIAN_POINT ( 'NONE',  ( 0.8019270111902716547, 0.1787899950787401604, 0.8218503936470251681 ) ) ;
#617=CARTESIAN_POINT ( 'NONE',  ( 0.7646288533564489232, -0.1113553986120547346, 0.4183070865066456645 ) ) ;
#619=CARTESIAN_POINT ( 'NONE',  ( 0.7495606340400177148, -0.1264236179284866091, 1.070374015694267600 ) ) ;
#625=ORIENTED_EDGE ( 'NONE', *, *, #36161, .F. ) ;
#627=CARTESIAN_POINT ( 'NONE',  ( -0.6971942568897637749, 2.189545951927499583E-17, 0.2386811023084413619 ) ) ;
#628=ORIENTED_EDGE ( 'NONE', *, *, #34521, .T. ) ;
#630=CARTESIAN_POINT ( 'NONE',  ( -0.9500414927467378812, 0.1787899950787401604, 1.643700787347811998 ) ) ;
#631=CARTESIAN_POINT ( 'NONE',  ( -1.054774247047244540, -0.07405724077823318263, 0.8858267715997791836 ) ) ;
#633=CARTESIAN_POINT ( 'NONE',  ( -1.054774247047244096, 0.000000000000000000, 1.124507873961984261 ) ) ;
#635=CARTESIAN_POINT ( 'NONE',  ( -0.6971942568897637749, 2.189545951927499583E-17, 0.4798228345919055560 ) ) ;
#636=( BOUNDED_CURVE ( )  B_SPLINE_CURVE ( 2, ( #787, #43949, #8233, #4159, #30330, #26237, #30102, #40335, #15451 ),
 .UNSPECIFIED., .F., .T. ) 
 B_SPLINE_CURVE_WITH_KNOTS ( ( 3, 2, 2, 2, 3 ),
 ( 0.8100000000000000533, 0.8125000000000000000, 0.8149999999999999467, 0.8175000000000000044, 0.8199999999999999512 ),
 .UNSPECIFIED. ) 
 CURVE ( )  GEOMETRIC_REPRESENTATION_ITEM ( )  RATIONAL_B_SPLINE_CURVE ( ( 1.000000000000000000, 0.9238795325112899581, 1.000000000000000000, 0.9238795325112869605, 1.000000000000000000, 0.9238795325112869605, 1.000000000000000000, 0.9238795325112829637, 1.000000000000000000 ) ) 
 REPRESENTATION_ITEM ( '' )  ) ;
#638=CARTESIAN_POINT ( 'NONE',  ( -0.6971942568897648851, -0.07405724077823297447, 1.978346456639149320 ) ) ;
#639=CARTESIAN_POINT ( 'NONE',  ( 0.8759842519685039353, 0.000000000000000000, 4.498031496062992574 ) ) ;
#640=CARTESIAN_POINT ( 'NONE',  ( 1.054774247047244540, 0.07405724077823318263, 0.06397637789899228433 ) ) ;
#644=CARTESIAN_POINT ( 'NONE',  ( -1.033464566929133799, 0.000000000000000000, 1.781496062992125928 ) ) ;
#646=CARTESIAN_POINT ( 'NONE',  ( -0.6971942568897626646, 0.07405724077823318263, 0.3149606298674962890 ) ) ;
#650=CARTESIAN_POINT ( 'NONE',  ( -0.8759842519685039353, 0.1787899950787401882, 1.375492125930488196 ) ) ;
#655=AXIS2_PLACEMENT_3D ( 'NONE', #20910, #35078, #2226 ) ;
#658=CARTESIAN_POINT ( 'NONE',  ( 1.033464566929133799, 0.000000000000000000, 0.4330708660342047489 ) ) ;
#659=CARTESIAN_POINT ( 'NONE',  ( -0.7646288533564489232, 0.1113553986120547346, 1.038385826664126155 ) ) ;
#661=CARTESIAN_POINT ( 'NONE',  ( 1.054774247047244540, 0.07405724077823318263, 0.6200787401037165525 ) ) ;
#662=CARTESIAN_POINT ( 'NONE',  ( -0.8107537697050254399, -0.1574803149606297803, 1.483759842412158747 ) ) ;
#667=CARTESIAN_POINT ( 'NONE',  ( -0.6971942568897637749, 2.189545951927499583E-17, 0.9522637794737952577 ) ) ;
#668=CARTESIAN_POINT ( 'NONE',  ( 0.7185039370078746268, 0.06523048226347956391, 0.9325787401574799906 ) ) ;
#669=VECTOR ( 'NONE', #5870, 39.37007874015748143 ) ;
#673=ORIENTED_EDGE ( 'NONE', *, *, #33785, .F. ) ;
#677=CARTESIAN_POINT ( 'NONE',  ( 1.002407869896990045, 0.1264236179284866091, 0.6963582676627716461 ) ) ;
#680=CARTESIAN_POINT ( 'NONE',  ( 1.033464566929136907, -0.06523048226347749612, 1.385334645669292541 ) ) ;
#684=CARTESIAN_POINT ( 'NONE',  ( 0.8759842519685039353, -0.1574803149606299191, 1.131889763672000004 ) ) ;
#687=CARTESIAN_POINT ( 'NONE',  ( -0.9500414927467378812, -0.1787899950787401604, 0.4872047243556847929 ) ) ;
#689=ORIENTED_EDGE ( 'NONE', *, *, #1840, .T. ) ;
#690=CARTESIAN_POINT ( 'NONE',  ( -0.8019270111902717657, -0.1787899950787401604, 1.825787401521040243 ) ) ;
#691=CARTESIAN_POINT ( 'NONE',  ( 0.9500414927467378812, -0.1787899950787401604, 1.673228346402929834 ) ) ;
#692=CARTESIAN_POINT ( 'NONE',  ( 0.8759842519685039353, 0.000000000000000000, 4.498031496062992574 ) ) ;
#693=CARTESIAN_POINT ( 'NONE',  ( 0.8019270111902717657, 0.1787899950787401604, 0.2362204723871814960 ) ) ;
#694=CARTESIAN_POINT ( 'NONE',  ( -1.054774247047244540, -0.07405724077823318263, 1.200787401521039355 ) ) ;
#695=CARTESIAN_POINT ( 'NONE',  ( -0.9500414927467378812, -0.1787899950787401604, 0.05905511805647267048 ) ) ;
#698=CARTESIAN_POINT ( 'NONE',  ( -1.054774247047244540, 0.07405724077823318263, 1.604330708607653921 ) ) ;
#699=CARTESIAN_POINT ( 'NONE',  ( -0.9412147342319837628, -0.1574803149606297803, 1.843011810916095561 ) ) ;
#701=CARTESIAN_POINT ( 'NONE',  ( -0.7646288533564489232, -0.1113553986120547346, 1.609251968503937036 ) ) ;
#703=CARTESIAN_POINT ( 'NONE',  ( 0.6971942568897648851, 0.07405724077823318263, 1.579724409395055318 ) ) ;
#706=CARTESIAN_POINT ( 'NONE',  ( 1.033464566929134687, 0.06523048226347956391, 0.2780511809948353341 ) ) ;
#707=EDGE_LOOP ( 'NONE', ( #31570, #13137, #36634, #7165 ) ) ;
#717=CARTESIAN_POINT ( 'NONE',  ( 0.8759842519685039353, 0.1787899950787401882, 1.803641732229700700 ) ) ;
#721=CARTESIAN_POINT ( 'NONE',  ( -1.033464566929133799, 0.000000000000000000, 1.062992125876724314 ) ) ;
#722=CARTESIAN_POINT ( 'NONE',  ( 0.6971942568897637749, 2.189545951927499583E-17, 0.7898622046706456068 ) ) ;
#726=CARTESIAN_POINT ( 'NONE',  ( 1.033464566929133799, 1.928577636452524610E-17, 4.498031496062992574 ) ) ;
#727=CARTESIAN_POINT ( 'NONE',  ( 0.6971942568897648851, 0.07405724077823318263, 1.815944881835999558 ) ) ;
#728=CARTESIAN_POINT ( 'NONE',  ( 0.8759842519685039353, -0.1574803149606299191, 1.879921259734992134 ) ) ;
#731=CARTESIAN_POINT ( 'NONE',  ( 0.8759842519685039353, -0.1574803149606299191, 0.1181102362204724532 ) ) ;
#736=CARTESIAN_POINT ( 'NONE',  ( 1.002407869896990045, -0.1264236179284866091, 0.1796259841982051075 ) ) ;
#739=CARTESIAN_POINT ( 'NONE',  ( -0.8759842519685039353, 0.1787899950787401882, 1.724901574749385880 ) ) ;
#740=VERTEX_POINT ( 'NONE', #18615 ) ;
#741=CARTESIAN_POINT ( 'NONE',  ( -0.9500414927467378812, 0.1787899950787401604, 1.333661417269071059 ) ) ;
#743=CARTESIAN_POINT ( 'NONE',  ( 1.054774247047244540, -0.07405724077823318263, 1.284448818843874740 ) ) ;
#745=CARTESIAN_POINT ( 'NONE',  ( -0.6971942568897648851, 0.07405724077823318263, 1.023622047190330342 ) ) ;
#748=CARTESIAN_POINT ( 'NONE',  ( 0.6971942568897637749, 2.189545951927499583E-17, 0.4010826771115905687 ) ) ;
#749=CARTESIAN_POINT ( 'NONE',  ( -0.9500414927467377701, -0.1787899950787401604, 0.3690944881352128393 ) ) ;
#750=CARTESIAN_POINT ( 'NONE',  ( -1.054774247047244540, -0.07405724077823318263, 0.8464566928596233275 ) ) ;
#756=CARTESIAN_POINT ( 'NONE',  ( -0.7646288533564489232, 0.1113553986120547346, 0.1033464566929133965 ) ) ;
#758=VERTEX_POINT ( 'NONE', #19081 ) ;
#759=CARTESIAN_POINT ( 'NONE',  ( -0.9500414927467378812, -0.1787899950787401604, 0.8858267715997791836 ) ) ;
#761=CARTESIAN_POINT ( 'NONE',  ( 1.033464566929133799, 0.000000000000000000, 0.3248031496062992463 ) ) ;
#768=CARTESIAN_POINT ( 'NONE',  ( 0.8019270111902717657, -0.1787899950787401604, 1.269685039316314601 ) ) ;
#769=AXIS2_PLACEMENT_3D ( 'NONE', #1035, #36541, #36769 ) ;
#770=CARTESIAN_POINT ( 'NONE',  ( 1.033464566929134687, 0.06523048226347956391, 1.587106299212598604 ) ) ;
#773=CARTESIAN_POINT ( 'NONE',  ( 0.6971942568897626646, -0.07405724077823297447, 0.1230314960092287191 ) ) ;
#777=EDGE_CURVE ( 'NONE', #24545, #4083, #7595, .T. ) ;
#779=CARTESIAN_POINT ( 'NONE',  ( -1.054774247047244096, 0.000000000000000000, 0.6176181101824566033 ) ) ;
#780=CARTESIAN_POINT ( 'NONE',  ( 0.7185039370078746268, -0.06523048226347956391, 0.2977362203649139283 ) ) ;
#784=CARTESIAN_POINT ( 'NONE',  ( 0.6971942568897648851, 0.07405724077823318263, 1.422244094434426120 ) ) ;
#785=CARTESIAN_POINT ( 'NONE',  ( 0.9500414927467377701, 0.1787899950787401604, 1.761811023568284229 ) ) ;
#787=CARTESIAN_POINT ( 'NONE',  ( -0.7185039370078739607, 1.928577636452523993E-17, 1.633858267609007875 ) ) ;
#788=CARTESIAN_POINT ( 'NONE',  ( -0.8107537697050254399, 0.1574803149606300301, 1.518208661417322913 ) ) ;
#792=CARTESIAN_POINT ( 'NONE',  ( -1.033464566929133799, 0.000000000000000000, 1.220472440837354400 ) ) ;
#793=CARTESIAN_POINT ( 'NONE',  ( 0.7495606340400177148, 0.1264236179284866091, 0.3518700786863940833 ) ) ;
#794=CARTESIAN_POINT ( 'NONE',  ( -0.8107537697050254399, -0.1574803149606297803, 1.719980314853102321 ) ) ;
#796=CARTESIAN_POINT ( 'NONE',  ( -0.8107537697050254399, 0.1574803149606300301, 0.7701771653543307838 ) ) ;
#797=CARTESIAN_POINT ( 'NONE',  ( -0.8019270111902717657, 0.1787899950787401604, 1.373031496009229135 ) ) ;
#798=CARTESIAN_POINT ( 'NONE',  ( 1.033464566929134687, 0.06523048226347956391, 0.7111220471365681250 ) ) ;
#800=CARTESIAN_POINT ( 'NONE',  ( -0.7646288533564489232, 0.1113553986120547346, 1.756889763779527547 ) ) ;
#806=CARTESIAN_POINT ( 'NONE',  ( -1.033464566929134687, 0.06523048226347956391, 1.104822834538142340 ) ) ;
#807=CARTESIAN_POINT ( 'NONE',  ( 0.8019270111902717657, 0.1787899950787401604, 1.530511810969859443 ) ) ;
#810=CARTESIAN_POINT ( 'NONE',  ( 0.9873396505805591694, 0.1113553986120547346, 1.904527559055118280 ) ) ;
#811=CARTESIAN_POINT ( 'NONE',  ( -1.033464566929134687, -0.06523048226347956391, 0.5093503935932608417 ) ) ;
#813=AXIS2_PLACEMENT_3D ( 'NONE', #15403, #44359, #29363 ) ;
#814=CARTESIAN_POINT ( 'NONE',  ( 0.8759842519685039353, 0.1574803149606299191, 1.309055118002708573 ) ) ;
#815=VERTEX_POINT ( 'NONE', #4446 ) ;
#818=CARTESIAN_POINT ( 'NONE',  ( 0.9500414927467377701, -0.1787899950787401604, 0.9251968503399373711 ) ) ;
#819=CARTESIAN_POINT ( 'NONE',  ( -0.8759842519685039353, 0.1787899950787401882, 1.528051181048598384 ) ) ;
#821=CARTESIAN_POINT ( 'NONE',  ( -0.8759842519685039353, -0.1787899950787401882, 1.237696850339937038 ) ) ;
#823=CARTESIAN_POINT ( 'NONE',  ( -1.054774247047244540, 0.07405724077823318263, 0.3444881889226146243 ) ) ;
#824=CARTESIAN_POINT ( 'NONE',  ( 1.033464566929133799, 1.928577636452524610E-17, 4.498031496062992574 ) ) ;
#825=DIRECTION ( 'NONE',  ( 1.822029033848725028E-16, 0.000000000000000000, 1.000000000000000000 ) ) ;
#831=DIRECTION ( 'NONE',  ( 1.000000000000000000, 0.000000000000000000, -1.822029033848725275E-16 ) ) ;
#833=CARTESIAN_POINT ( 'NONE',  ( 0.7185039370078714072, 0.06523048226347728795, 1.828248031388537198 ) ) ;
#837=EDGE_CURVE ( 'NONE', #23661, #38468, #18158, .T. ) ;
#840=CARTESIAN_POINT ( 'NONE',  ( -0.7495606340400177148, 0.1264236179284866091, 0.1993110235682838682 ) ) ;
#841=CARTESIAN_POINT ( 'NONE',  ( -1.033464566929134687, 0.06523048226347956391, 0.9571850393700783721 ) ) ;
#845=CARTESIAN_POINT ( 'NONE',  ( -1.033464566929134687, 0.06523048226347956391, 1.459153543199560144 ) ) ;
#846=CARTESIAN_POINT ( 'NONE',  ( 0.9500414927467378812, -0.1787899950787401604, 0.8858267715997791836 ) ) ;
#849=CARTESIAN_POINT ( 'NONE',  ( 0.7185039370078737386, 0.06523048226348011902, 0.5290354329633389918 ) ) ;
#850=CARTESIAN_POINT ( 'NONE',  ( 1.033464566929134687, 0.06523048226347956391, 1.350885826771654363 ) ) ;
#851=CARTESIAN_POINT ( 'NONE',  ( 0.7154772363482215791, 0.03734124201450598340, 1.982562885371508488 ) ) ;
#852=DIRECTION ( 'NONE',  ( 1.822029033848725028E-16, 0.000000000000000000, 1.000000000000000000 ) ) ;
#853=CYLINDRICAL_SURFACE ( 'NONE', #4451, 0.1574803149606299191 ) ;
#855=CARTESIAN_POINT ( 'NONE',  ( 0.8019270111902716547, -0.1787899950787401604, 0.8366141731745828647 ) ) ;
#857=CARTESIAN_POINT ( 'NONE',  ( 1.054774247047244540, -0.07405724077823318263, 1.756889763725764553 ) ) ;
#861=CARTESIAN_POINT ( 'NONE',  ( 1.033464566929134687, 0.06523048226347956391, 1.075295275590550048 ) ) ;
#863=CARTESIAN_POINT ( 'NONE',  ( -0.7185039370078746268, -0.06523048226347956391, 0.1008858266641264878 ) ) ;
#864=CARTESIAN_POINT ( 'NONE',  ( 0.8019270111902717657, -0.1787899950787401604, 1.112204724355684959 ) ) ;
#869=EDGE_LOOP ( 'NONE', ( #32440, #31673, #26613, #9439 ) ) ;
#871=CARTESIAN_POINT ( 'NONE',  ( -0.8759842519685039353, -0.1787899950787401882, 0.2485236219934806867 ) ) ;
#872=CARTESIAN_POINT ( 'NONE',  ( -0.7185039370078739607, 1.928577636452523993E-17, 0.6200787401574803237 ) ) ;
#877=CARTESIAN_POINT ( 'NONE',  ( -0.6971942568897637749, 2.189545951927499583E-17, 0.9473425196312755814 ) ) ;
#878=CARTESIAN_POINT ( 'NONE',  ( -0.7495606340400177148, -0.1264236179284866091, 0.4847440944344252323 ) ) ;
#879=DIRECTION ( 'NONE',  ( 1.822029033848725028E-16, 0.000000000000000000, 1.000000000000000000 ) ) ;
#885=CARTESIAN_POINT ( 'NONE',  ( 0.8759842519685039353, 0.000000000000000000, 4.498031496062992574 ) ) ;
#886=CYLINDRICAL_SURFACE ( 'NONE', #39424, 0.1574803149606299191 ) ;
#888=CARTESIAN_POINT ( 'NONE',  ( -0.6971942568897626646, -0.07405724077823297447, 0.3198818897100162983 ) ) ;
#893=CARTESIAN_POINT ( 'NONE',  ( -0.6971942568897637749, 2.189545951927499583E-17, 1.464074803095842370 ) ) ;
#898=( BOUNDED_CURVE ( )  B_SPLINE_CURVE ( 2, ( #25785, #18803, #810, #11640, #18103, #40125, #10697, #22157, #37254 ),
 .UNSPECIFIED., .F., .T. ) 
 B_SPLINE_CURVE_WITH_KNOTS ( ( 3, 2, 2, 2, 3 ),
 ( 0.9599999999999999645, 0.9625000000000000222, 0.9649999999999999689, 0.9675000000000000266, 0.9699999999999999734 ),
 .UNSPECIFIED. ) 
 CURVE ( )  GEOMETRIC_REPRESENTATION_ITEM ( )  RATIONAL_B_SPLINE_CURVE ( ( 1.000000000000000000, 0.9238795325112869605, 1.000000000000000000, 0.9238795325112869605, 1.000000000000000000, 0.9238795325112869605, 1.000000000000000000, 0.9238795325112869605, 1.000000000000000000 ) ) 
 REPRESENTATION_ITEM ( '' )  ) ;
#901=CARTESIAN_POINT ( 'NONE',  ( 1.033464566929133799, 0.000000000000000000, 0.2066929133858267931 ) ) ;
#903=DIRECTION ( 'NONE',  ( 1.822029033848725028E-16, 0.000000000000000000, 1.000000000000000000 ) ) ;
#904=CARTESIAN_POINT ( 'NONE',  ( -0.9873396505805591694, 0.1113553986120547346, 1.107283464459401623 ) ) ;
#905=CARTESIAN_POINT ( 'NONE',  ( 0.7495606340400177148, 0.1264236179284866091, 0.5142716534895434011 ) ) ;
#908=VECTOR ( 'NONE', #12308, 39.37007874015748143 ) ;
#909=CARTESIAN_POINT ( 'NONE',  ( 0.7646288533564489232, -0.1113553986120547346, 1.953740157372787500 ) ) ;
#911=EDGE_CURVE ( 'NONE', #13663, #9851, #36610, .T. ) ;
#912=CARTESIAN_POINT ( 'NONE',  ( 0.7185039370078739607, 1.928577636452523993E-17, 0.9744094488188976833 ) ) ;
#913=CARTESIAN_POINT ( 'NONE',  ( -0.8759842519685039353, -0.1787899950787401882, 1.040846456639149764 ) ) ;
#914=CARTESIAN_POINT ( 'NONE',  ( 0.9873396505805591694, 0.1113553986120547346, 0.9596456692913386544 ) ) ;
#929=CARTESIAN_POINT ( 'NONE',  ( 1.033464566929134687, -0.06523048226347956391, 1.099901574695622886 ) ) ;
#930=( BOUNDED_CURVE ( )  B_SPLINE_CURVE ( 2, ( #28913, #10684, #25292, #39880, #29164, #18090, #14741, #32736, #25546 ),
 .UNSPECIFIED., .F., .T. ) 
 B_SPLINE_CURVE_WITH_KNOTS ( ( 3, 2, 2, 2, 3 ),
 ( 0.6099999999999999867, 0.6125000000000000444, 0.6149999999999999911, 0.6175000000000000488, 0.6199999999999999956 ),
 .UNSPECIFIED. ) 
 CURVE ( )  GEOMETRIC_REPRESENTATION_ITEM ( )  RATIONAL_B_SPLINE_CURVE ( ( 1.000000000000000000, 0.9238795325112869605, 1.000000000000000000, 0.9238795325112869605, 1.000000000000000000, 0.9238795325112869605, 1.000000000000000000, 0.9238795325112869605, 1.000000000000000000 ) ) 
 REPRESENTATION_ITEM ( '' )  ) ;
#933=CARTESIAN_POINT ( 'NONE',  ( -0.6971942568897648851, 0.07405724077823318263, 1.815944881835999558 ) ) ;
#934=CARTESIAN_POINT ( 'NONE',  ( 0.8759842519685039353, -0.1787899950787401882, 1.710137795221826851 ) ) ;
#935=CARTESIAN_POINT ( 'NONE',  ( -0.7495606340400177148, -0.1264236179284866091, 0.9178149605761574126 ) ) ;
#937=CARTESIAN_POINT ( 'NONE',  ( 0.7495606340400177148, 0.1264236179284866091, 0.2780511810485988278 ) ) ;
#938=CARTESIAN_POINT ( 'NONE',  ( -1.054774247047244540, -0.07405724077823318263, 1.437007873961985371 ) ) ;
#940=CARTESIAN_POINT ( 'NONE',  ( -0.8759842519685039353, -0.1787899950787401882, 1.311515747977732405 ) ) ;
#941=CARTESIAN_POINT ( 'NONE',  ( -0.7495606340400177148, 0.1264236179284866091, 0.7849409448281259305 ) ) ;
#942=CARTESIAN_POINT ( 'NONE',  ( -0.8019270111902717657, -0.1787899950787401604, 0.1328740156942679607 ) ) ;
#944=CARTESIAN_POINT ( 'NONE',  ( -0.6971942568897648851, -0.07405724077823297447, 1.624015747977732849 ) ) ;
#945=CARTESIAN_POINT ( 'NONE',  ( -1.054774247047244540, 0.07405724077823318263, 0.06889763774151215492 ) ) ;
#946=CARTESIAN_POINT ( 'NONE',  ( -1.033464566929134687, -0.06523048226347956391, 1.582185039370078927 ) ) ;
#947=CARTESIAN_POINT ( 'NONE',  ( 1.033464566929133799, 0.000000000000000000, 0.7185039370078739607 ) ) ;
#948=CARTESIAN_POINT ( 'NONE',  ( 0.8019270111902716547, 0.1787899950787401604, 1.574803149552536530 ) ) ;
#950=LINE ( 'NONE', #23504, #21058 ) ;
#952=ORIENTED_EDGE ( 'NONE', *, *, #13535, .F. ) ;
#955=VERTEX_POINT ( 'NONE', #12405 ) ;
#956=CARTESIAN_POINT ( 'NONE',  ( -1.054774247047244096, 0.000000000000000000, 1.168799212544661348 ) ) ;
#962=CARTESIAN_POINT ( 'NONE',  ( 0.7646288533564489232, -0.1113553986120547346, 0.3100393700787401619 ) ) ;
#966=EDGE_CURVE ( 'NONE', #3817, #13566, #5414, .T. ) ;
#967=CARTESIAN_POINT ( 'NONE',  ( 0.8019270111902717657, 0.1787899950787401604, 0.7824803149068669805 ) ) ;
#969=CARTESIAN_POINT ( 'NONE',  ( 1.033464566929134687, -0.06523048226347956391, 1.139271653435781184 ) ) ;
#972=CARTESIAN_POINT ( 'NONE',  ( 0.6971942568897637749, 2.189545951927499583E-17, 1.818405511757259729 ) ) ;
#975=CARTESIAN_POINT ( 'NONE',  ( 0.7646288533564489232, -0.1113553986120547346, 0.1525590551181102428 ) ) ;
#980=CARTESIAN_POINT ( 'NONE',  ( 0.6971942568897637749, 2.189545951927499583E-17, 0.2042322834108035723 ) ) ;
#981=DIRECTION ( 'NONE',  ( 1.000000000000000000, 0.000000000000000000, -1.822029033848725275E-16 ) ) ;
#982=CARTESIAN_POINT ( 'NONE',  ( -0.6971942568897648851, 0.07405724077823318263, 1.692913385773008539 ) ) ;
#984=CARTESIAN_POINT ( 'NONE',  ( -0.8019270111902717657, -0.1787899950787401604, 1.313976377898992132 ) ) ;
#985=CARTESIAN_POINT ( 'NONE',  ( -0.9412147342319837628, 0.1574803149606300301, 0.3321850393700786497 ) ) ;
#986=CARTESIAN_POINT ( 'NONE',  ( 1.002407869896990045, 0.1264236179284866091, 1.291830708607653477 ) ) ;
#988=CARTESIAN_POINT ( 'NONE',  ( -1.002407869896990045, -0.1264236179284866091, 0.5339566928596221063 ) ) ;
#989=CARTESIAN_POINT ( 'NONE',  ( 1.054774247047244540, -0.07405724077823318263, 1.909448818843873186 ) ) ;
#990=CARTESIAN_POINT ( 'NONE',  ( -1.002407869896990045, -0.1264236179284866091, 1.001476377898992132 ) ) ;
#993=CARTESIAN_POINT ( 'NONE',  ( 0.7646288533564489232, 0.1113553986120547346, 1.205708661417322913 ) ) ;
#994=CARTESIAN_POINT ( 'NONE',  ( 1.054774247047244096, 0.000000000000000000, 0.4995078739619842612 ) ) ;
#995=CARTESIAN_POINT ( 'NONE',  ( -1.054774247047244540, 0.07405724077823318263, 0.3395669290800949480 ) ) ;
#996=CARTESIAN_POINT ( 'NONE',  ( -0.9500414927467378812, -0.1787899950787401604, 0.8415354330171019859 ) ) ;
#1000=VERTEX_POINT ( 'NONE', #42057 ) ;
#1001=CARTESIAN_POINT ( 'NONE',  ( 0.8759842519685039353, -0.1787899950787401882, 0.9227362204186770889 ) ) ;
#1002=CARTESIAN_POINT ( 'NONE',  ( -0.9873396505805591694, -0.1113553986120547346, 0.1230314960629921295 ) ) ;
#1006=CARTESIAN_POINT ( 'NONE',  ( -0.9500414927467378812, 0.1787899950787401604, 0.9005905511273389896 ) ) ;
#1008=DIRECTION ( 'NONE',  ( 0.000000000000000000, 0.000000000000000000, -1.000000000000000000 ) ) ;
#1014=ORIENTED_EDGE ( 'NONE', *, *, #13181, .F. ) ;
#1015=CARTESIAN_POINT ( 'NONE',  ( -0.8107537697050254399, 0.1574803149606300301, 0.8390748030420788206 ) ) ;
#1017=EDGE_CURVE ( 'NONE', #32743, #28431, #42763, .T. ) ;
#1018=CARTESIAN_POINT ( 'NONE',  ( 1.054774247047244540, 0.07405724077823318263, 1.638779527505292988 ) ) ;
#1019=CARTESIAN_POINT ( 'NONE',  ( 0.9500414927467378812, 0.1787899950787401604, 0.2263779527021421711 ) ) ;
#1023=CARTESIAN_POINT ( 'NONE',  ( -0.7185039370078714072, 0.06523048226347728795, 1.749507873908221045 ) ) ;
#1026=EDGE_CURVE ( 'NONE', #14442, #15222, #38252, .T. ) ;
#1027=CARTESIAN_POINT ( 'NONE',  ( -1.002407869896990045, -0.1264236179284866091, 0.6520669290800944484 ) ) ;
#1032=CARTESIAN_POINT ( 'NONE',  ( 0.8759842519685039353, 0.1787899950787401882, 1.296751968450173154 ) ) ;
#1033=CARTESIAN_POINT ( 'NONE',  ( 0.6971942568897648851, -0.07405724077823297447, 1.894685039316315489 ) ) ;
#1034=CARTESIAN_POINT ( 'NONE',  ( 0.9500414927467377701, 0.1787899950787401604, 0.2657480314422993595 ) ) ;
#1035=CARTESIAN_POINT ( 'NONE',  ( -0.8759842519685039353, 0.000000000000000000, 0.000000000000000000 ) ) ;
#1040=CARTESIAN_POINT ( 'NONE',  ( -0.8107537697050254399, 0.1574803149606300301, 1.232775590443654812 ) ) ;
#1041=CARTESIAN_POINT ( 'NONE',  ( 0.8759842519685039353, -0.1787899950787401882, 0.3666338582139531677 ) ) ;
#1043=CARTESIAN_POINT ( 'NONE',  ( -0.7185039370078739607, 1.928577636452523993E-17, 1.250000000000000000 ) ) ;
#1046=CARTESIAN_POINT ( 'NONE',  ( -0.9500414927467378812, -0.1787899950787401604, 1.313976377898992132 ) ) ;
#1047=CARTESIAN_POINT ( 'NONE',  ( 0.8759842519685039353, 0.1574803149606299191, 0.6791338581601890079 ) ) ;
#1048=ORIENTED_EDGE ( 'NONE', *, *, #37438, .T. ) ;
#1054=CARTESIAN_POINT ( 'NONE',  ( 0.9500414927467378812, 0.1787899950787401604, 1.604330708607653921 ) ) ;
#1055=CARTESIAN_POINT ( 'NONE',  ( -1.033464566929133799, 0.000000000000000000, 1.190944881889763884 ) ) ;
#1056=CARTESIAN_POINT ( 'NONE',  ( -0.7646288533564489232, 0.1113553986120547346, 1.156496062884598608 ) ) ;
#1057=CARTESIAN_POINT ( 'NONE',  ( -0.9412147342319837628, 0.1574803149606300301, 0.9227362204724415262 ) ) ;
#1058=CARTESIAN_POINT ( 'NONE',  ( 0.8759842519685039353, 0.1574803149606299191, 1.948818897637795367 ) ) ;
#1059=CARTESIAN_POINT ( 'NONE',  ( 0.7185039370078760701, 0.06523048226348075740, 0.3715551180027094613 ) ) ;
#1060=ORIENTED_EDGE ( 'NONE', *, *, #16668, .T. ) ;
#1063=CARTESIAN_POINT ( 'NONE',  ( 0.7495606340400177148, -0.1264236179284866091, 0.6815944881352126172 ) ) ;
#1064=CARTESIAN_POINT ( 'NONE',  ( -1.002407869896990045, 0.1264236179284866091, 1.523129921206078707 ) ) ;
#1066=CARTESIAN_POINT ( 'NONE',  ( -1.054774247047244540, -0.07405724077823318263, 1.323818897584032817 ) ) ;
#1069=CARTESIAN_POINT ( 'NONE',  ( -0.8019270111902717657, -0.1787899950787401604, 0.3297244093950552069 ) ) ;
#1070=DIRECTION ( 'NONE',  ( 0.000000000000000000, 0.000000000000000000, -1.000000000000000000 ) ) ;
#1074=EDGE_LOOP ( 'NONE', ( #27931, #18471, #35975, #5562 ) ) ;
#1076=ORIENTED_EDGE ( 'NONE', *, *, #45990, .T. ) ;
#1082=EDGE_CURVE ( 'NONE', #21217, #8391, #23509, .T. ) ;
#1083=CARTESIAN_POINT ( 'NONE',  ( -1.033464566929134687, 0.06523048226347956391, 0.8390748031496061410 ) ) ;
#1084=DIRECTION ( 'NONE',  ( 1.822029033848725028E-16, 0.000000000000000000, 1.000000000000000000 ) ) ;
#1088=CARTESIAN_POINT ( 'NONE',  ( -0.8759842519685039353, -0.1574803149606299191, 1.564960629813732185 ) ) ;
#1090=CARTESIAN_POINT ( 'NONE',  ( 1.002407869896990045, 0.1264236179284866091, 0.8587598424659212970 ) ) ;
#1091=CARTESIAN_POINT ( 'NONE',  ( 1.002407869896990045, 0.1264236179284866091, 1.405019684985606476 ) ) ;
#1092=CARTESIAN_POINT ( 'NONE',  ( -0.7185039370078739607, 1.928577636452523993E-17, 0.4625984251968504046 ) ) ;
#1093=CARTESIAN_POINT ( 'NONE',  ( 0.8107537697050253289, 0.1574803149606300301, 1.636318897637794700 ) ) ;
#1094=CARTESIAN_POINT ( 'NONE',  ( 0.7117081823007622710, -0.03022371456366571355, 1.983825291605011643 ) ) ;
#1099=CARTESIAN_POINT ( 'NONE',  ( 0.8759842519685039353, 0.1787899950787401882, 0.8981299212060788184 ) ) ;
#1100=CARTESIAN_POINT ( 'NONE',  ( -0.9873396505805591694, -0.1113553986120547346, 1.422244094488188892 ) ) ;
#1101=CARTESIAN_POINT ( 'NONE',  ( 1.054774247047244096, 0.000000000000000000, 1.838090551127338657 ) ) ;
#1104=ORIENTED_EDGE ( 'NONE', *, *, #45815, .T. ) ;
#1105=CARTESIAN_POINT ( 'NONE',  ( 0.7646288533564489232, 0.1113553986120547346, 1.087598425196850460 ) ) ;
#1107=CARTESIAN_POINT ( 'NONE',  ( -0.9873396505805591694, -0.1113553986120547346, 0.07381889753026830980 ) ) ;
#1108=CARTESIAN_POINT ( 'NONE',  ( 0.6971942568897637749, 2.189545951927499583E-17, 1.065452755851747924 ) ) ;
#1112=AXIS2_PLACEMENT_3D ( 'NONE', #692, #36914, #11285 ) ;
#1113=CYLINDRICAL_SURFACE ( 'NONE', #14538, 0.1574803149606299191 ) ;
#1114=CARTESIAN_POINT ( 'NONE',  ( -1.054774247047244096, 0.000000000000000000, 0.2977362204186775885 ) ) ;
#1119=CARTESIAN_POINT ( 'NONE',  ( -0.9500414927467378812, -0.1787899950787401604, 1.865157480261195877 ) ) ;
#1121=CARTESIAN_POINT ( 'NONE',  ( -0.9500414927467378812, 0.1787899950787401604, 1.131889763725763665 ) ) ;
#1122=CARTESIAN_POINT ( 'NONE',  ( -0.9500414927467378812, 0.1787899950787401604, 0.5856299212060785964 ) ) ;
#1124=CARTESIAN_POINT ( 'NONE',  ( -0.8107537697050234415, -0.1574803149606297803, 0.1058070865066461363 ) ) ;
#1126=CARTESIAN_POINT ( 'NONE',  ( -1.033464566929134687, 0.06523048226347956391, 0.3174212597349925224 ) ) ;
#1130=FACE_OUTER_BOUND ( 'NONE', #21280, .T. ) ;
#1131=CARTESIAN_POINT ( 'NONE',  ( 1.033464566929133799, 0.000000000000000000, 1.938976377952756014 ) ) ;
#1132=EDGE_CURVE ( 'NONE', #37374, #5152, #28405, .T. ) ;
#1134=CARTESIAN_POINT ( 'NONE',  ( -0.6971942568897626646, -0.07405724077823297447, 0.5167322834108034613 ) ) ;
#1137=CARTESIAN_POINT ( 'NONE',  ( -0.6971942568897648851, -0.07405724077823297447, 1.505905511757261062 ) ) ;
#1141=CARTESIAN_POINT ( 'NONE',  ( 0.9873396505805591694, 0.1113553986120547346, 0.4478346456692913202 ) ) ;
#1142=AXIS2_PLACEMENT_3D ( 'NONE', #179, #21291, #43334 ) ;
#1144=CARTESIAN_POINT ( 'NONE',  ( -0.7185039370078739607, 1.928577636452523993E-17, 1.082677165246803241 ) ) ;
#1145=CARTESIAN_POINT ( 'NONE',  ( 0.6971942568897637749, 2.189545951927499583E-17, 0.5585629920722204877 ) ) ;
#1147=CARTESIAN_POINT ( 'NONE',  ( 0.7646288533564489232, -0.1113553986120547346, 1.756889763671999782 ) ) ;
#1150=CARTESIAN_POINT ( 'NONE',  ( 0.7646288533564489232, 0.1113553986120547346, 1.983267716427905558 ) ) ;
#1151=EDGE_LOOP ( 'NONE', ( #21562, #26634, #30176, #184 ) ) ;
#1153=CARTESIAN_POINT ( 'NONE',  ( -0.8759842519685039353, 0.1787899950787401882, 1.099901574749385880 ) ) ;
#1154=CARTESIAN_POINT ( 'NONE',  ( 0.7185039370078739607, 1.928577636452523993E-17, 0.9744094488188976833 ) ) ;
#1155=CYLINDRICAL_SURFACE ( 'NONE', #17449, 0.1574803149606299191 ) ;
#1158=CARTESIAN_POINT ( 'NONE',  ( 1.033464566929133799, 0.000000000000000000, 0.5905511809948347235 ) ) ;
#1162=CARTESIAN_POINT ( 'NONE',  ( -0.8759842519685039353, 0.000000000000000000, 0.000000000000000000 ) ) ;
#1163=CARTESIAN_POINT ( 'NONE',  ( 0.8759842519685039353, 0.1574803149606299191, 1.279527559055118280 ) ) ;
#1164=CARTESIAN_POINT ( 'NONE',  ( -0.9412147342319837628, 0.1574803149606300301, 0.4404527557979849850 ) ) ;
#1168=CARTESIAN_POINT ( 'NONE',  ( 0.8107537697050253289, 0.1574803149606300301, 1.114665354223180804 ) ) ;
#1172=CARTESIAN_POINT ( 'NONE',  ( -0.7495606340400177148, 0.1264236179284866091, 1.734744094434425232 ) ) ;
#1173=CARTESIAN_POINT ( 'NONE',  ( 0.8759842519685039353, 0.1787899950787401882, 1.887303149552535420 ) ) ;
#1177=CARTESIAN_POINT ( 'NONE',  ( 1.054774247047244540, 0.07405724077823318263, 0.4625984251430869665 ) ) ;
#1178=CARTESIAN_POINT ( 'NONE',  ( -1.002407869896990045, -0.1264236179284866091, 1.316437007820252081 ) ) ;
#1180=CARTESIAN_POINT ( 'NONE',  ( -0.9500414927467377701, -0.1787899950787401604, 1.235236220418678199 ) ) ;
#1181=CARTESIAN_POINT ( 'NONE',  ( -0.8019270111902716547, 0.1787899950787401604, 0.7824803149068668695 ) ) ;
#1182=CARTESIAN_POINT ( 'NONE',  ( -0.8759842519685039353, 0.1787899950787401882, 0.8981299212060788184 ) ) ;
#1183=CARTESIAN_POINT ( 'NONE',  ( -1.054774247047244096, 0.000000000000000000, 0.1058070865604096300 ) ) ;
#1186=CARTESIAN_POINT ( 'NONE',  ( -1.002407869896990045, -0.1264236179284866091, 1.715059055064346527 ) ) ;
#1187=CARTESIAN_POINT ( 'NONE',  ( -0.9873396505805591694, -0.1113553986120547346, 2.002952755797984263 ) ) ;
#1188=CARTESIAN_POINT ( 'NONE',  ( -0.8107537697050253289, 0.1574803149606300301, 1.557578740157481212 ) ) ;
#1189=FACE_OUTER_BOUND ( 'NONE', #29440, .T. ) ;
#1190=CARTESIAN_POINT ( 'NONE',  ( 1.002407869896990045, -0.1264236179284866091, 1.557578740103716441 ) ) ;
#1192=LINE ( 'NONE', #30474, #15730 ) ;
#1199=( BOUNDED_CURVE ( )  B_SPLINE_CURVE ( 2, ( #19737, #45366, #23812, #12580, #27208, #38431, #31258, #13505, #13971 ),
 .UNSPECIFIED., .F., .T. ) 
 B_SPLINE_CURVE_WITH_KNOTS ( ( 3, 2, 2, 2, 3 ),
 ( 0.9699999999999999734, 0.9725000000000000311, 0.9749999999999999778, 0.9775000000000000355, 0.9799999999999999822 ),
 .UNSPECIFIED. ) 
 CURVE ( )  GEOMETRIC_REPRESENTATION_ITEM ( )  RATIONAL_B_SPLINE_CURVE ( ( 1.000000000000000000, 0.9238795325112939549, 1.000000000000000000, 0.9238795325112869605, 1.000000000000000000, 0.9238795325112869605, 1.000000000000000000, 0.9238795325112869605, 1.000000000000000000 ) ) 
 REPRESENTATION_ITEM ( '' )  ) ;
#1203=CARTESIAN_POINT ( 'NONE',  ( -0.8759842519685039353, 0.000000000000000000, 0.000000000000000000 ) ) ;
#1204=CARTESIAN_POINT ( 'NONE',  ( 1.054774247047244096, 0.000000000000000000, 1.833169291284818758 ) ) ;
#1209=CARTESIAN_POINT ( 'NONE',  ( 0.7495606340400177148, 0.1264236179284866091, 0.8243110235682834519 ) ) ;
#1210=( BOUNDED_CURVE ( )  B_SPLINE_CURVE ( 2, ( #33886, #41720, #19230, #37208, #26923, #30523, #30070, #19702, #12061 ),
 .UNSPECIFIED., .F., .F. ) 
 B_SPLINE_CURVE_WITH_KNOTS ( ( 3, 2, 2, 2, 3 ),
 ( 0.1499999999999999944, 0.1524999999999999967, 0.1549999999999999989, 0.1575000000000000011, 0.1600000000000000033 ),
 .UNSPECIFIED. ) 
 CURVE ( )  GEOMETRIC_REPRESENTATION_ITEM ( )  RATIONAL_B_SPLINE_CURVE ( ( 1.000000000000000000, 0.9238795325112869605, 1.000000000000000000, 0.9238795325112869605, 1.000000000000000000, 0.9238795325112869605, 1.000000000000000000, 0.9238795325112869605, 1.000000000000000000 ) ) 
 REPRESENTATION_ITEM ( '' )  ) ;
#1212=CARTESIAN_POINT ( 'NONE',  ( -0.7185039370078739607, 1.928577636452523993E-17, 1.525590551181102317 ) ) ;
#1214=CARTESIAN_POINT ( 'NONE',  ( 1.002407869896990045, -0.1264236179284866091, 1.872539370024976391 ) ) ;
#1215=CARTESIAN_POINT ( 'NONE',  ( 1.033464566929134687, -0.06523048226347956391, 0.1648622047244094890 ) ) ;
#1220=CARTESIAN_POINT ( 'NONE',  ( 1.054774247047244540, 0.07405724077823318263, 0.1870078739619845387 ) ) ;
#1221=CARTESIAN_POINT ( 'NONE',  ( -0.8019270111902717657, 0.1787899950787401604, 1.806102362150961316 ) ) ;
#1223=CARTESIAN_POINT ( 'NONE',  ( -0.6971942568897637749, 2.189545951927499583E-17, 1.227854330654897685 ) ) ;
#1224=CARTESIAN_POINT ( 'NONE',  ( -0.7185039370078739607, 1.928577636452523993E-17, 1.328740157480315043 ) ) ;
#1225=CARTESIAN_POINT ( 'NONE',  ( 0.8019270111902717657, 0.1787899950787401604, 1.299212598371432215 ) ) ;
#1226=CARTESIAN_POINT ( 'NONE',  ( -0.6971942568897626646, 0.07405724077823318263, 0.5561023621509617598 ) ) ;
#1227=CARTESIAN_POINT ( 'NONE',  ( 0.6971942568897648851, -0.07405724077823297447, 1.973425196796630088 ) ) ;
#1228=CARTESIAN_POINT ( 'NONE',  ( -0.6971942568897648851, -0.07405724077823297447, 1.225393700733637514 ) ) ;
#1229=APPLICATION_CONTEXT ( 'automotive_design' ) ;
#1231=CARTESIAN_POINT ( 'NONE',  ( 0.9873396505805591694, 0.1113553986120547346, 1.195866141732283561 ) ) ;
#1232=CARTESIAN_POINT ( 'NONE',  ( 1.054774247047244540, 0.07405724077823318263, 0.4625984251430869665 ) ) ;
#1233=CARTESIAN_POINT ( 'NONE',  ( -0.8019270111902716547, 0.1787899950787401604, 0.3887795275052913224 ) ) ;
#1238=CARTESIAN_POINT ( 'NONE',  ( 1.054774247047244540, -0.07405724077823318263, 0.8907480314422986378 ) ) ;
#1239=CARTESIAN_POINT ( 'NONE',  ( -0.7185039370078746268, -0.06523048226347956391, 0.2682086614173231909 ) ) ;
#1241=CARTESIAN_POINT ( 'NONE',  ( -0.7646288533564489232, 0.1113553986120547346, 0.4872047243019220208 ) ) ;
#1246=CARTESIAN_POINT ( 'NONE',  ( -0.8759842519685039353, -0.1574803149606299191, 0.1968503937007874127 ) ) ;
#1251=CARTESIAN_POINT ( 'NONE',  ( -0.8759842519685039353, -0.1574803149606299191, 0.07874015748031495954 ) ) ;
#1255=CARTESIAN_POINT ( 'NONE',  ( -1.033464566929133799, 0.000000000000000000, 1.545275590551181244 ) ) ;
#1256=CARTESIAN_POINT ( 'NONE',  ( 0.8759842519685039353, -0.1787899950787401882, 0.1697834645131655606 ) ) ;
#1260=CARTESIAN_POINT ( 'NONE',  ( 0.5314960629921260393, 0.000000000000000000, 4.498031496062992574 ) ) ;
#1262=EDGE_CURVE ( 'NONE', #3955, #45154, #243, .T. ) ;
#1263=CARTESIAN_POINT ( 'NONE',  ( -0.8759842519685039353, -0.1787899950787401882, 0.6077755904974173617 ) ) ;
#1267=FACE_OUTER_BOUND ( 'NONE', #22288, .T. ) ;
#1268=DIRECTION ( 'NONE',  ( 1.822029033848725028E-16, 0.000000000000000000, 1.000000000000000000 ) ) ;
#1269=CARTESIAN_POINT ( 'NONE',  ( 0.6971942568897648851, 0.07405724077823318263, 1.304133858213953667 ) ) ;
#1270=CARTESIAN_POINT ( 'NONE',  ( 1.054774247047244540, -0.07405724077823318263, 1.870078740103715331 ) ) ;
#1271=CARTESIAN_POINT ( 'NONE',  ( 0.9500414927467377701, -0.1787899950787401604, 0.2903543306548980185 ) ) ;
#1273=CARTESIAN_POINT ( 'NONE',  ( -0.7185039370078739607, 0.000000000000000000, -2.869337061179095023E-17 ) ) ;
#1274=CARTESIAN_POINT ( 'NONE',  ( -0.8759842519685039353, -0.1574803149606299191, 1.446850393593259732 ) ) ;
#1276=CARTESIAN_POINT ( 'NONE',  ( 0.8759842519685039353, -0.1787899950787401882, 0.4847440944344252323 ) ) ;
#1277=CARTESIAN_POINT ( 'NONE',  ( 0.7495606340400177148, -0.1264236179284866091, 1.306594488135212728 ) ) ;
#1278=CARTESIAN_POINT ( 'NONE',  ( -1.033464566929134687, -0.06523048226347956391, 0.7554133858267708668 ) ) ;
#1279=CARTESIAN_POINT ( 'NONE',  ( -0.8759842519685039353, 0.000000000000000000, 0.000000000000000000 ) ) ;
#1281=CARTESIAN_POINT ( 'NONE',  ( -0.6971942568897648851, 0.07405724077823318263, 1.338582677111590069 ) ) ;
#1282=CARTESIAN_POINT ( 'NONE',  ( 0.7646288533564489232, 0.1113553986120547346, 0.8809055117034961802 ) ) ;
#1283=VERTEX_POINT ( 'NONE', #42877 ) ;
#1284=CARTESIAN_POINT ( 'NONE',  ( -0.8107537697050254399, 0.1574803149606300301, 0.7997047243019207441 ) ) ;
#1286=ORIENTED_EDGE ( 'NONE', *, *, #30075, .F. ) ;
#1287=EDGE_CURVE ( 'NONE', #34753, #1625, #41935, .T. ) ;
#1290=CARTESIAN_POINT ( 'NONE',  ( -0.8107537697050253289, -0.1574803149606297803, 0.5782480313885360879 ) ) ;
#1291=CARTESIAN_POINT ( 'NONE',  ( 1.054774247047244096, 0.000000000000000000, 1.557578740103716441 ) ) ;
#1292=CARTESIAN_POINT ( 'NONE',  ( -0.8759842519685039353, 0.1574803149606299191, 1.279527559055118280 ) ) ;
#1293=CARTESIAN_POINT ( 'NONE',  ( 1.033464566929133799, 0.000000000000000000, 0.2066929133858267931 ) ) ;
#1295=CARTESIAN_POINT ( 'NONE',  ( 0.9412147342319837628, 0.1574803149606300301, 1.946358267716537638 ) ) ;
#1298=ORIENTED_EDGE ( 'NONE', *, *, #37653, .F. ) ;
#1301=CARTESIAN_POINT ( 'NONE',  ( 0.7646288533564489232, -0.1113553986120547346, 0.5856299212598424786 ) ) ;
#1303=CARTESIAN_POINT ( 'NONE',  ( 0.8759842519685039353, 0.1787899950787401882, 0.6668307086076534773 ) ) ;
#1304=CARTESIAN_POINT ( 'NONE',  ( 0.9500414927467377701, 0.1787899950787401604, 0.9793307086076531442 ) ) ;
#1305=CARTESIAN_POINT ( 'NONE',  ( -0.8019270111902716547, -0.1787899950787401604, 1.505905511757261062 ) ) ;
#1307=CARTESIAN_POINT ( 'NONE',  ( -0.6971942568897648851, 0.07405724077823318263, 1.264763779473795813 ) ) ;
#1314=ORIENTED_EDGE ( 'NONE', *, *, #8215, .T. ) ;
#1315=CARTESIAN_POINT ( 'NONE',  ( 0.8107537697050254399, -0.1574803149606297803, 1.208169291231056430 ) ) ;
#1319=( BOUNDED_CURVE ( )  B_SPLINE_CURVE ( 2, ( #8751, #5155, #41080, #19776, #19540, #34409, #4427, #23616, #16201 ),
 .UNSPECIFIED., .F., .T. ) 
 B_SPLINE_CURVE_WITH_KNOTS ( ( 3, 2, 2, 2, 3 ),
 ( 0.02999999999999999889, 0.03250000000000000111, 0.03500000000000000333, 0.03749999999999999861, 0.04000000000000000083 ),
 .UNSPECIFIED. ) 
 CURVE ( )  GEOMETRIC_REPRESENTATION_ITEM ( )  RATIONAL_B_SPLINE_CURVE ( ( 1.000000000000000000, 0.9238795325112869605, 1.000000000000000000, 0.9238795325112869605, 1.000000000000000000, 0.9238795325112869605, 1.000000000000000000, 0.9238795325112869605, 1.000000000000000000 ) ) 
 REPRESENTATION_ITEM ( '' )  ) ;
#1320=CARTESIAN_POINT ( 'NONE',  ( -0.7495606340400177148, -0.1264236179284866091, 0.2091535432533232486 ) ) ;
#1321=CARTESIAN_POINT ( 'NONE',  ( -0.9873396505805591694, -0.1113553986120547346, 0.9104330708661417804 ) ) ;
#1324=CARTESIAN_POINT ( 'NONE',  ( 0.7495606340400177148, 0.1264236179284866091, 0.8686023621509606496 ) ) ;
#1325=CARTESIAN_POINT ( 'NONE',  ( 0.7495606340400177148, -0.1264236179284866091, 1.424704724355685181 ) ) ;
#1326=CARTESIAN_POINT ( 'NONE',  ( -0.7185039370078739607, 1.928577636452523993E-17, 0.8562992125984251190 ) ) ;
#1327=CARTESIAN_POINT ( 'NONE',  ( 0.9412147342319837628, -0.1574803149606297803, 1.537893700787401841 ) ) ;
#1328=CARTESIAN_POINT ( 'NONE',  ( 0.7301145607164034601, -0.08514804839641164358, 1.984932717043631056 ) ) ;
#1332=CARTESIAN_POINT ( 'NONE',  ( -0.9873396505805591694, 0.1113553986120547346, 1.619094488081448846 ) ) ;
#1333=VECTOR ( 'NONE', #26259, 39.37007874015748143 ) ;
#1334=CARTESIAN_POINT ( 'NONE',  ( 1.033464566929133799, 0.000000000000000000, 1.427165354330708569 ) ) ;
#1335=CARTESIAN_POINT ( 'NONE',  ( 0.6971942568897637749, 2.189545951927499583E-17, 0.9867125983714331028 ) ) ;
#1336=CARTESIAN_POINT ( 'NONE',  ( 1.054774247047244540, -0.07405724077823318263, 1.874999999946236784 ) ) ;
#1338=CARTESIAN_POINT ( 'NONE',  ( 0.8107537697050253289, 0.1574803149606300301, 0.4060039369003469734 ) ) ;
#1341=LINE ( 'NONE', #8065, #13865 ) ;
#1344=CARTESIAN_POINT ( 'NONE',  ( -0.9873396505805591694, -0.1113553986120547346, 0.1131889762704257896 ) ) ;
#1345=CARTESIAN_POINT ( 'NONE',  ( 0.8759842519685039353, -0.1787899950787401882, 1.075295275536787276 ) ) ;
#1349=EDGE_CURVE ( 'NONE', #33650, #35903, #5146, .T. ) ;
#1350=CARTESIAN_POINT ( 'NONE',  ( -0.9500414927467378812, 0.1787899950787401604, 0.1870078739619845387 ) ) ;
#1354=CARTESIAN_POINT ( 'NONE',  ( -0.6971942568897648851, 0.07405724077823318263, 1.889763779473794258 ) ) ;
#1355=CARTESIAN_POINT ( 'NONE',  ( -1.002407869896990045, 0.1264236179284866091, 0.8932086613635591421 ) ) ;
#1357=CARTESIAN_POINT ( 'NONE',  ( -0.6971942568897637749, 2.189545951927499583E-17, 0.5585629920722204877 ) ) ;
#1368=CARTESIAN_POINT ( 'NONE',  ( -1.054774247047244540, -0.07405724077823318263, 0.4527559054580477249 ) ) ;
#1370=CARTESIAN_POINT ( 'NONE',  ( -0.8759842519685039353, -0.1787899950787401882, 1.552657480261196765 ) ) ;
#1373=( CONVERSION_BASED_UNIT ( 'INCH', #8573 ) LENGTH_UNIT ( ) NAMED_UNIT ( #37463 ) ) ;
#1375=CARTESIAN_POINT ( 'NONE',  ( 1.033464566929133799, 1.928577636452524610E-17, 4.498031496062992574 ) ) ;
#1376=CARTESIAN_POINT ( 'NONE',  ( -0.8759842519685039353, -0.1574803149606299191, 1.289370078632629868 ) ) ;
#1377=CARTESIAN_POINT ( 'NONE',  ( 0.7495606340400177148, -0.1264236179284866091, 0.5241141731745827537 ) ) ;
#1379=CARTESIAN_POINT ( 'NONE',  ( 0.8107537697050254399, -0.1574803149606297803, 0.3518700787401575769 ) ) ;
#1380=CARTESIAN_POINT ( 'NONE',  ( -1.033464566929134687, 0.06523048226347956391, 0.4060039370078741827 ) ) ;
#1384=CARTESIAN_POINT ( 'NONE',  ( -1.054774247047244096, 0.000000000000000000, 1.050688976324189117 ) ) ;
#1385=CARTESIAN_POINT ( 'NONE',  ( 0.7185039370078746268, 0.06523048226347956391, 1.168799212598425896 ) ) ;
#1387=CARTESIAN_POINT ( 'NONE',  ( 1.033464566929133355, -0.06523048226348075740, 0.5880905510735754405 ) ) ;
#1388=CARTESIAN_POINT ( 'NONE',  ( -0.8759842519685039353, 0.000000000000000000, 1.990649606245448844 ) ) ;
#1392=ADVANCED_FACE ( 'NONE', ( #33283 ), #26320, .T. ) ;
#1394=EDGE_LOOP ( 'NONE', ( #19452, #2996, #3138, #1298 ) ) ;
#1395=CARTESIAN_POINT ( 'NONE',  ( 0.7646288533564489232, 0.1113553986120547346, 1.284448818897637956 ) ) ;
#1401=CARTESIAN_POINT ( 'NONE',  ( 0.7646288533564489232, 0.1113553986120547346, 1.077755905404283565 ) ) ;
#1403=ORIENTED_EDGE ( 'NONE', *, *, #27999, .T. ) ;
#1405=CARTESIAN_POINT ( 'NONE',  ( -0.7495606340400177148, 0.1264236179284866091, 1.695374015694267822 ) ) ;
#1406=CARTESIAN_POINT ( 'NONE',  ( 1.054774247047244540, -0.07405724077823318263, 1.796259842465923073 ) ) ;
#1409=CARTESIAN_POINT ( 'NONE',  ( 1.002407869896990045, 0.1264236179284866091, 0.4256889763241890057 ) ) ;
#1410=CARTESIAN_POINT ( 'NONE',  ( -0.6971942568897637749, 2.189545951927499583E-17, 1.380413385773007873 ) ) ;
#1411=CYLINDRICAL_SURFACE ( 'NONE', #33531, 0.1574803149606299191 ) ;
#1412=CARTESIAN_POINT ( 'NONE',  ( -0.9500414927467377701, 0.1787899950787401604, 1.407480314906865981 ) ) ;
#1413=CARTESIAN_POINT ( 'NONE',  ( -1.002407869896990045, -0.1264236179284866091, 0.8046259841982047467 ) ) ;
#1414=CARTESIAN_POINT ( 'NONE',  ( -0.6971942568897626646, -0.07405724077823297447, 0.8710629920722218200 ) ) ;
#1415=CARTESIAN_POINT ( 'NONE',  ( -1.054774247047244540, 0.07405724077823318263, 0.1476377952218269618 ) ) ;
#1416=DIRECTION ( 'NONE',  ( 0.000000000000000000, 0.000000000000000000, -1.000000000000000000 ) ) ;
#1417=CARTESIAN_POINT ( 'NONE',  ( -0.9500414927467378812, -0.1787899950787401604, 1.712598425143087688 ) ) ;
#1418=CARTESIAN_POINT ( 'NONE',  ( -1.054774247047244540, -0.07405724077823318263, 0.1033464566391498751 ) ) ;
#1419=CARTESIAN_POINT ( 'NONE',  ( -0.9412147342319837628, -0.1574803149606297803, 1.695374015748031482 ) ) ;
#1420=CARTESIAN_POINT ( 'NONE',  ( -0.8107537697050254399, 0.1574803149606300301, 0.2977362204724410821 ) ) ;
#1421=CARTESIAN_POINT ( 'NONE',  ( 0.7495606340400177148, -0.1264236179284866091, 1.587106299158834721 ) ) ;
#1423=CARTESIAN_POINT ( 'NONE',  ( -0.8759842519685039353, 0.000000000000000000, 0.000000000000000000 ) ) ;
#1426=CARTESIAN_POINT ( 'NONE',  ( -0.8019270111902716547, 0.1787899950787401604, 1.181102362150960428 ) ) ;
#1432=CARTESIAN_POINT ( 'NONE',  ( 0.7495606340400177148, 0.1264236179284866091, 1.847933070812378009 ) ) ;
#1439=CARTESIAN_POINT ( 'NONE',  ( 0.6971942568897626646, 0.07405724077823318263, 0.9055118109698585549 ) ) ;
#1441=DIRECTION ( 'NONE',  ( 0.000000000000000000, 0.000000000000000000, -1.000000000000000000 ) ) ;
#1443=CARTESIAN_POINT ( 'NONE',  ( 0.9500414927467378812, -0.1787899950787401604, 1.988188976324187562 ) ) ;
#1449=CARTESIAN_POINT ( 'NONE',  ( -0.7185039370078739607, 0.000000000000000000, -2.869337061179095023E-17 ) ) ;
#1452=CARTESIAN_POINT ( 'NONE',  ( -1.054774247047244540, -0.07405724077823318263, 1.751968503883245765 ) ) ;
#1454=CARTESIAN_POINT ( 'NONE',  ( -0.8759842519685039353, 0.1787899950787401882, 1.375492125930488196 ) ) ;
#1455=CARTESIAN_POINT ( 'NONE',  ( 0.8019270111902717657, 0.1787899950787401604, 1.456692913332062744 ) ) ;
#1457=CARTESIAN_POINT ( 'NONE',  ( -0.7495606340400177148, -0.1264236179284866091, 0.5241141731745827537 ) ) ;
#1458=CARTESIAN_POINT ( 'NONE',  ( -1.002407869896990045, -0.1264236179284866091, 1.158956692859621995 ) ) ;
#1461=CARTESIAN_POINT ( 'NONE',  ( 1.054774247047244540, -0.07405724077823318263, 0.4576771653005669016 ) ) ;
#1462=CARTESIAN_POINT ( 'NONE',  ( -0.7495606340400177148, 0.1264236179284866091, 0.3912401574265515491 ) ) ;
#1464=( BOUNDED_CURVE ( )  B_SPLINE_CURVE ( 2, ( #11705, #33769, #32816, #14821, #25384, #29256, #36626, #26330, #29487 ),
 .UNSPECIFIED., .F., .T. ) 
 B_SPLINE_CURVE_WITH_KNOTS ( ( 3, 2, 2, 2, 3 ),
 ( 0.1799999999999999933, 0.1824999999999999956, 0.1849999999999999978, 0.1875000000000000000, 0.1900000000000000022 ),
 .UNSPECIFIED. ) 
 CURVE ( )  GEOMETRIC_REPRESENTATION_ITEM ( )  RATIONAL_B_SPLINE_CURVE ( ( 1.000000000000000000, 0.9238795325112869605, 1.000000000000000000, 0.9238795325112869605, 1.000000000000000000, 0.9238795325112869605, 1.000000000000000000, 0.9238795325112869605, 1.000000000000000000 ) ) 
 REPRESENTATION_ITEM ( '' )  ) ;
#1467=VERTEX_POINT ( 'NONE', #10334 ) ;
#1468=CARTESIAN_POINT ( 'NONE',  ( -0.7185039370078739607, 1.928577636452523993E-17, 0.2657480314960630197 ) ) ;
#1470=CARTESIAN_POINT ( 'NONE',  ( -1.002407869896990045, -0.1264236179284866091, 1.946358267662771757 ) ) ;
#1471=CARTESIAN_POINT ( 'NONE',  ( -0.7185039370078746268, -0.06523048226347956391, 1.961122047244095778 ) ) ;
#1472=ORIENTED_EDGE ( 'NONE', *, *, #29449, .F. ) ;
#1474=CARTESIAN_POINT ( 'NONE',  ( -0.6971942568897648851, 0.07405724077823318263, 1.028543307032851795 ) ) ;
#1476=CARTESIAN_POINT ( 'NONE',  ( -0.6971942568897626646, 0.07405724077823318263, 0.03937007868639404856 ) ) ;
#1479=CARTESIAN_POINT ( 'NONE',  ( -0.9412147342319837628, 0.1574803149606300301, 0.1648622046168823629 ) ) ;
#1481=CARTESIAN_POINT ( 'NONE',  ( 1.033464566929133799, 0.000000000000000000, 1.692913385719244213 ) ) ;
#1484=CARTESIAN_POINT ( 'NONE',  ( 0.8759842519685039353, 0.1574803149606299191, 1.466535432963338437 ) ) ;
#1485=DIRECTION ( 'NONE',  ( 1.822029033848725028E-16, 0.000000000000000000, 1.000000000000000000 ) ) ;
#1486=( BOUNDED_CURVE ( )  B_SPLINE_CURVE ( 2, ( #17218, #9568, #24880, #43066, #31853, #38789, #17678, #5946, #39240 ),
 .UNSPECIFIED., .F., .T. ) 
 B_SPLINE_CURVE_WITH_KNOTS ( ( 3, 2, 2, 2, 3 ),
 ( 0.3300000000000000155, 0.3325000000000000178, 0.3350000000000000200, 0.3375000000000000222, 0.3400000000000000244 ),
 .UNSPECIFIED. ) 
 CURVE ( )  GEOMETRIC_REPRESENTATION_ITEM ( )  RATIONAL_B_SPLINE_CURVE ( ( 1.000000000000000000, 0.9238795325112869605, 1.000000000000000000, 0.9238795325112869605, 1.000000000000000000, 0.9238795325112869605, 1.000000000000000000, 0.9238795325112869605, 1.000000000000000000 ) ) 
 REPRESENTATION_ITEM ( '' )  ) ;
#1495=CARTESIAN_POINT ( 'NONE',  ( -0.8759842519685039353, 0.1787899950787401882, 0.6274606298674959559 ) ) ;
#1501=CARTESIAN_POINT ( 'NONE',  ( 0.6971942568897648851, 0.07405724077823318263, 1.579724409395055318 ) ) ;
#1503=CARTESIAN_POINT ( 'NONE',  ( 0.6971942568897637749, 2.189545951927499583E-17, 1.892224409395055096 ) ) ;
#1506=ADVANCED_FACE ( 'NONE', ( #36617 ), #1113, .T. ) ;
#1510=CARTESIAN_POINT ( 'NONE',  ( 1.033464566929133799, 0.000000000000000000, 0.5118110235145204578 ) ) ;
#1511=CARTESIAN_POINT ( 'NONE',  ( 1.054774247047244096, 0.000000000000000000, 0.4552165353793071745 ) ) ;
#1512=CARTESIAN_POINT ( 'NONE',  ( -0.7185039370078739607, 1.928577636452523993E-17, 1.722440944881889813 ) ) ;
#1515=CARTESIAN_POINT ( 'NONE',  ( -0.7495606340400177148, -0.1264236179284866091, 1.306594488135212728 ) ) ;
#1516=CARTESIAN_POINT ( 'NONE',  ( 0.7646288533564489232, 0.1113553986120547346, 0.8021653542231811373 ) ) ;
#1519=CARTESIAN_POINT ( 'NONE',  ( 0.8019270111902717657, 0.1787899950787401604, 0.9842519684501742638 ) ) ;
#1520=VERTEX_POINT ( 'NONE', #24946 ) ;
#1522=CARTESIAN_POINT ( 'NONE',  ( -0.9412147342319837628, -0.1574803149606297803, 0.5437992124908979097 ) ) ;
#1524=CARTESIAN_POINT ( 'NONE',  ( 0.9500414927467378812, 0.1787899950787401604, 1.722440944828125930 ) ) ;
#1525=CARTESIAN_POINT ( 'NONE',  ( -1.033464566929134687, -0.06523048226347956391, 1.306594488188977055 ) ) ;
#1529=CARTESIAN_POINT ( 'NONE',  ( 1.002407869896990045, -0.1264236179284866091, 0.06151574797773248782 ) ) ;
#1530=CARTESIAN_POINT ( 'NONE',  ( 0.7185039370078746268, -0.06523048226347956391, 1.360728346349165285 ) ) ;
#1531=VERTEX_POINT ( 'NONE', #22453 ) ;
#1535=VERTEX_POINT ( 'NONE', #39542 ) ;
#1536=CARTESIAN_POINT ( 'NONE',  ( -1.002407869896990045, 0.1264236179284866091, 1.601870078686393750 ) ) ;
#1538=CARTESIAN_POINT ( 'NONE',  ( -1.002407869896990045, -0.1264236179284866091, 1.478838582623401399 ) ) ;
#1550=ORIENTED_EDGE ( 'NONE', *, *, #36171, .F. ) ;
#1551=CARTESIAN_POINT ( 'NONE',  ( 0.7185039370078739607, 1.928577636452523993E-17, 1.751968503829480106 ) ) ;
#1555=CARTESIAN_POINT ( 'NONE',  ( -0.9500414927467377701, 0.1787899950787401604, 0.1525590550643468324 ) ) ;
#1556=CARTESIAN_POINT ( 'NONE',  ( -1.033464566929134687, 0.06523048226347956391, 0.9965551181102363376 ) ) ;
#1560=CARTESIAN_POINT ( 'NONE',  ( 0.8019270111902717657, -0.1787899950787401604, 0.8809055117572599514 ) ) ;
#1561=CARTESIAN_POINT ( 'NONE',  ( 1.002407869896990045, -0.1264236179284866091, 1.434547244040724534 ) ) ;
#1565=CARTESIAN_POINT ( 'NONE',  ( 0.8107537697050253289, -0.1574803149606297803, 1.532972440944882608 ) ) ;
#1566=CARTESIAN_POINT ( 'NONE',  ( 0.8184489996385461152, 0.1487827445626105083, 1.979498570521418532 ) ) ;
#1567=CARTESIAN_POINT ( 'NONE',  ( 0.7185039370078739607, 0.000000000000000000, 4.498031496062992574 ) ) ;
#1569=DIRECTION ( 'NONE',  ( 1.822029033848725028E-16, 0.000000000000000000, 1.000000000000000000 ) ) ;
#1572=CARTESIAN_POINT ( 'NONE',  ( 1.054774247047244540, -0.07405724077823318263, 1.003937007820253413 ) ) ;
#1573=CARTESIAN_POINT ( 'NONE',  ( 0.9500414927467377701, -0.1787899950787401604, 1.791338582623401177 ) ) ;
#1574=CARTESIAN_POINT ( 'NONE',  ( 0.8759842519685039353, -0.1574803149606299191, 0.3051181101286932762 ) ) ;
#1575=ORIENTED_EDGE ( 'NONE', *, *, #29905, .T. ) ;
#1576=DIRECTION ( 'NONE',  ( 1.822029033848725028E-16, 0.000000000000000000, 1.000000000000000000 ) ) ;
#1579=CARTESIAN_POINT ( 'NONE',  ( -0.8107537697050253289, 0.1574803149606300301, 0.2485236219397170265 ) ) ;
#1581=CARTESIAN_POINT ( 'NONE',  ( 0.6971942568897637749, 2.189545951927499583E-17, 1.301673228292692830 ) ) ;
#1584=LINE ( 'NONE', #16237, #3828 ) ;
#1585=CARTESIAN_POINT ( 'NONE',  ( -0.9500414927467378812, -0.1787899950787401604, 0.6053149605761579677 ) ) ;
#1591=CARTESIAN_POINT ( 'NONE',  ( -0.6971942568897648851, -0.07405724077823297447, 1.776574803095843924 ) ) ;
#1592=EDGE_LOOP ( 'NONE', ( #42543, #7954, #19874, #27330 ) ) ;
#1593=CARTESIAN_POINT ( 'NONE',  ( -0.6971942568897637749, 2.189545951927499583E-17, 0.5979330708123780092 ) ) ;
#1599=DIRECTION ( 'NONE',  ( -1.000000000000000000, 0.000000000000000000, 0.000000000000000000 ) ) ;
#1602=CARTESIAN_POINT ( 'NONE',  ( -1.033464566929133799, 0.000000000000000000, 1.771653543199558811 ) ) ;
#1603=CARTESIAN_POINT ( 'NONE',  ( -0.6971942568897626646, 0.07405724077823318263, 0.5118110235682844511 ) ) ;
#1610=CARTESIAN_POINT ( 'NONE',  ( -0.6971942568897637749, 2.189545951927499583E-17, 1.503444881836000002 ) ) ;
#1611=EDGE_CURVE ( 'NONE', #8914, #32474, #33311, .T. ) ;
#1615=CARTESIAN_POINT ( 'NONE',  ( 0.8107537697050234415, -0.1574803149606297803, 0.1943897637795276023 ) ) ;
#1616=CARTESIAN_POINT ( 'NONE',  ( 0.7185039370078739607, 1.928577636452523993E-17, 0.4625984251968504046 ) ) ;
#1619=CARTESIAN_POINT ( 'NONE',  ( -0.7646288533564489232, -0.1113553986120547346, 1.245078740049952559 ) ) ;
#1620=CARTESIAN_POINT ( 'NONE',  ( 0.7495606340400177148, -0.1264236179284866091, 0.5634842519147401640 ) ) ;
#1621=CARTESIAN_POINT ( 'NONE',  ( 0.7495606340400177148, -0.1264236179284866091, 0.04675196845017354913 ) ) ;
#1625=VERTEX_POINT ( 'NONE', #45907 ) ;
#1627=ADVANCED_FACE ( 'NONE', ( #42320 ), #19809, .T. ) ;
#1628=CARTESIAN_POINT ( 'NONE',  ( -0.8759842519685039353, 0.1787899950787401882, 1.139271653489543290 ) ) ;
#1629=CARTESIAN_POINT ( 'NONE',  ( 0.8107537697050253289, -0.1574803149606297803, 1.178641732283464583 ) ) ;
#1631=CARTESIAN_POINT ( 'NONE',  ( -1.002407869896990045, -0.1264236179284866091, 1.990649606245448844 ) ) ;
#1638=VERTEX_POINT ( 'NONE', #30404 ) ;
#1642=VERTEX_POINT ( 'NONE', #12881 ) ;
#1649=CARTESIAN_POINT ( 'NONE',  ( 0.9873396505805591694, -0.1113553986120547346, 1.294291338475149544 ) ) ;
#1650=CARTESIAN_POINT ( 'NONE',  ( -0.7185039370078714072, 0.06523048226347728795, 1.867618110128693720 ) ) ;
#1653=CARTESIAN_POINT ( 'NONE',  ( -0.8759842519685039353, 0.1787899950787401882, 1.690452755851748146 ) ) ;
#1654=CARTESIAN_POINT ( 'NONE',  ( 0.8759842519685039353, -0.1787899950787401882, 1.828248031442299082 ) ) ;
#1656=CARTESIAN_POINT ( 'NONE',  ( 1.033464566929134687, -0.06523048226347956391, 0.5585629921259840369 ) ) ;
#1657=CARTESIAN_POINT ( 'NONE',  ( 1.002407869896990045, -0.1264236179284866091, 0.3764763778989925203 ) ) ;
#1658=CARTESIAN_POINT ( 'NONE',  ( -0.6971942568897637749, 2.189545951927499583E-17, 1.341043307032850462 ) ) ;
#1659=CARTESIAN_POINT ( 'NONE',  ( 0.7185039370078739607, 1.928577636452523993E-17, 0.6988188976377952555 ) ) ;
#1660=CARTESIAN_POINT ( 'NONE',  ( -0.6971942568897626646, 0.07405724077823318263, 0.8661417322297003674 ) ) ;
#1661=CARTESIAN_POINT ( 'NONE',  ( -1.054774247047244096, 0.000000000000000000, 0.1451771653005673179 ) ) ;
#1662=CARTESIAN_POINT ( 'NONE',  ( 0.7185039370078746268, -0.06523048226347956391, 1.567421259842519454 ) ) ;
#1663=CARTESIAN_POINT ( 'NONE',  ( -0.8019270111902717657, -0.1787899950787401604, 1.786417322780882388 ) ) ;
#1664=CARTESIAN_POINT ( 'NONE',  ( -1.054774247047244540, -0.07405724077823318263, 0.06397637789899228433 ) ) ;
#1666=CARTESIAN_POINT ( 'NONE',  ( -0.7646288533564489232, -0.1113553986120547346, 1.766732283464566899 ) ) ;
#1667=CARTESIAN_POINT ( 'NONE',  ( 1.002407869896990045, -0.1264236179284866091, 1.675688976324189117 ) ) ;
#1669=DIRECTION ( 'NONE',  ( 0.000000000000000000, 0.000000000000000000, 1.000000000000000000 ) ) ;
#1673=ORIENTED_EDGE ( 'NONE', *, *, #12185, .T. ) ;
#1677=VECTOR ( 'NONE', #22205, 39.37007874015748143 ) ;
#1680=CARTESIAN_POINT ( 'NONE',  ( -0.9412147342319837628, -0.1574803149606297803, 0.5930118110236221041 ) ) ;
#1684=CARTESIAN_POINT ( 'NONE',  ( -0.9412147342319837628, -0.1574803149606297803, 0.8587598424121576368 ) ) ;
#1686=CARTESIAN_POINT ( 'NONE',  ( 0.7495606340400177148, 0.1264236179284866091, 0.9424212597887559051 ) ) ;
#1689=CARTESIAN_POINT ( 'NONE',  ( 0.7495606340400177148, 0.1264236179284866091, 1.970964566875370139 ) ) ;
#1690=CARTESIAN_POINT ( 'NONE',  ( 0.7185039370078739607, 1.928577636452523993E-17, 0.2263779527559055260 ) ) ;
#1691=CARTESIAN_POINT ( 'NONE',  ( 0.8759842519685039353, 0.000000000000000000, 4.498031496062992574 ) ) ;
#1693=CARTESIAN_POINT ( 'NONE',  ( 1.033464566929133799, 1.928577636452524610E-17, 4.498031496062992574 ) ) ;
#1696=CARTESIAN_POINT ( 'NONE',  ( -0.8019270111902717657, -0.1787899950787401604, 1.742125984198204858 ) ) ;
#1697=VERTEX_POINT ( 'NONE', #27757 ) ;
#1699=CARTESIAN_POINT ( 'NONE',  ( 0.8759842519685039353, -0.1787899950787401882, 1.434547244040724534 ) ) ;
#1700=CARTESIAN_POINT ( 'NONE',  ( -0.6971942568897637749, 2.189545951927499583E-17, 0.5191929133320630774 ) ) ;
#1703=CARTESIAN_POINT ( 'NONE',  ( -0.9500414927467378812, -0.1787899950787401604, 1.274606299158834277 ) ) ;
#1706=CARTESIAN_POINT ( 'NONE',  ( 0.8759842519685039353, 0.1787899950787401882, 0.5487204723871811352 ) ) ;
#1707=CARTESIAN_POINT ( 'NONE',  ( -0.9500414927467377701, 0.1787899950787401604, 0.5019685038832443214 ) ) ;
#1708=CARTESIAN_POINT ( 'NONE',  ( -1.002407869896990045, 0.1264236179284866091, 0.8144685038832440993 ) ) ;
#1714=CARTESIAN_POINT ( 'NONE',  ( -0.8759842519685039353, -0.1574803149606299191, 0.3543307086614173040 ) ) ;
#1715=CARTESIAN_POINT ( 'NONE',  ( 0.6971942568897637749, 2.189545951927499583E-17, 1.188484251914740275 ) ) ;
#1717=CARTESIAN_POINT ( 'NONE',  ( -0.7185039370078739607, 1.928577636452523993E-17, 0.4921259841444416971 ) ) ;
#1719=EDGE_CURVE ( 'NONE', #3727, #47141, #38174, .T. ) ;
#1720=CARTESIAN_POINT ( 'NONE',  ( -0.9500414927467378812, -0.1787899950787401604, 0.9645669290800953366 ) ) ;
#1721=EDGE_CURVE ( 'NONE', #24716, #11036, #37626, .T. ) ;
#1722=CARTESIAN_POINT ( 'NONE',  ( -1.002407869896990045, -0.1264236179284866091, 0.2140748030958428971 ) ) ;
#1724=ORIENTED_EDGE ( 'NONE', *, *, #18503, .F. ) ;
#1729=CARTESIAN_POINT ( 'NONE',  ( 1.002407869896990045, 0.1264236179284866091, 1.286909448765133801 ) ) ;
#1730=EDGE_CURVE ( 'NONE', #47099, #3114, #36085, .T. ) ;
#1733=VECTOR ( 'NONE', #44365, 39.37007874015748143 ) ;
#1734=DIRECTION ( 'NONE',  ( -1.000000000000000000, 0.000000000000000000, 0.000000000000000000 ) ) ;
#1735=CARTESIAN_POINT ( 'NONE',  ( 0.6971942568897648851, 0.07405724077823318263, 1.574803149552536530 ) ) ;
#1740=CARTESIAN_POINT ( 'NONE',  ( 0.7495606340400177148, 0.1264236179284866091, 0.4699803149068661479 ) ) ;
#1741=CARTESIAN_POINT ( 'NONE',  ( -1.054774247047244540, 0.07405724077823318263, 0.7381889763241898939 ) ) ;
#1745=CARTESIAN_POINT ( 'NONE',  ( -0.7919991761111997430, -0.1498786536115133128, 1.986579935406608932 ) ) ;
#1751=CARTESIAN_POINT ( 'NONE',  ( 0.8759842519685039353, -0.1787899950787401882, 1.513287401521039355 ) ) ;
#1752=CARTESIAN_POINT ( 'NONE',  ( 1.054774247047244540, 0.07405724077823318263, 1.796259842465920853 ) ) ;
#1753=CARTESIAN_POINT ( 'NONE',  ( 0.9500414927467377701, 0.1787899950787401604, 0.4625984251430869665 ) ) ;
#1756=DIRECTION ( 'NONE',  ( 0.000000000000000000, 0.000000000000000000, -1.000000000000000000 ) ) ;
#1757=DIRECTION ( 'NONE',  ( 0.8660254037844389297, 1.060575238724907285E-16, -0.4999999999999994449 ) ) ;
#1759=CARTESIAN_POINT ( 'NONE',  ( 1.002407869896990045, 0.1264236179284866091, 0.4207677164816693294 ) ) ;
#1760=CARTESIAN_POINT ( 'NONE',  ( 0.7791120256548125234, -0.1328245026793817840, 0.03936940671680725506 ) ) ;
#1761=CARTESIAN_POINT ( 'NONE',  ( -0.8759842519685039353, 0.000000000000000000, 0.000000000000000000 ) ) ;
#1762=CARTESIAN_POINT ( 'NONE',  ( 0.8759842519685039353, 0.1574803149606299191, 0.8464566929133857665 ) ) ;
#1763=CARTESIAN_POINT ( 'NONE',  ( -0.8759842519685039353, 0.1787899950787401882, 1.370570866087968520 ) ) ;
#1764=CARTESIAN_POINT ( 'NONE',  ( 0.9873396505805591694, 0.1113553986120547346, 0.8316929132782993062 ) ) ;
#1766=CARTESIAN_POINT ( 'NONE',  ( 0.6971942568897637749, 2.189545951927499583E-17, 1.070374015694267600 ) ) ;
#1770=CARTESIAN_POINT ( 'NONE',  ( -0.7185039370078746268, -0.06523048226347956391, 0.6126968502861739330 ) ) ;
#1772=CARTESIAN_POINT ( 'NONE',  ( 0.7495606340400177148, -0.1264236179284866091, 1.700295275536787498 ) ) ;
#1773=CARTESIAN_POINT ( 'NONE',  ( -0.9412147342319837628, 0.1574803149606300301, 1.316437007874015519 ) ) ;
#1774=CARTESIAN_POINT ( 'NONE',  ( -0.8107537697050254399, 0.1574803149606300301, 1.154035432963338659 ) ) ;
#1775=DIRECTION ( 'NONE',  ( 1.822029033848725028E-16, 0.000000000000000000, 1.000000000000000000 ) ) ;
#1776=CARTESIAN_POINT ( 'NONE',  ( 0.8759842519685039353, -0.1787899950787401882, 0.1353346456155279653 ) ) ;
#1777=CARTESIAN_POINT ( 'NONE',  ( 0.7185039370078746268, 0.06523048226347956391, 1.395177165246804130 ) ) ;
#1778=EDGE_LOOP ( 'NONE', ( #39006, #25813, #3590, #30137 ) ) ;
#1782=CARTESIAN_POINT ( 'NONE',  ( 1.054774247047244540, -0.07405724077823318263, 0.6938976377415123631 ) ) ;
#1783=CARTESIAN_POINT ( 'NONE',  ( -0.6971942568897648851, -0.07405724077823297447, 1.619094488135213838 ) ) ;
#1787=ORIENTED_EDGE ( 'NONE', *, *, #21920, .F. ) ;
#1788=( BOUNDED_CURVE ( )  B_SPLINE_CURVE ( 2, ( #25686, #25908, #14180, #33358, #3134, #36463, #35974, #32410, #3620 ),
 .UNSPECIFIED., .F., .F. ) 
 B_SPLINE_CURVE_WITH_KNOTS ( ( 3, 2, 2, 2, 3 ),
 ( 0.1600000000000000033, 0.1625000000000000056, 0.1650000000000000078, 0.1675000000000000100, 0.1700000000000000122 ),
 .UNSPECIFIED. ) 
 CURVE ( )  GEOMETRIC_REPRESENTATION_ITEM ( )  RATIONAL_B_SPLINE_CURVE ( ( 1.000000000000000000, 0.9238795325112869605, 1.000000000000000000, 0.9238795325112869605, 1.000000000000000000, 0.9238795325112869605, 1.000000000000000000, 0.9238795325112869605, 1.000000000000000000 ) ) 
 REPRESENTATION_ITEM ( '' )  ) ;
#1790=CARTESIAN_POINT ( 'NONE',  ( -1.033464566929133799, 0.000000000000000000, 0.2362204723334177248 ) ) ;
#1795=EDGE_LOOP ( 'NONE', ( #46640, #41069, #14398, #46541 ) ) ;
#1796=ADVANCED_FACE ( 'NONE', ( #42541 ), #24822, .T. ) ;
#1797=ORIENTED_EDGE ( 'NONE', *, *, #45159, .F. ) ;
#1798=EDGE_CURVE ( 'NONE', #8209, #31760, #18021, .T. ) ;
#1799=LINE ( 'NONE', #12615, #43945 ) ;
#1801=CARTESIAN_POINT ( 'NONE',  ( 0.9873396505805591694, -0.1113553986120547346, 1.855314960629921295 ) ) ;
#1803=CARTESIAN_POINT ( 'NONE',  ( -0.9500414927467377701, -0.1787899950787401604, 0.1377952755367876370 ) ) ;
#1804=CARTESIAN_POINT ( 'NONE',  ( -0.9873396505805591694, -0.1113553986120547346, 1.107283464566929165 ) ) ;
#1807=CARTESIAN_POINT ( 'NONE',  ( 1.002407869896990045, -0.1264236179284866091, 1.085137795221826629 ) ) ;
#1808=DIRECTION ( 'NONE',  ( 1.000000000000000000, 0.000000000000000000, -1.822029033848725275E-16 ) ) ;
#1810=CARTESIAN_POINT ( 'NONE',  ( 0.7646288533564489232, 0.1113553986120547346, 1.560039370078740273 ) ) ;
#1813=CARTESIAN_POINT ( 'NONE',  ( 0.8107537697050254399, -0.1574803149606297803, 0.4601377951680635792 ) ) ;
#1814=CARTESIAN_POINT ( 'NONE',  ( -0.7185039370078746268, 0.06523048226347956391, 1.631397637687747926 ) ) ;
#1815=CARTESIAN_POINT ( 'NONE',  ( -0.9873396505805591694, -0.1113553986120547346, 0.7037401573727875004 ) ) ;
#1816=CARTESIAN_POINT ( 'NONE',  ( 0.6971942568897637749, 2.189545951927499583E-17, 0.9473425196312755814 ) ) ;
#1817=CARTESIAN_POINT ( 'NONE',  ( 0.8019270111902716547, 0.1787899950787401604, 1.771653543253322249 ) ) ;
#1818=CARTESIAN_POINT ( 'NONE',  ( 0.8107537697050234415, -0.1574803149606297803, 0.2632874014672759722 ) ) ;
#1819=ORIENTED_EDGE ( 'NONE', *, *, #20179, .T. ) ;
#1821=CARTESIAN_POINT ( 'NONE',  ( 1.031250533963468774, 0.03915069072625195629, 0.03937005934756545450 ) ) ;
#1823=CARTESIAN_POINT ( 'NONE',  ( -0.8759842519685039353, -0.1574803149606299191, 0.2657480313885358103 ) ) ;
#1824=CARTESIAN_POINT ( 'NONE',  ( 0.8019270111902717657, -0.1787899950787401604, 1.269685039316314601 ) ) ;
#1828=LINE ( 'NONE', #34439, #32941 ) ;
#1829=CARTESIAN_POINT ( 'NONE',  ( -0.6971942568897626646, -0.07405724077823297447, 0.5561023621509617598 ) ) ;
#1832=CYLINDRICAL_SURFACE ( 'NONE', #7128, 0.1574803149606299191 ) ;
#1834=CARTESIAN_POINT ( 'NONE',  ( -0.9500414927467378812, 0.1787899950787401604, 1.058070866087969186 ) ) ;
#1836=CARTESIAN_POINT ( 'NONE',  ( -0.6971942568897648851, 0.07405724077823318263, 0.9842519684501743749 ) ) ;
#1838=CARTESIAN_POINT ( 'NONE',  ( -1.054774247047244540, 0.07405724077823318263, 0.6594488188438737408 ) ) ;
#1840=EDGE_CURVE ( 'NONE', #13298, #37374, #35390, .T. ) ;
#1842=CARTESIAN_POINT ( 'NONE',  ( 0.8107537697050254399, -0.1574803149606297803, 1.808562992125984481 ) ) ;
#1847=CARTESIAN_POINT ( 'NONE',  ( 0.7185039370078739607, 1.928577636452523993E-17, 0.8169291338582678197 ) ) ;
#1850=CARTESIAN_POINT ( 'NONE',  ( -1.054774247047244096, 0.000000000000000000, 0.5339566928596221063 ) ) ;
#1851=CARTESIAN_POINT ( 'NONE',  ( -0.7185039370078746268, -0.06523048226347956391, 0.3863188976377952000 ) ) ;
#1852=ORIENTED_EDGE ( 'NONE', *, *, #42070, .T. ) ;
#1856=FILL_AREA_STYLE ('',( #14599 ) ) ;
#1858=CARTESIAN_POINT ( 'NONE',  ( 1.033464566929133799, 0.000000000000000000, 0.5610236220472440971 ) ) ;
#1860=CARTESIAN_POINT ( 'NONE',  ( 0.7185039370078739607, 1.928577636452523993E-17, 0.9350393700787401619 ) ) ;
#1861=CARTESIAN_POINT ( 'NONE',  ( -0.8107537697050253289, -0.1574803149606297803, 1.247539369971212508 ) ) ;
#1863=CARTESIAN_POINT ( 'NONE',  ( 0.8019270111902716547, 0.1787899950787401604, 0.07381889758403178958 ) ) ;
#1865=CARTESIAN_POINT ( 'NONE',  ( 0.7185039370078766252, -0.06523048226348168721, 1.754429133750741832 ) ) ;
#1869=CARTESIAN_POINT ( 'NONE',  ( 1.033464566929134687, 0.06523048226347956391, 1.035925196850394192 ) ) ;
#1871=CARTESIAN_POINT ( 'NONE',  ( -0.9300548450171354231, -0.1677133419385780366, 1.989159733827547516 ) ) ;
#1874=CARTESIAN_POINT ( 'NONE',  ( 0.7185039370078746268, -0.06523048226347956391, 0.5733267715460159675 ) ) ;
#1875=CARTESIAN_POINT ( 'NONE',  ( -0.8107537697050254399, -0.1574803149606297803, 1.956200787294048338 ) ) ;
#1876=DIRECTION ( 'NONE',  ( -1.000000000000000000, 0.000000000000000000, 0.000000000000000000 ) ) ;
#1880=AXIS2_PLACEMENT_3D ( 'NONE', #16154, #30324, #19006 ) ;
#1881=DIRECTION ( 'NONE',  ( 1.822029033848725028E-16, 0.000000000000000000, 1.000000000000000000 ) ) ;
#1882=CARTESIAN_POINT ( 'NONE',  ( -1.002407869896990045, 0.1264236179284866091, 1.055610236166708793 ) ) ;
#1883=CARTESIAN_POINT ( 'NONE',  ( 0.6971942568897637749, 2.189545951927499583E-17, 0.8686023621509606496 ) ) ;
#1890=CARTESIAN_POINT ( 'NONE',  ( 1.033464566929134687, -0.06523048226347956391, 1.218011810916095117 ) ) ;
#1891=CARTESIAN_POINT ( 'NONE',  ( -0.7185039370078739607, 1.928577636452523993E-17, 1.870078740049952559 ) ) ;
#1894=CARTESIAN_POINT ( 'NONE',  ( -0.6971942568897648851, 0.07405724077823318263, 1.894685039316315489 ) ) ;
#1895=EDGE_LOOP ( 'NONE', ( #12411, #29985, #27803, #34322 ) ) ;
#1897=CARTESIAN_POINT ( 'NONE',  ( 1.002407869896990045, 0.1264236179284866091, 0.5044291338045039375 ) ) ;
#1898=CARTESIAN_POINT ( 'NONE',  ( -1.054774247047244096, 0.000000000000000000, 1.400098425143086800 ) ) ;
#1899=CARTESIAN_POINT ( 'NONE',  ( -0.7495606340400177148, -0.1264236179284866091, 0.9916338582139527791 ) ) ;
#1900=EDGE_CURVE ( 'NONE', #30530, #3057, #37258, .T. ) ;
#1901=CARTESIAN_POINT ( 'NONE',  ( -0.7495606340400177148, -0.1264236179284866091, 0.1697834645131657827 ) ) ;
#1902=( BOUNDED_CURVE ( )  B_SPLINE_CURVE ( 2, ( #11378, #19011, #7762, #8470, #44878, #788, #26953, #37476, #15452 ),
 .UNSPECIFIED., .F., .T. ) 
 B_SPLINE_CURVE_WITH_KNOTS ( ( 3, 2, 2, 2, 3 ),
 ( 0.7600000000000000089, 0.7624999999999999556, 0.7650000000000000133, 0.7674999999999999600, 0.7700000000000000178 ),
 .UNSPECIFIED. ) 
 CURVE ( )  GEOMETRIC_REPRESENTATION_ITEM ( )  RATIONAL_B_SPLINE_CURVE ( ( 1.000000000000000000, 0.9238795325112869605, 1.000000000000000000, 0.9238795325112869605, 1.000000000000000000, 0.9238795325112869605, 1.000000000000000000, 0.9238795325112869605, 1.000000000000000000 ) ) 
 REPRESENTATION_ITEM ( '' )  ) ;
#1904=CARTESIAN_POINT ( 'NONE',  ( -1.033464566929133799, 0.000000000000000000, 0.5118110235145196807 ) ) ;
#1905=CARTESIAN_POINT ( 'NONE',  ( -0.7495606340400177148, -0.1264236179284866091, 1.744586614119464807 ) ) ;
#1906=CARTESIAN_POINT ( 'NONE',  ( -1.002407869896990045, 0.1264236179284866091, 0.1107283464029293202 ) ) ;
#1907=CARTESIAN_POINT ( 'NONE',  ( 1.033464566929136907, -0.06523048226347749612, 1.414862204616882835 ) ) ;
#1908=CARTESIAN_POINT ( 'NONE',  ( -0.7185039370078739607, 1.928577636452523993E-17, 1.761811023622047223 ) ) ;
#1909=DIRECTION ( 'NONE',  ( 1.000000000000000000, 0.000000000000000000, -1.822029033848725275E-16 ) ) ;
#1910=CARTESIAN_POINT ( 'NONE',  ( 0.8019270111902716547, -0.1787899950787401604, 1.747047244040724312 ) ) ;
#1914=VERTEX_POINT ( 'NONE', #37030 ) ;
#1915=VERTEX_POINT ( 'NONE', #33707 ) ;
#1919=CARTESIAN_POINT ( 'NONE',  ( -0.7185039370078739607, 1.928577636452523993E-17, 0.5807086614173228023 ) ) ;
#1920=CARTESIAN_POINT ( 'NONE',  ( 1.002407869896990045, -0.1264236179284866091, 0.4109251967966299213 ) ) ;
#1923=CARTESIAN_POINT ( 'NONE',  ( -0.8759842519685039353, 0.1574803149606299191, 0.7578740156405039397 ) ) ;
#1926=CARTESIAN_POINT ( 'NONE',  ( 1.002407869896990045, 0.1264236179284866091, 0.9325787401037164415 ) ) ;
#1929=CARTESIAN_POINT ( 'NONE',  ( 1.033464566929134687, -0.06523048226347956391, 0.07627952745152805081 ) ) ;
#1934=CARTESIAN_POINT ( 'NONE',  ( 0.7495606340400177148, -0.1264236179284866091, 0.3666338582139531677 ) ) ;
#1935=CYLINDRICAL_SURFACE ( 'NONE', #4743, 0.1574803149606299191 ) ;
#1936=CARTESIAN_POINT ( 'NONE',  ( -0.8019270111902717657, -0.1787899950787401604, 1.938976377898990799 ) ) ;
#1939=CARTESIAN_POINT ( 'NONE',  ( -0.9500414927467378812, -0.1787899950787401604, 1.515748031442299526 ) ) ;
#1940=FACE_OUTER_BOUND ( 'NONE', #45893, .T. ) ;
#1942=CARTESIAN_POINT ( 'NONE',  ( 0.8759842519685039353, -0.1787899950787401882, 1.395177165300567124 ) ) ;
#1948=CARTESIAN_POINT ( 'NONE',  ( -0.7495606340400177148, 0.1264236179284866091, 0.5536417322297008115 ) ) ;
#1949=CARTESIAN_POINT ( 'NONE',  ( 1.054774247047244540, 0.07405724077823318263, 0.1082677164816695514 ) ) ;
#1950=CARTESIAN_POINT ( 'NONE',  ( -0.6971942568897648851, -0.07405724077823297447, 1.186023621993481658 ) ) ;
#1952=CARTESIAN_POINT ( 'NONE',  ( 0.8019270111902716547, -0.1787899950787401604, 0.5659448818360001132 ) ) ;
#1953=CARTESIAN_POINT ( 'NONE',  ( -0.7495606340400177148, -0.1264236179284866091, 0.5191929133320630774 ) ) ;
#1954=EDGE_CURVE ( 'NONE', #35241, #13693, #27859, .T. ) ;
#1957=CARTESIAN_POINT ( 'NONE',  ( -1.033464566929134687, 0.06523048226347956391, 0.2485236220472441526 ) ) ;
#1958=CARTESIAN_POINT ( 'NONE',  ( 1.002407869896990045, -0.1264236179284866091, 1.321358267662771757 ) ) ;
#1960=ORIENTED_EDGE ( 'NONE', *, *, #29711, .T. ) ;
#1961=EDGE_CURVE ( 'NONE', #23847, #13064, #10940, .T. ) ;
#1962=CARTESIAN_POINT ( 'NONE',  ( 0.8759842519685039353, 0.000000000000000000, 4.498031496062992574 ) ) ;
#1963=CARTESIAN_POINT ( 'NONE',  ( -0.8019270111902717657, -0.1787899950787401604, 0.9990157479777320715 ) ) ;
#1965=CARTESIAN_POINT ( 'NONE',  ( -0.6971942568897637749, 2.189545951927499583E-17, 0.1993110235682838682 ) ) ;
#1967=CARTESIAN_POINT ( 'NONE',  ( -0.8759842519685039353, 0.1574803149606299191, 0.1673228345381423399 ) ) ;
#1971=CARTESIAN_POINT ( 'NONE',  ( 1.002407869896990045, 0.1264236179284866091, 1.365649606245448844 ) ) ;
#1975=CYLINDRICAL_SURFACE ( 'NONE', #2691, 0.1574803149606299191 ) ;
#1976=CARTESIAN_POINT ( 'NONE',  ( 0.8759842519685039353, -0.1787899950787401882, 1.587106299158834721 ) ) ;
#1977=VECTOR ( 'NONE', #17777, 39.37007874015748143 ) ;
#1981=DIRECTION ( 'NONE',  ( 1.822029033848725028E-16, 0.000000000000000000, 1.000000000000000000 ) ) ;
#1982=CARTESIAN_POINT ( 'NONE',  ( 1.054774247047244096, 0.000000000000000000, 0.4945866141194645849 ) ) ;
#1984=CARTESIAN_POINT ( 'NONE',  ( -0.6971942568897637749, 2.189545951927499583E-17, 0.8735236219934803259 ) ) ;
#1988=CARTESIAN_POINT ( 'NONE',  ( -0.9412147342319837628, 0.1574803149606300301, 1.031003936900347639 ) ) ;
#1989=CARTESIAN_POINT ( 'NONE',  ( 0.8019270111902717657, 0.1787899950787401604, 1.535433070812378675 ) ) ;
#1990=CARTESIAN_POINT ( 'NONE',  ( 1.054774247047244540, -0.07405724077823318263, 1.791338582623401177 ) ) ;
#1991=CARTESIAN_POINT ( 'NONE',  ( 0.8759842519685039353, -0.1787899950787401882, 0.3666338582139531677 ) ) ;
#1992=ORIENTED_EDGE ( 'NONE', *, *, #20083, .T. ) ;
#1995=B_SPLINE_CURVE_WITH_KNOTS ( 'NONE', 3,
 ( #2475, #32211, #28634, #2244, #28147, #28384, #42952, #35792, #16864, #2934, #43191, #10160, #6068, #10403, #13060, #42707, #25005, #9925, #20926, #39132, #6547, #24769 ),
 .UNSPECIFIED., .F., .F.,
 ( 4, 2, 2, 2, 2, 2, 2, 2, 2, 2, 4 ),
 ( 0.000000000000000000, 0.06250000000000008327, 0.1250000000000001665, 0.1875000000000002498, 0.2500000000000003331, 0.3750000000000002776, 0.5000000000000002220, 0.6250000000000001110, 0.7500000000000001110, 0.8750000000000000000, 1.000000000000000000 ),
 .UNSPECIFIED. ) ;
#1996=DIRECTION ( 'NONE',  ( 0.000000000000000000, 0.000000000000000000, -1.000000000000000000 ) ) ;
#1999=CARTESIAN_POINT ( 'NONE',  ( -0.9412147342319837628, 0.1574803149606300301, 0.1747047244094490082 ) ) ;
#2000=CARTESIAN_POINT ( 'NONE',  ( 0.9500414927467378812, -0.1787899950787401604, 0.5265748030958428139 ) ) ;
#2001=CARTESIAN_POINT ( 'NONE',  ( 0.7185039370078746268, -0.06523048226347956391, 0.07135826771653554224 ) ) ;
#2003=CARTESIAN_POINT ( 'NONE',  ( 0.7185039370078746268, 0.06523048226347956391, 0.2239173228346459099 ) ) ;
#2004=CARTESIAN_POINT ( 'NONE',  ( -0.8019270111902717657, -0.1787899950787401604, 1.427165354276944687 ) ) ;
#2005=CARTESIAN_POINT ( 'NONE',  ( 0.9412147342319837628, 0.1574803149606300301, 0.8735236219397174429 ) ) ;
#2008=CARTESIAN_POINT ( 'NONE',  ( 0.8759842519685039353, 0.1787899950787401882, 1.021161417269070837 ) ) ;
#2011=CARTESIAN_POINT ( 'NONE',  ( -0.8759842519685039353, 0.1574803149606299191, 0.5610236219397165547 ) ) ;
#2013=CARTESIAN_POINT ( 'NONE',  ( -0.8759842519685039353, 0.1574803149606299191, 1.397637795275590511 ) ) ;
#2015=DIRECTION ( 'NONE',  ( 0.000000000000000000, 0.000000000000000000, -1.000000000000000000 ) ) ;
#2017=CARTESIAN_POINT ( 'NONE',  ( 0.6971942568897626646, 0.07405724077823318263, 0.1624015747493861017 ) ) ;
#2018=CARTESIAN_POINT ( 'NONE',  ( 0.8107537697050253289, 0.1574803149606300301, 1.429625984144440531 ) ) ;
#2021=CARTESIAN_POINT ( 'NONE',  ( -0.8759842519685039353, 0.000000000000000000, 0.000000000000000000 ) ) ;
#2023=CARTESIAN_POINT ( 'NONE',  ( 0.6971942568897626646, 0.07405724077823318263, 0.7135826771115916234 ) ) ;
#2024=CARTESIAN_POINT ( 'NONE',  ( -1.002407869896990045, 0.1264236179284866091, 1.641240157426551161 ) ) ;
#2026=EDGE_LOOP ( 'NONE', ( #6463, #36198, #44216, #7732 ) ) ;
#2035=CARTESIAN_POINT ( 'NONE',  ( -0.8759842519685039353, -0.1574803149606299191, 1.456692913385826849 ) ) ;
#2036=CARTESIAN_POINT ( 'NONE',  ( 1.033464566929134687, -0.06523048226347956391, 1.818405511811023167 ) ) ;
#2038=CARTESIAN_POINT ( 'NONE',  ( -0.6971942568897648851, 0.07405724077823318263, 0.3986220471903311746 ) ) ;
#2039=CARTESIAN_POINT ( 'NONE',  ( -0.7185039370078746268, -0.06523048226347956391, 1.055610236220473341 ) ) ;
#2042=CARTESIAN_POINT ( 'NONE',  ( 0.6971942568897648851, -0.07405724077823297447, 1.072834645615528659 ) ) ;
#2043=CARTESIAN_POINT ( 'NONE',  ( 0.7495606340400177148, -0.1264236179284866091, 0.2042322834108035723 ) ) ;
#2045=ADVANCED_FACE ( 'NONE', ( #29886 ), #21945, .T. ) ;
#2046=CARTESIAN_POINT ( 'NONE',  ( 0.8759842519685039353, -0.1574803149606299191, 1.535433070866141669 ) ) ;
#2047=CARTESIAN_POINT ( 'NONE',  ( 0.8483274250313047604, 0.1565762035813350328, 1.978884771285821742 ) ) ;
#2048=CARTESIAN_POINT ( 'NONE',  ( 0.9412147342319837628, 0.1574803149606300301, 1.710137795275591843 ) ) ;
#2049=CARTESIAN_POINT ( 'NONE',  ( 1.033464566929133799, 0.000000000000000000, 1.456692913278299084 ) ) ;
#2051=CARTESIAN_POINT ( 'NONE',  ( -1.033464566929134687, -0.06523048226347956391, 1.651082677057826853 ) ) ;
#2052=ADVANCED_FACE ( 'NONE', ( #15008 ), #44201, .T. ) ;
#2054=CARTESIAN_POINT ( 'NONE',  ( 0.6971942568897648851, -0.07405724077823297447, 0.9498031495525356416 ) ) ;
#2055=CARTESIAN_POINT ( 'NONE',  ( 0.8759842519685039353, -0.1787899950787401882, 1.946358267662771757 ) ) ;
#2056=CARTESIAN_POINT ( 'NONE',  ( 0.9873396505805591694, -0.1113553986120547346, 0.3887795274515282729 ) ) ;
#2062=CARTESIAN_POINT ( 'NONE',  ( -1.033464566929134687, 0.06523048226347956391, 0.2780511809948349455 ) ) ;
#2064=CARTESIAN_POINT ( 'NONE',  ( 0.6971942568897648851, -0.07405724077823297447, 1.304133858213953667 ) ) ;
#2068=CARTESIAN_POINT ( 'NONE',  ( -1.033464566929133799, 0.000000000000000000, 1.860236220472440971 ) ) ;
#2069=( BOUNDED_CURVE ( )  B_SPLINE_CURVE ( 2, ( #25128, #14583, #3562, #46683, #43801, #3789, #24900, #18406, #17931 ),
 .UNSPECIFIED., .F., .T. ) 
 B_SPLINE_CURVE_WITH_KNOTS ( ( 3, 2, 2, 2, 3 ),
 ( 0.1400000000000000133, 0.1424999999999999878, 0.1449999999999999900, 0.1474999999999999922, 0.1499999999999999944 ),
 .UNSPECIFIED. ) 
 CURVE ( )  GEOMETRIC_REPRESENTATION_ITEM ( )  RATIONAL_B_SPLINE_CURVE ( ( 1.000000000000000000, 0.9238795325112869605, 1.000000000000000000, 0.9238795325112869605, 1.000000000000000000, 0.9238795325112869605, 1.000000000000000000, 0.9238795325112869605, 1.000000000000000000 ) ) 
 REPRESENTATION_ITEM ( '' )  ) ;
#2070=CARTESIAN_POINT ( 'NONE',  ( -1.054774247047244096, 0.000000000000000000, 0.6520669290800944484 ) ) ;
#2071=CARTESIAN_POINT ( 'NONE',  ( -1.033464566929133799, 0.000000000000000000, 0.2854330708661417804 ) ) ;
#2072=LINE ( 'NONE', #13565, #23069 ) ;
#2076=CARTESIAN_POINT ( 'NONE',  ( -0.9500414927467378812, -0.1787899950787401604, 1.043307086560409269 ) ) ;
#2077=CARTESIAN_POINT ( 'NONE',  ( -0.9500414927467378812, -0.1787899950787401604, 1.943897637741510254 ) ) ;
#2080=CARTESIAN_POINT ( 'NONE',  ( 0.7646288533564489232, -0.1113553986120547346, 1.806102362204724532 ) ) ;
#2082=ORIENTED_EDGE ( 'NONE', *, *, #29973, .F. ) ;
#2088=CARTESIAN_POINT ( 'NONE',  ( -0.8019270111902717657, 0.1787899950787401604, 0.5462598424659214080 ) ) ;
#2089=CARTESIAN_POINT ( 'NONE',  ( 0.8759842519685039353, 0.1574803149606299191, 1.348425196742866206 ) ) ;
#2091=CARTESIAN_POINT ( 'NONE',  ( -1.054774247047244540, 0.07405724077823318263, 1.683070866087970074 ) ) ;
#2093=LINE ( 'NONE', #31355, #18026 ) ;
#2096=CARTESIAN_POINT ( 'NONE',  ( 0.9873396505805591694, -0.1113553986120547346, 0.9498031496062993018 ) ) ;
#2097=CARTESIAN_POINT ( 'NONE',  ( -0.9412147342319837628, -0.1574803149606297803, 1.173720472333417586 ) ) ;
#2098=CARTESIAN_POINT ( 'NONE',  ( 0.9500414927467378812, -0.1787899950787401604, 0.6496062991588353874 ) ) ;
#2104=CARTESIAN_POINT ( 'NONE',  ( -0.8759842519685039353, -0.1787899950787401882, 1.080216535379306952 ) ) ;
#2105=CARTESIAN_POINT ( 'NONE',  ( 0.9873396505805591694, 0.1113553986120547346, 1.038385826771653475 ) ) ;
#2110=DIRECTION ( 'NONE',  ( 1.000000000000000000, 0.000000000000000000, -1.822029033848725275E-16 ) ) ;
#2113=LINE ( 'NONE', #5940, #4706 ) ;
#2114=ORIENTED_EDGE ( 'NONE', *, *, #26641, .T. ) ;
#2115=CARTESIAN_POINT ( 'NONE',  ( 0.8759842519685039353, 0.1574803149606299191, 1.161417322834645605 ) ) ;
#2116=CARTESIAN_POINT ( 'NONE',  ( 0.7495606340400177148, -0.1264236179284866091, 0.7554133857730077617 ) ) ;
#2118=VERTEX_POINT ( 'NONE', #8978 ) ;
#2119=CARTESIAN_POINT ( 'NONE',  ( 0.7185039370078739607, 1.928577636452523993E-17, 1.525590551181102317 ) ) ;
#2120=CARTESIAN_POINT ( 'NONE',  ( -0.7185039370078739607, 1.928577636452523993E-17, 0.5413385826771653919 ) ) ;
#2124=CARTESIAN_POINT ( 'NONE',  ( 1.033464566929134687, -0.06523048226347956391, 1.257381889656253193 ) ) ;
#2126=VECTOR ( 'NONE', #1756, 39.37007874015748143 ) ;
#2128=CARTESIAN_POINT ( 'NONE',  ( -1.054774247047244540, -0.07405724077823318263, 1.874999999946236784 ) ) ;
#2129=CARTESIAN_POINT ( 'NONE',  ( 0.9500414927467378812, 0.1787899950787401604, 1.845472440891119392 ) ) ;
#2132=CARTESIAN_POINT ( 'NONE',  ( -0.8759842519685039353, -0.1787899950787401882, 1.547736220418677089 ) ) ;
#2133=DIRECTION ( 'NONE',  ( 1.000000000000000000, 0.000000000000000000, -1.822029033848725275E-16 ) ) ;
#2134=CARTESIAN_POINT ( 'NONE',  ( -0.6971942568897637749, 2.189545951927499583E-17, 0.9867125983714331028 ) ) ;
#2136=CARTESIAN_POINT ( 'NONE',  ( -1.054774247047244096, 0.000000000000000000, 0.2239173227808822775 ) ) ;
#2138=CARTESIAN_POINT ( 'NONE',  ( -1.054774247047244096, 0.000000000000000000, 1.719980314906866203 ) ) ;
#2140=CARTESIAN_POINT ( 'NONE',  ( -0.8107537697050253289, -0.1574803149606297803, 1.690452755905512916 ) ) ;
#2141=CARTESIAN_POINT ( 'NONE',  ( -0.8759842519685039353, 0.000000000000000000, 0.000000000000000000 ) ) ;
#2143=CARTESIAN_POINT ( 'NONE',  ( 1.054774247047244096, 0.000000000000000000, 1.719980314906866203 ) ) ;
#2149=CARTESIAN_POINT ( 'NONE',  ( -0.8759842519685039353, 0.1787899950787401882, 1.296751968450173154 ) ) ;
#2157=CARTESIAN_POINT ( 'NONE',  ( -0.8107537697050253289, 0.1574803149606300301, 0.8390748030420787096 ) ) ;
#2158=CARTESIAN_POINT ( 'NONE',  ( -0.7185039370078746268, 0.06523048226347956391, 0.6569881889763781180 ) ) ;
#2160=CARTESIAN_POINT ( 'NONE',  ( 0.6971942568897637749, 2.189545951927499583E-17, 0.9867125983714331028 ) ) ;
#2165=CARTESIAN_POINT ( 'NONE',  ( 0.9500414927467378812, -0.1787899950787401604, 1.909448818843873186 ) ) ;
#2166=CARTESIAN_POINT ( 'NONE',  ( 0.7185039370078739607, 1.928577636452523993E-17, 0.1870078740157480324 ) ) ;
#2167=CARTESIAN_POINT ( 'NONE',  ( 0.8759842519685039353, 0.000000000000000000, 4.498031496062992574 ) ) ;
#2170=( BOUNDED_CURVE ( )  B_SPLINE_CURVE ( 2, ( #31566, #46147, #23887, #5903, #16463, #38259, #41824, #24358, #6121 ),
 .UNSPECIFIED., .F., .T. ) 
 B_SPLINE_CURVE_WITH_KNOTS ( ( 3, 2, 2, 2, 3 ),
 ( 0.4899999999999999911, 0.4924999999999999933, 0.4949999999999999956, 0.4974999999999999978, 0.5000000000000000000 ),
 .UNSPECIFIED. ) 
 CURVE ( )  GEOMETRIC_REPRESENTATION_ITEM ( )  RATIONAL_B_SPLINE_CURVE ( ( 1.000000000000000000, 0.9238795325112869605, 1.000000000000000000, 0.9238795325112869605, 1.000000000000000000, 0.9238795325112869605, 1.000000000000000000, 0.9238795325112869605, 1.000000000000000000 ) ) 
 REPRESENTATION_ITEM ( '' )  ) ;
#2171=CARTESIAN_POINT ( 'NONE',  ( -0.8759842519685039353, 0.000000000000000000, 0.000000000000000000 ) ) ;
#2172=CARTESIAN_POINT ( 'NONE',  ( -1.002407869896990045, -0.1264236179284866091, 1.946358267662771757 ) ) ;
#2174=CARTESIAN_POINT ( 'NONE',  ( -1.002407869896990045, -0.1264236179284866091, 1.400098425143086800 ) ) ;
#2175=CARTESIAN_POINT ( 'NONE',  ( 0.6971942568897648851, -0.07405724077823297447, 1.348425196796630976 ) ) ;
#2177=CARTESIAN_POINT ( 'NONE',  ( -1.002407869896990045, 0.1264236179284866091, 0.5831692912848189803 ) ) ;
#2178=CARTESIAN_POINT ( 'NONE',  ( 1.054774247047244096, 0.000000000000000000, 0.06643700782025216411 ) ) ;
#2179=CARTESIAN_POINT ( 'NONE',  ( -1.054774247047244096, 0.000000000000000000, 1.163877952702141672 ) ) ;
#2181=CARTESIAN_POINT ( 'NONE',  ( 0.9500414927467377701, -0.1787899950787401604, 0.6102362204186774219 ) ) ;
#2182=CARTESIAN_POINT ( 'NONE',  ( -1.054774247047244540, -0.07405724077823318263, 0.5314960629383620461 ) ) ;
#2184=AXIS2_PLACEMENT_3D ( 'NONE', #36061, #18327, #37237 ) ;
#2186=ORIENTED_EDGE ( 'NONE', *, *, #13562, .F. ) ;
#2187=CARTESIAN_POINT ( 'NONE',  ( -0.9873396505805591694, -0.1113553986120547346, 0.2411417322834645827 ) ) ;
#2189=CARTESIAN_POINT ( 'NONE',  ( 0.8019270111902716547, 0.1787899950787401604, 1.299212598371434435 ) ) ;
#2193=CARTESIAN_POINT ( 'NONE',  ( -0.6971942568897637749, 2.189545951927499583E-17, 1.031003936954110189 ) ) ;
#2195=( BOUNDED_CURVE ( )  B_SPLINE_CURVE ( 2, ( #39405, #24575, #2981, #17614, #39174, #43241, #21439, #25545, #17374 ),
 .UNSPECIFIED., .F., .T. ) 
 B_SPLINE_CURVE_WITH_KNOTS ( ( 3, 2, 2, 2, 3 ),
 ( 0.9000000000000000222, 0.9024999999999999689, 0.9050000000000000266, 0.9074999999999999734, 0.9100000000000000311 ),
 .UNSPECIFIED. ) 
 CURVE ( )  GEOMETRIC_REPRESENTATION_ITEM ( )  RATIONAL_B_SPLINE_CURVE ( ( 1.000000000000000000, 0.9238795325112869605, 1.000000000000000000, 0.9238795325112869605, 1.000000000000000000, 0.9238795325112869605, 1.000000000000000000, 0.9238795325112829637, 1.000000000000000000 ) ) 
 REPRESENTATION_ITEM ( '' )  ) ;
#2200=CARTESIAN_POINT ( 'NONE',  ( 0.7185039370078739607, 1.928577636452523993E-17, 0.3838582677165354173 ) ) ;
#2201=EDGE_LOOP ( 'NONE', ( #25060, #15373, #39420, #6603 ) ) ;
#2202=CARTESIAN_POINT ( 'NONE',  ( 1.002407869896990045, 0.1264236179284866091, 1.405019684985606476 ) ) ;
#2212=DIRECTION ( 'NONE',  ( 0.000000000000000000, 0.000000000000000000, -1.000000000000000000 ) ) ;
#2213=CARTESIAN_POINT ( 'NONE',  ( 0.6971942568897626646, 0.07405724077823318263, 0.4330708660879683536 ) ) ;
#2214=CARTESIAN_POINT ( 'NONE',  ( -0.8019270111902716547, 0.1787899950787401604, 0.7874015747493863238 ) ) ;
#2215=EDGE_CURVE ( 'NONE', #13663, #4590, #3334, .T. ) ;
#2217=CARTESIAN_POINT ( 'NONE',  ( 0.8759842519685039353, 0.000000000000000000, 1.995570866087968520 ) ) ;
#2219=CARTESIAN_POINT ( 'NONE',  ( 0.7495606340400177148, -0.1264236179284866091, 1.587106299158834721 ) ) ;
#2220=CARTESIAN_POINT ( 'NONE',  ( 0.6971942568897637749, 2.189545951927499583E-17, 1.970964566875370139 ) ) ;
#2222=CARTESIAN_POINT ( 'NONE',  ( 0.6971942568897637749, 2.189545951927499583E-17, 0.3961614172690708924 ) ) ;
#2224=EDGE_CURVE ( 'NONE', #36581, #7779, #22925, .T. ) ;
#2225=CARTESIAN_POINT ( 'NONE',  ( 1.033464566929133799, 0.000000000000000000, 0.8661417321759370402 ) ) ;
#2226=DIRECTION ( 'NONE',  ( -1.000000000000000000, 0.000000000000000000, 0.000000000000000000 ) ) ;
#2231=CARTESIAN_POINT ( 'NONE',  ( 1.054774247047244540, -0.07405724077823318263, 0.4527559054580477249 ) ) ;
#2233=CARTESIAN_POINT ( 'NONE',  ( 0.7947666225829561615, -0.1415185883302085834, 0.03937007183037401215 ) ) ;
#2234=DIRECTION ( 'NONE',  ( 1.822029033848725028E-16, 0.000000000000000000, 1.000000000000000000 ) ) ;
#2235=ORIENTED_EDGE ( 'NONE', *, *, #20610, .T. ) ;
#2236=VECTOR ( 'NONE', #15764, 39.37007874015748143 ) ;
#2237=CARTESIAN_POINT ( 'NONE',  ( 1.054774247047244540, 0.07405724077823318263, 1.053149606245450176 ) ) ;
#2240=CARTESIAN_POINT ( 'NONE',  ( -1.033464566929133799, 0.000000000000000000, 0.5118110235145204578 ) ) ;
#2241=CARTESIAN_POINT ( 'NONE',  ( -1.033464566929134687, -0.06523048226347956391, 1.345964566929133133 ) ) ;
#2242=LINE ( 'NONE', #5611, #32006 ) ;
#2244=CARTESIAN_POINT ( 'NONE',  ( -0.7037739381401700856, 0.04180313491334981812, 0.03937007874015843040 ) ) ;
#2245=CARTESIAN_POINT ( 'NONE',  ( 1.054774247047244096, 0.000000000000000000, 0.1058070865604096300 ) ) ;
#2246=CARTESIAN_POINT ( 'NONE',  ( -1.054774247047244540, 0.07405724077823318263, 0.1427165353793073133 ) ) ;
#2247=CARTESIAN_POINT ( 'NONE',  ( 0.9873396505805591694, -0.1113553986120547346, 1.412401574695621997 ) ) ;
#2253=CARTESIAN_POINT ( 'NONE',  ( -0.6971942568897648851, 0.07405724077823318263, 1.771653543253322249 ) ) ;
#2254=ORIENTED_EDGE ( 'NONE', *, *, #30710, .T. ) ;
#2257=CARTESIAN_POINT ( 'NONE',  ( 0.7646288533564489232, -0.1113553986120547346, 1.599409448711369919 ) ) ;
#2259=ORIENTED_EDGE ( 'NONE', *, *, #27251, .F. ) ;
#2263=CARTESIAN_POINT ( 'NONE',  ( 0.8759842519685039353, 0.1787899950787401882, 1.094980314906866203 ) ) ;
#2264=EDGE_CURVE ( 'NONE', #33124, #758, #10410, .T. ) ;
#2266=LINE ( 'NONE', #20712, #5444 ) ;
#2267=CARTESIAN_POINT ( 'NONE',  ( 1.033464566929134687, 0.06523048226347956391, 1.823326771653542178 ) ) ;
#2271=CARTESIAN_POINT ( 'NONE',  ( -0.6971942568897626646, 0.07405724077823318263, 0.2805118109698587214 ) ) ;
#2272=CARTESIAN_POINT ( 'NONE',  ( -0.9873396505805591694, -0.1113553986120547346, 0.9891732283464568232 ) ) ;
#2273=CYLINDRICAL_SURFACE ( 'NONE', #20992, 0.1574803149606299191 ) ;
#2276=CARTESIAN_POINT ( 'NONE',  ( 1.054774247047244540, 0.07405724077823318263, 1.092519684985605810 ) ) ;
#2277=CARTESIAN_POINT ( 'NONE',  ( 0.6971942568897648851, -0.07405724077823297447, 1.500984251914741829 ) ) ;
#2278=CARTESIAN_POINT ( 'NONE',  ( -0.7185039370078739607, 0.000000000000000000, -2.869337061179095023E-17 ) ) ;
#2279=CARTESIAN_POINT ( 'NONE',  ( 0.9873396505805591694, -0.1113553986120547346, 1.658464566929134021 ) ) ;
#2281=CARTESIAN_POINT ( 'NONE',  ( -0.9412147342319837628, -0.1574803149606297803, 1.104822834645669882 ) ) ;
#2283=CARTESIAN_POINT ( 'NONE',  ( -0.7646288533564489232, 0.1113553986120547346, 1.560039370078740273 ) ) ;
#2284=CARTESIAN_POINT ( 'NONE',  ( 0.7495606340400177148, 0.1264236179284866091, 1.021161417269070837 ) ) ;
#2286=CARTESIAN_POINT ( 'NONE',  ( 0.9412147342319837628, -0.1574803149606297803, 0.2682086613097960370 ) ) ;
#2289=CARTESIAN_POINT ( 'NONE',  ( -0.7185039370078746268, 0.06523048226347956391, 0.2534448817822366751 ) ) ;
#2290=CARTESIAN_POINT ( 'NONE',  ( 0.7495606340400177148, -0.1264236179284866091, 1.267224409395055096 ) ) ;
#2291=FACE_OUTER_BOUND ( 'NONE', #37130, .T. ) ;
#2292=CARTESIAN_POINT ( 'NONE',  ( -1.033464566929134687, 0.06523048226347956391, 0.2780511809948353341 ) ) ;
#2294=VECTOR ( 'NONE', #5738, 39.37007874015748143 ) ;
#2296=ORIENTED_EDGE ( 'NONE', *, *, #17744, .F. ) ;
#2301=CARTESIAN_POINT ( 'NONE',  ( -0.8759842519685039353, 0.1787899950787401882, 1.409940944828126153 ) ) ;
#2304=CARTESIAN_POINT ( 'NONE',  ( -0.6971942568897648851, -0.07405724077823297447, 0.9940944881352130613 ) ) ;
#2305=CARTESIAN_POINT ( 'NONE',  ( -0.8019270111902717657, 0.1787899950787401604, 1.924212598371433325 ) ) ;
#2307=CARTESIAN_POINT ( 'NONE',  ( -0.9500414927467378812, -0.1787899950787401604, 0.6889763778989935750 ) ) ;
#2309=CARTESIAN_POINT ( 'NONE',  ( -0.8759842519685039353, 0.000000000000000000, 0.000000000000000000 ) ) ;
#2313=ORIENTED_EDGE ( 'NONE', *, *, #6559, .F. ) ;
#2316=CARTESIAN_POINT ( 'NONE',  ( -1.002407869896990045, -0.1264236179284866091, 0.6865157479777322935 ) ) ;
#2321=CARTESIAN_POINT ( 'NONE',  ( -0.6971942568897648851, -0.07405724077823297447, 1.702755905458047003 ) ) ;
#2322=VECTOR ( 'NONE', #39942, 39.37007874015748143 ) ;
#2326=CARTESIAN_POINT ( 'NONE',  ( -0.7646288533564489232, -0.1113553986120547346, 0.1820866140657015630 ) ) ;
#2327=CARTESIAN_POINT ( 'NONE',  ( 0.7185039370078746268, 0.06523048226347956391, 0.6569881889763780070 ) ) ;
#2331=CARTESIAN_POINT ( 'NONE',  ( -1.033464566929134687, -0.06523048226347956391, 1.218011810916095117 ) ) ;
#2332=CARTESIAN_POINT ( 'NONE',  ( 0.8019270111902717657, -0.1787899950787401604, 0.6446850393163160442 ) ) ;
#2335=CARTESIAN_POINT ( 'NONE',  ( 1.033464566929133799, 0.000000000000000000, 0.9940944881889764995 ) ) ;
#2336=ORIENTED_EDGE ( 'NONE', *, *, #44618, .F. ) ;
#2338=CARTESIAN_POINT ( 'NONE',  ( 0.7646288533564489232, -0.1113553986120547346, 1.097440944881889813 ) ) ;
#2346=CARTESIAN_POINT ( 'NONE',  ( 0.6971942568897626646, 0.07405724077823318263, 0.8661417322297003674 ) ) ;
#2348=DIRECTION ( 'NONE',  ( 1.822029033848725028E-16, 0.000000000000000000, 1.000000000000000000 ) ) ;
#2352=CARTESIAN_POINT ( 'NONE',  ( -1.033464566929134687, 0.06523048226347956391, 1.852854330601134469 ) ) ;
#2353=ORIENTED_EDGE ( 'NONE', *, *, #25974, .F. ) ;
#2354=CARTESIAN_POINT ( 'NONE',  ( -0.7495606340400177148, 0.1264236179284866091, 1.931594488135212728 ) ) ;
#2356=VERTEX_POINT ( 'NONE', #39746 ) ;
#2359=CARTESIAN_POINT ( 'NONE',  ( -0.6971942568897648851, 0.07405724077823318263, 1.535433070812378675 ) ) ;
#2361=CARTESIAN_POINT ( 'NONE',  ( -0.8019270111902717657, 0.1787899950787401604, 1.018700787347811110 ) ) ;
#2363=CARTESIAN_POINT ( 'NONE',  ( -0.7495606340400177148, 0.1264236179284866091, 1.852854330654897685 ) ) ;
#2365=CARTESIAN_POINT ( 'NONE',  ( -1.033464566929134687, -0.06523048226347956391, 1.700295275590550936 ) ) ;
#2372=CARTESIAN_POINT ( 'NONE',  ( -0.8759842519685039353, 0.1574803149606299191, 0.04921259831766984505 ) ) ;
#2374=ORIENTED_EDGE ( 'NONE', *, *, #36808, .F. ) ;
#2376=EDGE_CURVE ( 'NONE', #19774, #31278, #9778, .T. ) ;
#2380=CARTESIAN_POINT ( 'NONE',  ( -1.033464566929134687, 0.06523048226347956391, 1.537893700679874076 ) ) ;
#2384=CARTESIAN_POINT ( 'NONE',  ( -0.9412147342319837628, -0.1574803149606297803, 0.7406496061916858498 ) ) ;
#2385=CARTESIAN_POINT ( 'NONE',  ( -0.7185039370078746268, 0.06523048226347956391, 0.6963582677165359724 ) ) ;
#2387=VECTOR ( 'NONE', #36112, 39.37007874015748143 ) ;
#2389=CARTESIAN_POINT ( 'NONE',  ( 0.9500414927467378812, -0.1787899950787401604, 0.9202755904974182499 ) ) ;
#2390=AXIS2_PLACEMENT_3D ( 'NONE', #23864, #42522, #1808 ) ;
#2393=CARTESIAN_POINT ( 'NONE',  ( 0.7495606340400177148, -0.1264236179284866091, 1.941437007820252081 ) ) ;
#2396=CARTESIAN_POINT ( 'NONE',  ( -0.8759842519685039353, -0.1574803149606299191, 0.7775590550105826448 ) ) ;
#2401=CARTESIAN_POINT ( 'NONE',  ( 0.8019270111902717657, -0.1787899950787401604, 0.3297244093950552069 ) ) ;
#2402=CARTESIAN_POINT ( 'NONE',  ( -0.8019270111902717657, 0.1787899950787401604, 1.963582677111591401 ) ) ;
#2404=CARTESIAN_POINT ( 'NONE',  ( -0.6971942568897648851, 0.07405724077823318263, 1.500984251914741607 ) ) ;
#2405=CARTESIAN_POINT ( 'NONE',  ( 0.9500414927467378812, -0.1787899950787401604, 1.437007873961985371 ) ) ;
#2408=CARTESIAN_POINT ( 'NONE',  ( -0.6971942568897626646, -0.07405724077823297447, 0.6791338582139527791 ) ) ;
#2409=LINE ( 'NONE', #17041, #30487 ) ;
#2410=CARTESIAN_POINT ( 'NONE',  ( -0.9412147342319837628, 0.1574803149606300301, 1.621555118002709683 ) ) ;
#2411=CARTESIAN_POINT ( 'NONE',  ( 0.9500414927467377701, 0.1787899950787401604, 0.5856299212060785964 ) ) ;
#2412=CARTESIAN_POINT ( 'NONE',  ( -0.9500414927467377701, -0.1787899950787401604, 0.5659448818360001132 ) ) ;
#2416=ORIENTED_EDGE ( 'NONE', *, *, #22181, .F. ) ;
#2417=CARTESIAN_POINT ( 'NONE',  ( -1.054774247047244096, 0.000000000000000000, 1.483759842465921075 ) ) ;
#2419=CARTESIAN_POINT ( 'NONE',  ( -0.9873396505805591694, -0.1113553986120547346, 0.5167322834645668994 ) ) ;
#2420=CARTESIAN_POINT ( 'NONE',  ( 1.054774247047244096, 0.000000000000000000, 1.286909448765133801 ) ) ;
#2423=VECTOR ( 'NONE', #41247, 39.37007874015748143 ) ;
#2427=CARTESIAN_POINT ( 'NONE',  ( -0.7495606340400177148, -0.1264236179284866091, 1.035925196796629866 ) ) ;
#2430=VERTEX_POINT ( 'NONE', #44529 ) ;
#2432=CARTESIAN_POINT ( 'NONE',  ( 0.8759842519685039353, -0.1787899950787401882, 1.390255905458047447 ) ) ;
#2436=DIRECTION ( 'NONE',  ( 0.000000000000000000, 0.000000000000000000, -1.000000000000000000 ) ) ;
#2437=CARTESIAN_POINT ( 'NONE',  ( -1.033464566929134687, -0.06523048226347956391, 0.9817913384751512096 ) ) ;
#2441=CARTESIAN_POINT ( 'NONE',  ( 0.7495606340400177148, 0.1264236179284866091, 0.4306102361667086820 ) ) ;
#2442=( BOUNDED_SURFACE ( )  B_SPLINE_SURFACE ( 1, 2, ( 
 ( #7254, #10389, #28367, #21634, #21876, #31961, #25488, #6770, #7007, #7475, #17799, #29105, #2923, #14449, #43660, #28620, #40054, #36268, #36496, #47024, #18035, #14684, #22094, #24994, #32681, #17558, #3652, #39589, #18273, #3169, #39351, #32196, #10627, #42936, #32916, #25721, #13970, #40290, #14219, #36721, #43180, #32446, #21146, #3883, #28860, #46546, #24755, #43419, #21387, #10146, #6532, #36012, #25230, #47270, #39818, #18730, #23043, #33621, #22326, #34090, #4328, #26186, #736, #37410, #44354, #1220, #15398, #23289, #37184, #8415, #33390, #506, #980, #15163, #29807, #30042, #36954, #37903, #18502, #37661, #18961, #15872, #4817, #4111, #33159, #22802, #11562, #44587, #44827, #280, #40754, #14925, #7950, #11329, #19202, #15638, #8651, #11804, #26423, #30275, #25941, #40991, #22569, #12040, #19440, #30499, #26662, #41210, #8177, #45059, #4568, #33861, #12273, #7711, #26894, #41451, #29590, #44131, #40521, #19678, #46249, #16344, #35022, #2401, #13448, #9381, #5998, #16793, #20618, #12755, #41929, #5060, #30734, #23752, #34794, #16568, #9135, #28077, #1934, #42639, #13220, #9849, #31200, #45771, #27620, #10551, #21798, #32607, #17718, #29274, #15089, #25865, #199, #25150, #22249, #29022, #32368, #25639, #4036, #3093, #44056, #39982, #11021, #11481, #36423, #33072, #39740, #14845, #33313, #47195, #437, #22021, #29736, #44278, #3581, #43822, #21550, #26103, #3807, #40675, #7873, #14138, #6927, #18199, #47434, #36188, #17949, #40911, #33789, #19607, #4987, #26351, #8821, #23456, #45222, #22970, #11732, #4255, #905, #22488, #19842, #30206, #1377, #27066, #29968, #8344, #37107, #12195, #37578, #16035, #12444, #4739, #15314, #19365, #34020, #22731, #1145, #5214, #1620, #37337, #15803, #37830, #8578, #38059, #4487, #34471, #16270, #30662, #15567, #30902, #27309, #30431, #45459, #44984, #41378, #26821, #12684, #33545, #19125, #41859, #18890, #661, #44515, #23216, #38532, #23925, #5462, #20314, #31828, #20077, #10009, #2332, #6157, #2098, #28476, #34723, #20779, #38292, #2559, #31364, #42793, #46414, #28230, #9063, #39222, #21009, #17423, #32060, #46648, #24858, #10739, #33019, #15038, #11204, #32310, #25817, #28967, #3277, #25347, #14550, #21490, #40393, #39930, #386, #14322, #142, #10494, #25092, #25589, #39683, #43294, #7117, #14078, #43045, #10253, #14794, #43524, #7582, #29456, #28725, #39458, #47378, #36122, #21741, #21972, #6634, #46889, #21254, #6869, #35878, #43767, #40161, #33262, #36372, #3527, #7360, #3031, #18140, #17901, #36597, #44002, #22195, #3754, #18377, #32784, #36832, #29222, #10970, #32549, #47137, #3982, #18601, #17662, #19550, #41090, #44229, #41554, #33492, #1090, #27010, #8763, #19313, #1324, #33965, #34197, #22679, #26299, #1560, #29687, #846, #44691, #8287, #26051, #15982, #11432, #30603, #30382, #19782, #37280, #4435, #19067, #37056, #15506, #11907, #15748, #45167, #34417, #8052, #44928, #608, #12389, #33736, #23399, #30150, #4207, #15265, #22913, #40624, #4927, #23155, #44460, #38003, #26531, #5164, #11675, #37527, #18837, #7818, #4683, #22434, #29912, #12142, #40857, #26766, #41323, #8525, #37770, #16902, #16446, #31074, #20720, #31304, #20018, #2508, #17132, #38933, #16675, #5395, #45413, #9244, #16215, #13540, #23863, #13320, #35363, #23626, #20255, #30846, #5885, #45883, #46122, #6095, #34902, #9003, #13095, #2042, #34658, #27728, #46356, #42735, #1807, #42290, #31542, #2276, #31775, #45639, #28174, #9950, #27951, #5644, #24559, #20951, #9488, #39162, #24108, #35130, #20492, #6334, #27249, #12857, #35596, #42518, #41803, #12626, #38715, #27491, #38237, #9721, #24335, #10913, #46590, #3698, #21428, #39627, #43227, #7520, #28411, #32488, #31998, #43465, #24798, #36539, #17842, #13770, #22141, #25536, #32959, #10432, #36055, #47317, #42982, #47070, #40104, #10190, #18321, #39391, #46826, #35820, #10670, #29401, #7298, #14492, #2967, #21918, #25032, #32245, #39866, #81, #14014, #43707, #3213, #25278, #25762, #14262, #29152, #28904, #32725, #14729, #7055, #43946, #21681, #11143, #40332, #36311, #3466, #18077, #1032, #44632, #19253, #1269, #26710, #26945, #37233, #33435, #22621, #41501, #7758, #550, #15689, #30326, #40567, #8705, #41265, #7996, #15921, #8465, #22376, #3927, #41036, #15207, #15446, #44873, #18547, #36999, #33204, #4155, #29632, #37472, #12086, #36767, #4378, #19007, #23094, #44171, #8230, #29858, #37713, #4865, #19493, #45111, #12330, #22855, #327, #33671, #4619, #44398, #25985, #784, #18781, #14977, #11373, #11614, #26235, #40801, #27193, #42231, #20669, #35311, #13035, #42464, #27671, #27901, #16394, #19960, #42683, #23342, #41979, #38418, #34844, #19726, #9668, #5102, #24284, #24053, #13493, #31015, #45581, #12803, #30788, #9185, #5588, #9434, #38879, #28124, #1751, #38656, #41746, #6042, #27437, #2449, #23802, #45355, #8951, #1989, #34363, #46066, #16839, #38177, #17076, #20195, #31716, #5339, #16618, #12567, #46305, #31247, #37954, #16156, #45824, #34600, #5829, #1501, #20436, #35070, #2219, #23571, #31479, #13270, #24983, #13719, #25474, #43171, #17548, #39578, #28847, #35771, #40044, #6756, #14674, #28609, #47259, #24744, #39339, #39808, #6519, #10135, #21378, #28356, #29346, #7242, #10376, #32186, #36003, #43408, #2913, #21863, #3161, #9898, #17788, #14439, #21136, #46772, #6996, #13958, #32435, #47012, #42924, #24510, #39107, #29093, #14207, #36488, #43651, #10618, #6281, #25217, #21623, #36256, #3408, #20904, #18024, #35544, #32670, #2687, #10859, #3643, #24, #18261, #32907, #17314, #31952, #4320, #40514, #40982, #15631, #12031, #4560, #22797, #18953, #19193, #29799, #30035, #22317, #33145, #26176, #270, #44819, #33853, #7942, #11090, #8409, #14913, #15389, #41203, #23037, #33613, #30268, #727, #972, #36946, #7703, #15865, #43890, #15155, #11554, #22558, #40280, #26656, #25709, #37652, #44578, #34084, #4100, #18722, #33380, #3874, #40744, #37176, #11798, #4807, #1214, #497, #26415, #29576, #19433, #8169, #7467, #37403, #18492, #44121, #22087, #36711, #11320, #25933, #45296, #2165, #12749, #46010, #12513, #16337, #19672, #9613, #27379, #13213, #23282, #41922, #27137, #12976, #2393, #41687, #8891, #31193, #30727, #23523, #35014, #45525, #34314, #5287, #19905, #37896, #1689, #9130, #34788, #27848, #20612, #38128, #16560, #1443, #16789, #34535, #31427 ),
 ( #35260, #16103, #30959, #27612, #42167, #23745, #42411, #24232, #5770, #38356, #5528, #12264, #20142, #30491, #38829, #1929, #9373, #5991, #5053, #45764, #45051, #23996, #38594, #20376, #26887, #41443, #8644, #32123, #2854, #20847, #35718, #47205, #43593, #35489, #46712, #32378, #3103, #3352, #2628, #17961, #29033, #46959, #10075, #10804, #21808, #24689, #14385, #28547, #35944, #6700, #21561, #28072, #17260, #6939, #14148, #42633, #17027, #39287, #46481, #39053, #13441, #24453, #25162, #9844, #32617, #21079, #6462, #42861, #36433, #6223, #13900, #31664, #10319, #31899, #25417, #43113, #46240, #13661, #39750, #39991, #17492, #24930, #28791, #28299, #39523, #36197, #21315, #7183, #17729, #43356, #10562, #1818, #38486, #2286, #24348, #12638, #20265, #5176, #38726, #27262, #5894, #5409, #41571, #19794, #12870, #30617, #9500, #27740, #1574, #20506, #16455, #16916, #16226, #20030, #23411, #13333, #31088, #31555, #27022, #45652, #30858, #16690, #6111, #45421, #41814, #34913, #34428, #9015, #35143, #27503, #38015, #46133, #34671, #23637, #42054, #5656, #38248, #27962, #9255, #38945, #23875, #24121, #2056, #31317, #45892, #13109, #42306, #42529, #9731, #1338, #15994, #45181, #12402, #8776, #39882, #39176, #35376, #25044, #46605, #46839, #47082, #2520, #24577, #17146, #6349, #13553, #21441, #17856, #10925, #6589, #35837, #32498, #28189, #28676, #17376, #14276, #7066, #36326, #28915, #43478, #43244, #10686, #21203, #6822, #13784, #9966, #2983, #20963, #21694, #25293, #32261, #31790, #32738, #35609, #39640, #18092, #47333, #10446, #3480, #36069, #14504, #28430, #32013, #40117, #20735, #39407, #17615, #14029, #46372, #29166, #42748, #43720, #3224, #25547, #42995, #10205, #24809, #2750, #26000, #22388, #19023, #97, #15221, #3939, #4393, #26485, #22872, #15463, #33687, #29869, #30113, #40581, #40811, #33219, #43959, #37015, #11158, #8246, #44644, #18793, #21931, #19267, #25775, #26248, #4637, #33922, #44411, #41048, #11629, #11861, #343, #18562, #26725, #7312, #7772, #4169, #33449, #3712, #37484, #36551, #1047, #8007, #44888, #14992, #29644, #44185, #14744, #565, #22636, #37241, #15704, #12101, #11387, #798, #40347, #30339, #18335, #32973, #29415, #7538, #22150, #36783, #37728, #16631, #34859, #8720, #13049, #23583, #9451, #23356, #27210, #30564, #20450, #38192, #24065, #34154, #5353, #37966, #23815, #13907, #5116, #19740, #41993, #41515, #34377, #45840, #8963, #45126, #38674, #41760, #1516, #19976, #12818, #16169, #5842, #34615, #46721, #12584, #31262, #30803, #45369, #38434, #1764, #16405, #31031, #12342, #41280, #8480, #27685, #45598, #35726, #42247, #26962, #23114, #27450, #9197, #5601, #20208, #4882, #2005, #19506, #2862, #1282, #17498, #32129, #15938, #14393, #43601, #47453, #6948, #11273, #25425, #33333, #47212, #18447, #43363, #10571, #11044, #25172, #28799, #39999, #46966, #456, #28553, #33096, #29042, #25887, #217, #14155, #43122, #32859, #21569, #7192, #7424, #10326, #32385, #24938, #39756, #21323, #29295, #25660, #18673, #10813, #21817, #40236, #35954, #36445, #36207, #22043, #14867, #44077, #36668, #3826, #3597, #29526, #18218, #14626, #3359, #17735, #43843, #17971, #40468, #7651, #22268, #39531, #36904, #32625, #4058, #6710, #3112, #4765, #34270, #19392, #19629, #8128, #11752, #34494, #15109, #33813, #30225, #26611, #11505, #1401, #44302, #16060, #15827, #5243, #22751, #37358, #4510, #22511, #929, #44772, #34043, #30687, #19869, #40932, #1168, #33567, #45251, #19146, #12471, #15587, #37127, #684, #41164, #26127, #37855, #8602, #29992, #27092, #11988, #41643, #44536, #8367, #4276, #8847, #22993, #23484, #7893, #37605, #26373, #45008, #29755, #30452, #12221, #26844, #15339, #41405, #38085, #23242, #18910, #40697, #5010, #38560, #17222, #39244, #5725, #35214, #1890, #6181, #20341, #20805, #34979, #9089, #16525, #27814, #27337, #46435, #42592, #31154, #13615, #9572, #28256, #45723, #2124, #5489, #10030, #38793, #24651, #23708, #16985, #16754, #31624, #21035, #46204, #13403, #28033, #9805, #6418, #1649, #16293, #7839, #26552, #11643, #8021, #814, #15477, #41063, #12115, #22884, #7549, #30355, #41293, #26017, #40594, #23127, #22159, #16185, #12830, #34390, #20695, #35338, #5858, #34628, #13296, #35100, #1530, #30576, #20223, #41773, #42008, #42263, #45139, #19758, #12357, #30815, #8734, #16647, #13063, #6071, #1777, #31044, #27701, #23370, #23833, #12599, #9463, #2247, #31511, #24081, #38689, #38446, #20465, #16417, #2018, #8975, #5130, #45612, #45384, #16867, #46092, #27461, #26975, #27924, #27221, #34872, #42488, #9694, #5616, #24308, #31276, #38909, #23594, #38208, #15954, #41528, #9211, #45854, #37978, #5369, #19988, #31746, #21652, #3189, #40073, #42955, #24771, #39369, #9929, #21163, #17575, #6784, #2479, #39607, #2938, #32465, #25248, #35795, #42711, #32216, #46803, #6305, #13988, #32696, #29123, #20928, #28638, #17818, #36028, #36285, #35569, #3437, #14464, #47043, #10163, #43675, #7273, #6551, #47286, #43196, #21403, #14235, #7027, #13517, #2714, #39836, #28877, #28150, #17104, #10407, #31976, #24536, #46333, #39136, #10643, #17341, #18050, #25009, #43435, #28386, #21891, #46561, #10885, #13745, #25505, #43914, #30058, #40536, #3667, #4583, #37197, #44600, #295, #44146, #7965, #52, #25956, #4341, #36512, #41003, #36737, #14942, #25736, #22584, #14700, #22815, #8192, #29604, #37430, #4123, #3895, #33637, #22110, #11345, #22342, #36970, #33405, #15180, #18974, #29024, #35709, #14377, #43582, #28537, #10796, #21552, #25408, #29278, #3095, #39742, #17482, #39984, #6929, #7175, #43824, #21801, #22023, #32370, #43104, #17722, #36649, #2846, #10311, #36426, #3582, #32116, #18201, #32842, #47437, #46948, #21072, #13656, #24923, #31892, #11024, #39515, #14605, #25642, #39280, #35935, #40217, #28293, #7407, #14142, #21307, #6690, #3809, #10066, #28783, #46472, #25152, #6455, #42855, #43349, #24683, #46703, #13893, #10553, #36189, #3345, #17953, #32609, #47197, #8348, #37833, #34024, #7637, #15092, #201, #11735, #44988, #41145, #30210, #11257, #22974, #44281, #14849, #8111, #37582, #18425, #11972, #40682, #40915, #41381, #4259, #15571, #22252, #909, #44755, #29739, #26593, #22734, #4744, #15806, #37112, #26354, #4039, #19370, #37339, #1150, #30434, #12198, #8582, #18893, #11485, #33548, #23220, #36886, #26107, #26825 ) ),
 .UNSPECIFIED., .F., .F., .T. ) 
 B_SPLINE_SURFACE_WITH_KNOTS ( ( 2, 2 ),
 ( 3, 2, 2, 2, 2, 2, 2, 2, 2, 2, 2, 2, 2, 2, 2, 2, 2, 2, 2, 2, 2, 2, 2, 2, 2, 2, 2, 2, 2, 2, 2, 2, 2, 2, 2, 2, 2, 2, 2, 2, 2, 2, 2, 2, 2, 2, 2, 2, 2, 2, 2, 2, 2, 2, 2, 2, 2, 2, 2, 2, 2, 2, 2, 2, 2, 2, 2, 2, 2, 2, 2, 2, 2, 2, 2, 2, 2, 2, 2, 2, 2, 2, 2, 2, 2, 2, 2, 2, 2, 2, 2, 2, 2, 2, 2, 2, 2, 2, 2, 2, 2, 2, 2, 2, 2, 2, 2, 2, 2, 2, 2, 2, 2, 2, 2, 2, 2, 2, 2, 2, 2, 2, 2, 2, 2, 2, 2, 2, 2, 2, 2, 2, 2, 2, 2, 2, 2, 2, 2, 2, 2, 2, 2, 2, 2, 2, 2, 2, 2, 2, 2, 2, 2, 2, 2, 2, 2, 2, 2, 2, 2, 2, 2, 2, 2, 2, 2, 2, 2, 2, 2, 2, 2, 2, 2, 2, 2, 2, 2, 2, 2, 2, 2, 2, 2, 2, 2, 2, 2, 2, 2, 2, 2, 2, 2, 2, 2, 2, 2, 2, 2, 2, 2, 2, 2, 2, 2, 2, 2, 2, 2, 2, 2, 2, 2, 2, 2, 2, 2, 2, 2, 2, 2, 2, 2, 2, 2, 2, 2, 2, 2, 2, 2, 2, 2, 2, 2, 2, 2, 2, 2, 2, 2, 2, 2, 2, 2, 2, 2, 2, 2, 2, 2, 2, 2, 2, 2, 2, 2, 2, 2, 2, 2, 2, 2, 2, 2, 2, 2, 2, 2, 2, 2, 2, 2, 2, 2, 2, 2, 2, 2, 2, 2, 2, 2, 2, 2, 2, 2, 2, 2, 2, 2, 2, 2, 2, 2, 2, 2, 2, 2, 2, 2, 2, 2, 2, 2, 2, 2, 2, 2, 2, 2, 2, 2, 2, 2, 2, 2, 2, 2, 2, 2, 2, 2, 2, 2, 2, 2, 2, 2, 2, 2, 2, 2, 2, 2, 2, 2, 2, 2, 2, 2, 2, 2, 2, 2, 2, 2, 2, 2, 2, 2, 2, 2, 2, 2, 2, 2, 2, 2, 2, 2, 2, 2, 2, 2, 2, 2, 2, 2, 2, 2, 2, 2, 2, 2, 2, 2, 2, 2, 2, 2, 2, 2, 2, 2, 2, 2, 2, 2, 2, 2, 2, 2, 2, 2, 2, 2, 2, 3 ),
 ( 0.000000000000000000, 1.000000000000000000 ),
 ( 0.000000000000000000, 0.002500000000000000052, 0.005000000000000000104, 0.007499999999999999722, 0.01000000000000000021, 0.01250000000000000069, 0.01499999999999999944, 0.01750000000000000167, 0.02000000000000000042, 0.02249999999999999917, 0.02500000000000000139, 0.02750000000000000014, 0.02999999999999999889, 0.03250000000000000111, 0.03500000000000000333, 0.03749999999999999861, 0.04000000000000000083, 0.04250000000000000305, 0.04499999999999999833, 0.04750000000000000056, 0.05000000000000000278, 0.05249999999999999806, 0.05500000000000000028, 0.05750000000000000250, 0.05999999999999999778, 0.06250000000000000000, 0.06500000000000000222, 0.06750000000000000444, 0.07000000000000000666, 0.07249999999999999500, 0.07499999999999999722, 0.07749999999999999944, 0.08000000000000000167, 0.08250000000000000389, 0.08500000000000000611, 0.08749999999999999445, 0.08999999999999999667, 0.09249999999999999889, 0.09500000000000000111, 0.09750000000000000333, 0.1000000000000000056, 0.1024999999999999939, 0.1049999999999999961, 0.1074999999999999983, 0.1100000000000000006, 0.1125000000000000028, 0.1150000000000000050, 0.1174999999999999933, 0.1199999999999999956, 0.1224999999999999978, 0.1250000000000000000, 0.1275000000000000022, 0.1300000000000000044, 0.1325000000000000067, 0.1350000000000000089, 0.1375000000000000111, 0.1400000000000000133, 0.1424999999999999878, 0.1449999999999999900, 0.1474999999999999922, 0.1499999999999999944, 0.1524999999999999967, 0.1549999999999999989, 0.1575000000000000011, 0.1600000000000000033, 0.1625000000000000056, 0.1650000000000000078, 0.1675000000000000100, 0.1700000000000000122, 0.1724999999999999867, 0.1749999999999999889, 0.1774999999999999911, 0.1799999999999999933, 0.1824999999999999956, 0.1849999999999999978, 0.1875000000000000000, 0.1900000000000000022, 0.1925000000000000044, 0.1950000000000000067, 0.1975000000000000089, 0.2000000000000000111, 0.2025000000000000133, 0.2049999999999999878, 0.2074999999999999900, 0.2099999999999999922, 0.2124999999999999944, 0.2149999999999999967, 0.2174999999999999989, 0.2200000000000000011, 0.2225000000000000033, 0.2250000000000000056, 0.2275000000000000078, 0.2300000000000000100, 0.2325000000000000122, 0.2349999999999999867, 0.2374999999999999889, 0.2399999999999999911, 0.2424999999999999933, 0.2449999999999999956, 0.2474999999999999978, 0.2500000000000000000, 0.2525000000000000022, 0.2550000000000000044, 0.2575000000000000067, 0.2600000000000000089, 0.2625000000000000111, 0.2650000000000000133, 0.2675000000000000155, 0.2700000000000000178, 0.2725000000000000200, 0.2750000000000000222, 0.2775000000000000244, 0.2800000000000000266, 0.2824999999999999734, 0.2849999999999999756, 0.2874999999999999778, 0.2899999999999999800, 0.2924999999999999822, 0.2949999999999999845, 0.2974999999999999867, 0.2999999999999999889, 0.3024999999999999911, 0.3049999999999999933, 0.3074999999999999956, 0.3099999999999999978, 0.3125000000000000000, 0.3150000000000000022, 0.3175000000000000044, 0.3200000000000000067, 0.3225000000000000089, 0.3250000000000000111, 0.3275000000000000133, 0.3300000000000000155, 0.3325000000000000178, 0.3350000000000000200, 0.3375000000000000222, 0.3400000000000000244, 0.3425000000000000266, 0.3449999999999999734, 0.3474999999999999756, 0.3499999999999999778, 0.3524999999999999800, 0.3549999999999999822, 0.3574999999999999845, 0.3599999999999999867, 0.3624999999999999889, 0.3649999999999999911, 0.3674999999999999933, 0.3699999999999999956, 0.3724999999999999978, 0.3750000000000000000, 0.3775000000000000022, 0.3800000000000000044, 0.3825000000000000067, 0.3850000000000000089, 0.3875000000000000111, 0.3900000000000000133, 0.3925000000000000155, 0.3950000000000000178, 0.3975000000000000200, 0.4000000000000000222, 0.4025000000000000244, 0.4050000000000000266, 0.4074999999999999734, 0.4099999999999999756, 0.4124999999999999778, 0.4149999999999999800, 0.4174999999999999822, 0.4199999999999999845, 0.4224999999999999867, 0.4249999999999999889, 0.4274999999999999911, 0.4299999999999999933, 0.4324999999999999956, 0.4349999999999999978, 0.4375000000000000000, 0.4400000000000000022, 0.4425000000000000044, 0.4450000000000000067, 0.4475000000000000089, 0.4500000000000000111, 0.4525000000000000133, 0.4550000000000000155, 0.4575000000000000178, 0.4600000000000000200, 0.4625000000000000222, 0.4650000000000000244, 0.4675000000000000266, 0.4699999999999999734, 0.4724999999999999756, 0.4749999999999999778, 0.4774999999999999800, 0.4799999999999999822, 0.4824999999999999845, 0.4849999999999999867, 0.4874999999999999889, 0.4899999999999999911, 0.4924999999999999933, 0.4949999999999999956, 0.4974999999999999978, 0.5000000000000000000, 0.5024999999999999467, 0.5050000000000000044, 0.5074999999999999512, 0.5100000000000000089, 0.5124999999999999556, 0.5150000000000000133, 0.5174999999999999600, 0.5200000000000000178, 0.5224999999999999645, 0.5250000000000000222, 0.5274999999999999689, 0.5300000000000000266, 0.5324999999999999734, 0.5350000000000000311, 0.5374999999999999778, 0.5400000000000000355, 0.5424999999999999822, 0.5450000000000000400, 0.5474999999999999867, 0.5500000000000000444, 0.5524999999999999911, 0.5550000000000000488, 0.5574999999999999956, 0.5600000000000000533, 0.5625000000000000000, 0.5649999999999999467, 0.5675000000000000044, 0.5699999999999999512, 0.5725000000000000089, 0.5749999999999999556, 0.5775000000000000133, 0.5799999999999999600, 0.5825000000000000178, 0.5849999999999999645, 0.5875000000000000222, 0.5899999999999999689, 0.5925000000000000266, 0.5949999999999999734, 0.5975000000000000311, 0.5999999999999999778, 0.6025000000000000355, 0.6049999999999999822, 0.6075000000000000400, 0.6099999999999999867, 0.6125000000000000444, 0.6149999999999999911, 0.6175000000000000488, 0.6199999999999999956, 0.6225000000000000533, 0.6250000000000000000, 0.6274999999999999467, 0.6300000000000000044, 0.6324999999999999512, 0.6350000000000000089, 0.6374999999999999556, 0.6400000000000000133, 0.6424999999999999600, 0.6450000000000000178, 0.6474999999999999645, 0.6500000000000000222, 0.6524999999999999689, 0.6550000000000000266, 0.6574999999999999734, 0.6600000000000000311, 0.6624999999999999778, 0.6650000000000000355, 0.6674999999999999822, 0.6700000000000000400, 0.6724999999999999867, 0.6750000000000000444, 0.6774999999999999911, 0.6800000000000000488, 0.6824999999999999956, 0.6850000000000000533, 0.6875000000000000000, 0.6899999999999999467, 0.6925000000000000044, 0.6949999999999999512, 0.6975000000000000089, 0.6999999999999999556, 0.7025000000000000133, 0.7049999999999999600, 0.7075000000000000178, 0.7099999999999999645, 0.7125000000000000222, 0.7149999999999999689, 0.7175000000000000266, 0.7199999999999999734, 0.7225000000000000311, 0.7249999999999999778, 0.7275000000000000355, 0.7299999999999999822, 0.7325000000000000400, 0.7349999999999999867, 0.7375000000000000444, 0.7399999999999999911, 0.7425000000000000488, 0.7449999999999999956, 0.7475000000000000533, 0.7500000000000000000, 0.7524999999999999467, 0.7550000000000000044, 0.7574999999999999512, 0.7600000000000000089, 0.7624999999999999556, 0.7650000000000000133, 0.7674999999999999600, 0.7700000000000000178, 0.7724999999999999645, 0.7750000000000000222, 0.7774999999999999689, 0.7800000000000000266, 0.7824999999999999734, 0.7850000000000000311, 0.7874999999999999778, 0.7900000000000000355, 0.7924999999999999822, 0.7950000000000000400, 0.7974999999999999867, 0.8000000000000000444, 0.8024999999999999911, 0.8050000000000000488, 0.8074999999999999956, 0.8100000000000000533, 0.8125000000000000000, 0.8149999999999999467, 0.8175000000000000044, 0.8199999999999999512, 0.8225000000000000089, 0.8249999999999999556, 0.8275000000000000133, 0.8299999999999999600, 0.8325000000000000178, 0.8349999999999999645, 0.8375000000000000222, 0.8399999999999999689, 0.8425000000000000266, 0.8449999999999999734, 0.8475000000000000311, 0.8499999999999999778, 0.8525000000000000355, 0.8549999999999999822, 0.8575000000000000400, 0.8599999999999999867, 0.8625000000000000444, 0.8649999999999999911, 0.8675000000000000488, 0.8699999999999999956, 0.8725000000000000533, 0.8750000000000000000, 0.8774999999999999467, 0.8800000000000000044, 0.8824999999999999512, 0.8850000000000000089, 0.8874999999999999556, 0.8900000000000000133, 0.8924999999999999600, 0.8950000000000000178, 0.8974999999999999645, 0.9000000000000000222, 0.9024999999999999689, 0.9050000000000000266, 0.9074999999999999734, 0.9100000000000000311, 0.9124999999999999778, 0.9150000000000000355, 0.9174999999999999822, 0.9200000000000000400, 0.9224999999999999867, 0.9250000000000000444, 0.9274999999999999911, 0.9300000000000000488, 0.9324999999999999956, 0.9350000000000000533, 0.9375000000000000000, 0.9399999999999999467, 0.9425000000000000044, 0.9449999999999999512, 0.9475000000000000089, 0.9499999999999999556, 0.9525000000000000133, 0.9549999999999999600, 0.9575000000000000178, 0.9599999999999999645, 0.9625000000000000222, 0.9649999999999999689, 0.9675000000000000266, 0.9699999999999999734, 0.9725000000000000311, 0.9749999999999999778, 0.9775000000000000355, 0.9799999999999999822, 0.9825000000000000400, 0.9849999999999999867, 0.9875000000000000444, 0.9899999999999999911, 0.9925000000000000488, 0.9949999999999999956, 0.9975000000000000533, 1.000000000000000000 ),
 .UNSPECIFIED. ) 
 GEOMETRIC_REPRESENTATION_ITEM ( )  RATIONAL_B_SPLINE_SURFACE ( (
 ( 1.000000000000000000, 0.9238795325112869605, 1.000000000000000000, 0.9238795325112869605, 1.000000000000000000, 0.9238795325112869605, 1.000000000000000000, 0.9238795325112869605, 1.000000000000000000, 0.9238795325112869605, 1.000000000000000000, 0.9238795325112869605, 1.000000000000000000, 0.9238795325112869605, 1.000000000000000000, 0.9238795325112869605, 1.000000000000000000, 0.9238795325112869605, 1.000000000000000000, 0.9238795325112869605, 1.000000000000000000, 0.9238795325112869605, 1.000000000000000000, 0.9238795325112869605, 1.000000000000000000, 0.9238795325112869605, 1.000000000000000000, 0.9238795325112869605, 1.000000000000000000, 0.9238795325112869605, 1.000000000000000000, 0.9238795325112869605, 1.000000000000000000, 0.9238795325112869605, 1.000000000000000000, 0.9238795325112869605, 1.000000000000000000, 0.9238795325112869605, 1.000000000000000000, 0.9238795325112869605, 1.000000000000000000, 0.9238795325112869605, 1.000000000000000000, 0.9238795325112869605, 1.000000000000000000, 0.9238795325112869605, 1.000000000000000000, 0.9238795325112869605, 1.000000000000000000, 0.9238795325112869605, 1.000000000000000000, 0.9238795325112869605, 1.000000000000000000, 0.9238795325112869605, 1.000000000000000000, 0.9238795325112869605, 1.000000000000000000, 0.9238795325112869605, 1.000000000000000000, 0.9238795325112869605, 1.000000000000000000, 0.9238795325112869605, 1.000000000000000000, 0.9238795325112869605, 1.000000000000000000, 0.9238795325112869605, 1.000000000000000000, 0.9238795325112869605, 1.000000000000000000, 0.9238795325112869605, 1.000000000000000000, 0.9238795325112869605, 1.000000000000000000, 0.9238795325112869605, 1.000000000000000000, 0.9238795325112869605, 1.000000000000000000, 0.9238795325112869605, 1.000000000000000000, 0.9238795325112869605, 1.000000000000000000, 0.9238795325112869605, 1.000000000000000000, 0.9238795325112869605, 1.000000000000000000, 0.9238795325112869605, 1.000000000000000000, 0.9238795325112869605, 1.000000000000000000, 0.9238795325112869605, 1.000000000000000000, 0.9238795325112869605, 1.000000000000000000, 0.9238795325112869605, 1.000000000000000000, 0.9238795325112869605, 1.000000000000000000, 0.9238795325112869605, 1.000000000000000000, 0.9238795325112869605, 1.000000000000000000, 0.9238795325112869605, 1.000000000000000000, 0.9238795325112869605, 1.000000000000000000, 0.9238795325112869605, 1.000000000000000000, 0.9238795325112869605, 1.000000000000000000, 0.9238795325112869605, 1.000000000000000000, 0.9238795325112869605, 1.000000000000000000, 0.9238795325112869605, 1.000000000000000000, 0.9238795325112869605, 1.000000000000000000, 0.9238795325112869605, 1.000000000000000000, 0.9238795325112869605, 1.000000000000000000, 0.9238795325112869605, 1.000000000000000000, 0.9238795325112869605, 1.000000000000000000, 0.9238795325112869605, 1.000000000000000000, 0.9238795325112869605, 1.000000000000000000, 0.9238795325112869605, 1.000000000000000000, 0.9238795325112869605, 1.000000000000000000, 0.9238795325112869605, 1.000000000000000000, 0.9238795325112869605, 1.000000000000000000, 0.9238795325112869605, 1.000000000000000000, 0.9238795325112869605, 1.000000000000000000, 0.9238795325112869605, 1.000000000000000000, 0.9238795325112869605, 1.000000000000000000, 0.9238795325112869605, 1.000000000000000000, 0.9238795325112869605, 1.000000000000000000, 0.9238795325112869605, 1.000000000000000000, 0.9238795325112869605, 1.000000000000000000, 0.9238795325112869605, 1.000000000000000000, 0.9238795325112869605, 1.000000000000000000, 0.9238795325112869605, 1.000000000000000000, 0.9238795325112869605, 1.000000000000000000, 0.9238795325112869605, 1.000000000000000000, 0.9238795325112869605, 1.000000000000000000, 0.9238795325112869605, 1.000000000000000000, 0.9238795325112869605, 1.000000000000000000, 0.9238795325112869605, 1.000000000000000000, 0.9238795325112869605, 1.000000000000000000, 0.9238795325112869605, 1.000000000000000000, 0.9238795325112869605, 1.000000000000000000, 0.9238795325112869605, 1.000000000000000000, 0.9238795325112869605, 1.000000000000000000, 0.9238795325112869605, 1.000000000000000000, 0.9238795325112869605, 1.000000000000000000, 0.9238795325112869605, 1.000000000000000000, 0.9238795325112869605, 1.000000000000000000, 0.9238795325112869605, 1.000000000000000000, 0.9238795325112869605, 1.000000000000000000, 0.9238795325112869605, 1.000000000000000000, 0.9238795325112869605, 1.000000000000000000, 0.9238795325112869605, 1.000000000000000000, 0.9238795325112869605, 1.000000000000000000, 0.9238795325112869605, 1.000000000000000000, 0.9238795325112869605, 1.000000000000000000, 0.9238795325112869605, 1.000000000000000000, 0.9238795325112869605, 1.000000000000000000, 0.9238795325112869605, 1.000000000000000000, 0.9238795325112869605, 1.000000000000000000, 0.9238795325112869605, 1.000000000000000000, 0.9238795325112869605, 1.000000000000000000, 0.9238795325112869605, 1.000000000000000000, 0.9238795325112869605, 1.000000000000000000, 0.9238795325112869605, 1.000000000000000000, 0.9238795325112869605, 1.000000000000000000, 0.9238795325112869605, 1.000000000000000000, 0.9238795325112869605, 1.000000000000000000, 0.9238795325112869605, 1.000000000000000000, 0.9238795325112869605, 1.000000000000000000, 0.9238795325112869605, 1.000000000000000000, 0.9238795325112869605, 1.000000000000000000, 0.9238795325112869605, 1.000000000000000000, 0.9238795325112869605, 1.000000000000000000, 0.9238795325112869605, 1.000000000000000000, 0.9238795325112869605, 1.000000000000000000, 0.9238795325112869605, 1.000000000000000000, 0.9238795325112869605, 1.000000000000000000, 0.9238795325112869605, 1.000000000000000000, 0.9238795325112869605, 1.000000000000000000, 0.9238795325112869605, 1.000000000000000000, 0.9238795325112869605, 1.000000000000000000, 0.9238795325112869605, 1.000000000000000000, 0.9238795325112869605, 1.000000000000000000, 0.9238795325112869605, 1.000000000000000000, 0.9238795325112869605, 1.000000000000000000, 0.9238795325112869605, 1.000000000000000000, 0.9238795325112869605, 1.000000000000000000, 0.9238795325112869605, 1.000000000000000000, 0.9238795325112869605, 1.000000000000000000, 0.9238795325112869605, 1.000000000000000000, 0.9238795325112869605, 1.000000000000000000, 0.9238795325112869605, 1.000000000000000000, 0.9238795325112869605, 1.000000000000000000, 0.9238795325112869605, 1.000000000000000000, 0.9238795325112869605, 1.000000000000000000, 0.9238795325112869605, 1.000000000000000000, 0.9238795325112869605, 1.000000000000000000, 0.9238795325112869605, 1.000000000000000000, 0.9238795325112869605, 1.000000000000000000, 0.9238795325112869605, 1.000000000000000000, 0.9238795325112869605, 1.000000000000000000, 0.9238795325112869605, 1.000000000000000000, 0.9238795325112869605, 1.000000000000000000, 0.9238795325112869605, 1.000000000000000000, 0.9238795325112869605, 1.000000000000000000, 0.9238795325112869605, 1.000000000000000000, 0.9238795325112869605, 1.000000000000000000, 0.9238795325112869605, 1.000000000000000000, 0.9238795325112869605, 1.000000000000000000, 0.9238795325112869605, 1.000000000000000000, 0.9238795325112869605, 1.000000000000000000, 0.9238795325112869605, 1.000000000000000000, 0.9238795325112869605, 1.000000000000000000, 0.9238795325112869605, 1.000000000000000000, 0.9238795325112869605, 1.000000000000000000, 0.9238795325112869605, 1.000000000000000000, 0.9238795325112869605, 1.000000000000000000, 0.9238795325112869605, 1.000000000000000000, 0.9238795325112869605, 1.000000000000000000, 0.9238795325112869605, 1.000000000000000000, 0.9238795325112869605, 1.000000000000000000, 0.9238795325112869605, 1.000000000000000000, 0.9238795325112869605, 1.000000000000000000, 0.9238795325112869605, 1.000000000000000000, 0.9238795325112869605, 1.000000000000000000, 0.9238795325112869605, 1.000000000000000000, 0.9238795325112869605, 1.000000000000000000, 0.9238795325112869605, 1.000000000000000000, 0.9238795325112869605, 1.000000000000000000, 0.9238795325112869605, 1.000000000000000000, 0.9238795325112869605, 1.000000000000000000, 0.9238795325112869605, 1.000000000000000000, 0.9238795325112869605, 1.000000000000000000, 0.9238795325112869605, 1.000000000000000000, 0.9238795325112869605, 1.000000000000000000, 0.9238795325112869605, 1.000000000000000000, 0.9238795325112869605, 1.000000000000000000, 0.9238795325112869605, 1.000000000000000000, 0.9238795325112869605, 1.000000000000000000, 0.9238795325112869605, 1.000000000000000000, 0.9238795325112869605, 1.000000000000000000, 0.9238795325112869605, 1.000000000000000000, 0.9238795325112869605, 1.000000000000000000, 0.9238795325112869605, 1.000000000000000000, 0.9238795325112869605, 1.000000000000000000, 0.9238795325112869605, 1.000000000000000000, 0.9238795325112869605, 1.000000000000000000, 0.9238795325112869605, 1.000000000000000000, 0.9238795325112869605, 1.000000000000000000, 0.9238795325112869605, 1.000000000000000000, 0.9238795325112869605, 1.000000000000000000, 0.9238795325112869605, 1.000000000000000000, 0.9238795325112869605, 1.000000000000000000, 0.9238795325112869605, 1.000000000000000000, 0.9238795325112869605, 1.000000000000000000, 0.9238795325112869605, 1.000000000000000000, 0.9238795325112869605, 1.000000000000000000, 0.9238795325112869605, 1.000000000000000000, 0.9238795325112869605, 1.000000000000000000, 0.9238795325112869605, 1.000000000000000000, 0.9238795325112869605, 1.000000000000000000, 0.9238795325112869605, 1.000000000000000000, 0.9238795325112869605, 1.000000000000000000, 0.9238795325112869605, 1.000000000000000000, 0.9238795325112869605, 1.000000000000000000, 0.9238795325112869605, 1.000000000000000000, 0.9238795325112869605, 1.000000000000000000, 0.9238795325112869605, 1.000000000000000000, 0.9238795325112869605, 1.000000000000000000, 0.9238795325112869605, 1.000000000000000000, 0.9238795325112869605, 1.000000000000000000, 0.9238795325112869605, 1.000000000000000000, 0.9238795325112869605, 1.000000000000000000, 0.9238795325112869605, 1.000000000000000000, 0.9238795325112869605, 1.000000000000000000, 0.9238795325112869605, 1.000000000000000000, 0.9238795325112869605, 1.000000000000000000, 0.9238795325112869605, 1.000000000000000000, 0.9238795325112869605, 1.000000000000000000, 0.9238795325112869605, 1.000000000000000000, 0.9238795325112869605, 1.000000000000000000, 0.9238795325112869605, 1.000000000000000000, 0.9238795325112869605, 1.000000000000000000, 0.9238795325112869605, 1.000000000000000000, 0.9238795325112869605, 1.000000000000000000, 0.9238795325112869605, 1.000000000000000000, 0.9238795325112869605, 1.000000000000000000, 0.9238795325112869605, 1.000000000000000000, 0.9238795325112869605, 1.000000000000000000, 0.9238795325112869605, 1.000000000000000000, 0.9238795325112869605, 1.000000000000000000, 0.9238795325112869605, 1.000000000000000000, 0.9238795325112869605, 1.000000000000000000, 0.9238795325112869605, 1.000000000000000000, 0.9238795325112869605, 1.000000000000000000, 0.9238795325112869605, 1.000000000000000000, 0.9238795325112869605, 1.000000000000000000, 0.9238795325112869605, 1.000000000000000000, 0.9238795325112869605, 1.000000000000000000, 0.9238795325112869605, 1.000000000000000000, 0.9238795325112869605, 1.000000000000000000, 0.9238795325112869605, 1.000000000000000000, 0.9238795325112869605, 1.000000000000000000, 0.9238795325112869605, 1.000000000000000000, 0.9238795325112869605, 1.000000000000000000, 0.9238795325112869605, 1.000000000000000000, 0.9238795325112869605, 1.000000000000000000, 0.9238795325112869605, 1.000000000000000000, 0.9238795325112869605, 1.000000000000000000, 0.9238795325112869605, 1.000000000000000000, 0.9238795325112869605, 1.000000000000000000, 0.9238795325112869605, 1.000000000000000000, 0.9238795325112869605, 1.000000000000000000, 0.9238795325112869605, 1.000000000000000000, 0.9238795325112869605, 1.000000000000000000, 0.9238795325112869605, 1.000000000000000000, 0.9238795325112869605, 1.000000000000000000, 0.9238795325112869605, 1.000000000000000000, 0.9238795325112869605, 1.000000000000000000, 0.9238795325112869605, 1.000000000000000000, 0.9238795325112869605, 1.000000000000000000, 0.9238795325112869605, 1.000000000000000000, 0.9238795325112869605, 1.000000000000000000, 0.9238795325112869605, 1.000000000000000000, 0.9238795325112869605, 1.000000000000000000, 0.9238795325112869605, 1.000000000000000000, 0.9238795325112869605, 1.000000000000000000, 0.9238795325112869605, 1.000000000000000000, 0.9238795325112869605, 1.000000000000000000, 0.9238795325112869605, 1.000000000000000000, 0.9238795325112869605, 1.000000000000000000, 0.9238795325112869605, 1.000000000000000000, 0.9238795325112869605, 1.000000000000000000, 0.9238795325112869605, 1.000000000000000000, 0.9238795325112869605, 1.000000000000000000, 0.9238795325112869605, 1.000000000000000000, 0.9238795325112869605, 1.000000000000000000, 0.9238795325112869605, 1.000000000000000000, 0.9238795325112869605, 1.000000000000000000, 0.9238795325112869605, 1.000000000000000000, 0.9238795325112869605, 1.000000000000000000, 0.9238795325112869605, 1.000000000000000000, 0.9238795325112869605, 1.000000000000000000, 0.9238795325112869605, 1.000000000000000000, 0.9238795325112869605, 1.000000000000000000, 0.9238795325112869605, 1.000000000000000000, 0.9238795325112869605, 1.000000000000000000, 0.9238795325112869605, 1.000000000000000000, 0.9238795325112869605, 1.000000000000000000, 0.9238795325112869605, 1.000000000000000000, 0.9238795325112869605, 1.000000000000000000, 0.9238795325112869605, 1.000000000000000000, 0.9238795325112869605, 1.000000000000000000, 0.9238795325112869605, 1.000000000000000000, 0.9238795325112869605, 1.000000000000000000, 0.9238795325112869605, 1.000000000000000000, 0.9238795325112869605, 1.000000000000000000, 0.9238795325112869605, 1.000000000000000000, 0.9238795325112869605, 1.000000000000000000, 0.9238795325112869605, 1.000000000000000000, 0.9238795325112869605, 1.000000000000000000, 0.9238795325112869605, 1.000000000000000000, 0.9238795325112869605, 1.000000000000000000, 0.9238795325112869605, 1.000000000000000000, 0.9238795325112869605, 1.000000000000000000, 0.9238795325112869605, 1.000000000000000000, 0.9238795325112869605, 1.000000000000000000, 0.9238795325112869605, 1.000000000000000000, 0.9238795325112869605, 1.000000000000000000, 0.9238795325112869605, 1.000000000000000000, 0.9238795325112869605, 1.000000000000000000, 0.9238795325112869605, 1.000000000000000000, 0.9238795325112869605, 1.000000000000000000, 0.9238795325112869605, 1.000000000000000000, 0.9238795325112869605, 1.000000000000000000, 0.9238795325112869605, 1.000000000000000000, 0.9238795325112869605, 1.000000000000000000, 0.9238795325112869605, 1.000000000000000000, 0.9238795325112869605, 1.000000000000000000, 0.9238795325112869605, 1.000000000000000000, 0.9238795325112869605, 1.000000000000000000, 0.9238795325112869605, 1.000000000000000000, 0.9238795325112869605, 1.000000000000000000, 0.9238795325112869605, 1.000000000000000000, 0.9238795325112869605, 1.000000000000000000, 0.9238795325112869605, 1.000000000000000000, 0.9238795325112869605, 1.000000000000000000, 0.9238795325112869605, 1.000000000000000000, 0.9238795325112869605, 1.000000000000000000, 0.9238795325112869605, 1.000000000000000000, 0.9238795325112869605, 1.000000000000000000, 0.9238795325112869605, 1.000000000000000000, 0.9238795325112869605, 1.000000000000000000, 0.9238795325112869605, 1.000000000000000000, 0.9238795325112869605, 1.000000000000000000, 0.9238795325112869605, 1.000000000000000000, 0.9238795325112869605, 1.000000000000000000, 0.9238795325112869605, 1.000000000000000000, 0.9238795325112869605, 1.000000000000000000, 0.9238795325112869605, 1.000000000000000000, 0.9238795325112869605, 1.000000000000000000, 0.9238795325112869605, 1.000000000000000000, 0.9238795325112869605, 1.000000000000000000, 0.9238795325112869605, 1.000000000000000000, 0.9238795325112869605, 1.000000000000000000, 0.9238795325112869605, 1.000000000000000000, 0.9238795325112869605, 1.000000000000000000, 0.9238795325112869605, 1.000000000000000000, 0.9238795325112869605, 1.000000000000000000, 0.9238795325112869605, 1.000000000000000000, 0.9238795325112869605, 1.000000000000000000, 0.9238795325112869605, 1.000000000000000000, 0.9238795325112869605, 1.000000000000000000, 0.9238795325112869605, 1.000000000000000000, 0.9238795325112869605, 1.000000000000000000, 0.9238795325112869605, 1.000000000000000000, 0.9238795325112869605, 1.000000000000000000, 0.9238795325112869605, 1.000000000000000000, 0.9238795325112869605, 1.000000000000000000, 0.9238795325112869605, 1.000000000000000000, 0.9238795325112869605, 1.000000000000000000, 0.9238795325112869605, 1.000000000000000000, 0.9238795325112869605, 1.000000000000000000, 0.9238795325112869605, 1.000000000000000000, 0.9238795325112869605, 1.000000000000000000, 0.9238795325112869605, 1.000000000000000000, 0.9238795325112869605, 1.000000000000000000, 0.9238795325112869605, 1.000000000000000000, 0.9238795325112869605, 1.000000000000000000, 0.9238795325112869605, 1.000000000000000000, 0.9238795325112869605, 1.000000000000000000, 0.9238795325112869605, 1.000000000000000000, 0.9238795325112869605, 1.000000000000000000, 0.9238795325112869605, 1.000000000000000000, 0.9238795325112869605, 1.000000000000000000, 0.9238795325112869605, 1.000000000000000000, 0.9238795325112869605, 1.000000000000000000, 0.9238795325112869605, 1.000000000000000000, 0.9238795325112869605, 1.000000000000000000, 0.9238795325112869605, 1.000000000000000000, 0.9238795325112869605, 1.000000000000000000, 0.9238795325112869605, 1.000000000000000000, 0.9238795325112869605, 1.000000000000000000, 0.9238795325112869605, 1.000000000000000000, 0.9238795325112869605, 1.000000000000000000, 0.9238795325112869605, 1.000000000000000000, 0.9238795325112869605, 1.000000000000000000, 0.9238795325112869605, 1.000000000000000000, 0.9238795325112869605, 1.000000000000000000, 0.9238795325112869605, 1.000000000000000000, 0.9238795325112869605, 1.000000000000000000, 0.9238795325112869605, 1.000000000000000000, 0.9238795325112869605, 1.000000000000000000),
 ( 1.000000000000000000, 0.9238795325112869605, 1.000000000000000000, 0.9238795325112869605, 1.000000000000000000, 0.9238795325112869605, 1.000000000000000000, 0.9238795325112869605, 1.000000000000000000, 0.9238795325112869605, 1.000000000000000000, 0.9238795325112869605, 1.000000000000000000, 0.9238795325112869605, 1.000000000000000000, 0.9238795325112869605, 1.000000000000000000, 0.9238795325112869605, 1.000000000000000000, 0.9238795325112869605, 1.000000000000000000, 0.9238795325112869605, 1.000000000000000000, 0.9238795325112869605, 1.000000000000000000, 0.9238795325112869605, 1.000000000000000000, 0.9238795325112869605, 1.000000000000000000, 0.9238795325112869605, 1.000000000000000000, 0.9238795325112869605, 1.000000000000000000, 0.9238795325112869605, 1.000000000000000000, 0.9238795325112869605, 1.000000000000000000, 0.9238795325112869605, 1.000000000000000000, 0.9238795325112869605, 1.000000000000000000, 0.9238795325112869605, 1.000000000000000000, 0.9238795325112869605, 1.000000000000000000, 0.9238795325112869605, 1.000000000000000000, 0.9238795325112869605, 1.000000000000000000, 0.9238795325112869605, 1.000000000000000000, 0.9238795325112869605, 1.000000000000000000, 0.9238795325112869605, 1.000000000000000000, 0.9238795325112869605, 1.000000000000000000, 0.9238795325112869605, 1.000000000000000000, 0.9238795325112869605, 1.000000000000000000, 0.9238795325112869605, 1.000000000000000000, 0.9238795325112869605, 1.000000000000000000, 0.9238795325112869605, 1.000000000000000000, 0.9238795325112869605, 1.000000000000000000, 0.9238795325112869605, 1.000000000000000000, 0.9238795325112869605, 1.000000000000000000, 0.9238795325112869605, 1.000000000000000000, 0.9238795325112869605, 1.000000000000000000, 0.9238795325112869605, 1.000000000000000000, 0.9238795325112869605, 1.000000000000000000, 0.9238795325112869605, 1.000000000000000000, 0.9238795325112869605, 1.000000000000000000, 0.9238795325112869605, 1.000000000000000000, 0.9238795325112869605, 1.000000000000000000, 0.9238795325112869605, 1.000000000000000000, 0.9238795325112869605, 1.000000000000000000, 0.9238795325112869605, 1.000000000000000000, 0.9238795325112869605, 1.000000000000000000, 0.9238795325112869605, 1.000000000000000000, 0.9238795325112869605, 1.000000000000000000, 0.9238795325112869605, 1.000000000000000000, 0.9238795325112869605, 1.000000000000000000, 0.9238795325112869605, 1.000000000000000000, 0.9238795325112869605, 1.000000000000000000, 0.9238795325112869605, 1.000000000000000000, 0.9238795325112869605, 1.000000000000000000, 0.9238795325112869605, 1.000000000000000000, 0.9238795325112869605, 1.000000000000000000, 0.9238795325112869605, 1.000000000000000000, 0.9238795325112869605, 1.000000000000000000, 0.9238795325112869605, 1.000000000000000000, 0.9238795325112869605, 1.000000000000000000, 0.9238795325112869605, 1.000000000000000000, 0.9238795325112869605, 1.000000000000000000, 0.9238795325112869605, 1.000000000000000000, 0.9238795325112869605, 1.000000000000000000, 0.9238795325112869605, 1.000000000000000000, 0.9238795325112869605, 1.000000000000000000, 0.9238795325112869605, 1.000000000000000000, 0.9238795325112869605, 1.000000000000000000, 0.9238795325112869605, 1.000000000000000000, 0.9238795325112869605, 1.000000000000000000, 0.9238795325112869605, 1.000000000000000000, 0.9238795325112869605, 1.000000000000000000, 0.9238795325112869605, 1.000000000000000000, 0.9238795325112869605, 1.000000000000000000, 0.9238795325112869605, 1.000000000000000000, 0.9238795325112869605, 1.000000000000000000, 0.9238795325112869605, 1.000000000000000000, 0.9238795325112869605, 1.000000000000000000, 0.9238795325112869605, 1.000000000000000000, 0.9238795325112869605, 1.000000000000000000, 0.9238795325112869605, 1.000000000000000000, 0.9238795325112869605, 1.000000000000000000, 0.9238795325112869605, 1.000000000000000000, 0.9238795325112869605, 1.000000000000000000, 0.9238795325112869605, 1.000000000000000000, 0.9238795325112869605, 1.000000000000000000, 0.9238795325112869605, 1.000000000000000000, 0.9238795325112869605, 1.000000000000000000, 0.9238795325112869605, 1.000000000000000000, 0.9238795325112869605, 1.000000000000000000, 0.9238795325112869605, 1.000000000000000000, 0.9238795325112869605, 1.000000000000000000, 0.9238795325112869605, 1.000000000000000000, 0.9238795325112869605, 1.000000000000000000, 0.9238795325112869605, 1.000000000000000000, 0.9238795325112869605, 1.000000000000000000, 0.9238795325112869605, 1.000000000000000000, 0.9238795325112869605, 1.000000000000000000, 0.9238795325112869605, 1.000000000000000000, 0.9238795325112869605, 1.000000000000000000, 0.9238795325112869605, 1.000000000000000000, 0.9238795325112869605, 1.000000000000000000, 0.9238795325112869605, 1.000000000000000000, 0.9238795325112869605, 1.000000000000000000, 0.9238795325112869605, 1.000000000000000000, 0.9238795325112869605, 1.000000000000000000, 0.9238795325112869605, 1.000000000000000000, 0.9238795325112869605, 1.000000000000000000, 0.9238795325112869605, 1.000000000000000000, 0.9238795325112869605, 1.000000000000000000, 0.9238795325112869605, 1.000000000000000000, 0.9238795325112869605, 1.000000000000000000, 0.9238795325112869605, 1.000000000000000000, 0.9238795325112869605, 1.000000000000000000, 0.9238795325112869605, 1.000000000000000000, 0.9238795325112869605, 1.000000000000000000, 0.9238795325112869605, 1.000000000000000000, 0.9238795325112869605, 1.000000000000000000, 0.9238795325112869605, 1.000000000000000000, 0.9238795325112869605, 1.000000000000000000, 0.9238795325112869605, 1.000000000000000000, 0.9238795325112869605, 1.000000000000000000, 0.9238795325112869605, 1.000000000000000000, 0.9238795325112869605, 1.000000000000000000, 0.9238795325112869605, 1.000000000000000000, 0.9238795325112869605, 1.000000000000000000, 0.9238795325112869605, 1.000000000000000000, 0.9238795325112869605, 1.000000000000000000, 0.9238795325112869605, 1.000000000000000000, 0.9238795325112869605, 1.000000000000000000, 0.9238795325112869605, 1.000000000000000000, 0.9238795325112869605, 1.000000000000000000, 0.9238795325112869605, 1.000000000000000000, 0.9238795325112869605, 1.000000000000000000, 0.9238795325112869605, 1.000000000000000000, 0.9238795325112869605, 1.000000000000000000, 0.9238795325112869605, 1.000000000000000000, 0.9238795325112869605, 1.000000000000000000, 0.9238795325112869605, 1.000000000000000000, 0.9238795325112869605, 1.000000000000000000, 0.9238795325112869605, 1.000000000000000000, 0.9238795325112869605, 1.000000000000000000, 0.9238795325112869605, 1.000000000000000000, 0.9238795325112869605, 1.000000000000000000, 0.9238795325112869605, 1.000000000000000000, 0.9238795325112869605, 1.000000000000000000, 0.9238795325112869605, 1.000000000000000000, 0.9238795325112869605, 1.000000000000000000, 0.9238795325112869605, 1.000000000000000000, 0.9238795325112869605, 1.000000000000000000, 0.9238795325112869605, 1.000000000000000000, 0.9238795325112869605, 1.000000000000000000, 0.9238795325112869605, 1.000000000000000000, 0.9238795325112869605, 1.000000000000000000, 0.9238795325112869605, 1.000000000000000000, 0.9238795325112869605, 1.000000000000000000, 0.9238795325112869605, 1.000000000000000000, 0.9238795325112869605, 1.000000000000000000, 0.9238795325112869605, 1.000000000000000000, 0.9238795325112869605, 1.000000000000000000, 0.9238795325112869605, 1.000000000000000000, 0.9238795325112869605, 1.000000000000000000, 0.9238795325112869605, 1.000000000000000000, 0.9238795325112869605, 1.000000000000000000, 0.9238795325112869605, 1.000000000000000000, 0.9238795325112869605, 1.000000000000000000, 0.9238795325112869605, 1.000000000000000000, 0.9238795325112869605, 1.000000000000000000, 0.9238795325112869605, 1.000000000000000000, 0.9238795325112869605, 1.000000000000000000, 0.9238795325112869605, 1.000000000000000000, 0.9238795325112869605, 1.000000000000000000, 0.9238795325112869605, 1.000000000000000000, 0.9238795325112869605, 1.000000000000000000, 0.9238795325112869605, 1.000000000000000000, 0.9238795325112869605, 1.000000000000000000, 0.9238795325112869605, 1.000000000000000000, 0.9238795325112869605, 1.000000000000000000, 0.9238795325112869605, 1.000000000000000000, 0.9238795325112869605, 1.000000000000000000, 0.9238795325112869605, 1.000000000000000000, 0.9238795325112869605, 1.000000000000000000, 0.9238795325112869605, 1.000000000000000000, 0.9238795325112869605, 1.000000000000000000, 0.9238795325112869605, 1.000000000000000000, 0.9238795325112869605, 1.000000000000000000, 0.9238795325112869605, 1.000000000000000000, 0.9238795325112869605, 1.000000000000000000, 0.9238795325112869605, 1.000000000000000000, 0.9238795325112869605, 1.000000000000000000, 0.9238795325112869605, 1.000000000000000000, 0.9238795325112869605, 1.000000000000000000, 0.9238795325112869605, 1.000000000000000000, 0.9238795325112869605, 1.000000000000000000, 0.9238795325112869605, 1.000000000000000000, 0.9238795325112869605, 1.000000000000000000, 0.9238795325112869605, 1.000000000000000000, 0.9238795325112869605, 1.000000000000000000, 0.9238795325112869605, 1.000000000000000000, 0.9238795325112869605, 1.000000000000000000, 0.9238795325112869605, 1.000000000000000000, 0.9238795325112869605, 1.000000000000000000, 0.9238795325112869605, 1.000000000000000000, 0.9238795325112869605, 1.000000000000000000, 0.9238795325112869605, 1.000000000000000000, 0.9238795325112869605, 1.000000000000000000, 0.9238795325112869605, 1.000000000000000000, 0.9238795325112869605, 1.000000000000000000, 0.9238795325112869605, 1.000000000000000000, 0.9238795325112869605, 1.000000000000000000, 0.9238795325112869605, 1.000000000000000000, 0.9238795325112869605, 1.000000000000000000, 0.9238795325112869605, 1.000000000000000000, 0.9238795325112869605, 1.000000000000000000, 0.9238795325112869605, 1.000000000000000000, 0.9238795325112869605, 1.000000000000000000, 0.9238795325112869605, 1.000000000000000000, 0.9238795325112869605, 1.000000000000000000, 0.9238795325112869605, 1.000000000000000000, 0.9238795325112869605, 1.000000000000000000, 0.9238795325112869605, 1.000000000000000000, 0.9238795325112869605, 1.000000000000000000, 0.9238795325112869605, 1.000000000000000000, 0.9238795325112869605, 1.000000000000000000, 0.9238795325112869605, 1.000000000000000000, 0.9238795325112869605, 1.000000000000000000, 0.9238795325112869605, 1.000000000000000000, 0.9238795325112869605, 1.000000000000000000, 0.9238795325112869605, 1.000000000000000000, 0.9238795325112869605, 1.000000000000000000, 0.9238795325112869605, 1.000000000000000000, 0.9238795325112869605, 1.000000000000000000, 0.9238795325112869605, 1.000000000000000000, 0.9238795325112869605, 1.000000000000000000, 0.9238795325112869605, 1.000000000000000000, 0.9238795325112869605, 1.000000000000000000, 0.9238795325112869605, 1.000000000000000000, 0.9238795325112869605, 1.000000000000000000, 0.9238795325112869605, 1.000000000000000000, 0.9238795325112869605, 1.000000000000000000, 0.9238795325112869605, 1.000000000000000000, 0.9238795325112869605, 1.000000000000000000, 0.9238795325112869605, 1.000000000000000000, 0.9238795325112869605, 1.000000000000000000, 0.9238795325112869605, 1.000000000000000000, 0.9238795325112869605, 1.000000000000000000, 0.9238795325112869605, 1.000000000000000000, 0.9238795325112869605, 1.000000000000000000, 0.9238795325112869605, 1.000000000000000000, 0.9238795325112869605, 1.000000000000000000, 0.9238795325112869605, 1.000000000000000000, 0.9238795325112869605, 1.000000000000000000, 0.9238795325112869605, 1.000000000000000000, 0.9238795325112869605, 1.000000000000000000, 0.9238795325112869605, 1.000000000000000000, 0.9238795325112869605, 1.000000000000000000, 0.9238795325112869605, 1.000000000000000000, 0.9238795325112869605, 1.000000000000000000, 0.9238795325112869605, 1.000000000000000000, 0.9238795325112869605, 1.000000000000000000, 0.9238795325112869605, 1.000000000000000000, 0.9238795325112869605, 1.000000000000000000, 0.9238795325112869605, 1.000000000000000000, 0.9238795325112869605, 1.000000000000000000, 0.9238795325112869605, 1.000000000000000000, 0.9238795325112869605, 1.000000000000000000, 0.9238795325112869605, 1.000000000000000000, 0.9238795325112869605, 1.000000000000000000, 0.9238795325112869605, 1.000000000000000000, 0.9238795325112869605, 1.000000000000000000, 0.9238795325112869605, 1.000000000000000000, 0.9238795325112869605, 1.000000000000000000, 0.9238795325112869605, 1.000000000000000000, 0.9238795325112869605, 1.000000000000000000, 0.9238795325112869605, 1.000000000000000000, 0.9238795325112869605, 1.000000000000000000, 0.9238795325112869605, 1.000000000000000000, 0.9238795325112869605, 1.000000000000000000, 0.9238795325112869605, 1.000000000000000000, 0.9238795325112869605, 1.000000000000000000, 0.9238795325112869605, 1.000000000000000000, 0.9238795325112869605, 1.000000000000000000, 0.9238795325112869605, 1.000000000000000000, 0.9238795325112869605, 1.000000000000000000, 0.9238795325112869605, 1.000000000000000000, 0.9238795325112869605, 1.000000000000000000, 0.9238795325112869605, 1.000000000000000000, 0.9238795325112869605, 1.000000000000000000, 0.9238795325112869605, 1.000000000000000000, 0.9238795325112869605, 1.000000000000000000, 0.9238795325112869605, 1.000000000000000000, 0.9238795325112869605, 1.000000000000000000, 0.9238795325112869605, 1.000000000000000000, 0.9238795325112869605, 1.000000000000000000, 0.9238795325112869605, 1.000000000000000000, 0.9238795325112869605, 1.000000000000000000, 0.9238795325112869605, 1.000000000000000000, 0.9238795325112869605, 1.000000000000000000, 0.9238795325112869605, 1.000000000000000000, 0.9238795325112869605, 1.000000000000000000, 0.9238795325112869605, 1.000000000000000000, 0.9238795325112869605, 1.000000000000000000, 0.9238795325112869605, 1.000000000000000000, 0.9238795325112869605, 1.000000000000000000, 0.9238795325112869605, 1.000000000000000000, 0.9238795325112869605, 1.000000000000000000, 0.9238795325112869605, 1.000000000000000000, 0.9238795325112869605, 1.000000000000000000, 0.9238795325112869605, 1.000000000000000000, 0.9238795325112869605, 1.000000000000000000, 0.9238795325112869605, 1.000000000000000000, 0.9238795325112869605, 1.000000000000000000, 0.9238795325112869605, 1.000000000000000000, 0.9238795325112869605, 1.000000000000000000, 0.9238795325112869605, 1.000000000000000000, 0.9238795325112869605, 1.000000000000000000, 0.9238795325112869605, 1.000000000000000000, 0.9238795325112869605, 1.000000000000000000, 0.9238795325112869605, 1.000000000000000000, 0.9238795325112869605, 1.000000000000000000, 0.9238795325112869605, 1.000000000000000000, 0.9238795325112869605, 1.000000000000000000, 0.9238795325112869605, 1.000000000000000000, 0.9238795325112869605, 1.000000000000000000, 0.9238795325112869605, 1.000000000000000000, 0.9238795325112869605, 1.000000000000000000, 0.9238795325112869605, 1.000000000000000000, 0.9238795325112869605, 1.000000000000000000, 0.9238795325112869605, 1.000000000000000000, 0.9238795325112869605, 1.000000000000000000, 0.9238795325112869605, 1.000000000000000000, 0.9238795325112869605, 1.000000000000000000, 0.9238795325112869605, 1.000000000000000000, 0.9238795325112869605, 1.000000000000000000, 0.9238795325112869605, 1.000000000000000000, 0.9238795325112869605, 1.000000000000000000, 0.9238795325112869605, 1.000000000000000000, 0.9238795325112869605, 1.000000000000000000, 0.9238795325112869605, 1.000000000000000000, 0.9238795325112869605, 1.000000000000000000, 0.9238795325112869605, 1.000000000000000000, 0.9238795325112869605, 1.000000000000000000, 0.9238795325112869605, 1.000000000000000000, 0.9238795325112869605, 1.000000000000000000, 0.9238795325112869605, 1.000000000000000000, 0.9238795325112869605, 1.000000000000000000, 0.9238795325112869605, 1.000000000000000000, 0.9238795325112869605, 1.000000000000000000, 0.9238795325112869605, 1.000000000000000000, 0.9238795325112869605, 1.000000000000000000, 0.9238795325112869605, 1.000000000000000000, 0.9238795325112869605, 1.000000000000000000, 0.9238795325112869605, 1.000000000000000000, 0.9238795325112869605, 1.000000000000000000, 0.9238795325112869605, 1.000000000000000000, 0.9238795325112869605, 1.000000000000000000, 0.9238795325112869605, 1.000000000000000000, 0.9238795325112869605, 1.000000000000000000, 0.9238795325112869605, 1.000000000000000000, 0.9238795325112869605, 1.000000000000000000, 0.9238795325112869605, 1.000000000000000000, 0.9238795325112869605, 1.000000000000000000, 0.9238795325112869605, 1.000000000000000000, 0.9238795325112869605, 1.000000000000000000, 0.9238795325112869605, 1.000000000000000000, 0.9238795325112869605, 1.000000000000000000, 0.9238795325112869605, 1.000000000000000000, 0.9238795325112869605, 1.000000000000000000, 0.9238795325112869605, 1.000000000000000000, 0.9238795325112869605, 1.000000000000000000, 0.9238795325112869605, 1.000000000000000000, 0.9238795325112869605, 1.000000000000000000, 0.9238795325112869605, 1.000000000000000000, 0.9238795325112869605, 1.000000000000000000, 0.9238795325112869605, 1.000000000000000000, 0.9238795325112869605, 1.000000000000000000, 0.9238795325112869605, 1.000000000000000000, 0.9238795325112869605, 1.000000000000000000, 0.9238795325112869605, 1.000000000000000000, 0.9238795325112869605, 1.000000000000000000, 0.9238795325112869605, 1.000000000000000000, 0.9238795325112869605, 1.000000000000000000, 0.9238795325112869605, 1.000000000000000000, 0.9238795325112869605, 1.000000000000000000, 0.9238795325112869605, 1.000000000000000000, 0.9238795325112869605, 1.000000000000000000, 0.9238795325112869605, 1.000000000000000000, 0.9238795325112869605, 1.000000000000000000, 0.9238795325112869605, 1.000000000000000000, 0.9238795325112869605, 1.000000000000000000, 0.9238795325112869605, 1.000000000000000000, 0.9238795325112869605, 1.000000000000000000, 0.9238795325112869605, 1.000000000000000000, 0.9238795325112869605, 1.000000000000000000, 0.9238795325112869605, 1.000000000000000000, 0.9238795325112869605, 1.000000000000000000, 0.9238795325112869605, 1.000000000000000000, 0.9238795325112869605, 1.000000000000000000) ) ) 
 REPRESENTATION_ITEM ( '' )  SURFACE ( )  ) ;
#2443=CARTESIAN_POINT ( 'NONE',  ( -1.054774247047244540, -0.07405724077823318263, 0.8513779527021426707 ) ) ;
#2447=CARTESIAN_POINT ( 'NONE',  ( -0.7495874582379994377, -0.1138864663351371320, 1.985572741735574853 ) ) ;
#2449=CARTESIAN_POINT ( 'NONE',  ( 1.054774247047244540, 0.07405724077823318263, 1.525590551127340433 ) ) ;
#2452=CARTESIAN_POINT ( 'NONE',  ( 0.9500414927467377701, -0.1787899950787401604, 0.3297244093950555954 ) ) ;
#2453=ORIENTED_EDGE ( 'NONE', *, *, #10481, .F. ) ;
#2458=FACE_OUTER_BOUND ( 'NONE', #2611, .T. ) ;
#2460=CARTESIAN_POINT ( 'NONE',  ( 1.054774247047244540, 0.07405724077823318263, 0.6151574802611965431 ) ) ;
#2462=CARTESIAN_POINT ( 'NONE',  ( 0.7952710522841902607, -0.1417631204022561375, 0.03937007543464863396 ) ) ;
#2464=CARTESIAN_POINT ( 'NONE',  ( -0.9500414927467378812, -0.1787899950787401604, 1.510826771599780294 ) ) ;
#2467=CARTESIAN_POINT ( 'NONE',  ( 0.6971942568897626646, 0.07405724077823318263, 0.9498031495525356416 ) ) ;
#2468=ORIENTED_EDGE ( 'NONE', *, *, #9973, .F. ) ;
#2469=CARTESIAN_POINT ( 'NONE',  ( -0.7646288533564489232, -0.1113553986120547346, 0.7332677164279054471 ) ) ;
#2471=CARTESIAN_POINT ( 'NONE',  ( 1.054774247047244096, 0.000000000000000000, 1.715059055064346527 ) ) ;
#2472=CARTESIAN_POINT ( 'NONE',  ( -0.8759842519685039353, 0.1574803149606299191, 1.358267716535433323 ) ) ;
#2473=CARTESIAN_POINT ( 'NONE',  ( -0.7495606340400177148, -0.1264236179284866091, 0.8341535432533228045 ) ) ;
#2475=CARTESIAN_POINT ( 'NONE',  ( -0.7108038343253642033, 0.06841996760810098444, 0.03937007874015843040 ) ) ;
#2476=CARTESIAN_POINT ( 'NONE',  ( 1.002407869896990045, -0.1264236179284866091, 0.1402559054580474474 ) ) ;
#2477=CARTESIAN_POINT ( 'NONE',  ( -0.9500414927467377701, -0.1787899950787401604, 0.1328740156942679884 ) ) ;
#2479=CARTESIAN_POINT ( 'NONE',  ( 0.8107537697050253289, -0.1574803149606297803, 1.523129921152316379 ) ) ;
#2481=( BOUNDED_CURVE ( )  B_SPLINE_CURVE ( 2, ( #14931, #40526, #18967, #3657, #36961, #11809, #41215, #33867, #11104 ),
 .UNSPECIFIED., .F., .T. ) 
 B_SPLINE_CURVE_WITH_KNOTS ( ( 3, 2, 2, 2, 3 ),
 ( 0.4400000000000000022, 0.4425000000000000044, 0.4450000000000000067, 0.4475000000000000089, 0.4500000000000000111 ),
 .UNSPECIFIED. ) 
 CURVE ( )  GEOMETRIC_REPRESENTATION_ITEM ( )  RATIONAL_B_SPLINE_CURVE ( ( 1.000000000000000000, 0.9238795325112869605, 1.000000000000000000, 0.9238795325112869605, 1.000000000000000000, 0.9238795325112869605, 1.000000000000000000, 0.9238795325112869605, 1.000000000000000000 ) ) 
 REPRESENTATION_ITEM ( '' )  ) ;
#2484=CARTESIAN_POINT ( 'NONE',  ( -0.6971942568897648851, -0.07405724077823297447, 1.658464566875369472 ) ) ;
#2487=EDGE_CURVE ( 'NONE', #45388, #23548, #40954, .T. ) ;
#2493=ORIENTED_EDGE ( 'NONE', *, *, #39271, .F. ) ;
#2498=DIRECTION ( 'NONE',  ( 1.822029033848725028E-16, 0.000000000000000000, 1.000000000000000000 ) ) ;
#2499=EDGE_CURVE ( 'NONE', #37113, #40492, #32754, .T. ) ;
#2500=CARTESIAN_POINT ( 'NONE',  ( 0.8759842519685039353, -0.1574803149606299191, 1.811023622047244208 ) ) ;
#2504=CARTESIAN_POINT ( 'NONE',  ( -0.8019270111902716547, -0.1787899950787401604, 0.4084645668753704162 ) ) ;
#2505=CARTESIAN_POINT ( 'NONE',  ( -0.9873396505805591694, -0.1113553986120547346, 1.067913385826771755 ) ) ;
#2507=DIRECTION ( 'NONE',  ( 0.000000000000000000, 0.000000000000000000, -1.000000000000000000 ) ) ;
#2508=CARTESIAN_POINT ( 'NONE',  ( 0.9500414927467378812, 0.1787899950787401604, 1.018700787347811110 ) ) ;
#2509=CARTESIAN_POINT ( 'NONE',  ( 0.8759842519685039353, 0.1787899950787401882, 1.567421259788755794 ) ) ;
#2513=CARTESIAN_POINT ( 'NONE',  ( -0.9873396505805591694, -0.1113553986120547346, 1.687992125876724536 ) ) ;
#2514=VECTOR ( 'NONE', #2680, 39.37007874015748143 ) ;
#2516=CARTESIAN_POINT ( 'NONE',  ( 0.8759842519685039353, 0.1787899950787401882, 1.094980314906866203 ) ) ;
#2518=CARTESIAN_POINT ( 'NONE',  ( 0.9500414927467377701, -0.1787899950787401604, 1.948818897584033705 ) ) ;
#2519=CARTESIAN_POINT ( 'NONE',  ( -0.7495606340400177148, 0.1264236179284866091, 1.139271653489543290 ) ) ;
#2520=CARTESIAN_POINT ( 'NONE',  ( 1.033464566929134687, 0.06523048226347956391, 0.4355314959554649756 ) ) ;
#2523=CARTESIAN_POINT ( 'NONE',  ( 1.033416983624987129, 0.02228945808267622855, 0.03936935455931785816 ) ) ;
#2526=CARTESIAN_POINT ( 'NONE',  ( -0.7185039370078746268, 0.06523048226347956391, 0.2928149605223941965 ) ) ;
#2527=ORIENTED_EDGE ( 'NONE', *, *, #37062, .T. ) ;
#2528=CARTESIAN_POINT ( 'NONE',  ( 0.8019270111902717657, 0.1787899950787401604, 1.254921259788757348 ) ) ;
#2529=DIRECTION ( 'NONE',  ( -4.336808689942014285E-16, 0.000000000000000000, -1.000000000000000000 ) ) ;
#2530=CARTESIAN_POINT ( 'NONE',  ( 0.8759842519685039353, 0.000000000000000000, 4.498031496062992574 ) ) ;
#2531=CARTESIAN_POINT ( 'NONE',  ( 0.8759842519685039353, 0.1574803149606299191, 0.7283464566929134243 ) ) ;
#2532=AXIS2_PLACEMENT_3D ( 'NONE', #20521, #46857, #28201 ) ;
#2535=CARTESIAN_POINT ( 'NONE',  ( -0.9412147342319837628, 0.1574803149606300301, 0.2042322833570397733 ) ) ;
#2536=ADVANCED_FACE ( 'NONE', ( #5943 ), #34036, .T. ) ;
#2538=CARTESIAN_POINT ( 'NONE',  ( -0.6971942568897648851, 0.07405724077823318263, 1.338582677111590069 ) ) ;
#2540=CARTESIAN_POINT ( 'NONE',  ( -1.054774247047244540, -0.07405724077823318263, 0.9301181101824563813 ) ) ;
#2541=CARTESIAN_POINT ( 'NONE',  ( -0.8759842519685039353, -0.1787899950787401882, 1.980807086560409491 ) ) ;
#2542=CARTESIAN_POINT ( 'NONE',  ( -0.8019270111902716547, -0.1787899950787401604, 1.072834645615528659 ) ) ;
#2543=CARTESIAN_POINT ( 'NONE',  ( -0.8019270111902717657, 0.1787899950787401604, 0.6692913385289144257 ) ) ;
#2544=CARTESIAN_POINT ( 'NONE',  ( -0.8759842519685039353, 0.1574803149606299191, 0.08858267705782735257 ) ) ;
#2546=EDGE_LOOP ( 'NONE', ( #2786, #19871, #46673, #40472 ) ) ;
#2550=CARTESIAN_POINT ( 'NONE',  ( 1.033464566929133799, 0.000000000000000000, 0.7972440944881890035 ) ) ;
#2551=CARTESIAN_POINT ( 'NONE',  ( -0.8759842519685039353, 0.1787899950787401882, 0.7012795275052913224 ) ) ;
#2553=ORIENTED_EDGE ( 'NONE', *, *, #17261, .F. ) ;
#2554=CARTESIAN_POINT ( 'NONE',  ( -1.002407869896990045, 0.1264236179284866091, 1.606791338528913426 ) ) ;
#2556=CARTESIAN_POINT ( 'NONE',  ( -0.9412147342319837628, 0.1574803149606300301, 0.4896653543307082357 ) ) ;
#2557=CYLINDRICAL_SURFACE ( 'NONE', #31701, 0.1574803149606299191 ) ;
#2558=CARTESIAN_POINT ( 'NONE',  ( -0.9412147342319837628, 0.1574803149606300301, 1.385334645561763667 ) ) ;
#2559=CARTESIAN_POINT ( 'NONE',  ( 1.002407869896990045, 0.1264236179284866091, 0.6619094487651338010 ) ) ;
#2562=CARTESIAN_POINT ( 'NONE',  ( 0.8759842519685039353, 0.000000000000000000, 4.498031496062992574 ) ) ;
#2564=CARTESIAN_POINT ( 'NONE',  ( -0.7185039370078739607, 1.928577636452523993E-17, 0.6889763778452283605 ) ) ;
#2565=CARTESIAN_POINT ( 'NONE',  ( 0.9412147342319837628, -0.1574803149606297803, 1.222933070866141669 ) ) ;
#2567=LINE ( 'NONE', #3038, #197 ) ;
#2569=CARTESIAN_POINT ( 'NONE',  ( 1.002407869896990045, -0.1264236179284866091, 0.6865157479777322935 ) ) ;
#2577=CARTESIAN_POINT ( 'NONE',  ( 0.8019270111902717657, 0.1787899950787401604, 0.9005905511273389896 ) ) ;
#2578=EDGE_CURVE ( 'NONE', #11036, #3082, #8218, .T. ) ;
#2584=( BOUNDED_CURVE ( )  B_SPLINE_CURVE ( 2, ( #46113, #31991, #9235, #24786, #2035, #16436, #27940, #27716, #42282 ),
 .UNSPECIFIED., .F., .T. ) 
 B_SPLINE_CURVE_WITH_KNOTS ( ( 3, 2, 2, 2, 3 ),
 ( 0.7299999999999999822, 0.7325000000000000400, 0.7349999999999999867, 0.7375000000000000444, 0.7399999999999999911 ),
 .UNSPECIFIED. ) 
 CURVE ( )  GEOMETRIC_REPRESENTATION_ITEM ( )  RATIONAL_B_SPLINE_CURVE ( ( 1.000000000000000000, 0.9238795325112869605, 1.000000000000000000, 0.9238795325112869605, 1.000000000000000000, 0.9238795325112869605, 1.000000000000000000, 0.9238795325112869605, 1.000000000000000000 ) ) 
 REPRESENTATION_ITEM ( '' )  ) ;
#2587=CARTESIAN_POINT ( 'NONE',  ( -0.8759842519685039353, -0.1787899950787401882, 1.906988188922614125 ) ) ;
#2590=CARTESIAN_POINT ( 'NONE',  ( -0.9873396505805591694, -0.1113553986120547346, 0.8218503935932598425 ) ) ;
#2591=ORIENTED_EDGE ( 'NONE', *, *, #46408, .T. ) ;
#2594=CARTESIAN_POINT ( 'NONE',  ( -1.054774247047244540, 0.07405724077823318263, 1.919291338528913649 ) ) ;
#2595=CARTESIAN_POINT ( 'NONE',  ( -1.054774247047244540, -0.07405724077823318263, 1.594488188922613237 ) ) ;
#2596=FACE_OUTER_BOUND ( 'NONE', #27100, .T. ) ;
#2597=CARTESIAN_POINT ( 'NONE',  ( -1.054774247047244540, 0.07405724077823318263, 0.9694881889226144578 ) ) ;
#2598=CARTESIAN_POINT ( 'NONE',  ( -0.8019270111902717657, 0.1787899950787401604, 0.2362204723871814960 ) ) ;
#2600=CARTESIAN_POINT ( 'NONE',  ( -0.7495606340400177148, 0.1264236179284866091, 1.892224409395055096 ) ) ;
#2601=CARTESIAN_POINT ( 'NONE',  ( 0.8107537697050254399, -0.1574803149606297803, 1.405019684931842816 ) ) ;
#2602=CARTESIAN_POINT ( 'NONE',  ( -0.8759842519685039353, -0.1574803149606299191, 1.850393700787401619 ) ) ;
#2610=CARTESIAN_POINT ( 'NONE',  ( -0.6971942568897637749, 2.189545951927499583E-17, 1.227854330654897685 ) ) ;
#2611=EDGE_LOOP ( 'NONE', ( #44157, #40450, #15239, #25019 ) ) ;
#2614=( NAMED_UNIT ( * ) PLANE_ANGLE_UNIT ( ) SI_UNIT ( $, .RADIAN. ) ) ;
#2618=CARTESIAN_POINT ( 'NONE',  ( -0.9873396505805591694, 0.1113553986120547346, 0.7529527557979842634 ) ) ;
#2619=CARTESIAN_POINT ( 'NONE',  ( -0.8107537697050253289, -0.1574803149606297803, 0.7849409448818904789 ) ) ;
#2622=CARTESIAN_POINT ( 'NONE',  ( 0.8107537697050253289, -0.1574803149606297803, 0.8243110236220465570 ) ) ;
#2624=CARTESIAN_POINT ( 'NONE',  ( -0.7646288533564489232, 0.1113553986120547346, 1.245078740157480324 ) ) ;
#2625=CARTESIAN_POINT ( 'NONE',  ( 1.033464566929134687, 0.06523048226347956391, 0.6028543307086614567 ) ) ;
#2626=DIRECTION ( 'NONE',  ( 1.822029033848725028E-16, 0.000000000000000000, 1.000000000000000000 ) ) ;
#2627=CARTESIAN_POINT ( 'NONE',  ( 1.033464566929133799, 0.000000000000000000, 1.102362204616881947 ) ) ;
#2628=CARTESIAN_POINT ( 'NONE',  ( 0.7646288533564489232, 0.1113553986120547346, 0.1328740156405045225 ) ) ;
#2630=EDGE_CURVE ( 'NONE', #12184, #12474, #42498, .T. ) ;
#2631=ORIENTED_EDGE ( 'NONE', *, *, #43981, .F. ) ;
#2632=CARTESIAN_POINT ( 'NONE',  ( 1.033464566929133799, 0.000000000000000000, 0.3937007872940480047 ) ) ;
#2636=CARTESIAN_POINT ( 'NONE',  ( -0.8019270111902717657, 0.1787899950787401604, 1.845472440891119392 ) ) ;
#2638=CARTESIAN_POINT ( 'NONE',  ( -1.054774247047244540, -0.07405724077823318263, 1.441929133804504604 ) ) ;
#2640=CARTESIAN_POINT ( 'NONE',  ( 1.002407869896990045, 0.1264236179284866091, 1.606791338528913426 ) ) ;
#2641=CARTESIAN_POINT ( 'NONE',  ( 0.7646288533564489232, -0.1113553986120547346, 0.9301181101286929431 ) ) ;
#2642=CARTESIAN_POINT ( 'NONE',  ( -1.002407869896990045, -0.1264236179284866091, 0.6126968503399370380 ) ) ;
#2643=CARTESIAN_POINT ( 'NONE',  ( 0.7495606340400177148, -0.1264236179284866091, 0.1304133857730082613 ) ) ;
#2646=CARTESIAN_POINT ( 'NONE',  ( 0.8019270111902716547, 0.1787899950787401604, 0.6692913385289143147 ) ) ;
#2647=CARTESIAN_POINT ( 'NONE',  ( -0.8759842519685039353, 0.1787899950787401882, 0.5831692912848189803 ) ) ;
#2648=CARTESIAN_POINT ( 'NONE',  ( 0.7646288533564489232, -0.1113553986120547346, 0.6250000000000000000 ) ) ;
#2649=CARTESIAN_POINT ( 'NONE',  ( -0.7185039370078739607, 1.928577636452523993E-17, 0.8562992125984251190 ) ) ;
#2651=CARTESIAN_POINT ( 'NONE',  ( -1.002407869896990045, 0.1264236179284866091, 1.409940944828126153 ) ) ;
#2653=VECTOR ( 'NONE', #15346, 39.37007874015748143 ) ;
#2654=CARTESIAN_POINT ( 'NONE',  ( -0.9873396505805591694, 0.1113553986120547346, 1.471456692913385877 ) ) ;
#2655=CARTESIAN_POINT ( 'NONE',  ( -0.7185039370078739607, 1.928577636452523993E-17, 0.4232283464566928832 ) ) ;
#2656=CARTESIAN_POINT ( 'NONE',  ( 1.002407869896990045, -0.1264236179284866091, 1.281988188922614125 ) ) ;
#2658=VECTOR ( 'NONE', #14061, 39.37007874015748143 ) ;
#2666=CARTESIAN_POINT ( 'NONE',  ( 0.8759842519685039353, -0.1787899950787401882, 1.429625984198204858 ) ) ;
#2667=CARTESIAN_POINT ( 'NONE',  ( -0.8759842519685039353, 0.000000000000000000, 0.000000000000000000 ) ) ;
#2669=CARTESIAN_POINT ( 'NONE',  ( 0.8107537697050254399, 0.1574803149606300301, 1.045767716535432879 ) ) ;
#2671=CARTESIAN_POINT ( 'NONE',  ( 1.054774247047244540, -0.07405724077823318263, 0.3346456692375748831 ) ) ;
#2674=CARTESIAN_POINT ( 'NONE',  ( -0.8759842519685039353, 0.000000000000000000, 0.000000000000000000 ) ) ;
#2677=CARTESIAN_POINT ( 'NONE',  ( 1.054774247047244540, -0.07405724077823318263, 0.5314960629383620461 ) ) ;
#2678=CARTESIAN_POINT ( 'NONE',  ( -1.002407869896990045, 0.1264236179284866091, 0.8193897637257637756 ) ) ;
#2680=DIRECTION ( 'NONE',  ( 1.822029033848725028E-16, 0.000000000000000000, 1.000000000000000000 ) ) ;
#2686=CARTESIAN_POINT ( 'NONE',  ( -1.033464566929133799, 0.000000000000000000, 1.259842519577511810 ) ) ;
#2687=CARTESIAN_POINT ( 'NONE',  ( 0.8019270111902717657, 0.1787899950787401604, 1.732283464513166615 ) ) ;
#2688=CARTESIAN_POINT ( 'NONE',  ( 0.9500414927467377701, -0.1787899950787401604, 1.943897637741510254 ) ) ;
#2690=CARTESIAN_POINT ( 'NONE',  ( 0.6971942568897637749, 2.189545951927499583E-17, 0.3567913385289137596 ) ) ;
#2691=AXIS2_PLACEMENT_3D ( 'NONE', #28111, #2436, #1734 ) ;
#2696=CARTESIAN_POINT ( 'NONE',  ( 1.054774247047244540, -0.07405724077823318263, 0.5708661416785201226 ) ) ;
#2702=ORIENTED_EDGE ( 'NONE', *, *, #7149, .T. ) ;
#2703=CARTESIAN_POINT ( 'NONE',  ( 0.7185039370078739607, 1.928577636452523993E-17, 0.1476377952755905387 ) ) ;
#2704=CARTESIAN_POINT ( 'NONE',  ( 1.002407869896990045, -0.1264236179284866091, 1.203248031442299304 ) ) ;
#2706=CARTESIAN_POINT ( 'NONE',  ( -0.8107537697050253289, 0.1574803149606300301, 0.6815944880814486240 ) ) ;
#2707=CARTESIAN_POINT ( 'NONE',  ( 0.8759842519685039353, 0.1787899950787401882, 1.882381889710015743 ) ) ;
#2708=CARTESIAN_POINT ( 'NONE',  ( -1.033464566929133799, 0.000000000000000000, 1.427165354330708569 ) ) ;
#2709=CARTESIAN_POINT ( 'NONE',  ( -0.7495606340400177148, 0.1264236179284866091, 0.8636811023084409733 ) ) ;
#2713=CARTESIAN_POINT ( 'NONE',  ( 0.7495606340400177148, 0.1264236179284866091, 0.1599409448281264023 ) ) ;
#2714=CARTESIAN_POINT ( 'NONE',  ( 0.8107537697050253289, -0.1574803149606297803, 1.601870078632630756 ) ) ;
#2717=CARTESIAN_POINT ( 'NONE',  ( -0.8019270111902716547, -0.1787899950787401604, 1.702755905458047003 ) ) ;
#2718=DIRECTION ( 'NONE',  ( 1.822029033848725028E-16, 0.000000000000000000, 1.000000000000000000 ) ) ;
#2723=CIRCLE ( 'NONE', #21903, 0.5019685039370077595 ) ;
#2729=CARTESIAN_POINT ( 'NONE',  ( 0.8107537697050253289, 0.1574803149606300301, 1.911909448818899238 ) ) ;
#2730=ORIENTED_EDGE ( 'NONE', *, *, #11013, .T. ) ;
#2731=CARTESIAN_POINT ( 'NONE',  ( -1.054774247047244540, 0.07405724077823318263, 0.3051181101824569919 ) ) ;
#2734=CARTESIAN_POINT ( 'NONE',  ( 0.8019270111902716547, 0.1787899950787401604, 1.491141732229701145 ) ) ;
#2736=CARTESIAN_POINT ( 'NONE',  ( -0.8107537697050254399, 0.1574803149606300301, 1.911909448818897017 ) ) ;
#2739=CARTESIAN_POINT ( 'NONE',  ( 0.9873396505805591694, 0.1113553986120547346, 1.707677165354330562 ) ) ;
#2741=CARTESIAN_POINT ( 'NONE',  ( -0.9412147342319837628, -0.1574803149606297803, 1.685531495955465697 ) ) ;
#2743=CARTESIAN_POINT ( 'NONE',  ( 0.8759842519685039353, 0.1787899950787401882, 0.1894685038832444879 ) ) ;
#2744=( BOUNDED_CURVE ( )  B_SPLINE_CURVE ( 2, ( #47341, #3720, #40821, #3486, #43729, #15003, #29654, #18101, #33458 ),
 .UNSPECIFIED., .F., .T. ) 
 B_SPLINE_CURVE_WITH_KNOTS ( ( 3, 2, 2, 2, 3 ),
 ( 0.5300000000000000266, 0.5324999999999999734, 0.5350000000000000311, 0.5374999999999999778, 0.5400000000000000355 ),
 .UNSPECIFIED. ) 
 CURVE ( )  GEOMETRIC_REPRESENTATION_ITEM ( )  RATIONAL_B_SPLINE_CURVE ( ( 1.000000000000000000, 0.9238795325112869605, 1.000000000000000000, 0.9238795325112869605, 1.000000000000000000, 0.9238795325112869605, 1.000000000000000000, 0.9238795325112869605, 1.000000000000000000 ) ) 
 REPRESENTATION_ITEM ( '' )  ) ;
#2745=FACE_OUTER_BOUND ( 'NONE', #47152, .T. ) ;
#2747=CARTESIAN_POINT ( 'NONE',  ( 0.8019270111902716547, 0.1787899950787401604, 1.176181102308441195 ) ) ;
#2748=CARTESIAN_POINT ( 'NONE',  ( -0.8759842519685039353, 0.1574803149606299191, 1.948818897637795367 ) ) ;
#2749=CARTESIAN_POINT ( 'NONE',  ( 0.6971942568897648851, -0.07405724077823297447, 1.978346456639149098 ) ) ;
#2750=CARTESIAN_POINT ( 'NONE',  ( 0.7185039370078746268, -0.06523048226347956391, 0.5733267715460159675 ) ) ;
#2752=CARTESIAN_POINT ( 'NONE',  ( 1.033464566929133799, 1.928577636452524610E-17, 4.498031496062992574 ) ) ;
#2753=CARTESIAN_POINT ( 'NONE',  ( 1.024574034319794436, 0.06442505785855824618, 0.03937402314509768492 ) ) ;
#2754=CIRCLE ( 'NONE', #29619, 0.1574803149606299191 ) ;
#2756=CARTESIAN_POINT ( 'NONE',  ( -1.033464566929134687, -0.06523048226347956391, 0.3518700786326304231 ) ) ;
#2757=VERTEX_POINT ( 'NONE', #40689 ) ;
#2758=CARTESIAN_POINT ( 'NONE',  ( 0.8759842519685039353, -0.1787899950787401882, 1.429625984198204858 ) ) ;
#2759=CARTESIAN_POINT ( 'NONE',  ( -0.7646288533564489232, -0.1113553986120547346, 1.766732283464566899 ) ) ;
#2762=CARTESIAN_POINT ( 'NONE',  ( 0.8107537697050254399, 0.1574803149606300301, 0.7308070866141727073 ) ) ;
#2765=LINE ( 'NONE', #46619, #44483 ) ;
#2766=VERTEX_POINT ( 'NONE', #7882 ) ;
#2767=CARTESIAN_POINT ( 'NONE',  ( 0.6971942568897626646, -0.07405724077823297447, 0.4035433070328508509 ) ) ;
#2769=CARTESIAN_POINT ( 'NONE',  ( -0.7495606340400177148, -0.1264236179284866091, 1.424704724355685181 ) ) ;
#2771=CARTESIAN_POINT ( 'NONE',  ( -1.054774247047244096, 0.000000000000000000, 0.9325787401037164415 ) ) ;
#2772=CARTESIAN_POINT ( 'NONE',  ( -1.002407869896990045, -0.1264236179284866091, 1.985728346402929168 ) ) ;
#2773=ORIENTED_EDGE ( 'NONE', *, *, #9440, .F. ) ;
#2774=CARTESIAN_POINT ( 'NONE',  ( -0.8019270111902716547, 0.1787899950787401604, 1.018700787347811110 ) ) ;
#2775=CARTESIAN_POINT ( 'NONE',  ( -1.054774247047244096, 0.000000000000000000, 0.6176181101824566033 ) ) ;
#2779=CARTESIAN_POINT ( 'NONE',  ( -0.7646288533564489232, 0.1113553986120547346, 0.06397637795275590289 ) ) ;
#2780=VERTEX_POINT ( 'NONE', #27079 ) ;
#2781=CARTESIAN_POINT ( 'NONE',  ( -0.7646288533564489232, -0.1113553986120547346, 0.3395669290263311213 ) ) ;
#2782=DIRECTION ( 'NONE',  ( 1.822029033848725028E-16, 0.000000000000000000, 1.000000000000000000 ) ) ;
#2784=CARTESIAN_POINT ( 'NONE',  ( -0.9500414927467378812, -0.1787899950787401604, 0.6840551180564720113 ) ) ;
#2785=LINE ( 'NONE', #46171, #32247 ) ;
#2786=ORIENTED_EDGE ( 'NONE', *, *, #1840, .F. ) ;
#2787=CARTESIAN_POINT ( 'NONE',  ( -0.8759842519685039353, -0.1787899950787401882, 1.592027559001354398 ) ) ;
#2789=CARTESIAN_POINT ( 'NONE',  ( -1.033464566929134687, 0.06523048226347956391, 0.4847440944881890590 ) ) ;
#2792=CARTESIAN_POINT ( 'NONE',  ( 0.7646288533564489232, 0.1113553986120547346, 0.6446850392625511628 ) ) ;
#2793=CARTESIAN_POINT ( 'NONE',  ( -1.033464566929134687, -0.06523048226347956391, 1.414862204616882835 ) ) ;
#2796=DIRECTION ( 'NONE',  ( 0.000000000000000000, 0.000000000000000000, -1.000000000000000000 ) ) ;
#2797=CARTESIAN_POINT ( 'NONE',  ( 0.7646288533564489232, -0.1113553986120547346, 1.294291338582677309 ) ) ;
#2798=CARTESIAN_POINT ( 'NONE',  ( -1.033464566929133799, 1.928577636452524610E-17, 2.869337061179095023E-17 ) ) ;
#2800=CARTESIAN_POINT ( 'NONE',  ( 0.9873396505805591694, -0.1113553986120547346, 1.973425196850393970 ) ) ;
#2803=CARTESIAN_POINT ( 'NONE',  ( 1.054774247047244540, -0.07405724077823318263, 0.6889763778989936860 ) ) ;
#2809=CARTESIAN_POINT ( 'NONE',  ( 1.033464566929133799, 0.000000000000000000, 1.742125984251968518 ) ) ;
#2811=CARTESIAN_POINT ( 'NONE',  ( 0.9500414927467378812, 0.1787899950787401604, 0.8956692912848198684 ) ) ;
#2812=CARTESIAN_POINT ( 'NONE',  ( 1.033464566929133799, 0.000000000000000000, 1.466535433070866201 ) ) ;
#2818=CARTESIAN_POINT ( 'NONE',  ( -0.8759842519685039353, 0.1787899950787401882, 1.966043307032850462 ) ) ;
#2819=CARTESIAN_POINT ( 'NONE',  ( 0.9500414927467378812, 0.1787899950787401604, 1.924212598371433325 ) ) ;
#2822=CARTESIAN_POINT ( 'NONE',  ( -1.002407869896990045, 0.1264236179284866091, 1.882381889710015743 ) ) ;
#2823=CARTESIAN_POINT ( 'NONE',  ( -0.6971942568897637749, 2.189545951927499583E-17, 1.577263779473795369 ) ) ;
#2824=CARTESIAN_POINT ( 'NONE',  ( -0.8759842519685039353, -0.1787899950787401882, 0.2534448818360003908 ) ) ;
#2825=DIRECTION ( 'NONE',  ( 0.000000000000000000, 0.000000000000000000, -1.000000000000000000 ) ) ;
#2826=CARTESIAN_POINT ( 'NONE',  ( -1.002407869896990045, -0.1264236179284866091, 1.951279527505291433 ) ) ;
#2827=CARTESIAN_POINT ( 'NONE',  ( -1.054774247047244096, 0.000000000000000000, 0.1451771653005673179 ) ) ;
#2828=CARTESIAN_POINT ( 'NONE',  ( -0.9412147342319837628, 0.1574803149606300301, 1.867618110236221707 ) ) ;
#2832=CARTESIAN_POINT ( 'NONE',  ( 0.8759842519685039353, 0.000000000000000000, 4.498031496062992574 ) ) ;
#2833=CARTESIAN_POINT ( 'NONE',  ( -0.8759842519685039353, -0.1787899950787401882, 0.1304133857730082613 ) ) ;
#2835=CARTESIAN_POINT ( 'NONE',  ( -0.9500414927467377701, -0.1787899950787401604, 1.279527559001355730 ) ) ;
#2841=( NAMED_UNIT ( * ) SI_UNIT ( $, .STERADIAN. ) SOLID_ANGLE_UNIT ( ) ) ;
#2843=CARTESIAN_POINT ( 'NONE',  ( -0.8759842519685039353, 0.000000000000000000, 0.03937007874015843040 ) ) ;
#2844=CARTESIAN_POINT ( 'NONE',  ( -0.8759842519685039353, 0.1574803149606299191, 0.7283464566929134243 ) ) ;
#2846=CARTESIAN_POINT ( 'NONE',  ( 0.7185039370078739607, 1.928577636452523993E-17, 1.791338582569637738 ) ) ;
#2847=ORIENTED_EDGE ( 'NONE', *, *, #23390, .T. ) ;
#2848=CARTESIAN_POINT ( 'NONE',  ( 0.7646288533564489232, 0.1113553986120547346, 0.7332677165354331006 ) ) ;
#2850=CARTESIAN_POINT ( 'NONE',  ( -1.033464566929133799, 0.000000000000000000, 1.614173228238929170 ) ) ;
#2851=( BOUNDED_CURVE ( )  B_SPLINE_CURVE ( 2, ( #38158, #30306, #27652, #42208, #1251, #38633, #19938, #8685, #37934 ),
 .UNSPECIFIED., .F., .T. ) 
 B_SPLINE_CURVE_WITH_KNOTS ( ( 3, 2, 2, 2, 3 ),
 ( 0.02999999999999999889, 0.03250000000000000111, 0.03500000000000000333, 0.03749999999999999861, 0.04000000000000000083 ),
 .UNSPECIFIED. ) 
 CURVE ( )  GEOMETRIC_REPRESENTATION_ITEM ( )  RATIONAL_B_SPLINE_CURVE ( ( 1.000000000000000000, 0.9238795325112869605, 1.000000000000000000, 0.9238795325112869605, 1.000000000000000000, 0.9238795325112869605, 1.000000000000000000, 0.9238795325112869605, 1.000000000000000000 ) ) 
 REPRESENTATION_ITEM ( '' )  ) ;
#2852=DIRECTION ( 'NONE',  ( 0.000000000000000000, 0.000000000000000000, -1.000000000000000000 ) ) ;
#2854=CARTESIAN_POINT ( 'NONE',  ( 0.8759842519685039353, -0.1574803149606299191, 0.1082677164279060994 ) ) ;
#2856=ORIENTED_EDGE ( 'NONE', *, *, #40837, .F. ) ;
#2857=CYLINDRICAL_SURFACE ( 'NONE', #40098, 0.1574803149606299191 ) ;
#2858=CARTESIAN_POINT ( 'NONE',  ( -0.7661220286720177297, 0.1429759811008071424, 0.03937007874015843040 ) ) ;
#2862=CARTESIAN_POINT ( 'NONE',  ( 0.8107537697050253289, 0.1574803149606300301, 0.8784448817822366751 ) ) ;
#2863=CARTESIAN_POINT ( 'NONE',  ( 1.033464566929134687, 0.06523048226347956391, 0.5241141732283461918 ) ) ;
#2864=CARTESIAN_POINT ( 'NONE',  ( -0.6971942568897626646, -0.07405724077823297447, 0.3986220471903312301 ) ) ;
#2865=ORIENTED_EDGE ( 'NONE', *, *, #33136, .F. ) ;
#2868=CARTESIAN_POINT ( 'NONE',  ( -0.8759842519685039353, -0.1787899950787401882, 1.473917322780881722 ) ) ;
#2869=CARTESIAN_POINT ( 'NONE',  ( 0.8759842519685039353, 0.1787899950787401882, 1.572342519631275692 ) ) ;
#2870=VERTEX_POINT ( 'NONE', #40346 ) ;
#2871=CARTESIAN_POINT ( 'NONE',  ( 0.9873396505805591694, -0.1113553986120547346, 0.9399606298137322957 ) ) ;
#2872=CARTESIAN_POINT ( 'NONE',  ( -1.054774247047244540, 0.07405724077823318263, 0.6200787401037165525 ) ) ;
#2874=CARTESIAN_POINT ( 'NONE',  ( 0.8019270111902716547, 0.1787899950787401604, 0.7480314960092282472 ) ) ;
#2875=DIRECTION ( 'NONE',  ( -1.000000000000000000, 0.000000000000000000, 0.000000000000000000 ) ) ;
#2876=CARTESIAN_POINT ( 'NONE',  ( 0.8759842519685039353, 0.1574803149606299191, 1.072834645561763889 ) ) ;
#2878=CARTESIAN_POINT ( 'NONE',  ( -0.9500414927467378812, -0.1787899950787401604, 1.397637795221827295 ) ) ;
#2879=DIRECTION ( 'NONE',  ( 1.822029033848725028E-16, 0.000000000000000000, 1.000000000000000000 ) ) ;
#2880=CARTESIAN_POINT ( 'NONE',  ( -0.8107537697050253289, 0.1574803149606300301, 0.4945866141732282451 ) ) ;
#2881=CARTESIAN_POINT ( 'NONE',  ( 0.8759842519685039353, -0.1787899950787401882, 1.355807086560409491 ) ) ;
#2883=ORIENTED_EDGE ( 'NONE', *, *, #45099, .T. ) ;
#2884=CARTESIAN_POINT ( 'NONE',  ( -0.9412147342319837628, -0.1574803149606297803, 0.5536417322834641386 ) ) ;
#2887=CARTESIAN_POINT ( 'NONE',  ( 0.8107537697050254399, -0.1574803149606297803, 0.3912401574803148208 ) ) ;
#2889=CARTESIAN_POINT ( 'NONE',  ( 0.8019270111902717657, 0.1787899950787401604, 1.451771653489543290 ) ) ;
#2892=VECTOR ( 'NONE', #27863, 39.37007874015748143 ) ;
#2894=EDGE_CURVE ( 'NONE', #41647, #34447, #13153, .T. ) ;
#2898=CARTESIAN_POINT ( 'NONE',  ( 0.8019270111902717657, -0.1787899950787401604, 0.2854330708123783422 ) ) ;
#2899=EDGE_CURVE ( 'NONE', #33124, #34176, #36831, .T. ) ;
#2903=DIRECTION ( 'NONE',  ( 1.822029033848725028E-16, 0.000000000000000000, 1.000000000000000000 ) ) ;
#2906=CARTESIAN_POINT ( 'NONE',  ( 0.6971942568897637749, 2.189545951927499583E-17, 0.5536417322297008115 ) ) ;
#2907=CARTESIAN_POINT ( 'NONE',  ( -0.7495606340400177148, 0.1264236179284866091, 1.026082677111590513 ) ) ;
#2909=CARTESIAN_POINT ( 'NONE',  ( 1.033464566929133799, 1.928577636452524610E-17, 4.498031496062992574 ) ) ;
#2911=CARTESIAN_POINT ( 'NONE',  ( -0.8817724199485534875, -0.1746201713974357972, 1.988283497529828914 ) ) ;
#2912=CARTESIAN_POINT ( 'NONE',  ( -0.8759842519685039353, 0.000000000000000000, 1.990649606245448844 ) ) ;
#2913=CARTESIAN_POINT ( 'NONE',  ( 0.6971942568897637749, 2.189545951927499583E-17, 1.660925196796630088 ) ) ;
#2916=ORIENTED_EDGE ( 'NONE', *, *, #24893, .F. ) ;
#2921=CARTESIAN_POINT ( 'NONE',  ( 0.8019270111902717657, -0.1787899950787401604, 0.6003937007336380693 ) ) ;
#2923=CARTESIAN_POINT ( 'NONE',  ( 0.8759842519685039353, -0.1787899950787401882, 0.05659448813521291560 ) ) ;
#2924=CARTESIAN_POINT ( 'NONE',  ( 0.6971942568897648851, 0.07405724077823318263, 0.5511811023084406402 ) ) ;
#2927=CARTESIAN_POINT ( 'NONE',  ( 0.7495606340400177148, 0.1264236179284866091, 1.104822834591905556 ) ) ;
#2929=CARTESIAN_POINT ( 'NONE',  ( -1.033464566929134687, 0.06523048226347956391, 0.7111220471365681250 ) ) ;
#2930=CARTESIAN_POINT ( 'NONE',  ( 0.8019270111902717657, -0.1787899950787401604, 1.781496062938362934 ) ) ;
#2931=CARTESIAN_POINT ( 'NONE',  ( -0.9412147342319837628, -0.1574803149606297803, 1.341043307086615455 ) ) ;
#2932=CARTESIAN_POINT ( 'NONE',  ( -1.002407869896990045, -0.1264236179284866091, 0.8439960629383622681 ) ) ;
#2934=CARTESIAN_POINT ( 'NONE',  ( -0.7046433452555540544, -0.02693604437337100005, 0.03937007874015843040 ) ) ;
#2935=CARTESIAN_POINT ( 'NONE',  ( 0.9500414927467377701, -0.1787899950787401604, 0.3740157479777325711 ) ) ;
#2937=CARTESIAN_POINT ( 'NONE',  ( -0.8019270111902717657, 0.1787899950787401604, 0.5462598424659214080 ) ) ;
#2938=CARTESIAN_POINT ( 'NONE',  ( 0.9412147342319837628, -0.1574803149606297803, 1.528051180994836056 ) ) ;
#2939=ORIENTED_EDGE ( 'NONE', *, *, #6637, .T. ) ;
#2943=EDGE_LOOP ( 'NONE', ( #18676, #32852, #16050, #18806 ) ) ;
#2945=CARTESIAN_POINT ( 'NONE',  ( 0.6971942568897637749, 2.189545951927499583E-17, 0.8341535432533228045 ) ) ;
#2946=CARTESIAN_POINT ( 'NONE',  ( -1.002407869896990045, 0.1264236179284866091, 1.719980314906866203 ) ) ;
#2948=CARTESIAN_POINT ( 'NONE',  ( -0.7646288533564489232, 0.1113553986120547346, 0.6545275590551181688 ) ) ;
#2953=VERTEX_POINT ( 'NONE', #22870 ) ;
#2954=CARTESIAN_POINT ( 'NONE',  ( 0.8019270111902717657, 0.1787899950787401604, 1.097440944828127041 ) ) ;
#2956=CARTESIAN_POINT ( 'NONE',  ( -0.9412147342319837628, 0.1574803149606300301, 0.9916338581601894520 ) ) ;
#2959=CARTESIAN_POINT ( 'NONE',  ( 0.9500414927467378812, -0.1787899950787401604, 0.05413385821395302888 ) ) ;
#2963=EDGE_CURVE ( 'NONE', #28992, #31452, #45863, .T. ) ;
#2964=CARTESIAN_POINT ( 'NONE',  ( -1.054774247047244096, 0.000000000000000000, 0.3813976377415121966 ) ) ;
#2967=CARTESIAN_POINT ( 'NONE',  ( 0.8759842519685039353, -0.1787899950787401882, 1.237696850339937038 ) ) ;
#2969=CARTESIAN_POINT ( 'NONE',  ( 0.9500414927467377701, 0.1787899950787401604, 1.525590551127339989 ) ) ;
#2970=CARTESIAN_POINT ( 'NONE',  ( 0.6971942568897626646, 0.07405724077823318263, 0.1968503936470238636 ) ) ;
#2972=CARTESIAN_POINT ( 'NONE',  ( 1.033464566929134687, 0.06523048226347956391, 1.705216535433070613 ) ) ;
#2974=CARTESIAN_POINT ( 'NONE',  ( 0.8759842519685039353, -0.1574803149606299191, 1.446850393593259732 ) ) ;
#2975=CARTESIAN_POINT ( 'NONE',  ( 0.7185039370078746268, -0.06523048226347956391, 0.7701771652468031304 ) ) ;
#2976=CARTESIAN_POINT ( 'NONE',  ( -0.7185039370078739607, 1.928577636452523993E-17, 1.751968503829480106 ) ) ;
#2978=CARTESIAN_POINT ( 'NONE',  ( 0.6971942568897626646, 0.07405724077823318263, 0.1968503936470238913 ) ) ;
#2979=CARTESIAN_POINT ( 'NONE',  ( 0.7033435294390766312, 0.03857964621150825751, 0.03937085465571968368 ) ) ;
#2980=CARTESIAN_POINT ( 'NONE',  ( 1.002407869896990045, 0.1264236179284866091, 1.168799212544661348 ) ) ;
#2981=CARTESIAN_POINT ( 'NONE',  ( -0.9873396505805591694, 0.1113553986120547346, 1.815944881782236120 ) ) ;
#2982=CARTESIAN_POINT ( 'NONE',  ( -0.7185039370078739607, 1.928577636452523993E-17, 1.368110236220472675 ) ) ;
#2983=CARTESIAN_POINT ( 'NONE',  ( 0.7646288533564489232, -0.1113553986120547346, 0.4970472439869613734 ) ) ;
#2985=CARTESIAN_POINT ( 'NONE',  ( -1.002407869896990045, -0.1264236179284866091, 1.045767716481669440 ) ) ;
#2986=DIRECTION ( 'NONE',  ( 1.822029033848725028E-16, 0.000000000000000000, 1.000000000000000000 ) ) ;
#2987=CARTESIAN_POINT ( 'NONE',  ( 0.9662619894878454740, 0.1420933317043502342, 0.03937004641417764239 ) ) ;
#2988=CARTESIAN_POINT ( 'NONE',  ( -1.033464566929133799, 0.000000000000000000, 0.3543307085538902057 ) ) ;
#2990=CARTESIAN_POINT ( 'NONE',  ( 1.054774247047244096, 0.000000000000000000, 1.518208661363559031 ) ) ;
#2991=CYLINDRICAL_SURFACE ( 'NONE', #16263, 0.1574803149606299191 ) ;
#2994=DIRECTION ( 'NONE',  ( 1.000000000000000000, 0.000000000000000000, -1.822029033848725275E-16 ) ) ;
#2995=VECTOR ( 'NONE', #35727, 39.37007874015748143 ) ;
#2996=ORIENTED_EDGE ( 'NONE', *, *, #28580, .T. ) ;
#2999=CARTESIAN_POINT ( 'NONE',  ( 0.9500414927467378812, 0.1787899950787401604, 0.5462598424659214080 ) ) ;
#3001=CARTESIAN_POINT ( 'NONE',  ( -0.6971942568897637749, 2.189545951927499583E-17, 1.341043307032850462 ) ) ;
#3003=CARTESIAN_POINT ( 'NONE',  ( -0.6971942568897648851, 0.07405724077823318263, 1.186023621993481658 ) ) ;
#3004=CARTESIAN_POINT ( 'NONE',  ( -1.002407869896990045, 0.1264236179284866091, 1.090059055064346527 ) ) ;
#3006=CARTESIAN_POINT ( 'NONE',  ( -0.9500414927467378812, -0.1787899950787401604, 0.7677165353793073965 ) ) ;
#3007=( BOUNDED_CURVE ( )  B_SPLINE_CURVE ( 2, ( #47135, #40159, #37052, #29453, #7115, #3525, #25815, #10736, #18835 ),
 .UNSPECIFIED., .F., .T. ) 
 B_SPLINE_CURVE_WITH_KNOTS ( ( 3, 2, 2, 2, 3 ),
 ( 0.1799999999999999933, 0.1824999999999999956, 0.1849999999999999978, 0.1875000000000000000, 0.1900000000000000022 ),
 .UNSPECIFIED. ) 
 CURVE ( )  GEOMETRIC_REPRESENTATION_ITEM ( )  RATIONAL_B_SPLINE_CURVE ( ( 1.000000000000000000, 0.9238795325112869605, 1.000000000000000000, 0.9238795325112869605, 1.000000000000000000, 0.9238795325112869605, 1.000000000000000000, 0.9238795325112869605, 1.000000000000000000 ) ) 
 REPRESENTATION_ITEM ( '' )  ) ;
#3008=CARTESIAN_POINT ( 'NONE',  ( -1.054774247047244540, 0.07405724077823318263, 0.1476377952218269618 ) ) ;
#3009=CARTESIAN_POINT ( 'NONE',  ( -0.9873396505805591694, -0.1113553986120547346, 0.3592519685039369803 ) ) ;
#3015=CARTESIAN_POINT ( 'NONE',  ( 0.9412147342319837628, 0.1574803149606300301, 0.7652559055118115516 ) ) ;
#3017=CARTESIAN_POINT ( 'NONE',  ( -0.7495606340400177148, -0.1264236179284866091, 0.5585629920722204877 ) ) ;
#3020=CARTESIAN_POINT ( 'NONE',  ( -0.7495606340400177148, 0.1264236179284866091, 1.734744094434425232 ) ) ;
#3023=( BOUNDED_CURVE ( )  B_SPLINE_CURVE ( 2, ( #15187, #37209, #37688, #18989, #12062, #29835, #8680, #26924, #761 ),
 .UNSPECIFIED., .F., .F. ) 
 B_SPLINE_CURVE_WITH_KNOTS ( ( 3, 2, 2, 2, 3 ),
 ( 0.1499999999999999944, 0.1524999999999999967, 0.1549999999999999989, 0.1575000000000000011, 0.1600000000000000033 ),
 .UNSPECIFIED. ) 
 CURVE ( )  GEOMETRIC_REPRESENTATION_ITEM ( )  RATIONAL_B_SPLINE_CURVE ( ( 1.000000000000000000, 0.9238795325112869605, 1.000000000000000000, 0.9238795325112869605, 1.000000000000000000, 0.9238795325112869605, 1.000000000000000000, 0.9238795325112869605, 1.000000000000000000 ) ) 
 REPRESENTATION_ITEM ( '' )  ) ;
#3026=CARTESIAN_POINT ( 'NONE',  ( 1.033464566929134687, 0.06523048226347956391, 0.6422244094488180899 ) ) ;
#3027=CARTESIAN_POINT ( 'NONE',  ( 0.7646288533564489232, -0.1113553986120547346, 0.6250000000000000000 ) ) ;
#3030=CARTESIAN_POINT ( 'NONE',  ( -0.8107537697050253289, -0.1574803149606297803, 1.365649606191684295 ) ) ;
#3031=CARTESIAN_POINT ( 'NONE',  ( 0.8759842519685039353, -0.1787899950787401882, 0.8046259841982047467 ) ) ;
#3033=CARTESIAN_POINT ( 'NONE',  ( 1.033464566929134687, 0.06523048226347956391, 1.616633858160190229 ) ) ;
#3035=CARTESIAN_POINT ( 'NONE',  ( 1.033464566929134687, 0.06523048226347956391, 0.1599409447743626866 ) ) ;
#3036=CARTESIAN_POINT ( 'NONE',  ( 0.7185039370078746268, -0.06523048226347956391, 1.252460629921259061 ) ) ;
#3037=CARTESIAN_POINT ( 'NONE',  ( 0.7464489022532936335, -0.1098404454055766921, 1.985481321410791367 ) ) ;
#3038=CARTESIAN_POINT ( 'NONE',  ( 0.7185039370078739607, 0.000000000000000000, 4.498031496062992574 ) ) ;
#3040=CARTESIAN_POINT ( 'NONE',  ( 0.9412147342319837628, -0.1574803149606297803, 1.734744094488190003 ) ) ;
#3041=CARTESIAN_POINT ( 'NONE',  ( 0.7495606340400177148, 0.1264236179284866091, 0.6274606298674959559 ) ) ;
#3043=CARTESIAN_POINT ( 'NONE',  ( -0.7646288533564489232, -0.1113553986120547346, 0.3789370077664886427 ) ) ;
#3045=FACE_OUTER_BOUND ( 'NONE', #6887, .T. ) ;
#3047=CARTESIAN_POINT ( 'NONE',  ( 0.8019270111902717657, 0.1787899950787401604, 0.9793307086076531442 ) ) ;
#3048=CARTESIAN_POINT ( 'NONE',  ( 0.8759842519685039353, 0.1574803149606299191, 1.476377952755905554 ) ) ;
#3056=CARTESIAN_POINT ( 'NONE',  ( -0.8019270111902717657, -0.1787899950787401604, 0.1279527558517483676 ) ) ;
#3057=VERTEX_POINT ( 'NONE', #11156 ) ;
#3059=CARTESIAN_POINT ( 'NONE',  ( 1.054774247047244540, 0.07405724077823318263, 1.958661417269071947 ) ) ;
#3061=CARTESIAN_POINT ( 'NONE',  ( -0.8759842519685039353, -0.1787899950787401882, 1.946358267662771757 ) ) ;
#3062=CARTESIAN_POINT ( 'NONE',  ( -0.9500414927467378812, 0.1787899950787401604, 1.525590551127340433 ) ) ;
#3063=CARTESIAN_POINT ( 'NONE',  ( 0.8759842519685039353, -0.1787899950787401882, 0.8439960629383622681 ) ) ;
#3064=CARTESIAN_POINT ( 'NONE',  ( -0.7495606340400177148, 0.1264236179284866091, 0.8243110235682834519 ) ) ;
#3065=CARTESIAN_POINT ( 'NONE',  ( -0.8019270111902717657, 0.1787899950787401604, 0.3543307086076538659 ) ) ;
#3067=CARTESIAN_POINT ( 'NONE',  ( -0.8107537697050254399, -0.1574803149606297803, 0.6668307086614162493 ) ) ;
#3068=CARTESIAN_POINT ( 'NONE',  ( -1.002407869896990045, 0.1264236179284866091, 1.921751968450173376 ) ) ;
#3069=CARTESIAN_POINT ( 'NONE',  ( -1.033464566929134687, 0.06523048226347956391, 1.468996062992126150 ) ) ;
#3070=CARTESIAN_POINT ( 'NONE',  ( -0.9412147342319837628, -0.1574803149606297803, 1.852854330708662012 ) ) ;
#3073=EDGE_CURVE ( 'NONE', #43630, #31988, #3937, .T. ) ;
#3078=VECTOR ( 'NONE', #13038, 39.37007874015748143 ) ;
#3079=VECTOR ( 'NONE', #879, 39.37007874015748143 ) ;
#3080=CARTESIAN_POINT ( 'NONE',  ( -0.8019270111902717657, 0.1787899950787401604, 0.1131889763241894359 ) ) ;
#3082=VERTEX_POINT ( 'NONE', #40809 ) ;
#3084=CARTESIAN_POINT ( 'NONE',  ( -1.002407869896990045, -0.1264236179284866091, 1.203248031442299304 ) ) ;
#3085=ORIENTED_EDGE ( 'NONE', *, *, #10473, .F. ) ;
#3091=CARTESIAN_POINT ( 'NONE',  ( -0.7185039370078739607, 1.928577636452523993E-17, 0.8858267715460158565 ) ) ;
#3092=CARTESIAN_POINT ( 'NONE',  ( -0.9412147342319837628, 0.1574803149606300301, 0.7652559055118115516 ) ) ;
#3093=CARTESIAN_POINT ( 'NONE',  ( 1.054774247047244540, -0.07405724077823318263, 0.4183070865604097133 ) ) ;
#3095=CARTESIAN_POINT ( 'NONE',  ( 0.8107537697050253289, -0.1574803149606297803, 1.759350393593260842 ) ) ;
#3098=CARTESIAN_POINT ( 'NONE',  ( 0.7185039370078746268, 0.06523048226347956391, 0.8144685039370082036 ) ) ;
#3099=CARTESIAN_POINT ( 'NONE',  ( -0.7646288533564489232, 0.1113553986120547346, 1.087598425196850460 ) ) ;
#3100=AXIS2_PLACEMENT_3D ( 'NONE', #44837, #45313, #7327 ) ;
#3101=CARTESIAN_POINT ( 'NONE',  ( 0.8759842519685039353, 0.000000000000000000, 4.498031496062992574 ) ) ;
#3103=CARTESIAN_POINT ( 'NONE',  ( 0.8759842519685039353, 0.1574803149606299191, 0.1279527557979848462 ) ) ;
#3112=CARTESIAN_POINT ( 'NONE',  ( 0.7185039370078746268, -0.06523048226347956391, 1.045767716427905114 ) ) ;
#3114=VERTEX_POINT ( 'NONE', #14802 ) ;
#3115=CARTESIAN_POINT ( 'NONE',  ( -0.6971942568897637749, 2.189545951927499583E-17, 1.582185039316315045 ) ) ;
#3118=CARTESIAN_POINT ( 'NONE',  ( 1.002407869896990045, -0.1264236179284866091, 1.596948818843874074 ) ) ;
#3120=CARTESIAN_POINT ( 'NONE',  ( -0.7495606340400177148, 0.1264236179284866091, 0.6323818897100157432 ) ) ;
#3122=CARTESIAN_POINT ( 'NONE',  ( -0.7185039370078746268, -0.06523048226347956391, 0.4552165353255435698 ) ) ;
#3123=CARTESIAN_POINT ( 'NONE',  ( -1.054774247047244540, 0.07405724077823318263, 0.7332677164816705506 ) ) ;
#3127=CARTESIAN_POINT ( 'NONE',  ( -0.8019270111902717657, 0.1787899950787401604, 1.417322834591906222 ) ) ;
#3130=CARTESIAN_POINT ( 'NONE',  ( -0.7185039370078739607, 1.928577636452523993E-17, 0.3838582677165354173 ) ) ;
#3132=CARTESIAN_POINT ( 'NONE',  ( 0.8019270111902716547, 0.1787899950787401604, 1.456692913332062522 ) ) ;
#3134=CARTESIAN_POINT ( 'NONE',  ( -0.8759842519685039353, 0.1574803149606299191, 0.3641732282389295583 ) ) ;
#3138=ORIENTED_EDGE ( 'NONE', *, *, #37885, .T. ) ;
#3139=CARTESIAN_POINT ( 'NONE',  ( 0.7495606340400177148, 0.1264236179284866091, 1.454232283410803017 ) ) ;
#3143=DIRECTION ( 'NONE',  ( 1.822029033848725028E-16, 0.000000000000000000, 1.000000000000000000 ) ) ;
#3145=( BOUNDED_CURVE ( )  B_SPLINE_CURVE ( 2, ( #34490, #30682, #4272, #11747, #44297, #8362, #41638, #37851, #41399 ),
 .UNSPECIFIED., .F., .T. ) 
 B_SPLINE_CURVE_WITH_KNOTS ( ( 3, 2, 2, 2, 3 ),
 ( 0.8800000000000000044, 0.8824999999999999512, 0.8850000000000000089, 0.8874999999999999556, 0.8900000000000000133 ),
 .UNSPECIFIED. ) 
 CURVE ( )  GEOMETRIC_REPRESENTATION_ITEM ( )  RATIONAL_B_SPLINE_CURVE ( ( 1.000000000000000000, 0.9238795325112869605, 1.000000000000000000, 0.9238795325112869605, 1.000000000000000000, 0.9238795325112869605, 1.000000000000000000, 0.9238795325112829637, 1.000000000000000000 ) ) 
 REPRESENTATION_ITEM ( '' )  ) ;
#3147=ADVANCED_FACE ( 'NONE', ( #18842 ), #8057, .T. ) ;
#3150=CARTESIAN_POINT ( 'NONE',  ( 0.8019270111902717657, 0.1787899950787401604, 0.3494094487651343006 ) ) ;
#3154=CARTESIAN_POINT ( 'NONE',  ( -0.8759842519685039353, -0.1574803149606299191, 1.692913385826771533 ) ) ;
#3155=CARTESIAN_POINT ( 'NONE',  ( 0.8759842519685039353, -0.1787899950787401882, 0.5634842519147401640 ) ) ;
#3156=CARTESIAN_POINT ( 'NONE',  ( -1.002407869896990045, 0.1264236179284866091, 0.9768700786863937502 ) ) ;
#3157=CARTESIAN_POINT ( 'NONE',  ( -0.9761154771909834604, 0.1345094614233016683, 0.03937007874015843734 ) ) ;
#3160=DIRECTION ( 'NONE',  ( -1.000000000000000000, 0.000000000000000000, 0.000000000000000000 ) ) ;
#3161=CARTESIAN_POINT ( 'NONE',  ( 0.7495606340400177148, -0.1264236179284866091, 1.665846456639149764 ) ) ;
#3162=CARTESIAN_POINT ( 'NONE',  ( 1.054774247047244540, -0.07405724077823318263, 1.948818897584033705 ) ) ;
#3167=CARTESIAN_POINT ( 'NONE',  ( 0.6971942568897626646, 0.07405724077823318263, 0.6692913385289144257 ) ) ;
#3169=CARTESIAN_POINT ( 'NONE',  ( 0.9500414927467378812, -0.1787899950787401604, 0.09842519679663024046 ) ) ;
#3172=CARTESIAN_POINT ( 'NONE',  ( -0.8759842519685039353, -0.1787899950787401882, 1.626476377898992132 ) ) ;
#3174=CARTESIAN_POINT ( 'NONE',  ( -0.7495606340400177148, 0.1264236179284866091, 1.104822834591905556 ) ) ;
#3176=CARTESIAN_POINT ( 'NONE',  ( 0.8759842519685039353, 0.1787899950787401882, 1.099901574749385880 ) ) ;
#3178=CARTESIAN_POINT ( 'NONE',  ( -0.9873396505805591694, 0.1113553986120547346, 0.6742125983176693316 ) ) ;
#3180=CARTESIAN_POINT ( 'NONE',  ( 0.8759842519685039353, -0.1787899950787401882, 1.862696850339937038 ) ) ;
#3181=CARTESIAN_POINT ( 'NONE',  ( -0.8107537697050253289, 0.1574803149606300301, 0.5733267716535435099 ) ) ;
#3182=CARTESIAN_POINT ( 'NONE',  ( -1.054774247047244540, 0.07405724077823318263, 0.8513779527021426707 ) ) ;
#3186=CARTESIAN_POINT ( 'NONE',  ( 0.9500414927467377701, -0.1787899950787401604, 0.2952755904974176948 ) ) ;
#3187=CARTESIAN_POINT ( 'NONE',  ( -0.8759842519685039353, -0.1787899950787401882, 0.2091535432533232486 ) ) ;
#3188=CARTESIAN_POINT ( 'NONE',  ( -1.002407869896990045, -0.1264236179284866091, 0.5684055117572598403 ) ) ;
#3189=CARTESIAN_POINT ( 'NONE',  ( 0.9873396505805591694, 0.1113553986120547346, 1.500984251860976171 ) ) ;
#3190=ORIENTED_EDGE ( 'NONE', *, *, #36320, .T. ) ;
#3193=ORIENTED_EDGE ( 'NONE', *, *, #21733, .T. ) ;
#3194=CARTESIAN_POINT ( 'NONE',  ( 1.054774247047244540, -0.07405724077823318263, 0.8120078739619844832 ) ) ;
#3196=CARTESIAN_POINT ( 'NONE',  ( -0.7495606340400177148, 0.1264236179284866091, 1.847933070812378009 ) ) ;
#3198=CARTESIAN_POINT ( 'NONE',  ( 0.8759842519685039353, 0.000000000000000000, 4.498031496062992574 ) ) ;
#3199=FACE_OUTER_BOUND ( 'NONE', #16797, .T. ) ;
#3204=AXIS2_PLACEMENT_3D ( 'NONE', #17491, #2626, #35943 ) ;
#3207=CARTESIAN_POINT ( 'NONE',  ( 0.9873396505805591694, -0.1113553986120547346, 1.934055118110236338 ) ) ;
#3210=CARTESIAN_POINT ( 'NONE',  ( -0.9500414927467377701, 0.1787899950787401604, 0.4281496062454490659 ) ) ;
#3213=CARTESIAN_POINT ( 'NONE',  ( 0.8759842519685039353, 0.1787899950787401882, 1.257381889710015743 ) ) ;
#3214=CARTESIAN_POINT ( 'NONE',  ( 1.002407869896990045, -0.1264236179284866091, 1.473917322780881722 ) ) ;
#3217=CARTESIAN_POINT ( 'NONE',  ( 0.7185039370078746268, 0.06523048226347956391, 0.6865157479239700766 ) ) ;
#3218=CARTESIAN_POINT ( 'NONE',  ( -0.7646288533564489232, 0.1113553986120547346, 1.668307086506645609 ) ) ;
#3220=CARTESIAN_POINT ( 'NONE',  ( 0.7495606340400177148, 0.1264236179284866091, 0.1550196849856066983 ) ) ;
#3221=CARTESIAN_POINT ( 'NONE',  ( 0.7058544154350729904, 0.05181626514163805569, 0.03937118780267125084 ) ) ;
#3222=CARTESIAN_POINT ( 'NONE',  ( 0.8019270111902716547, 0.1787899950787401604, 1.136811023568283119 ) ) ;
#3224=CARTESIAN_POINT ( 'NONE',  ( 0.8759842519685039353, 0.1574803149606299191, 0.5610236219397165547 ) ) ;
#3225=ORIENTED_EDGE ( 'NONE', *, *, #6637, .F. ) ;
#3226=CARTESIAN_POINT ( 'NONE',  ( -1.054774247047244096, 0.000000000000000000, 1.050688976324189117 ) ) ;
#3228=CARTESIAN_POINT ( 'NONE',  ( 0.9907320134992387839, 0.1205351961251636961, 0.03937007592068544892 ) ) ;
#3231=CARTESIAN_POINT ( 'NONE',  ( -1.033464566929134687, 0.06523048226347956391, 0.3567913384751500994 ) ) ;
#3233=CARTESIAN_POINT ( 'NONE',  ( 0.6971942568897648851, 0.07405724077823318263, 1.377952755851748146 ) ) ;
#3235=CARTESIAN_POINT ( 'NONE',  ( 0.7185039370078746268, -0.06523048226347956391, 1.173720472440945350 ) ) ;
#3237=VERTEX_POINT ( 'NONE', #3536 ) ;
#3238=CARTESIAN_POINT ( 'NONE',  ( 0.7185039370078746268, 0.06523048226347956391, 0.4502952754830242821 ) ) ;
#3239=EDGE_CURVE ( 'NONE', #6537, #18481, #9773, .T. ) ;
#3245=CARTESIAN_POINT ( 'NONE',  ( 0.8019270111902717657, -0.1787899950787401604, 0.6053149605761579677 ) ) ;
#3246=ORIENTED_EDGE ( 'NONE', *, *, #27251, .T. ) ;
#3249=CARTESIAN_POINT ( 'NONE',  ( -0.8759842519685039353, -0.1787899950787401882, 1.158956692859621995 ) ) ;
#3250=VECTOR ( 'NONE', #35313, 39.37007874015748143 ) ;
#3251=CARTESIAN_POINT ( 'NONE',  ( -0.7646288533564489232, -0.1113553986120547346, 0.07381889763779526936 ) ) ;
#3252=VERTEX_POINT ( 'NONE', #40862 ) ;
#3253=CARTESIAN_POINT ( 'NONE',  ( -1.054774247047244540, -0.07405724077823318263, 1.161417322780881278 ) ) ;
#3255=CARTESIAN_POINT ( 'NONE',  ( -0.6971942568897626646, -0.07405724077823297447, 0.2460629920722207375 ) ) ;
#3256=CARTESIAN_POINT ( 'NONE',  ( 0.9412147342319837628, 0.1574803149606300301, 0.7947834644594015119 ) ) ;
#3259=ORIENTED_EDGE ( 'NONE', *, *, #37025, .T. ) ;
#3261=CARTESIAN_POINT ( 'NONE',  ( 0.7374060038789669314, 0.1135695039425618086, 0.03936553649663185328 ) ) ;
#3265=CARTESIAN_POINT ( 'NONE',  ( -0.9500414927467378812, 0.1787899950787401604, 0.6594488188438737408 ) ) ;
#3267=CARTESIAN_POINT ( 'NONE',  ( -0.6971942568897648851, -0.07405724077823297447, 1.781496062938362934 ) ) ;
#3273=CARTESIAN_POINT ( 'NONE',  ( 0.8759842519685039353, 0.1574803149606299191, 0.6889763779527560139 ) ) ;
#3275=CARTESIAN_POINT ( 'NONE',  ( -0.7185039370078739607, 1.928577636452523993E-17, 0.9744094488188976833 ) ) ;
#3276=CARTESIAN_POINT ( 'NONE',  ( -0.9873396505805591694, -0.1113553986120547346, 1.451771653435779408 ) ) ;
#3277=CARTESIAN_POINT ( 'NONE',  ( 0.8019270111902717657, 0.1787899950787401604, 0.7086614172690703928 ) ) ;
#3281=VERTEX_POINT ( 'NONE', #37060 ) ;
#3283=CARTESIAN_POINT ( 'NONE',  ( 0.7646288533564489232, -0.1113553986120547346, 1.254921259842519676 ) ) ;
#3284=CARTESIAN_POINT ( 'NONE',  ( 0.7756356084717642707, -0.1385908279522278519, 1.986213216910492907 ) ) ;
#3288=CARTESIAN_POINT ( 'NONE',  ( 0.6971942568897648851, 0.07405724077823318263, 0.6299212597887560161 ) ) ;
#3290=CARTESIAN_POINT ( 'NONE',  ( -0.9412147342319837628, 0.1574803149606300301, 0.6865157480314956207 ) ) ;
#3294=DIRECTION ( 'NONE',  ( -1.000000000000000000, 0.000000000000000000, 0.000000000000000000 ) ) ;
#3295=CARTESIAN_POINT ( 'NONE',  ( 0.7185039370078739607, 1.928577636452523993E-17, 0.6988188976377952555 ) ) ;
#3296=CARTESIAN_POINT ( 'NONE',  ( 0.6971942568897626646, 0.07405724077823318263, 0.9842519684501742638 ) ) ;
#3303=( BOUNDED_CURVE ( )  B_SPLINE_CURVE ( 2, ( #6642, #7126, #11680, #22684, #37286, #33024, #11210, #37061, #21749 ),
 .UNSPECIFIED., .F., .T. ) 
 B_SPLINE_CURVE_WITH_KNOTS ( ( 3, 2, 2, 2, 3 ),
 ( 0.1400000000000000133, 0.1424999999999999878, 0.1449999999999999900, 0.1474999999999999922, 0.1499999999999999944 ),
 .UNSPECIFIED. ) 
 CURVE ( )  GEOMETRIC_REPRESENTATION_ITEM ( )  RATIONAL_B_SPLINE_CURVE ( ( 1.000000000000000000, 0.9238795325112869605, 1.000000000000000000, 0.9238795325112869605, 1.000000000000000000, 0.9238795325112869605, 1.000000000000000000, 0.9238795325112869605, 1.000000000000000000 ) ) 
 REPRESENTATION_ITEM ( '' )  ) ;
#3304=EDGE_CURVE ( 'NONE', #26454, #17892, #7366, .T. ) ;
#3305=CARTESIAN_POINT ( 'NONE',  ( -0.7495606340400177148, 0.1264236179284866091, 0.07627952750529173875 ) ) ;
#3306=DIRECTION ( 'NONE',  ( 0.000000000000000000, 0.000000000000000000, -1.000000000000000000 ) ) ;
#3310=DIRECTION ( 'NONE',  ( 1.822029033848725028E-16, 0.000000000000000000, 1.000000000000000000 ) ) ;
#3311=CARTESIAN_POINT ( 'NONE',  ( -0.6971942568897637749, 2.189545951927499583E-17, 1.695374015694267822 ) ) ;
#3312=CARTESIAN_POINT ( 'NONE',  ( 0.6971942568897648851, 0.07405724077823318263, 0.9104330708123777871 ) ) ;
#3314=CARTESIAN_POINT ( 'NONE',  ( -0.8759842519685039353, -0.1787899950787401882, 1.075295275536787276 ) ) ;
#3315=CARTESIAN_POINT ( 'NONE',  ( -1.054774247047244540, -0.07405724077823318263, 0.4183070865604097133 ) ) ;
#3316=CARTESIAN_POINT ( 'NONE',  ( -0.8759842519685039353, -0.1574803149606299191, 0.6692913385826771977 ) ) ;
#3317=CARTESIAN_POINT ( 'NONE',  ( -0.8759842519685039353, 0.1787899950787401882, 1.887303149552535420 ) ) ;
#3318=CARTESIAN_POINT ( 'NONE',  ( -0.7646288533564489232, 0.1113553986120547346, 1.481299212598425230 ) ) ;
#3319=CARTESIAN_POINT ( 'NONE',  ( -1.033464566929134687, 0.06523048226347956391, 1.862696850393700254 ) ) ;
#3320=CARTESIAN_POINT ( 'NONE',  ( -0.7185039370078746268, 0.06523048226347956391, 0.3026574803149607029 ) ) ;
#3324=LINE ( 'NONE', #29009, #47096 ) ;
#3328=( BOUNDED_CURVE ( )  B_SPLINE_CURVE ( 2, ( #43763, #21484, #7111, #14789, #26045, #17896, #18595, #29215, #37049, #25087, #32543, #10965, #43998, #7355, #381, #22191, #14318, #40388, #36825, #21735, #3977, #22428, #21968, #4202, #39925, #36592, #47131, #18831, #11200, #33486, #43520, #47373, #10488, #14545, #10733, #6864, #36116, #25342, #3522, #37274, #45162, #1803, #4678, #41799, #8521, #15977, #34192, #1555, #8044, #44683, #34412, #8757, #22674, #44455, #19307, #26523, #19061, #40850, #4429, #5158, #33729, #45409, #16211, #23149, #11669, #8999, #840, #12383, #23623, #38233, #1320, #30842, #26761, #15743, #33961, #34653, #16442, #26293, #44923, #12137, #4922, #12622, #15499, #27245, #30145, #41084, #11901, #41318, #19545, #8282, #22908, #27004, #5391, #37521, #20014, #23394, #37999, #45635, #5640, #2271, #35359, #42732, #31996, #16670, #9717, #27487, #6331, #24555, #13091, #2731, #13316, #46588, #27724, #16895, #20252, #10187, #27947, #13768, #23858, #38711, #28409, #42286, #5881, #21184, #20487, #42038, #9947, #13537, #34897, #42978, #31537, #35816, #17128, #20947, #31299, #39160, #24793, #39389, #35125, #6573, #2964, #9486, #24104, #31071, #46118, #42514, #24330, #2038, #9240, #38470, #38929, #2504, #31770, #46353, #36053, #32241, #21913, #43459, #36763, #3210, #46823, #32721, #3921, #29629, #76, #40329, #18544, #44166, #32954, #10666, #11369, #22371, #25273, #14972, #29146, #36535, #7293, #22136, #28659, #17840, #7514, #43224, #17599, #39861, #47067, #39625, #14011, #25030, #25759, #10429, #33200, #21676, #7052, #36307, #36996, #6805, #47312, #21424, #10910, #32485, #322, #14487, #3462, #18073, #7753, #14258, #28900, #43702, #25533, #40099, #3694, #25980, #18316, #40563, #14724, #29397, #43941, #11139, #15683, #19720, #45105, #34358, #44393, #12323, #22849, #30781, #18777, #26231, #37465, #8458, #4613, #41492, #1263, #7990, #34133, #15915, #779, #30542, #41258, #26939, #1495, #33665, #19247, #40797, #45348, #33905, #16150, #11609, #11841, #23333, #1027, #12561, #4858, #8224, #27186, #23088, #4372, #8698, #30320, #22615, #15202, #37705, #37948, #37227, #5096, #41739, #8944, #26468, #23564, #4151, #19002, #44867, #33432, #19484, #12079, #547, #29853, #26703, #15439, #30094, #44626, #41030, #34591, #45574, #46297, #1741, #39099, #42225, #27664, #16614, #42918, #16386, #20430, #5331, #31474, #12794, #24505, #31712, #19951, #9892, #20899, #10129, #38167, #9427, #5822, #2214, #31005, #42679, #27430, #6273, #38873, #28349, #31240, #28119, #16834, #35538, #13488, #6037, #2678, #41970, #13712, #17309, #9179, #23795, #24047, #42457, #38647, #31945, #35306, #38411, #20660, #2443, #34839, #17071, #27895, #46531, #5582, #35063, #46058, #20188, #1984, #13266, #45817, #13027, #9661, #24278, #10613, #22737, #26110, #28843, #33795, #44284, #24978, #29975, #39803, #28603, #35767, #30213, #44758, #40919, #43166, #11738, #4263, #32429, #22495, #44523, #32180, #43404, #24738, #14435, #25211, #7878, #667, #6992, #17542, #21618, #36251, #10371, #3402, #8114, #4493, #29087, #3156, #47007, #39573, #18014, #19131, #6513, #6750, #46767, #40685, #37115, #15574, #32666, #47254, #18896, #13952, #11489, #21371, #33551, #26358, #15322, #2907, #39335, #14199, #35998, #17781, #37342, #913, #21132, #12921, #30669, #1384, #37837, #31370, #37585, #41621, #26596, #5220, #34027, #45703, #8830, #45229, #12453, #2104, #41148, #4747, #27073, #23463, #38065, #19374, #31135, #1153, #27551, #27317, #12202, #4995, #42103, #19849, #9309, #20084, #23932, #26828, #34730, #34476, #38539, #41384, #8586, #1628, #45466, #41866, #34959, #23688, #23223, #27601, #8151, #26871, #22779, #19177, #33837, #956, #37635, #8629, #12014, #30253, #1426, #26637, #8394, #30711, #13882, #42618, #39504, #42844, #24435, #3084, #13643, #42396, #46693, #35471, #45993, #20366, #46938, #10300, #27836, #2610, #28282, #43095, #14127, #17245, #24913, #9596, #5974, #24671, #20595, #17012, #31882, #46460, #42149, #9356, #6679, #10056, #21059, #21295, #35922, #35699, #2835, #17707, #32358, #17470, #23979, #38582, #35003, #2149, #16776, #31416, #33537, #36413, #26094, #40205, #185, #18417, #25393, #25856, #425, #44269, #36869, #7623, #36637, #4024, #14595, #14834, #7164, #10541, #32828, #29267, #39729, #39971, #33064, #11470, #21539, #18643, #36177, #47423, #43340, #650, #3571, #43811, #40437, #29726, #14368, #7399, #25138, #33301, #22240, #43570, #15080, #11011, #40666, #10783, #25631, #17939, #3798, #11245, #7862, #22480, #28770, #22012, #21787, #18188, #18879, #29499, #6916, #37095, #4244, #32594, #3335, #44046, #47185, #29014, #5206, #893, #8569, #34241, #19831, #20067, #34011, #34460, #30197, #44741, #41606, #11960, #15555, #12186, #26579, #34711, #15305, #1610, #1137, #12672, #16258, #41135, #8334, #44973, #30893, #27298, #8808, #38049, #9054, #23675, #30652, #22962, #5452, #29958, #4730, #26342, #26811, #1370, #4976, #8099, #22720, #19355, #37329, #23445, #4477, #23204, #19118, #15797, #16027, #41370, #37820, #31590, #38522, #2787, #39212, #13370, #16489, #13826, #5693, #2554, #46641, #28469, #35647, #42785, #31122, #21002, #32053, #43035, #42340, #20541, #46406, #45685, #16953, #6388, #21243, #17414, #20303, #45933, #10244, #17187, #5923, #24850, #13584, #31821, #34944, #39449, #35176, #6627, #28222, #12906, #2091, #10000, #27538, #24614, #9536, #42090, #9296, #23916, #2321, #16720, #38981, #46172, #42562, #31352, #13145, #27781, #24159, #9770, #38763, #24380, #6145, #3020, #40154, #14315, #10729, #36113, #32776, #29682, #17655, #6859, #43287, #36590, #40615, #25335, #33252, #47372, #7353, #25583, #40383, #46880, #3267, #25811, #33011, #14066, #35870, #39922, #17893, #10486, #25084, #39676, #43997, #21478, #3976, #7576, #29212, #32538, #15031, #47125, #21965, #44221, #11422, #3748, #22187, #18131, #7109, #36367, #26041, #7810, #28959, #3518, #43760, #10962, #18593, #18370, #134, #14784, #29448, #35450, #10282, #39488, #17228, #2822, #10523, #21769, #46443, #14348, #24891, #32809, #20812, #42825, #6665, #25121, #17926, #7145, #39251, #32339, #2594, #28997, #47165, #21044, #25375, #35906, #36399, #35685, #21281, #10038, #47405, #3061, #3556, #13624, #13864, #39954, #24657, #46920, #39713, #43555, #10996, #17688, #10767, #17454, #32089, #36156, #28509, #6425, #14109, #43077 ),
 .UNSPECIFIED., .F., .F. ) 
 B_SPLINE_CURVE_WITH_KNOTS ( ( 3, 2, 2, 2, 2, 2, 2, 2, 2, 2, 2, 2, 2, 2, 2, 2, 2, 2, 2, 2, 2, 2, 2, 2, 2, 2, 2, 2, 2, 2, 2, 2, 2, 2, 2, 2, 2, 2, 2, 2, 2, 2, 2, 2, 2, 2, 2, 2, 2, 2, 2, 2, 2, 2, 2, 2, 2, 2, 2, 2, 2, 2, 2, 2, 2, 2, 2, 2, 2, 2, 2, 2, 2, 2, 2, 2, 2, 2, 2, 2, 2, 2, 2, 2, 2, 2, 2, 2, 2, 2, 2, 2, 2, 2, 2, 2, 2, 2, 2, 2, 2, 2, 2, 2, 2, 2, 2, 2, 2, 2, 2, 2, 2, 2, 2, 2, 2, 2, 2, 2, 2, 2, 2, 2, 2, 2, 2, 2, 2, 2, 2, 2, 2, 2, 2, 2, 2, 2, 2, 2, 2, 2, 2, 2, 2, 2, 2, 2, 2, 2, 2, 2, 2, 2, 2, 2, 2, 2, 2, 2, 2, 2, 2, 2, 2, 2, 2, 2, 2, 2, 2, 2, 2, 2, 2, 2, 2, 2, 2, 2, 2, 2, 2, 2, 2, 2, 2, 2, 2, 2, 2, 2, 2, 2, 2, 2, 2, 2, 2, 2, 2, 2, 2, 2, 2, 2, 2, 2, 2, 2, 2, 2, 2, 2, 2, 2, 2, 2, 2, 2, 2, 2, 2, 2, 2, 2, 2, 2, 2, 2, 2, 2, 2, 2, 2, 2, 2, 2, 2, 2, 2, 2, 2, 2, 2, 2, 2, 2, 2, 2, 2, 2, 2, 2, 2, 2, 2, 2, 2, 2, 2, 2, 2, 2, 2, 2, 2, 2, 2, 2, 2, 2, 2, 2, 2, 2, 2, 2, 2, 2, 2, 2, 2, 2, 2, 2, 2, 2, 2, 2, 2, 2, 2, 2, 2, 2, 2, 2, 2, 2, 2, 2, 2, 2, 2, 2, 2, 2, 2, 2, 2, 2, 2, 2, 2, 2, 2, 2, 2, 2, 2, 2, 2, 2, 2, 2, 2, 2, 2, 2, 2, 2, 2, 2, 2, 2, 2, 2, 2, 2, 2, 2, 2, 2, 2, 2, 2, 2, 2, 2, 2, 2, 2, 2, 2, 2, 2, 2, 2, 2, 2, 2, 2, 2, 2, 2, 2, 2, 2, 2, 2, 2, 2, 2, 2, 2, 2, 2, 2, 2, 2, 2, 2, 2, 2, 2, 2, 2, 2, 2, 2, 2, 2, 2, 2, 2, 2, 3 ),
 ( 0.006250000026272810663, 0.007499999999999999722, 0.01000000000000000021, 0.01250000000000000069, 0.01499999999999999944, 0.01750000000000000167, 0.02000000000000000042, 0.02249999999999999917, 0.02500000000000000139, 0.02749999999999999667, 0.02999999999999999889, 0.03250000000000000111, 0.03500000000000000333, 0.03749999999999999861, 0.04000000000000000083, 0.04250000000000000305, 0.04499999999999999833, 0.04750000000000000056, 0.05000000000000000278, 0.05250000000000000500, 0.05500000000000000028, 0.05750000000000000250, 0.05999999999999999778, 0.06250000000000000000, 0.06500000000000000222, 0.06750000000000000444, 0.07000000000000000666, 0.07249999999999999500, 0.07499999999999999722, 0.07749999999999999944, 0.08000000000000000167, 0.08250000000000000389, 0.08500000000000000611, 0.08749999999999999445, 0.08999999999999999667, 0.09249999999999999889, 0.09500000000000000111, 0.09750000000000000333, 0.1000000000000000056, 0.1024999999999999939, 0.1049999999999999961, 0.1074999999999999983, 0.1100000000000000006, 0.1125000000000000028, 0.1150000000000000050, 0.1174999999999999933, 0.1199999999999999956, 0.1224999999999999978, 0.1250000000000000000, 0.1275000000000000022, 0.1300000000000000044, 0.1325000000000000067, 0.1350000000000000089, 0.1375000000000000111, 0.1400000000000000133, 0.1424999999999999878, 0.1449999999999999900, 0.1474999999999999922, 0.1499999999999999944, 0.1524999999999999967, 0.1549999999999999989, 0.1575000000000000011, 0.1600000000000000033, 0.1625000000000000056, 0.1650000000000000078, 0.1674999999999999822, 0.1700000000000000122, 0.1724999999999999867, 0.1749999999999999889, 0.1774999999999999911, 0.1799999999999999933, 0.1824999999999999956, 0.1849999999999999978, 0.1875000000000000000, 0.1900000000000000022, 0.1925000000000000044, 0.1950000000000000067, 0.1975000000000000089, 0.2000000000000000111, 0.2025000000000000133, 0.2049999999999999878, 0.2074999999999999900, 0.2099999999999999922, 0.2124999999999999944, 0.2149999999999999967, 0.2174999999999999989, 0.2200000000000000011, 0.2225000000000000033, 0.2250000000000000056, 0.2275000000000000078, 0.2299999999999999822, 0.2325000000000000122, 0.2349999999999999867, 0.2374999999999999889, 0.2399999999999999911, 0.2424999999999999933, 0.2449999999999999956, 0.2474999999999999978, 0.2500000000000000000, 0.2525000000000000022, 0.2550000000000000044, 0.2575000000000000067, 0.2600000000000000089, 0.2625000000000000111, 0.2650000000000000133, 0.2675000000000000155, 0.2700000000000000733, 0.2725000000000000200, 0.2750000000000000222, 0.2775000000000000244, 0.2800000000000000266, 0.2824999999999999734, 0.2849999999999999756, 0.2874999999999999778, 0.2899999999999999800, 0.2924999999999999822, 0.2949999999999999845, 0.2974999999999999867, 0.2999999999999999889, 0.3024999999999999911, 0.3049999999999999933, 0.3074999999999999956, 0.3099999999999999978, 0.3125000000000000000, 0.3150000000000000022, 0.3175000000000000044, 0.3200000000000000067, 0.3225000000000000089, 0.3250000000000000111, 0.3275000000000000133, 0.3300000000000000155, 0.3325000000000000178, 0.3350000000000000200, 0.3375000000000000222, 0.3400000000000000244, 0.3425000000000000266, 0.3449999999999999734, 0.3474999999999999756, 0.3499999999999999778, 0.3524999999999999800, 0.3549999999999999822, 0.3574999999999999845, 0.3599999999999999867, 0.3624999999999999889, 0.3649999999999999911, 0.3674999999999999933, 0.3699999999999999956, 0.3724999999999999978, 0.3750000000000000000, 0.3775000000000000022, 0.3800000000000000044, 0.3825000000000000067, 0.3850000000000000089, 0.3875000000000000111, 0.3900000000000000133, 0.3925000000000000155, 0.3950000000000000733, 0.3975000000000000200, 0.4000000000000000222, 0.4025000000000000244, 0.4050000000000000266, 0.4074999999999999734, 0.4099999999999999756, 0.4124999999999999778, 0.4149999999999999800, 0.4174999999999999822, 0.4199999999999999845, 0.4224999999999999867, 0.4249999999999999889, 0.4274999999999999911, 0.4299999999999999933, 0.4324999999999999956, 0.4349999999999999978, 0.4375000000000000000, 0.4400000000000000022, 0.4425000000000000044, 0.4450000000000000067, 0.4475000000000000089, 0.4500000000000000111, 0.4525000000000000133, 0.4550000000000000155, 0.4575000000000000178, 0.4600000000000000200, 0.4625000000000000222, 0.4650000000000000244, 0.4675000000000000266, 0.4699999999999999734, 0.4724999999999999756, 0.4749999999999999778, 0.4774999999999999800, 0.4799999999999999822, 0.4824999999999999845, 0.4849999999999999867, 0.4874999999999999889, 0.4899999999999999911, 0.4924999999999999933, 0.4949999999999999956, 0.4974999999999999978, 0.5000000000000000000, 0.5024999999999999467, 0.5050000000000000044, 0.5074999999999999512, 0.5100000000000000089, 0.5124999999999999556, 0.5150000000000000133, 0.5174999999999999600, 0.5200000000000000178, 0.5224999999999999645, 0.5250000000000000222, 0.5274999999999999689, 0.5300000000000000266, 0.5324999999999999734, 0.5350000000000000311, 0.5374999999999999778, 0.5400000000000000355, 0.5424999999999999822, 0.5450000000000000400, 0.5474999999999999867, 0.5500000000000000444, 0.5524999999999999911, 0.5550000000000000488, 0.5574999999999999956, 0.5600000000000000533, 0.5625000000000000000, 0.5650000000000000577, 0.5675000000000000044, 0.5699999999999999512, 0.5725000000000000089, 0.5749999999999999556, 0.5775000000000000133, 0.5799999999999999600, 0.5825000000000000178, 0.5849999999999999645, 0.5875000000000000222, 0.5899999999999999689, 0.5925000000000000266, 0.5949999999999999734, 0.5975000000000000311, 0.5999999999999999778, 0.6025000000000000355, 0.6049999999999999822, 0.6075000000000000400, 0.6099999999999999867, 0.6125000000000000444, 0.6149999999999999911, 0.6175000000000000488, 0.6199999999999999956, 0.6225000000000000533, 0.6250000000000000000, 0.6274999999999999467, 0.6300000000000000044, 0.6324999999999999512, 0.6350000000000000089, 0.6374999999999999556, 0.6400000000000000133, 0.6424999999999999600, 0.6450000000000000178, 0.6474999999999999645, 0.6500000000000000222, 0.6524999999999999689, 0.6550000000000000266, 0.6574999999999999734, 0.6600000000000000311, 0.6624999999999999778, 0.6650000000000000355, 0.6674999999999999822, 0.6700000000000000400, 0.6724999999999999867, 0.6750000000000000444, 0.6774999999999999911, 0.6800000000000000488, 0.6824999999999999956, 0.6850000000000000533, 0.6875000000000000000, 0.6899999999999999467, 0.6925000000000000044, 0.6949999999999999512, 0.6975000000000000089, 0.6999999999999999556, 0.7025000000000000133, 0.7049999999999999600, 0.7075000000000000178, 0.7099999999999999645, 0.7125000000000000222, 0.7149999999999999689, 0.7175000000000000266, 0.7199999999999999734, 0.7225000000000000311, 0.7249999999999999778, 0.7275000000000000355, 0.7299999999999999822, 0.7325000000000000400, 0.7349999999999999867, 0.7375000000000000444, 0.7399999999999999911, 0.7425000000000000488, 0.7449999999999999956, 0.7475000000000000533, 0.7500000000000000000, 0.7524999999999999467, 0.7550000000000000044, 0.7574999999999999512, 0.7600000000000000089, 0.7624999999999999556, 0.7650000000000000133, 0.7674999999999999600, 0.7700000000000000178, 0.7724999999999999645, 0.7750000000000000222, 0.7774999999999999689, 0.7800000000000000266, 0.7824999999999999734, 0.7850000000000000311, 0.7874999999999999778, 0.7900000000000000355, 0.7924999999999999822, 0.7950000000000000400, 0.7974999999999999867, 0.8000000000000000444, 0.8024999999999999911, 0.8050000000000000488, 0.8074999999999999956, 0.8100000000000000533, 0.8125000000000000000, 0.8150000000000000577, 0.8175000000000000044, 0.8199999999999999512, 0.8225000000000000089, 0.8249999999999999556, 0.8275000000000000133, 0.8299999999999999600, 0.8325000000000000178, 0.8349999999999999645, 0.8375000000000000222, 0.8399999999999999689, 0.8425000000000000266, 0.8449999999999999734, 0.8475000000000000311, 0.8499999999999999778, 0.8525000000000000355, 0.8549999999999999822, 0.8575000000000000400, 0.8599999999999999867, 0.8625000000000000444, 0.8649999999999999911, 0.8675000000000000488, 0.8699999999999999956, 0.8725000000000000533, 0.8750000000000000000, 0.8774999999999999467, 0.8800000000000000044, 0.8824999999999999512, 0.8850000000000000089, 0.8874999999999999556, 0.8900000000000000133, 0.8924999999999999600, 0.8950000000000000178, 0.8974999999999999645, 0.9000000000000000222, 0.9024999999999999689, 0.9050000000000000266, 0.9074999999999999734, 0.9100000000000000311, 0.9124999999999999778, 0.9150000000000000355, 0.9174999999999999822, 0.9200000000000000400, 0.9224999999999999867, 0.9250000000000000444, 0.9274999999999999911, 0.9300000000000000488, 0.9324999999999999956, 0.9350000000000000533, 0.9375000000000000000, 0.9399999999999999467, 0.9425000000000000044, 0.9449999999999999512, 0.9475000000000000089, 0.9499999999999999556, 0.9525000000000000133, 0.9549999999999999600, 0.9575000000000000178, 0.9599999999999999645, 0.9625000000000000222, 0.9649999999999999689, 0.9675000000000000266, 0.9699999999999999734, 0.9725000000000000311, 0.9749999999999999778, 0.9775000000000000355, 0.9799999999999999822, 0.9825000000000000400, 0.9849999999999999867, 0.9875000000000000444, 0.9899999999999999911, 0.9925000000000000488, 0.9949999999999999956, 0.9975000000000000533 ),
 .UNSPECIFIED. ) 
 CURVE ( )  GEOMETRIC_REPRESENTATION_ITEM ( )  RATIONAL_B_SPLINE_CURVE ( ( 0.9619397662556429252, 0.9619397670556029123, 1.000000000000000000, 0.9238795325112869605, 1.000000000000000000, 0.9238795325112869605, 1.000000000000000000, 0.9238795325112869605, 1.000000000000000000, 0.9238795325112869605, 1.000000000000000000, 0.9238795325112869605, 1.000000000000000000, 0.9238795325112869605, 1.000000000000000000, 0.9238795325112869605, 1.000000000000000000, 0.9238795325112869605, 1.000000000000000000, 0.9238795325112869605, 1.000000000000000000, 0.9238795325112869605, 1.000000000000000000, 0.9238795325112869605, 1.000000000000000000, 0.9238795325112869605, 1.000000000000000000, 0.9238795325112869605, 1.000000000000000000, 0.9238795325112869605, 1.000000000000000000, 0.9238795325112869605, 1.000000000000000000, 0.9238795325112869605, 1.000000000000000000, 0.9238795325112869605, 1.000000000000000000, 0.9238795325112869605, 1.000000000000000000, 0.9238795325112869605, 1.000000000000000000, 0.9238795325112869605, 1.000000000000000000, 0.9238795325112869605, 1.000000000000000000, 0.9238795325112869605, 1.000000000000000000, 0.9238795325112869605, 1.000000000000000000, 0.9238795325112869605, 1.000000000000000000, 0.9238795325112869605, 1.000000000000000000, 0.9238795325112869605, 1.000000000000000000, 0.9238795325112869605, 1.000000000000000000, 0.9238795325112869605, 1.000000000000000000, 0.9238795325112869605, 1.000000000000000000, 0.9238795325112869605, 1.000000000000000000, 0.9238795325112869605, 1.000000000000000000, 0.9238795325112869605, 1.000000000000000000, 0.9238795325112869605, 1.000000000000000000, 0.9238795325112869605, 1.000000000000000000, 0.9238795325112869605, 1.000000000000000000, 0.9238795325112869605, 1.000000000000000000, 0.9238795325112869605, 1.000000000000000000, 0.9238795325112869605, 1.000000000000000000, 0.9238795325112869605, 1.000000000000000000, 0.9238795325112869605, 1.000000000000000000, 0.9238795325112869605, 1.000000000000000000, 0.9238795325112869605, 1.000000000000000000, 0.9238795325112869605, 1.000000000000000000, 0.9238795325112869605, 1.000000000000000000, 0.9238795325112869605, 1.000000000000000000, 0.9238795325112869605, 1.000000000000000000, 0.9238795325112869605, 1.000000000000000000, 0.9238795325112869605, 1.000000000000000000, 0.9238795325112869605, 1.000000000000000000, 0.9238795325112869605, 1.000000000000000000, 0.9238795325112869605, 1.000000000000000000, 0.9238795325112869605, 1.000000000000000000, 0.9238795325112869605, 1.000000000000000000, 0.9238795325112869605, 1.000000000000000000, 0.9238795325112869605, 1.000000000000000000, 0.9238795325112869605, 1.000000000000000000, 0.9238795325112869605, 1.000000000000000000, 0.9238795325112869605, 1.000000000000000000, 0.9238795325112869605, 1.000000000000000000, 0.9238795325112869605, 1.000000000000000000, 0.9238795325112869605, 1.000000000000000000, 0.9238795325112869605, 1.000000000000000000, 0.9238795325112869605, 1.000000000000000000, 0.9238795325112869605, 1.000000000000000000, 0.9238795325112869605, 1.000000000000000000, 0.9238795325112869605, 1.000000000000000000, 0.9238795325112869605, 1.000000000000000000, 0.9238795325112869605, 1.000000000000000000, 0.9238795325112869605, 1.000000000000000000, 0.9238795325112869605, 1.000000000000000000, 0.9238795325112869605, 1.000000000000000000, 0.9238795325112869605, 1.000000000000000000, 0.9238795325112869605, 1.000000000000000000, 0.9238795325112869605, 1.000000000000000000, 0.9238795325112869605, 1.000000000000000000, 0.9238795325112869605, 1.000000000000000000, 0.9238795325112869605, 1.000000000000000000, 0.9238795325112869605, 1.000000000000000000, 0.9238795325112869605, 1.000000000000000000, 0.9238795325112869605, 1.000000000000000000, 0.9238795325112869605, 1.000000000000000000, 0.9238795325112869605, 1.000000000000000000, 0.9238795325112869605, 1.000000000000000000, 0.9238795325112869605, 1.000000000000000000, 0.9238795325112869605, 1.000000000000000000, 0.9238795325112869605, 1.000000000000000000, 0.9238795325112869605, 1.000000000000000000, 0.9238795325112869605, 1.000000000000000000, 0.9238795325112869605, 1.000000000000000000, 0.9238795325112869605, 1.000000000000000000, 0.9238795325112869605, 1.000000000000000000, 0.9238795325112869605, 1.000000000000000000, 0.9238795325112869605, 1.000000000000000000, 0.9238795325112869605, 1.000000000000000000, 0.9238795325112869605, 1.000000000000000000, 0.9238795325112869605, 1.000000000000000000, 0.9238795325112869605, 1.000000000000000000, 0.9238795325112869605, 1.000000000000000000, 0.9238795325112869605, 1.000000000000000000, 0.9238795325112869605, 1.000000000000000000, 0.9238795325112869605, 1.000000000000000000, 0.9238795325112869605, 1.000000000000000000, 0.9238795325112869605, 1.000000000000000000, 0.9238795325112869605, 1.000000000000000000, 0.9238795325112869605, 1.000000000000000000, 0.9238795325112869605, 1.000000000000000000, 0.9238795325112869605, 1.000000000000000000, 0.9238795325112869605, 1.000000000000000000, 0.9238795325112869605, 1.000000000000000000, 0.9238795325112869605, 1.000000000000000000, 0.9238795325112869605, 1.000000000000000000, 0.9238795325112869605, 1.000000000000000000, 0.9238795325112869605, 1.000000000000000000, 0.9238795325112869605, 1.000000000000000000, 0.9238795325112869605, 1.000000000000000000, 0.9238795325112869605, 1.000000000000000000, 0.9238795325112869605, 1.000000000000000000, 0.9238795325112869605, 1.000000000000000000, 0.9238795325112869605, 1.000000000000000000, 0.9238795325112869605, 1.000000000000000000, 0.9238795325112869605, 1.000000000000000000, 0.9238795325112869605, 1.000000000000000000, 0.9238795325112869605, 1.000000000000000000, 0.9238795325112869605, 1.000000000000000000, 0.9238795325112869605, 1.000000000000000000, 0.9238795325112869605, 1.000000000000000000, 0.9238795325112869605, 1.000000000000000000, 0.9238795325112869605, 1.000000000000000000, 0.9238795325112869605, 1.000000000000000000, 0.9238795325112869605, 1.000000000000000000, 0.9238795325112869605, 1.000000000000000000, 0.9238795325112869605, 1.000000000000000000, 0.9238795325112869605, 1.000000000000000000, 0.9238795325112869605, 1.000000000000000000, 0.9238795325112869605, 1.000000000000000000, 0.9238795325112869605, 1.000000000000000000, 0.9238795325112869605, 1.000000000000000000, 0.9238795325112869605, 1.000000000000000000, 0.9238795325112869605, 1.000000000000000000, 0.9238795325112869605, 1.000000000000000000, 0.9238795325112869605, 1.000000000000000000, 0.9238795325112869605, 1.000000000000000000, 0.9238795325112869605, 1.000000000000000000, 0.9238795325112869605, 1.000000000000000000, 0.9238795325112869605, 1.000000000000000000, 0.9238795325112869605, 1.000000000000000000, 0.9238795325112869605, 1.000000000000000000, 0.9238795325112869605, 1.000000000000000000, 0.9238795325112869605, 1.000000000000000000, 0.9238795325112869605, 1.000000000000000000, 0.9238795325112869605, 1.000000000000000000, 0.9238795325112869605, 1.000000000000000000, 0.9238795325112869605, 1.000000000000000000, 0.9238795325112869605, 1.000000000000000000, 0.9238795325112869605, 1.000000000000000000, 0.9238795325112869605, 1.000000000000000000, 0.9238795325112869605, 1.000000000000000000, 0.9238795325112869605, 1.000000000000000000, 0.9238795325112869605, 1.000000000000000000, 0.9238795325112869605, 1.000000000000000000, 0.9238795325112869605, 1.000000000000000000, 0.9238795325112869605, 1.000000000000000000, 0.9238795325112869605, 1.000000000000000000, 0.9238795325112869605, 1.000000000000000000, 0.9238795325112869605, 1.000000000000000000, 0.9238795325112869605, 1.000000000000000000, 0.9238795325112869605, 1.000000000000000000, 0.9238795325112869605, 1.000000000000000000, 0.9238795325112869605, 1.000000000000000000, 0.9238795325112869605, 1.000000000000000000, 0.9238795325112869605, 1.000000000000000000, 0.9238795325112869605, 1.000000000000000000, 0.9238795325112869605, 1.000000000000000000, 0.9238795325112869605, 1.000000000000000000, 0.9238795325112869605, 1.000000000000000000, 0.9238795325112869605, 1.000000000000000000, 0.9238795325112869605, 1.000000000000000000, 0.9238795325112869605, 1.000000000000000000, 0.9238795325112869605, 1.000000000000000000, 0.9238795325112869605, 1.000000000000000000, 0.9238795325112869605, 1.000000000000000000, 0.9238795325112869605, 1.000000000000000000, 0.9238795325112869605, 1.000000000000000000, 0.9238795325112869605, 1.000000000000000000, 0.9238795325112869605, 1.000000000000000000, 0.9238795325112869605, 1.000000000000000000, 0.9238795325112869605, 1.000000000000000000, 0.9238795325112869605, 1.000000000000000000, 0.9238795325112869605, 1.000000000000000000, 0.9238795325112869605, 1.000000000000000000, 0.9238795325112869605, 1.000000000000000000, 0.9238795325112869605, 1.000000000000000000, 0.9238795325112869605, 1.000000000000000000, 0.9238795325112869605, 1.000000000000000000, 0.9238795325112869605, 1.000000000000000000, 0.9238795325112869605, 1.000000000000000000, 0.9238795325112869605, 1.000000000000000000, 0.9238795325112869605, 1.000000000000000000, 0.9238795325112869605, 1.000000000000000000, 0.9238795325112869605, 1.000000000000000000, 0.9238795325112869605, 1.000000000000000000, 0.9238795325112869605, 1.000000000000000000, 0.9238795325112869605, 1.000000000000000000, 0.9238795325112869605, 1.000000000000000000, 0.9238795325112869605, 1.000000000000000000, 0.9238795325112869605, 1.000000000000000000, 0.9238795325112869605, 1.000000000000000000, 0.9238795325112869605, 1.000000000000000000, 0.9238795325112869605, 1.000000000000000000, 0.9238795325112869605, 1.000000000000000000, 0.9238795325112869605, 1.000000000000000000, 0.9238795325112869605, 1.000000000000000000, 0.9238795325112869605, 1.000000000000000000, 0.9238795325112869605, 1.000000000000000000, 0.9238795325112869605, 1.000000000000000000, 0.9238795325112869605, 1.000000000000000000, 0.9238795325112869605, 1.000000000000000000, 0.9238795325112869605, 1.000000000000000000, 0.9238795325112869605, 1.000000000000000000, 0.9238795325112869605, 1.000000000000000000, 0.9238795325112869605, 1.000000000000000000, 0.9238795325112869605, 1.000000000000000000, 0.9238795325112869605, 1.000000000000000000, 0.9238795325112869605, 1.000000000000000000, 0.9238795325112869605, 1.000000000000000000, 0.9238795325112869605, 1.000000000000000000, 0.9238795325112869605, 1.000000000000000000, 0.9238795325112869605, 1.000000000000000000, 0.9238795325112869605, 1.000000000000000000, 0.9238795325112869605, 1.000000000000000000, 0.9238795325112869605, 1.000000000000000000, 0.9238795325112869605, 1.000000000000000000, 0.9238795325112869605, 1.000000000000000000, 0.9238795325112869605, 1.000000000000000000, 0.9238795325112869605, 1.000000000000000000, 0.9238795325112869605, 1.000000000000000000, 0.9238795325112869605, 1.000000000000000000, 0.9238795325112869605, 1.000000000000000000, 0.9238795325112869605, 1.000000000000000000, 0.9238795325112869605, 1.000000000000000000, 0.9238795325112869605, 1.000000000000000000, 0.9238795325112869605, 1.000000000000000000, 0.9238795325112869605, 1.000000000000000000, 0.9238795325112869605, 1.000000000000000000, 0.9238795325112869605, 1.000000000000000000, 0.9238795325112869605, 1.000000000000000000, 0.9238795325112869605, 1.000000000000000000, 0.9238795325112869605, 1.000000000000000000, 0.9238795325112869605, 1.000000000000000000, 0.9238795325112869605, 1.000000000000000000, 0.9238795325112869605, 1.000000000000000000, 0.9238795325112869605, 1.000000000000000000, 0.9238795325112869605, 1.000000000000000000, 0.9238795325112869605, 1.000000000000000000, 0.9238795325112869605, 1.000000000000000000, 0.9238795325112869605, 1.000000000000000000, 0.9238795325112869605, 1.000000000000000000, 0.9238795325112869605, 1.000000000000000000, 0.9238795325112869605, 1.000000000000000000, 0.9238795325112869605, 1.000000000000000000, 0.9238795325112869605, 1.000000000000000000, 0.9238795325112869605, 1.000000000000000000, 0.9238795325112869605, 1.000000000000000000, 0.9238795325112869605, 1.000000000000000000, 0.9238795325112869605, 1.000000000000000000, 0.9238795325112869605, 1.000000000000000000, 0.9238795325112869605, 1.000000000000000000, 0.9238795325112869605, 1.000000000000000000, 0.9238795325112869605, 1.000000000000000000, 0.9238795325112869605, 1.000000000000000000, 0.9238795325112869605, 1.000000000000000000, 0.9238795325112869605, 1.000000000000000000, 0.9238795325112869605, 1.000000000000000000, 0.9238795325112869605, 1.000000000000000000, 0.9238795325112869605, 1.000000000000000000, 0.9238795325112869605, 1.000000000000000000, 0.9238795325112869605, 1.000000000000000000, 0.9238795325112869605, 1.000000000000000000, 0.9238795325112869605, 1.000000000000000000, 0.9238795325112869605, 1.000000000000000000, 0.9238795325112869605, 1.000000000000000000, 0.9238795325112869605, 1.000000000000000000, 0.9238795325112869605, 1.000000000000000000, 0.9238795325112869605, 1.000000000000000000, 0.9238795325112869605, 1.000000000000000000, 0.9238795325112869605, 1.000000000000000000, 0.9238795325112869605, 1.000000000000000000, 0.9238795325112869605, 1.000000000000000000, 0.9238795325112869605, 1.000000000000000000, 0.9238795325112869605, 1.000000000000000000, 0.9238795325112869605, 1.000000000000000000, 0.9238795325112869605, 1.000000000000000000, 0.9238795325112869605, 1.000000000000000000, 0.9238795325112869605, 1.000000000000000000, 0.9238795325112869605, 1.000000000000000000, 0.9238795325112869605, 1.000000000000000000, 0.9238795325112869605, 1.000000000000000000, 0.9238795325112869605, 1.000000000000000000, 0.9238795325112869605, 1.000000000000000000, 0.9238795325112869605, 1.000000000000000000, 0.9238795325112869605, 1.000000000000000000, 0.9238795325112869605, 1.000000000000000000, 0.9238795325112869605, 1.000000000000000000, 0.9238795325112869605, 1.000000000000000000, 0.9238795325112869605, 1.000000000000000000, 0.9238795325112869605, 1.000000000000000000, 0.9238795325112869605, 1.000000000000000000, 0.9238795325112869605, 1.000000000000000000, 0.9238795325112869605, 1.000000000000000000, 0.9238795325112869605, 1.000000000000000000, 0.9238795325112869605, 1.000000000000000000, 0.9238795325112869605, 1.000000000000000000, 0.9238795325112869605, 1.000000000000000000, 0.9238795325112869605, 1.000000000000000000, 0.9238795325112869605, 1.000000000000000000, 0.9238795325112869605, 1.000000000000000000, 0.9238795325112869605, 1.000000000000000000, 0.9238795325112869605, 1.000000000000000000, 0.9238795325112869605, 1.000000000000000000, 0.9238795325112869605, 1.000000000000000000, 0.9238795325112869605, 1.000000000000000000, 0.9238795325112869605, 1.000000000000000000, 0.9238795325112869605, 1.000000000000000000, 0.9238795325112869605, 1.000000000000000000, 0.9238795325112869605, 1.000000000000000000, 0.9238795325112869605, 1.000000000000000000, 0.9238795325112869605, 1.000000000000000000, 0.9238795325112869605, 1.000000000000000000, 0.9238795325112869605, 1.000000000000000000, 0.9238795325112869605, 1.000000000000000000, 0.9238795325112869605, 1.000000000000000000, 0.9238795325112869605, 1.000000000000000000, 0.9238795325112869605, 1.000000000000000000, 0.9238795325112869605, 1.000000000000000000, 0.9238795325112869605, 1.000000000000000000, 0.9238795325112869605, 1.000000000000000000, 0.9238795325112869605, 1.000000000000000000, 0.9238795325112869605, 1.000000000000000000, 0.9238795325112869605, 1.000000000000000000, 0.9238795325112869605, 1.000000000000000000, 0.9238795325112869605, 1.000000000000000000, 0.9238795325112869605, 1.000000000000000000, 0.9238795325112869605, 1.000000000000000000, 0.9238795325112869605, 1.000000000000000000, 0.9238795325112869605, 1.000000000000000000, 0.9238795325112869605, 1.000000000000000000, 0.9238795325112869605, 1.000000000000000000, 0.9238795325112869605, 1.000000000000000000, 0.9238795325112869605, 1.000000000000000000, 0.9238795325112869605, 1.000000000000000000, 0.9238795325112869605, 1.000000000000000000, 0.9238795325112869605, 1.000000000000000000, 0.9238795325112869605, 1.000000000000000000, 0.9238795325112869605, 1.000000000000000000, 0.9238795325112869605, 1.000000000000000000, 0.9238795325112869605, 1.000000000000000000, 0.9238795325112869605, 1.000000000000000000, 0.9238795325112869605, 1.000000000000000000, 0.9238795325112869605, 1.000000000000000000, 0.9238795325112869605, 1.000000000000000000, 0.9238795325112869605, 1.000000000000000000, 0.9238795325112869605, 1.000000000000000000, 0.9238795325112869605, 1.000000000000000000, 0.9238795325112869605, 1.000000000000000000, 0.9238795325112869605, 1.000000000000000000, 0.9238795325112869605, 1.000000000000000000, 0.9238795325112869605, 1.000000000000000000, 0.9238795325112869605, 1.000000000000000000, 0.9238795325112869605, 1.000000000000000000, 0.9238795325112869605, 1.000000000000000000, 0.9238795325112869605, 1.000000000000000000, 0.9238795325112869605, 1.000000000000000000, 0.9238795325112869605, 1.000000000000000000, 0.9238795325112869605, 1.000000000000000000, 0.9238795325112869605, 1.000000000000000000, 0.9238795325112869605, 1.000000000000000000, 0.9238795325112869605, 1.000000000000000000, 0.9238795325112869605, 1.000000000000000000, 0.9238795325112869605, 1.000000000000000000, 0.9238795325112869605, 1.000000000000000000, 0.9238795325112869605, 1.000000000000000000, 0.9238795325112869605, 1.000000000000000000, 0.9238795325112869605, 1.000000000000000000, 0.9238795325112869605, 1.000000000000000000, 0.9238795325112869605, 1.000000000000000000, 0.9238795325112869605, 1.000000000000000000, 0.9238795325112869605, 1.000000000000000000, 0.9238795325112869605, 1.000000000000000000, 0.9238795325112869605, 1.000000000000000000, 0.9238795325112869605, 1.000000000000000000, 0.9238795325112869605, 1.000000000000000000, 0.9238795325112869605, 1.000000000000000000, 0.9238795325112869605, 1.000000000000000000, 0.9238795325112869605, 1.000000000000000000, 0.9238795325112869605, 1.000000000000000000, 0.9238795325112869605, 1.000000000000000000 ) ) 
 REPRESENTATION_ITEM ( '' )  ) ;
#3329=CARTESIAN_POINT ( 'NONE',  ( -0.9500414927467378812, -0.1787899950787401604, 0.1328740156942679607 ) ) ;
#3331=VERTEX_POINT ( 'NONE', #7823 ) ;
#3332=VERTEX_POINT ( 'NONE', #15512 ) ;
#3334=( BOUNDED_CURVE ( )  B_SPLINE_CURVE ( 2, ( #34876, #16652, #1301, #31280, #41296, #4900, #15959, #17108, #39139 ),
 .UNSPECIFIED., .F., .F. ) 
 B_SPLINE_CURVE_WITH_KNOTS ( ( 3, 2, 2, 2, 3 ),
 ( 0.2899999999999999800, 0.2924999999999999822, 0.2949999999999999845, 0.2974999999999999867, 0.2999999999999999889 ),
 .UNSPECIFIED. ) 
 CURVE ( )  GEOMETRIC_REPRESENTATION_ITEM ( )  RATIONAL_B_SPLINE_CURVE ( ( 1.000000000000000000, 0.9238795325112869605, 1.000000000000000000, 0.9238795325112869605, 1.000000000000000000, 0.9238795325112869605, 1.000000000000000000, 0.9238795325112869605, 1.000000000000000000 ) ) 
 REPRESENTATION_ITEM ( '' )  ) ;
#3335=CARTESIAN_POINT ( 'NONE',  ( -0.9500414927467377701, 0.1787899950787401604, 1.451771653489543290 ) ) ;
#3340=DIRECTION ( 'NONE',  ( 0.000000000000000000, 0.000000000000000000, -1.000000000000000000 ) ) ;
#3342=CARTESIAN_POINT ( 'NONE',  ( 0.7185039370078739607, 0.000000000000000000, 4.498031496062992574 ) ) ;
#3343=CARTESIAN_POINT ( 'NONE',  ( -0.7185039370078746268, -0.06523048226347956391, 0.8882874014672753615 ) ) ;
#3345=CARTESIAN_POINT ( 'NONE',  ( 0.9873396505805591694, -0.1113553986120547346, 1.884842519577511810 ) ) ;
#3346=ORIENTED_EDGE ( 'NONE', *, *, #18537, .F. ) ;
#3348=CARTESIAN_POINT ( 'NONE',  ( 0.8759842519685039353, 0.1574803149606299191, 0.7677165354330708347 ) ) ;
#3349=CARTESIAN_POINT ( 'NONE',  ( -0.8759842519685039353, 0.1574803149606299191, 1.240157480314960647 ) ) ;
#3350=CARTESIAN_POINT ( 'NONE',  ( -0.7185039370078746268, -0.06523048226347956391, 0.4650590551181104093 ) ) ;
#3351=CARTESIAN_POINT ( 'NONE',  ( 1.033464566929133799, 0.000000000000000000, 1.505905511811023612 ) ) ;
#3352=CARTESIAN_POINT ( 'NONE',  ( 0.8107537697050253289, 0.1574803149606300301, 0.1304133857192446289 ) ) ;
#3353=EDGE_LOOP ( 'NONE', ( #10961, #43358, #12842, #5629 ) ) ;
#3354=CARTESIAN_POINT ( 'NONE',  ( 0.8759842519685039353, 0.000000000000000000, 1.995570866087968520 ) ) ;
#3357=CARTESIAN_POINT ( 'NONE',  ( -1.033464566929134687, -0.06523048226347956391, 0.1550196849318430659 ) ) ;
#3359=CARTESIAN_POINT ( 'NONE',  ( 0.9412147342319837628, -0.1574803149606297803, 1.016240157372787722 ) ) ;
#3360=CARTESIAN_POINT ( 'NONE',  ( 0.7646288533564489232, 0.1113553986120547346, 0.5364173228346457156 ) ) ;
#3361=EDGE_CURVE ( 'NONE', #37199, #1915, #34421, .T. ) ;
#3362=CARTESIAN_POINT ( 'NONE',  ( -1.002407869896990045, -0.1264236179284866091, 0.4109251967966299213 ) ) ;
#3363=ORIENTED_EDGE ( 'NONE', *, *, #21846, .F. ) ;
#3366=CARTESIAN_POINT ( 'NONE',  ( -1.054774247047244540, -0.07405724077823318263, 1.560039370024977057 ) ) ;
#3368=CARTESIAN_POINT ( 'NONE',  ( 1.054774247047244096, 0.000000000000000000, 1.483759842465921075 ) ) ;
#3371=CARTESIAN_POINT ( 'NONE',  ( -0.6971942568897626646, 0.07405724077823318263, 0.8316929133320636325 ) ) ;
#3372=CARTESIAN_POINT ( 'NONE',  ( 1.002407869896990045, 0.1264236179284866091, 0.2288385826234019815 ) ) ;
#3373=CARTESIAN_POINT ( 'NONE',  ( -0.7185039370078746268, 0.06523048226347956391, 0.2632874015748031260 ) ) ;
#3374=CARTESIAN_POINT ( 'NONE',  ( 1.002407869896990045, -0.1264236179284866091, 0.7701771653005669016 ) ) ;
#3375=CARTESIAN_POINT ( 'NONE',  ( -0.8759842519685039353, 0.1787899950787401882, 0.6619094487651338010 ) ) ;
#3378=CARTESIAN_POINT ( 'NONE',  ( 0.9412147342319837628, -0.1574803149606297803, 1.144192913385827737 ) ) ;
#3380=CARTESIAN_POINT ( 'NONE',  ( -0.9873396505805591694, -0.1113553986120547346, 1.845472440837354178 ) ) ;
#3383=CARTESIAN_POINT ( 'NONE',  ( -0.8759842519685039353, 0.1574803149606299191, 0.4133858267716535861 ) ) ;
#3384=CARTESIAN_POINT ( 'NONE',  ( 0.9500414927467377701, -0.1787899950787401604, 1.437007873961985593 ) ) ;
#3387=VERTEX_POINT ( 'NONE', #41095 ) ;
#3392=DIRECTION ( 'NONE',  ( -1.000000000000000000, 0.000000000000000000, 0.000000000000000000 ) ) ;
#3394=CARTESIAN_POINT ( 'NONE',  ( 0.7495606340400177148, -0.1264236179284866091, 0.3223425196312759144 ) ) ;
#3395=VECTOR ( 'NONE', #12019, 39.37007874015748143 ) ;
#3401=CARTESIAN_POINT ( 'NONE',  ( 0.8019270111902717657, 0.1787899950787401604, 0.6643700786863951935 ) ) ;
#3402=CARTESIAN_POINT ( 'NONE',  ( -1.002407869896990045, -0.1264236179284866091, 0.9670275590013542866 ) ) ;
#3403=CARTESIAN_POINT ( 'NONE',  ( -1.004065995148841539, 0.1041443272423887983, 0.03937007874015843734 ) ) ;
#3407=CARTESIAN_POINT ( 'NONE',  ( 1.033464566929133799, 0.000000000000000000, 1.702755905511810885 ) ) ;
#3408=CARTESIAN_POINT ( 'NONE',  ( 1.054774247047244096, 0.000000000000000000, 1.719980314906866203 ) ) ;
#3409=CARTESIAN_POINT ( 'NONE',  ( 1.033464566929133799, 0.000000000000000000, 0.6299212597349921339 ) ) ;
#3410=DIRECTION ( 'NONE',  ( 0.000000000000000000, 0.000000000000000000, 1.000000000000000000 ) ) ;
#3411=EDGE_CURVE ( 'NONE', #20105, #45765, #4689, .T. ) ;
#3414=CARTESIAN_POINT ( 'NONE',  ( 0.7646288533564489232, -0.1113553986120547346, 1.323818897530267602 ) ) ;
#3416=CARTESIAN_POINT ( 'NONE',  ( -0.6971942568897626646, -0.07405724077823297447, 0.4429133857730075952 ) ) ;
#3418=CARTESIAN_POINT ( 'NONE',  ( 0.8759842519685039353, 0.000000000000000000, 4.498031496062992574 ) ) ;
#3419=CARTESIAN_POINT ( 'NONE',  ( 1.033464566929133799, 0.000000000000000000, 1.102362204616881947 ) ) ;
#3420=EDGE_CURVE ( 'NONE', #11324, #20929, #5400, .T. ) ;
#3421=CARTESIAN_POINT ( 'NONE',  ( -0.9500414927467378812, -0.1787899950787401604, 1.628937007820252303 ) ) ;
#3424=CARTESIAN_POINT ( 'NONE',  ( -0.7495606340400177148, -0.1264236179284866091, 1.193405511757259951 ) ) ;
#3425=CARTESIAN_POINT ( 'NONE',  ( 0.8759842519685039353, -0.1574803149606299191, 0.4330708661417322913 ) ) ;
#3426=CARTESIAN_POINT ( 'NONE',  ( 1.002407869896990045, -0.1264236179284866091, 1.163877952702141672 ) ) ;
#3428=CARTESIAN_POINT ( 'NONE',  ( -1.033464566929134687, -0.06523048226347956391, 0.6668307085538908163 ) ) ;
#3429=CARTESIAN_POINT ( 'NONE',  ( 0.7495606340400177148, -0.1264236179284866091, 1.897145669237574772 ) ) ;
#3430=CARTESIAN_POINT ( 'NONE',  ( -0.8759842519685039353, -0.1574803149606299191, 0.5905511811023621549 ) ) ;
#3431=CARTESIAN_POINT ( 'NONE',  ( -0.6971942568897626646, 0.07405724077823318263, 0.8267716534895444003 ) ) ;
#3433=CARTESIAN_POINT ( 'NONE',  ( 1.054774247047244540, -0.07405724077823318263, 0.3395669290800949480 ) ) ;
#3434=CARTESIAN_POINT ( 'NONE',  ( -1.002407869896990045, -0.1264236179284866091, 0.2140748030958428971 ) ) ;
#3436=CARTESIAN_POINT ( 'NONE',  ( -0.8759842519685039353, 0.1787899950787401882, 0.7800196849856062542 ) ) ;
#3437=CARTESIAN_POINT ( 'NONE',  ( 0.9873396505805591694, -0.1113553986120547346, 1.569881889656251861 ) ) ;
#3440=ORIENTED_EDGE ( 'NONE', *, *, #25746, .T. ) ;
#3441=CARTESIAN_POINT ( 'NONE',  ( 1.054774247047244540, -0.07405724077823318263, 0.8513779527021426707 ) ) ;
#3442=CARTESIAN_POINT ( 'NONE',  ( 1.002407869896990045, -0.1264236179284866091, 1.085137795221826629 ) ) ;
#3443=CARTESIAN_POINT ( 'NONE',  ( -0.8759842519685039353, 0.1787899950787401882, 1.921751968450173376 ) ) ;
#3444=CARTESIAN_POINT ( 'NONE',  ( 0.6971942568897637749, 2.189545951927499583E-17, 1.892224409395055096 ) ) ;
#3446=( BOUNDED_CURVE ( )  B_SPLINE_CURVE ( 2, ( #28470, #25086, #10731, #43519, #26229, #24851, #40794, #7988, #39924 ),
 .UNSPECIFIED., .F., .T. ) 
 B_SPLINE_CURVE_WITH_KNOTS ( ( 3, 2, 2, 2, 3 ),
 ( 0.5500000000000000444, 0.5524999999999999911, 0.5550000000000000488, 0.5574999999999999956, 0.5600000000000000533 ),
 .UNSPECIFIED. ) 
 CURVE ( )  GEOMETRIC_REPRESENTATION_ITEM ( )  RATIONAL_B_SPLINE_CURVE ( ( 1.000000000000000000, 0.9238795325112869605, 1.000000000000000000, 0.9238795325112869605, 1.000000000000000000, 0.9238795325112869605, 1.000000000000000000, 0.9238795325112869605, 1.000000000000000000 ) ) 
 REPRESENTATION_ITEM ( '' )  ) ;
#3447=CARTESIAN_POINT ( 'NONE',  ( -0.7646288533564489232, -0.1113553986120547346, 0.1919291338582677087 ) ) ;
#3452=CARTESIAN_POINT ( 'NONE',  ( 0.7495606340400177148, -0.1264236179284866091, 1.227854330654897685 ) ) ;
#3455=CARTESIAN_POINT ( 'NONE',  ( 1.054774247047244096, 0.000000000000000000, 0.06151574797773248782 ) ) ;
#3462=CARTESIAN_POINT ( 'NONE',  ( -1.002407869896990045, -0.1264236179284866091, 0.5339566928596221063 ) ) ;
#3465=CARTESIAN_POINT ( 'NONE',  ( 0.9873396505805591694, 0.1113553986120547346, 1.432086614173228245 ) ) ;
#3466=CARTESIAN_POINT ( 'NONE',  ( 1.002407869896990045, 0.1264236179284866091, 1.291830708607653477 ) ) ;
#3467=CARTESIAN_POINT ( 'NONE',  ( 0.8019270111902716547, 0.1787899950787401604, 1.727362204670645385 ) ) ;
#3469=CARTESIAN_POINT ( 'NONE',  ( -1.033464566929133799, 0.000000000000000000, 0.5905511809948347235 ) ) ;
#3470=CARTESIAN_POINT ( 'NONE',  ( -1.033464566929133799, 0.000000000000000000, 0.9940944881889764995 ) ) ;
#3473=CARTESIAN_POINT ( 'NONE',  ( -0.9412147342319837628, 0.1574803149606300301, 1.660925196742867760 ) ) ;
#3474=CARTESIAN_POINT ( 'NONE',  ( 0.8019270111902717657, -0.1787899950787401604, 0.1279527558517483676 ) ) ;
#3476=CARTESIAN_POINT ( 'NONE',  ( 0.7495606340400177148, 0.1264236179284866091, 1.218011810969858111 ) ) ;
#3477=DIRECTION ( 'NONE',  ( -1.000000000000000000, 0.000000000000000000, 0.000000000000000000 ) ) ;
#3479=CARTESIAN_POINT ( 'NONE',  ( -1.002407869896990045, -0.1264236179284866091, 1.198326771599779628 ) ) ;
#3480=CARTESIAN_POINT ( 'NONE',  ( 0.7646288533564489232, 0.1113553986120547346, 0.5265748030420794867 ) ) ;
#3481=ORIENTED_EDGE ( 'NONE', *, *, #16668, .F. ) ;
#3482=CARTESIAN_POINT ( 'NONE',  ( 0.8772383532517480376, 0.1744612781842942717, 0.03936828611531264371 ) ) ;
#3483=CARTESIAN_POINT ( 'NONE',  ( -0.7185039370078746268, -0.06523048226347956391, 0.3371062991050715607 ) ) ;
#3484=ORIENTED_EDGE ( 'NONE', *, *, #10963, .F. ) ;
#3485=CARTESIAN_POINT ( 'NONE',  ( 0.6971942568897637749, 2.189545951927499583E-17, 1.498523621993480326 ) ) ;
#3486=CARTESIAN_POINT ( 'NONE',  ( -0.8107537697050254399, -0.1574803149606297803, 1.090059055010582423 ) ) ;
#3487=CARTESIAN_POINT ( 'NONE',  ( 1.033464566929133799, 0.000000000000000000, 1.023622047136567126 ) ) ;
#3488=DIRECTION ( 'NONE',  ( 0.000000000000000000, 0.000000000000000000, 1.000000000000000000 ) ) ;
#3494=CARTESIAN_POINT ( 'NONE',  ( -0.7646288533564489232, 0.1113553986120547346, 0.3789370078740157410 ) ) ;
#3496=ORIENTED_EDGE ( 'NONE', *, *, #34588, .F. ) ;
#3497=CARTESIAN_POINT ( 'NONE',  ( 0.8019270111902717657, 0.1787899950787401604, 0.5905511810485987167 ) ) ;
#3499=CARTESIAN_POINT ( 'NONE',  ( -0.7495606340400177148, -0.1264236179284866091, 1.503444881836000002 ) ) ;
#3502=CARTESIAN_POINT ( 'NONE',  ( -0.8107537697050234415, -0.1574803149606297803, 0.1156496062992125873 ) ) ;
#3504=CARTESIAN_POINT ( 'NONE',  ( -1.002407869896990045, -0.1264236179284866091, 1.040846456639149764 ) ) ;
#3505=CARTESIAN_POINT ( 'NONE',  ( -1.002407869896990045, -0.1264236179284866091, 0.7701771653005669016 ) ) ;
#3507=CARTESIAN_POINT ( 'NONE',  ( -0.6971942568897626646, -0.07405724077823297447, 0.1673228345919059168 ) ) ;
#3508=CARTESIAN_POINT ( 'NONE',  ( 0.8759842519685039353, 0.1574803149606299191, 0.7972440943806614611 ) ) ;
#3512=CARTESIAN_POINT ( 'NONE',  ( 1.033464566929134687, -0.06523048226347956391, 1.070374015748031038 ) ) ;
#3514=CARTESIAN_POINT ( 'NONE',  ( -0.7185039370078739607, 1.928577636452523993E-17, 1.722440944881889813 ) ) ;
#3516=CARTESIAN_POINT ( 'NONE',  ( -0.9500414927467378812, 0.1787899950787401604, 0.7381889763241898939 ) ) ;
#3518=CARTESIAN_POINT ( 'NONE',  ( -0.7495606340400177148, 0.1264236179284866091, 1.852854330654897685 ) ) ;
#3520=ORIENTED_EDGE ( 'NONE', *, *, #32106, .T. ) ;
#3522=CARTESIAN_POINT ( 'NONE',  ( -0.7495606340400177148, -0.1264236179284866091, 0.1304133857730082613 ) ) ;
#3523=CARTESIAN_POINT ( 'NONE',  ( 1.033464566929134687, -0.06523048226347956391, 0.6373031496062994128 ) ) ;
#3525=CARTESIAN_POINT ( 'NONE',  ( -0.8107537697050254399, 0.1574803149606300301, 0.4060039369003470289 ) ) ;
#3526=CARTESIAN_POINT ( 'NONE',  ( -0.8759842519685039353, -0.1574803149606299191, 1.328740157372787278 ) ) ;
#3527=CARTESIAN_POINT ( 'NONE',  ( 0.7495606340400177148, -0.1264236179284866091, 0.7997047243556849594 ) ) ;
#3528=EDGE_CURVE ( 'NONE', #20346, #18121, #39692, .T. ) ;
#3532=EDGE_CURVE ( 'NONE', #47083, #10797, #23209, .T. ) ;
#3534=CARTESIAN_POINT ( 'NONE',  ( 0.7646288533564489232, 0.1113553986120547346, 1.205708661417322913 ) ) ;
#3535=CARTESIAN_POINT ( 'NONE',  ( 0.7698820887372280763, -0.1341113977068105756, 1.986080103382252826 ) ) ;
#3536=CARTESIAN_POINT ( 'NONE',  ( -1.033464566929133799, 0.000000000000000000, 0.8267716534357796299 ) ) ;
#3539=ORIENTED_EDGE ( 'NONE', *, *, #34881, .T. ) ;
#3541=CARTESIAN_POINT ( 'NONE',  ( 0.8019270111902716547, 0.1787899950787401604, 0.6249999999462366729 ) ) ;
#3542=CARTESIAN_POINT ( 'NONE',  ( -0.8759842519685039353, 0.000000000000000000, 0.000000000000000000 ) ) ;
#3544=CARTESIAN_POINT ( 'NONE',  ( 0.8107537697050254399, 0.1574803149606300301, 1.557578740157481212 ) ) ;
#3545=CARTESIAN_POINT ( 'NONE',  ( -1.033464566929133799, 0.000000000000000000, 1.151574803149606474 ) ) ;
#3547=CARTESIAN_POINT ( 'NONE',  ( 0.6971942568897648851, 0.07405724077823318263, 1.023622047190330342 ) ) ;
#3552=CARTESIAN_POINT ( 'NONE',  ( -0.9500414927467378812, -0.1787899950787401604, 0.1722440944344254266 ) ) ;
#3553=CARTESIAN_POINT ( 'NONE',  ( 0.7646288533564489232, 0.1113553986120547346, 1.756889763779527547 ) ) ;
#3554=ORIENTED_EDGE ( 'NONE', *, *, #31241, .F. ) ;
#3556=CARTESIAN_POINT ( 'NONE',  ( -0.9500414927467377701, -0.1787899950787401604, 1.948818897584033705 ) ) ;
#3557=CARTESIAN_POINT ( 'NONE',  ( -1.054774247047244540, -0.07405724077823318263, 1.673228346402929834 ) ) ;
#3559=CARTESIAN_POINT ( 'NONE',  ( -1.054774247047244540, 0.07405724077823318263, 1.048228346402928723 ) ) ;
#3560=CARTESIAN_POINT ( 'NONE',  ( -1.054774247047244540, 0.07405724077823318263, 0.3444881889226146243 ) ) ;
#3562=CARTESIAN_POINT ( 'NONE',  ( 0.9873396505805591694, 0.1113553986120547346, 0.2903543307086614012 ) ) ;
#3563=CARTESIAN_POINT ( 'NONE',  ( -0.7646288533564489232, 0.1113553986120547346, 1.875000000000000000 ) ) ;
#3568=CARTESIAN_POINT ( 'NONE',  ( -0.9500414927467378812, -0.1787899950787401604, 0.2903543306548980185 ) ) ;
#3571=CARTESIAN_POINT ( 'NONE',  ( -0.8019270111902716547, 0.1787899950787401604, 1.377952755851748368 ) ) ;
#3577=CARTESIAN_POINT ( 'NONE',  ( 0.9412147342319837628, -0.1574803149606297803, 0.3961614173228344971 ) ) ;
#3580=CARTESIAN_POINT ( 'NONE',  ( -0.8107537697050253289, 0.1574803149606300301, 0.9571850392625528281 ) ) ;
#3581=CARTESIAN_POINT ( 'NONE',  ( 1.002407869896990045, -0.1264236179284866091, 0.4552165353793071745 ) ) ;
#3582=CARTESIAN_POINT ( 'NONE',  ( 0.8107537697050253289, -0.1574803149606297803, 1.798720472333418918 ) ) ;
#3585=CARTESIAN_POINT ( 'NONE',  ( 0.7646288533564489232, 0.1113553986120547346, 0.8120078740157481434 ) ) ;
#3588=CARTESIAN_POINT ( 'NONE',  ( 1.033464566929134687, -0.06523048226347956391, 0.7554133858267708668 ) ) ;
#3590=ORIENTED_EDGE ( 'NONE', *, *, #47018, .T. ) ;
#3591=CARTESIAN_POINT ( 'NONE',  ( -0.8107537697050254399, -0.1574803149606297803, 0.6176181101286931652 ) ) ;
#3595=CARTESIAN_POINT ( 'NONE',  ( -0.9412147342319837628, 0.1574803149606300301, 0.1648622046168823629 ) ) ;
#3597=CARTESIAN_POINT ( 'NONE',  ( 0.7185039370078746268, -0.06523048226347956391, 1.006397637687749036 ) ) ;
#3599=CARTESIAN_POINT ( 'NONE',  ( -1.054774247047244096, 0.000000000000000000, 0.3371062991588349989 ) ) ;
#3601=ORIENTED_EDGE ( 'NONE', *, *, #10246, .F. ) ;
#3603=CARTESIAN_POINT ( 'NONE',  ( -1.054774247047244540, 0.07405724077823318263, 1.604330708607653921 ) ) ;
#3604=EDGE_LOOP ( 'NONE', ( #26995, #473, #33235, #7368 ) ) ;
#3605=CARTESIAN_POINT ( 'NONE',  ( 0.9500414927467378812, 0.1787899950787401604, 1.569881889710015299 ) ) ;
#3607=CARTESIAN_POINT ( 'NONE',  ( -0.8759842519685039353, 0.1787899950787401882, 0.8243110235682834519 ) ) ;
#3608=CARTESIAN_POINT ( 'NONE',  ( -0.9412147342319837628, -0.1574803149606297803, 0.4650590550105836440 ) ) ;
#3609=CARTESIAN_POINT ( 'NONE',  ( -1.054774247047244540, -0.07405724077823318263, 0.7677165353793073965 ) ) ;
#3611=( BOUNDED_CURVE ( )  B_SPLINE_CURVE ( 2, ( #23975, #31875, #5971, #13637, #28276, #46221, #42839, #31175, #35694 ),
 .UNSPECIFIED., .F., .T. ) 
 B_SPLINE_CURVE_WITH_KNOTS ( ( 3, 2, 2, 2, 3 ),
 ( 0.7500000000000000000, 0.7524999999999999467, 0.7550000000000000044, 0.7574999999999999512, 0.7600000000000000089 ),
 .UNSPECIFIED. ) 
 CURVE ( )  GEOMETRIC_REPRESENTATION_ITEM ( )  RATIONAL_B_SPLINE_CURVE ( ( 1.000000000000000000, 0.9238795325112869605, 1.000000000000000000, 0.9238795325112869605, 1.000000000000000000, 0.9238795325112869605, 1.000000000000000000, 0.9238795325112869605, 1.000000000000000000 ) ) 
 REPRESENTATION_ITEM ( '' )  ) ;
#3613=CARTESIAN_POINT ( 'NONE',  ( -0.9500414927467378812, -0.1787899950787401604, 1.515748031442299526 ) ) ;
#3614=CARTESIAN_POINT ( 'NONE',  ( -0.7185039370078746268, -0.06523048226347956391, 1.872539369971213841 ) ) ;
#3616=( BOUNDED_CURVE ( )  B_SPLINE_CURVE ( 2, ( #15712, #37971, #12824, #31269, #37734, #19749, #30347, #5362, #16177 ),
 .UNSPECIFIED., .F., .F. ) 
 B_SPLINE_CURVE_WITH_KNOTS ( ( 3, 2, 2, 2, 3 ),
 ( 0.4000000000000000222, 0.4025000000000000244, 0.4050000000000000266, 0.4074999999999999734, 0.4099999999999999756 ),
 .UNSPECIFIED. ) 
 CURVE ( )  GEOMETRIC_REPRESENTATION_ITEM ( )  RATIONAL_B_SPLINE_CURVE ( ( 1.000000000000000000, 0.9238795325112869605, 1.000000000000000000, 0.9238795325112869605, 1.000000000000000000, 0.9238795325112869605, 1.000000000000000000, 0.9238795325112849621, 1.000000000000000000 ) ) 
 REPRESENTATION_ITEM ( '' )  ) ;
#3617=CARTESIAN_POINT ( 'NONE',  ( 0.8759842519685039353, -0.1574803149606299191, 0.9744094487113701408 ) ) ;
#3618=CARTESIAN_POINT ( 'NONE',  ( 0.7495606340400177148, 0.1264236179284866091, 1.498523621993480326 ) ) ;
#3620=CARTESIAN_POINT ( 'NONE',  ( -0.7185039370078739607, 1.928577636452523993E-17, 0.3740157479239689664 ) ) ;
#3623=VERTEX_POINT ( 'NONE', #42524 ) ;
#3625=CYLINDRICAL_SURFACE ( 'NONE', #33839, 0.1574803149606299191 ) ;
#3629=CARTESIAN_POINT ( 'NONE',  ( 0.6971942568897637749, 2.189545951927499583E-17, 0.3567913385289137596 ) ) ;
#3637=CARTESIAN_POINT ( 'NONE',  ( 1.002407869896990045, -0.1264236179284866091, 0.5684055117572598403 ) ) ;
#3638=CARTESIAN_POINT ( 'NONE',  ( -0.9909871089404796995, 0.1202360962797062310, 0.03937007874015843040 ) ) ;
#3639=CARTESIAN_POINT ( 'NONE',  ( 1.033464566929134687, 0.06523048226347956391, 1.114665354330708125 ) ) ;
#3643=CARTESIAN_POINT ( 'NONE',  ( 0.6971942568897648851, 0.07405724077823318263, 1.737204724355685848 ) ) ;
#3649=CARTESIAN_POINT ( 'NONE',  ( -1.002407869896990045, 0.1264236179284866091, 0.4650590550643464716 ) ) ;
#3652=CARTESIAN_POINT ( 'NONE',  ( 0.7495606340400177148, -0.1264236179284866091, 0.09104330703285078152 ) ) ;
#3654=CARTESIAN_POINT ( 'NONE',  ( -1.054774247047244540, -0.07405724077823318263, 1.633858267662771313 ) ) ;
#3655=VERTEX_POINT ( 'NONE', #24567 ) ;
#3656=CARTESIAN_POINT ( 'NONE',  ( -1.002407869896990045, 0.1264236179284866091, 1.213090551127338435 ) ) ;
#3657=CARTESIAN_POINT ( 'NONE',  ( -0.9412147342319837628, 0.1574803149606300301, 0.8833661417322832277 ) ) ;
#3658=CARTESIAN_POINT ( 'NONE',  ( 0.8019270111902717657, -0.1787899950787401604, 1.117125984198206412 ) ) ;
#3659=CARTESIAN_POINT ( 'NONE',  ( 0.9500414927467378812, -0.1787899950787401604, 1.865157480261195877 ) ) ;
#3660=CARTESIAN_POINT ( 'NONE',  ( -0.9412147342319837628, -0.1574803149606297803, 0.6323818897637792924 ) ) ;
#3661=CARTESIAN_POINT ( 'NONE',  ( -0.6971942568897637749, 2.189545951927499583E-17, 1.026082677111590513 ) ) ;
#3664=CARTESIAN_POINT ( 'NONE',  ( 0.7495606340400177148, 0.1264236179284866091, 0.2780511810485988278 ) ) ;
#3665=CARTESIAN_POINT ( 'NONE',  ( -1.002407869896990045, 0.1264236179284866091, 0.3026574802611972648 ) ) ;
#3666=CARTESIAN_POINT ( 'NONE',  ( -0.6971942568897626646, 0.07405724077823318263, 0.6692913385289144257 ) ) ;
#3667=CARTESIAN_POINT ( 'NONE',  ( 0.9412147342319837628, 0.1574803149606300301, 1.660925196742867760 ) ) ;
#3668=VERTEX_POINT ( 'NONE', #46595 ) ;
#3669=EDGE_CURVE ( 'NONE', #8361, #5177, #6963, .T. ) ;
#3671=CARTESIAN_POINT ( 'NONE',  ( 1.054774247047244096, 0.000000000000000000, 0.7750984251430865779 ) ) ;
#3672=CARTESIAN_POINT ( 'NONE',  ( 0.7495606340400177148, 0.1264236179284866091, 1.026082677111590513 ) ) ;
#3673=CARTESIAN_POINT ( 'NONE',  ( -0.6971942568897637749, 2.189545951927499583E-17, 1.931594488135212728 ) ) ;
#3674=CARTESIAN_POINT ( 'NONE',  ( 1.054774247047244540, -0.07405724077823318263, 1.948818897584033927 ) ) ;
#3678=ORIENTED_EDGE ( 'NONE', *, *, #17590, .F. ) ;
#3680=EDGE_CURVE ( 'NONE', #36578, #22073, #43222, .T. ) ;
#3683=CARTESIAN_POINT ( 'NONE',  ( 0.7495606340400177148, -0.1264236179284866091, 1.149114173174582643 ) ) ;
#3687=CARTESIAN_POINT ( 'NONE',  ( 0.8019270111902717657, 0.1787899950787401604, 1.530511810969859443 ) ) ;
#3688=CARTESIAN_POINT ( 'NONE',  ( 1.033464566929134687, -0.06523048226347956391, 1.975885826771653475 ) ) ;
#3694=CARTESIAN_POINT ( 'NONE',  ( -0.7495606340400177148, 0.1264236179284866091, 0.5536417322297008115 ) ) ;
#3696=CARTESIAN_POINT ( 'NONE',  ( -0.7103770212304942877, 0.007401083536364823356, 1.983133876338081913 ) ) ;
#3697=CARTESIAN_POINT ( 'NONE',  ( -0.7185039370078739607, 1.928577636452523993E-17, 1.210629921259842590 ) ) ;
#3698=CARTESIAN_POINT ( 'NONE',  ( 0.9500414927467378812, -0.1787899950787401604, 1.161417322780881278 ) ) ;
#3699=CARTESIAN_POINT ( 'NONE',  ( 0.6971942568897648851, -0.07405724077823297447, 1.737204724355685626 ) ) ;
#3700=CARTESIAN_POINT ( 'NONE',  ( 0.9412147342319837628, 0.1574803149606300301, 1.503444881782235232 ) ) ;
#3701=DIRECTION ( 'NONE',  ( 1.822029033848725028E-16, 0.000000000000000000, 1.000000000000000000 ) ) ;
#3702=CARTESIAN_POINT ( 'NONE',  ( -0.7733127964711655755, 0.1243806286706488490, 1.980518068217838268 ) ) ;
#3705=CARTESIAN_POINT ( 'NONE',  ( 0.9412147342319837628, 0.1574803149606300301, 0.7554133857192454338 ) ) ;
#3707=CARTESIAN_POINT ( 'NONE',  ( 1.002407869896990045, 0.1264236179284866091, 0.2239173227808822775 ) ) ;
#3708=CARTESIAN_POINT ( 'NONE',  ( 0.7322234030063883292, -0.08795665246346720534, 0.03937064163498438241 ) ) ;
#3709=CARTESIAN_POINT ( 'NONE',  ( 0.6971942568897637749, 2.189545951927499583E-17, 1.222933070812378009 ) ) ;
#3710=DIRECTION ( 'NONE',  ( 1.822029033848725028E-16, 0.000000000000000000, 1.000000000000000000 ) ) ;
#3711=CARTESIAN_POINT ( 'NONE',  ( -1.054774247047244096, 0.000000000000000000, 1.203248031442299304 ) ) ;
#3712=CARTESIAN_POINT ( 'NONE',  ( 1.033464566929134687, 0.06523048226347956391, 0.6717519683964102706 ) ) ;
#3715=CARTESIAN_POINT ( 'NONE',  ( 0.9291354005038431341, 0.1626576089091155419, 0.03937007862967787514 ) ) ;
#3716=CARTESIAN_POINT ( 'NONE',  ( 0.7185039370078739607, 1.928577636452523993E-17, 0.8464566928058583350 ) ) ;
#3717=CARTESIAN_POINT ( 'NONE',  ( -0.9873396505805591694, 0.1113553986120547346, 0.3592519683964098820 ) ) ;
#3719=CARTESIAN_POINT ( 'NONE',  ( 1.002407869896990045, -0.1264236179284866091, 1.395177165300567124 ) ) ;
#3720=CARTESIAN_POINT ( 'NONE',  ( -0.7185039370078746268, -0.06523048226347956391, 1.085137795168063191 ) ) ;
#3721=CYLINDRICAL_SURFACE ( 'NONE', #12744, 0.1574803149606299191 ) ;
#3725=( BOUNDED_CURVE ( )  B_SPLINE_CURVE ( 2, ( #35668, #14564, #28738, #28244, #10020, #3544, #43782, #21265, #10507 ),
 .UNSPECIFIED., .F., .T. ) 
 B_SPLINE_CURVE_WITH_KNOTS ( ( 3, 2, 2, 2, 3 ),
 ( 0.7800000000000000266, 0.7824999999999999734, 0.7850000000000000311, 0.7874999999999999778, 0.7900000000000000355 ),
 .UNSPECIFIED. ) 
 CURVE ( )  GEOMETRIC_REPRESENTATION_ITEM ( )  RATIONAL_B_SPLINE_CURVE ( ( 1.000000000000000000, 0.9238795325112869605, 1.000000000000000000, 0.9238795325112869605, 1.000000000000000000, 0.9238795325112869605, 1.000000000000000000, 0.9238795325112869605, 1.000000000000000000 ) ) 
 REPRESENTATION_ITEM ( '' )  ) ;
#3727=VERTEX_POINT ( 'NONE', #20087 ) ;
#3728=CARTESIAN_POINT ( 'NONE',  ( 0.6971942568897637749, 2.189545951927499583E-17, 0.5191929133320630774 ) ) ;
#3731=CARTESIAN_POINT ( 'NONE',  ( -0.8019270111902717657, -0.1787899950787401604, 1.077755905458048113 ) ) ;
#3734=CARTESIAN_POINT ( 'NONE',  ( -0.7185039370078746268, 0.06523048226347956391, 0.4896653542231815259 ) ) ;
#3735=CARTESIAN_POINT ( 'NONE',  ( -0.6971942568897626646, 0.07405724077823318263, 0.8316929133320636325 ) ) ;
#3737=CARTESIAN_POINT ( 'NONE',  ( -1.054774247047244096, 0.000000000000000000, 0.2632874015210397434 ) ) ;
#3740=CARTESIAN_POINT ( 'NONE',  ( 0.8107537697050254399, -0.1574803149606297803, 1.060531496062992352 ) ) ;
#3743=CARTESIAN_POINT ( 'NONE',  ( -0.7185039370078739607, 1.928577636452523993E-17, 0.5413385826771653919 ) ) ;
#3746=CARTESIAN_POINT ( 'NONE',  ( -0.9500414927467378812, -0.1787899950787401604, 0.7627952755367881643 ) ) ;
#3748=CARTESIAN_POINT ( 'NONE',  ( -1.002407869896990045, -0.1264236179284866091, 1.833169291284818758 ) ) ;
#3750=CARTESIAN_POINT ( 'NONE',  ( 0.7646288533564489232, -0.1113553986120547346, 0.6643700787401575214 ) ) ;
#3753=CARTESIAN_POINT ( 'NONE',  ( -0.8107537697050253289, -0.1574803149606297803, 1.483759842412158525 ) ) ;
#3754=CARTESIAN_POINT ( 'NONE',  ( 1.002407869896990045, 0.1264236179284866091, 0.8193897637257637756 ) ) ;
#3756=CARTESIAN_POINT ( 'NONE',  ( 0.7185039370078746268, 0.06523048226347956391, 1.483759842519686067 ) ) ;
#3758=CARTESIAN_POINT ( 'NONE',  ( 0.8502105270501296719, -0.1718181285865334196, 1.987735233414207769 ) ) ;
#3762=CARTESIAN_POINT ( 'NONE',  ( 0.8759842519685039353, -0.1787899950787401882, 0.7997047243556849594 ) ) ;
#3768=DIRECTION ( 'NONE',  ( -4.336808689942014285E-16, 0.000000000000000000, -1.000000000000000000 ) ) ;
#3770=CARTESIAN_POINT ( 'NONE',  ( 0.6971942568897637749, 2.189545951927499583E-17, 0.9079724408911180600 ) ) ;
#3777=CARTESIAN_POINT ( 'NONE',  ( -1.054774247047244096, 0.000000000000000000, 1.995570866087968520 ) ) ;
#3779=CARTESIAN_POINT ( 'NONE',  ( 0.7185039370078739607, 1.928577636452523993E-17, 0.9350393700787401619 ) ) ;
#3781=CARTESIAN_POINT ( 'NONE',  ( -0.6971942568897637749, 2.189545951927499583E-17, 1.656003936954110412 ) ) ;
#3782=ORIENTED_EDGE ( 'NONE', *, *, #13868, .F. ) ;
#3784=CARTESIAN_POINT ( 'NONE',  ( -0.8019270111902717657, 0.1787899950787401604, 1.058070866087969186 ) ) ;
#3785=CARTESIAN_POINT ( 'NONE',  ( -0.8759842519685039353, 0.1787899950787401882, 0.4306102361667086820 ) ) ;
#3786=EDGE_CURVE ( 'NONE', #40728, #6896, #36945, .T. ) ;
#3787=LINE ( 'NONE', #43799, #29921 ) ;
#3789=CARTESIAN_POINT ( 'NONE',  ( 0.8107537697050254399, 0.1574803149606300301, 0.2977362204724410821 ) ) ;
#3790=CARTESIAN_POINT ( 'NONE',  ( 0.6971942568897626646, -0.07405724077823297447, 0.08366141726907129483 ) ) ;
#3793=CYLINDRICAL_SURFACE ( 'NONE', #25751, 0.1574803149606299191 ) ;
#3796=CARTESIAN_POINT ( 'NONE',  ( -0.8759842519685039353, -0.1787899950787401882, 0.3666338582139531677 ) ) ;
#3798=CARTESIAN_POINT ( 'NONE',  ( -0.8019270111902716547, 0.1787899950787401604, 1.417322834591906444 ) ) ;
#3805=DIRECTION ( 'NONE',  ( 0.000000000000000000, 0.000000000000000000, -1.000000000000000000 ) ) ;
#3806=CARTESIAN_POINT ( 'NONE',  ( -0.7185039370078746268, 0.06523048226347956391, 1.080216535325543958 ) ) ;
#3807=CARTESIAN_POINT ( 'NONE',  ( 1.002407869896990045, 0.1264236179284866091, 0.4650590550643464716 ) ) ;
#3809=CARTESIAN_POINT ( 'NONE',  ( 1.033464566929134687, 0.06523048226347956391, 1.852854330601134691 ) ) ;
#3811=CARTESIAN_POINT ( 'NONE',  ( 0.9412147342319837628, -0.1574803149606297803, 0.9473425196850395746 ) ) ;
#3814=CARTESIAN_POINT ( 'NONE',  ( 0.9873396505805591694, -0.1113553986120547346, 1.540354330708661568 ) ) ;
#3815=CARTESIAN_POINT ( 'NONE',  ( 0.7646288533564489232, -0.1113553986120547346, 0.7824803149606299746 ) ) ;
#3817=VERTEX_POINT ( 'NONE', #28483 ) ;
#3824=CARTESIAN_POINT ( 'NONE',  ( -0.9873396505805591694, 0.1113553986120547346, 0.08366141721530767628 ) ) ;
#3826=CARTESIAN_POINT ( 'NONE',  ( 0.7185039370078739607, 1.928577636452523993E-17, 1.003937007766488199 ) ) ;
#3828=VECTOR ( 'NONE', #39185, 39.37007874015748143 ) ;
#3829=ORIENTED_EDGE ( 'NONE', *, *, #27144, .T. ) ;
#3831=ORIENTED_EDGE ( 'NONE', *, *, #9928, .T. ) ;
#3832=CARTESIAN_POINT ( 'NONE',  ( -0.9500414927467378812, 0.1787899950787401604, 1.569881889710015299 ) ) ;
#3833=CARTESIAN_POINT ( 'NONE',  ( 1.054774247047244540, -0.07405724077823318263, 1.678149606245448622 ) ) ;
#3835=CARTESIAN_POINT ( 'NONE',  ( -0.8759842519685039353, 0.1787899950787401882, 0.7455708660879684091 ) ) ;
#3836=CARTESIAN_POINT ( 'NONE',  ( 0.8019270111902717657, -0.1787899950787401604, 0.3297244093950552069 ) ) ;
#3837=CARTESIAN_POINT ( 'NONE',  ( -0.7646288533564489232, -0.1113553986120547346, 0.4576771652468039631 ) ) ;
#3838=CARTESIAN_POINT ( 'NONE',  ( -1.054774247047244540, 0.07405724077823318263, 0.6938976377415124741 ) ) ;
#3840=CARTESIAN_POINT ( 'NONE',  ( -0.8759842519685039353, 0.000000000000000000, 0.000000000000000000 ) ) ;
#3841=EDGE_CURVE ( 'NONE', #8310, #43583, #2567, .T. ) ;
#3842=CARTESIAN_POINT ( 'NONE',  ( -0.7185039370078739607, 1.928577636452523993E-17, 1.673228346349165285 ) ) ;
#3843=CARTESIAN_POINT ( 'NONE',  ( -0.8759842519685039353, -0.1787899950787401882, 1.631397637741511808 ) ) ;
#3844=CARTESIAN_POINT ( 'NONE',  ( -0.8759842519685039353, -0.1574803149606299191, 1.840551180994834501 ) ) ;
#3846=CARTESIAN_POINT ( 'NONE',  ( -1.033464566929134687, -0.06523048226347956391, 1.621555118110237004 ) ) ;
#3848=CARTESIAN_POINT ( 'NONE',  ( 0.8759842519685039353, -0.1787899950787401882, 1.395177165300567124 ) ) ;
#3850=CARTESIAN_POINT ( 'NONE',  ( -0.8759842519685039353, -0.1574803149606299191, 1.574803149606299302 ) ) ;
#3852=EDGE_CURVE ( 'NONE', #33479, #32278, #44586, .T. ) ;
#3860=AXIS2_PLACEMENT_3D ( 'NONE', #42916, #11255, #46765 ) ;
#3861=CARTESIAN_POINT ( 'NONE',  ( 0.8759842519685039353, 0.000000000000000000, 1.990649606245448844 ) ) ;
#3863=CARTESIAN_POINT ( 'NONE',  ( 1.054774247047244540, 0.07405724077823318263, 1.796259842465923073 ) ) ;
#3868=CARTESIAN_POINT ( 'NONE',  ( 0.8107537697050234415, -0.1574803149606297803, 0.1451771652468037688 ) ) ;
#3869=CARTESIAN_POINT ( 'NONE',  ( 0.7495606340400177148, -0.1264236179284866091, 0.5585629920722204877 ) ) ;
#3874=CARTESIAN_POINT ( 'NONE',  ( 0.6971942568897648851, -0.07405724077823297447, 1.860236220418677089 ) ) ;
#3876=CARTESIAN_POINT ( 'NONE',  ( 1.033464566929136907, -0.06523048226347749612, 1.887303149498772425 ) ) ;
#3880=CARTESIAN_POINT ( 'NONE',  ( -0.6971942568897626646, -0.07405724077823297447, 0.4822834645131655606 ) ) ;
#3883=CARTESIAN_POINT ( 'NONE',  ( 0.8019270111902717657, -0.1787899950787401604, 0.1328740156942679607 ) ) ;
#3885=CARTESIAN_POINT ( 'NONE',  ( -1.054774247047244540, 0.07405724077823318263, 1.599409448765135133 ) ) ;
#3888=CARTESIAN_POINT ( 'NONE',  ( 0.8759842519685039353, -0.1787899950787401882, 0.05659448813521291560 ) ) ;
#3889=CARTESIAN_POINT ( 'NONE',  ( -0.7185039370078739607, 1.928577636452523993E-17, 0.5413385826771653919 ) ) ;
#3890=CARTESIAN_POINT ( 'NONE',  ( -0.8019270111902717657, 0.1787899950787401604, 1.018700787347811110 ) ) ;
#3892=CARTESIAN_POINT ( 'NONE',  ( 0.7495606340400177148, -0.1264236179284866091, 0.3666338582139531677 ) ) ;
#3893=CARTESIAN_POINT ( 'NONE',  ( -0.9500414927467377701, 0.1787899950787401604, 0.3051181101824569919 ) ) ;
#3894=CARTESIAN_POINT ( 'NONE',  ( -1.054774247047244540, -0.07405724077823318263, 0.8070866141194653620 ) ) ;
#3895=CARTESIAN_POINT ( 'NONE',  ( 0.7185039370078746268, -0.06523048226347956391, 1.715059055010583311 ) ) ;
#3899=CARTESIAN_POINT ( 'NONE',  ( 0.9500414927467377701, -0.1787899950787401604, 1.122047244040725422 ) ) ;
#3900=CARTESIAN_POINT ( 'NONE',  ( -0.7495606340400177148, -0.1264236179284866091, 1.818405511757259729 ) ) ;
#3904=CARTESIAN_POINT ( 'NONE',  ( 0.6971942568897648851, 0.07405724077823318263, 1.889763779473794258 ) ) ;
#3906=DIRECTION ( 'NONE',  ( 1.000000000000000000, 0.000000000000000000, -1.822029033848725275E-16 ) ) ;
#3912=CARTESIAN_POINT ( 'NONE',  ( 0.7495606340400177148, 0.1264236179284866091, 1.178641732229700922 ) ) ;
#3914=CARTESIAN_POINT ( 'NONE',  ( 0.7185039370078692977, 0.06523048226347515077, 1.395177165246803908 ) ) ;
#3915=CARTESIAN_POINT ( 'NONE',  ( 1.054774247047244540, -0.07405724077823318263, 1.476377952702141449 ) ) ;
#3916=CARTESIAN_POINT ( 'NONE',  ( 0.6971942568897637749, 2.189545951927499583E-17, 0.1599409448281264023 ) ) ;
#3921=CARTESIAN_POINT ( 'NONE',  ( -0.7495606340400177148, 0.1264236179284866091, 0.4355314960092284138 ) ) ;
#3922=CARTESIAN_POINT ( 'NONE',  ( -0.9412147342319837628, -0.1574803149606297803, 1.291830708553889595 ) ) ;
#3925=CARTESIAN_POINT ( 'NONE',  ( -0.7096583094928544666, -0.002683553454102774460, 1.983317742401899286 ) ) ;
#3926=CARTESIAN_POINT ( 'NONE',  ( 0.7646288533564489232, 0.1113553986120547346, 1.441929133858267598 ) ) ;
#3927=CARTESIAN_POINT ( 'NONE',  ( 0.6971942568897648851, -0.07405724077823297447, 1.348425196796630976 ) ) ;
#3928=CARTESIAN_POINT ( 'NONE',  ( 0.8759842519685039353, 0.1787899950787401882, 1.685531496009228469 ) ) ;
#3932=DIRECTION ( 'NONE',  ( 0.000000000000000000, 0.000000000000000000, -1.000000000000000000 ) ) ;
#3933=CARTESIAN_POINT ( 'NONE',  ( 0.8759842519685039353, 0.1574803149606299191, 0.7578740156405039397 ) ) ;
#3934=CARTESIAN_POINT ( 'NONE',  ( 0.8019270111902717657, -0.1787899950787401604, 0.2854330708123783422 ) ) ;
#3935=CARTESIAN_POINT ( 'NONE',  ( -0.7185039370078739607, 0.000000000000000000, -2.869337061179095023E-17 ) ) ;
#3937=LINE ( 'NONE', #341, #13875 ) ;
#3938=CARTESIAN_POINT ( 'NONE',  ( -0.6971942568897648851, 0.07405724077823318263, 1.259842519631276359 ) ) ;
#3939=CARTESIAN_POINT ( 'NONE',  ( 1.033464566929134687, -0.06523048226347956391, 0.5880905510735753294 ) ) ;
#3940=VERTEX_POINT ( 'NONE', #24864 ) ;
#3942=CARTESIAN_POINT ( 'NONE',  ( 0.9297866679844647431, 0.1623955463951254619, 0.03937007045119578913 ) ) ;
#3943=DIRECTION ( 'NONE',  ( 0.000000000000000000, -1.000000000000000000, 0.000000000000000000 ) ) ;
#3944=CARTESIAN_POINT ( 'NONE',  ( 0.6971942568897648851, 0.07405724077823318263, 1.574803149552536530 ) ) ;
#3947=CARTESIAN_POINT ( 'NONE',  ( 0.8107537697050254399, -0.1574803149606297803, 1.178641732283464583 ) ) ;
#3949=ORIENTED_EDGE ( 'NONE', *, *, #32760, .F. ) ;
#3954=CARTESIAN_POINT ( 'NONE',  ( 0.8759842519685039353, 0.1787899950787401882, 0.6274606298674959559 ) ) ;
#3955=VERTEX_POINT ( 'NONE', #28016 ) ;
#3956=CARTESIAN_POINT ( 'NONE',  ( -0.9500414927467377701, -0.1787899950787401604, 1.471456692859622217 ) ) ;
#3958=CARTESIAN_POINT ( 'NONE',  ( -0.6971942568897648851, -0.07405724077823297447, 1.072834645615528659 ) ) ;
#3962=CARTESIAN_POINT ( 'NONE',  ( -0.7495606340400177148, -0.1264236179284866091, 0.7603346456155274380 ) ) ;
#3963=AXIS2_PLACEMENT_3D ( 'NONE', #21985, #36607, #33273 ) ;
#3965=CARTESIAN_POINT ( 'NONE',  ( -1.054774247047244540, -0.07405724077823318263, 0.2214566928596220785 ) ) ;
#3974=CARTESIAN_POINT ( 'NONE',  ( -0.9500414927467378812, -0.1787899950787401604, 0.7234251967966300878 ) ) ;
#3976=CARTESIAN_POINT ( 'NONE',  ( -0.8019270111902716547, 0.1787899950787401604, 1.811023621993480548 ) ) ;
#3977=CARTESIAN_POINT ( 'NONE',  ( -0.6971942568897637749, 2.189545951927499583E-17, 0.08612204719033110523 ) ) ;
#3978=CARTESIAN_POINT ( 'NONE',  ( -1.033464566929133799, 0.000000000000000000, 0.9153543307086614567 ) ) ;
#3981=CARTESIAN_POINT ( 'NONE',  ( -0.9873396505805591694, -0.1113553986120547346, 1.569881889656251861 ) ) ;
#3982=CARTESIAN_POINT ( 'NONE',  ( 0.7495606340400177148, -0.1264236179284866091, 0.8390748030958424808 ) ) ;
#3985=CARTESIAN_POINT ( 'NONE',  ( 0.7646288533564489232, -0.1113553986120547346, 1.451771653543306950 ) ) ;
#3986=CARTESIAN_POINT ( 'NONE',  ( 0.9720564657138344167, -0.1495739268380064380, 1.989996134449682375 ) ) ;
#3987=DIRECTION ( 'NONE',  ( 1.822029033848725028E-16, 0.000000000000000000, 1.000000000000000000 ) ) ;
#3988=( BOUNDED_CURVE ( )  B_SPLINE_CURVE ( 2, ( #12209, #27561, #16513, #38072, #8356, #38547, #26833, #27323, #5711 ),
 .UNSPECIFIED., .F., .T. ) 
 B_SPLINE_CURVE_WITH_KNOTS ( ( 3, 2, 2, 2, 3 ),
 ( 0.6199999999999999956, 0.6225000000000000533, 0.6250000000000000000, 0.6274999999999999467, 0.6300000000000000044 ),
 .UNSPECIFIED. ) 
 CURVE ( )  GEOMETRIC_REPRESENTATION_ITEM ( )  RATIONAL_B_SPLINE_CURVE ( ( 1.000000000000000000, 0.9238795325112869605, 1.000000000000000000, 0.9238795325112869605, 1.000000000000000000, 0.9238795325112869605, 1.000000000000000000, 0.9238795325112829637, 1.000000000000000000 ) ) 
 REPRESENTATION_ITEM ( '' )  ) ;
#3989=CARTESIAN_POINT ( 'NONE',  ( 0.8759842519685039353, 0.1787899950787401882, 0.8587598424659212970 ) ) ;
#3993=CARTESIAN_POINT ( 'NONE',  ( 0.9873396505805591694, 0.1113553986120547346, 1.077755905511811108 ) ) ;
#3996=CARTESIAN_POINT ( 'NONE',  ( 1.002407869896990045, 0.1264236179284866091, 1.050688976324189117 ) ) ;
#4002=CARTESIAN_POINT ( 'NONE',  ( -0.8759842519685039353, 0.1787899950787401882, 0.2288385826234019815 ) ) ;
#4003=CARTESIAN_POINT ( 'NONE',  ( 0.9873396505805591694, 0.1113553986120547346, 1.747047244094488194 ) ) ;
#4006=CARTESIAN_POINT ( 'NONE',  ( -0.9500414927467378812, 0.1787899950787401604, 1.683070866087970074 ) ) ;
#4007=CARTESIAN_POINT ( 'NONE',  ( -1.002407869896990045, -0.1264236179284866091, 0.8439960629383622681 ) ) ;
#4008=CARTESIAN_POINT ( 'NONE',  ( -0.9500414927467378812, 0.1787899950787401604, 1.053149606245450176 ) ) ;
#4009=( BOUNDED_CURVE ( )  B_SPLINE_CURVE ( 2, ( #28269, #18174, #24662, #10529, #47408, #29255, #25126, #29001, #6668 ),
 .UNSPECIFIED., .F., .T. ) 
 B_SPLINE_CURVE_WITH_KNOTS ( ( 3, 2, 2, 2, 3 ),
 ( 0.8900000000000000133, 0.8924999999999999600, 0.8950000000000000178, 0.8974999999999999645, 0.9000000000000000222 ),
 .UNSPECIFIED. ) 
 CURVE ( )  GEOMETRIC_REPRESENTATION_ITEM ( )  RATIONAL_B_SPLINE_CURVE ( ( 1.000000000000000000, 0.9238795325112899581, 1.000000000000000000, 0.9238795325112869605, 1.000000000000000000, 0.9238795325112869605, 1.000000000000000000, 0.9238795325112869605, 1.000000000000000000 ) ) 
 REPRESENTATION_ITEM ( '' )  ) ;
#4013=CARTESIAN_POINT ( 'NONE',  ( -0.7185039370078739607, 1.928577636452523993E-17, 0.3346456691838114450 ) ) ;
#4014=CARTESIAN_POINT ( 'NONE',  ( 1.002407869896990045, 0.1264236179284866091, 0.02706692908009476414 ) ) ;
#4018=DIRECTION ( 'NONE',  ( 1.000000000000000000, 0.000000000000000000, 0.000000000000000000 ) ) ;
#4020=CARTESIAN_POINT ( 'NONE',  ( -0.8019270111902717657, -0.1787899950787401604, 0.3641732282926931630 ) ) ;
#4022=CARTESIAN_POINT ( 'NONE',  ( 0.7185039370078741827, 0.06523048226347841205, 0.8144685039370075375 ) ) ;
#4023=EDGE_LOOP ( 'NONE', ( #45619, #3829, #31901, #19977 ) ) ;
#4024=CARTESIAN_POINT ( 'NONE',  ( -0.8759842519685039353, 0.1787899950787401882, 1.336122047190330786 ) ) ;
#4029=LINE ( 'NONE', #32833, #13335 ) ;
#4031=CARTESIAN_POINT ( 'NONE',  ( 0.8759842519685039353, 0.1574803149606299191, 0.4133858267716535861 ) ) ;
#4033=FACE_OUTER_BOUND ( 'NONE', #33455, .T. ) ;
#4034=CARTESIAN_POINT ( 'NONE',  ( -1.033464566929133799, 0.000000000000000000, 1.062992125876724314 ) ) ;
#4036=CARTESIAN_POINT ( 'NONE',  ( 1.002407869896990045, -0.1264236179284866091, 0.4158464566391496531 ) ) ;
#4037=CARTESIAN_POINT ( 'NONE',  ( 1.033464566929134687, 0.06523048226347956391, 0.5536417321759372623 ) ) ;
#4039=CARTESIAN_POINT ( 'NONE',  ( 0.9412147342319837628, 0.1574803149606300301, 1.975885826664125711 ) ) ;
#4043=CARTESIAN_POINT ( 'NONE',  ( 0.7185039370078746268, 0.06523048226347956391, 1.011318897637796033 ) ) ;
#4047=CARTESIAN_POINT ( 'NONE',  ( 0.8107537697050254399, -0.1574803149606297803, 0.7455708661417325134 ) ) ;
#4049=EDGE_CURVE ( 'NONE', #20929, #39852, #37902, .T. ) ;
#4051=ORIENTED_EDGE ( 'NONE', *, *, #11781, .F. ) ;
#4052=EDGE_LOOP ( 'NONE', ( #2493, #38155, #12831, #11444 ) ) ;
#4053=CARTESIAN_POINT ( 'NONE',  ( -0.7646288533564489232, -0.1113553986120547346, 0.6151574802074331050 ) ) ;
#4058=CARTESIAN_POINT ( 'NONE',  ( 0.7185039370078746268, 0.06523048226347956391, 1.040846456585385882 ) ) ;
#4059=CARTESIAN_POINT ( 'NONE',  ( 0.7185039370078746268, 0.06523048226347956391, 1.838090551181102317 ) ) ;
#4061=ORIENTED_EDGE ( 'NONE', *, *, #26809, .T. ) ;
#4064=CARTESIAN_POINT ( 'NONE',  ( -0.8759842519685039353, -0.1787899950787401882, 1.592027559001354398 ) ) ;
#4065=CARTESIAN_POINT ( 'NONE',  ( 0.6971942568897637749, 2.189545951927499583E-17, 1.779035433017102319 ) ) ;
#4066=CARTESIAN_POINT ( 'NONE',  ( -1.054774247047244540, 0.07405724077823318263, 0.8169291338045038264 ) ) ;
#4070=CARTESIAN_POINT ( 'NONE',  ( 0.8759842519685039353, 0.1787899950787401882, 0.3124999999462365619 ) ) ;
#4072=CARTESIAN_POINT ( 'NONE',  ( -0.6971942568897637749, 2.189545951927499583E-17, 1.262303149552535420 ) ) ;
#4075=CARTESIAN_POINT ( 'NONE',  ( -0.7495606340400177148, -0.1264236179284866091, 1.547736220418677089 ) ) ;
#4076=CARTESIAN_POINT ( 'NONE',  ( -0.9873396505805591694, 0.1113553986120547346, 1.855314960522393530 ) ) ;
#4079=CARTESIAN_POINT ( 'NONE',  ( 0.8759842519685039353, -0.1787899950787401882, 1.434547244040724534 ) ) ;
#4083=VERTEX_POINT ( 'NONE', #15259 ) ;
#4091=CARTESIAN_POINT ( 'NONE',  ( 1.033464566929133799, 0.000000000000000000, 1.348425196850393748 ) ) ;
#4093=CARTESIAN_POINT ( 'NONE',  ( 0.6971942568897626646, -0.07405724077823297447, 0.7135826771115916234 ) ) ;
#4094=EDGE_CURVE ( 'NONE', #47236, #43450, #29902, .T. ) ;
#4095=CARTESIAN_POINT ( 'NONE',  ( -0.9862283977965377035, 0.1251934987593905646, 0.03937007874015843734 ) ) ;
#4096=CARTESIAN_POINT ( 'NONE',  ( 1.033464566929133799, 0.000000000000000000, 1.771653543199558811 ) ) ;
#4099=FACE_OUTER_BOUND ( 'NONE', #40715, .T. ) ;
#4100=CARTESIAN_POINT ( 'NONE',  ( 0.7495606340400177148, 0.1264236179284866091, 1.852854330654897685 ) ) ;
#4103=ORIENTED_EDGE ( 'NONE', *, *, #34435, .T. ) ;
#4104=EDGE_CURVE ( 'NONE', #17196, #38075, #16827, .T. ) ;
#4105=CARTESIAN_POINT ( 'NONE',  ( 0.7185039370078746268, 0.06523048226347956391, 0.06643700787401589369 ) ) ;
#4109=CARTESIAN_POINT ( 'NONE',  ( 0.8759842519685039353, 0.000000000000000000, 4.498031496062992574 ) ) ;
#4111=CARTESIAN_POINT ( 'NONE',  ( 0.9500414927467378812, 0.1787899950787401604, 0.2312992125446618197 ) ) ;
#4112=CARTESIAN_POINT ( 'NONE',  ( 0.7646288533564489232, 0.1113553986120547346, 1.117125984144440975 ) ) ;
#4113=CARTESIAN_POINT ( 'NONE',  ( -0.9500414927467378812, 0.1787899950787401604, 1.643700787347811998 ) ) ;
#4114=ORIENTED_EDGE ( 'NONE', *, *, #15099, .T. ) ;
#4115=CARTESIAN_POINT ( 'NONE',  ( -0.8759842519685039353, -0.1787899950787401882, 1.158956692859621995 ) ) ;
#4116=CARTESIAN_POINT ( 'NONE',  ( -1.033464566929133799, 0.000000000000000000, 0.3248031496062992463 ) ) ;
#4117=CARTESIAN_POINT ( 'NONE',  ( 1.002407869896990045, -0.1264236179284866091, 0.06151574797773248782 ) ) ;
#4118=CARTESIAN_POINT ( 'NONE',  ( -1.002407869896990045, 0.1264236179284866091, 1.129429133804503937 ) ) ;
#4120=CARTESIAN_POINT ( 'NONE',  ( 0.7495606340400177148, -0.1264236179284866091, 0.4453740156942677664 ) ) ;
#4121=CARTESIAN_POINT ( 'NONE',  ( -0.6971942568897626646, 0.07405724077823318263, 0.2755905511273391006 ) ) ;
#4122=CARTESIAN_POINT ( 'NONE',  ( -1.002407869896990045, -0.1264236179284866091, 0.6865157479777322935 ) ) ;
#4123=CARTESIAN_POINT ( 'NONE',  ( 0.7185039370078739607, 1.928577636452523993E-17, 1.712598425089322918 ) ) ;
#4127=CARTESIAN_POINT ( 'NONE',  ( 0.6971942568897637749, 2.189545951927499583E-17, 0.8735236219934803259 ) ) ;
#4128=CARTESIAN_POINT ( 'NONE',  ( 1.054774247047244540, 0.07405724077823318263, 1.053149606245450176 ) ) ;
#4129=CARTESIAN_POINT ( 'NONE',  ( -0.9500414927467377701, -0.1787899950787401604, 1.904527559001354398 ) ) ;
#4130=ORIENTED_EDGE ( 'NONE', *, *, #20495, .F. ) ;
#4131=EDGE_CURVE ( 'NONE', #38785, #19774, #16494, .T. ) ;
#4132=CARTESIAN_POINT ( 'NONE',  ( 0.8759842519685039353, -0.1787899950787401882, 1.902066929080094448 ) ) ;
#4133=CARTESIAN_POINT ( 'NONE',  ( -0.6971942568897626646, 0.07405724077823318263, 0.8710629920722218200 ) ) ;
#4134=CARTESIAN_POINT ( 'NONE',  ( -0.8759842519685039353, 0.000000000000000000, 0.000000000000000000 ) ) ;
#4141=ORIENTED_EDGE ( 'NONE', *, *, #5419, .F. ) ;
#4142=CARTESIAN_POINT ( 'NONE',  ( 1.054774247047244540, -0.07405724077823318263, 1.122047244040725644 ) ) ;
#4144=ADVANCED_FACE ( 'NONE', ( #23147 ), #37762, .T. ) ;
#4145=CARTESIAN_POINT ( 'NONE',  ( 0.7495606340400177148, 0.1264236179284866091, 0.1943897637257641919 ) ) ;
#4151=CARTESIAN_POINT ( 'NONE',  ( -1.054774247047244540, 0.07405724077823318263, 0.6988188975840318173 ) ) ;
#4155=CARTESIAN_POINT ( 'NONE',  ( 1.054774247047244540, 0.07405724077823318263, 1.368110236166710125 ) ) ;
#4156=CARTESIAN_POINT ( 'NONE',  ( 0.8019270111902716547, -0.1787899950787401604, 1.663385826717890925 ) ) ;
#4159=CARTESIAN_POINT ( 'NONE',  ( -0.8107537697050254399, -0.1574803149606297803, 1.641240157372788389 ) ) ;
#4161=CARTESIAN_POINT ( 'NONE',  ( -0.7185039370078739607, 1.928577636452523993E-17, 1.437007873908220601 ) ) ;
#4162=CARTESIAN_POINT ( 'NONE',  ( -0.8216075239166756861, 0.1504252669448082336, 1.979429770448521531 ) ) ;
#4165=FACE_OUTER_BOUND ( 'NONE', #41792, .T. ) ;
#4166=CARTESIAN_POINT ( 'NONE',  ( -0.9412147342319837628, -0.1574803149606297803, 1.921751968396409493 ) ) ;
#4167=CARTESIAN_POINT ( 'NONE',  ( -0.9873396505805591694, 0.1113553986120547346, 0.9498031494987716483 ) ) ;
#4168=CARTESIAN_POINT ( 'NONE',  ( -0.8759842519685039353, 0.1787899950787401882, 1.173720472387181246 ) ) ;
#4169=CARTESIAN_POINT ( 'NONE',  ( 1.033464566929134687, -0.06523048226347956391, 0.6668307085538908163 ) ) ;
#4172=VERTEX_POINT ( 'NONE', #9654 ) ;
#4174=CARTESIAN_POINT ( 'NONE',  ( -0.7185039370078739607, 1.928577636452523993E-17, 1.604330708661417360 ) ) ;
#4175=CARTESIAN_POINT ( 'NONE',  ( 0.9500414927467378812, -0.1787899950787401604, 1.550196850339937926 ) ) ;
#4176=LINE ( 'NONE', #10695, #1333 ) ;
#4178=CARTESIAN_POINT ( 'NONE',  ( 1.033464566929134687, -0.06523048226347956391, 1.926673228238929170 ) ) ;
#4181=CARTESIAN_POINT ( 'NONE',  ( -0.7185039370078746268, 0.06523048226347956391, 0.3813976377952755237 ) ) ;
#4183=CARTESIAN_POINT ( 'NONE',  ( 0.9500414927467377701, 0.1787899950787401604, 0.8218503936470251681 ) ) ;
#4185=CARTESIAN_POINT ( 'NONE',  ( -0.6971942568897648851, 0.07405724077823318263, 1.343503936954111744 ) ) ;
#4189=CARTESIAN_POINT ( 'NONE',  ( -0.6971942568897637749, 2.189545951927499583E-17, 0.3617125983714334359 ) ) ;
#4191=CARTESIAN_POINT ( 'NONE',  ( 0.7646288533564489232, 0.1113553986120547346, 0.8021653542231811373 ) ) ;
#4202=CARTESIAN_POINT ( 'NONE',  ( -0.8019270111902716547, -0.1787899950787401604, 0.09350393695411057804 ) ) ;
#4203=CARTESIAN_POINT ( 'NONE',  ( -0.8759842519685039353, -0.1574803149606299191, 0.9448818897637796255 ) ) ;
#4206=CARTESIAN_POINT ( 'NONE',  ( -0.9873396505805591694, 0.1113553986120547346, 1.540354330601133803 ) ) ;
#4207=CARTESIAN_POINT ( 'NONE',  ( 0.7495606340400177148, 0.1264236179284866091, 0.9473425196312755814 ) ) ;
#4208=CARTESIAN_POINT ( 'NONE',  ( 1.054774247047244096, 0.000000000000000000, 1.360728346402929168 ) ) ;
#4210=EDGE_CURVE ( 'NONE', #34447, #9079, #42757, .T. ) ;
#4211=CARTESIAN_POINT ( 'NONE',  ( 0.7185039370078746268, -0.06523048226347956391, 1.409940944881891367 ) ) ;
#4212=CARTESIAN_POINT ( 'NONE',  ( 0.7332986977137438966, -0.09085960385660657446, 1.985055299648571969 ) ) ;
#4214=CARTESIAN_POINT ( 'NONE',  ( 0.7185039370078739607, 0.000000000000000000, 4.498031496062992574 ) ) ;
#4215=CARTESIAN_POINT ( 'NONE',  ( 0.6971942568897648851, -0.07405724077823297447, 0.7923228345919055560 ) ) ;
#4220=CARTESIAN_POINT ( 'NONE',  ( 0.7185039370078739607, 1.928577636452523993E-17, 0.9350393700787401619 ) ) ;
#4222=CARTESIAN_POINT ( 'NONE',  ( 0.8759842519685039353, -0.1787899950787401882, 1.193405511757259951 ) ) ;
#4225=CARTESIAN_POINT ( 'NONE',  ( -1.033464566929133799, 0.000000000000000000, 0.5216535433070865757 ) ) ;
#4227=CARTESIAN_POINT ( 'NONE',  ( -0.6971942568897626646, 0.07405724077823318263, 0.1968503936470238913 ) ) ;
#4228=DIRECTION ( 'NONE',  ( 0.000000000000000000, 0.000000000000000000, -1.000000000000000000 ) ) ;
#4230=CARTESIAN_POINT ( 'NONE',  ( -0.8019270111902717657, 0.1787899950787401604, 1.687992125930489307 ) ) ;
#4231=CARTESIAN_POINT ( 'NONE',  ( -0.8759842519685039353, -0.1787899950787401882, 0.8390748030958424808 ) ) ;
#4232=CARTESIAN_POINT ( 'NONE',  ( -0.8019270111902717657, -0.1787899950787401604, 0.5265748030958428139 ) ) ;
#4235=CARTESIAN_POINT ( 'NONE',  ( 1.002407869896990045, -0.1264236179284866091, 0.05659448813521283234 ) ) ;
#4239=VECTOR ( 'NONE', #39476, 39.37007874015748143 ) ;
#4241=CARTESIAN_POINT ( 'NONE',  ( -0.8019270111902717657, 0.1787899950787401604, 0.3887795275052913224 ) ) ;
#4244=CARTESIAN_POINT ( 'NONE',  ( -1.054774247047244540, 0.07405724077823318263, 1.446850393647023836 ) ) ;
#4245=ORIENTED_EDGE ( 'NONE', *, *, #837, .F. ) ;
#4249=( BOUNDED_CURVE ( )  B_SPLINE_CURVE ( 2, ( #20318, #1380, #13157, #8826, #38771, #5932, #16038, #30665, #13380 ),
 .UNSPECIFIED., .F., .T. ) 
 B_SPLINE_CURVE_WITH_KNOTS ( ( 3, 2, 2, 2, 3 ),
 ( 0.2000000000000000111, 0.2025000000000000133, 0.2049999999999999878, 0.2074999999999999900, 0.2099999999999999922 ),
 .UNSPECIFIED. ) 
 CURVE ( )  GEOMETRIC_REPRESENTATION_ITEM ( )  RATIONAL_B_SPLINE_CURVE ( ( 1.000000000000000000, 0.9238795325112869605, 1.000000000000000000, 0.9238795325112869605, 1.000000000000000000, 0.9238795325112869605, 1.000000000000000000, 0.9238795325112869605, 1.000000000000000000 ) ) 
 REPRESENTATION_ITEM ( '' )  ) ;
#4254=CARTESIAN_POINT ( 'NONE',  ( -0.7646288533564489232, 0.1113553986120547346, 1.117125984144440975 ) ) ;
#4255=CARTESIAN_POINT ( 'NONE',  ( 0.8019270111902717657, 0.1787899950787401604, 0.5118110235682844511 ) ) ;
#4256=CARTESIAN_POINT ( 'NONE',  ( -1.033464566929134687, -0.06523048226347956391, 1.493602362097197211 ) ) ;
#4258=EDGE_LOOP ( 'NONE', ( #4245, #23915, #16817, #44504 ) ) ;
#4259=CARTESIAN_POINT ( 'NONE',  ( 0.7185039370078746268, 0.06523048226347956391, 1.946358267609010095 ) ) ;
#4261=CARTESIAN_POINT ( 'NONE',  ( 0.8759842519685039353, -0.1574803149606300579, 0.03937007874015747977 ) ) ;
#4263=CARTESIAN_POINT ( 'NONE',  ( -1.002407869896990045, -0.1264236179284866091, 0.9276574802611967652 ) ) ;
#4264=CARTESIAN_POINT ( 'NONE',  ( 0.7185039370078739607, 1.928577636452523993E-17, 1.013779527559055094 ) ) ;
#4272=CARTESIAN_POINT ( 'NONE',  ( -0.9873396505805591694, 0.1113553986120547346, 1.776574803042078488 ) ) ;
#4276=CARTESIAN_POINT ( 'NONE',  ( 0.7185039370078746268, 0.06523048226347956391, 1.158956692805858113 ) ) ;
#4277=( BOUNDED_CURVE ( )  B_SPLINE_CURVE ( 2, ( #44654, #45381, #33700, #38203, #8490, #26734, #15715, #42003, #15472 ),
 .UNSPECIFIED., .F., .T. ) 
 B_SPLINE_CURVE_WITH_KNOTS ( ( 3, 2, 2, 2, 3 ),
 ( 0.2800000000000000266, 0.2824999999999999734, 0.2849999999999999756, 0.2874999999999999778, 0.2899999999999999800 ),
 .UNSPECIFIED. ) 
 CURVE ( )  GEOMETRIC_REPRESENTATION_ITEM ( )  RATIONAL_B_SPLINE_CURVE ( ( 1.000000000000000000, 0.9238795325112869605, 1.000000000000000000, 0.9238795325112869605, 1.000000000000000000, 0.9238795325112869605, 1.000000000000000000, 0.9238795325112869605, 1.000000000000000000 ) ) 
 REPRESENTATION_ITEM ( '' )  ) ;
#4279=CARTESIAN_POINT ( 'NONE',  ( -0.8019270111902717657, -0.1787899950787401604, 0.4822834645131655606 ) ) ;
#4281=ORIENTED_EDGE ( 'NONE', *, *, #43584, .T. ) ;
#4282=ORIENTED_EDGE ( 'NONE', *, *, #8277, .F. ) ;
#4283=CARTESIAN_POINT ( 'NONE',  ( -0.8019270111902717657, 0.1787899950787401604, 1.771653543253322249 ) ) ;
#4284=CARTESIAN_POINT ( 'NONE',  ( 0.8019270111902717657, -0.1787899950787401604, 1.707677165300566235 ) ) ;
#4285=CARTESIAN_POINT ( 'NONE',  ( -0.6971942568897637749, 2.189545951927499583E-17, 0.7947834645131652831 ) ) ;
#4287=CARTESIAN_POINT ( 'NONE',  ( 1.054774247047244540, 0.07405724077823318263, 0.3444881889226146243 ) ) ;
#4288=CARTESIAN_POINT ( 'NONE',  ( -0.9412147342319837628, 0.1574803149606300301, 1.503444881782235232 ) ) ;
#4289=CARTESIAN_POINT ( 'NONE',  ( -0.8019270111902716547, -0.1787899950787401604, 1.190944881836001112 ) ) ;
#4290=CARTESIAN_POINT ( 'NONE',  ( -0.6971942568897626646, -0.07405724077823297447, 0.9104330708123776761 ) ) ;
#4291=CARTESIAN_POINT ( 'NONE',  ( 0.8107537697050254399, 0.1574803149606300301, 0.9178149605223947516 ) ) ;
#4292=FACE_OUTER_BOUND ( 'NONE', #11893, .T. ) ;
#4293=CARTESIAN_POINT ( 'NONE',  ( -0.6971942568897637749, 2.189545951927499583E-17, 1.660925196796630088 ) ) ;
#4294=CARTESIAN_POINT ( 'NONE',  ( -0.8759842519685039353, 0.1574803149606299191, 1.820866141624755796 ) ) ;
#4295=ORIENTED_EDGE ( 'NONE', *, *, #5961, .T. ) ;
#4296=CARTESIAN_POINT ( 'NONE',  ( -0.9412147342319837628, 0.1574803149606300301, 1.631397637795275468 ) ) ;
#4297=CARTESIAN_POINT ( 'NONE',  ( -0.7185039370078739607, 1.928577636452523993E-17, 0.2263779527559055260 ) ) ;
#4298=CARTESIAN_POINT ( 'NONE',  ( 0.8019270111902716547, -0.1787899950787401604, 1.589566929080094226 ) ) ;
#4310=CARTESIAN_POINT ( 'NONE',  ( 0.9500414927467378812, 0.1787899950787401604, 1.801181102308441861 ) ) ;
#4313=CARTESIAN_POINT ( 'NONE',  ( -0.9412147342319837628, -0.1574803149606297803, 0.8981299211523156023 ) ) ;
#4314=CARTESIAN_POINT ( 'NONE',  ( 0.6971942568897626646, -0.07405724077823297447, 0.8316929133320636325 ) ) ;
#4315=CARTESIAN_POINT ( 'NONE',  ( -0.7185039370078739607, 1.928577636452523993E-17, 1.082677165246803241 ) ) ;
#4320=CARTESIAN_POINT ( 'NONE',  ( 0.9500414927467378812, -0.1787899950787401604, 1.751968503883245765 ) ) ;
#4323=CARTESIAN_POINT ( 'NONE',  ( 1.033464566929134687, -0.06523048226347956391, 0.04675196850393704279 ) ) ;
#4328=CARTESIAN_POINT ( 'NONE',  ( 0.8759842519685039353, -0.1787899950787401882, 0.1747047243556852092 ) ) ;
#4329=CARTESIAN_POINT ( 'NONE',  ( 0.8759842519685039353, 0.1574803149606299191, 1.112204724301921299 ) ) ;
#4330=CARTESIAN_POINT ( 'NONE',  ( -0.6971942568897648851, -0.07405724077823297447, 1.815944881835999558 ) ) ;
#4331=EDGE_LOOP ( 'NONE', ( #6224, #7246, #9355, #26838 ) ) ;
#4332=CARTESIAN_POINT ( 'NONE',  ( -1.054774247047244540, 0.07405724077823318263, 1.249999999946235896 ) ) ;
#4333=DIRECTION ( 'NONE',  ( 0.000000000000000000, 0.000000000000000000, -1.000000000000000000 ) ) ;
#4334=CARTESIAN_POINT ( 'NONE',  ( 1.054774247047244096, 0.000000000000000000, 1.326279527505291433 ) ) ;
#4335=CARTESIAN_POINT ( 'NONE',  ( 0.8759842519685039353, -0.1787899950787401882, 1.902066929080094448 ) ) ;
#4336=CARTESIAN_POINT ( 'NONE',  ( -0.9500414927467378812, -0.1787899950787401604, 1.038385826717890259 ) ) ;
#4338=CARTESIAN_POINT ( 'NONE',  ( 0.9873396505805591694, 0.1113553986120547346, 0.04429133847515007855 ) ) ;
#4339=CARTESIAN_POINT ( 'NONE',  ( 1.054774247047244096, 0.000000000000000000, 0.4601377952218267953 ) ) ;
#4340=CARTESIAN_POINT ( 'NONE',  ( -1.054774247047244096, 0.000000000000000000, 0.4158464566391496531 ) ) ;
#4341=CARTESIAN_POINT ( 'NONE',  ( 0.8759842519685039353, -0.1574803149606299191, 1.683070866034204638 ) ) ;
#4342=ORIENTED_EDGE ( 'NONE', *, *, #33149, .T. ) ;
#4343=ORIENTED_EDGE ( 'NONE', *, *, #45808, .T. ) ;
#4345=CARTESIAN_POINT ( 'NONE',  ( -0.7185039370078739607, 1.928577636452523993E-17, 0.06889763779527559306 ) ) ;
#4346=CARTESIAN_POINT ( 'NONE',  ( 0.6971942568897648851, -0.07405724077823297447, 1.033464566875371027 ) ) ;
#4347=CARTESIAN_POINT ( 'NONE',  ( -1.054774247047244540, -0.07405724077823318263, 1.948818897584033705 ) ) ;
#4351=ADVANCED_FACE ( 'NONE', ( #8 ), #36296, .T. ) ;
#4353=CARTESIAN_POINT ( 'NONE',  ( -0.7185039370078739607, 1.928577636452523993E-17, 1.870078740049952559 ) ) ;
#4355=ORIENTED_EDGE ( 'NONE', *, *, #17582, .F. ) ;
#4361=CARTESIAN_POINT ( 'NONE',  ( 0.8759842519685039353, -0.1787899950787401882, 1.193405511757259951 ) ) ;
#4362=EDGE_CURVE ( 'NONE', #19564, #25854, #22784, .T. ) ;
#4363=CARTESIAN_POINT ( 'NONE',  ( -0.7646288533564489232, 0.1113553986120547346, 0.8415354329633386588 ) ) ;
#4364=DIRECTION ( 'NONE',  ( 1.000000000000000000, 0.000000000000000000, -1.822029033848725275E-16 ) ) ;
#4367=CARTESIAN_POINT ( 'NONE',  ( 0.6971942568897637749, 2.189545951927499583E-17, 0.1205708660879689087 ) ) ;
#4371=CARTESIAN_POINT ( 'NONE',  ( 0.9412147342319837628, -0.1574803149606297803, 1.341043307086613456 ) ) ;
#4372=CARTESIAN_POINT ( 'NONE',  ( -0.8759842519685039353, 0.1787899950787401882, 0.6668307086076534773 ) ) ;
#4378=CARTESIAN_POINT ( 'NONE',  ( 0.7495606340400177148, 0.1264236179284866091, 1.380413385773007873 ) ) ;
#4379=CARTESIAN_POINT ( 'NONE',  ( 0.6971942568897648851, 0.07405724077823318263, 1.653543307032850462 ) ) ;
#4380=CYLINDRICAL_SURFACE ( 'NONE', #7763, 0.1574803149606299191 ) ;
#4381=DIRECTION ( 'NONE',  ( 0.000000000000000000, 0.000000000000000000, -1.000000000000000000 ) ) ;
#4386=CARTESIAN_POINT ( 'NONE',  ( 0.8759842519685039353, 0.1787899950787401882, 0.2682086613635594752 ) ) ;
#4387=( BOUNDED_CURVE ( )  B_SPLINE_CURVE ( 2, ( #45691, #15800, #30658, #45218, #30427, #27062, #23212, #8814, #38288 ),
 .UNSPECIFIED., .F., .T. ) 
 B_SPLINE_CURVE_WITH_KNOTS ( ( 3, 2, 2, 2, 3 ),
 ( 0.4799999999999999822, 0.4824999999999999845, 0.4849999999999999867, 0.4874999999999999889, 0.4899999999999999911 ),
 .UNSPECIFIED. ) 
 CURVE ( )  GEOMETRIC_REPRESENTATION_ITEM ( )  RATIONAL_B_SPLINE_CURVE ( ( 1.000000000000000000, 0.9238795325112869605, 1.000000000000000000, 0.9238795325112869605, 1.000000000000000000, 0.9238795325112869605, 1.000000000000000000, 0.9238795325112869605, 1.000000000000000000 ) ) 
 REPRESENTATION_ITEM ( '' )  ) ;
#4388=CARTESIAN_POINT ( 'NONE',  ( 0.7331294905545601148, -0.08922581545105803813, 0.03937007875388988387 ) ) ;
#4391=CARTESIAN_POINT ( 'NONE',  ( -0.8759842519685039353, 0.1574803149606299191, 0.9547244093412913246 ) ) ;
#4392=CARTESIAN_POINT ( 'NONE',  ( -1.002407869896990045, 0.1264236179284866091, 1.286909448765133801 ) ) ;
#4393=CARTESIAN_POINT ( 'NONE',  ( 1.033464566929133799, 0.000000000000000000, 0.5905511809948347235 ) ) ;
#4395=CARTESIAN_POINT ( 'NONE',  ( 0.8759842519685039353, 0.1574803149606299191, 1.397637795275590511 ) ) ;
#4397=EDGE_LOOP ( 'NONE', ( #42354, #25632, #16710, #37834 ) ) ;
#4400=EDGE_CURVE ( 'NONE', #26106, #15853, #7688, .T. ) ;
#4402=CARTESIAN_POINT ( 'NONE',  ( -0.8107537697050254399, 0.1574803149606300301, 1.114665354223180804 ) ) ;
#4403=CARTESIAN_POINT ( 'NONE',  ( -0.7646288533564489232, -0.1113553986120547346, 1.254921259842519676 ) ) ;
#4404=CARTESIAN_POINT ( 'NONE',  ( 0.8759842519685039353, 0.1574803149606299191, 0.2460629920184571051 ) ) ;
#4407=CARTESIAN_POINT ( 'NONE',  ( 0.9500414927467377701, -0.1787899950787401604, 0.05905511805647267048 ) ) ;
#4410=AXIS2_PLACEMENT_3D ( 'NONE', #21098, #12991, #35031 ) ;
#4411=CARTESIAN_POINT ( 'NONE',  ( -0.9412147342319837628, 0.1574803149606300301, 0.3715551181102362266 ) ) ;
#4412=CARTESIAN_POINT ( 'NONE',  ( 0.7495606340400177148, -0.1264236179284866091, 0.9178149605761574126 ) ) ;
#4413=CARTESIAN_POINT ( 'NONE',  ( -1.054774247047244096, 0.000000000000000000, 1.518208661363559031 ) ) ;
#4415=CARTESIAN_POINT ( 'NONE',  ( -0.8019270111902717657, -0.1787899950787401604, 1.235236220418678199 ) ) ;
#4419=CARTESIAN_POINT ( 'NONE',  ( 1.033464566929133799, 0.000000000000000000, 0.8661417321759370402 ) ) ;
#4424=VERTEX_POINT ( 'NONE', #26405 ) ;
#4426=CYLINDRICAL_SURFACE ( 'NONE', #28701, 0.1574803149606299191 ) ;
#4427=CARTESIAN_POINT ( 'NONE',  ( 0.9873396505805591694, -0.1113553986120547346, 0.1131889762704257896 ) ) ;
#4429=CARTESIAN_POINT ( 'NONE',  ( -1.002407869896990045, -0.1264236179284866091, 0.1796259841982051075 ) ) ;
#4430=CARTESIAN_POINT ( 'NONE',  ( -0.7646288533564489232, -0.1113553986120547346, 0.9399606299212598381 ) ) ;
#4431=DIRECTION ( 'NONE',  ( 1.000000000000000000, 0.000000000000000000, -1.822029033848725275E-16 ) ) ;
#4434=CARTESIAN_POINT ( 'NONE',  ( -0.7185039370078746268, -0.06523048226347956391, 1.557578740049953225 ) ) ;
#4435=CARTESIAN_POINT ( 'NONE',  ( 0.6971942568897626646, 0.07405724077823318263, 0.9104330708123776761 ) ) ;
#4436=CARTESIAN_POINT ( 'NONE',  ( 1.033464566929133799, 0.000000000000000000, 0.5118110235145204578 ) ) ;
#4437=CARTESIAN_POINT ( 'NONE',  ( 1.033464566929134687, -0.06523048226347956391, 1.345964566929133133 ) ) ;
#4438=CARTESIAN_POINT ( 'NONE',  ( 0.7275679244916588573, 0.06900988131655333424, 1.981898831895456681 ) ) ;
#4440=DIRECTION ( 'NONE',  ( 0.000000000000000000, 0.000000000000000000, -1.000000000000000000 ) ) ;
#4441=CARTESIAN_POINT ( 'NONE',  ( 0.9500414927467377701, 0.1787899950787401604, 0.8562992125446617919 ) ) ;
#4442=CARTESIAN_POINT ( 'NONE',  ( 0.8019270111902716547, -0.1787899950787401604, 1.786417322780882388 ) ) ;
#4446=CARTESIAN_POINT ( 'NONE',  ( -0.7185039370078739607, 1.928577636452523993E-17, 0.9744094488188976833 ) ) ;
#4447=CARTESIAN_POINT ( 'NONE',  ( 0.6971942568897637749, 2.189545951927499583E-17, 1.183562992072220599 ) ) ;
#4451=AXIS2_PLACEMENT_3D ( 'NONE', #29922, #3987, #36380 ) ;
#4452=ORIENTED_EDGE ( 'NONE', *, *, #12571, .F. ) ;
#4453=CARTESIAN_POINT ( 'NONE',  ( -1.054774247047244540, 0.07405724077823318263, 0.2608267715997796832 ) ) ;
#4457=CARTESIAN_POINT ( 'NONE',  ( -0.6971942568897637749, 2.189545951927499583E-17, 1.892224409395055096 ) ) ;
#4458=CARTESIAN_POINT ( 'NONE',  ( -0.6971942568897648851, 0.07405724077823318263, 0.9448818897100165204 ) ) ;
#4459=CARTESIAN_POINT ( 'NONE',  ( -1.054774247047244540, 0.07405724077823318263, 0.5019685038832442103 ) ) ;
#4461=CARTESIAN_POINT ( 'NONE',  ( -0.8107537697050234415, -0.1574803149606297803, 0.1550196850393702197 ) ) ;
#4468=CARTESIAN_POINT ( 'NONE',  ( -0.9412147342319837628, 0.1574803149606300301, 1.897145669183811778 ) ) ;
#4471=CARTESIAN_POINT ( 'NONE',  ( -1.033464566929134687, 0.06523048226347956391, 1.970964566821606034 ) ) ;
#4472=CARTESIAN_POINT ( 'NONE',  ( -1.054774247047244096, 0.000000000000000000, 0.2583661416785200671 ) ) ;
#4474=ORIENTED_EDGE ( 'NONE', *, *, #40182, .T. ) ;
#4476=EDGE_LOOP ( 'NONE', ( #32160, #30356, #15719, #2883 ) ) ;
#4477=CARTESIAN_POINT ( 'NONE',  ( -0.9500414927467377701, 0.1787899950787401604, 1.569881889710015299 ) ) ;
#4482=DIRECTION ( 'NONE',  ( 1.822029033848725028E-16, 0.000000000000000000, 1.000000000000000000 ) ) ;
#4483=CARTESIAN_POINT ( 'NONE',  ( 0.7646288533564489232, -0.1113553986120547346, 0.5068897637795275468 ) ) ;
#4485=CARTESIAN_POINT ( 'NONE',  ( -1.033464566929134687, -0.06523048226347956391, 1.060531495955465031 ) ) ;
#4487=CARTESIAN_POINT ( 'NONE',  ( 1.054774247047244096, 0.000000000000000000, 0.5782480314422993040 ) ) ;
#4489=CARTESIAN_POINT ( 'NONE',  ( -0.8759842519685039353, 0.000000000000000000, 0.000000000000000000 ) ) ;
#4490=CARTESIAN_POINT ( 'NONE',  ( -0.7185039370078739607, 1.928577636452523993E-17, 1.879921259842519676 ) ) ;
#4493=CARTESIAN_POINT ( 'NONE',  ( -1.054774247047244096, 0.000000000000000000, 0.9719488188438739629 ) ) ;
#4494=CARTESIAN_POINT ( 'NONE',  ( 1.033464566929133799, 0.000000000000000000, 0.9940944881889764995 ) ) ;
#4498=CARTESIAN_POINT ( 'NONE',  ( -1.033464566929133799, 1.928577636452524610E-17, 2.869337061179095023E-17 ) ) ;
#4501=EDGE_LOOP ( 'NONE', ( #6202, #25796, #24719, #33065 ) ) ;
#4503=CARTESIAN_POINT ( 'NONE',  ( 1.054774247047244096, 0.000000000000000000, 0.6914370078202519698 ) ) ;
#4504=EDGE_LOOP ( 'NONE', ( #35377, #46108, #45244, #25612 ) ) ;
#4506=CARTESIAN_POINT ( 'NONE',  ( -0.7185039370078739607, 0.000000000000000000, -2.869337061179095023E-17 ) ) ;
#4510=CARTESIAN_POINT ( 'NONE',  ( 0.9412147342319837628, -0.1574803149606297803, 1.094980314853103653 ) ) ;
#4511=CARTESIAN_POINT ( 'NONE',  ( 0.8759842519685039353, 0.1574803149606299191, 1.830708661417322913 ) ) ;
#4512=CARTESIAN_POINT ( 'NONE',  ( -1.054774247047244096, 0.000000000000000000, 0.4945866141194645849 ) ) ;
#4513=ORIENTED_EDGE ( 'NONE', *, *, #9113, .T. ) ;
#4514=CARTESIAN_POINT ( 'NONE',  ( -0.8759842519685039353, -0.1787899950787401882, 1.788877952702141672 ) ) ;
#4515=ORIENTED_EDGE ( 'NONE', *, *, #37372, .F. ) ;
#4516=EDGE_CURVE ( 'NONE', #39441, #47216, #7454, .T. ) ;
#4517=CARTESIAN_POINT ( 'NONE',  ( 0.9500414927467378812, 0.1787899950787401604, 1.687992125930489307 ) ) ;
#4519=CARTESIAN_POINT ( 'NONE',  ( -1.054774247047244096, 0.000000000000000000, 0.8932086613635591421 ) ) ;
#4521=CARTESIAN_POINT ( 'NONE',  ( -0.6971942568897637749, 2.189545951927499583E-17, 1.419783464513165505 ) ) ;
#4523=CARTESIAN_POINT ( 'NONE',  ( -0.8759842519685039353, -0.1787899950787401882, 1.193405511757259951 ) ) ;
#4525=CARTESIAN_POINT ( 'NONE',  ( -1.002407869896990045, -0.1264236179284866091, 0.06151574797773248782 ) ) ;
#4528=CARTESIAN_POINT ( 'NONE',  ( -0.9873396505805591694, 0.1113553986120547346, 1.658464566821606256 ) ) ;
#4529=CARTESIAN_POINT ( 'NONE',  ( -0.9500414927467378812, -0.1787899950787401604, 1.555118110182455382 ) ) ;
#4530=CARTESIAN_POINT ( 'NONE',  ( -0.9500414927467378812, 0.1787899950787401604, 0.07381889758403178958 ) ) ;
#4532=CARTESIAN_POINT ( 'NONE',  ( -0.7185039370078746268, -0.06523048226347956391, 1.567421259842519676 ) ) ;
#4533=CARTESIAN_POINT ( 'NONE',  ( 0.9412147342319837628, -0.1574803149606297803, 0.9768700786326298680 ) ) ;
#4534=CARTESIAN_POINT ( 'NONE',  ( 1.054774247047244540, -0.07405724077823318263, 1.599409448765134911 ) ) ;
#4536=CARTESIAN_POINT ( 'NONE',  ( 1.033464566929133799, 0.000000000000000000, 0.1968503935932602311 ) ) ;
#4538=CARTESIAN_POINT ( 'NONE',  ( 1.033464566929133799, 0.000000000000000000, 0.2755905510735752184 ) ) ;
#4542=( BOUNDED_CURVE ( )  B_SPLINE_CURVE ( 2, ( #40469, #22269, #26375, #8129, #4511, #36906, #45010, #4059, #12222 ),
 .UNSPECIFIED., .F., .F. ) 
 B_SPLINE_CURVE_WITH_KNOTS ( ( 3, 2, 2, 2, 3 ),
 ( 0.9200000000000000400, 0.9224999999999999867, 0.9250000000000000444, 0.9274999999999999911, 0.9300000000000000488 ),
 .UNSPECIFIED. ) 
 CURVE ( )  GEOMETRIC_REPRESENTATION_ITEM ( )  RATIONAL_B_SPLINE_CURVE ( ( 1.000000000000000000, 0.9238795325112869605, 1.000000000000000000, 0.9238795325112869605, 1.000000000000000000, 0.9238795325112869605, 1.000000000000000000, 0.9238795325112869605, 1.000000000000000000 ) ) 
 REPRESENTATION_ITEM ( '' )  ) ;
#4544=ORIENTED_EDGE ( 'NONE', *, *, #35034, .F. ) ;
#4549=CARTESIAN_POINT ( 'NONE',  ( 0.8019270111902717657, -0.1787899950787401604, 1.820866141678520789 ) ) ;
#4552=CARTESIAN_POINT ( 'NONE',  ( 1.033464566929133799, 1.928577636452524610E-17, 4.498031496062992574 ) ) ;
#4553=CARTESIAN_POINT ( 'NONE',  ( 0.8759842519685039353, 0.1787899950787401882, 0.7800196849856062542 ) ) ;
#4554=( BOUNDED_CURVE ( )  B_SPLINE_CURVE ( 2, ( #20692, #42259, #28633, #43190, #13742, #9691, #21158, #10159, #9458 ),
 .UNSPECIFIED., .F., .T. ) 
 B_SPLINE_CURVE_WITH_KNOTS ( ( 3, 2, 2, 2, 3 ),
 ( 0.2399999999999999911, 0.2424999999999999933, 0.2449999999999999956, 0.2474999999999999978, 0.2500000000000000000 ),
 .UNSPECIFIED. ) 
 CURVE ( )  GEOMETRIC_REPRESENTATION_ITEM ( )  RATIONAL_B_SPLINE_CURVE ( ( 1.000000000000000000, 0.9238795325112869605, 1.000000000000000000, 0.9238795325112869605, 1.000000000000000000, 0.9238795325112869605, 1.000000000000000000, 0.9238795325112869605, 1.000000000000000000 ) ) 
 REPRESENTATION_ITEM ( '' )  ) ;
#4558=DIRECTION ( 'NONE',  ( 0.000000000000000000, 0.000000000000000000, -1.000000000000000000 ) ) ;
#4559=CARTESIAN_POINT ( 'NONE',  ( -1.033464566929133799, 0.000000000000000000, 0.07874015737278799998 ) ) ;
#4560=CARTESIAN_POINT ( 'NONE',  ( 1.002407869896990045, 0.1264236179284866091, 1.764271653489543290 ) ) ;
#4562=CARTESIAN_POINT ( 'NONE',  ( 0.7185039370078746268, 0.06523048226347956391, 0.1451771653543309226 ) ) ;
#4563=CARTESIAN_POINT ( 'NONE',  ( -0.8759842519685039353, 0.000000000000000000, 0.000000000000000000 ) ) ;
#4568=CARTESIAN_POINT ( 'NONE',  ( 1.002407869896990045, -0.1264236179284866091, 0.2977362204186775885 ) ) ;
#4569=CARTESIAN_POINT ( 'NONE',  ( 0.8759842519685039353, 0.1574803149606299191, 0.05905511811023622659 ) ) ;
#4570=ADVANCED_FACE ( 'NONE', ( #16553 ), #16092, .T. ) ;
#4571=CARTESIAN_POINT ( 'NONE',  ( -0.9500414927467378812, -0.1787899950787401604, 1.825787401521040243 ) ) ;
#4572=ORIENTED_EDGE ( 'NONE', *, *, #20233, .T. ) ;
#4573=CARTESIAN_POINT ( 'NONE',  ( -0.8759842519685039353, -0.1787899950787401882, 1.277066929080094448 ) ) ;
#4575=CARTESIAN_POINT ( 'NONE',  ( 0.9500414927467378812, -0.1787899950787401604, 1.240157480261197431 ) ) ;
#4576=CARTESIAN_POINT ( 'NONE',  ( 0.8759842519685039353, 0.1787899950787401882, 1.921751968450173376 ) ) ;
#4577=CARTESIAN_POINT ( 'NONE',  ( -1.002407869896990045, -0.1264236179284866091, 1.080216535379306952 ) ) ;
#4578=FACE_OUTER_BOUND ( 'NONE', #46724, .T. ) ;
#4581=CARTESIAN_POINT ( 'NONE',  ( 1.002407869896990045, -0.1264236179284866091, 0.4158464566391496531 ) ) ;
#4582=CARTESIAN_POINT ( 'NONE',  ( -0.9500414927467377701, -0.1787899950787401604, 0.4084645668753704162 ) ) ;
#4583=CARTESIAN_POINT ( 'NONE',  ( 0.8759842519685039353, 0.1574803149606299191, 1.663385826664125933 ) ) ;
#4587=CARTESIAN_POINT ( 'NONE',  ( -0.8759842519685039353, -0.1574803149606299191, 0.07874015748031495954 ) ) ;
#4588=CARTESIAN_POINT ( 'NONE',  ( 0.7495606340400177148, -0.1264236179284866091, 1.154035433017102319 ) ) ;
#4590=VERTEX_POINT ( 'NONE', #8400 ) ;
#4591=CARTESIAN_POINT ( 'NONE',  ( 1.002407869896990045, -0.1264236179284866091, 1.985728346402929168 ) ) ;
#4592=CARTESIAN_POINT ( 'NONE',  ( -1.002407869896990045, 0.1264236179284866091, 0.8981299212060788184 ) ) ;
#4596=CARTESIAN_POINT ( 'NONE',  ( -1.002407869896990045, 0.1264236179284866091, 0.02706692908009476414 ) ) ;
#4602=CARTESIAN_POINT ( 'NONE',  ( 0.9500414927467378812, 0.1787899950787401604, 1.368110236166710125 ) ) ;
#4603=AXIS2_PLACEMENT_3D ( 'NONE', #24873, #32797, #3768 ) ;
#4605=CARTESIAN_POINT ( 'NONE',  ( 0.7185039370078760701, -0.06523048226348075740, 0.7308070865066462751 ) ) ;
#4607=CARTESIAN_POINT ( 'NONE',  ( 0.7495606340400177148, -0.1264236179284866091, 1.542814960576157413 ) ) ;
#4608=CARTESIAN_POINT ( 'NONE',  ( 0.9500414927467378812, -0.1787899950787401604, 0.1722440944344254266 ) ) ;
#4613=CARTESIAN_POINT ( 'NONE',  ( -0.7495606340400177148, -0.1264236179284866091, 0.6028543306548976854 ) ) ;
#4617=DIRECTION ( 'NONE',  ( 0.000000000000000000, 0.000000000000000000, -1.000000000000000000 ) ) ;
#4619=CARTESIAN_POINT ( 'NONE',  ( 0.8759842519685039353, 0.1787899950787401882, 1.414862204670645829 ) ) ;
#4620=CARTESIAN_POINT ( 'NONE',  ( 1.002407869896990045, -0.1264236179284866091, 1.828248031442299082 ) ) ;
#4621=CARTESIAN_POINT ( 'NONE',  ( 0.7495606340400177148, 0.1264236179284866091, 0.2731299212060791515 ) ) ;
#4623=EDGE_CURVE ( 'NONE', #18116, #2953, #18310, .T. ) ;
#4627=CARTESIAN_POINT ( 'NONE',  ( -0.8107537697050254399, -0.1574803149606297803, 1.926673228346456490 ) ) ;
#4628=CARTESIAN_POINT ( 'NONE',  ( -0.9873396505805591694, 0.1113553986120547346, 1.225393700679874076 ) ) ;
#4630=CARTESIAN_POINT ( 'NONE',  ( 0.7505145642813948470, -0.1098182161263852180, 0.03937465431229628110 ) ) ;
#4631=CARTESIAN_POINT ( 'NONE',  ( 0.8019270111902716547, 0.1787899950787401604, 1.254921259788757348 ) ) ;
#4635=CARTESIAN_POINT ( 'NONE',  ( -0.9873396505805591694, 0.1113553986120547346, 0.7627952755905511584 ) ) ;
#4636=CARTESIAN_POINT ( 'NONE',  ( -0.9500414927467378812, 0.1787899950787401604, 1.289370078686393750 ) ) ;
#4637=CARTESIAN_POINT ( 'NONE',  ( 0.8759842519685039353, 0.1574803149606299191, 0.6397637794200314865 ) ) ;
#4639=CARTESIAN_POINT ( 'NONE',  ( -0.7185039370078746268, 0.06523048226347956391, 1.759350393700788162 ) ) ;
#4640=EDGE_CURVE ( 'NONE', #11651, #16491, #15246, .T. ) ;
#4641=CARTESIAN_POINT ( 'NONE',  ( 0.8759842519685039353, 0.1574803149606299191, 0.6889763779527560139 ) ) ;
#4648=CARTESIAN_POINT ( 'NONE',  ( -1.033464566929134687, -0.06523048226347956391, 0.04675196850393695952 ) ) ;
#4649=CARTESIAN_POINT ( 'NONE',  ( 0.7495606340400177148, -0.1264236179284866091, 1.582185039316315045 ) ) ;
#4650=CARTESIAN_POINT ( 'NONE',  ( -0.9873396505805591694, 0.1113553986120547346, 1.235236220472440971 ) ) ;
#4653=CARTESIAN_POINT ( 'NONE',  ( -1.033464566929134687, 0.06523048226347956391, 1.823326771653542178 ) ) ;
#4654=LINE ( 'NONE', #33703, #22763 ) ;
#4658=ORIENTED_EDGE ( 'NONE', *, *, #12078, .F. ) ;
#4660=CARTESIAN_POINT ( 'NONE',  ( -0.9500414927467377701, 0.1787899950787401604, 1.525590551127339989 ) ) ;
#4662=CARTESIAN_POINT ( 'NONE',  ( -1.054774247047244096, 0.000000000000000000, 1.208169291284818980 ) ) ;
#4664=CARTESIAN_POINT ( 'NONE',  ( -0.7495606340400177148, -0.1264236179284866091, 0.3666338582139531677 ) ) ;
#4678=CARTESIAN_POINT ( 'NONE',  ( -1.002407869896990045, -0.1264236179284866091, 0.1402559054580474474 ) ) ;
#4679=CARTESIAN_POINT ( 'NONE',  ( -0.7185039370078746268, 0.06523048226347956391, 0.8144685039370082036 ) ) ;
#4681=CARTESIAN_POINT ( 'NONE',  ( 0.9873396505805591694, 0.1113553986120547346, 0.4084645669291339098 ) ) ;
#4682=CARTESIAN_POINT ( 'NONE',  ( -0.7646288533564489232, -0.1113553986120547346, 1.560039369971212508 ) ) ;
#4683=CARTESIAN_POINT ( 'NONE',  ( 0.8759842519685039353, 0.1787899950787401882, 0.9817913385289134265 ) ) ;
#4684=CARTESIAN_POINT ( 'NONE',  ( 0.8759842519685039353, 0.1787899950787401882, 1.409940944828126153 ) ) ;
#4685=CARTESIAN_POINT ( 'NONE',  ( 1.002407869896990045, 0.1264236179284866091, 0.1058070865604098382 ) ) ;
#4686=FACE_OUTER_BOUND ( 'NONE', #11455, .T. ) ;
#4687=CARTESIAN_POINT ( 'NONE',  ( 0.8759842519685039353, -0.1574803149606299191, 1.377952755905512028 ) ) ;
#4688=CARTESIAN_POINT ( 'NONE',  ( 0.7434085338012068611, 0.09442915021634661066, 1.981317316331754563 ) ) ;
#4689=LINE ( 'NONE', #16220, #17803 ) ;
#4690=DIRECTION ( 'NONE',  ( 0.000000000000000000, 0.000000000000000000, -1.000000000000000000 ) ) ;
#4693=CARTESIAN_POINT ( 'NONE',  ( 1.054774247047244096, 0.000000000000000000, 0.8882874015210394658 ) ) ;
#4694=CARTESIAN_POINT ( 'NONE',  ( 0.8759842519685039353, -0.1787899950787401882, 1.749507873961984483 ) ) ;
#4697=CARTESIAN_POINT ( 'NONE',  ( 0.8759842519685039353, 0.1574803149606299191, 0.9251968503937008093 ) ) ;
#4698=EDGE_CURVE ( 'NONE', #39085, #20854, #31420, .T. ) ;
#4700=CARTESIAN_POINT ( 'NONE',  ( -0.9412147342319837628, 0.1574803149606300301, 0.04675196839640998608 ) ) ;
#4701=CARTESIAN_POINT ( 'NONE',  ( 0.8759842519685039353, 0.1787899950787401882, 1.094980314906866203 ) ) ;
#4703=CARTESIAN_POINT ( 'NONE',  ( 0.7185039370078739607, 1.928577636452523993E-17, 1.486220472440944906 ) ) ;
#4706=VECTOR ( 'NONE', #35203, 39.37007874015748143 ) ;
#4708=CARTESIAN_POINT ( 'NONE',  ( -0.7495606340400177148, 0.1264236179284866091, 0.1943897637257641919 ) ) ;
#4710=VERTEX_POINT ( 'NONE', #13206 ) ;
#4715=CARTESIAN_POINT ( 'NONE',  ( -1.002407869896990045, 0.1264236179284866091, 1.838090551127338657 ) ) ;
#4716=CARTESIAN_POINT ( 'NONE',  ( -0.8759842519685039353, 0.1787899950787401882, 0.9374999999462362288 ) ) ;
#4717=CARTESIAN_POINT ( 'NONE',  ( -0.8759842519685039353, -0.1787899950787401882, 0.5684055117572598403 ) ) ;
#4720=DIRECTION ( 'NONE',  ( 0.000000000000000000, 0.000000000000000000, -1.000000000000000000 ) ) ;
#4727=CARTESIAN_POINT ( 'NONE',  ( -1.054774247047244096, 0.000000000000000000, 0.4158464566391496531 ) ) ;
#4728=ORIENTED_EDGE ( 'NONE', *, *, #31626, .T. ) ;
#4730=CARTESIAN_POINT ( 'NONE',  ( -0.6971942568897648851, -0.07405724077823297447, 1.545275590497419138 ) ) ;
#4736=CARTESIAN_POINT ( 'NONE',  ( 1.033464566929134687, -0.06523048226347956391, 0.4798228346456688831 ) ) ;
#4738=CARTESIAN_POINT ( 'NONE',  ( -0.7185039370078746268, -0.06523048226347956391, 1.124507873908221489 ) ) ;
#4739=CARTESIAN_POINT ( 'NONE',  ( 0.9500414927467378812, 0.1787899950787401604, 0.5462598424659214080 ) ) ;
#4743=AXIS2_PLACEMENT_3D ( 'NONE', #16569, #12981, #27621 ) ;
#4744=CARTESIAN_POINT ( 'NONE',  ( 1.033464566929134687, -0.06523048226347956391, 1.966043306979087246 ) ) ;
#4745=ORIENTED_EDGE ( 'NONE', *, *, #22232, .F. ) ;
#4746=CARTESIAN_POINT ( 'NONE',  ( -1.033464566929133799, 0.000000000000000000, 1.269685039370078705 ) ) ;
#4747=CARTESIAN_POINT ( 'NONE',  ( -1.002407869896990045, -0.1264236179284866091, 1.085137795221826629 ) ) ;
#4748=CARTESIAN_POINT ( 'NONE',  ( 0.7185039370078746268, -0.06523048226347956391, 0.8981299212598431447 ) ) ;
#4749=CARTESIAN_POINT ( 'NONE',  ( 0.9873396505805591694, 0.1113553986120547346, 1.353346456692913424 ) ) ;
#4751=DIRECTION ( 'NONE',  ( 0.000000000000000000, 0.000000000000000000, -1.000000000000000000 ) ) ;
#4752=CARTESIAN_POINT ( 'NONE',  ( -0.8759842519685039353, -0.1574803149606299191, 1.259842519685039353 ) ) ;
#4754=ORIENTED_EDGE ( 'NONE', *, *, #23441, .T. ) ;
#4757=CARTESIAN_POINT ( 'NONE',  ( 1.054774247047244540, 0.07405724077823318263, 0.7332677164816707727 ) ) ;
#4759=ORIENTED_EDGE ( 'NONE', *, *, #6572, .T. ) ;
#4760=CARTESIAN_POINT ( 'NONE',  ( 1.033464566929133799, 0.000000000000000000, 0.8366141732283465249 ) ) ;
#4761=CARTESIAN_POINT ( 'NONE',  ( -1.033464566929133799, 0.000000000000000000, 0.4330708660342047489 ) ) ;
#4765=CARTESIAN_POINT ( 'NONE',  ( 0.7646288533564489232, -0.1113553986120547346, 1.048228346349165507 ) ) ;
#4766=CARTESIAN_POINT ( 'NONE',  ( -0.7185039370078739607, 1.928577636452523993E-17, 1.643700787401574992 ) ) ;
#4769=CARTESIAN_POINT ( 'NONE',  ( -0.7495606340400177148, 0.1264236179284866091, 1.774114173174582643 ) ) ;
#4770=CARTESIAN_POINT ( 'NONE',  ( 1.002407869896990045, -0.1264236179284866091, 1.636318897584031484 ) ) ;
#4772=CYLINDRICAL_SURFACE ( 'NONE', #1112, 0.1574803149606299191 ) ;
#4773=CARTESIAN_POINT ( 'NONE',  ( 0.7495606340400177148, -0.1264236179284866091, 0.3666338582139531677 ) ) ;
#4774=CARTESIAN_POINT ( 'NONE',  ( -0.9500414927467378812, -0.1787899950787401604, 1.392716535379308285 ) ) ;
#4775=LINE ( 'NONE', #19403, #21284 ) ;
#4776=CARTESIAN_POINT ( 'NONE',  ( -0.7495606340400177148, -0.1264236179284866091, 1.227854330654897685 ) ) ;
#4777=CARTESIAN_POINT ( 'NONE',  ( -0.9500414927467378812, 0.1787899950787401604, 0.07381889758403178958 ) ) ;
#4779=CARTESIAN_POINT ( 'NONE',  ( -1.033464566929133799, 0.000000000000000000, 1.653543306979086580 ) ) ;
#4780=CARTESIAN_POINT ( 'NONE',  ( -1.054774247047244540, -0.07405724077823318263, 1.678149606245448622 ) ) ;
#4781=CARTESIAN_POINT ( 'NONE',  ( -1.054774247047244540, 0.07405724077823318263, 0.02952755900135457801 ) ) ;
#4782=CARTESIAN_POINT ( 'NONE',  ( 0.8759842519685039353, 0.000000000000000000, 4.498031496062992574 ) ) ;
#4783=CARTESIAN_POINT ( 'NONE',  ( -0.9412147342319837628, -0.1574803149606297803, 1.616633858267715551 ) ) ;
#4785=CARTESIAN_POINT ( 'NONE',  ( 1.002407869896990045, -0.1264236179284866091, 1.636318897584031484 ) ) ;
#4788=EDGE_LOOP ( 'NONE', ( #34300, #11258, #6246, #7072 ) ) ;
#4795=CARTESIAN_POINT ( 'NONE',  ( -0.9873396505805591694, 0.1113553986120547346, 1.274606299212598604 ) ) ;
#4799=CARTESIAN_POINT ( 'NONE',  ( -0.7646288533564489232, 0.1113553986120547346, 0.1427165354330708902 ) ) ;
#4800=CARTESIAN_POINT ( 'NONE',  ( 0.6971942568897637749, 2.189545951927499583E-17, 0.7504921259304880854 ) ) ;
#4803=EDGE_CURVE ( 'NONE', #16187, #36149, #6676, .T. ) ;
#4806=CARTESIAN_POINT ( 'NONE',  ( -0.7185039370078739607, 1.928577636452523993E-17, 1.318897637687747926 ) ) ;
#4807=CARTESIAN_POINT ( 'NONE',  ( 0.9500414927467378812, -0.1787899950787401604, 1.870078740103715331 ) ) ;
#4808=CARTESIAN_POINT ( 'NONE',  ( 0.9500414927467377701, 0.1787899950787401604, 1.412401574749386990 ) ) ;
#4810=ORIENTED_EDGE ( 'NONE', *, *, #9556, .F. ) ;
#4812=CARTESIAN_POINT ( 'NONE',  ( 0.9412147342319837628, -0.1574803149606297803, 0.08120078740157485320 ) ) ;
#4817=CARTESIAN_POINT ( 'NONE',  ( 1.002407869896990045, 0.1264236179284866091, 0.2288385826234019815 ) ) ;
#4818=CARTESIAN_POINT ( 'NONE',  ( -0.8019270111902717657, -0.1787899950787401604, 1.702755905458047003 ) ) ;
#4820=CARTESIAN_POINT ( 'NONE',  ( -1.054774247047244540, 0.07405724077823318263, 1.328740157426552049 ) ) ;
#4821=CARTESIAN_POINT ( 'NONE',  ( 0.6971942568897648851, 0.07405724077823318263, 1.264763779473795813 ) ) ;
#4822=CARTESIAN_POINT ( 'NONE',  ( 0.6971942568897626646, 0.07405724077823318263, 0.04429133852891373180 ) ) ;
#4823=CARTESIAN_POINT ( 'NONE',  ( -0.8019270111902717657, 0.1787899950787401604, 1.176181102308441417 ) ) ;
#4824=CARTESIAN_POINT ( 'NONE',  ( 0.8759842519685039353, 0.000000000000000000, 4.498031496062992574 ) ) ;
#4826=CARTESIAN_POINT ( 'NONE',  ( 0.7185039370078739607, 1.928577636452523993E-17, 0.05905511800270921846 ) ) ;
#4827=CARTESIAN_POINT ( 'NONE',  ( 1.054774247047244540, 0.07405724077823318263, 0.4232283464029293896 ) ) ;
#4828=CARTESIAN_POINT ( 'NONE',  ( -0.7495606340400177148, -0.1264236179284866091, 0.3223425196312759144 ) ) ;
#4830=( BOUNDED_CURVE ( )  B_SPLINE_CURVE ( 2, ( #792, #37479, #4628, #19263, #33917, #1040, #15698, #30335, #16848 ),
 .UNSPECIFIED., .F., .T. ) 
 B_SPLINE_CURVE_WITH_KNOTS ( ( 3, 2, 2, 2, 3 ),
 ( 0.5999999999999999778, 0.6025000000000000355, 0.6049999999999999822, 0.6075000000000000400, 0.6099999999999999867 ),
 .UNSPECIFIED. ) 
 CURVE ( )  GEOMETRIC_REPRESENTATION_ITEM ( )  RATIONAL_B_SPLINE_CURVE ( ( 1.000000000000000000, 0.9238795325112869605, 1.000000000000000000, 0.9238795325112869605, 1.000000000000000000, 0.9238795325112869605, 1.000000000000000000, 0.9238795325112829637, 1.000000000000000000 ) ) 
 REPRESENTATION_ITEM ( '' )  ) ;
#4831=FACE_OUTER_BOUND ( 'NONE', #23943, .T. ) ;
#4834=CARTESIAN_POINT ( 'NONE',  ( -0.8107537697050253289, -0.1574803149606297803, 0.3518700787401576324 ) ) ;
#4835=CARTESIAN_POINT ( 'NONE',  ( 1.054774247047244540, 0.07405724077823318263, 1.171259842465921741 ) ) ;
#4836=CARTESIAN_POINT ( 'NONE',  ( -1.054774247047244540, 0.07405724077823318263, 1.953740157426552715 ) ) ;
#4843=CARTESIAN_POINT ( 'NONE',  ( -0.8107537697050254399, 0.1574803149606300301, 1.390255905404285119 ) ) ;
#4847=AXIS2_PLACEMENT_3D ( 'NONE', #10792, #3805, #15312 ) ;
#4849=CARTESIAN_POINT ( 'NONE',  ( 0.9873396505805591694, -0.1113553986120547346, 0.7431102361129447997 ) ) ;
#4850=( BOUNDED_CURVE ( )  B_SPLINE_CURVE ( 2, ( #33240, #41470, #5314, #29437, #45325, #8437, #30985, #18353, #11185 ),
 .UNSPECIFIED., .F., .T. ) 
 B_SPLINE_CURVE_WITH_KNOTS ( ( 3, 2, 2, 2, 3 ),
 ( 0.6400000000000000133, 0.6424999999999999600, 0.6450000000000000178, 0.6474999999999999645, 0.6500000000000000222 ),
 .UNSPECIFIED. ) 
 CURVE ( )  GEOMETRIC_REPRESENTATION_ITEM ( )  RATIONAL_B_SPLINE_CURVE ( ( 1.000000000000000000, 0.9238795325112869605, 1.000000000000000000, 0.9238795325112869605, 1.000000000000000000, 0.9238795325112869605, 1.000000000000000000, 0.9238795325112829637, 1.000000000000000000 ) ) 
 REPRESENTATION_ITEM ( '' )  ) ;
#4851=CARTESIAN_POINT ( 'NONE',  ( -0.8107537697050254399, 0.1574803149606300301, 1.439468503937006760 ) ) ;
#4852=CARTESIAN_POINT ( 'NONE',  ( 0.6971942568897648851, -0.07405724077823297447, 1.579724409395055318 ) ) ;
#4853=CARTESIAN_POINT ( 'NONE',  ( 0.6971942568897626646, 0.07405724077823318263, 0.1574803149068664809 ) ) ;
#4858=CARTESIAN_POINT ( 'NONE',  ( -1.054774247047244096, 0.000000000000000000, 0.6569881889226141247 ) ) ;
#4859=EDGE_CURVE ( 'NONE', #36696, #20228, #11886, .T. ) ;
#4861=CARTESIAN_POINT ( 'NONE',  ( 1.033464566929133799, 0.000000000000000000, 0.3149606298137326843 ) ) ;
#4865=CARTESIAN_POINT ( 'NONE',  ( 0.9500414927467378812, -0.1787899950787401604, 1.397637795221827295 ) ) ;
#4866=CARTESIAN_POINT ( 'NONE',  ( 1.054774247047244096, 0.000000000000000000, 1.793799212544661348 ) ) ;
#4874=CARTESIAN_POINT ( 'NONE',  ( 0.9500414927467378812, -0.1787899950787401604, 0.3690944881352128393 ) ) ;
#4875=CARTESIAN_POINT ( 'NONE',  ( -0.9873396505805591694, -0.1113553986120547346, 0.7529527559055118058 ) ) ;
#4877=CARTESIAN_POINT ( 'NONE',  ( -0.7185039370078766252, -0.06523048226348168721, 1.321358267609009207 ) ) ;
#4881=CARTESIAN_POINT ( 'NONE',  ( -0.8019270111902717657, 0.1787899950787401604, 1.333661417269071059 ) ) ;
#4882=CARTESIAN_POINT ( 'NONE',  ( 0.9873396505805591694, 0.1113553986120547346, 0.8710629920184568276 ) ) ;
#4883=ORIENTED_EDGE ( 'NONE', *, *, #12877, .T. ) ;
#4884=CARTESIAN_POINT ( 'NONE',  ( -0.8107537697050254399, 0.1574803149606300301, 1.754429133858266932 ) ) ;
#4890=CARTESIAN_POINT ( 'NONE',  ( -0.9412147342319837628, -0.1574803149606297803, 1.222933070866141669 ) ) ;
#4891=CARTESIAN_POINT ( 'NONE',  ( 1.002407869896990045, 0.1264236179284866091, 1.562499999946236118 ) ) ;
#4892=CARTESIAN_POINT ( 'NONE',  ( -0.9873396505805591694, 0.1113553986120547346, 1.274606299212598604 ) ) ;
#4893=CARTESIAN_POINT ( 'NONE',  ( -1.033464566929134687, 0.06523048226347956391, 1.144192913278300194 ) ) ;
#4895=CARTESIAN_POINT ( 'NONE',  ( -0.7646288533564489232, -0.1113553986120547346, 0.4281496062992125595 ) ) ;
#4898=ORIENTED_EDGE ( 'NONE', *, *, #3304, .T. ) ;
#4900=CARTESIAN_POINT ( 'NONE',  ( 0.9412147342319837628, -0.1574803149606297803, 0.5930118110236221041 ) ) ;
#4902=CARTESIAN_POINT ( 'NONE',  ( -0.6971942568897648851, -0.07405724077823297447, 1.579724409395055318 ) ) ;
#4904=CARTESIAN_POINT ( 'NONE',  ( -0.8759842519685039353, 0.1787899950787401882, 1.218011810969858111 ) ) ;
#4905=ORIENTED_EDGE ( 'NONE', *, *, #35980, .T. ) ;
#4907=CARTESIAN_POINT ( 'NONE',  ( -0.8759842519685039353, -0.1787899950787401882, 0.3321850393163153226 ) ) ;
#4909=CARTESIAN_POINT ( 'NONE',  ( -0.7185039370078739607, 1.928577636452523993E-17, 0.6200787401574803237 ) ) ;
#4914=ADVANCED_FACE ( 'NONE', ( #17943 ), #9534, .T. ) ;
#4915=FACE_OUTER_BOUND ( 'NONE', #37759, .T. ) ;
#4917=ADVANCED_FACE ( 'NONE', ( #33068 ), #29504, .T. ) ;
#4918=CARTESIAN_POINT ( 'NONE',  ( -0.8759842519685039353, 0.000000000000000000, 0.000000000000000000 ) ) ;
#4922=CARTESIAN_POINT ( 'NONE',  ( -0.8759842519685039353, 0.1787899950787401882, 0.2337598424659216578 ) ) ;
#4923=CARTESIAN_POINT ( 'NONE',  ( -0.7185039370078746268, -0.06523048226347956391, 0.8587598425196850682 ) ) ;
#4927=CARTESIAN_POINT ( 'NONE',  ( 0.7495606340400177148, -0.1264236179284866091, 0.9571850393163149340 ) ) ;
#4928=DIRECTION ( 'NONE',  ( -1.000000000000000000, 0.000000000000000000, 0.000000000000000000 ) ) ;
#4929=CARTESIAN_POINT ( 'NONE',  ( 0.8759842519685039353, 0.1574803149606299191, 1.515748031496062964 ) ) ;
#4930=CARTESIAN_POINT ( 'NONE',  ( 0.7329509277787201738, 0.07874508389649351181, 1.981681257654730466 ) ) ;
#4935=CARTESIAN_POINT ( 'NONE',  ( 0.8759842519685039353, 0.1787899950787401882, 0.9768700786863937502 ) ) ;
#4936=CARTESIAN_POINT ( 'NONE',  ( 0.8019270111902716547, 0.1787899950787401604, 1.811023621993480548 ) ) ;
#4940=CARTESIAN_POINT ( 'NONE',  ( -0.8759842519685039353, 0.1574803149606299191, 0.8464566929133857665 ) ) ;
#4943=CARTESIAN_POINT ( 'NONE',  ( -0.9412147342319837628, -0.1574803149606297803, 0.1107283463491660208 ) ) ;
#4944=FACE_OUTER_BOUND ( 'NONE', #38741, .T. ) ;
#4945=CARTESIAN_POINT ( 'NONE',  ( 0.6971942568897648851, -0.07405724077823297447, 1.067913385773007651 ) ) ;
#4946=CARTESIAN_POINT ( 'NONE',  ( 1.033464566929133799, 1.928577636452524610E-17, 4.498031496062992574 ) ) ;
#4950=CARTESIAN_POINT ( 'NONE',  ( -1.054774247047244096, 0.000000000000000000, 0.2583661416785200671 ) ) ;
#4953=( GEOMETRIC_REPRESENTATION_CONTEXT ( 3 ) GLOBAL_UNCERTAINTY_ASSIGNED_CONTEXT ( ( #6183 ) ) GLOBAL_UNIT_ASSIGNED_CONTEXT ( ( #1373, #5455, #44977 ) ) REPRESENTATION_CONTEXT ( 'NONE', 'WORKASPACE' ) ) ;
#4954=CARTESIAN_POINT ( 'NONE',  ( -1.054774247047244540, 0.07405724077823318263, 1.835629921206078485 ) ) ;
#4955=CARTESIAN_POINT ( 'NONE',  ( -1.054774247047244540, 0.07405724077823318263, 0.9694881889226145688 ) ) ;
#4957=CARTESIAN_POINT ( 'NONE',  ( -1.002407869896990045, 0.1264236179284866091, 0.5044291338045039375 ) ) ;
#4960=LINE ( 'NONE', #18864, #19567 ) ;
#4965=CARTESIAN_POINT ( 'NONE',  ( 0.9412147342319837628, -0.1574803149606297803, 0.4749015748031497064 ) ) ;
#4966=DIRECTION ( 'NONE',  ( 0.000000000000000000, 0.000000000000000000, -1.000000000000000000 ) ) ;
#4969=CARTESIAN_POINT ( 'NONE',  ( -0.6971942568897637749, 2.189545951927499583E-17, 0.3961614172690708924 ) ) ;
#4970=( BOUNDED_CURVE ( )  B_SPLINE_CURVE ( 2, ( #24433, #6441, #24905, #27833, #2372, #42393, #17007, #38812, #46688 ),
 .UNSPECIFIED., .F., .T. ) 
 B_SPLINE_CURVE_WITH_KNOTS ( ( 3, 2, 2, 2, 3 ),
 ( 0.000000000000000000, 0.002500000000000000052, 0.005000000000000000104, 0.007499999999999998855, 0.01000000000000000021 ),
 .UNSPECIFIED. ) 
 CURVE ( )  GEOMETRIC_REPRESENTATION_ITEM ( )  RATIONAL_B_SPLINE_CURVE ( ( 1.000000000000000000, 0.9238795325112869605, 1.000000000000000000, 0.9238795325112869605, 1.000000000000000000, 0.9238795325112869605, 1.000000000000000000, 0.9238795325112869605, 1.000000000000000000 ) ) 
 REPRESENTATION_ITEM ( '' )  ) ;
#4973=ORIENTED_EDGE ( 'NONE', *, *, #44093, .T. ) ;
#4976=CARTESIAN_POINT ( 'NONE',  ( -0.9500414927467377701, -0.1787899950787401604, 1.555118110182457158 ) ) ;
#4982=CARTESIAN_POINT ( 'NONE',  ( 0.7185039370078746268, 0.06523048226347956391, 0.4995078740157484765 ) ) ;
#4986=CARTESIAN_POINT ( 'NONE',  ( -1.033464566929134687, 0.06523048226347956391, 1.183562992018456272 ) ) ;
#4987=CARTESIAN_POINT ( 'NONE',  ( 1.002407869896990045, -0.1264236179284866091, 0.4945866141194645849 ) ) ;
#4988=CARTESIAN_POINT ( 'NONE',  ( 0.9500414927467377701, -0.1787899950787401604, 0.05413385821395302888 ) ) ;
#4995=CARTESIAN_POINT ( 'NONE',  ( -0.6971942568897637749, 2.189545951927499583E-17, 1.109744094434425232 ) ) ;
#4996=CARTESIAN_POINT ( 'NONE',  ( 0.9412147342319837628, -0.1574803149606297803, 1.026082677165353729 ) ) ;
#4997=DIRECTION ( 'NONE',  ( -1.000000000000000000, 0.000000000000000000, 0.000000000000000000 ) ) ;
#4999=CARTESIAN_POINT ( 'NONE',  ( 0.7646288533564489232, 0.1113553986120547346, 0.6053149605223937524 ) ) ;
#5005=CARTESIAN_POINT ( 'NONE',  ( 0.9412147342319837628, -0.1574803149606297803, 0.8292322834645677876 ) ) ;
#5006=CARTESIAN_POINT ( 'NONE',  ( 0.9412147342319837628, -0.1574803149606297803, 0.9079724409448817202 ) ) ;
#5010=CARTESIAN_POINT ( 'NONE',  ( 0.7185039370078746268, -0.06523048226347956391, 1.203248031388535200 ) ) ;
#5012=ORIENTED_EDGE ( 'NONE', *, *, #46777, .T. ) ;
#5013=ORIENTED_EDGE ( 'NONE', *, *, #23048, .F. ) ;
#5014=CARTESIAN_POINT ( 'NONE',  ( -1.054774247047244540, -0.07405724077823318263, 1.796259842465923073 ) ) ;
#5015=CARTESIAN_POINT ( 'NONE',  ( 0.8759842519685039353, 0.1787899950787401882, 1.808562992072220377 ) ) ;
#5018=CARTESIAN_POINT ( 'NONE',  ( -0.8019270111902717657, 0.1787899950787401604, 0.9055118109698585549 ) ) ;
#5020=CARTESIAN_POINT ( 'NONE',  ( 0.7495606340400177148, 0.1264236179284866091, 0.3961614172690708924 ) ) ;
#5021=CARTESIAN_POINT ( 'NONE',  ( -0.6971942568897648851, -0.07405724077823297447, 1.304133858213953667 ) ) ;
#5024=CARTESIAN_POINT ( 'NONE',  ( -1.054774247047244540, 0.07405724077823318263, 0.1082677164816695514 ) ) ;
#5026=CARTESIAN_POINT ( 'NONE',  ( -0.7495606340400177148, 0.1264236179284866091, 1.813484251914740053 ) ) ;
#5027=DIRECTION ( 'NONE',  ( -6.938893903907229955E-15, 0.000000000000000000, -1.000000000000000000 ) ) ;
#5028=CARTESIAN_POINT ( 'NONE',  ( -0.7185039370078746268, 0.06523048226347956391, 1.798720472440944462 ) ) ;
#5029=CARTESIAN_POINT ( 'NONE',  ( -0.8759842519685039353, -0.1574803149606299191, 0.9448818897637796255 ) ) ;
#5030=CARTESIAN_POINT ( 'NONE',  ( 0.8759842519685039353, -0.1787899950787401882, 1.552657480261196765 ) ) ;
#5033=AXIS2_PLACEMENT_3D ( 'NONE', #38406, #23332, #30091 ) ;
#5035=EDGE_CURVE ( 'NONE', #11957, #27881, #4029, .T. ) ;
#5038=EDGE_CURVE ( 'NONE', #39764, #19512, #8104, .T. ) ;
#5041=CARTESIAN_POINT ( 'NONE',  ( -0.7185039370078746268, -0.06523048226347956391, 0.5831692913385827515 ) ) ;
#5043=MANIFOLD_SOLID_BREP ( 'U-Bolt', #7231 ) ;
#5050=CARTESIAN_POINT ( 'NONE',  ( 0.6971942568897626646, 0.07405724077823318263, 0.9842519684501742638 ) ) ;
#5052=DIRECTION ( 'NONE',  ( 0.000000000000000000, 0.000000000000000000, -1.000000000000000000 ) ) ;
#5053=CARTESIAN_POINT ( 'NONE',  ( 0.9873396505805591694, 0.1113553986120547346, 0.08366141721530767628 ) ) ;
#5054=CARTESIAN_POINT ( 'NONE',  ( 0.7185039370078739607, 1.928577636452523993E-17, 0.06889763779527559306 ) ) ;
#5055=CARTESIAN_POINT ( 'NONE',  ( 1.033464566929133799, 0.000000000000000000, 1.584645669291338654 ) ) ;
#5060=CARTESIAN_POINT ( 'NONE',  ( 0.9500414927467378812, 0.1787899950787401604, 0.3494094487651343006 ) ) ;
#5062=CARTESIAN_POINT ( 'NONE',  ( -0.7495606340400177148, 0.1264236179284866091, 1.729822834591905556 ) ) ;
#5064=CARTESIAN_POINT ( 'NONE',  ( -0.8019270111902717657, -0.1787899950787401604, 1.235236220418678199 ) ) ;
#5065=CARTESIAN_POINT ( 'NONE',  ( 0.6971942568897637749, 2.189545951927499583E-17, 1.464074803095842370 ) ) ;
#5066=CARTESIAN_POINT ( 'NONE',  ( -1.002407869896990045, -0.1264236179284866091, 0.4945866141194645849 ) ) ;
#5067=CARTESIAN_POINT ( 'NONE',  ( -0.8759842519685039353, 0.1787899950787401882, 1.252460629867496067 ) ) ;
#5068=CARTESIAN_POINT ( 'NONE',  ( 1.033464566929133799, 0.000000000000000000, 0.6692913384751496553 ) ) ;
#5070=CARTESIAN_POINT ( 'NONE',  ( 0.8759842519685039353, 0.1574803149606299191, 1.200787401574803237 ) ) ;
#5071=CARTESIAN_POINT ( 'NONE',  ( 0.7495606340400177148, 0.1264236179284866091, 0.4749015747493858242 ) ) ;
#5072=CARTESIAN_POINT ( 'NONE',  ( -1.054774247047244096, 0.000000000000000000, 0.3371062991588349989 ) ) ;
#5073=CARTESIAN_POINT ( 'NONE',  ( -1.033464566929134687, 0.06523048226347956391, 0.8686023620971983217 ) ) ;
#5074=ORIENTED_EDGE ( 'NONE', *, *, #19360, .F. ) ;
#5075=CARTESIAN_POINT ( 'NONE',  ( -0.7646288533564489232, 0.1113553986120547346, 0.3001968503937008093 ) ) ;
#5076=CARTESIAN_POINT ( 'NONE',  ( 0.7495606340400177148, -0.1264236179284866091, 1.232775590497417362 ) ) ;
#5077=CARTESIAN_POINT ( 'NONE',  ( -0.8019270111902716547, -0.1787899950787401604, 1.978346456639149098 ) ) ;
#5078=CARTESIAN_POINT ( 'NONE',  ( -0.9873396505805591694, -0.1113553986120547346, 1.973425196850393970 ) ) ;
#5080=DIRECTION ( 'NONE',  ( -1.000000000000000000, 0.000000000000000000, 0.000000000000000000 ) ) ;
#5081=EDGE_CURVE ( 'NONE', #6761, #11244, #34543, .T. ) ;
#5084=EDGE_LOOP ( 'NONE', ( #8206, #18474, #22572, #33078 ) ) ;
#5085=CARTESIAN_POINT ( 'NONE',  ( -1.033464566929134687, 0.06523048226347956391, 0.1599409447743626866 ) ) ;
#5088=CARTESIAN_POINT ( 'NONE',  ( 1.054774247047244096, 0.000000000000000000, 1.281988188922614125 ) ) ;
#5089=CARTESIAN_POINT ( 'NONE',  ( 0.7646288533564489232, 0.1113553986120547346, 0.8907480314960629642 ) ) ;
#5091=FACE_OUTER_BOUND ( 'NONE', #34210, .T. ) ;
#5092=CARTESIAN_POINT ( 'NONE',  ( 0.9500414927467378812, 0.1787899950787401604, 1.643700787347811998 ) ) ;
#5096=CARTESIAN_POINT ( 'NONE',  ( -0.8759842519685039353, -0.1787899950787401882, 0.6865157479777322935 ) ) ;
#5098=DIRECTION ( 'NONE',  ( 1.822029033848725028E-16, 0.000000000000000000, 1.000000000000000000 ) ) ;
#5100=CARTESIAN_POINT ( 'NONE',  ( 0.7185039370078739607, 1.928577636452523993E-17, 0.2263779527559055260 ) ) ;
#5102=CARTESIAN_POINT ( 'NONE',  ( 1.054774247047244540, -0.07405724077823318263, 1.481299212544662680 ) ) ;
#5103=CARTESIAN_POINT ( 'NONE',  ( 0.8019270111902716547, 0.1787899950787401604, 1.884842519631275026 ) ) ;
#5104=CARTESIAN_POINT ( 'NONE',  ( 1.054774247047244540, -0.07405724077823318263, 0.2952755904974176948 ) ) ;
#5106=DIRECTION ( 'NONE',  ( 1.822029033848725028E-16, 0.000000000000000000, 1.000000000000000000 ) ) ;
#5109=LINE ( 'NONE', #22862, #41211 ) ;
#5112=CARTESIAN_POINT ( 'NONE',  ( -1.033464566929133799, 0.000000000000000000, 0.1673228346456692994 ) ) ;
#5113=CARTESIAN_POINT ( 'NONE',  ( 0.7495606340400177148, 0.1264236179284866091, 0.4306102361667086820 ) ) ;
#5115=CARTESIAN_POINT ( 'NONE',  ( -1.033464566929133799, 0.000000000000000000, 1.574803149498771537 ) ) ;
#5116=CARTESIAN_POINT ( 'NONE',  ( 0.8759842519685039353, -0.1574803149606299191, 0.7775590550105826448 ) ) ;
#5119=CARTESIAN_POINT ( 'NONE',  ( 0.8481319853008726373, 0.1739929071186617493, 0.03937007952913684772 ) ) ;
#5120=ORIENTED_EDGE ( 'NONE', *, *, #43445, .T. ) ;
#5123=CARTESIAN_POINT ( 'NONE',  ( -0.7185039370078746268, -0.06523048226347956391, 0.5733267715460159675 ) ) ;
#5125=CARTESIAN_POINT ( 'NONE',  ( -0.8759842519685039353, 0.1574803149606299191, 1.240157480314960647 ) ) ;
#5126=CARTESIAN_POINT ( 'NONE',  ( -1.033464566929133799, 0.000000000000000000, 1.978346456692913646 ) ) ;
#5127=CARTESIAN_POINT ( 'NONE',  ( -0.8759842519685039353, 0.000000000000000000, 0.000000000000000000 ) ) ;
#5128=CARTESIAN_POINT ( 'NONE',  ( -0.7185039370078746268, 0.06523048226347956391, 0.7652559054042838982 ) ) ;
#5129=CARTESIAN_POINT ( 'NONE',  ( 0.8107537697050254399, -0.1574803149606297803, 1.916830708553890483 ) ) ;
#5130=CARTESIAN_POINT ( 'NONE',  ( 0.7185039370078746268, 0.06523048226347956391, 1.434547243986962428 ) ) ;
#5135=CARTESIAN_POINT ( 'NONE',  ( 0.9500414927467378812, -0.1787899950787401604, 0.6889763778989935750 ) ) ;
#5137=CARTESIAN_POINT ( 'NONE',  ( 0.6971942568897648851, -0.07405724077823297447, 0.9547244093950545407 ) ) ;
#5139=CARTESIAN_POINT ( 'NONE',  ( -0.6971942568897648851, -0.07405724077823297447, 1.230314960576156746 ) ) ;
#5142=( BOUNDED_CURVE ( )  B_SPLINE_CURVE ( 2, ( #16486, #13366, #34940, #38976, #46169, #38759, #27993, #5447, #1602 ),
 .UNSPECIFIED., .F., .T. ) 
 B_SPLINE_CURVE_WITH_KNOTS ( ( 3, 2, 2, 2, 3 ),
 ( 0.8699999999999999956, 0.8725000000000000533, 0.8750000000000000000, 0.8774999999999999467, 0.8800000000000000044 ),
 .UNSPECIFIED. ) 
 CURVE ( )  GEOMETRIC_REPRESENTATION_ITEM ( )  RATIONAL_B_SPLINE_CURVE ( ( 1.000000000000000000, 0.9238795325112899581, 1.000000000000000000, 0.9238795325112869605, 1.000000000000000000, 0.9238795325112869605, 1.000000000000000000, 0.9238795325112869605, 1.000000000000000000 ) ) 
 REPRESENTATION_ITEM ( '' )  ) ;
#5146=( BOUNDED_CURVE ( )  B_SPLINE_CURVE ( 2, ( #39064, #20858, #2641, #46492, #32137, #6474, #2871, #46730, #9142 ),
 .UNSPECIFIED., .F., .T. ) 
 B_SPLINE_CURVE_WITH_KNOTS ( ( 3, 2, 2, 2, 3 ),
 ( 0.4500000000000000111, 0.4525000000000000133, 0.4550000000000000155, 0.4575000000000000178, 0.4600000000000000200 ),
 .UNSPECIFIED. ) 
 CURVE ( )  GEOMETRIC_REPRESENTATION_ITEM ( )  RATIONAL_B_SPLINE_CURVE ( ( 1.000000000000000000, 0.9238795325112869605, 1.000000000000000000, 0.9238795325112869605, 1.000000000000000000, 0.9238795325112869605, 1.000000000000000000, 0.9238795325112869605, 1.000000000000000000 ) ) 
 REPRESENTATION_ITEM ( '' )  ) ;
#5147=CARTESIAN_POINT ( 'NONE',  ( 0.8759842519685039353, 0.1574803149606299191, 0.8759842518609765039 ) ) ;
#5149=ORIENTED_EDGE ( 'NONE', *, *, #33424, .F. ) ;
#5152=VERTEX_POINT ( 'NONE', #26816 ) ;
#5154=CARTESIAN_POINT ( 'NONE',  ( -0.7185039370078778465, -0.06523048226348396317, 1.400098425089323140 ) ) ;
#5155=CARTESIAN_POINT ( 'NONE',  ( 0.7185039370078746268, -0.06523048226347956391, 0.1008858266641264878 ) ) ;
#5158=CARTESIAN_POINT ( 'NONE',  ( -1.054774247047244540, -0.07405724077823318263, 0.1820866141194649179 ) ) ;
#5159=CARTESIAN_POINT ( 'NONE',  ( -1.033464566929133799, 0.000000000000000000, 1.072834645669291431 ) ) ;
#5163=CARTESIAN_POINT ( 'NONE',  ( 0.8759842519685039353, 0.1574803149606299191, 0.4133858267716535861 ) ) ;
#5164=CARTESIAN_POINT ( 'NONE',  ( 1.054774247047244540, -0.07405724077823318263, 0.9694881889226144578 ) ) ;
#5165=CARTESIAN_POINT ( 'NONE',  ( 1.054774247047244540, -0.07405724077823318263, 0.1377952755367876370 ) ) ;
#5166=CARTESIAN_POINT ( 'NONE',  ( -1.033464566929134687, 0.06523048226347956391, 0.6323818896562525271 ) ) ;
#5167=CARTESIAN_POINT ( 'NONE',  ( 0.9873396505805591694, -0.1113553986120547346, 1.540354330708661568 ) ) ;
#5168=CARTESIAN_POINT ( 'NONE',  ( 0.7252227560879499491, -0.07532008605015085012, 1.984724907739004562 ) ) ;
#5171=AXIS2_PLACEMENT_3D ( 'NONE', #10923, #36067, #17855 ) ;
#5174=CARTESIAN_POINT ( 'NONE',  ( 0.8759842519685039353, -0.1787899950787401882, 0.9571850393163149340 ) ) ;
#5175=CARTESIAN_POINT ( 'NONE',  ( 0.8759842519685039353, -0.1787899950787401882, 1.867618110182456714 ) ) ;
#5176=CARTESIAN_POINT ( 'NONE',  ( 1.033464566929134687, 0.06523048226347956391, 0.2780511809948349455 ) ) ;
#5177=VERTEX_POINT ( 'NONE', #12910 ) ;
#5178=CARTESIAN_POINT ( 'NONE',  ( 1.033464566929133799, 0.000000000000000000, 1.702755905511810885 ) ) ;
#5181=CARTESIAN_POINT ( 'NONE',  ( 0.8759842519685039353, 0.1787899950787401882, 1.173720472387181246 ) ) ;
#5185=CYLINDRICAL_SURFACE ( 'NONE', #16100, 0.1574803149606299191 ) ;
#5186=EDGE_CURVE ( 'NONE', #38980, #34169, #10341, .T. ) ;
#5187=CARTESIAN_POINT ( 'NONE',  ( -1.054774247047244540, 0.07405724077823318263, 0.5364173227808821665 ) ) ;
#5191=CARTESIAN_POINT ( 'NONE',  ( -1.002407869896990045, -0.1264236179284866091, 1.788877952702141672 ) ) ;
#5192=ORIENTED_EDGE ( 'NONE', *, *, #4803, .T. ) ;
#5193=CARTESIAN_POINT ( 'NONE',  ( -0.7495606340400177148, 0.1264236179284866091, 0.4749015747493858242 ) ) ;
#5200=DIRECTION ( 'NONE',  ( 1.822029033848725028E-16, 0.000000000000000000, 1.000000000000000000 ) ) ;
#5201=CARTESIAN_POINT ( 'NONE',  ( -1.033464566929133799, 1.928577636452524610E-17, 2.869337061179095023E-17 ) ) ;
#5203=CARTESIAN_POINT ( 'NONE',  ( -1.002407869896990045, -0.1264236179284866091, 0.4896653542769449086 ) ) ;
#5206=CARTESIAN_POINT ( 'NONE',  ( -0.6971942568897648851, 0.07405724077823318263, 1.461614173174583753 ) ) ;
#5210=CARTESIAN_POINT ( 'NONE',  ( 0.8107537697050253289, -0.1574803149606297803, 0.5093503937007877180 ) ) ;
#5213=CARTESIAN_POINT ( 'NONE',  ( -0.7185039370078746268, 0.06523048226347956391, 1.277066929026331898 ) ) ;
#5214=CARTESIAN_POINT ( 'NONE',  ( 0.6971942568897626646, -0.07405724077823297447, 0.5610236219934807700 ) ) ;
#5216=CARTESIAN_POINT ( 'NONE',  ( 0.7185039370078739607, 1.928577636452523993E-17, 1.092519685039370136 ) ) ;
#5218=ORIENTED_EDGE ( 'NONE', *, *, #13436, .F. ) ;
#5220=CARTESIAN_POINT ( 'NONE',  ( -0.7495606340400177148, 0.1264236179284866091, 1.065452755851747924 ) ) ;
#5221=CARTESIAN_POINT ( 'NONE',  ( 0.7185039370078739607, 1.928577636452523993E-17, 1.171259842519684957 ) ) ;
#5227=CARTESIAN_POINT ( 'NONE',  ( -0.7185039370078739607, 0.000000000000000000, -2.869337061179095023E-17 ) ) ;
#5230=CARTESIAN_POINT ( 'NONE',  ( 0.7185039370078739607, 1.928577636452523993E-17, 0.9251968502861732668 ) ) ;
#5231=ORIENTED_EDGE ( 'NONE', *, *, #1719, .T. ) ;
#5232=CARTESIAN_POINT ( 'NONE',  ( -0.7185039370078739607, 1.928577636452523993E-17, 0.5708661416247566844 ) ) ;
#5233=CARTESIAN_POINT ( 'NONE',  ( 1.033464566929133799, 0.000000000000000000, 0.8759842519685039353 ) ) ;
#5234=CARTESIAN_POINT ( 'NONE',  ( 1.002407869896990045, -0.1264236179284866091, 0.7258858267178898149 ) ) ;
#5236=EDGE_LOOP ( 'NONE', ( #11509, #43297, #18749, #39900 ) ) ;
#5243=CARTESIAN_POINT ( 'NONE',  ( 0.7646288533564489232, -0.1113553986120547346, 1.087598425089322918 ) ) ;
#5248=CARTESIAN_POINT ( 'NONE',  ( -0.8759842519685039353, -0.1787899950787401882, 1.828248031442299082 ) ) ;
#5250=EDGE_CURVE ( 'NONE', #17112, #40844, #28118, .T. ) ;
#5251=CARTESIAN_POINT ( 'NONE',  ( 0.8019270111902717657, -0.1787899950787401604, 1.904527559001354398 ) ) ;
#5254=CARTESIAN_POINT ( 'NONE',  ( 0.8759842519685039353, 0.1787899950787401882, 0.3912401574265515491 ) ) ;
#5255=CARTESIAN_POINT ( 'NONE',  ( -0.8019270111902717657, 0.1787899950787401604, 1.412401574749386990 ) ) ;
#5258=CARTESIAN_POINT ( 'NONE',  ( -0.7495606340400177148, 0.1264236179284866091, 0.9030511810485984947 ) ) ;
#5259=CARTESIAN_POINT ( 'NONE',  ( -0.7495606340400177148, -0.1264236179284866091, 0.09104330703285078152 ) ) ;
#5260=( BOUNDED_CURVE ( )  B_SPLINE_CURVE ( 2, ( #9765, #47117, #2781, #35642, #39915, #6855, #46403, #17408, #13365 ),
 .UNSPECIFIED., .F., .T. ) 
 B_SPLINE_CURVE_WITH_KNOTS ( ( 3, 2, 2, 2, 3 ),
 ( 0.1499999999999999944, 0.1524999999999999967, 0.1549999999999999989, 0.1575000000000000011, 0.1600000000000000033 ),
 .UNSPECIFIED. ) 
 CURVE ( )  GEOMETRIC_REPRESENTATION_ITEM ( )  RATIONAL_B_SPLINE_CURVE ( ( 1.000000000000000000, 0.9238795325112869605, 1.000000000000000000, 0.9238795325112869605, 1.000000000000000000, 0.9238795325112869605, 1.000000000000000000, 0.9238795325112869605, 1.000000000000000000 ) ) 
 REPRESENTATION_ITEM ( '' )  ) ;
#5261=CARTESIAN_POINT ( 'NONE',  ( 0.7185039370078739607, 0.000000000000000000, 4.498031496062992574 ) ) ;
#5262=CARTESIAN_POINT ( 'NONE',  ( -0.7495606340400177148, 0.1264236179284866091, 1.734744094434425232 ) ) ;
#5263=CARTESIAN_POINT ( 'NONE',  ( -0.8019270111902717657, -0.1787899950787401604, 0.05413385821395302888 ) ) ;
#5264=DIRECTION ( 'NONE',  ( 0.000000000000000000, 0.000000000000000000, -1.000000000000000000 ) ) ;
#5265=CARTESIAN_POINT ( 'NONE',  ( -0.9412147342319837628, -0.1574803149606297803, 1.734744094488190003 ) ) ;
#5266=CARTESIAN_POINT ( 'NONE',  ( 0.8759842519685039353, 0.000000000000000000, 4.498031496062992574 ) ) ;
#5268=CARTESIAN_POINT ( 'NONE',  ( 0.8759842519685039353, -0.1787899950787401882, 1.670767716481669440 ) ) ;
#5277=( BOUNDED_CURVE ( )  B_SPLINE_CURVE ( 2, ( #1790, #8506, #19998, #16428, #34178, #31056, #27230, #45621, #34882 ),
 .UNSPECIFIED., .F., .F. ) 
 B_SPLINE_CURVE_WITH_KNOTS ( ( 3, 2, 2, 2, 3 ),
 ( 0.1000000000000000056, 0.1024999999999999939, 0.1049999999999999961, 0.1074999999999999983, 0.1100000000000000006 ),
 .UNSPECIFIED. ) 
 CURVE ( )  GEOMETRIC_REPRESENTATION_ITEM ( )  RATIONAL_B_SPLINE_CURVE ( ( 1.000000000000000000, 0.9238795325112869605, 1.000000000000000000, 0.9238795325112869605, 1.000000000000000000, 0.9238795325112869605, 1.000000000000000000, 0.9238795325112869605, 1.000000000000000000 ) ) 
 REPRESENTATION_ITEM ( '' )  ) ;
#5283=CARTESIAN_POINT ( 'NONE',  ( 0.8759842519685039353, -0.1787899950787401882, 0.9571850393163149340 ) ) ;
#5287=CARTESIAN_POINT ( 'NONE',  ( 0.9500414927467378812, 0.1787899950787401604, 1.963582677111591401 ) ) ;
#5288=CARTESIAN_POINT ( 'NONE',  ( 0.8107537697050253289, 0.1574803149606300301, 0.2189960629921262614 ) ) ;
#5289=CARTESIAN_POINT ( 'NONE',  ( -0.7185039370078739607, 0.000000000000000000, -2.869337061179095023E-17 ) ) ;
#5291=CARTESIAN_POINT ( 'NONE',  ( 0.9412147342319837628, -0.1574803149606297803, 0.1205708661417322358 ) ) ;
#5293=EDGE_CURVE ( 'NONE', #955, #22060, #41209, .T. ) ;
#5295=CARTESIAN_POINT ( 'NONE',  ( -0.8019270111902717657, -0.1787899950787401604, 1.781496062938362934 ) ) ;
#5296=VERTEX_POINT ( 'NONE', #38984 ) ;
#5297=CARTESIAN_POINT ( 'NONE',  ( -0.6971942568897648851, -0.07405724077823297447, 1.230314960576156746 ) ) ;
#5298=CARTESIAN_POINT ( 'NONE',  ( -0.8759842519685039353, 0.000000000000000000, 0.000000000000000000 ) ) ;
#5299=CARTESIAN_POINT ( 'NONE',  ( 0.7495606340400177148, 0.1264236179284866091, 1.380413385773007873 ) ) ;
#5301=CARTESIAN_POINT ( 'NONE',  ( -0.6971942568897637749, 2.189545951927499583E-17, 1.262303149552535420 ) ) ;
#5305=CARTESIAN_POINT ( 'NONE',  ( 0.9500414927467377701, 0.1787899950787401604, 0.6249999999462356737 ) ) ;
#5306=CARTESIAN_POINT ( 'NONE',  ( -1.054774247047244540, 0.07405724077823318263, 0.3789370078202520253 ) ) ;
#5308=CARTESIAN_POINT ( 'NONE',  ( 0.7646288533564489232, 0.1113553986120547346, 1.668307086506645609 ) ) ;
#5310=CARTESIAN_POINT ( 'NONE',  ( -0.9873396505805591694, 0.1113553986120547346, 0.2903543307086614012 ) ) ;
#5311=VECTOR ( 'NONE', #47097, 39.37007874015748143 ) ;
#5312=CARTESIAN_POINT ( 'NONE',  ( 0.9500414927467377701, -0.1787899950787401604, 1.161417322780881278 ) ) ;
#5313=CARTESIAN_POINT ( 'NONE',  ( -0.9500414927467377701, -0.1787899950787401604, 1.943897637741510254 ) ) ;
#5314=CARTESIAN_POINT ( 'NONE',  ( 0.9873396505805591694, 0.1113553986120547346, 1.304133858160188897 ) ) ;
#5315=ORIENTED_EDGE ( 'NONE', *, *, #19796, .F. ) ;
#5316=CARTESIAN_POINT ( 'NONE',  ( -0.6971942568897626646, 0.07405724077823318263, 0.9104330708123776761 ) ) ;
#5319=VERTEX_POINT ( 'NONE', #9539 ) ;
#5320=CARTESIAN_POINT ( 'NONE',  ( -0.7646288533564489232, 0.1113553986120547346, 1.392716535325543292 ) ) ;
#5322=CARTESIAN_POINT ( 'NONE',  ( 0.7495606340400177148, -0.1264236179284866091, 1.345964566875370139 ) ) ;
#5324=CARTESIAN_POINT ( 'NONE',  ( 0.8759842519685039353, 0.1574803149606299191, 1.870078740157480324 ) ) ;
#5325=CARTESIAN_POINT ( 'NONE',  ( 1.054774247047244540, 0.07405724077823318263, 1.599409448765135133 ) ) ;
#5328=DIRECTION ( 'NONE',  ( 1.000000000000000000, 0.000000000000000000, -1.822029033848725275E-16 ) ) ;
#5329=CARTESIAN_POINT ( 'NONE',  ( 0.7495606340400177148, -0.1264236179284866091, 0.4404527558517480901 ) ) ;
#5331=CARTESIAN_POINT ( 'NONE',  ( -0.6971942568897648851, -0.07405724077823297447, 0.7578740156942688211 ) ) ;
#5335=CARTESIAN_POINT ( 'NONE',  ( -0.8100458409162250017, -0.1592901343197297148, 1.986959380109183826 ) ) ;
#5336=DIRECTION ( 'NONE',  ( 1.822029033848725028E-16, 0.000000000000000000, 1.000000000000000000 ) ) ;
#5339=CARTESIAN_POINT ( 'NONE',  ( 0.9500414927467378812, -0.1787899950787401604, 1.555118110182455382 ) ) ;
#5340=CARTESIAN_POINT ( 'NONE',  ( 0.8759842519685039353, 0.1787899950787401882, 1.803641732229700700 ) ) ;
#5341=CARTESIAN_POINT ( 'NONE',  ( 1.054774247047244096, 0.000000000000000000, 0.4552165353793071745 ) ) ;
#5344=FACE_OUTER_BOUND ( 'NONE', #37131, .T. ) ;
#5346=CARTESIAN_POINT ( 'NONE',  ( 0.6971942568897626646, -0.07405724077823297447, 0.3986220471903312301 ) ) ;
#5347=CARTESIAN_POINT ( 'NONE',  ( 0.7582988962546464151, -0.1171207568837268065, 0.03937125541389787514 ) ) ;
#5348=EDGE_CURVE ( 'NONE', #1520, #5296, #19558, .T. ) ;
#5352=CARTESIAN_POINT ( 'NONE',  ( -0.8759842519685039353, -0.1787899950787401882, 1.350885826717889815 ) ) ;
#5353=CARTESIAN_POINT ( 'NONE',  ( 0.7185039370078739607, 1.928577636452523993E-17, 0.7677165353255432922 ) ) ;
#5354=VERTEX_POINT ( 'NONE', #29906 ) ;
#5356=CARTESIAN_POINT ( 'NONE',  ( -0.8759842519685039353, 0.1574803149606299191, 0.7972440943806614611 ) ) ;
#5357=CARTESIAN_POINT ( 'NONE',  ( 0.6971942568897626646, 0.07405724077823318263, 0.9891732282926934960 ) ) ;
#5361=CARTESIAN_POINT ( 'NONE',  ( -0.7185039370078739607, 1.928577636452523993E-17, 0.6102362203649134287 ) ) ;
#5362=CARTESIAN_POINT ( 'NONE',  ( -0.7185039370078741827, 0.06523048226347841205, 0.8144685039370075375 ) ) ;
#5363=CARTESIAN_POINT ( 'NONE',  ( 0.6971942568897648851, -0.07405724077823297447, 1.737204724355685848 ) ) ;
#5364=CARTESIAN_POINT ( 'NONE',  ( -0.9873396505805591694, -0.1113553986120547346, 1.264763779527559029 ) ) ;
#5366=CARTESIAN_POINT ( 'NONE',  ( -1.033464566929133799, 1.928577636452524610E-17, 2.869337061179095023E-17 ) ) ;
#5368=CARTESIAN_POINT ( 'NONE',  ( 0.6971942568897626646, -0.07405724077823297447, 0.1279527558517483676 ) ) ;
#5369=CARTESIAN_POINT ( 'NONE',  ( 0.9873396505805591694, -0.1113553986120547346, 1.491141732175936818 ) ) ;
#5373=CARTESIAN_POINT ( 'NONE',  ( -0.7495606340400177148, 0.1264236179284866091, 1.611712598371433103 ) ) ;
#5375=CARTESIAN_POINT ( 'NONE',  ( -1.054774247047244540, 0.07405724077823318263, 1.368110236166710125 ) ) ;
#5379=CARTESIAN_POINT ( 'NONE',  ( 1.033464566929134687, 0.06523048226347956391, 1.852854330601134469 ) ) ;
#5382=VERTEX_POINT ( 'NONE', #33014 ) ;
#5386=CARTESIAN_POINT ( 'NONE',  ( 0.9873396505805591694, 0.1113553986120547346, 1.737204724301921299 ) ) ;
#5389=CARTESIAN_POINT ( 'NONE',  ( 1.033464566929133799, 0.000000000000000000, 1.781496062992125928 ) ) ;
#5391=CARTESIAN_POINT ( 'NONE',  ( -1.054774247047244096, 0.000000000000000000, 0.2632874015210397434 ) ) ;
#5392=CARTESIAN_POINT ( 'NONE',  ( -0.7185039370078746268, -0.06523048226347956391, 0.9768700787401572994 ) ) ;
#5394=CARTESIAN_POINT ( 'NONE',  ( 0.8107537697050254399, 0.1574803149606300301, 0.4158464566929134798 ) ) ;
#5395=CARTESIAN_POINT ( 'NONE',  ( 0.6971942568897648851, 0.07405724077823318263, 1.028543307032851795 ) ) ;
#5396=CARTESIAN_POINT ( 'NONE',  ( 0.8019270111902716547, 0.1787899950787401604, 1.451771653489543290 ) ) ;
#5397=CARTESIAN_POINT ( 'NONE',  ( 1.033464566929134687, -0.06523048226347956391, 0.2436023622047245041 ) ) ;
#5398=CARTESIAN_POINT ( 'NONE',  ( 0.9412147342319837628, -0.1574803149606297803, 1.498523622047243764 ) ) ;
#5399=CARTESIAN_POINT ( 'NONE',  ( 0.8282458751120667095, 0.1518331050034476271, 1.979292245347968660 ) ) ;
#5400=LINE ( 'NONE', #41329, #7843 ) ;
#5406=EDGE_CURVE ( 'NONE', #22273, #22073, #3328, .T. ) ;
#5407=CARTESIAN_POINT ( 'NONE',  ( 0.9500414927467377701, 0.1787899950787401604, 1.013779527505291878 ) ) ;
#5408=CARTESIAN_POINT ( 'NONE',  ( 0.7495606340400177148, 0.1264236179284866091, 1.813484251914740053 ) ) ;
#5409=CARTESIAN_POINT ( 'NONE',  ( 0.8107537697050253289, 0.1574803149606300301, 0.2878937006798746312 ) ) ;
#5411=AXIS2_PLACEMENT_3D ( 'NONE', #1162, #1881, #41634 ) ;
#5413=CARTESIAN_POINT ( 'NONE',  ( 1.006022016660639284, 0.1011351315952034868, 0.03936735655933119166 ) ) ;
#5414=LINE ( 'NONE', #23416, #18322 ) ;
#5416=CARTESIAN_POINT ( 'NONE',  ( -0.9873396505805591694, 0.1113553986120547346, 0.2805118109160948947 ) ) ;
#5418=CARTESIAN_POINT ( 'NONE',  ( 1.054774247047244540, -0.07405724077823318263, 1.279527559001355286 ) ) ;
#5419=EDGE_CURVE ( 'NONE', #19846, #11651, #28753, .T. ) ;
#5421=CARTESIAN_POINT ( 'NONE',  ( 0.9412147342319837628, 0.1574803149606300301, 1.227854330601133359 ) ) ;
#5424=( BOUNDED_CURVE ( )  B_SPLINE_CURVE ( 2, ( #27176, #20180, #23322, #8688, #27418, #37938, #5089, #8932, #26931 ),
 .UNSPECIFIED., .F., .T. ) 
 B_SPLINE_CURVE_WITH_KNOTS ( ( 3, 2, 2, 2, 3 ),
 ( 0.4400000000000000022, 0.4425000000000000044, 0.4450000000000000067, 0.4475000000000000089, 0.4500000000000000111 ),
 .UNSPECIFIED. ) 
 CURVE ( )  GEOMETRIC_REPRESENTATION_ITEM ( )  RATIONAL_B_SPLINE_CURVE ( ( 1.000000000000000000, 0.9238795325112869605, 1.000000000000000000, 0.9238795325112869605, 1.000000000000000000, 0.9238795325112869605, 1.000000000000000000, 0.9238795325112869605, 1.000000000000000000 ) ) 
 REPRESENTATION_ITEM ( '' )  ) ;
#5425=CARTESIAN_POINT ( 'NONE',  ( -1.054774247047244096, 0.000000000000000000, 0.6126968503399370380 ) ) ;
#5426=CARTESIAN_POINT ( 'NONE',  ( 0.9412147342319837628, 0.1574803149606300301, 0.2534448818897638289 ) ) ;
#5431=CARTESIAN_POINT ( 'NONE',  ( -1.002407869896990045, -0.1264236179284866091, 1.006397637741511808 ) ) ;
#5432=CARTESIAN_POINT ( 'NONE',  ( -0.6971942568897648851, 0.07405724077823318263, 1.850393700733638624 ) ) ;
#5433=VERTEX_POINT ( 'NONE', #6898 ) ;
#5434=CARTESIAN_POINT ( 'NONE',  ( -0.9500414927467378812, -0.1787899950787401604, 0.6102362204186774219 ) ) ;
#5438=CARTESIAN_POINT ( 'NONE',  ( 0.7185039370078739607, 1.928577636452523993E-17, 1.801181102362204633 ) ) ;
#5443=ORIENTED_EDGE ( 'NONE', *, *, #6158, .T. ) ;
#5444=VECTOR ( 'NONE', #2498, 39.37007874015748143 ) ;
#5447=CARTESIAN_POINT ( 'NONE',  ( -1.033464566929134687, -0.06523048226347956391, 1.769192913278299084 ) ) ;
#5448=CARTESIAN_POINT ( 'NONE',  ( -0.6971942568897637749, 2.189545951927499583E-17, 0.5142716534895434011 ) ) ;
#5449=CARTESIAN_POINT ( 'NONE',  ( 1.033464566929133799, 0.000000000000000000, 1.181102362097196989 ) ) ;
#5452=CARTESIAN_POINT ( 'NONE',  ( -0.6971942568897648851, 0.07405724077823318263, 1.540354330654897685 ) ) ;
#5455=( NAMED_UNIT ( * ) PLANE_ANGLE_UNIT ( ) SI_UNIT ( $, .RADIAN. ) ) ;
#5459=CARTESIAN_POINT ( 'NONE',  ( 0.8759842519685039353, 0.000000000000000000, 4.498031496062992574 ) ) ;
#5460=CARTESIAN_POINT ( 'NONE',  ( -0.8759842519685039353, -0.1574803149606299191, 1.171259842412157637 ) ) ;
#5461=EDGE_CURVE ( 'NONE', #5617, #3387, #32751, .T. ) ;
#5462=CARTESIAN_POINT ( 'NONE',  ( 0.7495606340400177148, 0.1264236179284866091, 0.6323818897100157432 ) ) ;
#5468=CARTESIAN_POINT ( 'NONE',  ( 0.7646288533564489232, -0.1113553986120547346, 1.136811023622047223 ) ) ;
#5470=CARTESIAN_POINT ( 'NONE',  ( -0.8904237653908255723, -0.1743634098521867348, 1.988438120113575014 ) ) ;
#5471=CARTESIAN_POINT ( 'NONE',  ( 0.8759842519685039353, 0.000000000000000000, 4.498031496062992574 ) ) ;
#5472=VECTOR ( 'NONE', #10974, 39.37007874015748143 ) ;
#5473=EDGE_CURVE ( 'NONE', #32643, #2780, #33026, .T. ) ;
#5474=CARTESIAN_POINT ( 'NONE',  ( 1.033464566929133799, 0.000000000000000000, 0.1673228346456692994 ) ) ;
#5476=CYLINDRICAL_SURFACE ( 'NONE', #30827, 0.1574803149606299191 ) ;
#5480=CARTESIAN_POINT ( 'NONE',  ( 0.9873396505805591694, -0.1113553986120547346, 0.2805118110236220486 ) ) ;
#5481=CARTESIAN_POINT ( 'NONE',  ( 0.7495606340400177148, 0.1264236179284866091, 0.7849409448281259305 ) ) ;
#5482=ORIENTED_EDGE ( 'NONE', *, *, #39785, .F. ) ;
#5484=CARTESIAN_POINT ( 'NONE',  ( 1.033464566929134687, -0.06523048226347956391, 0.9128937007874010634 ) ) ;
#5489=CARTESIAN_POINT ( 'NONE',  ( 1.033464566929133799, 0.000000000000000000, 1.259842519577511810 ) ) ;
#5490=CARTESIAN_POINT ( 'NONE',  ( -0.9873396505805591694, 0.1113553986120547346, 1.855314960522393530 ) ) ;
#5492=EDGE_LOOP ( 'NONE', ( #18344, #31919, #40127, #24759 ) ) ;
#5493=CARTESIAN_POINT ( 'NONE',  ( -1.054774247047244540, 0.07405724077823318263, 1.958661417269071947 ) ) ;
#5494=CARTESIAN_POINT ( 'NONE',  ( 0.9500414927467378812, -0.1787899950787401604, 1.909448818843873186 ) ) ;
#5497=CARTESIAN_POINT ( 'NONE',  ( 0.7495606340400177148, 0.1264236179284866091, 0.4749015747493858242 ) ) ;
#5498=CARTESIAN_POINT ( 'NONE',  ( -1.054774247047244540, -0.07405724077823318263, 1.397637795221827295 ) ) ;
#5500=CARTESIAN_POINT ( 'NONE',  ( -0.7495606340400177148, -0.1264236179284866091, 0.2485236219934806867 ) ) ;
#5501=CARTESIAN_POINT ( 'NONE',  ( -1.033464566929133799, 0.000000000000000000, 0.5610236220472440971 ) ) ;
#5502=CARTESIAN_POINT ( 'NONE',  ( -0.6971942568897648851, -0.07405724077823297447, 1.742125984198204858 ) ) ;
#5503=CARTESIAN_POINT ( 'NONE',  ( -0.6971942568897626646, -0.07405724077823297447, 0.08858267711159097113 ) ) ;
#5505=CARTESIAN_POINT ( 'NONE',  ( -0.8759842519685039353, 0.1574803149606299191, 1.791338582677165281 ) ) ;
#5507=CARTESIAN_POINT ( 'NONE',  ( 0.6971942568897637749, 2.189545951927499583E-17, 1.739665354276945131 ) ) ;
#5513=ORIENTED_EDGE ( 'NONE', *, *, #8435, .T. ) ;
#5516=EDGE_CURVE ( 'NONE', #26852, #19285, #33516, .T. ) ;
#5525=CARTESIAN_POINT ( 'NONE',  ( 1.002407869896990045, 0.1264236179284866091, 0.9719488188438739629 ) ) ;
#5526=CARTESIAN_POINT ( 'NONE',  ( 0.7185039370078739607, 1.928577636452523993E-17, 0.6200787401574803237 ) ) ;
#5528=CARTESIAN_POINT ( 'NONE',  ( 0.7646288533564489232, -0.1113553986120547346, 0.06397637784522892945 ) ) ;
#5530=CARTESIAN_POINT ( 'NONE',  ( -0.7197834393077419124, 0.09009865225401414435, 0.03937007874015843040 ) ) ;
#5534=( BOUNDED_CURVE ( )  B_SPLINE_CURVE ( 2, ( #13560, #17383, #27971, #6598, #32021, #24817, #6829, #32269, #32508 ),
 .UNSPECIFIED., .F., .T. ) 
 B_SPLINE_CURVE_WITH_KNOTS ( ( 3, 2, 2, 2, 3 ),
 ( 0.08999999999999999667, 0.09249999999999999889, 0.09500000000000000111, 0.09750000000000000333, 0.1000000000000000056 ),
 .UNSPECIFIED. ) 
 CURVE ( )  GEOMETRIC_REPRESENTATION_ITEM ( )  RATIONAL_B_SPLINE_CURVE ( ( 1.000000000000000000, 0.9238795325112869605, 1.000000000000000000, 0.9238795325112869605, 1.000000000000000000, 0.9238795325112869605, 1.000000000000000000, 0.9238795325112869605, 1.000000000000000000 ) ) 
 REPRESENTATION_ITEM ( '' )  ) ;
#5537=CARTESIAN_POINT ( 'NONE',  ( -0.6971942568897637749, 2.189545951927499583E-17, 1.892224409395055096 ) ) ;
#5539=CARTESIAN_POINT ( 'NONE',  ( -0.9500414927467378812, 0.1787899950787401604, 1.412401574749386990 ) ) ;
#5544=AXIS2_PLACEMENT_3D ( 'NONE', #26177, #3410, #7943 ) ;
#5545=CARTESIAN_POINT ( 'NONE',  ( -0.8759842519685039353, -0.1787899950787401882, 1.272145669237574772 ) ) ;
#5548=CARTESIAN_POINT ( 'NONE',  ( 0.8759842519685039353, -0.1787899950787401882, 0.5684055117572598403 ) ) ;
#5549=CARTESIAN_POINT ( 'NONE',  ( -0.6971942568897648851, -0.07405724077823297447, 0.4773622046706456068 ) ) ;
#5550=FACE_OUTER_BOUND ( 'NONE', #29046, .T. ) ;
#5553=CARTESIAN_POINT ( 'NONE',  ( -0.8759842519685039353, 0.1574803149606299191, 0.3740157480314960647 ) ) ;
#5554=CARTESIAN_POINT ( 'NONE',  ( 1.002407869896990045, 0.1264236179284866091, 1.370570866087968520 ) ) ;
#5557=CARTESIAN_POINT ( 'NONE',  ( -0.8759842519685039353, -0.1574803149606299191, 0.6299212598425196763 ) ) ;
#5558=CARTESIAN_POINT ( 'NONE',  ( -0.9500414927467378812, 0.1787899950787401604, 0.9793307086076531442 ) ) ;
#5560=CARTESIAN_POINT ( 'NONE',  ( -0.6971942568897626646, -0.07405724077823297447, 0.08366141726907129483 ) ) ;
#5562=ORIENTED_EDGE ( 'NONE', *, *, #7886, .F. ) ;
#5573=FACE_OUTER_BOUND ( 'NONE', #18222, .T. ) ;
#5580=ADVANCED_FACE ( 'NONE', ( #46270 ), #42889, .T. ) ;
#5581=CARTESIAN_POINT ( 'NONE',  ( 0.8759842519685039353, -0.1787899950787401882, 0.4847440944344252323 ) ) ;
#5582=CARTESIAN_POINT ( 'NONE',  ( -0.8759842519685039353, 0.1787899950787401882, 0.8636811023084409733 ) ) ;
#5586=CARTESIAN_POINT ( 'NONE',  ( -0.8485855016175685162, -0.1715156613748270442, 1.987705042127893895 ) ) ;
#5588=CARTESIAN_POINT ( 'NONE',  ( 0.6971942568897637749, 2.189545951927499583E-17, 1.503444881836000002 ) ) ;
#5589=CARTESIAN_POINT ( 'NONE',  ( 0.8019270111902716547, -0.1787899950787401604, 1.899606299158834943 ) ) ;
#5590=CARTESIAN_POINT ( 'NONE',  ( 1.054774247047244096, 0.000000000000000000, 0.4158464566391496531 ) ) ;
#5592=DIRECTION ( 'NONE',  ( 1.822029033848725028E-16, 0.000000000000000000, 1.000000000000000000 ) ) ;
#5595=CARTESIAN_POINT ( 'NONE',  ( 0.6971942568897626646, 0.07405724077823318263, 0.5118110235682844511 ) ) ;
#5597=CARTESIAN_POINT ( 'NONE',  ( 0.6971942568897637749, 2.189545951927499583E-17, 1.301673228292692830 ) ) ;
#5599=CARTESIAN_POINT ( 'NONE',  ( 1.033464566929133799, 0.000000000000000000, 0.2066929133858267931 ) ) ;
#5600=CARTESIAN_POINT ( 'NONE',  ( -0.8019270111902717657, 0.1787899950787401604, 1.491141732229701367 ) ) ;
#5601=CARTESIAN_POINT ( 'NONE',  ( 1.033464566929133799, 0.000000000000000000, 0.8661417321759370402 ) ) ;
#5604=CARTESIAN_POINT ( 'NONE',  ( 0.9500414927467378812, 0.1787899950787401604, 1.018700787347811110 ) ) ;
#5605=ORIENTED_EDGE ( 'NONE', *, *, #3420, .F. ) ;
#5608=CARTESIAN_POINT ( 'NONE',  ( -0.9873396505805591694, 0.1113553986120547346, 0.6348425195775118102 ) ) ;
#5609=CARTESIAN_POINT ( 'NONE',  ( -1.033464566929134687, 0.06523048226347956391, 1.390255905511810441 ) ) ;
#5611=CARTESIAN_POINT ( 'NONE',  ( 1.033464566929133799, 1.928577636452524610E-17, 4.498031496062992574 ) ) ;
#5612=FACE_OUTER_BOUND ( 'NONE', #20383, .T. ) ;
#5614=CARTESIAN_POINT ( 'NONE',  ( 1.002407869896990045, 0.1264236179284866091, 0.1894685038832444879 ) ) ;
#5615=CARTESIAN_POINT ( 'NONE',  ( -1.054774247047244540, -0.07405724077823318263, 0.09842519679663024046 ) ) ;
#5616=CARTESIAN_POINT ( 'NONE',  ( 0.9412147342319837628, 0.1574803149606300301, 1.464074803042079598 ) ) ;
#5617=VERTEX_POINT ( 'NONE', #25190 ) ;
#5621=CARTESIAN_POINT ( 'NONE',  ( 1.054774247047244540, 0.07405724077823318263, 0.9350393700249758355 ) ) ;
#5622=CARTESIAN_POINT ( 'NONE',  ( -1.054774247047244096, 0.000000000000000000, 1.675688976324189117 ) ) ;
#5627=DIRECTION ( 'NONE',  ( 1.000000000000000000, 0.000000000000000000, -1.822029033848725275E-16 ) ) ;
#5629=ORIENTED_EDGE ( 'NONE', *, *, #28993, .F. ) ;
#5637=CARTESIAN_POINT ( 'NONE',  ( 1.033464566929134687, -0.06523048226347956391, 1.897145669291339320 ) ) ;
#5639=EDGE_CURVE ( 'NONE', #9079, #45828, #21590, .T. ) ;
#5640=CARTESIAN_POINT ( 'NONE',  ( -0.7495606340400177148, 0.1264236179284866091, 0.2780511810485988278 ) ) ;
#5641=CARTESIAN_POINT ( 'NONE',  ( -1.033464566929134687, 0.06523048226347956391, 1.075295275590550048 ) ) ;
#5644=CARTESIAN_POINT ( 'NONE',  ( 0.6971942568897648851, 0.07405724077823318263, 1.107283464513165949 ) ) ;
#5645=CARTESIAN_POINT ( 'NONE',  ( 0.6971942568897637749, 2.189545951927499583E-17, 0.2386811023084413619 ) ) ;
#5646=CARTESIAN_POINT ( 'NONE',  ( 1.033464566929133799, 0.000000000000000000, 0.2460629921259842590 ) ) ;
#5647=CARTESIAN_POINT ( 'NONE',  ( 0.9873396505805591694, 0.1113553986120547346, 1.510826771653543288 ) ) ;
#5648=CARTESIAN_POINT ( 'NONE',  ( 1.033464566929134687, -0.06523048226347956391, 1.424704724409449064 ) ) ;
#5650=CARTESIAN_POINT ( 'NONE',  ( 1.033464566929134687, -0.06523048226347956391, 1.454232283357038691 ) ) ;
#5651=CARTESIAN_POINT ( 'NONE',  ( 0.9412147342319837628, -0.1574803149606297803, 0.4650590550105836440 ) ) ;
#5652=CARTESIAN_POINT ( 'NONE',  ( -0.9412147342319837628, -0.1574803149606297803, 1.646161417215307843 ) ) ;
#5654=CARTESIAN_POINT ( 'NONE',  ( 0.6971942568897648851, 0.07405724077823318263, 0.9448818897100165204 ) ) ;
#5655=CARTESIAN_POINT ( 'NONE',  ( 1.002407869896990045, 0.1264236179284866091, 1.961122047190330786 ) ) ;
#5656=CARTESIAN_POINT ( 'NONE',  ( 0.7185039370078746268, 0.06523048226347956391, 0.3715551180027090727 ) ) ;
#5657=ORIENTED_EDGE ( 'NONE', *, *, #23720, .T. ) ;
#5662=CARTESIAN_POINT ( 'NONE',  ( -0.8107537697050253289, 0.1574803149606300301, 0.2878937006798746312 ) ) ;
#5664=CARTESIAN_POINT ( 'NONE',  ( 0.6971942568897637749, 2.189545951927499583E-17, 1.341043307032850462 ) ) ;
#5668=CARTESIAN_POINT ( 'NONE',  ( -0.7185039370078714072, 0.06523048226347728795, 1.877460629921259727 ) ) ;
#5669=CARTESIAN_POINT ( 'NONE',  ( -1.002407869896990045, -0.1264236179284866091, 0.6471456692375747721 ) ) ;
#5670=CARTESIAN_POINT ( 'NONE',  ( 0.8107537697050254399, -0.1574803149606297803, 1.365649606191686294 ) ) ;
#5672=ORIENTED_EDGE ( 'NONE', *, *, #26289, .F. ) ;
#5675=CARTESIAN_POINT ( 'NONE',  ( -0.7495606340400177148, -0.1264236179284866091, 1.035925196796629866 ) ) ;
#5676=CARTESIAN_POINT ( 'NONE',  ( -0.9873396505805591694, -0.1113553986120547346, 0.04429133858267716300 ) ) ;
#5678=CARTESIAN_POINT ( 'NONE',  ( -1.002407869896990045, -0.1264236179284866091, 0.7308070865604093802 ) ) ;
#5684=CARTESIAN_POINT ( 'NONE',  ( -1.033464566929133799, 0.000000000000000000, 0.6692913384751496553 ) ) ;
#5686=LINE ( 'NONE', #8802, #12657 ) ;
#5688=CARTESIAN_POINT ( 'NONE',  ( -0.9500414927467378812, 0.1787899950787401604, 0.5413385826234012876 ) ) ;
#5691=ORIENTED_EDGE ( 'NONE', *, *, #41188, .F. ) ;
#5693=CARTESIAN_POINT ( 'NONE',  ( -1.054774247047244540, 0.07405724077823318263, 1.604330708607653921 ) ) ;
#5696=LINE ( 'NONE', #31822, #34890 ) ;
#5697=CARTESIAN_POINT ( 'NONE',  ( -1.033464566929134687, -0.06523048226347956391, 0.1943897636720005040 ) ) ;
#5700=CARTESIAN_POINT ( 'NONE',  ( -0.8107537697050253289, 0.1574803149606300301, 1.311515747923968744 ) ) ;
#5705=CARTESIAN_POINT ( 'NONE',  ( 0.8759842519685039353, 0.1574803149606299191, 1.043307086614173151 ) ) ;
#5706=CARTESIAN_POINT ( 'NONE',  ( -0.9720330238214066609, -0.1495884858916018134, 1.989995714837735408 ) ) ;
#5711=CARTESIAN_POINT ( 'NONE',  ( 0.7185039370078739607, 1.928577636452523993E-17, 1.279527558947590515 ) ) ;
#5718=AXIS2_PLACEMENT_3D ( 'NONE', #7993, #41262, #8948 ) ;
#5719=CARTESIAN_POINT ( 'NONE',  ( 1.002407869896990045, -0.1264236179284866091, 0.7652559054580472253 ) ) ;
#5721=CARTESIAN_POINT ( 'NONE',  ( 0.8759842519685039353, 0.000000000000000000, 4.498031496062992574 ) ) ;
#5725=CARTESIAN_POINT ( 'NONE',  ( 0.9412147342319837628, -0.1574803149606297803, 1.213090551073576107 ) ) ;
#5726=CARTESIAN_POINT ( 'NONE',  ( 0.8759842519685039353, -0.1574803149606299191, 1.171259842412157637 ) ) ;
#5728=VERTEX_POINT ( 'NONE', #23259 ) ;
#5729=CARTESIAN_POINT ( 'NONE',  ( -0.9500414927467378812, 0.1787899950787401604, 1.924212598371433325 ) ) ;
#5730=CARTESIAN_POINT ( 'NONE',  ( 1.054774247047244540, 0.07405724077823318263, 1.801181102308441861 ) ) ;
#5733=CARTESIAN_POINT ( 'NONE',  ( 0.9873396505805591694, -0.1113553986120547346, 1.776574803149606252 ) ) ;
#5734=CARTESIAN_POINT ( 'NONE',  ( -0.8019270111902717657, 0.1787899950787401604, 1.530511810969859443 ) ) ;
#5736=CARTESIAN_POINT ( 'NONE',  ( -0.8759842519685039353, -0.1787899950787401882, 0.9571850393163149340 ) ) ;
#5737=CARTESIAN_POINT ( 'NONE',  ( -0.9500414927467378812, -0.1787899950787401604, 0.2559055117572600624 ) ) ;
#5738=DIRECTION ( 'NONE',  ( 1.822029033848725028E-16, 0.000000000000000000, 1.000000000000000000 ) ) ;
#5739=CARTESIAN_POINT ( 'NONE',  ( -0.7495606340400177148, -0.1264236179284866091, 1.665846456639149764 ) ) ;
#5740=CARTESIAN_POINT ( 'NONE',  ( -1.054774247047244540, -0.07405724077823318263, 0.1427165353793072855 ) ) ;
#5741=LINE ( 'NONE', #17000, #42505 ) ;
#5742=CARTESIAN_POINT ( 'NONE',  ( -0.9412147342319837628, -0.1574803149606297803, 1.813484251968503935 ) ) ;
#5745=CARTESIAN_POINT ( 'NONE',  ( 0.7495606340400177148, 0.1264236179284866091, 1.734744094434425232 ) ) ;
#5749=AXIS2_PLACEMENT_3D ( 'NONE', #17965, #22262, #36661 ) ;
#5751=ORIENTED_EDGE ( 'NONE', *, *, #777, .F. ) ;
#5759=EDGE_CURVE ( 'NONE', #34930, #2118, #40913, .T. ) ;
#5762=CARTESIAN_POINT ( 'NONE',  ( 1.054774247047244096, 0.000000000000000000, 0.4158464566391496531 ) ) ;
#5764=CARTESIAN_POINT ( 'NONE',  ( -0.8759842519685039353, -0.1574803149606299191, 0.8169291337507401662 ) ) ;
#5765=CARTESIAN_POINT ( 'NONE',  ( -1.033464566929134687, -0.06523048226347956391, 0.6766732283464570452 ) ) ;
#5767=CARTESIAN_POINT ( 'NONE',  ( 1.002407869896990045, 0.1264236179284866091, 0.8538385826234016207 ) ) ;
#5770=CARTESIAN_POINT ( 'NONE',  ( 0.7185039370078739607, 1.928577636452523993E-17, 0.05905511800270921846 ) ) ;
#5772=DIRECTION ( 'NONE',  ( 1.822029033848725028E-16, 0.000000000000000000, 1.000000000000000000 ) ) ;
#5775=CYLINDRICAL_SURFACE ( 'NONE', #7049, 0.1574803149606299191 ) ;
#5776=CARTESIAN_POINT ( 'NONE',  ( -0.8019270111902717657, 0.1787899950787401604, 1.884842519631275026 ) ) ;
#5778=AXIS2_PLACEMENT_3D ( 'NONE', #11006, #25624, #40199 ) ;
#5779=CARTESIAN_POINT ( 'NONE',  ( -0.9500414927467378812, 0.1787899950787401604, 1.530511810969859443 ) ) ;
#5780=CARTESIAN_POINT ( 'NONE',  ( 0.8759842519685039353, 0.1787899950787401882, 1.375492125930488196 ) ) ;
#5784=CARTESIAN_POINT ( 'NONE',  ( -0.6971942568897637749, 2.189545951927499583E-17, 0.6766732282926929409 ) ) ;
#5785=CARTESIAN_POINT ( 'NONE',  ( 1.002407869896990045, 0.1264236179284866091, 0.1107283464029293202 ) ) ;
#5786=CARTESIAN_POINT ( 'NONE',  ( -0.9500414927467378812, 0.1787899950787401604, 1.289370078686393750 ) ) ;
#5787=EDGE_CURVE ( 'NONE', #426, #38785, #20126, .T. ) ;
#5789=CARTESIAN_POINT ( 'NONE',  ( 0.9500414927467377701, 0.1787899950787401604, 0.6643700786863929730 ) ) ;
#5790=CARTESIAN_POINT ( 'NONE',  ( -0.7495606340400177148, 0.1264236179284866091, 0.5880905511273386566 ) ) ;
#5794=CARTESIAN_POINT ( 'NONE',  ( -1.033464566929134687, 0.06523048226347956391, 0.3272637795275589734 ) ) ;
#5795=EDGE_CURVE ( 'NONE', #22721, #4172, #5741, .T. ) ;
#5796=CARTESIAN_POINT ( 'NONE',  ( 1.054774247047244540, -0.07405724077823318263, 1.323818897584032594 ) ) ;
#5798=CARTESIAN_POINT ( 'NONE',  ( -0.9873396505805591694, -0.1113553986120547346, 1.845472440837354178 ) ) ;
#5799=ORIENTED_EDGE ( 'NONE', *, *, #16805, .F. ) ;
#5801=CARTESIAN_POINT ( 'NONE',  ( -0.8759842519685039353, 0.1787899950787401882, 1.021161417269070837 ) ) ;
#5808=CIRCLE ( 'NONE', #22648, 0.1787899950787401049 ) ;
#5813=CARTESIAN_POINT ( 'NONE',  ( 0.8759842519685039353, 0.000000000000000000, 4.498031496062992574 ) ) ;
#5815=CARTESIAN_POINT ( 'NONE',  ( 0.8759842519685039353, 0.1787899950787401882, 1.567421259788755794 ) ) ;
#5820=CARTESIAN_POINT ( 'NONE',  ( 0.8019270111902717657, -0.1787899950787401604, 0.4822834645131655606 ) ) ;
#5821=( BOUNDED_CURVE ( )  B_SPLINE_CURVE ( 2, ( #15236, #43731, #10934, #29880, #36794, #29181, #40823, #14515, #39892 ),
 .UNSPECIFIED., .F., .T. ) 
 B_SPLINE_CURVE_WITH_KNOTS ( ( 3, 2, 2, 2, 3 ),
 ( 0.6899999999999999467, 0.6925000000000000044, 0.6949999999999999512, 0.6975000000000000089, 0.6999999999999999556 ),
 .UNSPECIFIED. ) 
 CURVE ( )  GEOMETRIC_REPRESENTATION_ITEM ( )  RATIONAL_B_SPLINE_CURVE ( ( 1.000000000000000000, 0.9238795325112899581, 1.000000000000000000, 0.9238795325112869605, 1.000000000000000000, 0.9238795325112869605, 1.000000000000000000, 0.9238795325112829637, 1.000000000000000000 ) ) 
 REPRESENTATION_ITEM ( '' )  ) ;
#5822=CARTESIAN_POINT ( 'NONE',  ( -0.8759842519685039353, 0.1787899950787401882, 0.7849409448281259305 ) ) ;
#5824=DIRECTION ( 'NONE',  ( 1.000000000000000000, 0.000000000000000000, 0.000000000000000000 ) ) ;
#5826=CARTESIAN_POINT ( 'NONE',  ( -0.7369741704597091436, -0.09768268266897506269, 1.985206247291391390 ) ) ;
#5828=CARTESIAN_POINT ( 'NONE',  ( -0.7185039370078746268, 0.06523048226347956391, 1.040846456585385882 ) ) ;
#5829=CARTESIAN_POINT ( 'NONE',  ( 0.7495606340400177148, 0.1264236179284866091, 1.577263779473795369 ) ) ;
#5831=CARTESIAN_POINT ( 'NONE',  ( 0.9500414927467377701, -0.1787899950787401604, 0.3690944881352128393 ) ) ;
#5833=CARTESIAN_POINT ( 'NONE',  ( 0.9412147342319837628, -0.1574803149606297803, 0.8587598424121577478 ) ) ;
#5837=CARTESIAN_POINT ( 'NONE',  ( 0.6971942568897626646, -0.07405724077823297447, 0.4379921259304882519 ) ) ;
#5839=CARTESIAN_POINT ( 'NONE',  ( 0.7185039370078739607, 1.928577636452523993E-17, 0.06889763779527559306 ) ) ;
#5841=CARTESIAN_POINT ( 'NONE',  ( -0.7495606340400177148, -0.1264236179284866091, 1.424704724355685181 ) ) ;
#5842=CARTESIAN_POINT ( 'NONE',  ( 0.7646288533564489232, -0.1113553986120547346, 0.8120078739082204899 ) ) ;
#5843=ORIENTED_EDGE ( 'NONE', *, *, #21607, .T. ) ;
#5844=CARTESIAN_POINT ( 'NONE',  ( -0.9873396505805591694, 0.1113553986120547346, 0.7923228345381417848 ) ) ;
#5845=CARTESIAN_POINT ( 'NONE',  ( 0.6971942568897637749, 2.189545951927499583E-17, 0.9916338582139527791 ) ) ;
#5848=CARTESIAN_POINT ( 'NONE',  ( -0.8107537697050253289, -0.1574803149606297803, 0.5388779526483779003 ) ) ;
#5850=CARTESIAN_POINT ( 'NONE',  ( 0.8759842519685039353, -0.1787899950787401882, 1.705216535379307174 ) ) ;
#5851=CARTESIAN_POINT ( 'NONE',  ( -0.7185039370078739607, 1.928577636452523993E-17, 1.446850393700787274 ) ) ;
#5855=DIRECTION ( 'NONE',  ( 0.000000000000000000, 0.000000000000000000, -1.000000000000000000 ) ) ;
#5856=CARTESIAN_POINT ( 'NONE',  ( 0.6971942568897637749, 2.189545951927499583E-17, 0.08612204719033110523 ) ) ;
#5857=CARTESIAN_POINT ( 'NONE',  ( -1.002407869896990045, -0.1264236179284866091, 0.1353346456155277433 ) ) ;
#5858=CARTESIAN_POINT ( 'NONE',  ( 0.8107537697050253289, 0.1574803149606300301, 1.350885826664126821 ) ) ;
#5861=( BOUNDED_CURVE ( )  B_SPLINE_CURVE ( 2, ( #10445, #37012, #29413, #28675, #36324, #4166, #7310, #25042, #6820 ),
 .UNSPECIFIED., .F., .T. ) 
 B_SPLINE_CURVE_WITH_KNOTS ( ( 3, 2, 2, 2, 3 ),
 ( 0.9499999999999999556, 0.9525000000000000133, 0.9549999999999999600, 0.9575000000000000178, 0.9599999999999999645 ),
 .UNSPECIFIED. ) 
 CURVE ( )  GEOMETRIC_REPRESENTATION_ITEM ( )  RATIONAL_B_SPLINE_CURVE ( ( 1.000000000000000000, 0.9238795325112939549, 1.000000000000000000, 0.9238795325112869605, 1.000000000000000000, 0.9238795325112869605, 1.000000000000000000, 0.9238795325112869605, 1.000000000000000000 ) ) 
 REPRESENTATION_ITEM ( '' )  ) ;
#5863=DIRECTION ( 'NONE',  ( 1.000000000000000000, 0.000000000000000000, -1.822029033848725275E-16 ) ) ;
#5866=CARTESIAN_POINT ( 'NONE',  ( -0.8019270111902716547, 0.1787899950787401604, 1.766732283410803239 ) ) ;
#5867=EDGE_CURVE ( 'NONE', #3082, #38318, #2069, .T. ) ;
#5868=VERTEX_POINT ( 'NONE', #6434 ) ;
#5870=DIRECTION ( 'NONE',  ( 0.000000000000000000, 0.000000000000000000, -1.000000000000000000 ) ) ;
#5874=VERTEX_POINT ( 'NONE', #10290 ) ;
#5878=CARTESIAN_POINT ( 'NONE',  ( 0.8107537697050253289, -0.1574803149606297803, 1.808562992125984703 ) ) ;
#5880=EDGE_CURVE ( 'NONE', #46851, #33302, #14964, .T. ) ;
#5881=CARTESIAN_POINT ( 'NONE',  ( -1.002407869896990045, -0.1264236179284866091, 0.3371062991588349989 ) ) ;
#5882=CARTESIAN_POINT ( 'NONE',  ( -0.8759842519685039353, -0.1574803149606299191, 1.102362204724409489 ) ) ;
#5885=CARTESIAN_POINT ( 'NONE',  ( 1.002407869896990045, 0.1264236179284866091, 1.055610236166708793 ) ) ;
#5886=CARTESIAN_POINT ( 'NONE',  ( 0.6971942568897648851, 0.07405724077823318263, 1.456692913332062522 ) ) ;
#5887=CARTESIAN_POINT ( 'NONE',  ( 0.7185039370078746268, -0.06523048226347956391, 0.2288385826771655862 ) ) ;
#5888=CARTESIAN_POINT ( 'NONE',  ( 0.9873396505805591694, -0.1113553986120547346, 1.697834645669291209 ) ) ;
#5891=CARTESIAN_POINT ( 'NONE',  ( -0.8107537697050254399, 0.1574803149606300301, 1.557578740157481212 ) ) ;
#5892=CARTESIAN_POINT ( 'NONE',  ( 0.8019270111902716547, -0.1787899950787401604, 0.9153543306548987957 ) ) ;
#5893=CARTESIAN_POINT ( 'NONE',  ( 0.6971942568897637749, 2.189545951927499583E-17, 1.975885826717889815 ) ) ;
#5894=CARTESIAN_POINT ( 'NONE',  ( 0.8759842519685039353, 0.1574803149606299191, 0.2854330707586145710 ) ) ;
#5895=EDGE_LOOP ( 'NONE', ( #46884, #7248, #20128, #30293 ) ) ;
#5897=CARTESIAN_POINT ( 'NONE',  ( 1.011659506949417420, 0.09243204465627147259, 0.03936570540571364407 ) ) ;
#5899=CARTESIAN_POINT ( 'NONE',  ( -1.033464566929134687, -0.06523048226347956391, 0.2337598424121580809 ) ) ;
#5900=CARTESIAN_POINT ( 'NONE',  ( 0.7495606340400177148, -0.1264236179284866091, 1.345964566875370139 ) ) ;
#5901=CARTESIAN_POINT ( 'NONE',  ( 0.7185039370078739607, 1.928577636452523993E-17, 1.240157480207432883 ) ) ;
#5903=CARTESIAN_POINT ( 'NONE',  ( -0.8107537697050254399, -0.1574803149606297803, 1.011318897530268712 ) ) ;
#5904=ADVANCED_FACE ( 'NONE', ( #43561 ), #34231, .T. ) ;
#5906=CARTESIAN_POINT ( 'NONE',  ( -0.7185039370078739607, 1.928577636452523993E-17, 0.2165354329633393804 ) ) ;
#5908=ORIENTED_EDGE ( 'NONE', *, *, #29325, .T. ) ;
#5910=CARTESIAN_POINT ( 'NONE',  ( -1.054774247047244540, -0.07405724077823318263, 1.008858267662772423 ) ) ;
#5911=CARTESIAN_POINT ( 'NONE',  ( -0.6971942568897648851, -0.07405724077823297447, 1.973425196796630088 ) ) ;
#5914=CARTESIAN_POINT ( 'NONE',  ( -0.8019270111902717657, 0.1787899950787401604, 0.7086614172690703928 ) ) ;
#5921=CARTESIAN_POINT ( 'NONE',  ( -0.6971942568897626646, 0.07405724077823318263, 0.6692913385289144257 ) ) ;
#5922=CARTESIAN_POINT ( 'NONE',  ( 1.033464566929133799, 0.000000000000000000, 1.338582677057826853 ) ) ;
#5923=CARTESIAN_POINT ( 'NONE',  ( -0.6971942568897648851, 0.07405724077823318263, 1.658464566875369472 ) ) ;
#5925=CARTESIAN_POINT ( 'NONE',  ( -0.8107537697050254399, 0.1574803149606300301, 0.4945866141732282451 ) ) ;
#5926=LINE ( 'NONE', #13373, #6286 ) ;
#5928=FACE_OUTER_BOUND ( 'NONE', #1151, .T. ) ;
#5929=CARTESIAN_POINT ( 'NONE',  ( -0.9873396505805591694, 0.1113553986120547346, 1.264763779420031486 ) ) ;
#5932=CARTESIAN_POINT ( 'NONE',  ( -0.8107537697050254399, 0.1574803149606300301, 0.4158464566929134798 ) ) ;
#5934=CARTESIAN_POINT ( 'NONE',  ( 0.7646288533564489232, 0.1113553986120547346, 1.126968503937007871 ) ) ;
#5936=CARTESIAN_POINT ( 'NONE',  ( 0.9412147342319837628, -0.1574803149606297803, 0.5831692912310552090 ) ) ;
#5940=CARTESIAN_POINT ( 'NONE',  ( 1.033464566929133799, 1.928577636452524610E-17, 4.498031496062992574 ) ) ;
#5942=CARTESIAN_POINT ( 'NONE',  ( -0.8107537697050254399, -0.1574803149606297803, 1.060531496062992352 ) ) ;
#5943=FACE_OUTER_BOUND ( 'NONE', #597, .T. ) ;
#5944=CARTESIAN_POINT ( 'NONE',  ( 0.9500414927467378812, 0.1787899950787401604, 0.8562992125446617919 ) ) ;
#5945=CARTESIAN_POINT ( 'NONE',  ( 0.9873396505805591694, -0.1113553986120547346, 1.461614173228346525 ) ) ;
#5946=CARTESIAN_POINT ( 'NONE',  ( 1.033464566929134687, -0.06523048226347956391, 0.7062007872940467834 ) ) ;
#5951=CARTESIAN_POINT ( 'NONE',  ( -0.7185039370078746268, 0.06523048226347956391, 1.405019685039369914 ) ) ;
#5952=EDGE_CURVE ( 'NONE', #8391, #34753, #14668, .T. ) ;
#5953=CIRCLE ( 'NONE', #39609, 0.1574803149606299191 ) ;
#5955=CARTESIAN_POINT ( 'NONE',  ( -0.9500414927467378812, -0.1787899950787401604, 1.988188976324187562 ) ) ;
#5956=CARTESIAN_POINT ( 'NONE',  ( 0.8759842519685039353, 0.1787899950787401882, 1.847933070812378009 ) ) ;
#5958=CARTESIAN_POINT ( 'NONE',  ( 0.8759842519685039353, 0.000000000000000000, 4.498031496062992574 ) ) ;
#5959=CARTESIAN_POINT ( 'NONE',  ( -0.6971942568897637749, 2.189545951927499583E-17, 1.498523621993480326 ) ) ;
#5961=EDGE_CURVE ( 'NONE', #47215, #32278, #4960, .T. ) ;
#5963=CARTESIAN_POINT ( 'NONE',  ( -0.6971942568897637749, 2.189545951927499583E-17, 0.2829724408911185041 ) ) ;
#5965=CARTESIAN_POINT ( 'NONE',  ( -0.6971942568897637749, 2.189545951927499583E-17, 1.936515747977732405 ) ) ;
#5967=CARTESIAN_POINT ( 'NONE',  ( -0.8759842519685039353, -0.1574803149606299191, 1.811023622047244208 ) ) ;
#5971=CARTESIAN_POINT ( 'NONE',  ( -0.7646288533564489232, -0.1113553986120547346, 1.491141732283464583 ) ) ;
#5974=CARTESIAN_POINT ( 'NONE',  ( -1.054774247047244540, -0.07405724077823318263, 1.245078740103716886 ) ) ;
#5980=CARTESIAN_POINT ( 'NONE',  ( -1.033464566929134687, -0.06523048226347956391, 1.375492125876724980 ) ) ;
#5981=CARTESIAN_POINT ( 'NONE',  ( 1.002407869896990045, 0.1264236179284866091, 0.4207677164816693294 ) ) ;
#5984=CARTESIAN_POINT ( 'NONE',  ( -1.033464566929134687, 0.06523048226347956391, 0.8292322833570401341 ) ) ;
#5985=CARTESIAN_POINT ( 'NONE',  ( -1.033464566929133799, 0.000000000000000000, 0.7185039370078739607 ) ) ;
#5987=CARTESIAN_POINT ( 'NONE',  ( 1.002407869896990045, 0.1264236179284866091, 0.8932086613635591421 ) ) ;
#5991=CARTESIAN_POINT ( 'NONE',  ( 1.033464566929134687, 0.06523048226347956391, 0.08120078729404769935 ) ) ;
#5994=CARTESIAN_POINT ( 'NONE',  ( 0.9412147342319837628, 0.1574803149606300301, 0.7160433069790875793 ) ) ;
#5996=ADVANCED_FACE ( 'NONE', ( #8559 ), #22468, .T. ) ;
#5998=CARTESIAN_POINT ( 'NONE',  ( 1.002407869896990045, -0.1264236179284866091, 0.3371062991588349989 ) ) ;
#6000=CARTESIAN_POINT ( 'NONE',  ( -0.8759842519685039353, 0.1787899950787401882, 1.843011810969858333 ) ) ;
#6002=CARTESIAN_POINT ( 'NONE',  ( -1.054774247047244540, -0.07405724077823318263, 1.481299212544662680 ) ) ;
#6003=CARTESIAN_POINT ( 'NONE',  ( 1.054774247047244540, 0.07405724077823318263, 1.407480314906865981 ) ) ;
#6005=CARTESIAN_POINT ( 'NONE',  ( -0.8019270111902717657, 0.1787899950787401604, 0.6692913385289144257 ) ) ;
#6006=CARTESIAN_POINT ( 'NONE',  ( 0.6971942568897626646, -0.07405724077823297447, 0.1279527558517483676 ) ) ;
#6009=CARTESIAN_POINT ( 'NONE',  ( 1.054774247047244096, 0.000000000000000000, 0.6176181101824566033 ) ) ;
#6010=CARTESIAN_POINT ( 'NONE',  ( -0.8759842519685039353, 0.1787899950787401882, 0.5437992125446614589 ) ) ;
#6013=VECTOR ( 'NONE', #21923, 39.37007874015748143 ) ;
#6015=CARTESIAN_POINT ( 'NONE',  ( -0.7185039370078746268, -0.06523048226347956391, 0.5044291338582675976 ) ) ;
#6016=CARTESIAN_POINT ( 'NONE',  ( 1.054774247047244540, 0.07405724077823318263, 1.249999999946235896 ) ) ;
#6020=CARTESIAN_POINT ( 'NONE',  ( -0.8019270111902717657, 0.1787899950787401604, 0.9842519684501742638 ) ) ;
#6023=ORIENTED_EDGE ( 'NONE', *, *, #9749, .T. ) ;
#6024=DIRECTION ( 'NONE',  ( 0.000000000000000000, 0.000000000000000000, -1.000000000000000000 ) ) ;
#6026=CYLINDRICAL_SURFACE ( 'NONE', #17014, 0.1574803149606299191 ) ;
#6030=CARTESIAN_POINT ( 'NONE',  ( -0.7185039370078739607, 1.928577636452523993E-17, 0.9645669290263307882 ) ) ;
#6036=CARTESIAN_POINT ( 'NONE',  ( 0.8759842519685039353, -0.1787899950787401882, 0.5241141731745827537 ) ) ;
#6037=CARTESIAN_POINT ( 'NONE',  ( -1.054774247047244540, 0.07405724077823318263, 0.8169291338045038264 ) ) ;
#6042=CARTESIAN_POINT ( 'NONE',  ( 1.054774247047244540, -0.07405724077823318263, 1.520669291284818758 ) ) ;
#6045=CARTESIAN_POINT ( 'NONE',  ( 0.7495606340400177148, -0.1264236179284866091, 0.4404527558517480901 ) ) ;
#6046=EDGE_CURVE ( 'NONE', #398, #11324, #8214, .T. ) ;
#6049=DIRECTION ( 'NONE',  ( 0.000000000000000000, 0.000000000000000000, -1.000000000000000000 ) ) ;
#6054=CARTESIAN_POINT ( 'NONE',  ( 0.9500414927467378812, -0.1787899950787401604, 0.4478346456155276045 ) ) ;
#6056=CARTESIAN_POINT ( 'NONE',  ( -1.033464566929134687, -0.06523048226347956391, 0.9424212597349931331 ) ) ;
#6057=CARTESIAN_POINT ( 'NONE',  ( -0.6971942568897648851, -0.07405724077823297447, 1.382874015694268044 ) ) ;
#6060=CARTESIAN_POINT ( 'NONE',  ( 0.7495606340400177148, 0.1264236179284866091, 0.9473425196312755814 ) ) ;
#6061=VERTEX_POINT ( 'NONE', #47361 ) ;
#6063=CARTESIAN_POINT ( 'NONE',  ( -0.8107537697050253289, 0.1574803149606300301, 0.5241141731208195376 ) ) ;
#6064=CARTESIAN_POINT ( 'NONE',  ( 0.7185039370078739607, 1.928577636452523993E-17, 1.801181102362204633 ) ) ;
#6065=CARTESIAN_POINT ( 'NONE',  ( -0.8107537697050253289, 0.1574803149606300301, 1.439468503937006538 ) ) ;
#6066=CARTESIAN_POINT ( 'NONE',  ( -0.6971942568897626646, -0.07405724077823297447, 0.8710629920722218200 ) ) ;
#6068=CARTESIAN_POINT ( 'NONE',  ( -0.7250449425850237217, -0.07798161211236025181, 0.03937007874015843734 ) ) ;
#6069=CARTESIAN_POINT ( 'NONE',  ( 0.9500414927467377701, 0.1787899950787401604, 0.1131889763241892000 ) ) ;
#6070=EDGE_CURVE ( 'NONE', #1625, #35241, #29694, .T. ) ;
#6071=CARTESIAN_POINT ( 'NONE',  ( 0.7646288533564489232, 0.1113553986120547346, 1.392716535325543292 ) ) ;
#6073=ORIENTED_EDGE ( 'NONE', *, *, #44618, .T. ) ;
#6074=CARTESIAN_POINT ( 'NONE',  ( -0.8759842519685039353, 0.1787899950787401882, 1.724901574749385880 ) ) ;
#6084=AXIS2_PLACEMENT_3D ( 'NONE', #9396, #46266, #20160 ) ;
#6085=CARTESIAN_POINT ( 'NONE',  ( -0.9873396505805591694, -0.1113553986120547346, 0.4281496061916850726 ) ) ;
#6086=( BOUNDED_SURFACE ( )  B_SPLINE_SURFACE ( 1, 2, ( 
 ( #41107, #12158, #39997, #4700, #41341, #33980, #14623, #19331, #26782, #14390, #11042, #6945, #11928, #7422, #1107, #30398, #36666, #29040, #3824, #18444, #10810, #33752, #37791, #34214, #25423, #863, #23174, #19570, #15766, #4943, #1344, #15998, #22930, #47451, #30622, #12408, #29293, #45186, #15523, #26547, #8299, #27029, #17969, #7190, #21567, #36205, #32623, #3357, #43841, #36443, #21815, #3595, #18215, #32857, #30165, #42532, #45656, #31095, #20035, #46377, #19800, #23881, #8781, #34918, #16230, #27966, #35146, #23418, #13338, #24351, #38949, #34676, #12874, #38730, #38020, #9262, #31559, #13557, #9735, #5899, #34432, #41578, #16459, #23641, #30864, #1579, #45426, #2289, #12643, #6114, #27508, #42059, #1823, #27269, #41818, #38493, #38254, #2062, #5416, #20739, #16919, #5662, #35381, #2526, #17152, #20270, #16694, #20511, #31322, #45899, #46141, #13114, #31793, #27747, #42312, #9504, #24126, #14035, #39179, #24813, #20967, #3483, #6594, #9970, #46844, #7318, #42751, #2756, #2988, #3231, #3717, #28681, #25297, #32017, #10691, #39886, #39412, #7071, #17862, #21698, #25550, #43249, #36074, #13788, #36331, #32503, #18098, #40122, #32742, #18338, #10450, #21207, #25050, #102, #28435, #35839, #47338, #14510, #42999, #29174, #39644, #28193, #14280, #43726, #10210, #10929, #21937, #36557, #17620, #24582, #6352, #35613, #32265, #17379, #47086, #6825, #21445, #28920, #43484, #26008, #33930, #40587, #37022, #19980, #31501, #27920, #19748, #16411, #35092, #13287, #31268, #24072, #2240, #42483, #16638, #41766, #9687, #6063, #8968, #46084, #12823, #20216, #38440, #5848, #12347, #1522, #38681, #45376, #45847, #20689, #12592, #27215, #2011, #16175, #30808, #20457, #31037, #5123, #26967, #1290, #15945, #24300, #34383, #42000, #34864, #38902, #30570, #34620, #45131, #23587, #38199, #13054, #5361, #1770, #45604, #27456, #41522, #8726, #23362, #9204, #37970, #23823, #5608, #27691, #42255, #9456, #28378, #6298, #21153, #7016, #31737, #20921, #42700, #10397, #39596, #3428, #24763, #39361, #3178, #9919, #17566, #2706, #17807, #47035, #28867, #32456, #14225, #32204, #43425, #6541, #25001, #31968, #35563, #2929, #17334, #10634, #25239, #46791, #46326, #39826, #46553, #36276, #2469, #42945, #13978, #2384, #12967, #34782, #38346, #20839, #2618, #30717, #1923, #45758, #42158, #27128, #35249, #12505, #17020, #31423, #35478, #16555, #20604, #9366, #46230, #24225, #23989, #35009, #13434, #45289, #23518, #31184, #41678, #8883, #38588, #31657, #5764, #38121, #16330, #20369, #19897, #5984, #28064, #45519, #42627, #2157, #9836, #12741, #16784, #34527, #24444, #46000, #39044, #1684, #13208, #27842, #27372, #42403, #6210, #41914, #9125, #43579, #25147, #39980, #3091, #3343, #10307, #21069, #46945, #35706, #18198, #7173, #28780, #46468, #43820, #46700, #36186, #14603, #25638, #6925, #36422, #14136, #21303, #24920, #22020, #36646, #13652, #35931, #43346, #10549, #28289, #21797, #42852, #3580, #17948, #10061, #39512, #32838, #39737, #47432, #10793, #21548, #32606, #40214, #39277, #28533, #17716, #6686, #47194, #14375, #29021, #25403, #11254, #36880, #29967, #196, #26589, #44750, #18653, #22969, #33544, #19364, #33312, #37105, #40446, #30430, #659, #34019, #44055, #15313, #436, #33788, #23215, #15088, #29735, #4485, #4034, #44276, #8342, #18889, #7632, #14844, #8577, #3806, #1144, #22248, #44514, #22730, #41143, #18423, #22487, #37577, #11480, #26102, #904, #40674, #7871, #11731, #4254, #33071, #29509, #4738, #26350, #15802, #44982, #40910, #25864, #8108, #37336, #19124, #15566, #30205, #12194, #11968, #26820, #41377, #38531, #34953, #28005, #23681, #5460, #2097, #30661, #9062, #16958, #4986, #12443, #12682, #12915, #13376, #38291, #16727, #41614, #20313, #31363, #34469, #45943, #27545, #13154, #2331, #20076, #45695, #23455, #27787, #42097, #42348, #31598, #9544, #42570, #34722, #1619, #1861, #9779, #8820, #16269, #24166, #38768, #38058, #5929, #16499, #37829, #23923, #20546, #5213, #46179, #19606, #34247, #45458, #1376, #16033, #45221, #41858, #27065, #9302, #31129, #19841, #30901, #5700, #27308, #39457, #6633, #28229, #21252, #7116, #3526, #42792, #35877, #10737, #36371, #6868, #47136, #25345, #18139, #39681, #17422, #32783, #29219, #32059, #21739, #3030, #43293, #14076, #28966, #35421, #24621, #14321, #21489, #2558, #24389, #46647, #6397, #46413, #31826, #13592, #32548, #10008, #39929, #28475, #17661, #2793, #38988, #39221, #46888, #6156, #28724, #21008, #47377, #17900, #35655, #43523, #14549, #10493, #25091, #36121, #3276, #40160, #26050, #845, #30381, #26529, #140, #7581, #7359, #15037, #44228, #21971, #22194, #3753, #33735, #36830, #36596, #44001, #8050, #44689, #37279, #18599, #22678, #15505, #18376, #29686, #10969, #607, #40623, #40855, #11906, #7817, #33018, #22433, #37053, #14793, #4206, #41089, #37526, #29454, #18836, #8286, #22912, #4434, #4682, #19312, #1088, #26298, #3981, #15747, #25587, #33261, #11203, #33491, #29911, #15264, #25816, #40392, #385, #11674, #19066, #29151, #37470, #41810, #12633, #41565, #15988, #8771, #1332, #30611, #45176, #38244, #9010, #1814, #12396, #12864, #27499, #23870, #38481, #5652, #20262, #2051, #20730, #25285, #36318, #3473, #46598, #24803, #3218, #35371, #21196, #43471, #25542, #21688, #42743, #2741, #2513, #10196, #39401, #17139, #17369, #46366, #28908, #32005, #31783, #6583, #32731, #13546, #28182, #28422, #28669, #29158, #35829, #17848, #9958, #36062, #32494, #13777, #47076, #43236, #14269, #18085, #2976, #14022, #39170, #10678, #10439, #39874, #47324, #7061, #43715, #17609, #42989, #32255, #10919, #24570, #46833, #14497, #6104, #6342, #20956, #25038, #35602, #39632, #6815, #21434, #11770, #26389, #44321, #25678, #4294, #26143, #25442, #21588, #11291, #32875, #29313, #7211, #3844, #699, #3380, #40015, #47228, #7671, #4076, #44552, #40253, #22059, #18690, #14412, #14884, #3614, #33349, #40714, #22528, #15127, #472, #29544, #29772, #7441, #40486, #17860, #43618, #36684, #10826, #7913, #11524, #18465, #17988, #18926, #21833, #25903, #33586, #15357, #44096, #37145, #33115, #11061, #14642, #6966, #32642, #29062, #240, #22287, #36923, #36458, #30007, #18232, #43860, #41660, #31169, #34059, #30940, #19648, #9106, #34511, #8621, #45267, #23726, #45742, #33825, #12239, #8143, #12951, #1187, #45500, #26863 ),
 ( #12006, #4781, #38101, #23498, #44791, #27354, #41423, #40949, #27113, #12725, #26626, #5263, #41897, #19882, #15846, #1664, #38331, #945, #45024, #4530, #30702, #23258, #16311, #15604, #8866, #5503, #19168, #37873, #34293, #20116, #30241, #1418, #37623, #34763, #1906, #16542, #41179, #8381, #16077, #23011, #12488, #19407, #30469, #35231, #28271, #42834, #24899, #5740, #2827, #3008, #33241, #25071, #7341, #18582, #366, #10949, #40373, #3507, #25320, #28945, #26028, #40603, #21230, #39907, #36352, #32763, #17642, #25799, #32288, #7560, #21954, #46867, #14301, #11188, #47360, #36809, #14772, #29198, #25569, #3965, #14053, #43272, #7095, #10474, #39662, #43506, #22173, #21721, #6846, #3255, #43748, #17879, #43983, #15020, #32523, #29672, #3737, #44210, #10714, #18357, #33000, #45150, #26510, #34179, #33473, #41071, #8029, #44912, #23382, #22661, #19048, #15728, #26278, #11656, #37752, #11887, #44437, #18817, #8743, #7799, #30587, #40838, #37508, #1069, #4907, #22415, #44671, #19528, #33716, #823, #26745, #15487, #30130, #8268, #22895, #37039, #4189, #26991, #4664, #591, #41540, #19291, #15248, #41304, #33948, #30366, #12124, #23136, #29893, #32443, #21631, #36265, #18269, #11559, #40751, #33156, #22566, #17796, #47021, #18499, #10865, #28856, #43416, #25485, #39815, #14681, #36717, #40287, #7004, #3416, #18032, #32678, #277, #47265, #29100, #40051, #7251, #21873, #3649, #32912, #32, #43897, #11095, #25718, #7472, #3880, #14922, #29587, #44128, #26432, #5066, #33869, #12761, #34549, #40997, #30972, #38369, #20155, #34100, #30504, #1700, #8183, #1457, #27391, #37420, #34802, #988, #8420, #19210, #15880, #30739, #30283, #37668, #44834, #1948, #1226, #26667, #45308, #16578, #41217, #12529, #41704, #20859, #21331, #31679, #42878, #2177, #10089, #24700, #9626, #39301, #35502, #6476, #43131, #46259, #6234, #31439, #21096, #2642, #35734, #10335, #2872, #35962, #13456, #24243, #28084, #3120, #16800, #38840, #17507, #32138, #46021, #46732, #42646, #17747, #31911, #13916, #13230, #28562, #24947, #39543, #6005, #6716, #45780, #5784, #2408, #12989, #17276, #9858, #27629, #42182, #24469, #38607, #39065, #46494, #27862, #13673, #24007, #20389, #35029, #20626, #35272, #7660, #18681, #44311, #227, #25433, #11513, #37135, #40008, #29763, #43851, #3835, #22051, #36913, #43371, #32633, #22277, #29535, #10583, #32394, #7202, #14403, #6957, #28810, #39766, #40476, #25181, #33340, #36452, #21824, #10820, #4285, #21577, #14634, #46972, #25670, #36218, #464, #25894, #14165, #4066, #15117, #26136, #3607, #18227, #44086, #3371, #42310, #40704, #17980, #7903, #47221, #29052, #43610, #32867, #29303, #11054, #40245, #7432, #22519, #36676, #18457, #33105, #14875, #11284, #40940, #41171, #37864, #9095, #15836, #27102, #4519, #27344, #33576, #23000, #29999, #5018, #44543, #19155, #45016, #34281, #935, #12229, #20525, #42548, #24594, #2540, #2771, #27763, #9276, #45913, #17395, #31105, #23896, #9751, #24365, #45668, #46392, #42324, #32034, #46156, #31807, #12886, #38963, #13569, #6128, #20282, #20752, #28205, #20049, #9518, #12656, #2304, #24142, #35395, #42768, #38746, #5431, #5910, #35160, #27519, #16932, #39192, #6367, #42073, #13351, #35629, #27283, #38504, #5675, #27979, #34928, #2076, #41831, #9034, #23656, #38266, #34691, #1834, #14765, #17637, #39902, #18115, #36572, #3958, #17875, #3731, #14048, #28696, #29194, #43264, #46861, #43500, #10468, #18580, #46624, #18351, #32519, #43978, #32995, #25065, #13808, #32758, #39657, #21461, #6840, #10710, #40367, #43017, #36092, #39432, #47355, #43741, #36805, #47105, #14295, #10946, #6611, #7090, #3249, #25565, #118, #29435, #7334, #40137, #21715, #21950, #28939, #14528, #25315, #3003, #36347, #11182, #25795, #7556, #22166, #10224, #24830, #21225, #4662, #30582, #45146, #22891, #4904, #15483, #37262, #40836, #23378, #5139, #33238, #4415, #821, #44667, #29668, #37746, #15015, #19525, #33943, #37985, #26273, #23132, #11883, #1307, #26742, #30127, #37504, #15962, #365, #26024, #19045, #44207, #11406, #8028, #34174, #33712, #40599, #18812, #41068, #7793, #8502, #41301, #589, #12366, #8266, #26984, #29890, #1066, #22410, #41535, #15724, #8742, #37036, #30360, #44435, #4185, #11650, #44908, #12121, #22657, #6724, #39073, #10591, #6484, #10344, #5375, #17514, #21340, #46740, #42654, #32149, #24953, #27228, #24481, #19765, #10099, #20869, #2878, #43138, #6245, #12607, #35513, #2651, #23603, #17284, #3127, #46980, #38215, #46501, #35971, #32404, #13927, #39551, #17758, #14173, #35742, #13463, #28818, #25188, #9868, #43381, #28321, #39310, #24709, #39775, #30822, #19996, #34398, #28571, #45392, #1538, #42888, #2417, #41781, #16191, #8982, #35280, #17047, #31688, #21104, #46268, #14883, #41178, #14641, #18689, #3613, #29771, #11060, #22766, #30006, #18231, #8142, #19167, #33824, #29543, #7670, #33585, #32874, #4075, #26388, #8380, #4529, #25677, #33114, #18603, #40485, #22286, #29312, #239, #43859, #11769, #44095, #40252, #36922, #15603, #7440, #22058, #11290, #11523, #12005, #33348, #698, #36683, #18925, #15356, #25902, #44551, #26142, #40948, #944, #471, #44320, #3843, #37373, #40713, #30240, #44790, #26625, #36457, #15126, #7912, #22527, #18464, #37144, #4293, #42138, #5739, #20356, #16076, #41659, #20115, #4780, #38100, #12950, #42385, #38572, #12238, #19647, #19406, #27112, #8865, #34058, #34292, #15845, #45741, #1417, #1186, #23497, #2138, #37622, #45023, #45266, #45499, #45980, #5262, #34762, #26862, #5502, #1905, #30701, #16541, #12724, #31168, #34993, #19881, #30939, #8620, #27589, #27353, #9348, #16765, #23968, #13189, #34510, #12487, #1663, #27825, #41422, #16310, #31405, #23010, #23257, #30468, #41896, #37872, #9105, #5026, #23725, #38330, #43329, #35911, #17233, #6669, #14116, #16999, #13631, #9584, #46682, #10046, #39495, #32346, #28270, #2363, #24663, #42833, #13415, #39258, #39718, #36163, #28047, #6433, #10530, #21525, #21286, #46927, #25127, #3317, #24898, #2600, #17930, #14355, #31869, #6903, #21049, #28513, #13871, #28759, #20584, #9821, #32585, #3068, #35230, #24203, #46449, #39027, #31639, #5965, #46215, #17698, #42607, #47171, #35691, #2826, #35458, #29002, #24426, #17460, #38806, #32093, #6195, #20819, #43086, #10289, #638, #7151, #43800, #33522, #40652, #21774, #43560, #18405 ) ),
 .UNSPECIFIED., .F., .F., .T. ) 
 B_SPLINE_SURFACE_WITH_KNOTS ( ( 2, 2 ),
 ( 3, 2, 2, 2, 2, 2, 2, 2, 2, 2, 2, 2, 2, 2, 2, 2, 2, 2, 2, 2, 2, 2, 2, 2, 2, 2, 2, 2, 2, 2, 2, 2, 2, 2, 2, 2, 2, 2, 2, 2, 2, 2, 2, 2, 2, 2, 2, 2, 2, 2, 2, 2, 2, 2, 2, 2, 2, 2, 2, 2, 2, 2, 2, 2, 2, 2, 2, 2, 2, 2, 2, 2, 2, 2, 2, 2, 2, 2, 2, 2, 2, 2, 2, 2, 2, 2, 2, 2, 2, 2, 2, 2, 2, 2, 2, 2, 2, 2, 2, 2, 2, 2, 2, 2, 2, 2, 2, 2, 2, 2, 2, 2, 2, 2, 2, 2, 2, 2, 2, 2, 2, 2, 2, 2, 2, 2, 2, 2, 2, 2, 2, 2, 2, 2, 2, 2, 2, 2, 2, 2, 2, 2, 2, 2, 2, 2, 2, 2, 2, 2, 2, 2, 2, 2, 2, 2, 2, 2, 2, 2, 2, 2, 2, 2, 2, 2, 2, 2, 2, 2, 2, 2, 2, 2, 2, 2, 2, 2, 2, 2, 2, 2, 2, 2, 2, 2, 2, 2, 2, 2, 2, 2, 2, 2, 2, 2, 2, 2, 2, 2, 2, 2, 2, 2, 2, 2, 2, 2, 2, 2, 2, 2, 2, 2, 2, 2, 2, 2, 2, 2, 2, 2, 2, 2, 2, 2, 2, 2, 2, 2, 2, 2, 2, 2, 2, 2, 2, 2, 2, 2, 2, 2, 2, 2, 2, 2, 2, 2, 2, 2, 2, 2, 2, 2, 2, 2, 2, 2, 2, 2, 2, 2, 2, 2, 2, 2, 2, 2, 2, 2, 2, 2, 2, 2, 2, 2, 2, 2, 2, 2, 2, 2, 2, 2, 2, 2, 2, 2, 2, 2, 2, 2, 2, 2, 2, 2, 2, 2, 2, 2, 2, 2, 2, 2, 2, 2, 2, 2, 2, 2, 2, 2, 2, 2, 2, 2, 2, 2, 2, 2, 2, 2, 2, 2, 2, 2, 2, 2, 2, 2, 2, 2, 2, 2, 2, 2, 2, 2, 2, 2, 2, 2, 2, 2, 2, 2, 2, 2, 2, 2, 2, 2, 2, 2, 2, 2, 2, 2, 2, 2, 2, 2, 2, 2, 2, 2, 2, 2, 2, 2, 2, 2, 2, 2, 2, 2, 2, 2, 2, 2, 2, 2, 2, 2, 2, 2, 2, 2, 2, 2, 2, 2, 2, 2, 2, 2, 2, 2, 2, 2, 3 ),
 ( 0.000000000000000000, 1.000000000000000000 ),
 ( 0.000000000000000000, 0.002500000000000000052, 0.005000000000000000104, 0.007499999999999999722, 0.01000000000000000021, 0.01250000000000000069, 0.01499999999999999944, 0.01750000000000000167, 0.02000000000000000042, 0.02249999999999999917, 0.02500000000000000139, 0.02750000000000000014, 0.02999999999999999889, 0.03250000000000000111, 0.03500000000000000333, 0.03749999999999999861, 0.04000000000000000083, 0.04250000000000000305, 0.04499999999999999833, 0.04750000000000000056, 0.05000000000000000278, 0.05249999999999999806, 0.05500000000000000028, 0.05750000000000000250, 0.05999999999999999778, 0.06250000000000000000, 0.06500000000000000222, 0.06750000000000000444, 0.07000000000000000666, 0.07249999999999999500, 0.07499999999999999722, 0.07749999999999999944, 0.08000000000000000167, 0.08250000000000000389, 0.08500000000000000611, 0.08749999999999999445, 0.08999999999999999667, 0.09249999999999999889, 0.09500000000000000111, 0.09750000000000000333, 0.1000000000000000056, 0.1024999999999999939, 0.1049999999999999961, 0.1074999999999999983, 0.1100000000000000006, 0.1125000000000000028, 0.1150000000000000050, 0.1174999999999999933, 0.1199999999999999956, 0.1224999999999999978, 0.1250000000000000000, 0.1275000000000000022, 0.1300000000000000044, 0.1325000000000000067, 0.1350000000000000089, 0.1375000000000000111, 0.1400000000000000133, 0.1424999999999999878, 0.1449999999999999900, 0.1474999999999999922, 0.1499999999999999944, 0.1524999999999999967, 0.1549999999999999989, 0.1575000000000000011, 0.1600000000000000033, 0.1625000000000000056, 0.1650000000000000078, 0.1675000000000000100, 0.1700000000000000122, 0.1724999999999999867, 0.1749999999999999889, 0.1774999999999999911, 0.1799999999999999933, 0.1824999999999999956, 0.1849999999999999978, 0.1875000000000000000, 0.1900000000000000022, 0.1925000000000000044, 0.1950000000000000067, 0.1975000000000000089, 0.2000000000000000111, 0.2025000000000000133, 0.2049999999999999878, 0.2074999999999999900, 0.2099999999999999922, 0.2124999999999999944, 0.2149999999999999967, 0.2174999999999999989, 0.2200000000000000011, 0.2225000000000000033, 0.2250000000000000056, 0.2275000000000000078, 0.2300000000000000100, 0.2325000000000000122, 0.2349999999999999867, 0.2374999999999999889, 0.2399999999999999911, 0.2424999999999999933, 0.2449999999999999956, 0.2474999999999999978, 0.2500000000000000000, 0.2525000000000000022, 0.2550000000000000044, 0.2575000000000000067, 0.2600000000000000089, 0.2625000000000000111, 0.2650000000000000133, 0.2675000000000000155, 0.2700000000000000178, 0.2725000000000000200, 0.2750000000000000222, 0.2775000000000000244, 0.2800000000000000266, 0.2824999999999999734, 0.2849999999999999756, 0.2874999999999999778, 0.2899999999999999800, 0.2924999999999999822, 0.2949999999999999845, 0.2974999999999999867, 0.2999999999999999889, 0.3024999999999999911, 0.3049999999999999933, 0.3074999999999999956, 0.3099999999999999978, 0.3125000000000000000, 0.3150000000000000022, 0.3175000000000000044, 0.3200000000000000067, 0.3225000000000000089, 0.3250000000000000111, 0.3275000000000000133, 0.3300000000000000155, 0.3325000000000000178, 0.3350000000000000200, 0.3375000000000000222, 0.3400000000000000244, 0.3425000000000000266, 0.3449999999999999734, 0.3474999999999999756, 0.3499999999999999778, 0.3524999999999999800, 0.3549999999999999822, 0.3574999999999999845, 0.3599999999999999867, 0.3624999999999999889, 0.3649999999999999911, 0.3674999999999999933, 0.3699999999999999956, 0.3724999999999999978, 0.3750000000000000000, 0.3775000000000000022, 0.3800000000000000044, 0.3825000000000000067, 0.3850000000000000089, 0.3875000000000000111, 0.3900000000000000133, 0.3925000000000000155, 0.3950000000000000178, 0.3975000000000000200, 0.4000000000000000222, 0.4025000000000000244, 0.4050000000000000266, 0.4074999999999999734, 0.4099999999999999756, 0.4124999999999999778, 0.4149999999999999800, 0.4174999999999999822, 0.4199999999999999845, 0.4224999999999999867, 0.4249999999999999889, 0.4274999999999999911, 0.4299999999999999933, 0.4324999999999999956, 0.4349999999999999978, 0.4375000000000000000, 0.4400000000000000022, 0.4425000000000000044, 0.4450000000000000067, 0.4475000000000000089, 0.4500000000000000111, 0.4525000000000000133, 0.4550000000000000155, 0.4575000000000000178, 0.4600000000000000200, 0.4625000000000000222, 0.4650000000000000244, 0.4675000000000000266, 0.4699999999999999734, 0.4724999999999999756, 0.4749999999999999778, 0.4774999999999999800, 0.4799999999999999822, 0.4824999999999999845, 0.4849999999999999867, 0.4874999999999999889, 0.4899999999999999911, 0.4924999999999999933, 0.4949999999999999956, 0.4974999999999999978, 0.5000000000000000000, 0.5024999999999999467, 0.5050000000000000044, 0.5074999999999999512, 0.5100000000000000089, 0.5124999999999999556, 0.5150000000000000133, 0.5174999999999999600, 0.5200000000000000178, 0.5224999999999999645, 0.5250000000000000222, 0.5274999999999999689, 0.5300000000000000266, 0.5324999999999999734, 0.5350000000000000311, 0.5374999999999999778, 0.5400000000000000355, 0.5424999999999999822, 0.5450000000000000400, 0.5474999999999999867, 0.5500000000000000444, 0.5524999999999999911, 0.5550000000000000488, 0.5574999999999999956, 0.5600000000000000533, 0.5625000000000000000, 0.5649999999999999467, 0.5675000000000000044, 0.5699999999999999512, 0.5725000000000000089, 0.5749999999999999556, 0.5775000000000000133, 0.5799999999999999600, 0.5825000000000000178, 0.5849999999999999645, 0.5875000000000000222, 0.5899999999999999689, 0.5925000000000000266, 0.5949999999999999734, 0.5975000000000000311, 0.5999999999999999778, 0.6025000000000000355, 0.6049999999999999822, 0.6075000000000000400, 0.6099999999999999867, 0.6125000000000000444, 0.6149999999999999911, 0.6175000000000000488, 0.6199999999999999956, 0.6225000000000000533, 0.6250000000000000000, 0.6274999999999999467, 0.6300000000000000044, 0.6324999999999999512, 0.6350000000000000089, 0.6374999999999999556, 0.6400000000000000133, 0.6424999999999999600, 0.6450000000000000178, 0.6474999999999999645, 0.6500000000000000222, 0.6524999999999999689, 0.6550000000000000266, 0.6574999999999999734, 0.6600000000000000311, 0.6624999999999999778, 0.6650000000000000355, 0.6674999999999999822, 0.6700000000000000400, 0.6724999999999999867, 0.6750000000000000444, 0.6774999999999999911, 0.6800000000000000488, 0.6824999999999999956, 0.6850000000000000533, 0.6875000000000000000, 0.6899999999999999467, 0.6925000000000000044, 0.6949999999999999512, 0.6975000000000000089, 0.6999999999999999556, 0.7025000000000000133, 0.7049999999999999600, 0.7075000000000000178, 0.7099999999999999645, 0.7125000000000000222, 0.7149999999999999689, 0.7175000000000000266, 0.7199999999999999734, 0.7225000000000000311, 0.7249999999999999778, 0.7275000000000000355, 0.7299999999999999822, 0.7325000000000000400, 0.7349999999999999867, 0.7375000000000000444, 0.7399999999999999911, 0.7425000000000000488, 0.7449999999999999956, 0.7475000000000000533, 0.7500000000000000000, 0.7524999999999999467, 0.7550000000000000044, 0.7574999999999999512, 0.7600000000000000089, 0.7624999999999999556, 0.7650000000000000133, 0.7674999999999999600, 0.7700000000000000178, 0.7724999999999999645, 0.7750000000000000222, 0.7774999999999999689, 0.7800000000000000266, 0.7824999999999999734, 0.7850000000000000311, 0.7874999999999999778, 0.7900000000000000355, 0.7924999999999999822, 0.7950000000000000400, 0.7974999999999999867, 0.8000000000000000444, 0.8024999999999999911, 0.8050000000000000488, 0.8074999999999999956, 0.8100000000000000533, 0.8125000000000000000, 0.8149999999999999467, 0.8175000000000000044, 0.8199999999999999512, 0.8225000000000000089, 0.8249999999999999556, 0.8275000000000000133, 0.8299999999999999600, 0.8325000000000000178, 0.8349999999999999645, 0.8375000000000000222, 0.8399999999999999689, 0.8425000000000000266, 0.8449999999999999734, 0.8475000000000000311, 0.8499999999999999778, 0.8525000000000000355, 0.8549999999999999822, 0.8575000000000000400, 0.8599999999999999867, 0.8625000000000000444, 0.8649999999999999911, 0.8675000000000000488, 0.8699999999999999956, 0.8725000000000000533, 0.8750000000000000000, 0.8774999999999999467, 0.8800000000000000044, 0.8824999999999999512, 0.8850000000000000089, 0.8874999999999999556, 0.8900000000000000133, 0.8924999999999999600, 0.8950000000000000178, 0.8974999999999999645, 0.9000000000000000222, 0.9024999999999999689, 0.9050000000000000266, 0.9074999999999999734, 0.9100000000000000311, 0.9124999999999999778, 0.9150000000000000355, 0.9174999999999999822, 0.9200000000000000400, 0.9224999999999999867, 0.9250000000000000444, 0.9274999999999999911, 0.9300000000000000488, 0.9324999999999999956, 0.9350000000000000533, 0.9375000000000000000, 0.9399999999999999467, 0.9425000000000000044, 0.9449999999999999512, 0.9475000000000000089, 0.9499999999999999556, 0.9525000000000000133, 0.9549999999999999600, 0.9575000000000000178, 0.9599999999999999645, 0.9625000000000000222, 0.9649999999999999689, 0.9675000000000000266, 0.9699999999999999734, 0.9725000000000000311, 0.9749999999999999778, 0.9775000000000000355, 0.9799999999999999822, 0.9825000000000000400, 0.9849999999999999867, 0.9875000000000000444, 0.9899999999999999911, 0.9925000000000000488, 0.9949999999999999956, 0.9975000000000000533, 1.000000000000000000 ),
 .UNSPECIFIED. ) 
 GEOMETRIC_REPRESENTATION_ITEM ( )  RATIONAL_B_SPLINE_SURFACE ( (
 ( 1.000000000000000000, 0.9238795325112869605, 1.000000000000000000, 0.9238795325112869605, 1.000000000000000000, 0.9238795325112869605, 1.000000000000000000, 0.9238795325112869605, 1.000000000000000000, 0.9238795325112869605, 1.000000000000000000, 0.9238795325112869605, 1.000000000000000000, 0.9238795325112869605, 1.000000000000000000, 0.9238795325112869605, 1.000000000000000000, 0.9238795325112869605, 1.000000000000000000, 0.9238795325112869605, 1.000000000000000000, 0.9238795325112869605, 1.000000000000000000, 0.9238795325112869605, 1.000000000000000000, 0.9238795325112869605, 1.000000000000000000, 0.9238795325112869605, 1.000000000000000000, 0.9238795325112869605, 1.000000000000000000, 0.9238795325112869605, 1.000000000000000000, 0.9238795325112869605, 1.000000000000000000, 0.9238795325112869605, 1.000000000000000000, 0.9238795325112869605, 1.000000000000000000, 0.9238795325112869605, 1.000000000000000000, 0.9238795325112869605, 1.000000000000000000, 0.9238795325112869605, 1.000000000000000000, 0.9238795325112869605, 1.000000000000000000, 0.9238795325112869605, 1.000000000000000000, 0.9238795325112869605, 1.000000000000000000, 0.9238795325112869605, 1.000000000000000000, 0.9238795325112869605, 1.000000000000000000, 0.9238795325112869605, 1.000000000000000000, 0.9238795325112869605, 1.000000000000000000, 0.9238795325112869605, 1.000000000000000000, 0.9238795325112869605, 1.000000000000000000, 0.9238795325112869605, 1.000000000000000000, 0.9238795325112869605, 1.000000000000000000, 0.9238795325112869605, 1.000000000000000000, 0.9238795325112869605, 1.000000000000000000, 0.9238795325112869605, 1.000000000000000000, 0.9238795325112869605, 1.000000000000000000, 0.9238795325112869605, 1.000000000000000000, 0.9238795325112869605, 1.000000000000000000, 0.9238795325112869605, 1.000000000000000000, 0.9238795325112869605, 1.000000000000000000, 0.9238795325112869605, 1.000000000000000000, 0.9238795325112869605, 1.000000000000000000, 0.9238795325112869605, 1.000000000000000000, 0.9238795325112869605, 1.000000000000000000, 0.9238795325112869605, 1.000000000000000000, 0.9238795325112869605, 1.000000000000000000, 0.9238795325112869605, 1.000000000000000000, 0.9238795325112869605, 1.000000000000000000, 0.9238795325112869605, 1.000000000000000000, 0.9238795325112869605, 1.000000000000000000, 0.9238795325112869605, 1.000000000000000000, 0.9238795325112869605, 1.000000000000000000, 0.9238795325112869605, 1.000000000000000000, 0.9238795325112869605, 1.000000000000000000, 0.9238795325112869605, 1.000000000000000000, 0.9238795325112869605, 1.000000000000000000, 0.9238795325112869605, 1.000000000000000000, 0.9238795325112869605, 1.000000000000000000, 0.9238795325112869605, 1.000000000000000000, 0.9238795325112869605, 1.000000000000000000, 0.9238795325112869605, 1.000000000000000000, 0.9238795325112869605, 1.000000000000000000, 0.9238795325112869605, 1.000000000000000000, 0.9238795325112869605, 1.000000000000000000, 0.9238795325112869605, 1.000000000000000000, 0.9238795325112869605, 1.000000000000000000, 0.9238795325112869605, 1.000000000000000000, 0.9238795325112869605, 1.000000000000000000, 0.9238795325112869605, 1.000000000000000000, 0.9238795325112869605, 1.000000000000000000, 0.9238795325112869605, 1.000000000000000000, 0.9238795325112869605, 1.000000000000000000, 0.9238795325112869605, 1.000000000000000000, 0.9238795325112869605, 1.000000000000000000, 0.9238795325112869605, 1.000000000000000000, 0.9238795325112869605, 1.000000000000000000, 0.9238795325112869605, 1.000000000000000000, 0.9238795325112869605, 1.000000000000000000, 0.9238795325112869605, 1.000000000000000000, 0.9238795325112869605, 1.000000000000000000, 0.9238795325112869605, 1.000000000000000000, 0.9238795325112869605, 1.000000000000000000, 0.9238795325112869605, 1.000000000000000000, 0.9238795325112869605, 1.000000000000000000, 0.9238795325112869605, 1.000000000000000000, 0.9238795325112869605, 1.000000000000000000, 0.9238795325112869605, 1.000000000000000000, 0.9238795325112869605, 1.000000000000000000, 0.9238795325112869605, 1.000000000000000000, 0.9238795325112869605, 1.000000000000000000, 0.9238795325112869605, 1.000000000000000000, 0.9238795325112869605, 1.000000000000000000, 0.9238795325112869605, 1.000000000000000000, 0.9238795325112869605, 1.000000000000000000, 0.9238795325112869605, 1.000000000000000000, 0.9238795325112869605, 1.000000000000000000, 0.9238795325112869605, 1.000000000000000000, 0.9238795325112869605, 1.000000000000000000, 0.9238795325112869605, 1.000000000000000000, 0.9238795325112869605, 1.000000000000000000, 0.9238795325112869605, 1.000000000000000000, 0.9238795325112869605, 1.000000000000000000, 0.9238795325112869605, 1.000000000000000000, 0.9238795325112869605, 1.000000000000000000, 0.9238795325112869605, 1.000000000000000000, 0.9238795325112869605, 1.000000000000000000, 0.9238795325112869605, 1.000000000000000000, 0.9238795325112869605, 1.000000000000000000, 0.9238795325112869605, 1.000000000000000000, 0.9238795325112869605, 1.000000000000000000, 0.9238795325112869605, 1.000000000000000000, 0.9238795325112869605, 1.000000000000000000, 0.9238795325112869605, 1.000000000000000000, 0.9238795325112869605, 1.000000000000000000, 0.9238795325112869605, 1.000000000000000000, 0.9238795325112869605, 1.000000000000000000, 0.9238795325112869605, 1.000000000000000000, 0.9238795325112869605, 1.000000000000000000, 0.9238795325112869605, 1.000000000000000000, 0.9238795325112869605, 1.000000000000000000, 0.9238795325112869605, 1.000000000000000000, 0.9238795325112869605, 1.000000000000000000, 0.9238795325112869605, 1.000000000000000000, 0.9238795325112869605, 1.000000000000000000, 0.9238795325112869605, 1.000000000000000000, 0.9238795325112869605, 1.000000000000000000, 0.9238795325112869605, 1.000000000000000000, 0.9238795325112869605, 1.000000000000000000, 0.9238795325112869605, 1.000000000000000000, 0.9238795325112869605, 1.000000000000000000, 0.9238795325112869605, 1.000000000000000000, 0.9238795325112869605, 1.000000000000000000, 0.9238795325112869605, 1.000000000000000000, 0.9238795325112869605, 1.000000000000000000, 0.9238795325112869605, 1.000000000000000000, 0.9238795325112869605, 1.000000000000000000, 0.9238795325112869605, 1.000000000000000000, 0.9238795325112869605, 1.000000000000000000, 0.9238795325112869605, 1.000000000000000000, 0.9238795325112869605, 1.000000000000000000, 0.9238795325112869605, 1.000000000000000000, 0.9238795325112869605, 1.000000000000000000, 0.9238795325112869605, 1.000000000000000000, 0.9238795325112869605, 1.000000000000000000, 0.9238795325112869605, 1.000000000000000000, 0.9238795325112869605, 1.000000000000000000, 0.9238795325112869605, 1.000000000000000000, 0.9238795325112869605, 1.000000000000000000, 0.9238795325112869605, 1.000000000000000000, 0.9238795325112869605, 1.000000000000000000, 0.9238795325112869605, 1.000000000000000000, 0.9238795325112869605, 1.000000000000000000, 0.9238795325112869605, 1.000000000000000000, 0.9238795325112869605, 1.000000000000000000, 0.9238795325112869605, 1.000000000000000000, 0.9238795325112869605, 1.000000000000000000, 0.9238795325112869605, 1.000000000000000000, 0.9238795325112869605, 1.000000000000000000, 0.9238795325112869605, 1.000000000000000000, 0.9238795325112869605, 1.000000000000000000, 0.9238795325112869605, 1.000000000000000000, 0.9238795325112869605, 1.000000000000000000, 0.9238795325112869605, 1.000000000000000000, 0.9238795325112869605, 1.000000000000000000, 0.9238795325112869605, 1.000000000000000000, 0.9238795325112869605, 1.000000000000000000, 0.9238795325112869605, 1.000000000000000000, 0.9238795325112869605, 1.000000000000000000, 0.9238795325112869605, 1.000000000000000000, 0.9238795325112869605, 1.000000000000000000, 0.9238795325112869605, 1.000000000000000000, 0.9238795325112869605, 1.000000000000000000, 0.9238795325112869605, 1.000000000000000000, 0.9238795325112869605, 1.000000000000000000, 0.9238795325112869605, 1.000000000000000000, 0.9238795325112869605, 1.000000000000000000, 0.9238795325112869605, 1.000000000000000000, 0.9238795325112869605, 1.000000000000000000, 0.9238795325112869605, 1.000000000000000000, 0.9238795325112869605, 1.000000000000000000, 0.9238795325112869605, 1.000000000000000000, 0.9238795325112869605, 1.000000000000000000, 0.9238795325112869605, 1.000000000000000000, 0.9238795325112869605, 1.000000000000000000, 0.9238795325112869605, 1.000000000000000000, 0.9238795325112869605, 1.000000000000000000, 0.9238795325112869605, 1.000000000000000000, 0.9238795325112869605, 1.000000000000000000, 0.9238795325112869605, 1.000000000000000000, 0.9238795325112869605, 1.000000000000000000, 0.9238795325112869605, 1.000000000000000000, 0.9238795325112869605, 1.000000000000000000, 0.9238795325112869605, 1.000000000000000000, 0.9238795325112869605, 1.000000000000000000, 0.9238795325112869605, 1.000000000000000000, 0.9238795325112869605, 1.000000000000000000, 0.9238795325112869605, 1.000000000000000000, 0.9238795325112869605, 1.000000000000000000, 0.9238795325112869605, 1.000000000000000000, 0.9238795325112869605, 1.000000000000000000, 0.9238795325112869605, 1.000000000000000000, 0.9238795325112869605, 1.000000000000000000, 0.9238795325112869605, 1.000000000000000000, 0.9238795325112869605, 1.000000000000000000, 0.9238795325112869605, 1.000000000000000000, 0.9238795325112869605, 1.000000000000000000, 0.9238795325112869605, 1.000000000000000000, 0.9238795325112869605, 1.000000000000000000, 0.9238795325112869605, 1.000000000000000000, 0.9238795325112869605, 1.000000000000000000, 0.9238795325112869605, 1.000000000000000000, 0.9238795325112869605, 1.000000000000000000, 0.9238795325112869605, 1.000000000000000000, 0.9238795325112869605, 1.000000000000000000, 0.9238795325112869605, 1.000000000000000000, 0.9238795325112869605, 1.000000000000000000, 0.9238795325112869605, 1.000000000000000000, 0.9238795325112869605, 1.000000000000000000, 0.9238795325112869605, 1.000000000000000000, 0.9238795325112869605, 1.000000000000000000, 0.9238795325112869605, 1.000000000000000000, 0.9238795325112869605, 1.000000000000000000, 0.9238795325112869605, 1.000000000000000000, 0.9238795325112869605, 1.000000000000000000, 0.9238795325112869605, 1.000000000000000000, 0.9238795325112869605, 1.000000000000000000, 0.9238795325112869605, 1.000000000000000000, 0.9238795325112869605, 1.000000000000000000, 0.9238795325112869605, 1.000000000000000000, 0.9238795325112869605, 1.000000000000000000, 0.9238795325112869605, 1.000000000000000000, 0.9238795325112869605, 1.000000000000000000, 0.9238795325112869605, 1.000000000000000000, 0.9238795325112869605, 1.000000000000000000, 0.9238795325112869605, 1.000000000000000000, 0.9238795325112869605, 1.000000000000000000, 0.9238795325112869605, 1.000000000000000000, 0.9238795325112869605, 1.000000000000000000, 0.9238795325112869605, 1.000000000000000000, 0.9238795325112869605, 1.000000000000000000, 0.9238795325112869605, 1.000000000000000000, 0.9238795325112869605, 1.000000000000000000, 0.9238795325112869605, 1.000000000000000000, 0.9238795325112869605, 1.000000000000000000, 0.9238795325112869605, 1.000000000000000000, 0.9238795325112869605, 1.000000000000000000, 0.9238795325112869605, 1.000000000000000000, 0.9238795325112869605, 1.000000000000000000, 0.9238795325112869605, 1.000000000000000000, 0.9238795325112869605, 1.000000000000000000, 0.9238795325112869605, 1.000000000000000000, 0.9238795325112869605, 1.000000000000000000, 0.9238795325112869605, 1.000000000000000000, 0.9238795325112869605, 1.000000000000000000, 0.9238795325112869605, 1.000000000000000000, 0.9238795325112869605, 1.000000000000000000, 0.9238795325112869605, 1.000000000000000000, 0.9238795325112869605, 1.000000000000000000, 0.9238795325112869605, 1.000000000000000000, 0.9238795325112869605, 1.000000000000000000, 0.9238795325112869605, 1.000000000000000000, 0.9238795325112869605, 1.000000000000000000, 0.9238795325112869605, 1.000000000000000000, 0.9238795325112869605, 1.000000000000000000, 0.9238795325112869605, 1.000000000000000000, 0.9238795325112869605, 1.000000000000000000, 0.9238795325112869605, 1.000000000000000000, 0.9238795325112869605, 1.000000000000000000, 0.9238795325112869605, 1.000000000000000000, 0.9238795325112869605, 1.000000000000000000, 0.9238795325112869605, 1.000000000000000000, 0.9238795325112869605, 1.000000000000000000, 0.9238795325112869605, 1.000000000000000000, 0.9238795325112869605, 1.000000000000000000, 0.9238795325112869605, 1.000000000000000000, 0.9238795325112869605, 1.000000000000000000, 0.9238795325112869605, 1.000000000000000000, 0.9238795325112869605, 1.000000000000000000, 0.9238795325112869605, 1.000000000000000000, 0.9238795325112869605, 1.000000000000000000, 0.9238795325112869605, 1.000000000000000000, 0.9238795325112869605, 1.000000000000000000, 0.9238795325112869605, 1.000000000000000000, 0.9238795325112869605, 1.000000000000000000, 0.9238795325112869605, 1.000000000000000000, 0.9238795325112869605, 1.000000000000000000, 0.9238795325112869605, 1.000000000000000000, 0.9238795325112869605, 1.000000000000000000, 0.9238795325112869605, 1.000000000000000000, 0.9238795325112869605, 1.000000000000000000, 0.9238795325112869605, 1.000000000000000000, 0.9238795325112869605, 1.000000000000000000, 0.9238795325112869605, 1.000000000000000000, 0.9238795325112869605, 1.000000000000000000, 0.9238795325112869605, 1.000000000000000000, 0.9238795325112869605, 1.000000000000000000, 0.9238795325112869605, 1.000000000000000000, 0.9238795325112869605, 1.000000000000000000, 0.9238795325112869605, 1.000000000000000000, 0.9238795325112869605, 1.000000000000000000, 0.9238795325112869605, 1.000000000000000000, 0.9238795325112869605, 1.000000000000000000, 0.9238795325112869605, 1.000000000000000000, 0.9238795325112869605, 1.000000000000000000, 0.9238795325112869605, 1.000000000000000000, 0.9238795325112869605, 1.000000000000000000, 0.9238795325112869605, 1.000000000000000000, 0.9238795325112869605, 1.000000000000000000, 0.9238795325112869605, 1.000000000000000000, 0.9238795325112869605, 1.000000000000000000, 0.9238795325112869605, 1.000000000000000000, 0.9238795325112869605, 1.000000000000000000, 0.9238795325112869605, 1.000000000000000000, 0.9238795325112869605, 1.000000000000000000, 0.9238795325112869605, 1.000000000000000000, 0.9238795325112869605, 1.000000000000000000, 0.9238795325112869605, 1.000000000000000000, 0.9238795325112869605, 1.000000000000000000, 0.9238795325112869605, 1.000000000000000000, 0.9238795325112869605, 1.000000000000000000, 0.9238795325112869605, 1.000000000000000000, 0.9238795325112869605, 1.000000000000000000, 0.9238795325112869605, 1.000000000000000000, 0.9238795325112869605, 1.000000000000000000, 0.9238795325112869605, 1.000000000000000000, 0.9238795325112869605, 1.000000000000000000, 0.9238795325112869605, 1.000000000000000000, 0.9238795325112869605, 1.000000000000000000, 0.9238795325112869605, 1.000000000000000000, 0.9238795325112869605, 1.000000000000000000, 0.9238795325112869605, 1.000000000000000000, 0.9238795325112869605, 1.000000000000000000, 0.9238795325112869605, 1.000000000000000000, 0.9238795325112869605, 1.000000000000000000, 0.9238795325112869605, 1.000000000000000000, 0.9238795325112869605, 1.000000000000000000, 0.9238795325112869605, 1.000000000000000000, 0.9238795325112869605, 1.000000000000000000, 0.9238795325112869605, 1.000000000000000000, 0.9238795325112869605, 1.000000000000000000, 0.9238795325112869605, 1.000000000000000000, 0.9238795325112869605, 1.000000000000000000, 0.9238795325112869605, 1.000000000000000000, 0.9238795325112869605, 1.000000000000000000, 0.9238795325112869605, 1.000000000000000000, 0.9238795325112869605, 1.000000000000000000, 0.9238795325112869605, 1.000000000000000000, 0.9238795325112869605, 1.000000000000000000, 0.9238795325112869605, 1.000000000000000000, 0.9238795325112869605, 1.000000000000000000, 0.9238795325112869605, 1.000000000000000000, 0.9238795325112869605, 1.000000000000000000, 0.9238795325112869605, 1.000000000000000000, 0.9238795325112869605, 1.000000000000000000, 0.9238795325112869605, 1.000000000000000000, 0.9238795325112869605, 1.000000000000000000, 0.9238795325112869605, 1.000000000000000000, 0.9238795325112869605, 1.000000000000000000, 0.9238795325112869605, 1.000000000000000000, 0.9238795325112869605, 1.000000000000000000, 0.9238795325112869605, 1.000000000000000000, 0.9238795325112869605, 1.000000000000000000, 0.9238795325112869605, 1.000000000000000000, 0.9238795325112869605, 1.000000000000000000, 0.9238795325112869605, 1.000000000000000000, 0.9238795325112869605, 1.000000000000000000, 0.9238795325112869605, 1.000000000000000000, 0.9238795325112869605, 1.000000000000000000, 0.9238795325112869605, 1.000000000000000000, 0.9238795325112869605, 1.000000000000000000, 0.9238795325112869605, 1.000000000000000000, 0.9238795325112869605, 1.000000000000000000, 0.9238795325112869605, 1.000000000000000000, 0.9238795325112869605, 1.000000000000000000, 0.9238795325112869605, 1.000000000000000000, 0.9238795325112869605, 1.000000000000000000, 0.9238795325112869605, 1.000000000000000000, 0.9238795325112869605, 1.000000000000000000, 0.9238795325112869605, 1.000000000000000000, 0.9238795325112869605, 1.000000000000000000, 0.9238795325112869605, 1.000000000000000000, 0.9238795325112869605, 1.000000000000000000, 0.9238795325112869605, 1.000000000000000000, 0.9238795325112869605, 1.000000000000000000, 0.9238795325112869605, 1.000000000000000000, 0.9238795325112869605, 1.000000000000000000, 0.9238795325112869605, 1.000000000000000000, 0.9238795325112869605, 1.000000000000000000, 0.9238795325112869605, 1.000000000000000000, 0.9238795325112869605, 1.000000000000000000, 0.9238795325112869605, 1.000000000000000000, 0.9238795325112869605, 1.000000000000000000, 0.9238795325112869605, 1.000000000000000000, 0.9238795325112869605, 1.000000000000000000, 0.9238795325112869605, 1.000000000000000000, 0.9238795325112869605, 1.000000000000000000, 0.9238795325112869605, 1.000000000000000000, 0.9238795325112869605, 1.000000000000000000, 0.9238795325112869605, 1.000000000000000000),
 ( 1.000000000000000000, 0.9238795325112869605, 1.000000000000000000, 0.9238795325112869605, 1.000000000000000000, 0.9238795325112869605, 1.000000000000000000, 0.9238795325112869605, 1.000000000000000000, 0.9238795325112869605, 1.000000000000000000, 0.9238795325112869605, 1.000000000000000000, 0.9238795325112869605, 1.000000000000000000, 0.9238795325112869605, 1.000000000000000000, 0.9238795325112869605, 1.000000000000000000, 0.9238795325112869605, 1.000000000000000000, 0.9238795325112869605, 1.000000000000000000, 0.9238795325112869605, 1.000000000000000000, 0.9238795325112869605, 1.000000000000000000, 0.9238795325112869605, 1.000000000000000000, 0.9238795325112869605, 1.000000000000000000, 0.9238795325112869605, 1.000000000000000000, 0.9238795325112869605, 1.000000000000000000, 0.9238795325112869605, 1.000000000000000000, 0.9238795325112869605, 1.000000000000000000, 0.9238795325112869605, 1.000000000000000000, 0.9238795325112869605, 1.000000000000000000, 0.9238795325112869605, 1.000000000000000000, 0.9238795325112869605, 1.000000000000000000, 0.9238795325112869605, 1.000000000000000000, 0.9238795325112869605, 1.000000000000000000, 0.9238795325112869605, 1.000000000000000000, 0.9238795325112869605, 1.000000000000000000, 0.9238795325112869605, 1.000000000000000000, 0.9238795325112869605, 1.000000000000000000, 0.9238795325112869605, 1.000000000000000000, 0.9238795325112869605, 1.000000000000000000, 0.9238795325112869605, 1.000000000000000000, 0.9238795325112869605, 1.000000000000000000, 0.9238795325112869605, 1.000000000000000000, 0.9238795325112869605, 1.000000000000000000, 0.9238795325112869605, 1.000000000000000000, 0.9238795325112869605, 1.000000000000000000, 0.9238795325112869605, 1.000000000000000000, 0.9238795325112869605, 1.000000000000000000, 0.9238795325112869605, 1.000000000000000000, 0.9238795325112869605, 1.000000000000000000, 0.9238795325112869605, 1.000000000000000000, 0.9238795325112869605, 1.000000000000000000, 0.9238795325112869605, 1.000000000000000000, 0.9238795325112869605, 1.000000000000000000, 0.9238795325112869605, 1.000000000000000000, 0.9238795325112869605, 1.000000000000000000, 0.9238795325112869605, 1.000000000000000000, 0.9238795325112869605, 1.000000000000000000, 0.9238795325112869605, 1.000000000000000000, 0.9238795325112869605, 1.000000000000000000, 0.9238795325112869605, 1.000000000000000000, 0.9238795325112869605, 1.000000000000000000, 0.9238795325112869605, 1.000000000000000000, 0.9238795325112869605, 1.000000000000000000, 0.9238795325112869605, 1.000000000000000000, 0.9238795325112869605, 1.000000000000000000, 0.9238795325112869605, 1.000000000000000000, 0.9238795325112869605, 1.000000000000000000, 0.9238795325112869605, 1.000000000000000000, 0.9238795325112869605, 1.000000000000000000, 0.9238795325112869605, 1.000000000000000000, 0.9238795325112869605, 1.000000000000000000, 0.9238795325112869605, 1.000000000000000000, 0.9238795325112869605, 1.000000000000000000, 0.9238795325112869605, 1.000000000000000000, 0.9238795325112869605, 1.000000000000000000, 0.9238795325112869605, 1.000000000000000000, 0.9238795325112869605, 1.000000000000000000, 0.9238795325112869605, 1.000000000000000000, 0.9238795325112869605, 1.000000000000000000, 0.9238795325112869605, 1.000000000000000000, 0.9238795325112869605, 1.000000000000000000, 0.9238795325112869605, 1.000000000000000000, 0.9238795325112869605, 1.000000000000000000, 0.9238795325112869605, 1.000000000000000000, 0.9238795325112869605, 1.000000000000000000, 0.9238795325112869605, 1.000000000000000000, 0.9238795325112869605, 1.000000000000000000, 0.9238795325112869605, 1.000000000000000000, 0.9238795325112869605, 1.000000000000000000, 0.9238795325112869605, 1.000000000000000000, 0.9238795325112869605, 1.000000000000000000, 0.9238795325112869605, 1.000000000000000000, 0.9238795325112869605, 1.000000000000000000, 0.9238795325112869605, 1.000000000000000000, 0.9238795325112869605, 1.000000000000000000, 0.9238795325112869605, 1.000000000000000000, 0.9238795325112869605, 1.000000000000000000, 0.9238795325112869605, 1.000000000000000000, 0.9238795325112869605, 1.000000000000000000, 0.9238795325112869605, 1.000000000000000000, 0.9238795325112869605, 1.000000000000000000, 0.9238795325112869605, 1.000000000000000000, 0.9238795325112869605, 1.000000000000000000, 0.9238795325112869605, 1.000000000000000000, 0.9238795325112869605, 1.000000000000000000, 0.9238795325112869605, 1.000000000000000000, 0.9238795325112869605, 1.000000000000000000, 0.9238795325112869605, 1.000000000000000000, 0.9238795325112869605, 1.000000000000000000, 0.9238795325112869605, 1.000000000000000000, 0.9238795325112869605, 1.000000000000000000, 0.9238795325112869605, 1.000000000000000000, 0.9238795325112869605, 1.000000000000000000, 0.9238795325112869605, 1.000000000000000000, 0.9238795325112869605, 1.000000000000000000, 0.9238795325112869605, 1.000000000000000000, 0.9238795325112869605, 1.000000000000000000, 0.9238795325112869605, 1.000000000000000000, 0.9238795325112869605, 1.000000000000000000, 0.9238795325112869605, 1.000000000000000000, 0.9238795325112869605, 1.000000000000000000, 0.9238795325112869605, 1.000000000000000000, 0.9238795325112869605, 1.000000000000000000, 0.9238795325112869605, 1.000000000000000000, 0.9238795325112869605, 1.000000000000000000, 0.9238795325112869605, 1.000000000000000000, 0.9238795325112869605, 1.000000000000000000, 0.9238795325112869605, 1.000000000000000000, 0.9238795325112869605, 1.000000000000000000, 0.9238795325112869605, 1.000000000000000000, 0.9238795325112869605, 1.000000000000000000, 0.9238795325112869605, 1.000000000000000000, 0.9238795325112869605, 1.000000000000000000, 0.9238795325112869605, 1.000000000000000000, 0.9238795325112869605, 1.000000000000000000, 0.9238795325112869605, 1.000000000000000000, 0.9238795325112869605, 1.000000000000000000, 0.9238795325112869605, 1.000000000000000000, 0.9238795325112869605, 1.000000000000000000, 0.9238795325112869605, 1.000000000000000000, 0.9238795325112869605, 1.000000000000000000, 0.9238795325112869605, 1.000000000000000000, 0.9238795325112869605, 1.000000000000000000, 0.9238795325112869605, 1.000000000000000000, 0.9238795325112869605, 1.000000000000000000, 0.9238795325112869605, 1.000000000000000000, 0.9238795325112869605, 1.000000000000000000, 0.9238795325112869605, 1.000000000000000000, 0.9238795325112869605, 1.000000000000000000, 0.9238795325112869605, 1.000000000000000000, 0.9238795325112869605, 1.000000000000000000, 0.9238795325112869605, 1.000000000000000000, 0.9238795325112869605, 1.000000000000000000, 0.9238795325112869605, 1.000000000000000000, 0.9238795325112869605, 1.000000000000000000, 0.9238795325112869605, 1.000000000000000000, 0.9238795325112869605, 1.000000000000000000, 0.9238795325112869605, 1.000000000000000000, 0.9238795325112869605, 1.000000000000000000, 0.9238795325112869605, 1.000000000000000000, 0.9238795325112869605, 1.000000000000000000, 0.9238795325112869605, 1.000000000000000000, 0.9238795325112869605, 1.000000000000000000, 0.9238795325112869605, 1.000000000000000000, 0.9238795325112869605, 1.000000000000000000, 0.9238795325112869605, 1.000000000000000000, 0.9238795325112869605, 1.000000000000000000, 0.9238795325112869605, 1.000000000000000000, 0.9238795325112869605, 1.000000000000000000, 0.9238795325112869605, 1.000000000000000000, 0.9238795325112869605, 1.000000000000000000, 0.9238795325112869605, 1.000000000000000000, 0.9238795325112869605, 1.000000000000000000, 0.9238795325112869605, 1.000000000000000000, 0.9238795325112869605, 1.000000000000000000, 0.9238795325112869605, 1.000000000000000000, 0.9238795325112869605, 1.000000000000000000, 0.9238795325112869605, 1.000000000000000000, 0.9238795325112869605, 1.000000000000000000, 0.9238795325112869605, 1.000000000000000000, 0.9238795325112869605, 1.000000000000000000, 0.9238795325112869605, 1.000000000000000000, 0.9238795325112869605, 1.000000000000000000, 0.9238795325112869605, 1.000000000000000000, 0.9238795325112869605, 1.000000000000000000, 0.9238795325112869605, 1.000000000000000000, 0.9238795325112869605, 1.000000000000000000, 0.9238795325112869605, 1.000000000000000000, 0.9238795325112869605, 1.000000000000000000, 0.9238795325112869605, 1.000000000000000000, 0.9238795325112869605, 1.000000000000000000, 0.9238795325112869605, 1.000000000000000000, 0.9238795325112869605, 1.000000000000000000, 0.9238795325112869605, 1.000000000000000000, 0.9238795325112869605, 1.000000000000000000, 0.9238795325112869605, 1.000000000000000000, 0.9238795325112869605, 1.000000000000000000, 0.9238795325112869605, 1.000000000000000000, 0.9238795325112869605, 1.000000000000000000, 0.9238795325112869605, 1.000000000000000000, 0.9238795325112869605, 1.000000000000000000, 0.9238795325112869605, 1.000000000000000000, 0.9238795325112869605, 1.000000000000000000, 0.9238795325112869605, 1.000000000000000000, 0.9238795325112869605, 1.000000000000000000, 0.9238795325112869605, 1.000000000000000000, 0.9238795325112869605, 1.000000000000000000, 0.9238795325112869605, 1.000000000000000000, 0.9238795325112869605, 1.000000000000000000, 0.9238795325112869605, 1.000000000000000000, 0.9238795325112869605, 1.000000000000000000, 0.9238795325112869605, 1.000000000000000000, 0.9238795325112869605, 1.000000000000000000, 0.9238795325112869605, 1.000000000000000000, 0.9238795325112869605, 1.000000000000000000, 0.9238795325112869605, 1.000000000000000000, 0.9238795325112869605, 1.000000000000000000, 0.9238795325112869605, 1.000000000000000000, 0.9238795325112869605, 1.000000000000000000, 0.9238795325112869605, 1.000000000000000000, 0.9238795325112869605, 1.000000000000000000, 0.9238795325112869605, 1.000000000000000000, 0.9238795325112869605, 1.000000000000000000, 0.9238795325112869605, 1.000000000000000000, 0.9238795325112869605, 1.000000000000000000, 0.9238795325112869605, 1.000000000000000000, 0.9238795325112869605, 1.000000000000000000, 0.9238795325112869605, 1.000000000000000000, 0.9238795325112869605, 1.000000000000000000, 0.9238795325112869605, 1.000000000000000000, 0.9238795325112869605, 1.000000000000000000, 0.9238795325112869605, 1.000000000000000000, 0.9238795325112869605, 1.000000000000000000, 0.9238795325112869605, 1.000000000000000000, 0.9238795325112869605, 1.000000000000000000, 0.9238795325112869605, 1.000000000000000000, 0.9238795325112869605, 1.000000000000000000, 0.9238795325112869605, 1.000000000000000000, 0.9238795325112869605, 1.000000000000000000, 0.9238795325112869605, 1.000000000000000000, 0.9238795325112869605, 1.000000000000000000, 0.9238795325112869605, 1.000000000000000000, 0.9238795325112869605, 1.000000000000000000, 0.9238795325112869605, 1.000000000000000000, 0.9238795325112869605, 1.000000000000000000, 0.9238795325112869605, 1.000000000000000000, 0.9238795325112869605, 1.000000000000000000, 0.9238795325112869605, 1.000000000000000000, 0.9238795325112869605, 1.000000000000000000, 0.9238795325112869605, 1.000000000000000000, 0.9238795325112869605, 1.000000000000000000, 0.9238795325112869605, 1.000000000000000000, 0.9238795325112869605, 1.000000000000000000, 0.9238795325112869605, 1.000000000000000000, 0.9238795325112869605, 1.000000000000000000, 0.9238795325112869605, 1.000000000000000000, 0.9238795325112869605, 1.000000000000000000, 0.9238795325112869605, 1.000000000000000000, 0.9238795325112869605, 1.000000000000000000, 0.9238795325112869605, 1.000000000000000000, 0.9238795325112869605, 1.000000000000000000, 0.9238795325112869605, 1.000000000000000000, 0.9238795325112869605, 1.000000000000000000, 0.9238795325112869605, 1.000000000000000000, 0.9238795325112869605, 1.000000000000000000, 0.9238795325112869605, 1.000000000000000000, 0.9238795325112869605, 1.000000000000000000, 0.9238795325112869605, 1.000000000000000000, 0.9238795325112869605, 1.000000000000000000, 0.9238795325112869605, 1.000000000000000000, 0.9238795325112869605, 1.000000000000000000, 0.9238795325112869605, 1.000000000000000000, 0.9238795325112869605, 1.000000000000000000, 0.9238795325112869605, 1.000000000000000000, 0.9238795325112869605, 1.000000000000000000, 0.9238795325112869605, 1.000000000000000000, 0.9238795325112869605, 1.000000000000000000, 0.9238795325112869605, 1.000000000000000000, 0.9238795325112869605, 1.000000000000000000, 0.9238795325112869605, 1.000000000000000000, 0.9238795325112869605, 1.000000000000000000, 0.9238795325112869605, 1.000000000000000000, 0.9238795325112869605, 1.000000000000000000, 0.9238795325112869605, 1.000000000000000000, 0.9238795325112869605, 1.000000000000000000, 0.9238795325112869605, 1.000000000000000000, 0.9238795325112869605, 1.000000000000000000, 0.9238795325112869605, 1.000000000000000000, 0.9238795325112869605, 1.000000000000000000, 0.9238795325112869605, 1.000000000000000000, 0.9238795325112869605, 1.000000000000000000, 0.9238795325112869605, 1.000000000000000000, 0.9238795325112869605, 1.000000000000000000, 0.9238795325112869605, 1.000000000000000000, 0.9238795325112869605, 1.000000000000000000, 0.9238795325112869605, 1.000000000000000000, 0.9238795325112869605, 1.000000000000000000, 0.9238795325112869605, 1.000000000000000000, 0.9238795325112869605, 1.000000000000000000, 0.9238795325112869605, 1.000000000000000000, 0.9238795325112869605, 1.000000000000000000, 0.9238795325112869605, 1.000000000000000000, 0.9238795325112869605, 1.000000000000000000, 0.9238795325112869605, 1.000000000000000000, 0.9238795325112869605, 1.000000000000000000, 0.9238795325112869605, 1.000000000000000000, 0.9238795325112869605, 1.000000000000000000, 0.9238795325112869605, 1.000000000000000000, 0.9238795325112869605, 1.000000000000000000, 0.9238795325112869605, 1.000000000000000000, 0.9238795325112869605, 1.000000000000000000, 0.9238795325112869605, 1.000000000000000000, 0.9238795325112869605, 1.000000000000000000, 0.9238795325112869605, 1.000000000000000000, 0.9238795325112869605, 1.000000000000000000, 0.9238795325112869605, 1.000000000000000000, 0.9238795325112869605, 1.000000000000000000, 0.9238795325112869605, 1.000000000000000000, 0.9238795325112869605, 1.000000000000000000, 0.9238795325112869605, 1.000000000000000000, 0.9238795325112869605, 1.000000000000000000, 0.9238795325112869605, 1.000000000000000000, 0.9238795325112869605, 1.000000000000000000, 0.9238795325112869605, 1.000000000000000000, 0.9238795325112869605, 1.000000000000000000, 0.9238795325112869605, 1.000000000000000000, 0.9238795325112869605, 1.000000000000000000, 0.9238795325112869605, 1.000000000000000000, 0.9238795325112869605, 1.000000000000000000, 0.9238795325112869605, 1.000000000000000000, 0.9238795325112869605, 1.000000000000000000, 0.9238795325112869605, 1.000000000000000000, 0.9238795325112869605, 1.000000000000000000, 0.9238795325112869605, 1.000000000000000000, 0.9238795325112869605, 1.000000000000000000, 0.9238795325112869605, 1.000000000000000000, 0.9238795325112869605, 1.000000000000000000, 0.9238795325112869605, 1.000000000000000000, 0.9238795325112869605, 1.000000000000000000, 0.9238795325112869605, 1.000000000000000000, 0.9238795325112869605, 1.000000000000000000, 0.9238795325112869605, 1.000000000000000000, 0.9238795325112869605, 1.000000000000000000, 0.9238795325112869605, 1.000000000000000000, 0.9238795325112869605, 1.000000000000000000, 0.9238795325112869605, 1.000000000000000000, 0.9238795325112869605, 1.000000000000000000, 0.9238795325112869605, 1.000000000000000000, 0.9238795325112869605, 1.000000000000000000, 0.9238795325112869605, 1.000000000000000000, 0.9238795325112869605, 1.000000000000000000, 0.9238795325112869605, 1.000000000000000000, 0.9238795325112869605, 1.000000000000000000, 0.9238795325112869605, 1.000000000000000000, 0.9238795325112869605, 1.000000000000000000, 0.9238795325112869605, 1.000000000000000000, 0.9238795325112869605, 1.000000000000000000, 0.9238795325112869605, 1.000000000000000000, 0.9238795325112869605, 1.000000000000000000, 0.9238795325112869605, 1.000000000000000000, 0.9238795325112869605, 1.000000000000000000, 0.9238795325112869605, 1.000000000000000000, 0.9238795325112869605, 1.000000000000000000, 0.9238795325112869605, 1.000000000000000000, 0.9238795325112869605, 1.000000000000000000, 0.9238795325112869605, 1.000000000000000000, 0.9238795325112869605, 1.000000000000000000, 0.9238795325112869605, 1.000000000000000000, 0.9238795325112869605, 1.000000000000000000, 0.9238795325112869605, 1.000000000000000000, 0.9238795325112869605, 1.000000000000000000, 0.9238795325112869605, 1.000000000000000000, 0.9238795325112869605, 1.000000000000000000, 0.9238795325112869605, 1.000000000000000000, 0.9238795325112869605, 1.000000000000000000, 0.9238795325112869605, 1.000000000000000000, 0.9238795325112869605, 1.000000000000000000, 0.9238795325112869605, 1.000000000000000000, 0.9238795325112869605, 1.000000000000000000, 0.9238795325112869605, 1.000000000000000000, 0.9238795325112869605, 1.000000000000000000, 0.9238795325112869605, 1.000000000000000000, 0.9238795325112869605, 1.000000000000000000, 0.9238795325112869605, 1.000000000000000000, 0.9238795325112869605, 1.000000000000000000, 0.9238795325112869605, 1.000000000000000000, 0.9238795325112869605, 1.000000000000000000, 0.9238795325112869605, 1.000000000000000000, 0.9238795325112869605, 1.000000000000000000, 0.9238795325112869605, 1.000000000000000000, 0.9238795325112869605, 1.000000000000000000, 0.9238795325112869605, 1.000000000000000000, 0.9238795325112869605, 1.000000000000000000, 0.9238795325112869605, 1.000000000000000000, 0.9238795325112869605, 1.000000000000000000, 0.9238795325112869605, 1.000000000000000000, 0.9238795325112869605, 1.000000000000000000, 0.9238795325112869605, 1.000000000000000000, 0.9238795325112869605, 1.000000000000000000, 0.9238795325112869605, 1.000000000000000000, 0.9238795325112869605, 1.000000000000000000, 0.9238795325112869605, 1.000000000000000000, 0.9238795325112869605, 1.000000000000000000, 0.9238795325112869605, 1.000000000000000000, 0.9238795325112869605, 1.000000000000000000, 0.9238795325112869605, 1.000000000000000000, 0.9238795325112869605, 1.000000000000000000, 0.9238795325112869605, 1.000000000000000000) ) ) 
 REPRESENTATION_ITEM ( '' )  SURFACE ( )  ) ;
#6087=CARTESIAN_POINT ( 'NONE',  ( 0.9412147342319837628, -0.1574803149606297803, 1.774114173228345859 ) ) ;
#6092=ADVANCED_FACE ( 'NONE', ( #17880 ), #14302, .T. ) ;
#6095=CARTESIAN_POINT ( 'NONE',  ( 0.8019270111902717657, 0.1787899950787401604, 1.062992125930488418 ) ) ;
#6096=CARTESIAN_POINT ( 'NONE',  ( 1.002407869896990045, -0.1264236179284866091, 1.552657480261196765 ) ) ;
#6097=CARTESIAN_POINT ( 'NONE',  ( 0.7495606340400177148, 0.1264236179284866091, 0.1943897637257641919 ) ) ;
#6100=CARTESIAN_POINT ( 'NONE',  ( 1.033464566929134687, 0.06523048226347956391, 1.665846456692914312 ) ) ;
#6101=CARTESIAN_POINT ( 'NONE',  ( 0.7185039370078739607, 1.928577636452523993E-17, 1.407480314960629864 ) ) ;
#6104=CARTESIAN_POINT ( 'NONE',  ( -0.7185039370078739607, 1.928577636452523993E-17, 1.791338582569637738 ) ) ;
#6106=( BOUNDED_CURVE ( )  B_SPLINE_CURVE ( 2, ( #26972, #31040, #41524, #23366, #8730, #19752, #45608, #12826, #27458 ),
 .UNSPECIFIED., .F., .T. ) 
 B_SPLINE_CURVE_WITH_KNOTS ( ( 3, 2, 2, 2, 3 ),
 ( 0.5100000000000000089, 0.5124999999999999556, 0.5150000000000000133, 0.5174999999999999600, 0.5200000000000000178 ),
 .UNSPECIFIED. ) 
 CURVE ( )  GEOMETRIC_REPRESENTATION_ITEM ( )  RATIONAL_B_SPLINE_CURVE ( ( 1.000000000000000000, 0.9238795325112869605, 1.000000000000000000, 0.9238795325112869605, 1.000000000000000000, 0.9238795325112869605, 1.000000000000000000, 0.9238795325112869605, 1.000000000000000000 ) ) 
 REPRESENTATION_ITEM ( '' )  ) ;
#6107=CARTESIAN_POINT ( 'NONE',  ( 0.8759842519685039353, -0.1574803149606299191, 1.653543307086614345 ) ) ;
#6108=CARTESIAN_POINT ( 'NONE',  ( 0.6971942568897637749, 2.189545951927499583E-17, 1.104822834591905556 ) ) ;
#6111=CARTESIAN_POINT ( 'NONE',  ( 0.7646288533564489232, -0.1113553986120547346, 0.3395669290263311213 ) ) ;
#6113=CARTESIAN_POINT ( 'NONE',  ( 1.054774247047244540, -0.07405724077823318263, 1.993110236166711013 ) ) ;
#6114=CARTESIAN_POINT ( 'NONE',  ( -0.7185039370078746268, -0.06523048226347956391, 0.2583661416247562959 ) ) ;
#6115=EDGE_LOOP ( 'NONE', ( #13999, #18124, #21961, #42666 ) ) ;
#6116=CARTESIAN_POINT ( 'NONE',  ( 0.9500414927467378812, -0.1787899950787401604, 1.274606299158834277 ) ) ;
#6118=DIRECTION ( 'NONE',  ( 0.000000000000000000, 0.000000000000000000, -1.000000000000000000 ) ) ;
#6121=CARTESIAN_POINT ( 'NONE',  ( -1.033464566929133799, 0.000000000000000000, 1.023622047136567126 ) ) ;
#6125=CARTESIAN_POINT ( 'NONE',  ( -0.8759842519685039353, -0.1787899950787401882, 1.350885826717889815 ) ) ;
#6128=CARTESIAN_POINT ( 'NONE',  ( -1.002407869896990045, 0.1264236179284866091, 0.9768700786863937502 ) ) ;
#6129=CARTESIAN_POINT ( 'NONE',  ( -0.7185039370078746268, 0.06523048226347956391, 0.02706692913385832025 ) ) ;
#6131=CARTESIAN_POINT ( 'NONE',  ( -1.002407869896990045, -0.1264236179284866091, 1.001476377898992132 ) ) ;
#6133=CARTESIAN_POINT ( 'NONE',  ( -0.8019270111902717657, -0.1787899950787401604, 0.6446850393163160442 ) ) ;
#6134=CARTESIAN_POINT ( 'NONE',  ( -0.9873396505805591694, 0.1113553986120547346, 0.08366141721530767628 ) ) ;
#6135=ORIENTED_EDGE ( 'NONE', *, *, #17009, .T. ) ;
#6141=CARTESIAN_POINT ( 'NONE',  ( -0.9500414927467378812, -0.1787899950787401604, 0.5659448818360001132 ) ) ;
#6142=CARTESIAN_POINT ( 'NONE',  ( 0.9873396505805591694, 0.1113553986120547346, 1.343503936900346529 ) ) ;
#6145=CARTESIAN_POINT ( 'NONE',  ( -0.8019270111902716547, 0.1787899950787401604, 1.732283464513166615 ) ) ;
#6154=CARTESIAN_POINT ( 'NONE',  ( 0.9412147342319837628, 0.1574803149606300301, 0.6077755905511815770 ) ) ;
#6156=CARTESIAN_POINT ( 'NONE',  ( -0.9412147342319837628, 0.1574803149606300301, 1.424704724301921743 ) ) ;
#6157=CARTESIAN_POINT ( 'NONE',  ( 0.8759842519685039353, -0.1787899950787401882, 0.6471456692375747721 ) ) ;
#6158=EDGE_CURVE ( 'NONE', #27709, #31512, #367, .T. ) ;
#6160=CARTESIAN_POINT ( 'NONE',  ( -0.7185039370078739607, 1.928577636452523993E-17, 0.6889763778452283605 ) ) ;
#6161=CARTESIAN_POINT ( 'NONE',  ( 0.8759842519685039353, 0.1574803149606299191, 1.624015747923968522 ) ) ;
#6165=CARTESIAN_POINT ( 'NONE',  ( 0.7185039370078746268, 0.06523048226347956391, 1.286909448818898127 ) ) ;
#6168=CARTESIAN_POINT ( 'NONE',  ( 0.9412147342319837628, -0.1574803149606297803, 1.970964566929134021 ) ) ;
#6171=CARTESIAN_POINT ( 'NONE',  ( 0.8019270111902716547, -0.1787899950787401604, 0.6397637794737947026 ) ) ;
#6176=CARTESIAN_POINT ( 'NONE',  ( 1.002407869896990045, -0.1264236179284866091, 0.8833661416785196785 ) ) ;
#6177=CARTESIAN_POINT ( 'NONE',  ( -0.8759842519685039353, 0.000000000000000000, 0.000000000000000000 ) ) ;
#6181=CARTESIAN_POINT ( 'NONE',  ( 1.033464566929133799, 0.000000000000000000, 1.220472440837354400 ) ) ;
#6182=CARTESIAN_POINT ( 'NONE',  ( -0.8107537697050254399, 0.1574803149606300301, 1.862696850286174710 ) ) ;
#6183=UNCERTAINTY_MEASURE_WITH_UNIT (LENGTH_MEASURE( 1.000000000000000082E-05 ), #1373, 'distance_accuracy_value', 'NONE') ;
#6184=CARTESIAN_POINT ( 'NONE',  ( -1.002407869896990045, -0.1264236179284866091, 1.872539370024976391 ) ) ;
#6185=CARTESIAN_POINT ( 'NONE',  ( 0.6971942568897648851, -0.07405724077823297447, 1.938976377898990799 ) ) ;
#6187=CARTESIAN_POINT ( 'NONE',  ( -0.9412147342319837628, -0.1574803149606297803, 1.852854330708662012 ) ) ;
#6189=CARTESIAN_POINT ( 'NONE',  ( -1.002407869896990045, -0.1264236179284866091, 1.592027559001354398 ) ) ;
#6191=CARTESIAN_POINT ( 'NONE',  ( -0.9500414927467378812, -0.1787899950787401604, 0.9990157479777320715 ) ) ;
#6192=VECTOR ( 'NONE', #29515, 39.37007874015748143 ) ;
#6193=CARTESIAN_POINT ( 'NONE',  ( -1.002407869896990045, -0.1264236179284866091, 0.1796259841982051075 ) ) ;
#6195=CARTESIAN_POINT ( 'NONE',  ( -0.8019270111902717657, 0.1787899950787401604, 1.968503936954110189 ) ) ;
#6197=CARTESIAN_POINT ( 'NONE',  ( -0.9412147342319837628, -0.1574803149606297803, 1.931594488188976166 ) ) ;
#6198=CARTESIAN_POINT ( 'NONE',  ( -0.7185039370078739607, 1.928577636452523993E-17, 1.879921259842519676 ) ) ;
#6202=ORIENTED_EDGE ( 'NONE', *, *, #34576, .F. ) ;
#6207=( LENGTH_UNIT ( ) NAMED_UNIT ( * ) SI_UNIT ( $, .METRE. ) ) ;
#6210=CARTESIAN_POINT ( 'NONE',  ( -0.9873396505805591694, 0.1113553986120547346, 0.8710629920184568276 ) ) ;
#6211=CARTESIAN_POINT ( 'NONE',  ( -0.9412147342319837628, -0.1574803149606297803, 0.7504921259842516346 ) ) ;
#6216=CARTESIAN_POINT ( 'NONE',  ( 0.7185039370078739607, 1.928577636452523993E-17, 0.7775590551181102983 ) ) ;
#6217=TOROIDAL_SURFACE ( 'NONE', #24609, 0.3444881889763780070, 0.1574803149606299191 ) ;
#6220=( BOUNDED_CURVE ( )  B_SPLINE_CURVE ( 2, ( #6630, #3026, #35181, #42344, #28226, #42789, #31594, #2327, #12385 ),
 .UNSPECIFIED., .F., .F. ) 
 B_SPLINE_CURVE_WITH_KNOTS ( ( 3, 2, 2, 2, 3 ),
 ( 0.3200000000000000067, 0.3225000000000000089, 0.3250000000000000111, 0.3275000000000000133, 0.3300000000000000155 ),
 .UNSPECIFIED. ) 
 CURVE ( )  GEOMETRIC_REPRESENTATION_ITEM ( )  RATIONAL_B_SPLINE_CURVE ( ( 1.000000000000000000, 0.9238795325112869605, 1.000000000000000000, 0.9238795325112869605, 1.000000000000000000, 0.9238795325112869605, 1.000000000000000000, 0.9238795325112869605, 1.000000000000000000 ) ) 
 REPRESENTATION_ITEM ( '' )  ) ;
#6223=CARTESIAN_POINT ( 'NONE',  ( 0.8107537697050253289, 0.1574803149606300301, 0.2091535431995598104 ) ) ;
#6224=ORIENTED_EDGE ( 'NONE', *, *, #45038, .F. ) ;
#6229=CARTESIAN_POINT ( 'NONE',  ( -0.6971942568897637749, 2.189545951927499583E-17, 1.852854330654897685 ) ) ;
#6230=ORIENTED_EDGE ( 'NONE', *, *, #29273, .F. ) ;
#6231=CARTESIAN_POINT ( 'NONE',  ( -1.002407869896990045, -0.1264236179284866091, 1.518208661363559031 ) ) ;
#6232=CARTESIAN_POINT ( 'NONE',  ( 1.054774247047244540, -0.07405724077823318263, 1.599409448765135133 ) ) ;
#6234=CARTESIAN_POINT ( 'NONE',  ( -0.8019270111902717657, -0.1787899950787401604, 0.6053149605761579677 ) ) ;
#6235=CARTESIAN_POINT ( 'NONE',  ( 0.6971942568897637749, 2.189545951927499583E-17, 0.2042322834108035723 ) ) ;
#6238=CARTESIAN_POINT ( 'NONE',  ( 0.8019270111902716547, 0.1787899950787401604, 0.6299212597887560161 ) ) ;
#6239=CARTESIAN_POINT ( 'NONE',  ( -0.8019270111902716547, 0.1787899950787401604, 0.5068897637257642197 ) ) ;
#6241=CARTESIAN_POINT ( 'NONE',  ( 0.9873396505805591694, -0.1113553986120547346, 0.6348425196850393526 ) ) ;
#6245=CARTESIAN_POINT ( 'NONE',  ( -1.054774247047244540, -0.07405724077823318263, 1.402559055064346971 ) ) ;
#6246=ORIENTED_EDGE ( 'NONE', *, *, #15494, .T. ) ;
#6247=CARTESIAN_POINT ( 'NONE',  ( -0.8107537697050253289, 0.1574803149606300301, 0.4552165354330702240 ) ) ;
#6248=CARTESIAN_POINT ( 'NONE',  ( 0.9500414927467377701, -0.1787899950787401604, 1.279527559001355730 ) ) ;
#6250=VECTOR ( 'NONE', #3143, 39.37007874015748143 ) ;
#6256=CARTESIAN_POINT ( 'NONE',  ( 0.9873396505805591694, -0.1113553986120547346, 1.619094488188976388 ) ) ;
#6257=CARTESIAN_POINT ( 'NONE',  ( 0.8759842519685039353, 0.000000000000000000, 4.498031496062992574 ) ) ;
#6260=EDGE_CURVE ( 'NONE', #31847, #38785, #36810, .T. ) ;
#6264=FACE_OUTER_BOUND ( 'NONE', #33801, .T. ) ;
#6265=CARTESIAN_POINT ( 'NONE',  ( -0.8759842519685039353, -0.1574803149606299191, 0.9744094487113701408 ) ) ;
#6269=AXIS2_PLACEMENT_3D ( 'NONE', #11085, #21373, #33141 ) ;
#6271=CARTESIAN_POINT ( 'NONE',  ( 0.6971942568897626646, 0.07405724077823318263, 0.5118110235682844511 ) ) ;
#6273=CARTESIAN_POINT ( 'NONE',  ( -0.6971942568897648851, -0.07405724077823297447, 0.7972440944344248992 ) ) ;
#6275=CARTESIAN_POINT ( 'NONE',  ( 0.8107537697050254399, 0.1574803149606300301, 1.124507874015748810 ) ) ;
#6277=CARTESIAN_POINT ( 'NONE',  ( -0.7725776124789660582, -0.1361825328364024978, 1.986138947217436668 ) ) ;
#6280=CARTESIAN_POINT ( 'NONE',  ( -0.8759842519685039353, -0.1574803149606299191, 1.249999999892472236 ) ) ;
#6281=CARTESIAN_POINT ( 'NONE',  ( 0.8759842519685039353, -0.1787899950787401882, 1.710137795221826851 ) ) ;
#6284=CARTESIAN_POINT ( 'NONE',  ( 0.8019270111902716547, 0.1787899950787401604, 0.3887795275052913224 ) ) ;
#6286=VECTOR ( 'NONE', #45938, 39.37007874015748143 ) ;
#6288=ORIENTED_EDGE ( 'NONE', *, *, #34010, .F. ) ;
#6292=CARTESIAN_POINT ( 'NONE',  ( 1.002407869896990045, -0.1264236179284866091, 0.6471456692375747721 ) ) ;
#6294=CARTESIAN_POINT ( 'NONE',  ( -0.9412147342319837628, -0.1574803149606297803, 0.9374999998924736788 ) ) ;
#6295=CARTESIAN_POINT ( 'NONE',  ( -0.9500414927467378812, -0.1787899950787401604, 1.432086614119464141 ) ) ;
#6297=CARTESIAN_POINT ( 'NONE',  ( 1.054774247047244540, 0.07405724077823318263, 1.013779527505291878 ) ) ;
#6298=CARTESIAN_POINT ( 'NONE',  ( -0.7185039370078746268, 0.06523048226347956391, 0.6471456691838121111 ) ) ;
#6299=CARTESIAN_POINT ( 'NONE',  ( 0.6971942568897648851, 0.07405724077823318263, 1.811023621993480548 ) ) ;
#6300=CARTESIAN_POINT ( 'NONE',  ( -0.8107537697050253289, -0.1574803149606297803, 1.375492125984252523 ) ) ;
#6301=CARTESIAN_POINT ( 'NONE',  ( -1.054774247047244540, -0.07405724077823318263, 0.8858267715997791836 ) ) ;
#6304=CARTESIAN_POINT ( 'NONE',  ( 1.054774247047244540, 0.07405724077823318263, 0.1082677164816695514 ) ) ;
#6305=CARTESIAN_POINT ( 'NONE',  ( 0.8759842519685039353, 0.1574803149606299191, 1.545275590443653480 ) ) ;
#6307=EDGE_CURVE ( 'NONE', #44763, #42069, #44317, .T. ) ;
#6309=CARTESIAN_POINT ( 'NONE',  ( -1.033464566929133799, -1.928577636452524610E-17, 2.007874015640504162 ) ) ;
#6311=CARTESIAN_POINT ( 'NONE',  ( -0.9500414927467377701, -0.1787899950787401604, 1.668307086560410157 ) ) ;
#6314=CARTESIAN_POINT ( 'NONE',  ( -0.8759842519685039353, 0.000000000000000000, 0.000000000000000000 ) ) ;
#6319=ORIENTED_EDGE ( 'NONE', *, *, #22404, .F. ) ;
#6322=CARTESIAN_POINT ( 'NONE',  ( 0.8759842519685039353, -0.1787899950787401882, 1.075295275536787276 ) ) ;
#6327=CARTESIAN_POINT ( 'NONE',  ( 0.9412147342319837628, 0.1574803149606300301, 1.867618110236221707 ) ) ;
#6331=CARTESIAN_POINT ( 'NONE',  ( -1.002407869896990045, -0.1264236179284866091, 0.2977362204186775885 ) ) ;
#6333=FACE_OUTER_BOUND ( 'NONE', #41239, .T. ) ;
#6334=CARTESIAN_POINT ( 'NONE',  ( 1.054774247047244540, -0.07405724077823318263, 1.126968503883244654 ) ) ;
#6335=CARTESIAN_POINT ( 'NONE',  ( 0.9500414927467377701, -0.1787899950787401604, 1.589566929080094226 ) ) ;
#6336=CARTESIAN_POINT ( 'NONE',  ( 1.002407869896990045, -0.1264236179284866091, 0.2140748030958428971 ) ) ;
#6338=CARTESIAN_POINT ( 'NONE',  ( 0.8759842491179902213, 0.1574803149606299191, 1.978346456692913646 ) ) ;
#6339=CARTESIAN_POINT ( 'NONE',  ( 0.7185039370078739607, 1.928577636452523993E-17, 1.515748031388535200 ) ) ;
#6341=CARTESIAN_POINT ( 'NONE',  ( 0.9412147342319837628, -0.1574803149606297803, 0.7800196849318437042 ) ) ;
#6342=CARTESIAN_POINT ( 'NONE',  ( -0.7185039370078746268, -0.06523048226347956391, 1.793799212490897244 ) ) ;
#6343=CARTESIAN_POINT ( 'NONE',  ( 1.054774247047244540, -0.07405724077823318263, 0.09842519679663024046 ) ) ;
#6346=CARTESIAN_POINT ( 'NONE',  ( 1.054774247047244540, -0.07405724077823318263, 1.122047244040725422 ) ) ;
#6348=CARTESIAN_POINT ( 'NONE',  ( 0.8019270111902716547, -0.1787899950787401604, 1.943897637741510254 ) ) ;
#6349=CARTESIAN_POINT ( 'NONE',  ( 0.8759842519685039353, 0.1574803149606299191, 0.4429133857192448787 ) ) ;
#6352=CARTESIAN_POINT ( 'NONE',  ( -0.7646288533564489232, -0.1113553986120547346, 0.4576771652468039631 ) ) ;
#6354=CARTESIAN_POINT ( 'NONE',  ( 1.054774247047244540, 0.07405724077823318263, 1.284448818843874740 ) ) ;
#6358=DIRECTION ( 'NONE',  ( 1.822029033848725028E-16, 0.000000000000000000, 1.000000000000000000 ) ) ;
#6363=CARTESIAN_POINT ( 'NONE',  ( 0.8019270111902717657, 0.1787899950787401604, 0.3937007873478115538 ) ) ;
#6364=ORIENTED_EDGE ( 'NONE', *, *, #16140, .F. ) ;
#6365=CARTESIAN_POINT ( 'NONE',  ( -0.7495606340400177148, -0.1264236179284866091, 1.385334645615527549 ) ) ;
#6367=CARTESIAN_POINT ( 'NONE',  ( -0.8759842519685039353, 0.1787899950787401882, 1.021161417269070837 ) ) ;
#6369=CARTESIAN_POINT ( 'NONE',  ( -0.8759842519685039353, 0.1787899950787401882, 1.921751968450173376 ) ) ;
#6370=ORIENTED_EDGE ( 'NONE', *, *, #5250, .F. ) ;
#6372=CARTESIAN_POINT ( 'NONE',  ( -0.6971942568897648851, 0.07405724077823318263, 1.062992125930488418 ) ) ;
#6373=CARTESIAN_POINT ( 'NONE',  ( -0.7495606340400177148, -0.1264236179284866091, 0.6028543306548976854 ) ) ;
#6374=( BOUNDED_CURVE ( )  B_SPLINE_CURVE ( 2, ( #34416, #30380, #19065, #30149, #19311, #33964, #41322, #46355, #13769 ),
 .UNSPECIFIED., .F., .F. ) 
 B_SPLINE_CURVE_WITH_KNOTS ( ( 3, 2, 2, 2, 3 ),
 ( 0.9599999999999999645, 0.9625000000000000222, 0.9649999999999999689, 0.9675000000000000266, 0.9699999999999999734 ),
 .UNSPECIFIED. ) 
 CURVE ( )  GEOMETRIC_REPRESENTATION_ITEM ( )  RATIONAL_B_SPLINE_CURVE ( ( 1.000000000000000000, 0.9238795325112869605, 1.000000000000000000, 0.9238795325112869605, 1.000000000000000000, 0.9238795325112869605, 1.000000000000000000, 0.9238795325112799661, 1.000000000000000000 ) ) 
 REPRESENTATION_ITEM ( '' )  ) ;
#6375=CARTESIAN_POINT ( 'NONE',  ( 1.033464566929133799, 0.000000000000000000, 1.820866141732283561 ) ) ;
#6383=CARTESIAN_POINT ( 'NONE',  ( 1.033464566929133799, 0.000000000000000000, 0.7578740157480314821 ) ) ;
#6384=FACE_OUTER_BOUND ( 'NONE', #19680, .T. ) ;
#6385=CARTESIAN_POINT ( 'NONE',  ( -0.8759842519685039353, 0.1787899950787401882, 0.6225393700249762796 ) ) ;
#6388=CARTESIAN_POINT ( 'NONE',  ( -1.054774247047244096, 0.000000000000000000, 1.641240157426551161 ) ) ;
#6392=( BOUNDED_CURVE ( )  B_SPLINE_CURVE ( 2, ( #26629, #45745, #42141, #9350, #5029, #30704, #9109, #41181, #8869 ),
 .UNSPECIFIED., .F., .F. ) 
 B_SPLINE_CURVE_WITH_KNOTS ( ( 3, 2, 2, 2, 3 ),
 ( 0.4699999999999999734, 0.4724999999999999756, 0.4749999999999999778, 0.4774999999999999800, 0.4799999999999999822 ),
 .UNSPECIFIED. ) 
 CURVE ( )  GEOMETRIC_REPRESENTATION_ITEM ( )  RATIONAL_B_SPLINE_CURVE ( ( 1.000000000000000000, 0.9238795325112879597, 1.000000000000000000, 0.9238795325112869605, 1.000000000000000000, 0.9238795325112869605, 1.000000000000000000, 0.9238795325112869605, 1.000000000000000000 ) ) 
 REPRESENTATION_ITEM ( '' )  ) ;
#6393=CARTESIAN_POINT ( 'NONE',  ( -0.7185039370078746268, 0.06523048226347956391, 0.4995078740157475883 ) ) ;
#6394=ORIENTED_EDGE ( 'NONE', *, *, #40067, .T. ) ;
#6397=CARTESIAN_POINT ( 'NONE',  ( -0.7646288533564489232, 0.1113553986120547346, 1.392716535325543292 ) ) ;
#6401=CARTESIAN_POINT ( 'NONE',  ( 0.8759842519685039353, -0.1574803149606299191, 1.259842519685039353 ) ) ;
#6403=FACE_OUTER_BOUND ( 'NONE', #12498, .T. ) ;
#6406=CARTESIAN_POINT ( 'NONE',  ( 0.7495606340400177148, -0.1264236179284866091, 0.5979330708123780092 ) ) ;
#6412=CARTESIAN_POINT ( 'NONE',  ( 0.8759842519685039353, -0.1787899950787401882, 0.8390748030958424808 ) ) ;
#6413=CARTESIAN_POINT ( 'NONE',  ( 0.7185039370078746268, -0.06523048226347956391, 1.291830708661417360 ) ) ;
#6418=CARTESIAN_POINT ( 'NONE',  ( 0.9412147342319837628, -0.1574803149606297803, 1.291830708553889817 ) ) ;
#6420=CARTESIAN_POINT ( 'NONE',  ( -0.6971942568897637749, 2.189545951927499583E-17, 1.936515747977732405 ) ) ;
#6421=ORIENTED_EDGE ( 'NONE', *, *, #5639, .F. ) ;
#6422=CARTESIAN_POINT ( 'NONE',  ( 1.054774247047244540, 0.07405724077823318263, 1.919291338528913871 ) ) ;
#6425=CARTESIAN_POINT ( 'NONE',  ( -0.8759842519685039353, -0.1787899950787401882, 1.985728346402929168 ) ) ;
#6426=CARTESIAN_POINT ( 'NONE',  ( -0.6971942568897648851, -0.07405724077823297447, 1.500984251914741607 ) ) ;
#6427=CARTESIAN_POINT ( 'NONE',  ( 1.054774247047244540, -0.07405724077823318263, 0.8907480314422985268 ) ) ;
#6429=CARTESIAN_POINT ( 'NONE',  ( -0.8019270111902717657, -0.1787899950787401604, 1.033464566875371027 ) ) ;
#6430=CARTESIAN_POINT ( 'NONE',  ( -0.9500414927467378812, -0.1787899950787401604, 0.2165354330171024577 ) ) ;
#6431=ADVANCED_FACE ( 'NONE', ( #19999 ), #23607, .T. ) ;
#6433=CARTESIAN_POINT ( 'NONE',  ( -1.002407869896990045, -0.1264236179284866091, 1.872539370024976391 ) ) ;
#6434=CARTESIAN_POINT ( 'NONE',  ( 0.7185039370078739607, 1.928577636452523993E-17, 1.122047243986960652 ) ) ;
#6435=CARTESIAN_POINT ( 'NONE',  ( -1.033464566929134687, 0.06523048226347956391, 1.902066929133858775 ) ) ;
#6441=CARTESIAN_POINT ( 'NONE',  ( -1.033464566929134687, 0.06523048226347956391, 0.04183070855389029591 ) ) ;
#6443=EDGE_CURVE ( 'NONE', #17493, #27640, #37620, .T. ) ;
#6444=CARTESIAN_POINT ( 'NONE',  ( -0.7495606340400177148, -0.1264236179284866091, 0.1254921259304885850 ) ) ;
#6445=ORIENTED_EDGE ( 'NONE', *, *, #5035, .T. ) ;
#6452=CARTESIAN_POINT ( 'NONE',  ( -0.8759842519685039353, 0.1574803149606299191, 0.8070866141732283561 ) ) ;
#6454=VECTOR ( 'NONE', #29910, 39.37007874015748143 ) ;
#6455=CARTESIAN_POINT ( 'NONE',  ( 0.7646288533564489232, 0.1113553986120547346, 1.865157480207432883 ) ) ;
#6456=CARTESIAN_POINT ( 'NONE',  ( -0.7646288533564489232, 0.1113553986120547346, 1.432086614065700925 ) ) ;
#6457=CARTESIAN_POINT ( 'NONE',  ( 0.7185039370078739607, 1.928577636452523993E-17, 0.8169291338582678197 ) ) ;
#6462=CARTESIAN_POINT ( 'NONE',  ( 0.9873396505805591694, 0.1113553986120547346, 0.2017716534357799352 ) ) ;
#6463=ORIENTED_EDGE ( 'NONE', *, *, #45495, .F. ) ;
#6465=CARTESIAN_POINT ( 'NONE',  ( 0.8107537697050254399, 0.1574803149606300301, 0.7209645668216064784 ) ) ;
#6469=CARTESIAN_POINT ( 'NONE',  ( -1.054774247047244096, 0.000000000000000000, 1.951279527505291433 ) ) ;
#6470=ORIENTED_EDGE ( 'NONE', *, *, #41431, .F. ) ;
#6471=CARTESIAN_POINT ( 'NONE',  ( -0.7495606340400177148, -0.1264236179284866091, 1.468996062938362046 ) ) ;
#6472=CARTESIAN_POINT ( 'NONE',  ( 1.002407869896990045, 0.1264236179284866091, 1.528051181048598384 ) ) ;
#6473=ORIENTED_EDGE ( 'NONE', *, *, #3528, .F. ) ;
#6474=CARTESIAN_POINT ( 'NONE',  ( 0.9412147342319837628, -0.1574803149606297803, 0.9374999998924736788 ) ) ;
#6476=CARTESIAN_POINT ( 'NONE',  ( -0.6971942568897637749, 2.189545951927499583E-17, 0.5979330708123780092 ) ) ;
#6477=CARTESIAN_POINT ( 'NONE',  ( 0.8019270111902717657, 0.1787899950787401604, 0.1968503936470238913 ) ) ;
#6479=CARTESIAN_POINT ( 'NONE',  ( -0.8759842519685039353, -0.1787899950787401882, 0.4847440944344252323 ) ) ;
#6480=CARTESIAN_POINT ( 'NONE',  ( 1.033464566929133799, 0.000000000000000000, 0.6397637795275591399 ) ) ;
#6482=CARTESIAN_POINT ( 'NONE',  ( 0.7185039370078739607, 1.928577636452523993E-17, 1.082677165246803241 ) ) ;
#6484=CARTESIAN_POINT ( 'NONE',  ( -1.054774247047244540, -0.07405724077823318263, 1.363188976324188895 ) ) ;
#6485=ORIENTED_EDGE ( 'NONE', *, *, #4623, .T. ) ;
#6487=CARTESIAN_POINT ( 'NONE',  ( -0.8107537697050253289, -0.1574803149606297803, 1.532972440944882608 ) ) ;
#6488=CARTESIAN_POINT ( 'NONE',  ( -0.7185039370078746268, 0.06523048226347956391, 0.4207677165354331561 ) ) ;
#6489=CARTESIAN_POINT ( 'NONE',  ( 1.002407869896990045, 0.1264236179284866091, 1.331200787347811110 ) ) ;
#6497=CARTESIAN_POINT ( 'NONE',  ( 0.8107537697050254399, 0.1574803149606300301, 0.8095472440944886383 ) ) ;
#6498=DIRECTION ( 'NONE',  ( 0.000000000000000000, 0.000000000000000000, -1.000000000000000000 ) ) ;
#6500=CARTESIAN_POINT ( 'NONE',  ( 0.8759842519685039353, 0.000000000000000000, 4.498031496062992574 ) ) ;
#6502=( BOUNDED_CURVE ( )  B_SPLINE_CURVE ( 2, ( #2812, #13852, #21270, #35895, #3048, #17677, #32328, #46908, #4703 ),
 .UNSPECIFIED., .F., .T. ) 
 B_SPLINE_CURVE_WITH_KNOTS ( ( 3, 2, 2, 2, 3 ),
 ( 0.7399999999999999911, 0.7425000000000000488, 0.7449999999999999956, 0.7475000000000000533, 0.7500000000000000000 ),
 .UNSPECIFIED. ) 
 CURVE ( )  GEOMETRIC_REPRESENTATION_ITEM ( )  RATIONAL_B_SPLINE_CURVE ( ( 1.000000000000000000, 0.9238795325112869605, 1.000000000000000000, 0.9238795325112869605, 1.000000000000000000, 0.9238795325112869605, 1.000000000000000000, 0.9238795325112869605, 1.000000000000000000 ) ) 
 REPRESENTATION_ITEM ( '' )  ) ;
#6506=CARTESIAN_POINT ( 'NONE',  ( 1.002407869896990045, -0.1264236179284866091, 1.670767716481669440 ) ) ;
#6507=CARTESIAN_POINT ( 'NONE',  ( 0.6971942568897637749, 2.189545951927499583E-17, 0.2780511810485988278 ) ) ;
#6511=CARTESIAN_POINT ( 'NONE',  ( 0.8759842519685039353, 0.1787899950787401882, 0.6225393700249762796 ) ) ;
#6513=CARTESIAN_POINT ( 'NONE',  ( -0.6971942568897648851, 0.07405724077823318263, 0.9891732282926936071 ) ) ;
#6515=CARTESIAN_POINT ( 'NONE',  ( 0.7185039370078739607, 1.928577636452523993E-17, 1.712598425089322918 ) ) ;
#6519=CARTESIAN_POINT ( 'NONE',  ( 1.002407869896990045, -0.1264236179284866091, 1.636318897584031484 ) ) ;
#6520=CARTESIAN_POINT ( 'NONE',  ( 1.002407869896990045, -0.1264236179284866091, 1.985728346402929168 ) ) ;
#6521=CARTESIAN_POINT ( 'NONE',  ( -1.033464566929133799, 0.000000000000000000, 1.820866141732283561 ) ) ;
#6530=CARTESIAN_POINT ( 'NONE',  ( 0.8759842519685039353, -0.1787899950787401882, 0.6422244093950550958 ) ) ;
#6532=CARTESIAN_POINT ( 'NONE',  ( 1.002407869896990045, 0.1264236179284866091, 0.1500984251430867999 ) ) ;
#6534=CARTESIAN_POINT ( 'NONE',  ( 0.7495606340400177148, 0.1264236179284866091, 0.5487204723871811352 ) ) ;
#6536=CARTESIAN_POINT ( 'NONE',  ( -1.054774247047244540, -0.07405724077823318263, 1.397637795221827295 ) ) ;
#6537=VERTEX_POINT ( 'NONE', #8093 ) ;
#6539=CARTESIAN_POINT ( 'NONE',  ( 1.002407869896990045, 0.1264236179284866091, 1.134350393647023614 ) ) ;
#6541=CARTESIAN_POINT ( 'NONE',  ( -0.9412147342319837628, -0.1574803149606297803, 0.7012795274515276622 ) ) ;
#6542=CARTESIAN_POINT ( 'NONE',  ( -1.033464566929133799, 0.000000000000000000, 0.3543307085538902057 ) ) ;
#6543=CARTESIAN_POINT ( 'NONE',  ( 1.054774247047244540, -0.07405724077823318263, 1.791338582623401177 ) ) ;
#6544=CARTESIAN_POINT ( 'NONE',  ( -0.9412147342319837628, 0.1574803149606300301, 1.355807086614173596 ) ) ;
#6545=CARTESIAN_POINT ( 'NONE',  ( -0.7495606340400177148, 0.1264236179284866091, 0.8243110235682834519 ) ) ;
#6546=CARTESIAN_POINT ( 'NONE',  ( 0.8107537697050254399, -0.1574803149606297803, 1.798720472333418918 ) ) ;
#6547=CARTESIAN_POINT ( 'NONE',  ( -0.8621503180216169016, -0.1583841767695347846, 0.03937007874015844427 ) ) ;
#6548=CARTESIAN_POINT ( 'NONE',  ( 0.6971942568897637749, 2.189545951927499583E-17, 0.3223425196312759144 ) ) ;
#6549=CARTESIAN_POINT ( 'NONE',  ( -0.8759842519685039353, -0.1787899950787401882, 0.09104330703285078152 ) ) ;
#6550=CARTESIAN_POINT ( 'NONE',  ( -0.6971942568897637749, 2.189545951927499583E-17, 0.6323818897100157432 ) ) ;
#6551=CARTESIAN_POINT ( 'NONE',  ( 0.8759842519685039353, 0.1574803149606299191, 1.584645669183810890 ) ) ;
#6552=ORIENTED_EDGE ( 'NONE', *, *, #11248, .F. ) ;
#6556=CARTESIAN_POINT ( 'NONE',  ( 0.6971942568897637749, 2.189545951927499583E-17, 0.7160433070328504623 ) ) ;
#6557=CARTESIAN_POINT ( 'NONE',  ( -0.7495606340400177148, 0.1264236179284866091, 1.690452755851748146 ) ) ;
#6559=EDGE_CURVE ( 'NONE', #27914, #36578, #47416, .T. ) ;
#6561=DIRECTION ( 'NONE',  ( 1.000000000000000000, 0.000000000000000000, -1.822029033848725275E-16 ) ) ;
#6564=ORIENTED_EDGE ( 'NONE', *, *, #7127, .F. ) ;
#6568=EDGE_LOOP ( 'NONE', ( #32510, #35002, #40047, #34155, #34537 ) ) ;
#6570=CARTESIAN_POINT ( 'NONE',  ( 0.8107537697050253289, 0.1574803149606300301, 1.951279527559056870 ) ) ;
#6572=EDGE_CURVE ( 'NONE', #38514, #8914, #33298, .T. ) ;
#6573=CARTESIAN_POINT ( 'NONE',  ( -1.054774247047244540, -0.07405724077823318263, 0.3789370078202520253 ) ) ;
#6574=CARTESIAN_POINT ( 'NONE',  ( -0.7144400811684905594, 0.03384972598730602578, 1.982630989409186251 ) ) ;
#6575=CYLINDRICAL_SURFACE ( 'NONE', #21800, 0.1574803149606299191 ) ;
#6576=CARTESIAN_POINT ( 'NONE',  ( 1.054774247047244540, -0.07405724077823318263, 1.476377952702141449 ) ) ;
#6577=CARTESIAN_POINT ( 'NONE',  ( 1.054774247047244096, 0.000000000000000000, 0.1796259841982051075 ) ) ;
#6578=CARTESIAN_POINT ( 'NONE',  ( -0.7646288533564489232, 0.1113553986120547346, 1.914370078740157632 ) ) ;
#6579=CARTESIAN_POINT ( 'NONE',  ( 0.9412147342319837628, 0.1574803149606300301, 1.670767716535433545 ) ) ;
#6581=CARTESIAN_POINT ( 'NONE',  ( 1.033464566929134687, -0.06523048226347956391, 1.532972440837355066 ) ) ;
#6582=CARTESIAN_POINT ( 'NONE',  ( 0.7646288533564489232, -0.1113553986120547346, 0.7726377951680629685 ) ) ;
#6583=CARTESIAN_POINT ( 'NONE',  ( -0.7185039370078746268, 0.06523048226347956391, 1.710137795168064079 ) ) ;
#6585=CARTESIAN_POINT ( 'NONE',  ( 1.054774247047244540, -0.07405724077823318263, 0.1377952755367876370 ) ) ;
#6586=CARTESIAN_POINT ( 'NONE',  ( 0.8759842519685039353, -0.1787899950787401882, 1.193405511757259951 ) ) ;
#6587=CARTESIAN_POINT ( 'NONE',  ( -0.9412147342319837628, -0.1574803149606297803, 0.5437992124908980207 ) ) ;
#6589=CARTESIAN_POINT ( 'NONE',  ( 0.7185039370078746268, -0.06523048226347956391, 0.4552165353255435698 ) ) ;
#6590=ORIENTED_EDGE ( 'NONE', *, *, #40334, .T. ) ;
#6592=CARTESIAN_POINT ( 'NONE',  ( -1.033464566929133799, 1.928577636452524610E-17, 2.869337061179095023E-17 ) ) ;
#6593=CARTESIAN_POINT ( 'NONE',  ( 0.9342451777971542137, 0.1605301618127781826, 0.03936975837968165887 ) ) ;
#6594=CARTESIAN_POINT ( 'NONE',  ( -0.7646288533564489232, -0.1113553986120547346, 0.3395669290263311213 ) ) ;
#6596=CARTESIAN_POINT ( 'NONE',  ( 1.002407869896990045, -0.1264236179284866091, 1.434547244040724534 ) ) ;
#6597=CARTESIAN_POINT ( 'NONE',  ( -0.9873396505805591694, 0.1113553986120547346, 0.09350393700787401619 ) ) ;
#6598=CARTESIAN_POINT ( 'NONE',  ( -0.8107537697050234415, -0.1574803149606297803, 0.2239173227271187561 ) ) ;
#6603=ORIENTED_EDGE ( 'NONE', *, *, #5035, .F. ) ;
#6606=CARTESIAN_POINT ( 'NONE',  ( 0.7495606340400177148, 0.1264236179284866091, 0.5142716534895434011 ) ) ;
#6607=ORIENTED_EDGE ( 'NONE', *, *, #10130, .T. ) ;
#6608=CARTESIAN_POINT ( 'NONE',  ( -0.6971942568897648851, 0.07405724077823318263, 1.377952755851748368 ) ) ;
#6611=CARTESIAN_POINT ( 'NONE',  ( -0.7495606340400177148, -0.1264236179284866091, 1.154035433017102319 ) ) ;
#6612=CARTESIAN_POINT ( 'NONE',  ( -0.8759842519685039353, -0.1574803149606299191, 0.03937007874015747977 ) ) ;
#6614=CARTESIAN_POINT ( 'NONE',  ( -0.6971942568897648851, -0.07405724077823297447, 1.146653543253323582 ) ) ;
#6616=CARTESIAN_POINT ( 'NONE',  ( -0.6971942568897626646, 0.07405724077823318263, 0.7529527558517473684 ) ) ;
#6617=EDGE_CURVE ( 'NONE', #22586, #4710, #24459, .T. ) ;
#6618=CARTESIAN_POINT ( 'NONE',  ( -0.7646288533564489232, -0.1113553986120547346, 0.3494094488188976277 ) ) ;
#6619=DIRECTION ( 'NONE',  ( 1.822029033848725028E-16, 0.000000000000000000, 1.000000000000000000 ) ) ;
#6623=CARTESIAN_POINT ( 'NONE',  ( -0.7646288533564489232, -0.1113553986120547346, 0.6545275589475906264 ) ) ;
#6625=CARTESIAN_POINT ( 'NONE',  ( -0.6971942568897637749, 2.189545951927499583E-17, 0.5536417322297008115 ) ) ;
#6627=CARTESIAN_POINT ( 'NONE',  ( -1.002407869896990045, -0.1264236179284866091, 1.675688976324189117 ) ) ;
#6630=CARTESIAN_POINT ( 'NONE',  ( 1.033464566929133799, 0.000000000000000000, 0.6397637795275591399 ) ) ;
#6633=CARTESIAN_POINT ( 'NONE',  ( -0.7185039370078739607, 1.928577636452523993E-17, 1.318897637687747926 ) ) ;
#6634=CARTESIAN_POINT ( 'NONE',  ( 1.054774247047244540, 0.07405724077823318263, 0.7775590550643479704 ) ) ;
#6636=LINE ( 'NONE', #35425, #5472 ) ;
#6637=EDGE_CURVE ( 'NONE', #36696, #42555, #31118, .T. ) ;
#6638=CARTESIAN_POINT ( 'NONE',  ( 0.9873396505805591694, 0.1113553986120547346, 0.1624015746956226358 ) ) ;
#6639=CARTESIAN_POINT ( 'NONE',  ( 1.033464566929134687, -0.06523048226347956391, 1.188484251968505268 ) ) ;
#6640=CARTESIAN_POINT ( 'NONE',  ( 0.7479160358676916198, -0.1116595215576704353, 1.985525107522427835 ) ) ;
#6642=CARTESIAN_POINT ( 'NONE',  ( 1.033464566929133799, 0.000000000000000000, 0.3149606298137326843 ) ) ;
#6644=CARTESIAN_POINT ( 'NONE',  ( 0.9500414927467377701, -0.1787899950787401604, 0.6446850393163160442 ) ) ;
#6648=EDGE_CURVE ( 'NONE', #26440, #30928, #5142, .T. ) ;
#6651=CARTESIAN_POINT ( 'NONE',  ( 0.8019270111902717657, 0.1787899950787401604, 1.058070866087969186 ) ) ;
#6660=CARTESIAN_POINT ( 'NONE',  ( -0.6971942568897626646, -0.07405724077823297447, 0.04429133852891373180 ) ) ;
#6662=CARTESIAN_POINT ( 'NONE',  ( 0.6971942568897637749, 2.189545951927499583E-17, 1.975885826717889815 ) ) ;
#6665=CARTESIAN_POINT ( 'NONE',  ( -0.8019270111902716547, -0.1787899950787401604, 1.904527559001354398 ) ) ;
#6666=CARTESIAN_POINT ( 'NONE',  ( -1.054774247047244540, -0.07405724077823318263, 1.476377952702141449 ) ) ;
#6667=CARTESIAN_POINT ( 'NONE',  ( -0.6971942568897626646, -0.07405724077823297447, 0.4035433070328508509 ) ) ;
#6668=CARTESIAN_POINT ( 'NONE',  ( -1.033464566929133799, 0.000000000000000000, 1.811023621939716444 ) ) ;
#6669=CARTESIAN_POINT ( 'NONE',  ( -0.8759842519685039353, -0.1787899950787401882, 1.828248031442299082 ) ) ;
#6670=CARTESIAN_POINT ( 'NONE',  ( -0.7185039370078746268, 0.06523048226347956391, 1.956200787401575880 ) ) ;
#6674=FACE_OUTER_BOUND ( 'NONE', #2026, .T. ) ;
#6676=( BOUNDED_CURVE ( )  B_SPLINE_CURVE ( 2, ( #35703, #21066, #17712, #24221, #46227, #32365, #43100, #5980, #16781 ),
 .UNSPECIFIED., .F., .T. ) 
 B_SPLINE_CURVE_WITH_KNOTS ( ( 3, 2, 2, 2, 3 ),
 ( 0.6700000000000000400, 0.6724999999999999867, 0.6750000000000000444, 0.6774999999999999911, 0.6800000000000000488 ),
 .UNSPECIFIED. ) 
 CURVE ( )  GEOMETRIC_REPRESENTATION_ITEM ( )  RATIONAL_B_SPLINE_CURVE ( ( 1.000000000000000000, 0.9238795325112899581, 1.000000000000000000, 0.9238795325112869605, 1.000000000000000000, 0.9238795325112869605, 1.000000000000000000, 0.9238795325112869605, 1.000000000000000000 ) ) 
 REPRESENTATION_ITEM ( '' )  ) ;
#6677=CARTESIAN_POINT ( 'NONE',  ( -0.8759842519685039353, 0.1787899950787401882, 0.2288385826234019815 ) ) ;
#6679=CARTESIAN_POINT ( 'NONE',  ( -0.6971942568897648851, 0.07405724077823318263, 1.264763779473795813 ) ) ;
#6680=EDGE_LOOP ( 'NONE', ( #13863, #40681, #3190, #33598 ) ) ;
#6686=CARTESIAN_POINT ( 'NONE',  ( -0.9412147342319837628, 0.1574803149606300301, 0.9916338581601894520 ) ) ;
#6687=CARTESIAN_POINT ( 'NONE',  ( -0.7646288533564489232, -0.1113553986120547346, 0.6643700787401575214 ) ) ;
#6690=CARTESIAN_POINT ( 'NONE',  ( 1.033464566929133799, 0.000000000000000000, 1.850393700679873854 ) ) ;
#6693=CARTESIAN_POINT ( 'NONE',  ( 0.7185039370078739607, 1.928577636452523993E-17, 0.2165354329633393804 ) ) ;
#6694=CARTESIAN_POINT ( 'NONE',  ( 0.9412147342319837628, -0.1574803149606297803, 0.7504921259842516346 ) ) ;
#6700=CARTESIAN_POINT ( 'NONE',  ( 1.033464566929134687, 0.06523048226347956391, 0.1599409447743626866 ) ) ;
#6702=ORIENTED_EDGE ( 'NONE', *, *, #5516, .F. ) ;
#6705=CARTESIAN_POINT ( 'NONE',  ( 0.7185039370078739607, 1.928577636452523993E-17, 0.8169291338582678197 ) ) ;
#6710=CARTESIAN_POINT ( 'NONE',  ( 0.7185039370078739607, 1.928577636452523993E-17, 1.043307086506645831 ) ) ;
#6711=CARTESIAN_POINT ( 'NONE',  ( -0.8759842519685039353, 0.1787899950787401882, 0.3469488188438744070 ) ) ;
#6712=VERTEX_POINT ( 'NONE', #42336 ) ;
#6713=CARTESIAN_POINT ( 'NONE',  ( -0.6971942568897648851, -0.07405724077823297447, 1.545275590497416696 ) ) ;
#6714=CARTESIAN_POINT ( 'NONE',  ( 0.6971942568897648851, -0.07405724077823297447, 1.584645669237574994 ) ) ;
#6715=CARTESIAN_POINT ( 'NONE',  ( 0.8759842519685039353, 0.000000000000000000, 4.498031496062992574 ) ) ;
#6716=CARTESIAN_POINT ( 'NONE',  ( -0.7495606340400177148, 0.1264236179284866091, 0.6717519684501732646 ) ) ;
#6717=CARTESIAN_POINT ( 'NONE',  ( 0.8019270111902717657, 0.1787899950787401604, 0.1574803149068664809 ) ) ;
#6719=CARTESIAN_POINT ( 'NONE',  ( 0.8759842519685039353, -0.1787899950787401882, 0.7258858267178898149 ) ) ;
#6720=CARTESIAN_POINT ( 'NONE',  ( -0.9500414927467377701, -0.1787899950787401604, 0.7234251967966300878 ) ) ;
#6724=CARTESIAN_POINT ( 'NONE',  ( -0.8759842519685039353, -0.1787899950787401882, 1.355807086560409491 ) ) ;
#6726=CARTESIAN_POINT ( 'NONE',  ( -0.9412147342319837628, 0.1574803149606300301, 0.5290354330708663122 ) ) ;
#6727=CARTESIAN_POINT ( 'NONE',  ( 0.8759842519685039353, -0.1787899950787401882, 1.513287401521039355 ) ) ;
#6730=ORIENTED_EDGE ( 'NONE', *, *, #12641, .F. ) ;
#6731=ADVANCED_FACE ( 'NONE', ( #24154 ), #29206, .T. ) ;
#6736=CARTESIAN_POINT ( 'NONE',  ( 0.9500414927467378812, 0.1787899950787401604, 1.407480314906865981 ) ) ;
#6738=AXIS2_PLACEMENT_3D ( 'NONE', #20587, #46218, #20821 ) ;
#6743=CARTESIAN_POINT ( 'NONE',  ( 0.8759842519685039353, 0.1787899950787401882, 0.2682086613635594752 ) ) ;
#6748=CARTESIAN_POINT ( 'NONE',  ( 0.8759842519685039353, -0.1787899950787401882, 0.6422244093950550958 ) ) ;
#6750=CARTESIAN_POINT ( 'NONE',  ( -0.6971942568897637749, 2.189545951927499583E-17, 0.9916338582139527791 ) ) ;
#6754=CARTESIAN_POINT ( 'NONE',  ( -0.8890799276390084493, -0.1744314460652860166, 1.988413549619085785 ) ) ;
#6756=CARTESIAN_POINT ( 'NONE',  ( 0.6971942568897648851, 0.07405724077823318263, 1.619094488135213838 ) ) ;
#6759=CARTESIAN_POINT ( 'NONE',  ( 1.054774247047244096, 0.000000000000000000, 0.5339566928596221063 ) ) ;
#6761=VERTEX_POINT ( 'NONE', #14062 ) ;
#6763=ORIENTED_EDGE ( 'NONE', *, *, #162, .F. ) ;
#6764=ADVANCED_FACE ( 'NONE', ( #35643 ), #32046, .T. ) ;
#6768=CARTESIAN_POINT ( 'NONE',  ( 0.8019270111902717657, 0.1787899950787401604, 0.6249999999462366729 ) ) ;
#6770=CARTESIAN_POINT ( 'NONE',  ( 0.6971942568897626646, 0.07405724077823318263, 0.04429133852891373180 ) ) ;
#6772=CARTESIAN_POINT ( 'NONE',  ( 0.8019270111902716547, 0.1787899950787401604, 0.5856299212060785964 ) ) ;
#6773=CARTESIAN_POINT ( 'NONE',  ( -0.7495606340400177148, -0.1264236179284866091, 1.582185039316315045 ) ) ;
#6774=ORIENTED_EDGE ( 'NONE', *, *, #30947, .F. ) ;
#6775=CARTESIAN_POINT ( 'NONE',  ( 1.033464566929134687, -0.06523048226347956391, 0.1648622047244094890 ) ) ;
#6776=CARTESIAN_POINT ( 'NONE',  ( 0.6971942568897648851, 0.07405724077823318263, 1.107283464513165949 ) ) ;
#6777=CARTESIAN_POINT ( 'NONE',  ( 0.6971942568897637749, 2.189545951927499583E-17, 1.774114173174582643 ) ) ;
#6778=CARTESIAN_POINT ( 'NONE',  ( -1.033464566929134687, 0.06523048226347956391, 0.5634842519685042683 ) ) ;
#6779=CARTESIAN_POINT ( 'NONE',  ( -0.8759842519685039353, -0.1787899950787401882, 0.8390748030958424808 ) ) ;
#6780=CARTESIAN_POINT ( 'NONE',  ( 1.033464566929133799, 1.928577636452524610E-17, 4.498031496062992574 ) ) ;
#6781=CARTESIAN_POINT ( 'NONE',  ( 0.8019270111902716547, -0.1787899950787401604, 0.2903543306548980185 ) ) ;
#6782=CARTESIAN_POINT ( 'NONE',  ( -0.7495606340400177148, -0.1264236179284866091, 0.2829724408911185041 ) ) ;
#6783=CARTESIAN_POINT ( 'NONE',  ( -1.054774247047244540, 0.07405724077823318263, 0.6545275590013545086 ) ) ;
#6784=CARTESIAN_POINT ( 'NONE',  ( 0.7646288533564489232, -0.1113553986120547346, 1.520669291231054876 ) ) ;
#6785=VERTEX_POINT ( 'NONE', #46637 ) ;
#6788=CARTESIAN_POINT ( 'NONE',  ( 0.9500414927467378812, -0.1787899950787401604, 0.8464566928596233275 ) ) ;
#6789=CARTESIAN_POINT ( 'NONE',  ( -0.7495606340400177148, -0.1264236179284866091, 1.857775590497417362 ) ) ;
#6790=( BOUNDED_CURVE ( )  B_SPLINE_CURVE ( 2, ( #31253, #9674, #45830, #13039, #35318, #5833, #20441, #35077, #2225 ),
 .UNSPECIFIED., .F., .F. ) 
 B_SPLINE_CURVE_WITH_KNOTS ( ( 3, 2, 2, 2, 3 ),
 ( 0.4099999999999999756, 0.4124999999999999778, 0.4149999999999999800, 0.4174999999999999822, 0.4199999999999999845 ),
 .UNSPECIFIED. ) 
 CURVE ( )  GEOMETRIC_REPRESENTATION_ITEM ( )  RATIONAL_B_SPLINE_CURVE ( ( 1.000000000000000000, 0.9238795325112879597, 1.000000000000000000, 0.9238795325112869605, 1.000000000000000000, 0.9238795325112869605, 1.000000000000000000, 0.9238795325112869605, 1.000000000000000000 ) ) 
 REPRESENTATION_ITEM ( '' )  ) ;
#6796=VERTEX_POINT ( 'NONE', #129 ) ;
#6798=CARTESIAN_POINT ( 'NONE',  ( 1.002407869896990045, 0.1264236179284866091, 1.090059055064346527 ) ) ;
#6801=CARTESIAN_POINT ( 'NONE',  ( 0.8107537697050253289, -0.1574803149606297803, 1.926673228346456490 ) ) ;
#6803=AXIS2_PLACEMENT_3D ( 'NONE', #4134, #63, #3906 ) ;
#6805=CARTESIAN_POINT ( 'NONE',  ( -0.6971942568897648851, 0.07405724077823318263, 0.5167322834108035723 ) ) ;
#6806=CARTESIAN_POINT ( 'NONE',  ( -0.7104269446534671184, 0.008049294727412099545, 1.983122017755077904 ) ) ;
#6809=CARTESIAN_POINT ( 'NONE',  ( 1.054774247047244540, 0.07405724077823318263, 1.560039370024976835 ) ) ;
#6810=CARTESIAN_POINT ( 'NONE',  ( -0.7646288533564489232, 0.1113553986120547346, 0.6053149605223937524 ) ) ;
#6811=EDGE_CURVE ( 'NONE', #23847, #19846, #45860, .T. ) ;
#6813=DIRECTION ( 'NONE',  ( 1.822029033848725028E-16, 0.000000000000000000, 1.000000000000000000 ) ) ;
#6815=CARTESIAN_POINT ( 'NONE',  ( -0.9873396505805591694, -0.1113553986120547346, 1.806102362097196767 ) ) ;
#6816=CARTESIAN_POINT ( 'NONE',  ( 0.9500414927467378812, -0.1787899950787401604, 0.2116141731745827814 ) ) ;
#6817=CARTESIAN_POINT ( 'NONE',  ( 0.7023594456989278312, -0.01011419101508406575, 0.03936580841072691989 ) ) ;
#6818=CARTESIAN_POINT ( 'NONE',  ( 0.9500414927467377701, -0.1787899950787401604, 1.077755905458048113 ) ) ;
#6819=CARTESIAN_POINT ( 'NONE',  ( -1.033464566929134687, 0.06523048226347956391, 1.941437007874014187 ) ) ;
#6820=CARTESIAN_POINT ( 'NONE',  ( -1.033464566929133799, 0.000000000000000000, 1.929133858160188897 ) ) ;
#6821=CARTESIAN_POINT ( 'NONE',  ( -0.6971942568897648851, -0.07405724077823297447, 1.146653543253323582 ) ) ;
#6822=CARTESIAN_POINT ( 'NONE',  ( 0.7185039370078746268, 0.06523048226347956391, 0.4896653542231815259 ) ) ;
#6825=CARTESIAN_POINT ( 'NONE',  ( -1.033464566929134687, -0.06523048226347956391, 0.4699803148531029318 ) ) ;
#6826=CARTESIAN_POINT ( 'NONE',  ( -0.9873396505805591694, -0.1113553986120547346, 1.540354330708661568 ) ) ;
#6827=CARTESIAN_POINT ( 'NONE',  ( 0.7495606340400177148, -0.1264236179284866091, 1.464074803095842370 ) ) ;
#6829=CARTESIAN_POINT ( 'NONE',  ( -0.9873396505805591694, -0.1113553986120547346, 0.2312992124908980207 ) ) ;
#6836=ORIENTED_EDGE ( 'NONE', *, *, #34771, .T. ) ;
#6837=CARTESIAN_POINT ( 'NONE',  ( 0.8759842519685039353, -0.1787899950787401882, 0.5684055117572598403 ) ) ;
#6840=CARTESIAN_POINT ( 'NONE',  ( -1.002407869896990045, -0.1264236179284866091, 1.124507873961984261 ) ) ;
#6841=CARTESIAN_POINT ( 'NONE',  ( -0.8759842519685039353, -0.1574803149606299191, 0.1968503937007874127 ) ) ;
#6842=CARTESIAN_POINT ( 'NONE',  ( -1.002407869896990045, -0.1264236179284866091, 1.158956692859621995 ) ) ;
#6844=CARTESIAN_POINT ( 'NONE',  ( -1.054774247047244540, -0.07405724077823318263, 0.8120078739619844832 ) ) ;
#6845=ADVANCED_FACE ( 'NONE', ( #6384 ), #36110, .T. ) ;
#6846=CARTESIAN_POINT ( 'NONE',  ( -0.6971942568897637749, 2.189545951927499583E-17, 0.2436023621509610382 ) ) ;
#6850=ORIENTED_EDGE ( 'NONE', *, *, #11781, .T. ) ;
#6855=CARTESIAN_POINT ( 'NONE',  ( -0.9412147342319837628, -0.1574803149606297803, 0.3469488187901108023 ) ) ;
#6856=CARTESIAN_POINT ( 'NONE',  ( -0.6971942568897626646, -0.07405724077823297447, 0.5954724408911187261 ) ) ;
#6857=LINE ( 'NONE', #14782, #2387 ) ;
#6859=CARTESIAN_POINT ( 'NONE',  ( -1.002407869896990045, -0.1264236179284866091, 1.754429133804503715 ) ) ;
#6864=CARTESIAN_POINT ( 'NONE',  ( -0.6971942568897626646, 0.07405724077823318263, 0.1230314960092287191 ) ) ;
#6865=CARTESIAN_POINT ( 'NONE',  ( 0.9412147342319837628, -0.1574803149606297803, 0.6323818897637792924 ) ) ;
#6867=CARTESIAN_POINT ( 'NONE',  ( 0.9412147342319837628, 0.1574803149606300301, 0.6373031494987716483 ) ) ;
#6868=CARTESIAN_POINT ( 'NONE',  ( -1.033464566929134687, 0.06523048226347956391, 1.341043306979086136 ) ) ;
#6869=CARTESIAN_POINT ( 'NONE',  ( 0.8759842519685039353, 0.1787899950787401882, 0.7849409448281259305 ) ) ;
#6874=CARTESIAN_POINT ( 'NONE',  ( 0.7646288533564489232, -0.1113553986120547346, 1.333661417322834719 ) ) ;
#6875=CARTESIAN_POINT ( 'NONE',  ( 0.7862461320375258023, -0.1462158868424255076, 1.986452941589757826 ) ) ;
#6878=CARTESIAN_POINT ( 'NONE',  ( 1.054774247047244540, 0.07405724077823318263, 0.6938976377415124741 ) ) ;
#6880=CARTESIAN_POINT ( 'NONE',  ( -0.9873396505805591694, 0.1113553986120547346, 0.6840551181102363376 ) ) ;
#6884=CARTESIAN_POINT ( 'NONE',  ( 0.9873396505805591694, -0.1113553986120547346, 1.737204724409448842 ) ) ;
#6885=CARTESIAN_POINT ( 'NONE',  ( 0.8759842519685039353, -0.1574803149606299191, 0.7086614173228346081 ) ) ;
#6886=CARTESIAN_POINT ( 'NONE',  ( 0.8019270111902717657, -0.1787899950787401604, 0.9153543306548987957 ) ) ;
#6887=EDGE_LOOP ( 'NONE', ( #17059, #29288, #13911, #36469 ) ) ;
#6888=CARTESIAN_POINT ( 'NONE',  ( -0.7185039370078739607, 0.000000000000000000, -2.869337061179095023E-17 ) ) ;
#6893=CARTESIAN_POINT ( 'NONE',  ( -0.8019270111902717657, 0.1787899950787401604, 0.1525590550643468046 ) ) ;
#6894=ORIENTED_EDGE ( 'NONE', *, *, #35349, .F. ) ;
#6896=VERTEX_POINT ( 'NONE', #3743 ) ;
#6898=CARTESIAN_POINT ( 'NONE',  ( -0.7185039370078739607, 1.928577636452523993E-17, 1.476377952648377789 ) ) ;
#6899=CARTESIAN_POINT ( 'NONE',  ( -0.6971942568897648851, -0.07405724077823297447, 1.658464566875369472 ) ) ;
#6900=CARTESIAN_POINT ( 'NONE',  ( -0.8019270111902717657, 0.1787899950787401604, 1.097440944828127041 ) ) ;
#6903=CARTESIAN_POINT ( 'NONE',  ( -0.7495606340400177148, -0.1264236179284866091, 1.902066929080094448 ) ) ;
#6904=CARTESIAN_POINT ( 'NONE',  ( -0.9412147342319837628, 0.1574803149606300301, 1.473917322834645605 ) ) ;
#6905=CARTESIAN_POINT ( 'NONE',  ( -0.8107537697050253289, 0.1574803149606300301, 1.951279527559056870 ) ) ;
#6906=CARTESIAN_POINT ( 'NONE',  ( -0.9873396505805591694, -0.1113553986120547346, 1.894685039370078927 ) ) ;
#6913=CARTESIAN_POINT ( 'NONE',  ( -0.8019270111902717657, -0.1787899950787401604, 0.08858267711159097113 ) ) ;
#6916=CARTESIAN_POINT ( 'NONE',  ( -1.054774247047244540, -0.07405724077823318263, 1.441929133804504604 ) ) ;
#6917=ORIENTED_EDGE ( 'NONE', *, *, #32102, .T. ) ;
#6922=CARTESIAN_POINT ( 'NONE',  ( 0.7646288533564489232, 0.1113553986120547346, 0.3789370078740157410 ) ) ;
#6925=CARTESIAN_POINT ( 'NONE',  ( -0.7185039370078746268, 0.06523048226347956391, 0.9227362203649142058 ) ) ;
#6926=CARTESIAN_POINT ( 'NONE',  ( -0.9412147342319837628, -0.1574803149606297803, 0.9473425196850395746 ) ) ;
#6927=CARTESIAN_POINT ( 'NONE',  ( 0.7495606340400177148, 0.1264236179284866091, 0.4749015747493858242 ) ) ;
#6929=CARTESIAN_POINT ( 'NONE',  ( 1.033464566929134687, -0.06523048226347956391, 1.769192913278299306 ) ) ;
#6932=CARTESIAN_POINT ( 'NONE',  ( 0.9873396505805591694, -0.1113553986120547346, 0.8710629921259842590 ) ) ;
#6934=CARTESIAN_POINT ( 'NONE',  ( 0.7185039370078739607, 1.928577636452523993E-17, 1.476377952648377789 ) ) ;
#6937=DIRECTION ( 'NONE',  ( -1.000000000000000000, 0.000000000000000000, 0.000000000000000000 ) ) ;
#6939=CARTESIAN_POINT ( 'NONE',  ( 0.8107537697050253289, 0.1574803149606300301, 0.1697834644594022058 ) ) ;
#6940=VERTEX_POINT ( 'NONE', #12132 ) ;
#6945=CARTESIAN_POINT ( 'NONE',  ( -0.8107537697050234415, -0.1574803149606297803, 0.06643700776648873985 ) ) ;
#6948=CARTESIAN_POINT ( 'NONE',  ( 0.9412147342319837628, -0.1574803149606297803, 0.8981299211523156023 ) ) ;
#6950=CARTESIAN_POINT ( 'NONE',  ( -0.8019270111902717657, -0.1787899950787401604, 0.4035433070328508509 ) ) ;
#6953=CARTESIAN_POINT ( 'NONE',  ( -0.6971942568897637749, 2.189545951927499583E-17, 1.660925196796630088 ) ) ;
#6955=CARTESIAN_POINT ( 'NONE',  ( 0.6971942568897648851, 0.07405724077823318263, 1.619094488135213838 ) ) ;
#6957=CARTESIAN_POINT ( 'NONE',  ( -1.054774247047244540, -0.07405724077823318263, 0.7726377952218265177 ) ) ;
#6958=CARTESIAN_POINT ( 'NONE',  ( 0.9500414927467378812, -0.1787899950787401604, 0.1771653542769452139 ) ) ;
#6960=CARTESIAN_POINT ( 'NONE',  ( 0.7495606340400177148, 0.1264236179284866091, 0.7898622046706456068 ) ) ;
#6961=CARTESIAN_POINT ( 'NONE',  ( -0.9500414927467377701, 0.1787899950787401604, 0.6594488188438737408 ) ) ;
#6962=CARTESIAN_POINT ( 'NONE',  ( 1.033464566929133799, 1.928577636452524610E-17, 4.498031496062992574 ) ) ;
#6963=( BOUNDED_CURVE ( )  B_SPLINE_CURVE ( 2, ( #6339, #9956, #10195, #28417, #46831, #16909, #24801, #6581, #35827 ),
 .UNSPECIFIED., .F., .F. ) 
 B_SPLINE_CURVE_WITH_KNOTS ( ( 3, 2, 2, 2, 3 ),
 ( 0.7500000000000000000, 0.7524999999999999467, 0.7550000000000000044, 0.7574999999999999512, 0.7600000000000000089 ),
 .UNSPECIFIED. ) 
 CURVE ( )  GEOMETRIC_REPRESENTATION_ITEM ( )  RATIONAL_B_SPLINE_CURVE ( ( 1.000000000000000000, 0.9238795325112899581, 1.000000000000000000, 0.9238795325112869605, 1.000000000000000000, 0.9238795325112869605, 1.000000000000000000, 0.9238795325112869605, 1.000000000000000000 ) ) 
 REPRESENTATION_ITEM ( '' )  ) ;
#6964=CARTESIAN_POINT ( 'NONE',  ( -0.8759842519685039353, -0.1574803149606299191, 0.8661417322834645827 ) ) ;
#6966=CARTESIAN_POINT ( 'NONE',  ( -0.8107537697050253289, 0.1574803149606300301, 1.941437007766490863 ) ) ;
#6968=CARTESIAN_POINT ( 'NONE',  ( -0.9873396505805591694, 0.1113553986120547346, 1.510826771653543288 ) ) ;
#6969=CARTESIAN_POINT ( 'NONE',  ( -0.7185039370078746268, 0.06523048226347956391, 0.4601377952755902889 ) ) ;
#6970=CARTESIAN_POINT ( 'NONE',  ( 1.054774247047244540, 0.07405724077823318263, 1.446850393647023836 ) ) ;
#6974=EDGE_CURVE ( 'NONE', #3940, #32303, #40946, .T. ) ;
#6975=AXIS2_PLACEMENT_3D ( 'NONE', #32062, #13835, #28478 ) ;
#6978=EDGE_CURVE ( 'NONE', #37979, #8121, #26584, .T. ) ;
#6985=CARTESIAN_POINT ( 'NONE',  ( -0.9873396505805591694, -0.1113553986120547346, 0.9793307085538898171 ) ) ;
#6986=CARTESIAN_POINT ( 'NONE',  ( 0.6971942568897626646, -0.07405724077823297447, 0.3592519684501735977 ) ) ;
#6991=CARTESIAN_POINT ( 'NONE',  ( 0.8759842519685039353, -0.1787899950787401882, 0.6815944881352126172 ) ) ;
#6992=CARTESIAN_POINT ( 'NONE',  ( -0.6971942568897648851, -0.07405724077823297447, 0.9547244093950545407 ) ) ;
#6996=CARTESIAN_POINT ( 'NONE',  ( 1.054774247047244096, 0.000000000000000000, 1.680610236166708793 ) ) ;
#7004=CARTESIAN_POINT ( 'NONE',  ( -0.6971942568897637749, 2.189545951927499583E-17, 0.4404527558517480901 ) ) ;
#7005=CARTESIAN_POINT ( 'NONE',  ( 1.054774247047244540, -0.07405724077823318263, 0.6102362204186774219 ) ) ;
#7007=CARTESIAN_POINT ( 'NONE',  ( 0.6971942568897637749, 2.189545951927499583E-17, 0.04675196845017354913 ) ) ;
#7008=CARTESIAN_POINT ( 'NONE',  ( -1.033464566929133799, 0.000000000000000000, 1.535433070758614127 ) ) ;
#7010=CARTESIAN_POINT ( 'NONE',  ( -0.8019270111902717657, 0.1787899950787401604, 1.648622047190331230 ) ) ;
#7011=VERTEX_POINT ( 'NONE', #22667 ) ;
#7012=CARTESIAN_POINT ( 'NONE',  ( -0.8019270111902717657, -0.1787899950787401604, 1.156496062938362046 ) ) ;
#7014=CARTESIAN_POINT ( 'NONE',  ( 1.054774247047244096, 0.000000000000000000, 1.129429133804503937 ) ) ;
#7016=CARTESIAN_POINT ( 'NONE',  ( -0.7185039370078746268, -0.06523048226347956391, 0.6520669290263312323 ) ) ;
#7018=AXIS2_PLACEMENT_3D ( 'NONE', #10683, #46370, #3477 ) ;
#7020=CARTESIAN_POINT ( 'NONE',  ( 0.6971942568897637749, 2.189545951927499583E-17, 1.892224409395055096 ) ) ;
#7021=CARTESIAN_POINT ( 'NONE',  ( -0.7185039370078746268, 0.06523048226347956391, 0.5388779527559054427 ) ) ;
#7022=CARTESIAN_POINT ( 'NONE',  ( -0.8019270111902717657, 0.1787899950787401604, 0.8612204723871809131 ) ) ;
#7024=CARTESIAN_POINT ( 'NONE',  ( 0.8019270111902716547, -0.1787899950787401604, 0.3297244093950555954 ) ) ;
#7025=CARTESIAN_POINT ( 'NONE',  ( -0.9500414927467377701, -0.1787899950787401604, 0.2903543306548980185 ) ) ;
#7026=CARTESIAN_POINT ( 'NONE',  ( -0.6971942568897626646, 0.07405724077823318263, 0.7480314960092282472 ) ) ;
#7027=CARTESIAN_POINT ( 'NONE',  ( 0.7185039370078746268, -0.06523048226347956391, 1.596948818790111080 ) ) ;
#7030=CARTESIAN_POINT ( 'NONE',  ( 1.002407869896990045, 0.1264236179284866091, 0.7406496062454487328 ) ) ;
#7031=CARTESIAN_POINT ( 'NONE',  ( 0.9500414927467377701, 0.1787899950787401604, 1.018700787347811110 ) ) ;
#7032=CARTESIAN_POINT ( 'NONE',  ( -1.054774247047244540, -0.07405724077823318263, 1.830708661363559253 ) ) ;
#7033=ADVANCED_FACE ( 'NONE', ( #4915 ), #4426, .T. ) ;
#7034=CARTESIAN_POINT ( 'NONE',  ( 0.6971942568897648851, -0.07405724077823297447, 1.973425196796630088 ) ) ;
#7037=CARTESIAN_POINT ( 'NONE',  ( 0.8759842519685039353, 0.1574803149606299191, 1.318897637795275690 ) ) ;
#7039=EDGE_LOOP ( 'NONE', ( #45728, #41884, #45115, #35610 ) ) ;
#7042=EDGE_LOOP ( 'NONE', ( #11508, #2865, #27213, #27416 ) ) ;
#7043=CARTESIAN_POINT ( 'NONE',  ( 0.8759842519685039353, 0.1787899950787401882, 1.213090551127338435 ) ) ;
#7047=CARTESIAN_POINT ( 'NONE',  ( 1.002407869896990045, -0.1264236179284866091, 0.09596456687537027741 ) ) ;
#7049=AXIS2_PLACEMENT_3D ( 'NONE', #2171, #44829, #41452 ) ;
#7052=CARTESIAN_POINT ( 'NONE',  ( -0.8759842519685039353, 0.1787899950787401882, 0.5093503936470236138 ) ) ;
#7055=CARTESIAN_POINT ( 'NONE',  ( 0.8759842519685039353, -0.1787899950787401882, 1.277066929080094448 ) ) ;
#7056=CARTESIAN_POINT ( 'NONE',  ( 0.8759842519685039353, -0.1787899950787401882, 1.665846456639149764 ) ) ;
#7057=CARTESIAN_POINT ( 'NONE',  ( -0.8759842519685039353, 0.1574803149606299191, 0.6003937006798740761 ) ) ;
#7058=FACE_OUTER_BOUND ( 'NONE', #33594, .T. ) ;
#7061=CARTESIAN_POINT ( 'NONE',  ( -1.033464566929134687, -0.06523048226347956391, 1.769192913278299306 ) ) ;
#7062=CARTESIAN_POINT ( 'NONE',  ( 1.054774247047244096, 0.000000000000000000, 0.2189960629383626012 ) ) ;
#7063=CARTESIAN_POINT ( 'NONE',  ( 0.6971942568897637749, 2.189545951927499583E-17, 1.183562992072220599 ) ) ;
#7065=CARTESIAN_POINT ( 'NONE',  ( -1.054774247047244540, 0.07405724077823318263, 1.205708661363558365 ) ) ;
#7066=CARTESIAN_POINT ( 'NONE',  ( 1.033464566929133799, 0.000000000000000000, 0.4724409447743622148 ) ) ;
#7067=ORIENTED_EDGE ( 'NONE', *, *, #19315, .F. ) ;
#7068=LINE ( 'NONE', #6592, #24563 ) ;
#7069=CARTESIAN_POINT ( 'NONE',  ( 0.9674136657275992368, 0.1412476989763037649, 0.03936995337663032335 ) ) ;
#7070=CARTESIAN_POINT ( 'NONE',  ( 0.8759842519685039353, -0.1574803149606299191, 0.2755905511811023723 ) ) ;
#7071=CARTESIAN_POINT ( 'NONE',  ( -0.7185039370078746268, -0.06523048226347956391, 0.3764763778452286935 ) ) ;
#7072=ORIENTED_EDGE ( 'NONE', *, *, #45431, .F. ) ;
#7073=CARTESIAN_POINT ( 'NONE',  ( 1.054774247047244540, -0.07405724077823318263, 1.437007873961985371 ) ) ;
#7074=CARTESIAN_POINT ( 'NONE',  ( -1.033464566929134687, 0.06523048226347956391, 1.154035433070866423 ) ) ;
#7075=CARTESIAN_POINT ( 'NONE',  ( -1.033464566929134687, -0.06523048226347956391, 1.779035433070867311 ) ) ;
#7076=FACE_OUTER_BOUND ( 'NONE', #18821, .T. ) ;
#7081=( BOUNDED_CURVE ( )  B_SPLINE_CURVE ( 2, ( #31833, #3033, #35659, #36124, #6161, #17425, #46650, #39685, #39226 ),
 .UNSPECIFIED., .F., .T. ) 
 B_SPLINE_CURVE_WITH_KNOTS ( ( 3, 2, 2, 2, 3 ),
 ( 0.8000000000000000444, 0.8024999999999999911, 0.8050000000000000488, 0.8074999999999999956, 0.8100000000000000533 ),
 .UNSPECIFIED. ) 
 CURVE ( )  GEOMETRIC_REPRESENTATION_ITEM ( )  RATIONAL_B_SPLINE_CURVE ( ( 1.000000000000000000, 0.9238795325112869605, 1.000000000000000000, 0.9238795325112869605, 1.000000000000000000, 0.9238795325112869605, 1.000000000000000000, 0.9238795325112829637, 1.000000000000000000 ) ) 
 REPRESENTATION_ITEM ( '' )  ) ;
#7083=EDGE_LOOP ( 'NONE', ( #26120, #43385, #40436, #24323 ) ) ;
#7085=DIRECTION ( 'NONE',  ( 0.000000000000000000, 0.000000000000000000, -1.000000000000000000 ) ) ;
#7086=CARTESIAN_POINT ( 'NONE',  ( 1.054774247047244540, 0.07405724077823318263, 0.5413385826234012876 ) ) ;
#7088=CARTESIAN_POINT ( 'NONE',  ( -1.002407869896990045, -0.1264236179284866091, 1.473917322780881722 ) ) ;
#7090=CARTESIAN_POINT ( 'NONE',  ( -0.8019270111902717657, -0.1787899950787401604, 1.156496062938362046 ) ) ;
#7091=VECTOR ( 'NONE', #34541, 39.37007874015748143 ) ;
#7092=CARTESIAN_POINT ( 'NONE',  ( -0.7185039370078739607, 1.928577636452523993E-17, 0.1870078740157480324 ) ) ;
#7095=CARTESIAN_POINT ( 'NONE',  ( -1.002407869896990045, 0.1264236179284866091, 0.2288385826234019815 ) ) ;
#7096=CARTESIAN_POINT ( 'NONE',  ( 1.033464566929133799, 0.000000000000000000, 1.653543306979086580 ) ) ;
#7103=EDGE_CURVE ( 'NONE', #46991, #32643, #1799, .T. ) ;
#7105=( BOUNDED_CURVE ( )  B_SPLINE_CURVE ( 2, ( #33215, #19019, #26244, #794, #33919, #22384, #11625, #22147, #30109 ),
 .UNSPECIFIED., .F., .T. ) 
 B_SPLINE_CURVE_WITH_KNOTS ( ( 3, 2, 2, 2, 3 ),
 ( 0.8499999999999999778, 0.8525000000000000355, 0.8549999999999999822, 0.8575000000000000400, 0.8599999999999999867 ),
 .UNSPECIFIED. ) 
 CURVE ( )  GEOMETRIC_REPRESENTATION_ITEM ( )  RATIONAL_B_SPLINE_CURVE ( ( 1.000000000000000000, 0.9238795325112939549, 1.000000000000000000, 0.9238795325112869605, 1.000000000000000000, 0.9238795325112869605, 1.000000000000000000, 0.9238795325112869605, 1.000000000000000000 ) ) 
 REPRESENTATION_ITEM ( '' )  ) ;
#7106=CARTESIAN_POINT ( 'NONE',  ( -1.054774247047244540, 0.07405724077823318263, 0.8120078739619844832 ) ) ;
#7108=ORIENTED_EDGE ( 'NONE', *, *, #1961, .T. ) ;
#7109=CARTESIAN_POINT ( 'NONE',  ( -1.054774247047244540, 0.07405724077823318263, 1.840551181048599938 ) ) ;
#7110=CARTESIAN_POINT ( 'NONE',  ( 0.7185039370078739607, 1.928577636452523993E-17, 1.328740157480315043 ) ) ;
#7111=CARTESIAN_POINT ( 'NONE',  ( -0.7495606340400177148, 0.1264236179284866091, 0.04183070860765386589 ) ) ;
#7113=CARTESIAN_POINT ( 'NONE',  ( 0.8759842519685039353, -0.1574803149606299191, 0.6692913385826771977 ) ) ;
#7115=CARTESIAN_POINT ( 'NONE',  ( -0.8759842519685039353, 0.1574803149606299191, 0.4035433069790866356 ) ) ;
#7116=CARTESIAN_POINT ( 'NONE',  ( -0.8107537697050253289, -0.1574803149606297803, 1.326279527451528661 ) ) ;
#7117=CARTESIAN_POINT ( 'NONE',  ( 0.9500414927467378812, 0.1787899950787401604, 0.7431102361667091261 ) ) ;
#7122=CARTESIAN_POINT ( 'NONE',  ( 0.7185039370078739607, 0.000000000000000000, 4.498031496062992574 ) ) ;
#7123=CARTESIAN_POINT ( 'NONE',  ( 0.7646288533564489232, 0.1113553986120547346, 1.323818897637795367 ) ) ;
#7124=CARTESIAN_POINT ( 'NONE',  ( 0.7775410103530361328, -0.1400450413635906666, 1.986256998439228871 ) ) ;
#7126=CARTESIAN_POINT ( 'NONE',  ( 1.033464566929134687, 0.06523048226347956391, 0.3174212597349925224 ) ) ;
#7127=EDGE_CURVE ( 'NONE', #20507, #36580, #13147, .T. ) ;
#7128=AXIS2_PLACEMENT_3D ( 'NONE', #11761, #16470, #19812 ) ;
#7129=CARTESIAN_POINT ( 'NONE',  ( 0.9500414927467377701, -0.1787899950787401604, 0.7234251967966300878 ) ) ;
#7136=CARTESIAN_POINT ( 'NONE',  ( 0.8759842519685039353, -0.1787899950787401882, 1.035925196796629866 ) ) ;
#7137=DIRECTION ( 'NONE',  ( 1.000000000000000000, 0.000000000000000000, 0.000000000000000000 ) ) ;
#7142=CARTESIAN_POINT ( 'NONE',  ( -0.8019270111902717657, -0.1787899950787401604, 0.1673228345919057225 ) ) ;
#7145=CARTESIAN_POINT ( 'NONE',  ( -1.002407869896990045, -0.1264236179284866091, 1.911909448765133801 ) ) ;
#7146=CARTESIAN_POINT ( 'NONE',  ( -0.7495606340400177148, 0.1264236179284866091, 1.729822834591905556 ) ) ;
#7147=CARTESIAN_POINT ( 'NONE',  ( -0.6971942568897648851, 0.07405724077823318263, 1.102362204670646495 ) ) ;
#7148=CARTESIAN_POINT ( 'NONE',  ( -1.002407869896990045, 0.1264236179284866091, 0.4256889763241890057 ) ) ;
#7149=EDGE_CURVE ( 'NONE', #4172, #9090, #16772, .T. ) ;
#7151=CARTESIAN_POINT ( 'NONE',  ( -0.7495606340400177148, -0.1264236179284866091, 1.980807086560409491 ) ) ;
#7153=CARTESIAN_POINT ( 'NONE',  ( -0.7185039370078746268, 0.06523048226347956391, 1.916830708661418248 ) ) ;
#7154=DIRECTION ( 'NONE',  ( 0.8660254037844389297, 0.000000000000000000, -0.4999999999999994449 ) ) ;
#7157=CARTESIAN_POINT ( 'NONE',  ( -1.033464566929133799, 0.000000000000000000, 0.9842519683964094934 ) ) ;
#7161=CARTESIAN_POINT ( 'NONE',  ( -0.6971942568897626646, -0.07405724077823297447, 0.2805118109698587214 ) ) ;
#7164=CARTESIAN_POINT ( 'NONE',  ( -0.6971942568897648851, 0.07405724077823318263, 1.343503936954111966 ) ) ;
#7165=ORIENTED_EDGE ( 'NONE', *, *, #45760, .T. ) ;
#7170=CARTESIAN_POINT ( 'NONE',  ( 1.033464566929133799, 0.000000000000000000, 0.4035433070866141780 ) ) ;
#7173=CARTESIAN_POINT ( 'NONE',  ( -1.033464566929134687, -0.06523048226347956391, 0.9030511809948348345 ) ) ;
#7175=CARTESIAN_POINT ( 'NONE',  ( 1.033464566929133799, 0.000000000000000000, 1.771653543199558811 ) ) ;
#7176=ORIENTED_EDGE ( 'NONE', *, *, #38109, .F. ) ;
#7178=CARTESIAN_POINT ( 'NONE',  ( -1.033464566929133799, 0.000000000000000000, 1.417322834538141674 ) ) ;
#7179=CARTESIAN_POINT ( 'NONE',  ( 0.8759842519685039353, 0.1574803149606299191, 0.8070866141732283561 ) ) ;
#7180=CARTESIAN_POINT ( 'NONE',  ( -1.033464566929134687, 0.06523048226347956391, 1.075295275590550048 ) ) ;
#7181=LINE ( 'NONE', #14612, #14096 ) ;
#7183=CARTESIAN_POINT ( 'NONE',  ( 0.7185039370078746268, 0.06523048226347956391, 0.2534448817822366751 ) ) ;
#7186=CARTESIAN_POINT ( 'NONE',  ( 0.7185039370078692977, 0.06523048226347515077, 1.906988188868851797 ) ) ;
#7187=CARTESIAN_POINT ( 'NONE',  ( -0.8107537697050254399, -0.1574803149606297803, 0.7750984250893222516 ) ) ;
#7190=CARTESIAN_POINT ( 'NONE',  ( -0.8107537697050234415, -0.1574803149606297803, 0.1451771652468037688 ) ) ;
#7192=CARTESIAN_POINT ( 'NONE',  ( 0.8759842519685039353, 0.1574803149606299191, 0.9547244093412913246 ) ) ;
#7194=CARTESIAN_POINT ( 'NONE',  ( -0.9500414927467378812, -0.1787899950787401604, 0.4084645668753704717 ) ) ;
#7198=CARTESIAN_POINT ( 'NONE',  ( -0.9500414927467378812, -0.1787899950787401604, 1.633858267662771313 ) ) ;
#7201=CARTESIAN_POINT ( 'NONE',  ( 0.6971942568897648851, -0.07405724077823297447, 1.505905511757261284 ) ) ;
#7202=CARTESIAN_POINT ( 'NONE',  ( -0.9500414927467378812, -0.1787899950787401604, 0.7677165353793073965 ) ) ;
#7203=CARTESIAN_POINT ( 'NONE',  ( 0.9500414927467378812, -0.1787899950787401604, 0.1377952755367876370 ) ) ;
#7205=CARTESIAN_POINT ( 'NONE',  ( 1.054774247047244540, 0.07405724077823318263, 0.7381889763241898939 ) ) ;
#7206=CARTESIAN_POINT ( 'NONE',  ( -0.6971942568897637749, 2.189545951927499583E-17, 0.6323818897100157432 ) ) ;
#7209=CARTESIAN_POINT ( 'NONE',  ( 0.7646288533564489232, 0.1113553986120547346, 1.077755905404283565 ) ) ;
#7211=CARTESIAN_POINT ( 'NONE',  ( -0.8107537697050253289, -0.1574803149606297803, 1.838090551073574774 ) ) ;
#7212=ORIENTED_EDGE ( 'NONE', *, *, #34931, .T. ) ;
#7213=CARTESIAN_POINT ( 'NONE',  ( -0.8107537697050253289, 0.1574803149606300301, 1.518208661417322469 ) ) ;
#7214=CARTESIAN_POINT ( 'NONE',  ( 0.9500414927467377701, 0.1787899950787401604, 1.451771653489543290 ) ) ;
#7218=EDGE_CURVE ( 'NONE', #12474, #9619, #20245, .T. ) ;
#7219=EDGE_CURVE ( 'NONE', #38209, #42434, #505, .T. ) ;
#7229=CARTESIAN_POINT ( 'NONE',  ( 0.8019270111902717657, -0.1787899950787401604, 1.742125984198204858 ) ) ;
#7230=CARTESIAN_POINT ( 'NONE',  ( 0.9500414927467378812, 0.1787899950787401604, 0.2657480314422993595 ) ) ;
#7231=CLOSED_SHELL ( 'NONE', ( #20807, #19087, #21475, #23283, #22901, #15739, #30708, #7033, #1627, #36746, #32999, #46243, #15559, #2052, #198, #22344, #23924, #4144, #17053, #26424, #38257, #42954, #18980, #28361, #15440, #18872, #46569, #5580, #21357, #19196, #30770, #43829, #17319, #44235, #8496, #12851, #31021, #38151, #27849, #35304, #21713, #39209, #42611, #41139, #38705, #2536, #25690, #15325, #17523, #29043, #13340, #46897, #28104, #14678, #45689, #43870, #516, #28098, #37572, #29327, #31727, #14838, #47446, #32153, #41682, #6845, #6731, #8390, #22074, #14298, #4570, #27484, #46237, #18610, #46397, #27755, #22673, #15026, #27156, #30880, #40309, #19314, #31529, #6092, #38207, #10321, #9269, #45035, #22839, #43647, #35670, #14010, #12123, #40828, #11652, #39000, #16728, #25163, #1796, #33848, #21829, #41582, #12578, #18766, #3147, #6431, #8051, #10286, #20021, #25874, #43931, #28985, #12696, #26086, #31571, #42593, #25223, #9374, #29861, #33387, #46731, #37273, #27845, #20995, #16034, #1506, #39856, #25453, #19427, #26971, #13311, #17427, #590, #7789, #30988, #32363, #8828, #44584, #42622, #29269, #5904, #43817, #36905, #10639, #24477, #25059, #37803, #41732, #27244, #11375, #7836, #6764, #28307, #41420, #30493, #27946, #18129, #32811, #37765, #11933, #9260, #9158, #21200, #25567, #28655, #44503, #40770, #16787, #39213, #36633, #17106, #26530, #42828, #29335, #42718, #10839, #16621, #9789, #43654, #34528, #8991, #13741, #10203, #33192, #11767, #39525, #4917, #5996, #26482, #12306, #47305, #23884, #15615, #1392, #21810, #44134, #34583, #40387, #37299, #46095, #36234, #34328, #32709, #13798, #38846, #31091, #12628, #36, #9103, #15279, #41518, #32387, #14606, #4351, #24220, #14566, #21510, #36955, #12251, #38856, #4914, #34805, #32342, #25727, #527, #2045, #7411, #25319 ) ) ;
#7236=CARTESIAN_POINT ( 'NONE',  ( 0.8759842519685039353, 0.1787899950787401882, 0.6619094487651338010 ) ) ;
#7237=CARTESIAN_POINT ( 'NONE',  ( -0.8512729243857075634, 0.1743046752856882431, 0.03937007874015844427 ) ) ;
#7238=CARTESIAN_POINT ( 'NONE',  ( 1.033464566929133799, 0.000000000000000000, 1.112204724409448842 ) ) ;
#7239=DIRECTION ( 'NONE',  ( 0.000000000000000000, 0.000000000000000000, -1.000000000000000000 ) ) ;
#7241=CARTESIAN_POINT ( 'NONE',  ( 0.8759842519685039353, 0.1574803149606299191, 0.9547244093412913246 ) ) ;
#7242=CARTESIAN_POINT ( 'NONE',  ( 0.9500414927467378812, 0.1787899950787401604, 1.648622047190331230 ) ) ;
#7243=CARTESIAN_POINT ( 'NONE',  ( -0.8759842519685039353, 0.000000000000000000, 0.000000000000000000 ) ) ;
#7245=CARTESIAN_POINT ( 'NONE',  ( 0.8019270111902716547, 0.1787899950787401604, 0.5068897637257642197 ) ) ;
#7246=ORIENTED_EDGE ( 'NONE', *, *, #37890, .F. ) ;
#7248=ORIENTED_EDGE ( 'NONE', *, *, #29609, .T. ) ;
#7251=CARTESIAN_POINT ( 'NONE',  ( -1.054774247047244096, 0.000000000000000000, 0.4601377952218267953 ) ) ;
#7254=CARTESIAN_POINT ( 'NONE',  ( 1.054774247047244096, 0.000000000000000000, 0.02706692908009476414 ) ) ;
#7256=CARTESIAN_POINT ( 'NONE',  ( -0.8019270111902717657, 0.1787899950787401604, 1.530511810969859443 ) ) ;
#7257=VERTEX_POINT ( 'NONE', #29139 ) ;
#7259=CARTESIAN_POINT ( 'NONE',  ( -0.6971942568897637749, 2.189545951927499583E-17, 1.188484251914740275 ) ) ;
#7262=CARTESIAN_POINT ( 'NONE',  ( 0.9500414927467378812, -0.1787899950787401604, 1.122047244040725644 ) ) ;
#7265=CARTESIAN_POINT ( 'NONE',  ( 0.7495606340400177148, -0.1264236179284866091, 1.818405511757259729 ) ) ;
#7266=CARTESIAN_POINT ( 'NONE',  ( -0.9873396505805591694, -0.1113553986120547346, 0.6348425196850393526 ) ) ;
#7267=CARTESIAN_POINT ( 'NONE',  ( -0.6971942568897648851, -0.07405724077823297447, 1.107283464513165949 ) ) ;
#7270=CARTESIAN_POINT ( 'NONE',  ( 0.8759842519685039353, -0.1787899950787401882, 0.2534448818360003908 ) ) ;
#7271=CARTESIAN_POINT ( 'NONE',  ( -0.9500414927467377701, 0.1787899950787401604, 0.2657480314422993595 ) ) ;
#7272=CARTESIAN_POINT ( 'NONE',  ( -1.054774247047244540, 0.07405724077823318263, 0.6938976377415123631 ) ) ;
#7273=CARTESIAN_POINT ( 'NONE',  ( 0.9412147342319837628, 0.1574803149606300301, 1.582185039262551607 ) ) ;
#7274=EDGE_LOOP ( 'NONE', ( #20749, #31049, #18927, #29137 ) ) ;
#7276=CARTESIAN_POINT ( 'NONE',  ( 0.7495606340400177148, -0.1264236179284866091, 0.7209645668753701386 ) ) ;
#7277=CARTESIAN_POINT ( 'NONE',  ( 1.054774247047244540, -0.07405724077823318263, 1.087598425143086578 ) ) ;
#7278=CARTESIAN_POINT ( 'NONE',  ( -0.6971942568897648851, -0.07405724077823297447, 1.894685039316315489 ) ) ;
#7279=CARTESIAN_POINT ( 'NONE',  ( 1.054774247047244540, -0.07405724077823318263, 1.870078740103715331 ) ) ;
#7285=CARTESIAN_POINT ( 'NONE',  ( 0.7495606340400177148, 0.1264236179284866091, 1.257381889710015743 ) ) ;
#7287=CARTESIAN_POINT ( 'NONE',  ( 0.7646288533564489232, 0.1113553986120547346, 1.392716535325543292 ) ) ;
#7288=CARTESIAN_POINT ( 'NONE',  ( 0.7185039370078746268, -0.06523048226347956391, 1.921751968503937480 ) ) ;
#7293=CARTESIAN_POINT ( 'NONE',  ( -0.8759842519685039353, 0.1787899950787401882, 0.4699803149068661479 ) ) ;
#7296=CARTESIAN_POINT ( 'NONE',  ( -0.7136811659038074795, -0.04132492306600986376, 1.984037415143555583 ) ) ;
#7297=CARTESIAN_POINT ( 'NONE',  ( -1.033464566929133799, 0.000000000000000000, 1.190944881889763884 ) ) ;
#7298=CARTESIAN_POINT ( 'NONE',  ( 0.7495606340400177148, -0.1264236179284866091, 1.232775590497417362 ) ) ;
#7299=CARTESIAN_POINT ( 'NONE',  ( 1.054774247047244096, 0.000000000000000000, 1.715059055064346527 ) ) ;
#7303=CARTESIAN_POINT ( 'NONE',  ( 1.033464566929134687, -0.06523048226347956391, 0.8243110235145210130 ) ) ;
#7305=CARTESIAN_POINT ( 'NONE',  ( -1.033464566929133799, 0.000000000000000000, 1.811023621939716444 ) ) ;
#7306=CARTESIAN_POINT ( 'NONE',  ( 0.9500414927467378812, -0.1787899950787401604, 0.1328740156942679607 ) ) ;
#7308=CARTESIAN_POINT ( 'NONE',  ( 0.7025502174926940846, -0.01165807630412045957, 0.03936777229701638597 ) ) ;
#7310=CARTESIAN_POINT ( 'NONE',  ( -0.9873396505805591694, -0.1113553986120547346, 1.924212598317669221 ) ) ;
#7311=CARTESIAN_POINT ( 'NONE',  ( -0.8019270111902717657, -0.1787899950787401604, 1.230314960576156746 ) ) ;
#7312=CARTESIAN_POINT ( 'NONE',  ( 0.9412147342319837628, -0.1574803149606297803, 0.6619094487113696967 ) ) ;
#7316=CARTESIAN_POINT ( 'NONE',  ( 0.9653975661131874997, 0.1427198071953197922, 0.03937007654474576623 ) ) ;
#7318=CARTESIAN_POINT ( 'NONE',  ( -0.9412147342319837628, -0.1574803149606297803, 0.3469488187901108023 ) ) ;
#7320=CARTESIAN_POINT ( 'NONE',  ( 0.9500414927467378812, -0.1787899950787401604, 1.392716535379308285 ) ) ;
#7322=CARTESIAN_POINT ( 'NONE',  ( 0.7185039370078739607, 1.928577636452523993E-17, 0.2657480314960630197 ) ) ;
#7323=CARTESIAN_POINT ( 'NONE',  ( -0.8107537697050254399, 0.1574803149606300301, 0.1008858267716536417 ) ) ;
#7326=ORIENTED_EDGE ( 'NONE', *, *, #32760, .T. ) ;
#7327=DIRECTION ( 'NONE',  ( 1.000000000000000000, 0.000000000000000000, -1.822029033848725275E-16 ) ) ;
#7331=CARTESIAN_POINT ( 'NONE',  ( 0.9500414927467378812, -0.1787899950787401604, 0.6496062991588353874 ) ) ;
#7334=CARTESIAN_POINT ( 'NONE',  ( -1.054774247047244096, 0.000000000000000000, 1.168799212544661348 ) ) ;
#7338=CARTESIAN_POINT ( 'NONE',  ( -1.002407869896990045, 0.1264236179284866091, 1.050688976324189117 ) ) ;
#7339=CARTESIAN_POINT ( 'NONE',  ( -0.9500414927467378812, 0.1787899950787401604, 0.7824803149068669805 ) ) ;
#7341=CARTESIAN_POINT ( 'NONE',  ( -0.8759842519685039353, 0.1787899950787401882, 0.1550196849856066983 ) ) ;
#7342=CARTESIAN_POINT ( 'NONE',  ( 0.9412147342319837628, -0.1574803149606297803, 1.813484251968503935 ) ) ;
#7343=CARTESIAN_POINT ( 'NONE',  ( 0.7185039370078739607, 1.928577636452523993E-17, 1.633858267609007875 ) ) ;
#7346=CARTESIAN_POINT ( 'NONE',  ( 0.7185039370078739607, 1.928577636452523993E-17, 0.3838582677165354173 ) ) ;
#7347=CARTESIAN_POINT ( 'NONE',  ( 0.7185039370078739607, 1.928577636452523993E-17, 1.053149606299212504 ) ) ;
#7350=CARTESIAN_POINT ( 'NONE',  ( 1.054774247047244096, 0.000000000000000000, 1.045767716481669440 ) ) ;
#7351=CARTESIAN_POINT ( 'NONE',  ( -0.7495606340400177148, 0.1264236179284866091, 0.7455708660879684091 ) ) ;
#7352=CARTESIAN_POINT ( 'NONE',  ( -0.7646288533564489232, -0.1113553986120547346, 0.5757874014672763607 ) ) ;
#7353=CARTESIAN_POINT ( 'NONE',  ( -0.8019270111902716547, 0.1787899950787401604, 1.771653543253322249 ) ) ;
#7354=AXIS2_PLACEMENT_3D ( 'NONE', #45958, #13173, #16520 ) ;
#7355=CARTESIAN_POINT ( 'NONE',  ( -1.054774247047244540, 0.07405724077823318263, 0.06889763774151215492 ) ) ;
#7356=CARTESIAN_POINT ( 'NONE',  ( 0.7646288533564489232, 0.1113553986120547346, 0.6151574803149606474 ) ) ;
#7359=CARTESIAN_POINT ( 'NONE',  ( -0.7646288533564489232, 0.1113553986120547346, 1.471456692805858113 ) ) ;
#7360=CARTESIAN_POINT ( 'NONE',  ( 0.8019270111902717657, -0.1787899950787401604, 0.8021653542769460188 ) ) ;
#7361=VECTOR ( 'NONE', #33663, 39.37007874015748143 ) ;
#7363=DIRECTION ( 'NONE',  ( 1.000000000000000000, 0.000000000000000000, -1.822029033848725275E-16 ) ) ;
#7364=CARTESIAN_POINT ( 'NONE',  ( 0.7646288533564489232, 0.1113553986120547346, 1.481299212598425230 ) ) ;
#7365=CARTESIAN_POINT ( 'NONE',  ( 0.9186159177457573488, -0.1711103661972301349, 1.988942757455733679 ) ) ;
#7366=LINE ( 'NONE', #25822, #14728 ) ;
#7367=CARTESIAN_POINT ( 'NONE',  ( 0.7646288533564489232, -0.1113553986120547346, 1.481299212490897466 ) ) ;
#7368=ORIENTED_EDGE ( 'NONE', *, *, #24534, .T. ) ;
#7369=( BOUNDED_CURVE ( )  B_SPLINE_CURVE ( 2, ( #42374, #38316, #16526, #42121, #5726, #9336, #23954, #20342, #31394 ),
 .UNSPECIFIED., .F., .T. ) 
 B_SPLINE_CURVE_WITH_KNOTS ( ( 3, 2, 2, 2, 3 ),
 ( 0.5699999999999999512, 0.5725000000000000089, 0.5749999999999999556, 0.5775000000000000133, 0.5799999999999999600 ),
 .UNSPECIFIED. ) 
 CURVE ( )  GEOMETRIC_REPRESENTATION_ITEM ( )  RATIONAL_B_SPLINE_CURVE ( ( 1.000000000000000000, 0.9238795325112899581, 1.000000000000000000, 0.9238795325112869605, 1.000000000000000000, 0.9238795325112869605, 1.000000000000000000, 0.9238795325112869605, 1.000000000000000000 ) ) 
 REPRESENTATION_ITEM ( '' )  ) ;
#7371=CARTESIAN_POINT ( 'NONE',  ( 0.9500414927467377701, -0.1787899950787401604, 0.7627952755367883864 ) ) ;
#7374=CYLINDRICAL_SURFACE ( 'NONE', #3963, 0.1574803149606299191 ) ;
#7376=CARTESIAN_POINT ( 'NONE',  ( -0.9873396505805591694, 0.1113553986120547346, 1.156496062992125928 ) ) ;
#7378=CARTESIAN_POINT ( 'NONE',  ( 1.054774247047244540, -0.07405724077823318263, 1.003937007820251193 ) ) ;
#7382=CARTESIAN_POINT ( 'NONE',  ( 0.7185039370078739607, 1.928577636452523993E-17, 1.250000000000000000 ) ) ;
#7383=ORIENTED_EDGE ( 'NONE', *, *, #26695, .T. ) ;
#7384=CARTESIAN_POINT ( 'NONE',  ( -1.054774247047244096, 0.000000000000000000, 0.1008858267178899676 ) ) ;
#7385=CARTESIAN_POINT ( 'NONE',  ( -0.7185039370078739607, 1.928577636452523993E-17, 0.6988188976377952555 ) ) ;
#7388=CARTESIAN_POINT ( 'NONE',  ( -0.8019270111902717657, -0.1787899950787401604, 0.3297244093950552069 ) ) ;
#7389=( BOUNDED_CURVE ( )  B_SPLINE_CURVE ( 2, ( #4436, #44692, #41326, #33494, #8054, #11436, #11910, #849, #26532 ),
 .UNSPECIFIED., .F., .F. ) 
 B_SPLINE_CURVE_WITH_KNOTS ( ( 3, 2, 2, 2, 3 ),
 ( 0.2399999999999999911, 0.2424999999999999933, 0.2449999999999999956, 0.2474999999999999978, 0.2500000000000000000 ),
 .UNSPECIFIED. ) 
 CURVE ( )  GEOMETRIC_REPRESENTATION_ITEM ( )  RATIONAL_B_SPLINE_CURVE ( ( 1.000000000000000000, 0.9238795325112869605, 1.000000000000000000, 0.9238795325112869605, 1.000000000000000000, 0.9238795325112869605, 1.000000000000000000, 0.9238795325112879597, 1.000000000000000000 ) ) 
 REPRESENTATION_ITEM ( '' )  ) ;
#7391=CARTESIAN_POINT ( 'NONE',  ( 0.9873396505805591694, -0.1113553986120547346, 0.9891732283464568232 ) ) ;
#7392=FACE_OUTER_BOUND ( 'NONE', #20550, .T. ) ;
#7397=CARTESIAN_POINT ( 'NONE',  ( -0.8759842519685039353, 0.000000000000000000, 4.498031496062992574 ) ) ;
#7398=CARTESIAN_POINT ( 'NONE',  ( -0.8759842519685039353, 0.1787899950787401882, 0.3469488188438744070 ) ) ;
#7399=CARTESIAN_POINT ( 'NONE',  ( -0.7495606340400177148, -0.1264236179284866091, 1.390255905458047447 ) ) ;
#7400=VERTEX_POINT ( 'NONE', #42970 ) ;
#7405=CYLINDRICAL_SURFACE ( 'NONE', #40036, 0.1574803149606299191 ) ;
#7407=CARTESIAN_POINT ( 'NONE',  ( 0.9412147342319837628, -0.1574803149606297803, 1.843011810916095561 ) ) ;
#7411=ADVANCED_FACE ( 'NONE', ( #39383 ), #27267, .T. ) ;
#7413=CARTESIAN_POINT ( 'NONE',  ( -0.8759842519685039353, -0.1574803149606299191, 0.8267716535433071723 ) ) ;
#7417=ORIENTED_EDGE ( 'NONE', *, *, #34073, .T. ) ;
#7422=CARTESIAN_POINT ( 'NONE',  ( -0.9412147342319837628, -0.1574803149606297803, 0.07135826760900840227 ) ) ;
#7424=CARTESIAN_POINT ( 'NONE',  ( 0.8107537697050253289, 0.1574803149606300301, 0.9571850392625528281 ) ) ;
#7425=CARTESIAN_POINT ( 'NONE',  ( 0.9412147342319837628, 0.1574803149606300301, 0.5290354330708663122 ) ) ;
#7426=CARTESIAN_POINT ( 'NONE',  ( -0.7495606340400177148, 0.1264236179284866091, 0.3518700786863940833 ) ) ;
#7427=ORIENTED_EDGE ( 'NONE', *, *, #7625, .T. ) ;
#7429=CARTESIAN_POINT ( 'NONE',  ( -0.7495606340400177148, 0.1264236179284866091, 1.656003936954110412 ) ) ;
#7431=CARTESIAN_POINT ( 'NONE',  ( 0.8019270111902717657, -0.1787899950787401604, 1.628937007820252303 ) ) ;
#7432=CARTESIAN_POINT ( 'NONE',  ( -0.9500414927467378812, 0.1787899950787401604, 0.8612204723871809131 ) ) ;
#7433=CARTESIAN_POINT ( 'NONE',  ( 0.6971942568897626646, 0.07405724077823318263, 0.2805118109698587214 ) ) ;
#7434=CARTESIAN_POINT ( 'NONE',  ( 1.033464566929133799, 1.928577636452524610E-17, 4.498031496062992574 ) ) ;
#7435=CARTESIAN_POINT ( 'NONE',  ( 0.6971942568897648851, 0.07405724077823318263, 0.7923228345919055560 ) ) ;
#7436=CARTESIAN_POINT ( 'NONE',  ( -0.8759842519685039353, -0.1787899950787401882, 0.6422244093950550958 ) ) ;
#7438=CARTESIAN_POINT ( 'NONE',  ( -0.8759842519685039353, 0.000000000000000000, 0.000000000000000000 ) ) ;
#7440=CARTESIAN_POINT ( 'NONE',  ( -0.8019270111902717657, -0.1787899950787401604, 1.589566929080094448 ) ) ;
#7441=CARTESIAN_POINT ( 'NONE',  ( -1.033464566929134687, 0.06523048226347956391, 1.892224409341292546 ) ) ;
#7443=CARTESIAN_POINT ( 'NONE',  ( 1.002407869896990045, 0.1264236179284866091, 1.528051181048598384 ) ) ;
#7444=CARTESIAN_POINT ( 'NONE',  ( -0.7185039370078739607, 1.928577636452523993E-17, 1.564960629921259949 ) ) ;
#7448=VERTEX_POINT ( 'NONE', #22603 ) ;
#7449=CARTESIAN_POINT ( 'NONE',  ( -0.8759842519685039353, -0.1574803149606299191, 1.141732283464567121 ) ) ;
#7454=LINE ( 'NONE', #256, #3395 ) ;
#7456=CARTESIAN_POINT ( 'NONE',  ( 0.8019270111902717657, -0.1787899950787401604, 1.781496062938362934 ) ) ;
#7459=CARTESIAN_POINT ( 'NONE',  ( 0.7185039370078739607, 1.928577636452523993E-17, 0.1377952754830242266 ) ) ;
#7460=CARTESIAN_POINT ( 'NONE',  ( 0.8019270111902717657, 0.1787899950787401604, 0.6249999999462366729 ) ) ;
#7463=CARTESIAN_POINT ( 'NONE',  ( -0.9027521039302758288, 0.1709455099970345893, 0.03937007874015843734 ) ) ;
#7466=CARTESIAN_POINT ( 'NONE',  ( 0.9873396505805591694, 0.1113553986120547346, 0.9498031494987716483 ) ) ;
#7467=CARTESIAN_POINT ( 'NONE',  ( 0.8759842519685039353, 0.1787899950787401882, 1.887303149552535420 ) ) ;
#7472=CARTESIAN_POINT ( 'NONE',  ( -0.6971942568897637749, 2.189545951927499583E-17, 0.4798228345919055560 ) ) ;
#7475=CARTESIAN_POINT ( 'NONE',  ( 0.6971942568897626646, -0.07405724077823297447, 0.04921259837143338034 ) ) ;
#7477=CARTESIAN_POINT ( 'NONE',  ( -1.002407869896990045, -0.1264236179284866091, 1.670767716481669440 ) ) ;
#7478=ORIENTED_EDGE ( 'NONE', *, *, #26809, .F. ) ;
#7479=CARTESIAN_POINT ( 'NONE',  ( -0.8019270111902717657, 0.1787899950787401604, 1.220472440891118504 ) ) ;
#7482=CARTESIAN_POINT ( 'NONE',  ( 1.054774247047244540, 0.07405724077823318263, 0.02952755900135457801 ) ) ;
#7483=CARTESIAN_POINT ( 'NONE',  ( -0.9412147342319837628, 0.1574803149606300301, 0.6471456692913395425 ) ) ;
#7484=CARTESIAN_POINT ( 'NONE',  ( -0.6971942568897637749, 2.189545951927499583E-17, 0.9867125983714331028 ) ) ;
#7485=CARTESIAN_POINT ( 'NONE',  ( -0.7185039370078746268, -0.06523048226347956391, 1.606791338582677309 ) ) ;
#7487=CARTESIAN_POINT ( 'NONE',  ( 0.7495606340400177148, 0.1264236179284866091, 0.3174212597887562382 ) ) ;
#7488=CARTESIAN_POINT ( 'NONE',  ( -0.7495606340400177148, 0.1264236179284866091, 0.2337598424659216578 ) ) ;
#7489=CARTESIAN_POINT ( 'NONE',  ( -0.8019270111902717657, -0.1787899950787401604, 0.7972440944344250102 ) ) ;
#7491=( BOUNDED_CURVE ( )  B_SPLINE_CURVE ( 2, ( #7347, #33005, #29204, #3740, #11193, #29441, #44215, #3512, #40608 ),
 .UNSPECIFIED., .F., .T. ) 
 B_SPLINE_CURVE_WITH_KNOTS ( ( 3, 2, 2, 2, 3 ),
 ( 0.5300000000000000266, 0.5324999999999999734, 0.5350000000000000311, 0.5374999999999999778, 0.5400000000000000355 ),
 .UNSPECIFIED. ) 
 CURVE ( )  GEOMETRIC_REPRESENTATION_ITEM ( )  RATIONAL_B_SPLINE_CURVE ( ( 1.000000000000000000, 0.9238795325112869605, 1.000000000000000000, 0.9238795325112869605, 1.000000000000000000, 0.9238795325112869605, 1.000000000000000000, 0.9238795325112869605, 1.000000000000000000 ) ) 
 REPRESENTATION_ITEM ( '' )  ) ;
#7492=CIRCLE ( 'NONE', #34303, 0.1574803149606300579 ) ;
#7495=CARTESIAN_POINT ( 'NONE',  ( 0.6971942568897626646, 0.07405724077823318263, 0.7529527558517473684 ) ) ;
#7496=CARTESIAN_POINT ( 'NONE',  ( 0.8019270111902716547, -0.1787899950787401604, 1.117125984198206412 ) ) ;
#7497=CARTESIAN_POINT ( 'NONE',  ( -0.9500414927467377701, 0.1787899950787401604, 1.840551181048599938 ) ) ;
#7499=CARTESIAN_POINT ( 'NONE',  ( 0.8019270111902717657, -0.1787899950787401604, 1.938976377898990799 ) ) ;
#7501=CARTESIAN_POINT ( 'NONE',  ( -0.7185039370078739607, 1.928577636452523993E-17, 0.1870078740157480324 ) ) ;
#7503=ORIENTED_EDGE ( 'NONE', *, *, #9522, .T. ) ;
#7506=ORIENTED_EDGE ( 'NONE', *, *, #10016, .T. ) ;
#7507=CARTESIAN_POINT ( 'NONE',  ( 0.7495606340400177148, 0.1264236179284866091, 1.218011810969858111 ) ) ;
#7509=CARTESIAN_POINT ( 'NONE',  ( -0.7185039370078746268, 0.06523048226347956391, 1.001476377845229804 ) ) ;
#7510=CARTESIAN_POINT ( 'NONE',  ( 1.002407869896990045, -0.1264236179284866091, 0.05659448813521283234 ) ) ;
#7514=CARTESIAN_POINT ( 'NONE',  ( -0.6971942568897637749, 2.189545951927499583E-17, 0.4798228345919055560 ) ) ;
#7518=CARTESIAN_POINT ( 'NONE',  ( -0.7105523864618353835, 0.009560899065524132434, 1.983094267893590334 ) ) ;
#7520=CARTESIAN_POINT ( 'NONE',  ( 1.054774247047244540, 0.07405724077823318263, 1.171259842465921741 ) ) ;
#7521=CARTESIAN_POINT ( 'NONE',  ( 0.8019270111902716547, 0.1787899950787401604, 1.648622047190331230 ) ) ;
#7526=LINE ( 'NONE', #40804, #6013 ) ;
#7528=CARTESIAN_POINT ( 'NONE',  ( -0.7185039370078739607, 1.928577636452523993E-17, 1.919291338582677309 ) ) ;
#7529=CARTESIAN_POINT ( 'NONE',  ( 0.8759842519685039353, -0.1574803149606299191, 0.5413385825696385156 ) ) ;
#7531=CARTESIAN_POINT ( 'NONE',  ( 1.054774247047244540, -0.07405724077823318263, 0.3346456692375748831 ) ) ;
#7532=CARTESIAN_POINT ( 'NONE',  ( 0.7099242514868753240, -0.04392859927252232982, 0.03937034313776070077 ) ) ;
#7533=CARTESIAN_POINT ( 'NONE',  ( 1.054774247047244540, -0.07405724077823318263, 1.279527559001355730 ) ) ;
#7534=CARTESIAN_POINT ( 'NONE',  ( -0.8759842519685039353, 0.000000000000000000, 0.000000000000000000 ) ) ;
#7537=CARTESIAN_POINT ( 'NONE',  ( -0.6971942568897637749, 2.189545951927499583E-17, 1.222933070812378009 ) ) ;
#7538=CARTESIAN_POINT ( 'NONE',  ( 0.7185039370078746268, 0.06523048226347956391, 0.7258858266641259327 ) ) ;
#7541=CARTESIAN_POINT ( 'NONE',  ( 0.8895385448872797918, 0.1731831457854506318, 0.03937007870486500943 ) ) ;
#7544=CARTESIAN_POINT ( 'NONE',  ( 0.6971942568897637749, 2.189545951927499583E-17, 1.459153543253322693 ) ) ;
#7545=CARTESIAN_POINT ( 'NONE',  ( -0.7185039370078746268, 0.06523048226347956391, 1.168799212598425896 ) ) ;
#7547=CARTESIAN_POINT ( 'NONE',  ( -0.8759842519685039353, 0.1787899950787401882, 0.07135826766277185429 ) ) ;
#7549=CARTESIAN_POINT ( 'NONE',  ( 0.7185039370078746268, -0.06523048226347956391, 1.321358267609009429 ) ) ;
#7551=CARTESIAN_POINT ( 'NONE',  ( -0.8107537697050254399, 0.1574803149606300301, 0.3764763779527559029 ) ) ;
#7553=CARTESIAN_POINT ( 'NONE',  ( 0.6971942568897626646, 0.07405724077823318263, 0.5561023621509617598 ) ) ;
#7556=CARTESIAN_POINT ( 'NONE',  ( -0.8019270111902717657, -0.1787899950787401604, 1.195866141678520345 ) ) ;
#7558=CARTESIAN_POINT ( 'NONE',  ( -1.002407869896990045, -0.1264236179284866091, 0.8489173227808819444 ) ) ;
#7559=CARTESIAN_POINT ( 'NONE',  ( 0.8759842519685039353, 0.000000000000000000, 2.007874015640504162 ) ) ;
#7560=CARTESIAN_POINT ( 'NONE',  ( -0.8019270111902717657, 0.1787899950787401604, 0.1968503936470238913 ) ) ;
#7565=CARTESIAN_POINT ( 'NONE',  ( -0.9873396505805591694, -0.1113553986120547346, 0.8612204723334173639 ) ) ;
#7571=CARTESIAN_POINT ( 'NONE',  ( -0.8759842519685039353, 0.1787899950787401882, 0.8193897637257637756 ) ) ;
#7573=EDGE_CURVE ( 'NONE', #3237, #43250, #236, .T. ) ;
#7576=CARTESIAN_POINT ( 'NONE',  ( -0.7495606340400177148, 0.1264236179284866091, 1.813484251914740053 ) ) ;
#7577=ORIENTED_EDGE ( 'NONE', *, *, #4400, .F. ) ;
#7578=CARTESIAN_POINT ( 'NONE',  ( 0.9873396505805591694, 0.1113553986120547346, 0.6840551181102363376 ) ) ;
#7581=CARTESIAN_POINT ( 'NONE',  ( -0.8107537697050253289, 0.1574803149606300301, 1.468996062884598830 ) ) ;
#7582=CARTESIAN_POINT ( 'NONE',  ( 0.6971942568897626646, -0.07405724077823297447, 0.7578740156942689321 ) ) ;
#7584=CARTESIAN_POINT ( 'NONE',  ( 0.7646288533564489232, -0.1113553986120547346, 1.412401574803149540 ) ) ;
#7585=CARTESIAN_POINT ( 'NONE',  ( 0.8111863842034094940, -0.1598013345783634853, 1.986982674346258415 ) ) ;
#7586=DIRECTION ( 'NONE',  ( 0.000000000000000000, 0.000000000000000000, -1.000000000000000000 ) ) ;
#7587=CARTESIAN_POINT ( 'NONE',  ( 0.8759842519685039353, -0.1574803149606299191, 1.722440944774362270 ) ) ;
#7589=CARTESIAN_POINT ( 'NONE',  ( 0.8019270111902716547, 0.1787899950787401604, 0.9005905511273391006 ) ) ;
#7590=CARTESIAN_POINT ( 'NONE',  ( -0.9412147342319837628, -0.1574803149606297803, 1.419783464566930054 ) ) ;
#7591=VECTOR ( 'NONE', #41985, 39.37007874015748143 ) ;
#7594=CARTESIAN_POINT ( 'NONE',  ( 0.7646288533564489232, 0.1113553986120547346, 0.9301181102362204856 ) ) ;
#7595=LINE ( 'NONE', #29236, #46591 ) ;
#7596=CARTESIAN_POINT ( 'NONE',  ( 0.9500414927467378812, 0.1787899950787401604, 0.9744094487651340231 ) ) ;
#7600=DIRECTION ( 'NONE',  ( -1.000000000000000000, 0.000000000000000000, 0.000000000000000000 ) ) ;
#7603=CARTESIAN_POINT ( 'NONE',  ( 0.7185039370078739607, 1.928577636452523993E-17, 1.761811023622047223 ) ) ;
#7605=CARTESIAN_POINT ( 'NONE',  ( 0.9873396505805591694, -0.1113553986120547346, 0.3494094487113705294 ) ) ;
#7606=CARTESIAN_POINT ( 'NONE',  ( -1.002407869896990045, -0.1264236179284866091, 1.749507873961984483 ) ) ;
#7607=CARTESIAN_POINT ( 'NONE',  ( -1.002407869896990045, 0.1264236179284866091, 0.8538385826234016207 ) ) ;
#7608=CARTESIAN_POINT ( 'NONE',  ( -0.9412147342319837628, -0.1574803149606297803, 0.1107283463491657988 ) ) ;
#7609=CARTESIAN_POINT ( 'NONE',  ( 0.7185039370078746268, -0.06523048226347956391, 0.9768700787401572994 ) ) ;
#7615=DIRECTION ( 'NONE',  ( 0.000000000000000000, 0.000000000000000000, 1.000000000000000000 ) ) ;
#7617=CARTESIAN_POINT ( 'NONE',  ( -1.002407869896990045, -0.1264236179284866091, 0.3715551180564728440 ) ) ;
#7620=EDGE_LOOP ( 'NONE', ( #17052, #7176, #27750, #25201 ) ) ;
#7623=CARTESIAN_POINT ( 'NONE',  ( -1.002407869896990045, 0.1264236179284866091, 1.331200787347811110 ) ) ;
#7625=EDGE_CURVE ( 'NONE', #28962, #38421, #18013, .T. ) ;
#7629=( BOUNDED_CURVE ( )  B_SPLINE_CURVE ( 2, ( #10437, #25037, #17368, #46832, #42741, #31782, #20728, #3217, #20499 ),
 .UNSPECIFIED., .F., .T. ) 
 B_SPLINE_CURVE_WITH_KNOTS ( ( 3, 2, 2, 2, 3 ),
 ( 0.3200000000000000067, 0.3225000000000000089, 0.3250000000000000111, 0.3275000000000000133, 0.3300000000000000155 ),
 .UNSPECIFIED. ) 
 CURVE ( )  GEOMETRIC_REPRESENTATION_ITEM ( )  RATIONAL_B_SPLINE_CURVE ( ( 1.000000000000000000, 0.9238795325112869605, 1.000000000000000000, 0.9238795325112869605, 1.000000000000000000, 0.9238795325112869605, 1.000000000000000000, 0.9238795325112869605, 1.000000000000000000 ) ) 
 REPRESENTATION_ITEM ( '' )  ) ;
#7632=CARTESIAN_POINT ( 'NONE',  ( -0.8759842519685039353, 0.1574803149606299191, 1.072834645561763889 ) ) ;
#7633=VECTOR ( 'NONE', #20931, 39.37007874015748143 ) ;
#7637=CARTESIAN_POINT ( 'NONE',  ( 0.8107537697050253289, 0.1574803149606300301, 1.902066929026330788 ) ) ;
#7638=EDGE_LOOP ( 'NONE', ( #36980, #44240, #20004, #27759 ) ) ;
#7640=CARTESIAN_POINT ( 'NONE',  ( 0.8107537697050253289, 0.1574803149606300301, 1.006397637795276800 ) ) ;
#7646=CARTESIAN_POINT ( 'NONE',  ( -0.8107537697050254399, -0.1574803149606297803, 0.9817913385826764205 ) ) ;
#7651=CARTESIAN_POINT ( 'NONE',  ( 0.9873396505805591694, 0.1113553986120547346, 1.028543306979086802 ) ) ;
#7654=CARTESIAN_POINT ( 'NONE',  ( -1.054774247047244096, 0.000000000000000000, 0.3764763778989925203 ) ) ;
#7658=CARTESIAN_POINT ( 'NONE',  ( -1.002407869896990045, -0.1264236179284866091, 1.636318897584031484 ) ) ;
#7659=CARTESIAN_POINT ( 'NONE',  ( 0.7495606340400177148, 0.1264236179284866091, 1.774114173174582643 ) ) ;
#7660=CARTESIAN_POINT ( 'NONE',  ( -0.7495606340400177148, -0.1264236179284866091, 0.7209645668753701386 ) ) ;
#7661=DIRECTION ( 'NONE',  ( 0.000000000000000000, 0.000000000000000000, -1.000000000000000000 ) ) ;
#7662=CARTESIAN_POINT ( 'NONE',  ( 0.9500414927467378812, 0.1787899950787401604, 0.3100393700249766682 ) ) ;
#7664=CARTESIAN_POINT ( 'NONE',  ( -0.8759842519685039353, -0.1574803149606299191, 0.4625984250893235838 ) ) ;
#7665=CARTESIAN_POINT ( 'NONE',  ( -1.002407869896990045, -0.1264236179284866091, 1.198326771599779628 ) ) ;
#7666=CARTESIAN_POINT ( 'NONE',  ( -1.054774247047244540, 0.07405724077823318263, 0.6545275590013546196 ) ) ;
#7667=CIRCLE ( 'NONE', #20659, 0.5019685039370077595 ) ;
#7669=CARTESIAN_POINT ( 'NONE',  ( -0.8759842519685039353, 0.1574803149606299191, 1.663385826664125933 ) ) ;
#7670=CARTESIAN_POINT ( 'NONE',  ( -0.6971942568897648851, 0.07405724077823318263, 1.540354330654897685 ) ) ;
#7671=CARTESIAN_POINT ( 'NONE',  ( -1.033464566929134687, 0.06523048226347956391, 1.852854330601134691 ) ) ;
#7674=CARTESIAN_POINT ( 'NONE',  ( 0.9412147342319837628, 0.1574803149606300301, 1.631397637795275468 ) ) ;
#7682=EDGE_CURVE ( 'NONE', #23548, #1642, #5424, .T. ) ;
#7688=LINE ( 'NONE', #22076, #15629 ) ;
#7690=CARTESIAN_POINT ( 'NONE',  ( 0.9500414927467378812, -0.1787899950787401604, 1.786417322780882388 ) ) ;
#7697=CARTESIAN_POINT ( 'NONE',  ( 1.054774247047244540, 0.07405724077823318263, 0.7726377952218265177 ) ) ;
#7698=CARTESIAN_POINT ( 'NONE',  ( -1.028254228867618192, 0.05473827914784732546, 0.03937007874015843040 ) ) ;
#7699=CARTESIAN_POINT ( 'NONE',  ( 0.7185039370078746268, -0.06523048226347956391, 1.124507873908221267 ) ) ;
#7702=CARTESIAN_POINT ( 'NONE',  ( 0.7185039370078746268, -0.06523048226347956391, 1.685531496062991019 ) ) ;
#7703=CARTESIAN_POINT ( 'NONE',  ( 0.7495606340400177148, -0.1264236179284866091, 1.823326771599779406 ) ) ;
#7705=CARTESIAN_POINT ( 'NONE',  ( 1.033464566929134687, -0.06523048226347956391, 0.1254921259842518844 ) ) ;
#7708=DIRECTION ( 'NONE',  ( 1.822029033848725028E-16, 0.000000000000000000, 1.000000000000000000 ) ) ;
#7711=CARTESIAN_POINT ( 'NONE',  ( 1.054774247047244540, 0.07405724077823318263, 0.3051181101824569919 ) ) ;
#7713=CARTESIAN_POINT ( 'NONE',  ( -1.002407869896990045, -0.1264236179284866091, 1.631397637741511808 ) ) ;
#7715=CARTESIAN_POINT ( 'NONE',  ( -0.8759842519685039353, -0.1787899950787401882, 1.119586614119464585 ) ) ;
#7716=CARTESIAN_POINT ( 'NONE',  ( 0.8759842519685039353, -0.1574803149606299191, 1.023622047244094446 ) ) ;
#7717=CARTESIAN_POINT ( 'NONE',  ( 1.054774247047244096, 0.000000000000000000, 1.286909448765133801 ) ) ;
#7718=CARTESIAN_POINT ( 'NONE',  ( 0.6971942568897648851, 0.07405724077823318263, 1.929133858213952335 ) ) ;
#7719=CARTESIAN_POINT ( 'NONE',  ( -0.8759842519685039353, 0.1787899950787401882, 1.055610236166708793 ) ) ;
#7722=CARTESIAN_POINT ( 'NONE',  ( 1.002407869896990045, 0.1264236179284866091, 0.3863188975840318173 ) ) ;
#7723=CARTESIAN_POINT ( 'NONE',  ( -0.7495606340400177148, -0.1264236179284866091, 0.2042322834108035723 ) ) ;
#7724=UNCERTAINTY_MEASURE_WITH_UNIT (LENGTH_MEASURE( 1.000000000000000082E-05 ), #39041, 'distance_accuracy_value', 'NONE') ;
#7725=CARTESIAN_POINT ( 'NONE',  ( -0.8759842519685039353, 0.1787899950787401882, 0.7406496062454487328 ) ) ;
#7726=EDGE_LOOP ( 'NONE', ( #8432, #10992, #38886, #15283 ) ) ;
#7727=AXIS2_PLACEMENT_3D ( 'NONE', #42526, #38723, #20732 ) ;
#7728=CARTESIAN_POINT ( 'NONE',  ( -0.7185039370078746268, 0.06523048226347956391, 0.8833661416247559073 ) ) ;
#7729=ORIENTED_EDGE ( 'NONE', *, *, #27158, .T. ) ;
#7730=CARTESIAN_POINT ( 'NONE',  ( 0.8019270111902717657, -0.1787899950787401604, 0.9202755904974182499 ) ) ;
#7731=CARTESIAN_POINT ( 'NONE',  ( -0.8019270111902716547, -0.1787899950787401604, 1.899606299158834943 ) ) ;
#7732=ORIENTED_EDGE ( 'NONE', *, *, #36038, .T. ) ;
#7736=EDGE_CURVE ( 'NONE', #31278, #26592, #22919, .T. ) ;
#7741=DIRECTION ( 'NONE',  ( 1.000000000000000000, 0.000000000000000000, -1.822029033848725275E-16 ) ) ;
#7745=CARTESIAN_POINT ( 'NONE',  ( 1.054774247047244540, -0.07405724077823318263, 1.161417322780881278 ) ) ;
#7749=CARTESIAN_POINT ( 'NONE',  ( 0.8019270111902717657, -0.1787899950787401604, 0.1673228345919057225 ) ) ;
#7753=CARTESIAN_POINT ( 'NONE',  ( -1.054774247047244096, 0.000000000000000000, 0.5388779527021417826 ) ) ;
#7754=CARTESIAN_POINT ( 'NONE',  ( 0.9873396505805591694, 0.1113553986120547346, 0.3690944881889763884 ) ) ;
#7756=CARTESIAN_POINT ( 'NONE',  ( -0.7106060021345387279, -0.02103896280498998572, 1.983649324475407427 ) ) ;
#7758=CARTESIAN_POINT ( 'NONE',  ( 1.002407869896990045, -0.1264236179284866091, 1.321358267662771757 ) ) ;
#7759=CARTESIAN_POINT ( 'NONE',  ( 1.002407869896990045, -0.1264236179284866091, 1.631397637741511808 ) ) ;
#7761=CARTESIAN_POINT ( 'NONE',  ( -0.7185039370078739607, 1.928577636452523993E-17, 1.013779527559055094 ) ) ;
#7762=CARTESIAN_POINT ( 'NONE',  ( -0.9873396505805591694, 0.1113553986120547346, 1.510826771653543288 ) ) ;
#7763=AXIS2_PLACEMENT_3D ( 'NONE', #37474, #25987, #553 ) ;
#7765=CARTESIAN_POINT ( 'NONE',  ( -0.8759842519685039353, -0.1574803149606299191, 1.929133858267716661 ) ) ;
#7767=CARTESIAN_POINT ( 'NONE',  ( 1.002407869896990045, 0.1264236179284866091, 0.3420275590013546751 ) ) ;
#7769=SHAPE_REPRESENTATION ( 'U-Bolt', ( #20860 ), #15520 ) ;
#7772=CARTESIAN_POINT ( 'NONE',  ( 0.9873396505805591694, -0.1113553986120547346, 0.6643700786326299790 ) ) ;
#7779=VERTEX_POINT ( 'NONE', #11996 ) ;
#7780=CARTESIAN_POINT ( 'NONE',  ( -0.7646288533564489232, 0.1113553986120547346, 1.599409448818897683 ) ) ;
#7781=CARTESIAN_POINT ( 'NONE',  ( 1.054774247047244540, -0.07405724077823318263, 1.633858267662771313 ) ) ;
#7782=CARTESIAN_POINT ( 'NONE',  ( -0.7185039370078741827, 0.06523048226347841205, 0.9325787401574796576 ) ) ;
#7783=CARTESIAN_POINT ( 'NONE',  ( 0.9873396505805591694, 0.1113553986120547346, 1.668307086614173373 ) ) ;
#7784=DIRECTION ( 'NONE',  ( 0.000000000000000000, 0.000000000000000000, -1.000000000000000000 ) ) ;
#7789=ADVANCED_FACE ( 'NONE', ( #25895 ), #4772, .T. ) ;
#7790=CARTESIAN_POINT ( 'NONE',  ( 0.8759842519685039353, -0.1787899950787401882, 0.8046259841982047467 ) ) ;
#7791=CARTESIAN_POINT ( 'NONE',  ( -0.8759842519685039353, 0.1787899950787401882, 1.488681102308440751 ) ) ;
#7793=CARTESIAN_POINT ( 'NONE',  ( -0.6971942568897648851, 0.07405724077823318263, 1.304133858213953667 ) ) ;
#7794=ORIENTED_EDGE ( 'NONE', *, *, #41040, .T. ) ;
#7795=VECTOR ( 'NONE', #5098, 39.37007874015748143 ) ;
#7799=CARTESIAN_POINT ( 'NONE',  ( -0.6971942568897626646, 0.07405724077823318263, 0.3198818897100162983 ) ) ;
#7803=ORIENTED_EDGE ( 'NONE', *, *, #36431, .F. ) ;
#7805=ORIENTED_EDGE ( 'NONE', *, *, #35245, .T. ) ;
#7810=CARTESIAN_POINT ( 'NONE',  ( -0.8759842519685039353, 0.1787899950787401882, 1.847933070812378009 ) ) ;
#7813=CARTESIAN_POINT ( 'NONE',  ( -0.9412147342319837628, 0.1574803149606300301, 0.9227362204724416372 ) ) ;
#7817=CARTESIAN_POINT ( 'NONE',  ( -0.9412147342319837628, -0.1574803149606297803, 1.528051180994836056 ) ) ;
#7818=CARTESIAN_POINT ( 'NONE',  ( 0.9500414927467378812, 0.1787899950787401604, 0.9793307086076531442 ) ) ;
#7821=CARTESIAN_POINT ( 'NONE',  ( 0.9873396505805591694, -0.1113553986120547346, 1.422244094488188892 ) ) ;
#7822=CARTESIAN_POINT ( 'NONE',  ( 0.7356779250440615980, 0.08313417247115993669, 1.981581519332723751 ) ) ;
#7823=CARTESIAN_POINT ( 'NONE',  ( 0.7185039370078739607, 1.928577636452523993E-17, 1.594488188868850242 ) ) ;
#7825=AXIS2_PLACEMENT_3D ( 'NONE', #9558, #35200, #46900 ) ;
#7826=CARTESIAN_POINT ( 'NONE',  ( 1.054774247047244540, 0.07405724077823318263, 0.7726377952218266287 ) ) ;
#7831=CARTESIAN_POINT ( 'NONE',  ( 0.9873396505805591694, 0.1113553986120547346, 0.9202755905511811330 ) ) ;
#7832=VECTOR ( 'NONE', #37334, 39.37007874015748143 ) ;
#7835=CARTESIAN_POINT ( 'NONE',  ( 0.6971942568897648851, -0.07405724077823297447, 1.107283464513165949 ) ) ;
#7836=ADVANCED_FACE ( 'NONE', ( #11760 ), #19156, .T. ) ;
#7839=CARTESIAN_POINT ( 'NONE',  ( 1.033464566929133799, 0.000000000000000000, 1.299212598317669221 ) ) ;
#7842=CARTESIAN_POINT ( 'NONE',  ( -0.8019270111902717657, -0.1787899950787401604, 0.2066929133320631329 ) ) ;
#7843=VECTOR ( 'NONE', #34202, 39.37007874015748143 ) ;
#7845=CARTESIAN_POINT ( 'NONE',  ( 0.7646288533564489232, 0.1113553986120547346, 0.3395669291338583307 ) ) ;
#7846=CARTESIAN_POINT ( 'NONE',  ( -0.8759842519685039353, -0.1787899950787401882, 1.626476377898992132 ) ) ;
#7847=CARTESIAN_POINT ( 'NONE',  ( -0.7495606340400177148, 0.1264236179284866091, 0.8636811023084409733 ) ) ;
#7848=CARTESIAN_POINT ( 'NONE',  ( -0.8759842519685039353, -0.1787899950787401882, 0.4502952755367874427 ) ) ;
#7850=CARTESIAN_POINT ( 'NONE',  ( 0.9412147342319837628, -0.1574803149606297803, 0.9867125984251977622 ) ) ;
#7851=CARTESIAN_POINT ( 'NONE',  ( 0.6971942568897637749, 2.189545951927499583E-17, 0.08120078734781142893 ) ) ;
#7859=CARTESIAN_POINT ( 'NONE',  ( -1.054774247047244540, 0.07405724077823318263, 0.3001968503399373711 ) ) ;
#7862=CARTESIAN_POINT ( 'NONE',  ( -0.6971942568897648851, 0.07405724077823318263, 1.422244094434425898 ) ) ;
#7863=VERTEX_POINT ( 'NONE', #26381 ) ;
#7869=CARTESIAN_POINT ( 'NONE',  ( 1.033464566929134687, -0.06523048226347956391, 0.3223425196850393526 ) ) ;
#7871=CARTESIAN_POINT ( 'NONE',  ( -0.8759842519685039353, 0.1574803149606299191, 1.112204724301921299 ) ) ;
#7873=CARTESIAN_POINT ( 'NONE',  ( 0.8759842519685039353, 0.1787899950787401882, 0.4699803149068661479 ) ) ;
#7877=ORIENTED_EDGE ( 'NONE', *, *, #11017, .F. ) ;
#7878=CARTESIAN_POINT ( 'NONE',  ( -0.6971942568897648851, 0.07405724077823318263, 0.9498031495525356416 ) ) ;
#7879=CARTESIAN_POINT ( 'NONE',  ( 0.7185039370078746268, -0.06523048226347956391, 0.9768700787401572994 ) ) ;
#7881=CARTESIAN_POINT ( 'NONE',  ( -0.7185039370078739607, 1.928577636452523993E-17, 0.8169291338582678197 ) ) ;
#7882=CARTESIAN_POINT ( 'NONE',  ( 0.7185039370078739607, 1.928577636452523993E-17, 1.712598425089322918 ) ) ;
#7885=CARTESIAN_POINT ( 'NONE',  ( 1.002407869896990045, 0.1264236179284866091, 0.7357283464029290565 ) ) ;
#7886=EDGE_CURVE ( 'NONE', #40994, #426, #33577, .T. ) ;
#7888=LINE ( 'NONE', #19386, #14960 ) ;
#7889=CARTESIAN_POINT ( 'NONE',  ( 1.033464566929134687, 0.06523048226347956391, 1.144192913278300194 ) ) ;
#7893=CARTESIAN_POINT ( 'NONE',  ( 0.8107537697050253289, -0.1574803149606297803, 1.168799212490898354 ) ) ;
#7897=CARTESIAN_POINT ( 'NONE',  ( -0.7495606340400177148, -0.1264236179284866091, 0.4798228345919055560 ) ) ;
#7898=VERTEX_POINT ( 'NONE', #15118 ) ;
#7899=VERTEX_POINT ( 'NONE', #11514 ) ;
#7900=EDGE_LOOP ( 'NONE', ( #23747, #42863, #46854, #25233 ) ) ;
#7902=CARTESIAN_POINT ( 'NONE',  ( 0.8019270111902717657, 0.1787899950787401604, 1.732283464513166615 ) ) ;
#7903=CARTESIAN_POINT ( 'NONE',  ( -0.8019270111902717657, -0.1787899950787401604, 0.8415354330171019859 ) ) ;
#7905=CARTESIAN_POINT ( 'NONE',  ( 0.6971942568897637749, 2.189545951927499583E-17, 0.2829724408911185041 ) ) ;
#7906=EDGE_CURVE ( 'NONE', #19295, #24379, #37365, .T. ) ;
#7907=CARTESIAN_POINT ( 'NONE',  ( -0.6971942568897648851, -0.07405724077823297447, 1.304133858213953667 ) ) ;
#7908=CARTESIAN_POINT ( 'NONE',  ( -0.9500414927467377701, 0.1787899950787401604, 0.7775590550643457499 ) ) ;
#7909=CARTESIAN_POINT ( 'NONE',  ( -1.002407869896990045, 0.1264236179284866091, 0.9325787401037164415 ) ) ;
#7910=CARTESIAN_POINT ( 'NONE',  ( 0.8759842519685039353, 0.1574803149606299191, 0.9153543306011338032 ) ) ;
#7911=CARTESIAN_POINT ( 'NONE',  ( -0.7185039370078692977, 0.06523048226347515077, 1.670767716427905780 ) ) ;
#7912=CARTESIAN_POINT ( 'NONE',  ( -0.8759842519685039353, 0.1787899950787401882, 1.651082677111590513 ) ) ;
#7913=CARTESIAN_POINT ( 'NONE',  ( -0.7185039370078746268, 0.06523048226347956391, 1.906988188868851797 ) ) ;
#7914=ORIENTED_EDGE ( 'NONE', *, *, #38750, .F. ) ;
#7916=CARTESIAN_POINT ( 'NONE',  ( -0.9873396505805591694, -0.1113553986120547346, 1.619094488188976388 ) ) ;
#7919=CARTESIAN_POINT ( 'NONE',  ( 0.8759842519685039353, -0.1574803149606299191, 1.013779527451527551 ) ) ;
#7921=( BOUNDED_CURVE ( )  B_SPLINE_CURVE ( 2, ( #41386, #34734, #27076, #8588, #23225, #41624, #37839, #38302, #31139 ),
 .UNSPECIFIED., .F., .T. ) 
 B_SPLINE_CURVE_WITH_KNOTS ( ( 3, 2, 2, 2, 3 ),
 ( 0.3400000000000000244, 0.3425000000000000266, 0.3449999999999999734, 0.3474999999999999756, 0.3499999999999999778 ),
 .UNSPECIFIED. ) 
 CURVE ( )  GEOMETRIC_REPRESENTATION_ITEM ( )  RATIONAL_B_SPLINE_CURVE ( ( 1.000000000000000000, 0.9238795325112869605, 1.000000000000000000, 0.9238795325112869605, 1.000000000000000000, 0.9238795325112869605, 1.000000000000000000, 0.9238795325112849621, 1.000000000000000000 ) ) 
 REPRESENTATION_ITEM ( '' )  ) ;
#7927=DIRECTION ( 'NONE',  ( 1.000000000000000000, 0.000000000000000000, 0.000000000000000000 ) ) ;
#7928=CARTESIAN_POINT ( 'NONE',  ( 1.054774247047244540, 0.07405724077823318263, 1.756889763725764553 ) ) ;
#7935=CARTESIAN_POINT ( 'NONE',  ( 0.6971942568897626646, 0.07405724077823318263, 0.8267716534895444003 ) ) ;
#7936=( BOUNDED_SURFACE ( )  B_SPLINE_SURFACE ( 1, 2, ( 
 ( #41474, #30765, #4596, #23074, #44609, #34345, #19465, #1476, #27169, #16134, #33417, #15664, #11825, #33887, #531, #37445, #30302, #41721, #8925, #44852, #26213, #34118, #40780, #22596, #10539, #5560, #17705, #6913, #46935, #28279, #32354, #25134, #27411, #24669, #19933, #10296, #21056, #3080, #43338, #39266, #12774, #35697, #6444, #23776, #2833, #3329, #47179, #38390, #17467, #21535, #32590, #14125, #39725, #36172, #14366, #35918, #13639, #29011, #25389, #42842, #17937, #32101, #39501, #24909, #43567, #30991, #20170, #10781, #28766, #45554, #34569, #10054, #1965, #41955, #16367, #9161, #39967, #34823, #1722, #16596, #31878, #28522, #46457, #46691, #6677, #13879, #43093, #21293, #43807, #8094, #44497, #18640, #21782, #19112, #11007, #26089, #4472, #33779, #44267, #26338, #36867, #11241, #14830, #44736, #26574, #7161, #25853, #22236, #33299, #3568, #11716, #36411, #40899, #7859, #11955, #181, #22715, #423, #37323, #646, #22477, #888, #25627, #30194, #47417, #40435, #18183, #32825, #15548, #14592, #40203, #11467, #7398, #15076, #29264, #29953, #15300, #22009, #36632, #4020, #3796, #18414, #7617, #33061, #29495, #29723, #44043, #40664, #37093, #4241, #18874, #33532, #4969, #19596, #41844, #41366, #8566, #45681, #8804, #44969, #4727, #45929, #13141, #9293, #12182, #34455, #12668, #31119, #41129, #12432, #12901, #23199, #37815, #23671, #34237, #1368, #38045, #26807, #8328, #22958, #27535, #27051, #38517, #42086, #16024, #37568, #45448, #30647, #45210, #41601, #5203, #34941, #19350, #23439, #34005, #9050, #38278, #31347, #19827, #1603, #5448, #1134, #16254, #30889, #20063, #23913, #27295, #34706, #1850, #15792, #16487, #5688, #20300, #2088, #16717, #30420, #6625, #35644, #3017, #13580, #13823, #6141, #16950, #9997, #31587, #28712, #17652, #39207, #42337, #39673, #46170, #46638, #25081, #6856, #17410, #46877, #24611, #31818, #35412, #17890, #47120, #27778, #46404, #42782, #6385, #24155, #32300, #9532, #14063, #28466, #32535, #20768, #43284, #20997, #10484, #21239, #43033, #21474, #13367, #3265, #20538, #28219, #38760, #5921, #36111, #35173, #27994, #32048, #42558, #2784, #2316, #9768, #35867, #24378, #38977, #10239, #2551, #17183, #24847, #39446, #29680, #21963, #33249, #25331, #29208, #3974, #40152, #377, #47371, #14542, #29445, #3516, #18128, #36818, #7351, #21730, #10726, #26038, #40612, #15028, #36365, #3746, #14781, #22184, #14313, #36584, #18591, #32774, #43757, #25808, #10959, #25579, #18366, #33008, #28953, #43517, #44219, #131, #39919, #11419, #43996, #7106, #11197, #40381, #7571, #9923, #6545, #3431, #38905, #28146, #2473, #10401, #6779, #47280, #2932, #31741, #43429, #3182, #24303, #28871, #39830, #7022, #2709, #28382, #21397, #6066, #24767, #47037, #29116, #25243, #46329, #6301, #20691, #13740, #42950, #35332, #20924, #13981, #21646, #17099, #17811, #10158, #36279, #13512, #42704, #24530, #31972, #14229, #39130, #36022, #35566, #39600, #32459, #17337, #10638, #46797, #18045, #32689, #39364, #17569, #46556, #14457, #32208, #9690, #21156, #35790, #28631, #43189, #25003, #29597, #33872, #14694, #7484, #40763, #26197, #46, #30053, #14936, #990, #29818, #33631, #29368, #7958, #44595, #22578, #3890, #37192, #745, #3661, #290, #43668, #33399, #44140, #4336, #18968, #11339, #36506, #25951, #40530, #43908, #7719, #26434, #22809, #11109, #22336, #11811, #8185, #15406, #40998, #37422, #4577, #11570, #36731, #19212, #15647, #18515, #10879, #36964, #15174, #515, #25499, #7267, #25730, #40066, #21885, #18284, #32926, #33168, #40301, #22103, #4118, #18741, #44363, #26669, #31209, #34326, #19683, #8659, #35030, #8422, #12530, #44836, #1458, #23295, #2179, #23051, #27150, #12047, #23536, #4823, #16580, #23761, #41219, #1950, #12990, #27631, #37912, #16117, #27393, #37671, #45311, #20156, #30285, #45782, #19446, #26900, #34101, #30740, #41705, #1228, #41461, #34551, #42183, #15881, #38371, #8905, #9390, #30506, #45067, #12282, #5067, #34804, #38138, #41937, #5301, #12762, #9144, #19919, #5545, #1703, #24008, #38609, #16349, #30973, #45540, #5786, #20391, #25182, #46260, #32140, #42132, #5021, #34053, #23251, #27580, #8374, #1178, #34505, #19876, #41173, #23719, #8612, #9343, #23493, #27347, #23003, #1658, #38326, #16304, #45019, #30932, #41890, #44784, #41415, #37366, #27106, #37867, #45493, #12720, #19640, #30234, #34284, #1410, #37615, #16071, #20110, #16535, #4774, #30696, #5498, #1898, #9098, #34758, #31164, #45734, #5255, #30461, #12947, #4521, #12232, #19159, #45260, #8859, #41655, #33821, #938, #19402, #15598, #11998, #26618, #15839, #26856, #12481, #38093, #20349, #31400, #13866, #34988, #39489, #28041, #28754, #6666, #42381, #17229, #42826, #43078, #43321, #42601, #10283, #38800, #5959, #6426, #20579, #24197, #20813, #9579, #23962, #38569, #21282, #9812, #35907, #3062, #35223, #5734, #10040, #2359, #46210, #16992, #35451, #17691, #2132, #31634, #16761, #24658, #21045, #14110, #24421, #39022, #35686, #45972, #31864, #13411, #2823, #32340, #46921, #13185, #27820, #46444, #6189, #2595, #39252, #13625, #47166, #40189, #14349, #11457, #411, #21997, #25122, #22459, #28998, #29483, #7846, #37082, #173, #29709, #36621, #14577, #18171, #630, #29939, #10524, #29251, #25615, #3781, #6899, #15062, #39714, #44255, #11229, #15288, #3557, #26073, #18401, #40645, #4006, #25840, #4230, #43556, #33517, #3311, #43798, #21520, #36157, #18859, #17927, #10768, #14818, #25378, #33048, #32580, #33288, #18627, #39955, #7146, #44025, #21770, #36400, #10997, #32810, #47406, #40422, #7606, #22220, #36853, #16245, #30408, #41832, #8314, #22944, #45198, #11940, #26562, #1591, #12169, #15537, #8080, #16475, #5191, #15779, #23657, #11699, #19098, #41120, #19341, #30876, #33765, #8794, #30180, #23428, #38032, #37552, #19815, #34226, #34443, #9035, #44957, #4954, #4715, #12659, #19581, #27284, #38267, #5432, #44484, #26793, #33992, #41350, #34692, #1119, #8554, #20051, #26327, #23188, #40886, #37801, #22702, #30636, #37308, #1354, #4457, #16011, #9985, #38747, #28206, #35632, #38505, #35161, #31106, #20753, #31576, #13570, #6369, #2305, #23899, #46157, #16933, #34929, #13352, #13809, #10225, #2077, #27982, #17396, #43019, #42769, #20983, #32035, #24831, #46393, #24144, #39435, #35851, #5911, #28450, #42549, #2541, #35398, #2772, #42074, #31332 ),
 ( #9752, #24366, #20526, #21226, #45669, #12887, #38964, #6129, #17168, #27520, #46625, #9277, #6612, #31808, #5676, #24595, #20285, #39195, #16703, #45914, #13129, #42325, #9519, #8434, #4345, #8198, #3251, #15415, #4587, #44603, #25316, #30066, #22821, #25066, #21716, #17638, #7968, #18751, #756, #41007, #36348, #10469, #33409, #3502, #21462, #526, #1002, #44847, #36093, #15183, #19223, #30296, #11819, #37436, #33880, #12056, #33642, #10711, #26680, #23063, #39903, #15656, #29829, #37202, #22589, #41229, #28697, #17876, #37681, #26442, #43267, #32283, #7092, #47108, #39658, #14049, #6841, #46864, #32520, #14296, #44372, #11580, #43501, #28940, #26207, #40772, #18979, #45549, #26912, #38618, #45791, #19456, #24016, #35041, #2187, #45322, #23545, #1957, #34110, #19927, #42195, #24252, #20401, #8671, #1468, #1239, #8916, #38147, #15893, #16126, #9153, #16809, #45078, #12997, #5310, #31448, #30517, #23304, #5075, #27161, #9401, #37921, #16590, #19695, #34814, #31215, #30752, #27641, #41947, #5794, #46032, #34562, #12769, #34336, #13242, #27405, #27869, #42428, #9635, #4834, #1714, #12539, #16361, #12290, #41714, #30982, #23771, #38380, #5553, #20162, #42656, #21343, #3130, #35514, #35972, #28575, #17759, #36230, #10101, #46741, #24482, #32408, #13930, #46983, #3383, #25191, #43622, #6488, #2655, #24713, #29064, #9870, #17286, #14177, #28820, #39075, #39777, #39313, #10829, #24955, #43382, #6247, #10593, #6969, #21592, #46505, #17991, #32645, #46271, #42891, #38850, #43140, #21106, #47230, #14415, #35745, #31691, #2880, #17516, #20872, #32151, #6015, #20636, #31921, #10346, #35282, #2419, #17049, #13465, #28094, #13684, #6726, #28322, #39553, #44778, #7021, #3889, #29115, #36505, #40065, #25729, #39599, #14228, #11108, #45, #6778, #43188, #36278, #43428, #3181, #21396, #36021, #40300, #17810, #36730, #18044, #3430, #39829, #11994, #32458, #43667, #10400, #43907, #21645, #28870, #10637, #25242, #32688, #47279, #10878, #22102, #33167, #25498, #3660, #7266, #18283, #14693, #29367, #30230, #7483, #289, #18514, #15592, #2158, #35250, #42853, #6687, #31424, #46701, #24445, #17717, #5765, #27843, #38822, #13435, #43102, #42404, #35707, #16785, #2385, #10062, #21304, #46001, #13890, #39045, #32367, #20370, #9604, #5985, #28065, #10308, #24226, #2844, #20605, #21070, #17480, #17021, #32114, #28290, #28535, #35932, #6211, #46469, #31658, #24921, #13653, #39513, #3092, #46946, #43347, #20840, #46231, #35479, #28781, #42628, #2619, #14137, #10550, #17252, #38589, #31889, #35010, #24681, #39278, #6452, #22909, #12138, #4679, #33487, #37522, #30378, #33258, #29907, #25148, #15500, #26294, #8283, #1083, #44456, #18596, #40851, #11670, #29683, #8045, #8522, #4923, #44224, #22675, #26762, #37766, #19308, #15744, #41319, #19546, #41085, #18832, #34193, #30599, #603, #23150, #37275, #44684, #30146, #44924, #36826, #26046, #1321, #33962, #3978, #39738, #15260, #7813, #382, #21549, #15034, #15978, #11428, #45163, #4430, #19062, #4203, #6926, #40619, #33730, #22429, #841, #37050, #11902, #26524, #27005, #31538, #42515, #9718, #5392, #31072, #24105, #8758, #27488, #2272, #31771, #27948, #1556, #9000, #23395, #16443, #45636, #20488, #38712, #34898, #35126, #12854, #13092, #38234, #30843, #42039, #45410, #13317, #16896, #23859, #38000, #24331, #12623, #31300, #38930, #20716, #2039, #46119, #9241, #38471, #20015, #2505, #12384, #5159, #5641, #16671, #27725, #19780, #35360, #34413, #17129, #42287, #27246, #34654, #41800, #5882, #23624, #1804, #19384, #23235, #16053, #30680, #45243, #27084, #23477, #34487, #26258, #47089, #39889, #40352, #29178, #11165, #14283, #28923, #43487, #10932, #7074, #32982, #25553, #40124, #105, #25782, #7545, #22156, #36791, #15471, #30349, #41768, #8488, #19984, #33933, #1055, #23365, #22880, #37492, #27217, #37736, #26495, #33698, #27457, #42002, #38202, #41057, #15947, #41523, #12594, #22647, #41288, #8971, #4650, #19276, #5125, #15714, #44897, #19514, #8255, #37251, #4403, #23590, #23123, #34623, #5364, #12110, #19031, #26970, #4892, #34162, #1292, #30573, #16412, #44653, #45134, #11870, #19751, #34386, #12825, #12351, #8729, #1525, #16179, #30810, #45379, #1773, #31039, #45606, #27695, #24302, #42949, #21155, #39129, #31971, #10157, #2931, #24529, #2241, #17568, #28630, #16861, #6544, #2472, #28145, #46328, #13739, #20217, #9457, #46555, #6300, #34865, #9206, #31504, #38684, #31271, #5609, #16641, #17336, #2013, #24766, #13290, #46087, #35094, #23826, #45850, #38904, #38441, #17098, #13057, #32207, #2708, #42257, #28381, #46796, #24075, #6065, #31740, #20923, #5851, #13511, #20460, #42703, #9922, #35565, #21105, #20870, #28573, #21342, #2654, #35744, #10592, #40018, #17285, #43621, #32406, #14033, #46504, #13682, #24711, #13929, #10828, #42890, #21591, #10100, #6968, #36229, #46982, #7213, #39776, #21836, #29315, #43862, #39312, #6487, #22768, #18928, #40953, #23012, #44794, #15847, #26146, #22290, #44323, #1188, #29547, #36925, #37376, #4532, #14886, #26628, #29774, #30470, #44555, #946, #44099, #19169, #41180, #33827, #18693, #15605, #30243, #18467, #15129, #11063, #701, #11526, #37625, #4783, #7916, #3846, #22530, #37148, #11293, #4296, #19409, #34060, #25682, #25905, #22061, #33588, #36686, #33354, #15359, #242, #33118, #30009, #474, #11773, #26391, #16766, #30941, #42386, #8868, #23499, #45744, #45268, #12489, #2140, #12726, #1419, #8622, #2365, #17002, #13191, #16078, #38332, #16544, #34995, #45026, #16313, #31407, #27114, #41662, #27591, #38102, #5265, #41899, #30703, #12241, #26864, #45982, #45502, #9586, #27827, #19884, #41425, #1908, #34513, #1666, #27356, #9108, #38808, #23260, #23728, #37875, #12953, #42140, #35233, #5505, #20118, #9349, #5028, #34765, #31171, #23970, #24205, #5967, #5742, #38573, #20357, #20586, #19650, #34294, #24664, #20820, #13872, #35459, #47173, #21527, #43087, #46216, #43562, #2602, #3070, #29004, #10773, #21288, #3319, #28515, #2828, #39259, #21776, #3563, #31641, #17461, #46684, #10291, #28049, #36165, #13417, #17932, #32348, #36405, #6435, #14356, #24901, #39960, #25129, #46928, #7153, #17235, #9823, #24428, #32095, #39028, #6197, #31871, #46450, #13633, #17700, #28272, #39496, #42836, #6905, #14118, #6670, #28760, #21051, #43330, #10532, #39719, #40428, #40195, #25846, #26332 ) ),
 .UNSPECIFIED., .F., .F., .F. ) 
 B_SPLINE_SURFACE_WITH_KNOTS ( ( 2, 2 ),
 ( 3, 2, 2, 2, 2, 2, 2, 2, 2, 2, 2, 2, 2, 2, 2, 2, 2, 2, 2, 2, 2, 2, 2, 2, 2, 2, 2, 2, 2, 2, 2, 2, 2, 2, 2, 2, 2, 2, 2, 2, 2, 2, 2, 2, 2, 2, 2, 2, 2, 2, 2, 2, 2, 2, 2, 2, 2, 2, 2, 2, 2, 2, 2, 2, 2, 2, 2, 2, 2, 2, 2, 2, 2, 2, 2, 2, 2, 2, 2, 2, 2, 2, 2, 2, 2, 2, 2, 2, 2, 2, 2, 2, 2, 2, 2, 2, 2, 2, 2, 2, 2, 2, 2, 2, 2, 2, 2, 2, 2, 2, 2, 2, 2, 2, 2, 2, 2, 2, 2, 2, 2, 2, 2, 2, 2, 2, 2, 2, 2, 2, 2, 2, 2, 2, 2, 2, 2, 2, 2, 2, 2, 2, 2, 2, 2, 2, 2, 2, 2, 2, 2, 2, 2, 2, 2, 2, 2, 2, 2, 2, 2, 2, 2, 2, 2, 2, 2, 2, 2, 2, 2, 2, 2, 2, 2, 2, 2, 2, 2, 2, 2, 2, 2, 2, 2, 2, 2, 2, 2, 2, 2, 2, 2, 2, 2, 2, 2, 2, 2, 2, 2, 2, 2, 2, 2, 2, 2, 2, 2, 2, 2, 2, 2, 2, 2, 2, 2, 2, 2, 2, 2, 2, 2, 2, 2, 2, 2, 2, 2, 2, 2, 2, 2, 2, 2, 2, 2, 2, 2, 2, 2, 2, 2, 2, 2, 2, 2, 2, 2, 2, 2, 2, 2, 2, 2, 2, 2, 2, 2, 2, 2, 2, 2, 2, 2, 2, 2, 2, 2, 2, 2, 2, 2, 2, 2, 2, 2, 2, 2, 2, 2, 2, 2, 2, 2, 2, 2, 2, 2, 2, 2, 2, 2, 2, 2, 2, 2, 2, 2, 2, 2, 2, 2, 2, 2, 2, 2, 2, 2, 2, 2, 2, 2, 2, 2, 2, 2, 2, 2, 2, 2, 2, 2, 2, 2, 2, 2, 2, 2, 2, 2, 2, 2, 2, 2, 2, 2, 2, 2, 2, 2, 2, 2, 2, 2, 2, 2, 2, 2, 2, 2, 2, 2, 2, 2, 2, 2, 2, 2, 2, 2, 2, 2, 2, 2, 2, 2, 2, 2, 2, 2, 2, 2, 2, 2, 2, 2, 2, 2, 2, 2, 2, 2, 2, 2, 2, 2, 2, 2, 2, 2, 2, 2, 2, 2, 2, 2, 2, 2, 2, 3 ),
 ( 0.000000000000000000, 1.000000000000000000 ),
 ( 0.000000000000000000, 0.002500000000000000052, 0.005000000000000000104, 0.007499999999999999722, 0.01000000000000000021, 0.01250000000000000069, 0.01499999999999999944, 0.01750000000000000167, 0.02000000000000000042, 0.02249999999999999917, 0.02500000000000000139, 0.02750000000000000014, 0.02999999999999999889, 0.03250000000000000111, 0.03500000000000000333, 0.03749999999999999861, 0.04000000000000000083, 0.04250000000000000305, 0.04499999999999999833, 0.04750000000000000056, 0.05000000000000000278, 0.05249999999999999806, 0.05500000000000000028, 0.05750000000000000250, 0.05999999999999999778, 0.06250000000000000000, 0.06500000000000000222, 0.06750000000000000444, 0.07000000000000000666, 0.07249999999999999500, 0.07499999999999999722, 0.07749999999999999944, 0.08000000000000000167, 0.08250000000000000389, 0.08500000000000000611, 0.08749999999999999445, 0.08999999999999999667, 0.09249999999999999889, 0.09500000000000000111, 0.09750000000000000333, 0.1000000000000000056, 0.1024999999999999939, 0.1049999999999999961, 0.1074999999999999983, 0.1100000000000000006, 0.1125000000000000028, 0.1150000000000000050, 0.1174999999999999933, 0.1199999999999999956, 0.1224999999999999978, 0.1250000000000000000, 0.1275000000000000022, 0.1300000000000000044, 0.1325000000000000067, 0.1350000000000000089, 0.1375000000000000111, 0.1400000000000000133, 0.1424999999999999878, 0.1449999999999999900, 0.1474999999999999922, 0.1499999999999999944, 0.1524999999999999967, 0.1549999999999999989, 0.1575000000000000011, 0.1600000000000000033, 0.1625000000000000056, 0.1650000000000000078, 0.1675000000000000100, 0.1700000000000000122, 0.1724999999999999867, 0.1749999999999999889, 0.1774999999999999911, 0.1799999999999999933, 0.1824999999999999956, 0.1849999999999999978, 0.1875000000000000000, 0.1900000000000000022, 0.1925000000000000044, 0.1950000000000000067, 0.1975000000000000089, 0.2000000000000000111, 0.2025000000000000133, 0.2049999999999999878, 0.2074999999999999900, 0.2099999999999999922, 0.2124999999999999944, 0.2149999999999999967, 0.2174999999999999989, 0.2200000000000000011, 0.2225000000000000033, 0.2250000000000000056, 0.2275000000000000078, 0.2300000000000000100, 0.2325000000000000122, 0.2349999999999999867, 0.2374999999999999889, 0.2399999999999999911, 0.2424999999999999933, 0.2449999999999999956, 0.2474999999999999978, 0.2500000000000000000, 0.2525000000000000022, 0.2550000000000000044, 0.2575000000000000067, 0.2600000000000000089, 0.2625000000000000111, 0.2650000000000000133, 0.2675000000000000155, 0.2700000000000000178, 0.2725000000000000200, 0.2750000000000000222, 0.2775000000000000244, 0.2800000000000000266, 0.2824999999999999734, 0.2849999999999999756, 0.2874999999999999778, 0.2899999999999999800, 0.2924999999999999822, 0.2949999999999999845, 0.2974999999999999867, 0.2999999999999999889, 0.3024999999999999911, 0.3049999999999999933, 0.3074999999999999956, 0.3099999999999999978, 0.3125000000000000000, 0.3150000000000000022, 0.3175000000000000044, 0.3200000000000000067, 0.3225000000000000089, 0.3250000000000000111, 0.3275000000000000133, 0.3300000000000000155, 0.3325000000000000178, 0.3350000000000000200, 0.3375000000000000222, 0.3400000000000000244, 0.3425000000000000266, 0.3449999999999999734, 0.3474999999999999756, 0.3499999999999999778, 0.3524999999999999800, 0.3549999999999999822, 0.3574999999999999845, 0.3599999999999999867, 0.3624999999999999889, 0.3649999999999999911, 0.3674999999999999933, 0.3699999999999999956, 0.3724999999999999978, 0.3750000000000000000, 0.3775000000000000022, 0.3800000000000000044, 0.3825000000000000067, 0.3850000000000000089, 0.3875000000000000111, 0.3900000000000000133, 0.3925000000000000155, 0.3950000000000000178, 0.3975000000000000200, 0.4000000000000000222, 0.4025000000000000244, 0.4050000000000000266, 0.4074999999999999734, 0.4099999999999999756, 0.4124999999999999778, 0.4149999999999999800, 0.4174999999999999822, 0.4199999999999999845, 0.4224999999999999867, 0.4249999999999999889, 0.4274999999999999911, 0.4299999999999999933, 0.4324999999999999956, 0.4349999999999999978, 0.4375000000000000000, 0.4400000000000000022, 0.4425000000000000044, 0.4450000000000000067, 0.4475000000000000089, 0.4500000000000000111, 0.4525000000000000133, 0.4550000000000000155, 0.4575000000000000178, 0.4600000000000000200, 0.4625000000000000222, 0.4650000000000000244, 0.4675000000000000266, 0.4699999999999999734, 0.4724999999999999756, 0.4749999999999999778, 0.4774999999999999800, 0.4799999999999999822, 0.4824999999999999845, 0.4849999999999999867, 0.4874999999999999889, 0.4899999999999999911, 0.4924999999999999933, 0.4949999999999999956, 0.4974999999999999978, 0.5000000000000000000, 0.5024999999999999467, 0.5050000000000000044, 0.5074999999999999512, 0.5100000000000000089, 0.5124999999999999556, 0.5150000000000000133, 0.5174999999999999600, 0.5200000000000000178, 0.5224999999999999645, 0.5250000000000000222, 0.5274999999999999689, 0.5300000000000000266, 0.5324999999999999734, 0.5350000000000000311, 0.5374999999999999778, 0.5400000000000000355, 0.5424999999999999822, 0.5450000000000000400, 0.5474999999999999867, 0.5500000000000000444, 0.5524999999999999911, 0.5550000000000000488, 0.5574999999999999956, 0.5600000000000000533, 0.5625000000000000000, 0.5649999999999999467, 0.5675000000000000044, 0.5699999999999999512, 0.5725000000000000089, 0.5749999999999999556, 0.5775000000000000133, 0.5799999999999999600, 0.5825000000000000178, 0.5849999999999999645, 0.5875000000000000222, 0.5899999999999999689, 0.5925000000000000266, 0.5949999999999999734, 0.5975000000000000311, 0.5999999999999999778, 0.6025000000000000355, 0.6049999999999999822, 0.6075000000000000400, 0.6099999999999999867, 0.6125000000000000444, 0.6149999999999999911, 0.6175000000000000488, 0.6199999999999999956, 0.6225000000000000533, 0.6250000000000000000, 0.6274999999999999467, 0.6300000000000000044, 0.6324999999999999512, 0.6350000000000000089, 0.6374999999999999556, 0.6400000000000000133, 0.6424999999999999600, 0.6450000000000000178, 0.6474999999999999645, 0.6500000000000000222, 0.6524999999999999689, 0.6550000000000000266, 0.6574999999999999734, 0.6600000000000000311, 0.6624999999999999778, 0.6650000000000000355, 0.6674999999999999822, 0.6700000000000000400, 0.6724999999999999867, 0.6750000000000000444, 0.6774999999999999911, 0.6800000000000000488, 0.6824999999999999956, 0.6850000000000000533, 0.6875000000000000000, 0.6899999999999999467, 0.6925000000000000044, 0.6949999999999999512, 0.6975000000000000089, 0.6999999999999999556, 0.7025000000000000133, 0.7049999999999999600, 0.7075000000000000178, 0.7099999999999999645, 0.7125000000000000222, 0.7149999999999999689, 0.7175000000000000266, 0.7199999999999999734, 0.7225000000000000311, 0.7249999999999999778, 0.7275000000000000355, 0.7299999999999999822, 0.7325000000000000400, 0.7349999999999999867, 0.7375000000000000444, 0.7399999999999999911, 0.7425000000000000488, 0.7449999999999999956, 0.7475000000000000533, 0.7500000000000000000, 0.7524999999999999467, 0.7550000000000000044, 0.7574999999999999512, 0.7600000000000000089, 0.7624999999999999556, 0.7650000000000000133, 0.7674999999999999600, 0.7700000000000000178, 0.7724999999999999645, 0.7750000000000000222, 0.7774999999999999689, 0.7800000000000000266, 0.7824999999999999734, 0.7850000000000000311, 0.7874999999999999778, 0.7900000000000000355, 0.7924999999999999822, 0.7950000000000000400, 0.7974999999999999867, 0.8000000000000000444, 0.8024999999999999911, 0.8050000000000000488, 0.8074999999999999956, 0.8100000000000000533, 0.8125000000000000000, 0.8149999999999999467, 0.8175000000000000044, 0.8199999999999999512, 0.8225000000000000089, 0.8249999999999999556, 0.8275000000000000133, 0.8299999999999999600, 0.8325000000000000178, 0.8349999999999999645, 0.8375000000000000222, 0.8399999999999999689, 0.8425000000000000266, 0.8449999999999999734, 0.8475000000000000311, 0.8499999999999999778, 0.8525000000000000355, 0.8549999999999999822, 0.8575000000000000400, 0.8599999999999999867, 0.8625000000000000444, 0.8649999999999999911, 0.8675000000000000488, 0.8699999999999999956, 0.8725000000000000533, 0.8750000000000000000, 0.8774999999999999467, 0.8800000000000000044, 0.8824999999999999512, 0.8850000000000000089, 0.8874999999999999556, 0.8900000000000000133, 0.8924999999999999600, 0.8950000000000000178, 0.8974999999999999645, 0.9000000000000000222, 0.9024999999999999689, 0.9050000000000000266, 0.9074999999999999734, 0.9100000000000000311, 0.9124999999999999778, 0.9150000000000000355, 0.9174999999999999822, 0.9200000000000000400, 0.9224999999999999867, 0.9250000000000000444, 0.9274999999999999911, 0.9300000000000000488, 0.9324999999999999956, 0.9350000000000000533, 0.9375000000000000000, 0.9399999999999999467, 0.9425000000000000044, 0.9449999999999999512, 0.9475000000000000089, 0.9499999999999999556, 0.9525000000000000133, 0.9549999999999999600, 0.9575000000000000178, 0.9599999999999999645, 0.9625000000000000222, 0.9649999999999999689, 0.9675000000000000266, 0.9699999999999999734, 0.9725000000000000311, 0.9749999999999999778, 0.9775000000000000355, 0.9799999999999999822, 0.9825000000000000400, 0.9849999999999999867, 0.9875000000000000444, 0.9899999999999999911, 0.9925000000000000488, 0.9949999999999999956, 0.9975000000000000533, 1.000000000000000000 ),
 .UNSPECIFIED. ) 
 GEOMETRIC_REPRESENTATION_ITEM ( )  RATIONAL_B_SPLINE_SURFACE ( (
 ( 1.000000000000000000, 0.9238795325112869605, 1.000000000000000000, 0.9238795325112869605, 1.000000000000000000, 0.9238795325112869605, 1.000000000000000000, 0.9238795325112869605, 1.000000000000000000, 0.9238795325112869605, 1.000000000000000000, 0.9238795325112869605, 1.000000000000000000, 0.9238795325112869605, 1.000000000000000000, 0.9238795325112869605, 1.000000000000000000, 0.9238795325112869605, 1.000000000000000000, 0.9238795325112869605, 1.000000000000000000, 0.9238795325112869605, 1.000000000000000000, 0.9238795325112869605, 1.000000000000000000, 0.9238795325112869605, 1.000000000000000000, 0.9238795325112869605, 1.000000000000000000, 0.9238795325112869605, 1.000000000000000000, 0.9238795325112869605, 1.000000000000000000, 0.9238795325112869605, 1.000000000000000000, 0.9238795325112869605, 1.000000000000000000, 0.9238795325112869605, 1.000000000000000000, 0.9238795325112869605, 1.000000000000000000, 0.9238795325112869605, 1.000000000000000000, 0.9238795325112869605, 1.000000000000000000, 0.9238795325112869605, 1.000000000000000000, 0.9238795325112869605, 1.000000000000000000, 0.9238795325112869605, 1.000000000000000000, 0.9238795325112869605, 1.000000000000000000, 0.9238795325112869605, 1.000000000000000000, 0.9238795325112869605, 1.000000000000000000, 0.9238795325112869605, 1.000000000000000000, 0.9238795325112869605, 1.000000000000000000, 0.9238795325112869605, 1.000000000000000000, 0.9238795325112869605, 1.000000000000000000, 0.9238795325112869605, 1.000000000000000000, 0.9238795325112869605, 1.000000000000000000, 0.9238795325112869605, 1.000000000000000000, 0.9238795325112869605, 1.000000000000000000, 0.9238795325112869605, 1.000000000000000000, 0.9238795325112869605, 1.000000000000000000, 0.9238795325112869605, 1.000000000000000000, 0.9238795325112869605, 1.000000000000000000, 0.9238795325112869605, 1.000000000000000000, 0.9238795325112869605, 1.000000000000000000, 0.9238795325112869605, 1.000000000000000000, 0.9238795325112869605, 1.000000000000000000, 0.9238795325112869605, 1.000000000000000000, 0.9238795325112869605, 1.000000000000000000, 0.9238795325112869605, 1.000000000000000000, 0.9238795325112869605, 1.000000000000000000, 0.9238795325112869605, 1.000000000000000000, 0.9238795325112869605, 1.000000000000000000, 0.9238795325112869605, 1.000000000000000000, 0.9238795325112869605, 1.000000000000000000, 0.9238795325112869605, 1.000000000000000000, 0.9238795325112869605, 1.000000000000000000, 0.9238795325112869605, 1.000000000000000000, 0.9238795325112869605, 1.000000000000000000, 0.9238795325112869605, 1.000000000000000000, 0.9238795325112869605, 1.000000000000000000, 0.9238795325112869605, 1.000000000000000000, 0.9238795325112869605, 1.000000000000000000, 0.9238795325112869605, 1.000000000000000000, 0.9238795325112869605, 1.000000000000000000, 0.9238795325112869605, 1.000000000000000000, 0.9238795325112869605, 1.000000000000000000, 0.9238795325112869605, 1.000000000000000000, 0.9238795325112869605, 1.000000000000000000, 0.9238795325112869605, 1.000000000000000000, 0.9238795325112869605, 1.000000000000000000, 0.9238795325112869605, 1.000000000000000000, 0.9238795325112869605, 1.000000000000000000, 0.9238795325112869605, 1.000000000000000000, 0.9238795325112869605, 1.000000000000000000, 0.9238795325112869605, 1.000000000000000000, 0.9238795325112869605, 1.000000000000000000, 0.9238795325112869605, 1.000000000000000000, 0.9238795325112869605, 1.000000000000000000, 0.9238795325112869605, 1.000000000000000000, 0.9238795325112869605, 1.000000000000000000, 0.9238795325112869605, 1.000000000000000000, 0.9238795325112869605, 1.000000000000000000, 0.9238795325112869605, 1.000000000000000000, 0.9238795325112869605, 1.000000000000000000, 0.9238795325112869605, 1.000000000000000000, 0.9238795325112869605, 1.000000000000000000, 0.9238795325112869605, 1.000000000000000000, 0.9238795325112869605, 1.000000000000000000, 0.9238795325112869605, 1.000000000000000000, 0.9238795325112869605, 1.000000000000000000, 0.9238795325112869605, 1.000000000000000000, 0.9238795325112869605, 1.000000000000000000, 0.9238795325112869605, 1.000000000000000000, 0.9238795325112869605, 1.000000000000000000, 0.9238795325112869605, 1.000000000000000000, 0.9238795325112869605, 1.000000000000000000, 0.9238795325112869605, 1.000000000000000000, 0.9238795325112869605, 1.000000000000000000, 0.9238795325112869605, 1.000000000000000000, 0.9238795325112869605, 1.000000000000000000, 0.9238795325112869605, 1.000000000000000000, 0.9238795325112869605, 1.000000000000000000, 0.9238795325112869605, 1.000000000000000000, 0.9238795325112869605, 1.000000000000000000, 0.9238795325112869605, 1.000000000000000000, 0.9238795325112869605, 1.000000000000000000, 0.9238795325112869605, 1.000000000000000000, 0.9238795325112869605, 1.000000000000000000, 0.9238795325112869605, 1.000000000000000000, 0.9238795325112869605, 1.000000000000000000, 0.9238795325112869605, 1.000000000000000000, 0.9238795325112869605, 1.000000000000000000, 0.9238795325112869605, 1.000000000000000000, 0.9238795325112869605, 1.000000000000000000, 0.9238795325112869605, 1.000000000000000000, 0.9238795325112869605, 1.000000000000000000, 0.9238795325112869605, 1.000000000000000000, 0.9238795325112869605, 1.000000000000000000, 0.9238795325112869605, 1.000000000000000000, 0.9238795325112869605, 1.000000000000000000, 0.9238795325112869605, 1.000000000000000000, 0.9238795325112869605, 1.000000000000000000, 0.9238795325112869605, 1.000000000000000000, 0.9238795325112869605, 1.000000000000000000, 0.9238795325112869605, 1.000000000000000000, 0.9238795325112869605, 1.000000000000000000, 0.9238795325112869605, 1.000000000000000000, 0.9238795325112869605, 1.000000000000000000, 0.9238795325112869605, 1.000000000000000000, 0.9238795325112869605, 1.000000000000000000, 0.9238795325112869605, 1.000000000000000000, 0.9238795325112869605, 1.000000000000000000, 0.9238795325112869605, 1.000000000000000000, 0.9238795325112869605, 1.000000000000000000, 0.9238795325112869605, 1.000000000000000000, 0.9238795325112869605, 1.000000000000000000, 0.9238795325112869605, 1.000000000000000000, 0.9238795325112869605, 1.000000000000000000, 0.9238795325112869605, 1.000000000000000000, 0.9238795325112869605, 1.000000000000000000, 0.9238795325112869605, 1.000000000000000000, 0.9238795325112869605, 1.000000000000000000, 0.9238795325112869605, 1.000000000000000000, 0.9238795325112869605, 1.000000000000000000, 0.9238795325112869605, 1.000000000000000000, 0.9238795325112869605, 1.000000000000000000, 0.9238795325112869605, 1.000000000000000000, 0.9238795325112869605, 1.000000000000000000, 0.9238795325112869605, 1.000000000000000000, 0.9238795325112869605, 1.000000000000000000, 0.9238795325112869605, 1.000000000000000000, 0.9238795325112869605, 1.000000000000000000, 0.9238795325112869605, 1.000000000000000000, 0.9238795325112869605, 1.000000000000000000, 0.9238795325112869605, 1.000000000000000000, 0.9238795325112869605, 1.000000000000000000, 0.9238795325112869605, 1.000000000000000000, 0.9238795325112869605, 1.000000000000000000, 0.9238795325112869605, 1.000000000000000000, 0.9238795325112869605, 1.000000000000000000, 0.9238795325112869605, 1.000000000000000000, 0.9238795325112869605, 1.000000000000000000, 0.9238795325112869605, 1.000000000000000000, 0.9238795325112869605, 1.000000000000000000, 0.9238795325112869605, 1.000000000000000000, 0.9238795325112869605, 1.000000000000000000, 0.9238795325112869605, 1.000000000000000000, 0.9238795325112869605, 1.000000000000000000, 0.9238795325112869605, 1.000000000000000000, 0.9238795325112869605, 1.000000000000000000, 0.9238795325112869605, 1.000000000000000000, 0.9238795325112869605, 1.000000000000000000, 0.9238795325112869605, 1.000000000000000000, 0.9238795325112869605, 1.000000000000000000, 0.9238795325112869605, 1.000000000000000000, 0.9238795325112869605, 1.000000000000000000, 0.9238795325112869605, 1.000000000000000000, 0.9238795325112869605, 1.000000000000000000, 0.9238795325112869605, 1.000000000000000000, 0.9238795325112869605, 1.000000000000000000, 0.9238795325112869605, 1.000000000000000000, 0.9238795325112869605, 1.000000000000000000, 0.9238795325112869605, 1.000000000000000000, 0.9238795325112869605, 1.000000000000000000, 0.9238795325112869605, 1.000000000000000000, 0.9238795325112869605, 1.000000000000000000, 0.9238795325112869605, 1.000000000000000000, 0.9238795325112869605, 1.000000000000000000, 0.9238795325112869605, 1.000000000000000000, 0.9238795325112869605, 1.000000000000000000, 0.9238795325112869605, 1.000000000000000000, 0.9238795325112869605, 1.000000000000000000, 0.9238795325112869605, 1.000000000000000000, 0.9238795325112869605, 1.000000000000000000, 0.9238795325112869605, 1.000000000000000000, 0.9238795325112869605, 1.000000000000000000, 0.9238795325112869605, 1.000000000000000000, 0.9238795325112869605, 1.000000000000000000, 0.9238795325112869605, 1.000000000000000000, 0.9238795325112869605, 1.000000000000000000, 0.9238795325112869605, 1.000000000000000000, 0.9238795325112869605, 1.000000000000000000, 0.9238795325112869605, 1.000000000000000000, 0.9238795325112869605, 1.000000000000000000, 0.9238795325112869605, 1.000000000000000000, 0.9238795325112869605, 1.000000000000000000, 0.9238795325112869605, 1.000000000000000000, 0.9238795325112869605, 1.000000000000000000, 0.9238795325112869605, 1.000000000000000000, 0.9238795325112869605, 1.000000000000000000, 0.9238795325112869605, 1.000000000000000000, 0.9238795325112869605, 1.000000000000000000, 0.9238795325112869605, 1.000000000000000000, 0.9238795325112869605, 1.000000000000000000, 0.9238795325112869605, 1.000000000000000000, 0.9238795325112869605, 1.000000000000000000, 0.9238795325112869605, 1.000000000000000000, 0.9238795325112869605, 1.000000000000000000, 0.9238795325112869605, 1.000000000000000000, 0.9238795325112869605, 1.000000000000000000, 0.9238795325112869605, 1.000000000000000000, 0.9238795325112869605, 1.000000000000000000, 0.9238795325112869605, 1.000000000000000000, 0.9238795325112869605, 1.000000000000000000, 0.9238795325112869605, 1.000000000000000000, 0.9238795325112869605, 1.000000000000000000, 0.9238795325112869605, 1.000000000000000000, 0.9238795325112869605, 1.000000000000000000, 0.9238795325112869605, 1.000000000000000000, 0.9238795325112869605, 1.000000000000000000, 0.9238795325112869605, 1.000000000000000000, 0.9238795325112869605, 1.000000000000000000, 0.9238795325112869605, 1.000000000000000000, 0.9238795325112869605, 1.000000000000000000, 0.9238795325112869605, 1.000000000000000000, 0.9238795325112869605, 1.000000000000000000, 0.9238795325112869605, 1.000000000000000000, 0.9238795325112869605, 1.000000000000000000, 0.9238795325112869605, 1.000000000000000000, 0.9238795325112869605, 1.000000000000000000, 0.9238795325112869605, 1.000000000000000000, 0.9238795325112869605, 1.000000000000000000, 0.9238795325112869605, 1.000000000000000000, 0.9238795325112869605, 1.000000000000000000, 0.9238795325112869605, 1.000000000000000000, 0.9238795325112869605, 1.000000000000000000, 0.9238795325112869605, 1.000000000000000000, 0.9238795325112869605, 1.000000000000000000, 0.9238795325112869605, 1.000000000000000000, 0.9238795325112869605, 1.000000000000000000, 0.9238795325112869605, 1.000000000000000000, 0.9238795325112869605, 1.000000000000000000, 0.9238795325112869605, 1.000000000000000000, 0.9238795325112869605, 1.000000000000000000, 0.9238795325112869605, 1.000000000000000000, 0.9238795325112869605, 1.000000000000000000, 0.9238795325112869605, 1.000000000000000000, 0.9238795325112869605, 1.000000000000000000, 0.9238795325112869605, 1.000000000000000000, 0.9238795325112869605, 1.000000000000000000, 0.9238795325112869605, 1.000000000000000000, 0.9238795325112869605, 1.000000000000000000, 0.9238795325112869605, 1.000000000000000000, 0.9238795325112869605, 1.000000000000000000, 0.9238795325112869605, 1.000000000000000000, 0.9238795325112869605, 1.000000000000000000, 0.9238795325112869605, 1.000000000000000000, 0.9238795325112869605, 1.000000000000000000, 0.9238795325112869605, 1.000000000000000000, 0.9238795325112869605, 1.000000000000000000, 0.9238795325112869605, 1.000000000000000000, 0.9238795325112869605, 1.000000000000000000, 0.9238795325112869605, 1.000000000000000000, 0.9238795325112869605, 1.000000000000000000, 0.9238795325112869605, 1.000000000000000000, 0.9238795325112869605, 1.000000000000000000, 0.9238795325112869605, 1.000000000000000000, 0.9238795325112869605, 1.000000000000000000, 0.9238795325112869605, 1.000000000000000000, 0.9238795325112869605, 1.000000000000000000, 0.9238795325112869605, 1.000000000000000000, 0.9238795325112869605, 1.000000000000000000, 0.9238795325112869605, 1.000000000000000000, 0.9238795325112869605, 1.000000000000000000, 0.9238795325112869605, 1.000000000000000000, 0.9238795325112869605, 1.000000000000000000, 0.9238795325112869605, 1.000000000000000000, 0.9238795325112869605, 1.000000000000000000, 0.9238795325112869605, 1.000000000000000000, 0.9238795325112869605, 1.000000000000000000, 0.9238795325112869605, 1.000000000000000000, 0.9238795325112869605, 1.000000000000000000, 0.9238795325112869605, 1.000000000000000000, 0.9238795325112869605, 1.000000000000000000, 0.9238795325112869605, 1.000000000000000000, 0.9238795325112869605, 1.000000000000000000, 0.9238795325112869605, 1.000000000000000000, 0.9238795325112869605, 1.000000000000000000, 0.9238795325112869605, 1.000000000000000000, 0.9238795325112869605, 1.000000000000000000, 0.9238795325112869605, 1.000000000000000000, 0.9238795325112869605, 1.000000000000000000, 0.9238795325112869605, 1.000000000000000000, 0.9238795325112869605, 1.000000000000000000, 0.9238795325112869605, 1.000000000000000000, 0.9238795325112869605, 1.000000000000000000, 0.9238795325112869605, 1.000000000000000000, 0.9238795325112869605, 1.000000000000000000, 0.9238795325112869605, 1.000000000000000000, 0.9238795325112869605, 1.000000000000000000, 0.9238795325112869605, 1.000000000000000000, 0.9238795325112869605, 1.000000000000000000, 0.9238795325112869605, 1.000000000000000000, 0.9238795325112869605, 1.000000000000000000, 0.9238795325112869605, 1.000000000000000000, 0.9238795325112869605, 1.000000000000000000, 0.9238795325112869605, 1.000000000000000000, 0.9238795325112869605, 1.000000000000000000, 0.9238795325112869605, 1.000000000000000000, 0.9238795325112869605, 1.000000000000000000, 0.9238795325112869605, 1.000000000000000000, 0.9238795325112869605, 1.000000000000000000, 0.9238795325112869605, 1.000000000000000000, 0.9238795325112869605, 1.000000000000000000, 0.9238795325112869605, 1.000000000000000000, 0.9238795325112869605, 1.000000000000000000, 0.9238795325112869605, 1.000000000000000000, 0.9238795325112869605, 1.000000000000000000, 0.9238795325112869605, 1.000000000000000000, 0.9238795325112869605, 1.000000000000000000, 0.9238795325112869605, 1.000000000000000000, 0.9238795325112869605, 1.000000000000000000, 0.9238795325112869605, 1.000000000000000000, 0.9238795325112869605, 1.000000000000000000, 0.9238795325112869605, 1.000000000000000000, 0.9238795325112869605, 1.000000000000000000, 0.9238795325112869605, 1.000000000000000000, 0.9238795325112869605, 1.000000000000000000, 0.9238795325112869605, 1.000000000000000000, 0.9238795325112869605, 1.000000000000000000, 0.9238795325112869605, 1.000000000000000000, 0.9238795325112869605, 1.000000000000000000, 0.9238795325112869605, 1.000000000000000000, 0.9238795325112869605, 1.000000000000000000, 0.9238795325112869605, 1.000000000000000000, 0.9238795325112869605, 1.000000000000000000, 0.9238795325112869605, 1.000000000000000000, 0.9238795325112869605, 1.000000000000000000, 0.9238795325112869605, 1.000000000000000000, 0.9238795325112869605, 1.000000000000000000, 0.9238795325112869605, 1.000000000000000000, 0.9238795325112869605, 1.000000000000000000, 0.9238795325112869605, 1.000000000000000000, 0.9238795325112869605, 1.000000000000000000, 0.9238795325112869605, 1.000000000000000000, 0.9238795325112869605, 1.000000000000000000, 0.9238795325112869605, 1.000000000000000000, 0.9238795325112869605, 1.000000000000000000, 0.9238795325112869605, 1.000000000000000000, 0.9238795325112869605, 1.000000000000000000, 0.9238795325112869605, 1.000000000000000000, 0.9238795325112869605, 1.000000000000000000, 0.9238795325112869605, 1.000000000000000000, 0.9238795325112869605, 1.000000000000000000, 0.9238795325112869605, 1.000000000000000000, 0.9238795325112869605, 1.000000000000000000, 0.9238795325112869605, 1.000000000000000000, 0.9238795325112869605, 1.000000000000000000, 0.9238795325112869605, 1.000000000000000000, 0.9238795325112869605, 1.000000000000000000, 0.9238795325112869605, 1.000000000000000000, 0.9238795325112869605, 1.000000000000000000, 0.9238795325112869605, 1.000000000000000000, 0.9238795325112869605, 1.000000000000000000, 0.9238795325112869605, 1.000000000000000000, 0.9238795325112869605, 1.000000000000000000, 0.9238795325112869605, 1.000000000000000000, 0.9238795325112869605, 1.000000000000000000, 0.9238795325112869605, 1.000000000000000000, 0.9238795325112869605, 1.000000000000000000, 0.9238795325112869605, 1.000000000000000000, 0.9238795325112869605, 1.000000000000000000, 0.9238795325112869605, 1.000000000000000000, 0.9238795325112869605, 1.000000000000000000, 0.9238795325112869605, 1.000000000000000000, 0.9238795325112869605, 1.000000000000000000, 0.9238795325112869605, 1.000000000000000000, 0.9238795325112869605, 1.000000000000000000, 0.9238795325112869605, 1.000000000000000000, 0.9238795325112869605, 1.000000000000000000, 0.9238795325112869605, 1.000000000000000000, 0.9238795325112869605, 1.000000000000000000, 0.9238795325112869605, 1.000000000000000000, 0.9238795325112869605, 1.000000000000000000, 0.9238795325112869605, 1.000000000000000000, 0.9238795325112869605, 1.000000000000000000, 0.9238795325112869605, 1.000000000000000000, 0.9238795325112869605, 1.000000000000000000, 0.9238795325112869605, 1.000000000000000000, 0.9238795325112869605, 1.000000000000000000, 0.9238795325112869605, 1.000000000000000000, 0.9238795325112869605, 1.000000000000000000),
 ( 1.000000000000000000, 0.9238795325112869605, 1.000000000000000000, 0.9238795325112869605, 1.000000000000000000, 0.9238795325112869605, 1.000000000000000000, 0.9238795325112869605, 1.000000000000000000, 0.9238795325112869605, 1.000000000000000000, 0.9238795325112869605, 1.000000000000000000, 0.9238795325112869605, 1.000000000000000000, 0.9238795325112869605, 1.000000000000000000, 0.9238795325112869605, 1.000000000000000000, 0.9238795325112869605, 1.000000000000000000, 0.9238795325112869605, 1.000000000000000000, 0.9238795325112869605, 1.000000000000000000, 0.9238795325112869605, 1.000000000000000000, 0.9238795325112869605, 1.000000000000000000, 0.9238795325112869605, 1.000000000000000000, 0.9238795325112869605, 1.000000000000000000, 0.9238795325112869605, 1.000000000000000000, 0.9238795325112869605, 1.000000000000000000, 0.9238795325112869605, 1.000000000000000000, 0.9238795325112869605, 1.000000000000000000, 0.9238795325112869605, 1.000000000000000000, 0.9238795325112869605, 1.000000000000000000, 0.9238795325112869605, 1.000000000000000000, 0.9238795325112869605, 1.000000000000000000, 0.9238795325112869605, 1.000000000000000000, 0.9238795325112869605, 1.000000000000000000, 0.9238795325112869605, 1.000000000000000000, 0.9238795325112869605, 1.000000000000000000, 0.9238795325112869605, 1.000000000000000000, 0.9238795325112869605, 1.000000000000000000, 0.9238795325112869605, 1.000000000000000000, 0.9238795325112869605, 1.000000000000000000, 0.9238795325112869605, 1.000000000000000000, 0.9238795325112869605, 1.000000000000000000, 0.9238795325112869605, 1.000000000000000000, 0.9238795325112869605, 1.000000000000000000, 0.9238795325112869605, 1.000000000000000000, 0.9238795325112869605, 1.000000000000000000, 0.9238795325112869605, 1.000000000000000000, 0.9238795325112869605, 1.000000000000000000, 0.9238795325112869605, 1.000000000000000000, 0.9238795325112869605, 1.000000000000000000, 0.9238795325112869605, 1.000000000000000000, 0.9238795325112869605, 1.000000000000000000, 0.9238795325112869605, 1.000000000000000000, 0.9238795325112869605, 1.000000000000000000, 0.9238795325112869605, 1.000000000000000000, 0.9238795325112869605, 1.000000000000000000, 0.9238795325112869605, 1.000000000000000000, 0.9238795325112869605, 1.000000000000000000, 0.9238795325112869605, 1.000000000000000000, 0.9238795325112869605, 1.000000000000000000, 0.9238795325112869605, 1.000000000000000000, 0.9238795325112869605, 1.000000000000000000, 0.9238795325112869605, 1.000000000000000000, 0.9238795325112869605, 1.000000000000000000, 0.9238795325112869605, 1.000000000000000000, 0.9238795325112869605, 1.000000000000000000, 0.9238795325112869605, 1.000000000000000000, 0.9238795325112869605, 1.000000000000000000, 0.9238795325112869605, 1.000000000000000000, 0.9238795325112869605, 1.000000000000000000, 0.9238795325112869605, 1.000000000000000000, 0.9238795325112869605, 1.000000000000000000, 0.9238795325112869605, 1.000000000000000000, 0.9238795325112869605, 1.000000000000000000, 0.9238795325112869605, 1.000000000000000000, 0.9238795325112869605, 1.000000000000000000, 0.9238795325112869605, 1.000000000000000000, 0.9238795325112869605, 1.000000000000000000, 0.9238795325112869605, 1.000000000000000000, 0.9238795325112869605, 1.000000000000000000, 0.9238795325112869605, 1.000000000000000000, 0.9238795325112869605, 1.000000000000000000, 0.9238795325112869605, 1.000000000000000000, 0.9238795325112869605, 1.000000000000000000, 0.9238795325112869605, 1.000000000000000000, 0.9238795325112869605, 1.000000000000000000, 0.9238795325112869605, 1.000000000000000000, 0.9238795325112869605, 1.000000000000000000, 0.9238795325112869605, 1.000000000000000000, 0.9238795325112869605, 1.000000000000000000, 0.9238795325112869605, 1.000000000000000000, 0.9238795325112869605, 1.000000000000000000, 0.9238795325112869605, 1.000000000000000000, 0.9238795325112869605, 1.000000000000000000, 0.9238795325112869605, 1.000000000000000000, 0.9238795325112869605, 1.000000000000000000, 0.9238795325112869605, 1.000000000000000000, 0.9238795325112869605, 1.000000000000000000, 0.9238795325112869605, 1.000000000000000000, 0.9238795325112869605, 1.000000000000000000, 0.9238795325112869605, 1.000000000000000000, 0.9238795325112869605, 1.000000000000000000, 0.9238795325112869605, 1.000000000000000000, 0.9238795325112869605, 1.000000000000000000, 0.9238795325112869605, 1.000000000000000000, 0.9238795325112869605, 1.000000000000000000, 0.9238795325112869605, 1.000000000000000000, 0.9238795325112869605, 1.000000000000000000, 0.9238795325112869605, 1.000000000000000000, 0.9238795325112869605, 1.000000000000000000, 0.9238795325112869605, 1.000000000000000000, 0.9238795325112869605, 1.000000000000000000, 0.9238795325112869605, 1.000000000000000000, 0.9238795325112869605, 1.000000000000000000, 0.9238795325112869605, 1.000000000000000000, 0.9238795325112869605, 1.000000000000000000, 0.9238795325112869605, 1.000000000000000000, 0.9238795325112869605, 1.000000000000000000, 0.9238795325112869605, 1.000000000000000000, 0.9238795325112869605, 1.000000000000000000, 0.9238795325112869605, 1.000000000000000000, 0.9238795325112869605, 1.000000000000000000, 0.9238795325112869605, 1.000000000000000000, 0.9238795325112869605, 1.000000000000000000, 0.9238795325112869605, 1.000000000000000000, 0.9238795325112869605, 1.000000000000000000, 0.9238795325112869605, 1.000000000000000000, 0.9238795325112869605, 1.000000000000000000, 0.9238795325112869605, 1.000000000000000000, 0.9238795325112869605, 1.000000000000000000, 0.9238795325112869605, 1.000000000000000000, 0.9238795325112869605, 1.000000000000000000, 0.9238795325112869605, 1.000000000000000000, 0.9238795325112869605, 1.000000000000000000, 0.9238795325112869605, 1.000000000000000000, 0.9238795325112869605, 1.000000000000000000, 0.9238795325112869605, 1.000000000000000000, 0.9238795325112869605, 1.000000000000000000, 0.9238795325112869605, 1.000000000000000000, 0.9238795325112869605, 1.000000000000000000, 0.9238795325112869605, 1.000000000000000000, 0.9238795325112869605, 1.000000000000000000, 0.9238795325112869605, 1.000000000000000000, 0.9238795325112869605, 1.000000000000000000, 0.9238795325112869605, 1.000000000000000000, 0.9238795325112869605, 1.000000000000000000, 0.9238795325112869605, 1.000000000000000000, 0.9238795325112869605, 1.000000000000000000, 0.9238795325112869605, 1.000000000000000000, 0.9238795325112869605, 1.000000000000000000, 0.9238795325112869605, 1.000000000000000000, 0.9238795325112869605, 1.000000000000000000, 0.9238795325112869605, 1.000000000000000000, 0.9238795325112869605, 1.000000000000000000, 0.9238795325112869605, 1.000000000000000000, 0.9238795325112869605, 1.000000000000000000, 0.9238795325112869605, 1.000000000000000000, 0.9238795325112869605, 1.000000000000000000, 0.9238795325112869605, 1.000000000000000000, 0.9238795325112869605, 1.000000000000000000, 0.9238795325112869605, 1.000000000000000000, 0.9238795325112869605, 1.000000000000000000, 0.9238795325112869605, 1.000000000000000000, 0.9238795325112869605, 1.000000000000000000, 0.9238795325112869605, 1.000000000000000000, 0.9238795325112869605, 1.000000000000000000, 0.9238795325112869605, 1.000000000000000000, 0.9238795325112869605, 1.000000000000000000, 0.9238795325112869605, 1.000000000000000000, 0.9238795325112869605, 1.000000000000000000, 0.9238795325112869605, 1.000000000000000000, 0.9238795325112869605, 1.000000000000000000, 0.9238795325112869605, 1.000000000000000000, 0.9238795325112869605, 1.000000000000000000, 0.9238795325112869605, 1.000000000000000000, 0.9238795325112869605, 1.000000000000000000, 0.9238795325112869605, 1.000000000000000000, 0.9238795325112869605, 1.000000000000000000, 0.9238795325112869605, 1.000000000000000000, 0.9238795325112869605, 1.000000000000000000, 0.9238795325112869605, 1.000000000000000000, 0.9238795325112869605, 1.000000000000000000, 0.9238795325112869605, 1.000000000000000000, 0.9238795325112869605, 1.000000000000000000, 0.9238795325112869605, 1.000000000000000000, 0.9238795325112869605, 1.000000000000000000, 0.9238795325112869605, 1.000000000000000000, 0.9238795325112869605, 1.000000000000000000, 0.9238795325112869605, 1.000000000000000000, 0.9238795325112869605, 1.000000000000000000, 0.9238795325112869605, 1.000000000000000000, 0.9238795325112869605, 1.000000000000000000, 0.9238795325112869605, 1.000000000000000000, 0.9238795325112869605, 1.000000000000000000, 0.9238795325112869605, 1.000000000000000000, 0.9238795325112869605, 1.000000000000000000, 0.9238795325112869605, 1.000000000000000000, 0.9238795325112869605, 1.000000000000000000, 0.9238795325112869605, 1.000000000000000000, 0.9238795325112869605, 1.000000000000000000, 0.9238795325112869605, 1.000000000000000000, 0.9238795325112869605, 1.000000000000000000, 0.9238795325112869605, 1.000000000000000000, 0.9238795325112869605, 1.000000000000000000, 0.9238795325112869605, 1.000000000000000000, 0.9238795325112869605, 1.000000000000000000, 0.9238795325112869605, 1.000000000000000000, 0.9238795325112869605, 1.000000000000000000, 0.9238795325112869605, 1.000000000000000000, 0.9238795325112869605, 1.000000000000000000, 0.9238795325112869605, 1.000000000000000000, 0.9238795325112869605, 1.000000000000000000, 0.9238795325112869605, 1.000000000000000000, 0.9238795325112869605, 1.000000000000000000, 0.9238795325112869605, 1.000000000000000000, 0.9238795325112869605, 1.000000000000000000, 0.9238795325112869605, 1.000000000000000000, 0.9238795325112869605, 1.000000000000000000, 0.9238795325112869605, 1.000000000000000000, 0.9238795325112869605, 1.000000000000000000, 0.9238795325112869605, 1.000000000000000000, 0.9238795325112869605, 1.000000000000000000, 0.9238795325112869605, 1.000000000000000000, 0.9238795325112869605, 1.000000000000000000, 0.9238795325112869605, 1.000000000000000000, 0.9238795325112869605, 1.000000000000000000, 0.9238795325112869605, 1.000000000000000000, 0.9238795325112869605, 1.000000000000000000, 0.9238795325112869605, 1.000000000000000000, 0.9238795325112869605, 1.000000000000000000, 0.9238795325112869605, 1.000000000000000000, 0.9238795325112869605, 1.000000000000000000, 0.9238795325112869605, 1.000000000000000000, 0.9238795325112869605, 1.000000000000000000, 0.9238795325112869605, 1.000000000000000000, 0.9238795325112869605, 1.000000000000000000, 0.9238795325112869605, 1.000000000000000000, 0.9238795325112869605, 1.000000000000000000, 0.9238795325112869605, 1.000000000000000000, 0.9238795325112869605, 1.000000000000000000, 0.9238795325112869605, 1.000000000000000000, 0.9238795325112869605, 1.000000000000000000, 0.9238795325112869605, 1.000000000000000000, 0.9238795325112869605, 1.000000000000000000, 0.9238795325112869605, 1.000000000000000000, 0.9238795325112869605, 1.000000000000000000, 0.9238795325112869605, 1.000000000000000000, 0.9238795325112869605, 1.000000000000000000, 0.9238795325112869605, 1.000000000000000000, 0.9238795325112869605, 1.000000000000000000, 0.9238795325112869605, 1.000000000000000000, 0.9238795325112869605, 1.000000000000000000, 0.9238795325112869605, 1.000000000000000000, 0.9238795325112869605, 1.000000000000000000, 0.9238795325112869605, 1.000000000000000000, 0.9238795325112869605, 1.000000000000000000, 0.9238795325112869605, 1.000000000000000000, 0.9238795325112869605, 1.000000000000000000, 0.9238795325112869605, 1.000000000000000000, 0.9238795325112869605, 1.000000000000000000, 0.9238795325112869605, 1.000000000000000000, 0.9238795325112869605, 1.000000000000000000, 0.9238795325112869605, 1.000000000000000000, 0.9238795325112869605, 1.000000000000000000, 0.9238795325112869605, 1.000000000000000000, 0.9238795325112869605, 1.000000000000000000, 0.9238795325112869605, 1.000000000000000000, 0.9238795325112869605, 1.000000000000000000, 0.9238795325112869605, 1.000000000000000000, 0.9238795325112869605, 1.000000000000000000, 0.9238795325112869605, 1.000000000000000000, 0.9238795325112869605, 1.000000000000000000, 0.9238795325112869605, 1.000000000000000000, 0.9238795325112869605, 1.000000000000000000, 0.9238795325112869605, 1.000000000000000000, 0.9238795325112869605, 1.000000000000000000, 0.9238795325112869605, 1.000000000000000000, 0.9238795325112869605, 1.000000000000000000, 0.9238795325112869605, 1.000000000000000000, 0.9238795325112869605, 1.000000000000000000, 0.9238795325112869605, 1.000000000000000000, 0.9238795325112869605, 1.000000000000000000, 0.9238795325112869605, 1.000000000000000000, 0.9238795325112869605, 1.000000000000000000, 0.9238795325112869605, 1.000000000000000000, 0.9238795325112869605, 1.000000000000000000, 0.9238795325112869605, 1.000000000000000000, 0.9238795325112869605, 1.000000000000000000, 0.9238795325112869605, 1.000000000000000000, 0.9238795325112869605, 1.000000000000000000, 0.9238795325112869605, 1.000000000000000000, 0.9238795325112869605, 1.000000000000000000, 0.9238795325112869605, 1.000000000000000000, 0.9238795325112869605, 1.000000000000000000, 0.9238795325112869605, 1.000000000000000000, 0.9238795325112869605, 1.000000000000000000, 0.9238795325112869605, 1.000000000000000000, 0.9238795325112869605, 1.000000000000000000, 0.9238795325112869605, 1.000000000000000000, 0.9238795325112869605, 1.000000000000000000, 0.9238795325112869605, 1.000000000000000000, 0.9238795325112869605, 1.000000000000000000, 0.9238795325112869605, 1.000000000000000000, 0.9238795325112869605, 1.000000000000000000, 0.9238795325112869605, 1.000000000000000000, 0.9238795325112869605, 1.000000000000000000, 0.9238795325112869605, 1.000000000000000000, 0.9238795325112869605, 1.000000000000000000, 0.9238795325112869605, 1.000000000000000000, 0.9238795325112869605, 1.000000000000000000, 0.9238795325112869605, 1.000000000000000000, 0.9238795325112869605, 1.000000000000000000, 0.9238795325112869605, 1.000000000000000000, 0.9238795325112869605, 1.000000000000000000, 0.9238795325112869605, 1.000000000000000000, 0.9238795325112869605, 1.000000000000000000, 0.9238795325112869605, 1.000000000000000000, 0.9238795325112869605, 1.000000000000000000, 0.9238795325112869605, 1.000000000000000000, 0.9238795325112869605, 1.000000000000000000, 0.9238795325112869605, 1.000000000000000000, 0.9238795325112869605, 1.000000000000000000, 0.9238795325112869605, 1.000000000000000000, 0.9238795325112869605, 1.000000000000000000, 0.9238795325112869605, 1.000000000000000000, 0.9238795325112869605, 1.000000000000000000, 0.9238795325112869605, 1.000000000000000000, 0.9238795325112869605, 1.000000000000000000, 0.9238795325112869605, 1.000000000000000000, 0.9238795325112869605, 1.000000000000000000, 0.9238795325112869605, 1.000000000000000000, 0.9238795325112869605, 1.000000000000000000, 0.9238795325112869605, 1.000000000000000000, 0.9238795325112869605, 1.000000000000000000, 0.9238795325112869605, 1.000000000000000000, 0.9238795325112869605, 1.000000000000000000, 0.9238795325112869605, 1.000000000000000000, 0.9238795325112869605, 1.000000000000000000, 0.9238795325112869605, 1.000000000000000000, 0.9238795325112869605, 1.000000000000000000, 0.9238795325112869605, 1.000000000000000000, 0.9238795325112869605, 1.000000000000000000, 0.9238795325112869605, 1.000000000000000000, 0.9238795325112869605, 1.000000000000000000, 0.9238795325112869605, 1.000000000000000000, 0.9238795325112869605, 1.000000000000000000, 0.9238795325112869605, 1.000000000000000000, 0.9238795325112869605, 1.000000000000000000, 0.9238795325112869605, 1.000000000000000000, 0.9238795325112869605, 1.000000000000000000, 0.9238795325112869605, 1.000000000000000000, 0.9238795325112869605, 1.000000000000000000, 0.9238795325112869605, 1.000000000000000000, 0.9238795325112869605, 1.000000000000000000, 0.9238795325112869605, 1.000000000000000000, 0.9238795325112869605, 1.000000000000000000, 0.9238795325112869605, 1.000000000000000000, 0.9238795325112869605, 1.000000000000000000, 0.9238795325112869605, 1.000000000000000000, 0.9238795325112869605, 1.000000000000000000, 0.9238795325112869605, 1.000000000000000000, 0.9238795325112869605, 1.000000000000000000, 0.9238795325112869605, 1.000000000000000000, 0.9238795325112869605, 1.000000000000000000, 0.9238795325112869605, 1.000000000000000000, 0.9238795325112869605, 1.000000000000000000, 0.9238795325112869605, 1.000000000000000000, 0.9238795325112869605, 1.000000000000000000, 0.9238795325112869605, 1.000000000000000000, 0.9238795325112869605, 1.000000000000000000, 0.9238795325112869605, 1.000000000000000000, 0.9238795325112869605, 1.000000000000000000, 0.9238795325112869605, 1.000000000000000000, 0.9238795325112869605, 1.000000000000000000, 0.9238795325112869605, 1.000000000000000000, 0.9238795325112869605, 1.000000000000000000, 0.9238795325112869605, 1.000000000000000000, 0.9238795325112869605, 1.000000000000000000, 0.9238795325112869605, 1.000000000000000000, 0.9238795325112869605, 1.000000000000000000, 0.9238795325112869605, 1.000000000000000000, 0.9238795325112869605, 1.000000000000000000, 0.9238795325112869605, 1.000000000000000000, 0.9238795325112869605, 1.000000000000000000, 0.9238795325112869605, 1.000000000000000000, 0.9238795325112869605, 1.000000000000000000, 0.9238795325112869605, 1.000000000000000000, 0.9238795325112869605, 1.000000000000000000, 0.9238795325112869605, 1.000000000000000000, 0.9238795325112869605, 1.000000000000000000, 0.9238795325112869605, 1.000000000000000000, 0.9238795325112869605, 1.000000000000000000, 0.9238795325112869605, 1.000000000000000000, 0.9238795325112869605, 1.000000000000000000, 0.9238795325112869605, 1.000000000000000000, 0.9238795325112869605, 1.000000000000000000, 0.9238795325112869605, 1.000000000000000000, 0.9238795325112869605, 1.000000000000000000, 0.9238795325112869605, 1.000000000000000000, 0.9238795325112869605, 1.000000000000000000, 0.9238795325112869605, 1.000000000000000000, 0.9238795325112869605, 1.000000000000000000, 0.9238795325112869605, 1.000000000000000000, 0.9238795325112869605, 1.000000000000000000, 0.9238795325112869605, 1.000000000000000000, 0.9238795325112869605, 1.000000000000000000, 0.9238795325112869605, 1.000000000000000000, 0.9238795325112869605, 1.000000000000000000) ) ) 
 REPRESENTATION_ITEM ( '' )  SURFACE ( )  ) ;
#7937=CARTESIAN_POINT ( 'NONE',  ( -0.7185039370078739607, 1.928577636452523993E-17, 1.555118110128692832 ) ) ;
#7938=LINE ( 'NONE', #2798, #32839 ) ;
#7939=CARTESIAN_POINT ( 'NONE',  ( -0.9893807788331910880, -0.1382476043231838647, 1.990360454373647947 ) ) ;
#7941=CARTESIAN_POINT ( 'NONE',  ( 0.7185039370078746268, -0.06523048226347956391, 1.252460629921259061 ) ) ;
#7942=CARTESIAN_POINT ( 'NONE',  ( 1.002407869896990045, -0.1264236179284866091, 1.793799212544661348 ) ) ;
#7943=DIRECTION ( 'NONE',  ( 1.000000000000000000, 0.000000000000000000, 0.000000000000000000 ) ) ;
#7945=CARTESIAN_POINT ( 'NONE',  ( 0.7185039370078746268, 0.06523048226347956391, 0.1058070866141733041 ) ) ;
#7950=CARTESIAN_POINT ( 'NONE',  ( 0.8759842519685039353, -0.1787899950787401882, 0.2534448818360003908 ) ) ;
#7952=CARTESIAN_POINT ( 'NONE',  ( 1.033464566929134687, 0.06523048226347956391, 0.05167322834645669133 ) ) ;
#7953=CARTESIAN_POINT ( 'NONE',  ( -0.6971942568897637749, 2.189545951927499583E-17, 1.813484251914740053 ) ) ;
#7954=ORIENTED_EDGE ( 'NONE', *, *, #25911, .F. ) ;
#7956=CARTESIAN_POINT ( 'NONE',  ( 1.054774247047244540, -0.07405724077823318263, 1.323818897584032817 ) ) ;
#7957=CARTESIAN_POINT ( 'NONE',  ( 1.002407869896990045, -0.1264236179284866091, 1.985728346402929168 ) ) ;
#7958=CARTESIAN_POINT ( 'NONE',  ( -1.002407869896990045, 0.1264236179284866091, 1.011318897584031484 ) ) ;
#7961=LINE ( 'NONE', #40069, #39215 ) ;
#7962=CARTESIAN_POINT ( 'NONE',  ( 0.9500414927467377701, 0.1787899950787401604, 0.5068897637257642197 ) ) ;
#7963=CARTESIAN_POINT ( 'NONE',  ( -1.002407869896990045, -0.1264236179284866091, 0.3715551180564728440 ) ) ;
#7964=CARTESIAN_POINT ( 'NONE',  ( -0.6971942568897637749, 2.189545951927499583E-17, 0.6717519684501732646 ) ) ;
#7965=CARTESIAN_POINT ( 'NONE',  ( 0.7185039370078746268, -0.06523048226347956391, 1.675688976270425679 ) ) ;
#7968=CARTESIAN_POINT ( 'NONE',  ( -0.8759842519685039353, 0.1574803149606299191, 0.09842519685039370636 ) ) ;
#7969=CARTESIAN_POINT ( 'NONE',  ( 0.8019270111902716547, -0.1787899950787401604, 1.077755905458048113 ) ) ;
#7970=CARTESIAN_POINT ( 'NONE',  ( -0.8759842519685039353, -0.1787899950787401882, 1.980807086560409491 ) ) ;
#7971=AXIS2_PLACEMENT_3D ( 'NONE', #21970, #25586, #32547 ) ;
#7973=CARTESIAN_POINT ( 'NONE',  ( -0.8019270111902717657, -0.1787899950787401604, 0.8809055117572599514 ) ) ;
#7980=CARTESIAN_POINT ( 'NONE',  ( 0.6971942568897648851, -0.07405724077823297447, 1.225393700733637514 ) ) ;
#7983=CARTESIAN_POINT ( 'NONE',  ( 1.002407869896990045, -0.1264236179284866091, 1.513287401521039355 ) ) ;
#7984=CARTESIAN_POINT ( 'NONE',  ( 0.6971942568897626646, 0.07405724077823318263, 0.1181102361667090567 ) ) ;
#7988=CARTESIAN_POINT ( 'NONE',  ( -1.033464566929134687, -0.06523048226347956391, 1.139271653435781184 ) ) ;
#7989=ORIENTED_EDGE ( 'NONE', *, *, #24157, .F. ) ;
#7990=CARTESIAN_POINT ( 'NONE',  ( -0.9500414927467377701, -0.1787899950787401604, 0.6102362204186774219 ) ) ;
#7993=CARTESIAN_POINT ( 'NONE',  ( 0.8759842519685039353, 0.000000000000000000, 4.498031496062992574 ) ) ;
#7996=CARTESIAN_POINT ( 'NONE',  ( 0.8019270111902717657, 0.1787899950787401604, 1.338582677111590069 ) ) ;
#7997=CARTESIAN_POINT ( 'NONE',  ( 0.7495606340400177148, 0.1264236179284866091, 1.651082677111590513 ) ) ;
#8002=CARTESIAN_POINT ( 'NONE',  ( 0.7646288533564489232, -0.1113553986120547346, 0.8120078739082204899 ) ) ;
#8004=EDGE_CURVE ( 'NONE', #10926, #31032, #27855, .T. ) ;
#8005=DIRECTION ( 'NONE',  ( 1.000000000000000000, 0.000000000000000000, -1.822029033848725275E-16 ) ) ;
#8007=CARTESIAN_POINT ( 'NONE',  ( 0.8107537697050253289, 0.1574803149606300301, 0.6815944880814486240 ) ) ;
#8009=CARTESIAN_POINT ( 'NONE',  ( -0.8019270111902717657, 0.1787899950787401604, 1.062992125930488418 ) ) ;
#8011=ORIENTED_EDGE ( 'NONE', *, *, #47, .T. ) ;
#8015=CARTESIAN_POINT ( 'NONE',  ( 1.002407869896990045, -0.1264236179284866091, 1.552657480261196765 ) ) ;
#8017=CARTESIAN_POINT ( 'NONE',  ( -0.7185039370078739607, 1.928577636452523993E-17, 0.9350393700787401619 ) ) ;
#8019=CARTESIAN_POINT ( 'NONE',  ( 0.8759842519685039353, 0.1574803149606299191, 0.3641732282389295583 ) ) ;
#8021=CARTESIAN_POINT ( 'NONE',  ( 0.9412147342319837628, 0.1574803149606300301, 1.306594488081449290 ) ) ;
#8022=EDGE_LOOP ( 'NONE', ( #19176, #42426, #17165, #14056 ) ) ;
#8025=CARTESIAN_POINT ( 'NONE',  ( 0.8019270111902717657, -0.1787899950787401604, 0.6840551180564720113 ) ) ;
#8026=CARTESIAN_POINT ( 'NONE',  ( 0.7495606340400177148, 0.1264236179284866091, 0.8686023621509606496 ) ) ;
#8028=CARTESIAN_POINT ( 'NONE',  ( -1.054774247047244540, 0.07405724077823318263, 1.289370078686393750 ) ) ;
#8029=CARTESIAN_POINT ( 'NONE',  ( -0.7495606340400177148, -0.1264236179284866091, 0.2878937007336381804 ) ) ;
#8033=DIRECTION ( 'NONE',  ( -1.000000000000000000, 0.000000000000000000, 0.000000000000000000 ) ) ;
#8043=( BOUNDED_CURVE ( )  B_SPLINE_CURVE ( 2, ( #3470, #35826, #21192, #17846, #39396, #25767, #40337, #10916, #39630 ),
 .UNSPECIFIED., .F., .T. ) 
 B_SPLINE_CURVE_WITH_KNOTS ( ( 3, 2, 2, 2, 3 ),
 ( 0.5000000000000000000, 0.5024999999999999467, 0.5050000000000000044, 0.5074999999999999512, 0.5100000000000000089 ),
 .UNSPECIFIED. ) 
 CURVE ( )  GEOMETRIC_REPRESENTATION_ITEM ( )  RATIONAL_B_SPLINE_CURVE ( ( 1.000000000000000000, 0.9238795325112869605, 1.000000000000000000, 0.9238795325112869605, 1.000000000000000000, 0.9238795325112869605, 1.000000000000000000, 0.9238795325112869605, 1.000000000000000000 ) ) 
 REPRESENTATION_ITEM ( '' )  ) ;
#8044=CARTESIAN_POINT ( 'NONE',  ( -0.8759842519685039353, 0.1787899950787401882, 0.1550196849856066983 ) ) ;
#8045=CARTESIAN_POINT ( 'NONE',  ( -0.7185039370078746268, 0.06523048226347956391, 0.8538385826771660581 ) ) ;
#8050=CARTESIAN_POINT ( 'NONE',  ( -1.033464566929133799, 0.000000000000000000, 1.496062992018456494 ) ) ;
#8051=ADVANCED_FACE ( 'NONE', ( #12718 ), #20578, .T. ) ;
#8052=CARTESIAN_POINT ( 'NONE',  ( 1.054774247047244540, -0.07405724077823318263, 0.9301181101824563813 ) ) ;
#8053=CARTESIAN_POINT ( 'NONE',  ( 0.8019270111902716547, -0.1787899950787401604, 0.1279527558517483676 ) ) ;
#8054=CARTESIAN_POINT ( 'NONE',  ( 0.8759842519685039353, 0.1574803149606299191, 0.5216535431995598104 ) ) ;
#8055=CARTESIAN_POINT ( 'NONE',  ( 0.8759842519685039353, -0.1574803149606299191, 1.338582677165354395 ) ) ;
#8056=CARTESIAN_POINT ( 'NONE',  ( 0.7249778915871685214, -0.07478501380931205922, 1.984713715274026846 ) ) ;
#8057=CYLINDRICAL_SURFACE ( 'NONE', #27660, 0.1574803149606299191 ) ;
#8060=CARTESIAN_POINT ( 'NONE',  ( 0.9500414927467377701, -0.1787899950787401604, 0.8809055117572600624 ) ) ;
#8065=CARTESIAN_POINT ( 'NONE',  ( -0.7185039370078739607, 0.000000000000000000, -2.869337061179095023E-17 ) ) ;
#8069=CARTESIAN_POINT ( 'NONE',  ( 0.6971942568897648851, -0.07405724077823297447, 1.146653543253323582 ) ) ;
#8070=EDGE_CURVE ( 'NONE', #6712, #7899, #21370, .T. ) ;
#8073=CARTESIAN_POINT ( 'NONE',  ( -0.7185039370078746268, -0.06523048226347956391, 0.5044291338582675976 ) ) ;
#8074=VERTEX_POINT ( 'NONE', #27345 ) ;
#8076=CARTESIAN_POINT ( 'NONE',  ( -0.6971942568897626646, 0.07405724077823318263, 0.2755905511273391006 ) ) ;
#8077=ORIENTED_EDGE ( 'NONE', *, *, #13535, .T. ) ;
#8078=CARTESIAN_POINT ( 'NONE',  ( -0.7646288533564489232, -0.1113553986120547346, 0.7037401574803149318 ) ) ;
#8080=CARTESIAN_POINT ( 'NONE',  ( -0.8759842519685039353, -0.1787899950787401882, 1.783956692859621995 ) ) ;
#8081=CARTESIAN_POINT ( 'NONE',  ( -0.7495606340400177148, 0.1264236179284866091, 0.9030511810485984947 ) ) ;
#8082=CARTESIAN_POINT ( 'NONE',  ( -1.054774247047244540, -0.07405724077823318263, 0.5364173227808821665 ) ) ;
#8083=CARTESIAN_POINT ( 'NONE',  ( -1.033464566929134687, -0.06523048226347956391, 0.1156496061916856694 ) ) ;
#8091=CARTESIAN_POINT ( 'NONE',  ( 1.033464566929134687, 0.06523048226347956391, 1.783956692913386544 ) ) ;
#8093=CARTESIAN_POINT ( 'NONE',  ( 0.7185039370078739607, 1.928577636452523993E-17, 1.555118110128692832 ) ) ;
#8094=CARTESIAN_POINT ( 'NONE',  ( -0.6971942568897626646, -0.07405724077823297447, 0.2411417322297011168 ) ) ;
#8099=CARTESIAN_POINT ( 'NONE',  ( -1.002407869896990045, -0.1264236179284866091, 1.557578740103716441 ) ) ;
#8100=ORIENTED_EDGE ( 'NONE', *, *, #20127, .F. ) ;
#8104=LINE ( 'NONE', #22726, #25588 ) ;
#8106=CARTESIAN_POINT ( 'NONE',  ( 1.033464566929134687, 0.06523048226347956391, 0.4847440944881890590 ) ) ;
#8108=CARTESIAN_POINT ( 'NONE',  ( -1.033464566929134687, -0.06523048226347956391, 1.139271653435780962 ) ) ;
#8109=EDGE_CURVE ( 'NONE', #20455, #1535, #42495, .T. ) ;
#8111=CARTESIAN_POINT ( 'NONE',  ( 1.033464566929133799, 0.000000000000000000, 1.929133858160188897 ) ) ;
#8113=CARTESIAN_POINT ( 'NONE',  ( 0.9873396505805591694, -0.1113553986120547346, 0.04429133858267716300 ) ) ;
#8114=CARTESIAN_POINT ( 'NONE',  ( -1.054774247047244540, -0.07405724077823318263, 0.9694881889226145688 ) ) ;
#8116=CARTESIAN_POINT ( 'NONE',  ( 0.7185039370078739607, 1.928577636452523993E-17, 1.525590551181102317 ) ) ;
#8121=VERTEX_POINT ( 'NONE', #41950 ) ;
#8124=CARTESIAN_POINT ( 'NONE',  ( 0.9412147342319837628, -0.1574803149606297803, 1.380413385826771533 ) ) ;
#8128=CARTESIAN_POINT ( 'NONE',  ( 0.9873396505805591694, -0.1113553986120547346, 1.058070866034204860 ) ) ;
#8129=CARTESIAN_POINT ( 'NONE',  ( 0.9412147342319837628, 0.1574803149606300301, 1.828248031496063630 ) ) ;
#8131=CARTESIAN_POINT ( 'NONE',  ( -0.8019270111902717657, 0.1787899950787401604, 0.4675196849856070869 ) ) ;
#8133=CARTESIAN_POINT ( 'NONE',  ( -0.6971942568897648851, -0.07405724077823297447, 1.742125984198204858 ) ) ;
#8134=CARTESIAN_POINT ( 'NONE',  ( 0.6971942568897648851, -0.07405724077823297447, 1.663385826717890925 ) ) ;
#8137=CARTESIAN_POINT ( 'NONE',  ( 0.7495606340400177148, 0.1264236179284866091, 0.2386811023084413619 ) ) ;
#8139=CARTESIAN_POINT ( 'NONE',  ( -1.002407869896990045, 0.1264236179284866091, 1.168799212544661348 ) ) ;
#8140=CARTESIAN_POINT ( 'NONE',  ( -0.9500414927467378812, 0.1787899950787401604, 0.1131889763241892138 ) ) ;
#8141=DIRECTION ( 'NONE',  ( 1.822029033848725028E-16, 0.000000000000000000, 1.000000000000000000 ) ) ;
#8142=CARTESIAN_POINT ( 'NONE',  ( -0.9500414927467378812, 0.1787899950787401604, 1.530511810969859443 ) ) ;
#8143=CARTESIAN_POINT ( 'NONE',  ( -0.8759842519685039353, -0.1574803149606299191, 1.998031495955464587 ) ) ;
#8145=CARTESIAN_POINT ( 'NONE',  ( 0.8107537697050254399, -0.1574803149606297803, 0.9719488187901104137 ) ) ;
#8146=CARTESIAN_POINT ( 'NONE',  ( 0.7495606340400177148, 0.1264236179284866091, 1.577263779473795369 ) ) ;
#8150=VERTEX_POINT ( 'NONE', #8674 ) ;
#8151=CARTESIAN_POINT ( 'NONE',  ( -0.8019270111902716547, -0.1787899950787401604, 1.156496062938362046 ) ) ;
#8155=EDGE_CURVE ( 'NONE', #31760, #30794, #4850, .T. ) ;
#8162=EDGE_CURVE ( 'NONE', #41227, #11128, #25026, .T. ) ;
#8164=CARTESIAN_POINT ( 'NONE',  ( 0.9500414927467378812, 0.1787899950787401604, 0.8169291338045038264 ) ) ;
#8165=CARTESIAN_POINT ( 'NONE',  ( -0.7646288533564489232, -0.1113553986120547346, 1.560039369971212508 ) ) ;
#8168=CARTESIAN_POINT ( 'NONE',  ( 0.8759842519685039353, 0.000000000000000000, 4.498031496062992574 ) ) ;
#8169=CARTESIAN_POINT ( 'NONE',  ( 0.9500414927467378812, 0.1787899950787401604, 1.884842519631275026 ) ) ;
#8170=CARTESIAN_POINT ( 'NONE',  ( 0.7646288533564489232, 0.1113553986120547346, 0.1427165354330708902 ) ) ;
#8171=CYLINDRICAL_SURFACE ( 'NONE', #16794, 0.1574803149606299191 ) ;
#8174=CARTESIAN_POINT ( 'NONE',  ( 1.033464566929133799, 0.000000000000000000, 0.4724409447743622148 ) ) ;
#8177=CARTESIAN_POINT ( 'NONE',  ( 0.8759842519685039353, -0.1787899950787401882, 0.2928149605761578567 ) ) ;
#8178=DIRECTION ( 'NONE',  ( 1.822029033848725028E-16, 0.000000000000000000, 1.000000000000000000 ) ) ;
#8179=CARTESIAN_POINT ( 'NONE',  ( -0.8019270111902717657, 0.1787899950787401604, 1.727362204670645385 ) ) ;
#8181=CARTESIAN_POINT ( 'NONE',  ( -0.8019270111902717657, 0.1787899950787401604, 1.259842519631276359 ) ) ;
#8182=CARTESIAN_POINT ( 'NONE',  ( -1.033464566929134687, 0.06523048226347956391, 0.3272637795275590289 ) ) ;
#8183=CARTESIAN_POINT ( 'NONE',  ( -0.6971942568897626646, -0.07405724077823297447, 0.5216535432533228045 ) ) ;
#8184=CARTESIAN_POINT ( 'NONE',  ( 1.002407869896990045, 0.1264236179284866091, 1.916830708607653477 ) ) ;
#8185=CARTESIAN_POINT ( 'NONE',  ( -0.7495606340400177148, -0.1264236179284866091, 1.070374015694267600 ) ) ;
#8189=CARTESIAN_POINT ( 'NONE',  ( 0.8019270111902716547, 0.1787899950787401604, 0.4724409448281262636 ) ) ;
#8190=CARTESIAN_POINT ( 'NONE',  ( -1.002407869896990045, 0.1264236179284866091, 0.4601377952218267953 ) ) ;
#8191=CARTESIAN_POINT ( 'NONE',  ( -0.9500414927467378812, 0.1787899950787401604, 0.8562992125446617919 ) ) ;
#8192=CARTESIAN_POINT ( 'NONE',  ( 0.8107537697050253289, 0.1574803149606300301, 1.705216535325545069 ) ) ;
#8195=( BOUNDED_CURVE ( )  B_SPLINE_CURVE ( 2, ( #29358, #7952, #22803, #18504, #4569, #29808, #19203, #15640, #44355 ),
 .UNSPECIFIED., .F., .T. ) 
 B_SPLINE_CURVE_WITH_KNOTS ( ( 3, 2, 2, 2, 3 ),
 ( 0.02000000000000000042, 0.02249999999999999917, 0.02500000000000000139, 0.02750000000000000014, 0.02999999999999999889 ),
 .UNSPECIFIED. ) 
 CURVE ( )  GEOMETRIC_REPRESENTATION_ITEM ( )  RATIONAL_B_SPLINE_CURVE ( ( 1.000000000000000000, 0.9238795325112869605, 1.000000000000000000, 0.9238795325112869605, 1.000000000000000000, 0.9238795325112869605, 1.000000000000000000, 0.9238795325112869605, 1.000000000000000000 ) ) 
 REPRESENTATION_ITEM ( '' )  ) ;
#8197=CARTESIAN_POINT ( 'NONE',  ( 0.9500414927467378812, 0.1787899950787401604, 0.9005905511273389896 ) ) ;
#8198=CARTESIAN_POINT ( 'NONE',  ( -0.7185039370078746268, -0.06523048226347956391, 0.07135826771653554224 ) ) ;
#8199=CARTESIAN_POINT ( 'NONE',  ( 0.8019270111902716547, 0.1787899950787401604, 1.220472440891118504 ) ) ;
#8201=ORIENTED_EDGE ( 'NONE', *, *, #16256, .T. ) ;
#8206=ORIENTED_EDGE ( 'NONE', *, *, #32698, .F. ) ;
#8209=VERTEX_POINT ( 'NONE', #16128 ) ;
#8210=CARTESIAN_POINT ( 'NONE',  ( 1.002407869896990045, 0.1264236179284866091, 1.326279527505291433 ) ) ;
#8212=FACE_OUTER_BOUND ( 'NONE', #869, .T. ) ;
#8214=( BOUNDED_CURVE ( )  B_SPLINE_CURVE ( 2, ( #5438, #34698, #2080, #1842, #28211, #7342, #35403, #18119, #6375 ),
 .UNSPECIFIED., .F., .F. ) 
 B_SPLINE_CURVE_WITH_KNOTS ( ( 3, 2, 2, 2, 3 ),
 ( 0.9100000000000000311, 0.9124999999999999778, 0.9150000000000000355, 0.9174999999999999822, 0.9200000000000000400 ),
 .UNSPECIFIED. ) 
 CURVE ( )  GEOMETRIC_REPRESENTATION_ITEM ( )  RATIONAL_B_SPLINE_CURVE ( ( 1.000000000000000000, 0.9238795325112869605, 1.000000000000000000, 0.9238795325112869605, 1.000000000000000000, 0.9238795325112869605, 1.000000000000000000, 0.9238795325112869605, 1.000000000000000000 ) ) 
 REPRESENTATION_ITEM ( '' )  ) ;
#8215=EDGE_CURVE ( 'NONE', #15970, #41905, #30755, .T. ) ;
#8216=CARTESIAN_POINT ( 'NONE',  ( 0.6971942568897637749, 2.189545951927499583E-17, 1.537893700733637736 ) ) ;
#8217=CARTESIAN_POINT ( 'NONE',  ( 0.7495606340400177148, 0.1264236179284866091, 0.1550196849856066983 ) ) ;
#8218=( BOUNDED_CURVE ( )  B_SPLINE_CURVE ( 2, ( #41875, #8840, #19622, #9080, #23699, #38308, #5480, #20095, #34741 ),
 .UNSPECIFIED., .F., .F. ) 
 B_SPLINE_CURVE_WITH_KNOTS ( ( 3, 2, 2, 2, 3 ),
 ( 0.1300000000000000044, 0.1325000000000000067, 0.1350000000000000089, 0.1375000000000000111, 0.1400000000000000133 ),
 .UNSPECIFIED. ) 
 CURVE ( )  GEOMETRIC_REPRESENTATION_ITEM ( )  RATIONAL_B_SPLINE_CURVE ( ( 1.000000000000000000, 0.9238795325112869605, 1.000000000000000000, 0.9238795325112869605, 1.000000000000000000, 0.9238795325112869605, 1.000000000000000000, 0.9238795325112869605, 1.000000000000000000 ) ) 
 REPRESENTATION_ITEM ( '' )  ) ;
#8219=EDGE_CURVE ( 'NONE', #5728, #26896, #34838, .T. ) ;
#8224=CARTESIAN_POINT ( 'NONE',  ( -1.054774247047244540, 0.07405724077823318263, 0.6594488188438737408 ) ) ;
#8226=CARTESIAN_POINT ( 'NONE',  ( 0.9412147342319837628, 0.1574803149606300301, 0.3715551181102362266 ) ) ;
#8228=CYLINDRICAL_SURFACE ( 'NONE', #38623, 0.1574803149606299191 ) ;
#8229=FACE_OUTER_BOUND ( 'NONE', #4023, .T. ) ;
#8230=CARTESIAN_POINT ( 'NONE',  ( 0.7495606340400177148, -0.1264236179284866091, 1.390255905458047447 ) ) ;
#8231=CARTESIAN_POINT ( 'NONE',  ( 0.7495606340400177148, -0.1264236179284866091, 1.779035433017102319 ) ) ;
#8232=CARTESIAN_POINT ( 'NONE',  ( 1.054774247047244540, 0.07405724077823318263, 0.2608267715997797387 ) ) ;
#8233=CARTESIAN_POINT ( 'NONE',  ( -0.7646288533564489232, -0.1113553986120547346, 1.638779527451527551 ) ) ;
#8234=ORIENTED_EDGE ( 'NONE', *, *, #34815, .F. ) ;
#8239=CARTESIAN_POINT ( 'NONE',  ( 0.6971942568897626646, 0.07405724077823318263, 0.2755905511273391006 ) ) ;
#8240=CARTESIAN_POINT ( 'NONE',  ( 0.7480772688632181255, -0.1073106677863766983, 0.03937439283920037697 ) ) ;
#8241=CARTESIAN_POINT ( 'NONE',  ( 1.054774247047244540, 0.07405724077823318263, 1.245078740103716886 ) ) ;
#8242=CARTESIAN_POINT ( 'NONE',  ( -1.002407869896990045, -0.1264236179284866091, 1.990649606245448844 ) ) ;
#8243=CARTESIAN_POINT ( 'NONE',  ( -1.033464566929133799, 0.000000000000000000, 1.338582677057826853 ) ) ;
#8245=CARTESIAN_POINT ( 'NONE',  ( -0.8107537697050254399, 0.1574803149606300301, 0.9571850392625507187 ) ) ;
#8246=CARTESIAN_POINT ( 'NONE',  ( 0.9412147342319837628, -0.1574803149606297803, 0.6225393699712132856 ) ) ;
#8248=CARTESIAN_POINT ( 'NONE',  ( 0.9412147342319837628, 0.1574803149606300301, 1.395177165354331672 ) ) ;
#8250=ORIENTED_EDGE ( 'NONE', *, *, #19908, .T. ) ;
#8254=CARTESIAN_POINT ( 'NONE',  ( 0.6971942568897637749, 2.189545951927499583E-17, 1.616633858213952779 ) ) ;
#8255=CARTESIAN_POINT ( 'NONE',  ( -0.7185039370078739607, 1.928577636452523993E-17, 1.250000000000000000 ) ) ;
#8259=CARTESIAN_POINT ( 'NONE',  ( 0.8759842519685039353, -0.1574803149606299191, 1.919291338475149544 ) ) ;
#8260=ORIENTED_EDGE ( 'NONE', *, *, #22232, .T. ) ;
#8263=ORIENTED_EDGE ( 'NONE', *, *, #20409, .F. ) ;
#8264=CARTESIAN_POINT ( 'NONE',  ( 1.002407869896990045, 0.1264236179284866091, 0.9374999999462362288 ) ) ;
#8266=CARTESIAN_POINT ( 'NONE',  ( -0.8759842519685039353, -0.1787899950787401882, 1.316437007820252081 ) ) ;
#8268=CARTESIAN_POINT ( 'NONE',  ( -0.8019270111902717657, 0.1787899950787401604, 0.3543307086076538659 ) ) ;
#8269=CARTESIAN_POINT ( 'NONE',  ( 1.033464566929133799, 1.928577636452524610E-17, 4.498031496062992574 ) ) ;
#8270=CARTESIAN_POINT ( 'NONE',  ( -0.7185039370078766252, -0.06523048226348168721, 1.872539369971213619 ) ) ;
#8277=EDGE_CURVE ( 'NONE', #31032, #16139, #13244, .T. ) ;
#8279=CARTESIAN_POINT ( 'NONE',  ( 0.8107537697050254399, 0.1574803149606300301, 1.823326771546017078 ) ) ;
#8282=CARTESIAN_POINT ( 'NONE',  ( -0.9500414927467377701, -0.1787899950787401604, 0.2559055117572600624 ) ) ;
#8283=CARTESIAN_POINT ( 'NONE',  ( -1.033464566929133799, 0.000000000000000000, 0.8366141732283465249 ) ) ;
#8285=CARTESIAN_POINT ( 'NONE',  ( 0.8107537697050254399, -0.1574803149606297803, 1.099901574803150650 ) ) ;
#8286=CARTESIAN_POINT ( 'NONE',  ( -0.7185039370078746268, 0.06523048226347956391, 1.552657480207433993 ) ) ;
#8287=CARTESIAN_POINT ( 'NONE',  ( 1.054774247047244540, -0.07405724077823318263, 0.8907480314422986378 ) ) ;
#8288=CARTESIAN_POINT ( 'NONE',  ( -0.7185039370078746268, 0.06523048226347956391, 0.4601377952755902889 ) ) ;
#8289=CARTESIAN_POINT ( 'NONE',  ( 0.7342868310752559413, 0.08092158428113763180, 1.981631876916298163 ) ) ;
#8292=CARTESIAN_POINT ( 'NONE',  ( -1.033464566929134687, 0.06523048226347956391, 1.547736220472440305 ) ) ;
#8293=CARTESIAN_POINT ( 'NONE',  ( 0.9500414927467377701, 0.1787899950787401604, 0.8169291338045038264 ) ) ;
#8295=CARTESIAN_POINT ( 'NONE',  ( 1.054774247047244540, -0.07405724077823318263, 1.835629921206078485 ) ) ;
#8298=CARTESIAN_POINT ( 'NONE',  ( 0.8759842519685039353, -0.1574803149606299191, 0.4232283463491653963 ) ) ;
#8299=CARTESIAN_POINT ( 'NONE',  ( -0.7185039370078739607, 1.928577636452523993E-17, 0.1377952754830242266 ) ) ;
#8300=CARTESIAN_POINT ( 'NONE',  ( 1.054774247047244540, 0.07405724077823318263, 1.205708661363558365 ) ) ;
#8301=CARTESIAN_POINT ( 'NONE',  ( -0.7185039370078746268, 0.06523048226347956391, 1.050688976377951889 ) ) ;
#8305=AXIS2_PLACEMENT_3D ( 'NONE', #44176, #28907, #29406 ) ;
#8308=CARTESIAN_POINT ( 'NONE',  ( -0.7495606340400177148, 0.1264236179284866091, 0.2731299212060791515 ) ) ;
#8309=ORIENTED_EDGE ( 'NONE', *, *, #40209, .F. ) ;
#8310=VERTEX_POINT ( 'NONE', #46986 ) ;
#8314=CARTESIAN_POINT ( 'NONE',  ( -0.8759842519685039353, 0.1787899950787401882, 1.764271653489543290 ) ) ;
#8315=CARTESIAN_POINT ( 'NONE',  ( -0.9500414927467377701, -0.1787899950787401604, 0.9596456692375763264 ) ) ;
#8317=CARTESIAN_POINT ( 'NONE',  ( -0.8759842519685039353, 0.1787899950787401882, 0.5487204723871811352 ) ) ;
#8323=CARTESIAN_POINT ( 'NONE',  ( -0.7185039370078739607, 1.928577636452523993E-17, 1.909448818790110192 ) ) ;
#8324=CARTESIAN_POINT ( 'NONE',  ( 0.9873396505805591694, -0.1113553986120547346, 1.934055118110236338 ) ) ;
#8328=CARTESIAN_POINT ( 'NONE',  ( -1.002407869896990045, 0.1264236179284866091, 0.4601377952218267953 ) ) ;
#8329=( BOUNDED_CURVE ( )  B_SPLINE_CURVE ( 2, ( #44708, #27031, #29701, #44245, #26550, #44475, #41109, #8301, #37542 ),
 .UNSPECIFIED., .F., .T. ) 
 B_SPLINE_CURVE_WITH_KNOTS ( ( 3, 2, 2, 2, 3 ),
 ( 0.5200000000000000178, 0.5224999999999999645, 0.5250000000000000222, 0.5274999999999999689, 0.5300000000000000266 ),
 .UNSPECIFIED. ) 
 CURVE ( )  GEOMETRIC_REPRESENTATION_ITEM ( )  RATIONAL_B_SPLINE_CURVE ( ( 1.000000000000000000, 0.9238795325112869605, 1.000000000000000000, 0.9238795325112869605, 1.000000000000000000, 0.9238795325112869605, 1.000000000000000000, 0.9238795325112869605, 1.000000000000000000 ) ) 
 REPRESENTATION_ITEM ( '' )  ) ;
#8330=LINE ( 'NONE', #38046, #9620 ) ;
#8331=EDGE_CURVE ( 'NONE', #35982, #28497, #21673, .T. ) ;
#8334=CARTESIAN_POINT ( 'NONE',  ( -0.9500414927467377701, -0.1787899950787401604, 1.515748031442299526 ) ) ;
#8335=ORIENTED_EDGE ( 'NONE', *, *, #43402, .F. ) ;
#8342=CARTESIAN_POINT ( 'NONE',  ( -0.9873396505805591694, 0.1113553986120547346, 1.067913385719243990 ) ) ;
#8344=CARTESIAN_POINT ( 'NONE',  ( 0.9500414927467378812, -0.1787899950787401604, 0.5314960629383620461 ) ) ;
#8345=CARTESIAN_POINT ( 'NONE',  ( 0.7108038354695511707, 0.06841997037041733232, 0.03937007863263043694 ) ) ;
#8348=CARTESIAN_POINT ( 'NONE',  ( 0.9873396505805591694, 0.1113553986120547346, 1.894685039262551163 ) ) ;
#8349=ORIENTED_EDGE ( 'NONE', *, *, #10464, .T. ) ;
#8351=CARTESIAN_POINT ( 'NONE',  ( 0.9873396505805591694, 0.1113553986120547346, 0.9202755905511811330 ) ) ;
#8356=CARTESIAN_POINT ( 'NONE',  ( 0.8759842519685039353, 0.1574803149606299191, 1.269685039262551163 ) ) ;
#8361=VERTEX_POINT ( 'NONE', #39556 ) ;
#8362=CARTESIAN_POINT ( 'NONE',  ( -0.8107537697050254399, 0.1574803149606300301, 1.783956692805859001 ) ) ;
#8363=CARTESIAN_POINT ( 'NONE',  ( -0.7646288533564489232, 0.1113553986120547346, 0.4478346455617645550 ) ) ;
#8367=CARTESIAN_POINT ( 'NONE',  ( 0.7646288533564489232, 0.1113553986120547346, 1.156496062884598608 ) ) ;
#8368=DIRECTION ( 'NONE',  ( -1.000000000000000000, 0.000000000000000000, 0.000000000000000000 ) ) ;
#8371=CARTESIAN_POINT ( 'NONE',  ( -0.7495606340400177148, -0.1264236179284866091, 1.744586614119464807 ) ) ;
#8372=CARTESIAN_POINT ( 'NONE',  ( 0.9500414927467378812, -0.1787899950787401604, 1.751968503883245765 ) ) ;
#8374=CARTESIAN_POINT ( 'NONE',  ( -0.9500414927467378812, -0.1787899950787401604, 1.313976377898992132 ) ) ;
#8375=CARTESIAN_POINT ( 'NONE',  ( -1.002407869896990045, 0.1264236179284866091, 1.208169291284818980 ) ) ;
#8376=CARTESIAN_POINT ( 'NONE',  ( -0.8019270111902717657, -0.1787899950787401604, 0.9153543306548987957 ) ) ;
#8377=CARTESIAN_POINT ( 'NONE',  ( -0.6971942568897626646, -0.07405724077823297447, 0.04921259837143338034 ) ) ;
#8380=CARTESIAN_POINT ( 'NONE',  ( -0.8759842519685039353, -0.1787899950787401882, 1.552657480261196765 ) ) ;
#8381=CARTESIAN_POINT ( 'NONE',  ( -0.8019270111902717657, 0.1787899950787401604, 0.1181102361667090567 ) ) ;
#8385=CARTESIAN_POINT ( 'NONE',  ( 1.002407869896990045, 0.1264236179284866091, 1.606791338528913426 ) ) ;
#8390=ADVANCED_FACE ( 'NONE', ( #29552 ), #11067, .T. ) ;
#8391=VERTEX_POINT ( 'NONE', #10596 ) ;
#8393=AXIS2_PLACEMENT_3D ( 'NONE', #11175, #33231, #26505 ) ;
#8394=CARTESIAN_POINT ( 'NONE',  ( -0.6971942568897648851, 0.07405724077823318263, 1.186023621993481658 ) ) ;
#8395=ORIENTED_EDGE ( 'NONE', *, *, #7886, .T. ) ;
#8400=CARTESIAN_POINT ( 'NONE',  ( 1.033464566929133799, 0.000000000000000000, 0.6003937007874016185 ) ) ;
#8403=CARTESIAN_POINT ( 'NONE',  ( -0.7185039370078739607, 1.928577636452523993E-17, 1.082677165246803241 ) ) ;
#8404=CARTESIAN_POINT ( 'NONE',  ( 0.8019270111902717657, 0.1787899950787401604, 0.7037401574265510495 ) ) ;
#8406=CYLINDRICAL_SURFACE ( 'NONE', #40708, 0.1574803149606299191 ) ;
#8407=CARTESIAN_POINT ( 'NONE',  ( -1.033464566929133799, 0.000000000000000000, 1.259842519577511810 ) ) ;
#8409=CARTESIAN_POINT ( 'NONE',  ( 1.054774247047244096, 0.000000000000000000, 1.798720472387181024 ) ) ;
#8410=CARTESIAN_POINT ( 'NONE',  ( 0.8759842519685039353, -0.1574803149606299191, 0.1574803149606299191 ) ) ;
#8413=CARTESIAN_POINT ( 'NONE',  ( 1.054774247047244096, 0.000000000000000000, 1.990649606245448844 ) ) ;
#8415=CARTESIAN_POINT ( 'NONE',  ( 0.8019270111902717657, 0.1787899950787401604, 0.1968503936470238913 ) ) ;
#8416=CARTESIAN_POINT ( 'NONE',  ( -1.054774247047244540, -0.07405724077823318263, 1.791338582623401177 ) ) ;
#8419=CARTESIAN_POINT ( 'NONE',  ( -1.054774247047244096, 0.000000000000000000, 1.247539370024976391 ) ) ;
#8420=CARTESIAN_POINT ( 'NONE',  ( -1.054774247047244540, -0.07405724077823318263, 0.5364173227808821665 ) ) ;
#8421=CARTESIAN_POINT ( 'NONE',  ( 0.9500414927467378812, 0.1787899950787401604, 1.958661417269071947 ) ) ;
#8422=CARTESIAN_POINT ( 'NONE',  ( -0.8019270111902717657, -0.1787899950787401604, 1.151574803095843036 ) ) ;
#8424=CARTESIAN_POINT ( 'NONE',  ( 0.8107537697050254399, -0.1574803149606297803, 0.6569881888688504645 ) ) ;
#8426=CARTESIAN_POINT ( 'NONE',  ( -0.8759842519685039353, 0.000000000000000000, 0.000000000000000000 ) ) ;
#8427=CARTESIAN_POINT ( 'NONE',  ( 0.8019270111902716547, 0.1787899950787401604, 0.5118110235682844511 ) ) ;
#8428=CARTESIAN_POINT ( 'NONE',  ( -0.6971942568897637749, 2.189545951927499583E-17, 0.4355314960092284138 ) ) ;
#8432=ORIENTED_EDGE ( 'NONE', *, *, #42070, .F. ) ;
#8433=CARTESIAN_POINT ( 'NONE',  ( 1.054774247047244096, 0.000000000000000000, 0.9325787401037164415 ) ) ;
#8434=CARTESIAN_POINT ( 'NONE',  ( -0.7185039370078746268, 0.06523048226347956391, 0.06643700787401589369 ) ) ;
#8435=EDGE_CURVE ( 'NONE', #460, #11565, #1788, .T. ) ;
#8436=CARTESIAN_POINT ( 'NONE',  ( 1.033464566929133799, 0.000000000000000000, 0.7086614172153071767 ) ) ;
#8437=CARTESIAN_POINT ( 'NONE',  ( 0.8107537697050254399, 0.1574803149606300301, 1.311515747923968744 ) ) ;
#8439=CARTESIAN_POINT ( 'NONE',  ( -0.9412147342319837628, -0.1574803149606297803, 1.301673228346455602 ) ) ;
#8444=ORIENTED_EDGE ( 'NONE', *, *, #5186, .F. ) ;
#8449=CARTESIAN_POINT ( 'NONE',  ( 0.7185039370078746268, 0.06523048226347956391, 1.601870078740158077 ) ) ;
#8450=CIRCLE ( 'NONE', #45174, 0.1574803149606299191 ) ;
#8452=CARTESIAN_POINT ( 'NONE',  ( 1.054774247047244096, 0.000000000000000000, 1.557578740103716441 ) ) ;
#8453=CARTESIAN_POINT ( 'NONE',  ( 1.054774247047244096, 0.000000000000000000, 0.1008858267178899676 ) ) ;
#8457=CARTESIAN_POINT ( 'NONE',  ( 0.7185039370078739607, 1.928577636452523993E-17, 1.948818897530267602 ) ) ;
#8458=CARTESIAN_POINT ( 'NONE',  ( -0.6971942568897648851, -0.07405724077823297447, 0.6003937007336389575 ) ) ;
#8465=CARTESIAN_POINT ( 'NONE',  ( 0.6971942568897648851, 0.07405724077823318263, 1.343503936954111744 ) ) ;
#8466=CARTESIAN_POINT ( 'NONE',  ( 1.054774247047244096, 0.000000000000000000, 1.833169291284818758 ) ) ;
#8467=CARTESIAN_POINT ( 'NONE',  ( 0.8759842519685039353, -0.1787899950787401882, 0.2878937007336381804 ) ) ;
#8468=CARTESIAN_POINT ( 'NONE',  ( 0.8759842519685039353, 0.000000000000000000, 4.498031496062992574 ) ) ;
#8469=VERTEX_POINT ( 'NONE', #36929 ) ;
#8470=CARTESIAN_POINT ( 'NONE',  ( -0.9412147342319837628, 0.1574803149606300301, 1.513287401574803681 ) ) ;
#8473=CARTESIAN_POINT ( 'NONE',  ( 0.8759842519685039353, -0.1787899950787401882, 0.3272637794737956463 ) ) ;
#8477=CARTESIAN_POINT ( 'NONE',  ( 1.033464566929134687, 0.06523048226347956391, 0.8390748031496062520 ) ) ;
#8478=CARTESIAN_POINT ( 'NONE',  ( -0.9412147342319837628, 0.1574803149606300301, 0.9522637794200313754 ) ) ;
#8479=CARTESIAN_POINT ( 'NONE',  ( -0.6971942568897637749, 2.189545951927499583E-17, 1.301673228292692830 ) ) ;
#8480=CARTESIAN_POINT ( 'NONE',  ( 0.7185039370078746268, 0.06523048226347956391, 0.8439960628845977197 ) ) ;
#8486=CARTESIAN_POINT ( 'NONE',  ( -0.9873396505805591694, -0.1113553986120547346, 1.225393700787401619 ) ) ;
#8487=CARTESIAN_POINT ( 'NONE',  ( 0.8759842519685039353, 0.1787899950787401882, 1.606791338528913426 ) ) ;
#8488=CARTESIAN_POINT ( 'NONE',  ( -0.9412147342319837628, -0.1574803149606297803, 1.183562992125983593 ) ) ;
#8490=CARTESIAN_POINT ( 'NONE',  ( 0.8759842519685039353, 0.1574803149606299191, 0.5708661417322835607 ) ) ;
#8493=CARTESIAN_POINT ( 'NONE',  ( 0.7495606340400177148, 0.1264236179284866091, 0.04183070860765386589 ) ) ;
#8496=ADVANCED_FACE ( 'NONE', ( #14647 ), #43866, .T. ) ;
#8499=CARTESIAN_POINT ( 'NONE',  ( 0.9500414927467377701, -0.1787899950787401604, 0.9645669290800954476 ) ) ;
#8500=CARTESIAN_POINT ( 'NONE',  ( -1.054774247047244540, -0.07405724077823318263, 1.555118110182457158 ) ) ;
#8502=CARTESIAN_POINT ( 'NONE',  ( -0.6971942568897637749, 2.189545951927499583E-17, 1.306594488135212728 ) ) ;
#8504=EDGE_CURVE ( 'NONE', #1531, #10984, #11890, .T. ) ;
#8506=CARTESIAN_POINT ( 'NONE',  ( -1.033464566929134687, 0.06523048226347956391, 0.2386811022546777294 ) ) ;
#8514=CARTESIAN_POINT ( 'NONE',  ( -0.9412147342319837628, -0.1574803149606297803, 0.2682086613097955929 ) ) ;
#8517=CARTESIAN_POINT ( 'NONE',  ( 0.7646288533564489232, 0.1113553986120547346, 1.825787401467275473 ) ) ;
#8521=CARTESIAN_POINT ( 'NONE',  ( -1.054774247047244096, 0.000000000000000000, 0.1451771653005673179 ) ) ;
#8522=CARTESIAN_POINT ( 'NONE',  ( -0.7185039370078739607, 1.928577636452523993E-17, 0.8562992125984251190 ) ) ;
#8525=CARTESIAN_POINT ( 'NONE',  ( 0.8019270111902717657, -0.1787899950787401604, 0.9990157479777320715 ) ) ;
#8527=CARTESIAN_POINT ( 'NONE',  ( 1.033464566929134687, -0.06523048226347956391, 1.542814960629920851 ) ) ;
#8528=EDGE_CURVE ( 'NONE', #19795, #17892, #29962, .T. ) ;
#8529=CARTESIAN_POINT ( 'NONE',  ( 0.7204945029520213318, 0.05328764782798792871, 1.982238686896746094 ) ) ;
#8531=CYLINDRICAL_SURFACE ( 'NONE', #17474, 0.1574803149606299191 ) ;
#8534=CARTESIAN_POINT ( 'NONE',  ( 0.8019270111902716547, -0.1787899950787401604, 0.9940944881352130613 ) ) ;
#8535=CARTESIAN_POINT ( 'NONE',  ( 0.7495606340400177148, -0.1264236179284866091, 1.823326771599779406 ) ) ;
#8537=VERTEX_POINT ( 'NONE', #44559 ) ;
#8543=CARTESIAN_POINT ( 'NONE',  ( 0.8759842519685039353, 0.1787899950787401882, 1.134350393647023614 ) ) ;
#8544=CARTESIAN_POINT ( 'NONE',  ( -0.7185039370078739607, 1.928577636452523993E-17, 1.171259842519684957 ) ) ;
#8549=CARTESIAN_POINT ( 'NONE',  ( -0.6971942568897626646, -0.07405724077823297447, 0.2017716534895435399 ) ) ;
#8550=VERTEX_POINT ( 'NONE', #38106 ) ;
#8554=CARTESIAN_POINT ( 'NONE',  ( -1.002407869896990045, -0.1264236179284866091, 1.867618110182456714 ) ) ;
#8555=CARTESIAN_POINT ( 'NONE',  ( -0.7495606340400177148, 0.1264236179284866091, 0.9424212597887559051 ) ) ;
#8557=CARTESIAN_POINT ( 'NONE',  ( -1.054774247047244540, -0.07405724077823318263, 0.4970472440407249226 ) ) ;
#8559=FACE_OUTER_BOUND ( 'NONE', #22777, .T. ) ;
#8564=LINE ( 'NONE', #37813, #20283 ) ;
#8566=CARTESIAN_POINT ( 'NONE',  ( -0.8759842519685039353, -0.1787899950787401882, 0.4060039369541102450 ) ) ;
#8568=VERTEX_POINT ( 'NONE', #37381 ) ;
#8569=CARTESIAN_POINT ( 'NONE',  ( -0.6971942568897648851, -0.07405724077823297447, 1.466535433017102763 ) ) ;
#8573=LENGTH_MEASURE_WITH_UNIT ( LENGTH_MEASURE( 0.02539999999999999897 ), #41373 ) ;
#8575=CARTESIAN_POINT ( 'NONE',  ( 0.9873396505805591694, 0.1113553986120547346, 0.4872047244094488416 ) ) ;
#8577=CARTESIAN_POINT ( 'NONE',  ( -0.7646288533564489232, 0.1113553986120547346, 1.077755905404283565 ) ) ;
#8578=CARTESIAN_POINT ( 'NONE',  ( 1.002407869896990045, -0.1264236179284866091, 0.5733267715997795166 ) ) ;
#8582=CARTESIAN_POINT ( 'NONE',  ( 0.7185039370078746268, -0.06523048226347956391, 1.990649606191687404 ) ) ;
#8586=CARTESIAN_POINT ( 'NONE',  ( -0.9500414927467377701, 0.1787899950787401604, 1.136811023568283119 ) ) ;
#8587=CARTESIAN_POINT ( 'NONE',  ( 0.9412147342319837628, 0.1574803149606300301, 1.158956692913385655 ) ) ;
#8588=CARTESIAN_POINT ( 'NONE',  ( -0.9412147342319837628, 0.1574803149606300301, 0.7160433069790875793 ) ) ;
#8596=CARTESIAN_POINT ( 'NONE',  ( 0.7495606340400177148, 0.1264236179284866091, 0.7455708660879684091 ) ) ;
#8602=CARTESIAN_POINT ( 'NONE',  ( 1.033464566929133799, 0.000000000000000000, 1.141732283357039357 ) ) ;
#8605=EDGE_LOOP ( 'NONE', ( #33049, #4973, #37361, #41956, #25139, #21350, #12757, #7503, #44802, #17634, #628, #47163, #36650, #39885, #20740, #10995, #32932, #5513, #27263, #3440, #1104, #45665, #6850, #14399, #8349, #39659, #35638, #11486, #15552, #40241, #38182, #12734, #29611, #21707, #3520, #7729, #30823, #3539, #7794, #43869, #38460, #34740, #37029, #4114, #20709, #4343, #16186, #43390, #26998, #47028, #21347, #4342, #17819, #29615, #44742, #27599, #21043, #41999, #13668, #15761, #32327, #5657, #17873, #27703, #14305, #26070, #42264, #21699, #5192, #37382, #14413, #14050, #38297, #6023, #44380, #21802, #31804, #41530, #2527, #16777, #28880, #39062, #30618, #45677, #9468, #29265, #22997, #22516, #13248, #43571, #9139, #40186, #39374, #1575, #15618, #32532, #45090, #47445, #27938, #41398, #36015, #27873 ) ) ;
#8607=CARTESIAN_POINT ( 'NONE',  ( -0.8759842519685039353, 0.1787899950787401882, 1.769192913332062966 ) ) ;
#8608=CARTESIAN_POINT ( 'NONE',  ( 0.6971942568897637749, 2.189545951927499583E-17, 1.897145669237574772 ) ) ;
#8611=CARTESIAN_POINT ( 'NONE',  ( 0.9500414927467378812, -0.1787899950787401604, 0.3740157479777325711 ) ) ;
#8612=CARTESIAN_POINT ( 'NONE',  ( -0.9500414927467378812, 0.1787899950787401604, 1.328740157426552049 ) ) ;
#8614=CARTESIAN_POINT ( 'NONE',  ( -0.9500414927467377701, 0.1787899950787401604, 1.289370078686393750 ) ) ;
#8615=EDGE_CURVE ( 'NONE', #3082, #5382, #950, .T. ) ;
#8616=CARTESIAN_POINT ( 'NONE',  ( -0.8019270111902717657, -0.1787899950787401604, 0.8759842519147408302 ) ) ;
#8617=FACE_OUTER_BOUND ( 'NONE', #21948, .T. ) ;
#8618=( BOUNDED_CURVE ( )  B_SPLINE_CURVE ( 2, ( #22489, #4037, #17306, #10370, #40676, #29510, #33546, #44279, #17778 ),
 .UNSPECIFIED., .F., .T. ) 
 B_SPLINE_CURVE_WITH_KNOTS ( ( 3, 2, 2, 2, 3 ),
 ( 0.2600000000000000089, 0.2625000000000000111, 0.2650000000000000133, 0.2675000000000000155, 0.2700000000000000178 ),
 .UNSPECIFIED. ) 
 CURVE ( )  GEOMETRIC_REPRESENTATION_ITEM ( )  RATIONAL_B_SPLINE_CURVE ( ( 1.000000000000000000, 0.9238795325112869605, 1.000000000000000000, 0.9238795325112869605, 1.000000000000000000, 0.9238795325112869605, 1.000000000000000000, 0.9238795325112869605, 1.000000000000000000 ) ) 
 REPRESENTATION_ITEM ( '' )  ) ;
#8620=CARTESIAN_POINT ( 'NONE',  ( -1.002407869896990045, 0.1264236179284866091, 1.764271653489543290 ) ) ;
#8621=CARTESIAN_POINT ( 'NONE',  ( -0.7646288533564489232, 0.1113553986120547346, 1.983267716427905558 ) ) ;
#8622=CARTESIAN_POINT ( 'NONE',  ( -0.9873396505805591694, -0.1113553986120547346, 1.697834645669291209 ) ) ;
#8623=DIRECTION ( 'NONE',  ( 0.000000000000000000, 0.000000000000000000, -1.000000000000000000 ) ) ;
#8624=CARTESIAN_POINT ( 'NONE',  ( 0.6971942568897648851, -0.07405724077823297447, 1.663385826717890925 ) ) ;
#8629=CARTESIAN_POINT ( 'NONE',  ( -1.002407869896990045, 0.1264236179284866091, 1.173720472387181246 ) ) ;
#8632=( BOUNDED_CURVE ( )  B_SPLINE_CURVE ( 2, ( #2649, #25676, #46499, #35740, #6964, #32147, #28816, #13678, #32873 ),
 .UNSPECIFIED., .F., .T. ) 
 B_SPLINE_CURVE_WITH_KNOTS ( ( 3, 2, 2, 2, 3 ),
 ( 0.4299999999999999933, 0.4324999999999999956, 0.4349999999999999978, 0.4375000000000000000, 0.4400000000000000022 ),
 .UNSPECIFIED. ) 
 CURVE ( )  GEOMETRIC_REPRESENTATION_ITEM ( )  RATIONAL_B_SPLINE_CURVE ( ( 1.000000000000000000, 0.9238795325112869605, 1.000000000000000000, 0.9238795325112869605, 1.000000000000000000, 0.9238795325112869605, 1.000000000000000000, 0.9238795325112869605, 1.000000000000000000 ) ) 
 REPRESENTATION_ITEM ( '' )  ) ;
#8635=CARTESIAN_POINT ( 'NONE',  ( 0.6971942568897648851, 0.07405724077823318263, 1.850393700733638624 ) ) ;
#8638=CARTESIAN_POINT ( 'NONE',  ( -0.7185039370078746268, -0.06523048226347956391, 0.8882874014672752505 ) ) ;
#8639=CARTESIAN_POINT ( 'NONE',  ( 1.054774247047244540, -0.07405724077823318263, 0.7677165353793073965 ) ) ;
#8641=CARTESIAN_POINT ( 'NONE',  ( -0.8107537697050254399, -0.1574803149606297803, 1.562499999892472013 ) ) ;
#8643=CARTESIAN_POINT ( 'NONE',  ( 0.8759842519685039353, 0.1574803149606299191, 0.4527559055118110520 ) ) ;
#8644=CARTESIAN_POINT ( 'NONE',  ( 0.7646288533564489232, -0.1113553986120547346, 0.1033464565853864231 ) ) ;
#8645=EDGE_CURVE ( 'NONE', #1915, #38980, #31473, .T. ) ;
#8647=CARTESIAN_POINT ( 'NONE',  ( 0.8759842519685039353, 0.1574803149606299191, 0.1377952755905511861 ) ) ;
#8651=CARTESIAN_POINT ( 'NONE',  ( 1.054774247047244096, 0.000000000000000000, 0.2632874015210397434 ) ) ;
#8654=CARTESIAN_POINT ( 'NONE',  ( -0.8019270111902717657, 0.1787899950787401604, 1.687992125930489307 ) ) ;
#8655=EDGE_LOOP ( 'NONE', ( #8977, #47339, #8395, #28372 ) ) ;
#8656=CARTESIAN_POINT ( 'NONE',  ( -0.6971942568897648851, -0.07405724077823297447, 1.348425196796630976 ) ) ;
#8657=CARTESIAN_POINT ( 'NONE',  ( 0.8759842519685039353, -0.1787899950787401882, 1.355807086560409491 ) ) ;
#8658=CARTESIAN_POINT ( 'NONE',  ( 0.8019270111902717657, -0.1787899950787401604, 0.09350393695411057804 ) ) ;
#8659=CARTESIAN_POINT ( 'NONE',  ( -0.6971942568897648851, -0.07405724077823297447, 1.146653543253323582 ) ) ;
#8660=CARTESIAN_POINT ( 'NONE',  ( 0.9412147342319837628, -0.1574803149606297803, 0.6619094487113718062 ) ) ;
#8662=CYLINDRICAL_SURFACE ( 'NONE', #15551, 0.1574803149606299191 ) ;
#8663=CARTESIAN_POINT ( 'NONE',  ( 0.9500414927467377701, 0.1787899950787401604, 0.4675196849856070314 ) ) ;
#8664=CARTESIAN_POINT ( 'NONE',  ( -0.8019270111902716547, -0.1787899950787401604, 0.4429133857730084833 ) ) ;
#8665=EDGE_CURVE ( 'NONE', #21217, #5874, #1192, .T. ) ;
#8666=CARTESIAN_POINT ( 'NONE',  ( -0.8759842519685039353, 0.1787899950787401882, 0.8193897637257637756 ) ) ;
#8669=ORIENTED_EDGE ( 'NONE', *, *, #10299, .T. ) ;
#8670=CARTESIAN_POINT ( 'NONE',  ( 0.8019270111902717657, -0.1787899950787401604, 0.8809055117572599514 ) ) ;
#8671=CARTESIAN_POINT ( 'NONE',  ( -0.7185039370078746268, 0.06523048226347956391, 0.2632874015748031260 ) ) ;
#8672=CARTESIAN_POINT ( 'NONE',  ( 0.8019270111902716547, 0.1787899950787401604, 1.141732283410804349 ) ) ;
#8673=CARTESIAN_POINT ( 'NONE',  ( 0.7185039370078739607, 1.928577636452523993E-17, 1.948818897530267602 ) ) ;
#8674=CARTESIAN_POINT ( 'NONE',  ( 1.033464566929133799, 0.000000000000000000, 0.08858267716535432601 ) ) ;
#8678=CARTESIAN_POINT ( 'NONE',  ( -1.054774247047244540, 0.07405724077823318263, 0.9744094487651340231 ) ) ;
#8680=CARTESIAN_POINT ( 'NONE',  ( 0.9873396505805591694, -0.1113553986120547346, 0.3198818897637795700 ) ) ;
#8683=CARTESIAN_POINT ( 'NONE',  ( -1.033464566929133799, 0.000000000000000000, 0.1574803148531029595 ) ) ;
#8685=CARTESIAN_POINT ( 'NONE',  ( -1.033464566929134687, -0.06523048226347956391, 0.08612204724409450174 ) ) ;
#8686=ORIENTED_EDGE ( 'NONE', *, *, #45806, .T. ) ;
#8687=CARTESIAN_POINT ( 'NONE',  ( 0.7495606340400177148, 0.1264236179284866091, 1.336122047190330786 ) ) ;
#8688=CARTESIAN_POINT ( 'NONE',  ( 0.9412147342319837628, 0.1574803149606300301, 0.8833661417322832277 ) ) ;
#8689=CARTESIAN_POINT ( 'NONE',  ( 0.8759842519685039353, 0.000000000000000000, 4.498031496062992574 ) ) ;
#8692=CARTESIAN_POINT ( 'NONE',  ( 0.9500414927467378812, -0.1787899950787401604, 1.628937007820252303 ) ) ;
#8693=CARTESIAN_POINT ( 'NONE',  ( 0.8019270111902717657, 0.1787899950787401604, 0.1131889763241894359 ) ) ;
#8697=CARTESIAN_POINT ( 'NONE',  ( 0.7185039370078739607, 1.928577636452523993E-17, 0.7775590551181102983 ) ) ;
#8698=CARTESIAN_POINT ( 'NONE',  ( -0.8019270111902716547, 0.1787899950787401604, 0.6692913385289143147 ) ) ;
#8704=DIRECTION ( 'NONE',  ( 1.000000000000000000, 0.000000000000000000, -1.822029033848725275E-16 ) ) ;
#8705=CARTESIAN_POINT ( 'NONE',  ( 0.9500414927467378812, 0.1787899950787401604, 1.333661417269071059 ) ) ;
#8706=CARTESIAN_POINT ( 'NONE',  ( 0.9500414927467377701, 0.1787899950787401604, 1.879921259788756016 ) ) ;
#8707=CARTESIAN_POINT ( 'NONE',  ( 1.002407869896990045, 0.1264236179284866091, 0.2632874015210397434 ) ) ;
#8710=CARTESIAN_POINT ( 'NONE',  ( -1.033464566929134687, -0.06523048226347956391, 0.1550196849318430659 ) ) ;
#8711=VERTEX_POINT ( 'NONE', #27360 ) ;
#8712=LINE ( 'NONE', #24290, #2126 ) ;
#8715=CARTESIAN_POINT ( 'NONE',  ( 1.054774247047244540, -0.07405724077823318263, 0.3740157479777325711 ) ) ;
#8716=CARTESIAN_POINT ( 'NONE',  ( 0.7495606340400177148, 0.1264236179284866091, 1.296751968450173154 ) ) ;
#8718=CARTESIAN_POINT ( 'NONE',  ( 0.9412147342319837628, 0.1574803149606300301, 0.8439960629921254842 ) ) ;
#8719=CARTESIAN_POINT ( 'NONE',  ( -1.002407869896990045, -0.1264236179284866091, 1.355807086560409491 ) ) ;
#8720=CARTESIAN_POINT ( 'NONE',  ( 0.9412147342319837628, -0.1574803149606297803, 0.7406496061916858498 ) ) ;
#8722=CARTESIAN_POINT ( 'NONE',  ( -0.9412147342319837628, 0.1574803149606300301, 0.7947834644594015119 ) ) ;
#8726=CARTESIAN_POINT ( 'NONE',  ( -0.9412147342319837628, -0.1574803149606297803, 0.6225393699712132856 ) ) ;
#8727=DIRECTION ( 'NONE',  ( 1.000000000000000000, 0.000000000000000000, -1.822029033848725275E-16 ) ) ;
#8728=CARTESIAN_POINT ( 'NONE',  ( 1.054774247047244540, -0.07405724077823318263, 1.673228346402929834 ) ) ;
#8729=CARTESIAN_POINT ( 'NONE',  ( -0.9873396505805591694, -0.1113553986120547346, 1.304133858267716661 ) ) ;
#8730=CARTESIAN_POINT ( 'NONE',  ( -0.8759842519685039353, -0.1574803149606299191, 1.053149606191685184 ) ) ;
#8732=CARTESIAN_POINT ( 'NONE',  ( -1.033464566929133799, 0.000000000000000000, 0.4429133858267716439 ) ) ;
#8733=CARTESIAN_POINT ( 'NONE',  ( 0.9412147342319837628, 0.1574803149606300301, 0.3617125983176697201 ) ) ;
#8734=CARTESIAN_POINT ( 'NONE',  ( 0.9412147342319837628, 0.1574803149606300301, 1.385334645561763667 ) ) ;
#8739=CARTESIAN_POINT ( 'NONE',  ( 0.8759842519685039353, -0.1787899950787401882, 0.6865157479777322935 ) ) ;
#8740=CARTESIAN_POINT ( 'NONE',  ( -1.054774247047244540, 0.07405724077823318263, 1.599409448765134911 ) ) ;
#8742=CARTESIAN_POINT ( 'NONE',  ( -0.9500414927467378812, 0.1787899950787401604, 1.333661417269071059 ) ) ;
#8743=CARTESIAN_POINT ( 'NONE',  ( -0.7495606340400177148, 0.1264236179284866091, 0.3174212597887562382 ) ) ;
#8750=DIRECTION ( 'NONE',  ( 0.000000000000000000, 0.000000000000000000, -1.000000000000000000 ) ) ;
#8751=CARTESIAN_POINT ( 'NONE',  ( 0.7185039370078739607, 1.928577636452523993E-17, 0.09842519674286673292 ) ) ;
#8753=CIRCLE ( 'NONE', #31734, 0.1870078740157481989 ) ;
#8757=CARTESIAN_POINT ( 'NONE',  ( -0.6971942568897626646, 0.07405724077823318263, 0.1624015747493861017 ) ) ;
#8758=CARTESIAN_POINT ( 'NONE',  ( -0.8759842519685039353, -0.1574803149606299191, 0.9842519685039370358 ) ) ;
#8763=CARTESIAN_POINT ( 'NONE',  ( 0.8759842519685039353, 0.1787899950787401882, 0.8636811023084409733 ) ) ;
#8764=EDGE_CURVE ( 'NONE', #11957, #7898, #46148, .T. ) ;
#8767=CARTESIAN_POINT ( 'NONE',  ( 0.8107537697050253289, 0.1574803149606300301, 1.596948818897636402 ) ) ;
#8768=CARTESIAN_POINT ( 'NONE',  ( 0.7172297754444691975, 0.04339135079164682662, 1.982441116835254036 ) ) ;
#8771=CARTESIAN_POINT ( 'NONE',  ( -1.033464566929134687, 0.06523048226347956391, 1.616633858160190229 ) ) ;
#8774=CARTESIAN_POINT ( 'NONE',  ( 0.8759842519685039353, 0.1787899950787401882, 1.055610236166708793 ) ) ;
#8775=CARTESIAN_POINT ( 'NONE',  ( 1.002407869896990045, -0.1264236179284866091, 1.833169291284818758 ) ) ;
#8776=CARTESIAN_POINT ( 'NONE',  ( 0.7185039370078746268, -0.06523048226347956391, 0.4158464565853862704 ) ) ;
#8778=CARTESIAN_POINT ( 'NONE',  ( 1.033464566929134687, -0.06523048226347956391, 1.257381889656253193 ) ) ;
#8779=CARTESIAN_POINT ( 'NONE',  ( 0.8759842519685039353, -0.1574803149606299191, 1.889763779527559251 ) ) ;
#8781=CARTESIAN_POINT ( 'NONE',  ( -0.9873396505805591694, -0.1113553986120547346, 0.1919291337507405548 ) ) ;
#8783=CARTESIAN_POINT ( 'NONE',  ( 0.6971942568897648851, 0.07405724077823318263, 1.141732283410804349 ) ) ;
#8784=VECTOR ( 'NONE', #13903, 39.37007874015748143 ) ;
#8787=CARTESIAN_POINT ( 'NONE',  ( -1.033464566929133799, 0.000000000000000000, 1.505905511811023612 ) ) ;
#8788=CARTESIAN_POINT ( 'NONE',  ( -0.9500414927467378812, -0.1787899950787401604, 0.5265748030958428139 ) ) ;
#8789=CARTESIAN_POINT ( 'NONE',  ( 0.7646288533564489232, -0.1113553986120547346, 1.363188976270427455 ) ) ;
#8790=CARTESIAN_POINT ( 'NONE',  ( -0.9500414927467378812, -0.1787899950787401604, 0.2116141731745827814 ) ) ;
#8791=( BOUNDED_CURVE ( )  B_SPLINE_CURVE ( 2, ( #20968, #39180, #46845, #14036, #10451, #32504, #6826, #21446, #41055 ),
 .UNSPECIFIED., .F., .F. ) 
 B_SPLINE_CURVE_WITH_KNOTS ( ( 3, 2, 2, 2, 3 ),
 ( 0.7700000000000000178, 0.7724999999999999645, 0.7750000000000000222, 0.7774999999999999689, 0.7800000000000000266 ),
 .UNSPECIFIED. ) 
 CURVE ( )  GEOMETRIC_REPRESENTATION_ITEM ( )  RATIONAL_B_SPLINE_CURVE ( ( 1.000000000000000000, 0.9238795325112869605, 1.000000000000000000, 0.9238795325112869605, 1.000000000000000000, 0.9238795325112869605, 1.000000000000000000, 0.9238795325112869605, 1.000000000000000000 ) ) 
 REPRESENTATION_ITEM ( '' )  ) ;
#8794=CARTESIAN_POINT ( 'NONE',  ( -0.6971942568897648851, 0.07405724077823318263, 1.811023621993480548 ) ) ;
#8795=CARTESIAN_POINT ( 'NONE',  ( -0.8759842519685039353, -0.1787899950787401882, 0.9965551180564724554 ) ) ;
#8796=CARTESIAN_POINT ( 'NONE',  ( -1.002407869896990045, -0.1264236179284866091, 0.5339566928596221063 ) ) ;
#8801=CARTESIAN_POINT ( 'NONE',  ( 0.8759842519685039353, 0.000000000000000000, 4.498031496062992574 ) ) ;
#8802=CARTESIAN_POINT ( 'NONE',  ( -0.7185039370078739607, 0.000000000000000000, -2.869337061179095023E-17 ) ) ;
#8804=CARTESIAN_POINT ( 'NONE',  ( -1.002407869896990045, -0.1264236179284866091, 0.4109251967966299213 ) ) ;
#8808=CARTESIAN_POINT ( 'NONE',  ( -1.054774247047244540, 0.07405724077823318263, 1.525590551127339989 ) ) ;
#8812=EDGE_CURVE ( 'NONE', #33302, #30681, #3611, .T. ) ;
#8813=PRESENTATION_STYLE_ASSIGNMENT (( #19602 ) ) ;
#8814=CARTESIAN_POINT ( 'NONE',  ( 0.7185039370078746268, 0.06523048226347956391, 0.9719488188976379561 ) ) ;
#8816=CARTESIAN_POINT ( 'NONE',  ( 0.7646288533564489232, -0.1113553986120547346, 0.4675196850393700809 ) ) ;
#8820=CARTESIAN_POINT ( 'NONE',  ( -0.9412147342319837628, -0.1574803149606297803, 1.252460629813731741 ) ) ;
#8821=CARTESIAN_POINT ( 'NONE',  ( 1.054774247047244096, 0.000000000000000000, 0.4995078739619842612 ) ) ;
#8822=CARTESIAN_POINT ( 'NONE',  ( 1.054774247047244540, -0.07405724077823318263, 0.09842519679663024046 ) ) ;
#8826=CARTESIAN_POINT ( 'NONE',  ( -0.9412147342319837628, 0.1574803149606300301, 0.4109251968503938590 ) ) ;
#8827=ORIENTED_EDGE ( 'NONE', *, *, #25936, .F. ) ;
#8828=ADVANCED_FACE ( 'NONE', ( #45748 ), #42613, .T. ) ;
#8830=CARTESIAN_POINT ( 'NONE',  ( -0.6971942568897648851, -0.07405724077823297447, 1.072834645615528659 ) ) ;
#8831=CARTESIAN_POINT ( 'NONE',  ( 0.9412147342319837628, -0.1574803149606297803, 1.065452755905511806 ) ) ;
#8839=CARTESIAN_POINT ( 'NONE',  ( 1.033464566929133799, 0.000000000000000000, 0.1968503935932602311 ) ) ;
#8840=CARTESIAN_POINT ( 'NONE',  ( 0.7185039370078746268, -0.06523048226347956391, 0.2682086614173227468 ) ) ;
#8841=CARTESIAN_POINT ( 'NONE',  ( 1.054774247047244540, -0.07405724077823318263, 0.6889763778989935750 ) ) ;
#8843=CARTESIAN_POINT ( 'NONE',  ( -0.7185039370078739607, 0.000000000000000000, -2.869337061179095023E-17 ) ) ;
#8847=CARTESIAN_POINT ( 'NONE',  ( 0.7185039370078739607, 1.928577636452523993E-17, 1.161417322727118284 ) ) ;
#8848=CARTESIAN_POINT ( 'NONE',  ( -0.9412147342319837628, 0.1574803149606300301, 1.857775590443653480 ) ) ;
#8849=CARTESIAN_POINT ( 'NONE',  ( -0.8759842519685039353, 0.1787899950787401882, 0.4650590550643464716 ) ) ;
#8851=ORIENTED_EDGE ( 'NONE', *, *, #45281, .T. ) ;
#8852=CARTESIAN_POINT ( 'NONE',  ( -0.6971942568897648851, -0.07405724077823297447, 1.781496062938362934 ) ) ;
#8854=CARTESIAN_POINT ( 'NONE',  ( 0.6971942568897648851, 0.07405724077823318263, 1.894685039316315489 ) ) ;
#8858=CARTESIAN_POINT ( 'NONE',  ( 0.6971942568897626646, 0.07405724077823318263, 0.3986220471903312301 ) ) ;
#8859=CARTESIAN_POINT ( 'NONE',  ( -0.8759842519685039353, -0.1787899950787401882, 1.429625984198204858 ) ) ;
#8861=CARTESIAN_POINT ( 'NONE',  ( -1.033464566929133799, 0.000000000000000000, 1.624015748031496287 ) ) ;
#8862=CARTESIAN_POINT ( 'NONE',  ( -0.8759842519685039353, -0.1787899950787401882, 0.8784448818360000022 ) ) ;
#8863=CARTESIAN_POINT ( 'NONE',  ( -1.054774247047244540, 0.07405724077823318263, 0.02952755900135457801 ) ) ;
#8864=CARTESIAN_POINT ( 'NONE',  ( -0.7185039370078746268, 0.06523048226347956391, 0.5782480314960627421 ) ) ;
#8865=CARTESIAN_POINT ( 'NONE',  ( -0.6971942568897637749, 2.189545951927499583E-17, 1.700295275536787498 ) ) ;
#8866=CARTESIAN_POINT ( 'NONE',  ( -0.6971942568897637749, 2.189545951927499583E-17, 0.08612204719033110523 ) ) ;
#8868=CARTESIAN_POINT ( 'NONE',  ( -0.7646288533564489232, 0.1113553986120547346, 1.678149606299212726 ) ) ;
#8869=CARTESIAN_POINT ( 'NONE',  ( -1.033464566929133799, 0.000000000000000000, 0.9547244094488189781 ) ) ;
#8876=ORIENTED_EDGE ( 'NONE', *, *, #20053, .F. ) ;
#8877=VERTEX_POINT ( 'NONE', #39262 ) ;
#8883=CARTESIAN_POINT ( 'NONE',  ( -0.7185039370078746268, -0.06523048226347956391, 0.8095472439869610959 ) ) ;
#8885=AXIS2_PLACEMENT_3D ( 'NONE', #11087, #7239, #11551 ) ;
#8888=CARTESIAN_POINT ( 'NONE',  ( 1.054774247047244096, 0.000000000000000000, 0.9670275590013542866 ) ) ;
#8890=CARTESIAN_POINT ( 'NONE',  ( 0.9412147342319837628, -0.1574803149606297803, 1.262303149606299746 ) ) ;
#8891=CARTESIAN_POINT ( 'NONE',  ( 0.8759842519685039353, -0.1787899950787401882, 1.946358267662771757 ) ) ;
#8893=CARTESIAN_POINT ( 'NONE',  ( 0.8759842519685039353, 0.1574803149606299191, 0.2165354330708661457 ) ) ;
#8894=CARTESIAN_POINT ( 'NONE',  ( -0.7185039370078739607, 1.928577636452523993E-17, 1.643700787401574992 ) ) ;
#8896=LINE ( 'NONE', #1449, #33944 ) ;
#8898=( BOUNDED_CURVE ( )  B_SPLINE_CURVE ( 2, ( #38140, #15408, #1231, #33874, #5070, #41939, #993, #44840, #23298 ),
 .UNSPECIFIED., .F., .T. ) 
 B_SPLINE_CURVE_WITH_KNOTS ( ( 3, 2, 2, 2, 3 ),
 ( 0.5999999999999999778, 0.6025000000000000355, 0.6049999999999999822, 0.6075000000000000400, 0.6099999999999999867 ),
 .UNSPECIFIED. ) 
 CURVE ( )  GEOMETRIC_REPRESENTATION_ITEM ( )  RATIONAL_B_SPLINE_CURVE ( ( 1.000000000000000000, 0.9238795325112869605, 1.000000000000000000, 0.9238795325112869605, 1.000000000000000000, 0.9238795325112869605, 1.000000000000000000, 0.9238795325112869605, 1.000000000000000000 ) ) 
 REPRESENTATION_ITEM ( '' )  ) ;
#8899=CARTESIAN_POINT ( 'NONE',  ( -0.9500414927467378812, 0.1787899950787401604, 1.761811023568284007 ) ) ;
#8901=CARTESIAN_POINT ( 'NONE',  ( -0.9500414927467378812, -0.1787899950787401604, 1.279527559001355286 ) ) ;
#8902=CARTESIAN_POINT ( 'NONE',  ( -0.9873396505805591694, 0.1113553986120547346, 1.313976377952756014 ) ) ;
#8903=CARTESIAN_POINT ( 'NONE',  ( 0.6971942568897637749, 2.189545951927499583E-17, 1.424704724355685181 ) ) ;
#8905=CARTESIAN_POINT ( 'NONE',  ( -1.054774247047244540, -0.07405724077823318263, 1.240157480261197431 ) ) ;
#8906=CARTESIAN_POINT ( 'NONE',  ( 0.7646288533564489232, 0.1113553986120547346, 1.550196850286173156 ) ) ;
#8908=CARTESIAN_POINT ( 'NONE',  ( 0.9412147342319837628, 0.1574803149606300301, 0.04675196839640998608 ) ) ;
#8909=CARTESIAN_POINT ( 'NONE',  ( 0.6971942568897637749, 2.189545951927499583E-17, 0.5979330708123780092 ) ) ;
#8910=CARTESIAN_POINT ( 'NONE',  ( -0.8019270111902716547, -0.1787899950787401604, 0.3641732282926931630 ) ) ;
#8914=VERTEX_POINT ( 'NONE', #46687 ) ;
#8916=CARTESIAN_POINT ( 'NONE',  ( -0.7646288533564489232, -0.1113553986120547346, 0.2706692913385826960 ) ) ;
#8917=CARTESIAN_POINT ( 'NONE',  ( 0.8019270111902716547, -0.1787899950787401604, 1.156496062938362046 ) ) ;
#8921=ORIENTED_EDGE ( 'NONE', *, *, #31084, .T. ) ;
#8922=CARTESIAN_POINT ( 'NONE',  ( -0.6971942568897626646, -0.07405724077823297447, 0.9547244093950547628 ) ) ;
#8923=( BOUNDED_CURVE ( )  B_SPLINE_CURVE ( 2, ( #14245, #10172, #13996, #9704, #21170, #10416, #2948, #31754, #35804 ),
 .UNSPECIFIED., .F., .T. ) 
 B_SPLINE_CURVE_WITH_KNOTS ( ( 3, 2, 2, 2, 3 ),
 ( 0.3200000000000000067, 0.3225000000000000089, 0.3250000000000000111, 0.3275000000000000133, 0.3300000000000000155 ),
 .UNSPECIFIED. ) 
 CURVE ( )  GEOMETRIC_REPRESENTATION_ITEM ( )  RATIONAL_B_SPLINE_CURVE ( ( 1.000000000000000000, 0.9238795325112869605, 1.000000000000000000, 0.9238795325112869605, 1.000000000000000000, 0.9238795325112869605, 1.000000000000000000, 0.9238795325112869605, 1.000000000000000000 ) ) 
 REPRESENTATION_ITEM ( '' )  ) ;
#8925=CARTESIAN_POINT ( 'NONE',  ( -1.002407869896990045, 0.1264236179284866091, 0.06643700782025216411 ) ) ;
#8927=ORIENTED_EDGE ( 'NONE', *, *, #45094, .F. ) ;
#8931=ORIENTED_EDGE ( 'NONE', *, *, #32872, .F. ) ;
#8932=CARTESIAN_POINT ( 'NONE',  ( 0.7185039370078746268, 0.06523048226347956391, 0.8932086614173216921 ) ) ;
#8936=CYLINDRICAL_SURFACE ( 'NONE', #24169, 0.1574803149606299191 ) ;
#8941=EDGE_CURVE ( 'NONE', #38112, #8361, #3324, .T. ) ;
#8942=CARTESIAN_POINT ( 'NONE',  ( 0.9500414927467378812, -0.1787899950787401604, 0.4478346456155276045 ) ) ;
#8944=CARTESIAN_POINT ( 'NONE',  ( -1.002407869896990045, -0.1264236179284866091, 0.6914370078202519698 ) ) ;
#8946=CARTESIAN_POINT ( 'NONE',  ( 1.033464566929134687, 0.06523048226347956391, 0.08120078729404769935 ) ) ;
#8948=DIRECTION ( 'NONE',  ( -1.000000000000000000, 0.000000000000000000, 0.000000000000000000 ) ) ;
#8951=CARTESIAN_POINT ( 'NONE',  ( 0.8759842519685039353, 0.1787899950787401882, 1.532972440891118060 ) ) ;
#8952=CARTESIAN_POINT ( 'NONE',  ( 1.054774247047244540, 0.07405724077823318263, 1.835629921206078485 ) ) ;
#8953=CARTESIAN_POINT ( 'NONE',  ( 0.6971942568897626646, 0.07405724077823318263, 0.3149606298674962890 ) ) ;
#8954=CARTESIAN_POINT ( 'NONE',  ( -0.9412147342319837628, -0.1574803149606297803, 0.1500984250893234173 ) ) ;
#8955=DIRECTION ( 'NONE',  ( 0.000000000000000000, 0.000000000000000000, -1.000000000000000000 ) ) ;
#8958=CARTESIAN_POINT ( 'NONE',  ( 0.7495606340400177148, -0.1264236179284866091, 0.5191929133320630774 ) ) ;
#8959=CARTESIAN_POINT ( 'NONE',  ( 0.7576286657187201179, -0.1165239664453579099, 0.03937184544582203460 ) ) ;
#8960=CARTESIAN_POINT ( 'NONE',  ( -0.7646288533564489232, 0.1113553986120547346, 1.717519685039369914 ) ) ;
#8962=CARTESIAN_POINT ( 'NONE',  ( -0.7495606340400177148, 0.1264236179284866091, 1.336122047190330786 ) ) ;
#8963=CARTESIAN_POINT ( 'NONE',  ( 0.9873396505805591694, 0.1113553986120547346, 0.7923228345381417848 ) ) ;
#8965=CARTESIAN_POINT ( 'NONE',  ( -1.054774247047244540, -0.07405724077823318263, 1.087598425143086578 ) ) ;
#8966=CARTESIAN_POINT ( 'NONE',  ( 0.8019270111902717657, 0.1787899950787401604, 1.062992125930488418 ) ) ;
#8968=CARTESIAN_POINT ( 'NONE',  ( -0.7646288533564489232, 0.1113553986120547346, 0.5265748030420794867 ) ) ;
#8969=CARTESIAN_POINT ( 'NONE',  ( -0.8759842519685039353, -0.1574803149606299191, 1.220472440944881942 ) ) ;
#8970=CARTESIAN_POINT ( 'NONE',  ( 1.054774247047244540, 0.07405724077823318263, 1.717519684985606476 ) ) ;
#8971=CARTESIAN_POINT ( 'NONE',  ( -1.033464566929134687, 0.06523048226347956391, 1.232775590551179912 ) ) ;
#8973=CARTESIAN_POINT ( 'NONE',  ( -0.7185039370078739607, 1.928577636452523993E-17, 0.7381889763779527769 ) ) ;
#8974=CARTESIAN_POINT ( 'NONE',  ( -0.9412147342319837628, -0.1574803149606297803, 0.5044291337507409434 ) ) ;
#8975=CARTESIAN_POINT ( 'NONE',  ( 0.7646288533564489232, 0.1113553986120547346, 1.432086614065700925 ) ) ;
#8977=ORIENTED_EDGE ( 'NONE', *, *, #6260, .F. ) ;
#8978=CARTESIAN_POINT ( 'NONE',  ( 0.7185039370078739607, 0.000000000000000000, 4.498031496062993462 ) ) ;
#8979=CARTESIAN_POINT ( 'NONE',  ( 0.7495606340400177148, 0.1264236179284866091, 0.9473425196312755814 ) ) ;
#8980=CARTESIAN_POINT ( 'NONE',  ( -0.9500414927467377701, 0.1787899950787401604, 1.604330708607653921 ) ) ;
#8982=CARTESIAN_POINT ( 'NONE',  ( -0.9500414927467378812, 0.1787899950787401604, 1.491141732229701367 ) ) ;
#8986=CARTESIAN_POINT ( 'NONE',  ( -1.033464566929133799, 1.928577636452524610E-17, 2.869337061179095023E-17 ) ) ;
#8991=ADVANCED_FACE ( 'NONE', ( #47414 ), #36863, .T. ) ;
#8993=CARTESIAN_POINT ( 'NONE',  ( -0.7646288533564489232, -0.1113553986120547346, 1.205708661309795371 ) ) ;
#8994=DIRECTION ( 'NONE',  ( 1.000000000000000000, 0.000000000000000000, -1.822029033848725275E-16 ) ) ;
#8996=CARTESIAN_POINT ( 'NONE',  ( 0.7185039370078746268, 0.06523048226347956391, 1.798720472440944462 ) ) ;
#8999=CARTESIAN_POINT ( 'NONE',  ( -0.8019270111902716547, 0.1787899950787401604, 0.1968503936470238636 ) ) ;
#9000=CARTESIAN_POINT ( 'NONE',  ( -0.9873396505805591694, 0.1113553986120547346, 0.9990157480314961758 ) ) ;
#9003=CARTESIAN_POINT ( 'NONE',  ( 0.6971942568897648851, 0.07405724077823318263, 1.067913385773007651 ) ) ;
#9005=CARTESIAN_POINT ( 'NONE',  ( 0.9873396505805591694, -0.1113553986120547346, 1.619094488188976388 ) ) ;
#9006=CARTESIAN_POINT ( 'NONE',  ( 0.7619656079993829545, 0.1146971827241134723, 1.980798226884399327 ) ) ;
#9008=CARTESIAN_POINT ( 'NONE',  ( 0.7646288533564489232, -0.1113553986120547346, 0.4576771652468039631 ) ) ;
#9010=CARTESIAN_POINT ( 'NONE',  ( -0.7646288533564489232, 0.1113553986120547346, 1.628937007766488199 ) ) ;
#9012=LINE ( 'NONE', #43832, #54 ) ;
#9013=CARTESIAN_POINT ( 'NONE',  ( 1.002407869896990045, -0.1264236179284866091, 0.9621062991588346103 ) ) ;
#9014=CARTESIAN_POINT ( 'NONE',  ( 0.6971942568897648851, -0.07405724077823297447, 1.860236220418677089 ) ) ;
#9015=CARTESIAN_POINT ( 'NONE',  ( 1.033464566929134687, -0.06523048226347956391, 0.3518700786326304231 ) ) ;
#9021=CARTESIAN_POINT ( 'NONE',  ( 0.6971942568897648851, -0.07405724077823297447, 1.343503936954111744 ) ) ;
#9025=CARTESIAN_POINT ( 'NONE',  ( -0.8759842519685039353, 0.1574803149606299191, 1.870078740157480324 ) ) ;
#9026=CARTESIAN_POINT ( 'NONE',  ( -0.8019270111902717657, -0.1787899950787401604, 0.5216535432533228045 ) ) ;
#9030=FACE_OUTER_BOUND ( 'NONE', #7042, .T. ) ;
#9034=CARTESIAN_POINT ( 'NONE',  ( -1.054774247047244540, -0.07405724077823318263, 1.048228346402930944 ) ) ;
#9035=CARTESIAN_POINT ( 'NONE',  ( -1.054774247047244540, -0.07405724077823318263, 1.830708661363559253 ) ) ;
#9037=CARTESIAN_POINT ( 'NONE',  ( -0.6971942568897637749, 2.189545951927499583E-17, 0.7160433070328504623 ) ) ;
#9038=( BOUNDED_CURVE ( )  B_SPLINE_CURVE ( 2, ( #40897, #8091, #19110, #33775, #37812, #34235, #30643, #15545, #23668 ),
 .UNSPECIFIED., .F., .T. ) 
 B_SPLINE_CURVE_WITH_KNOTS ( ( 3, 2, 2, 2, 3 ),
 ( 0.9000000000000000222, 0.9024999999999999689, 0.9050000000000000266, 0.9074999999999999734, 0.9100000000000000311 ),
 .UNSPECIFIED. ) 
 CURVE ( )  GEOMETRIC_REPRESENTATION_ITEM ( )  RATIONAL_B_SPLINE_CURVE ( ( 1.000000000000000000, 0.9238795325112869605, 1.000000000000000000, 0.9238795325112869605, 1.000000000000000000, 0.9238795325112869605, 1.000000000000000000, 0.9238795325112869605, 1.000000000000000000 ) ) 
 REPRESENTATION_ITEM ( '' )  ) ;
#9040=ORIENTED_EDGE ( 'NONE', *, *, #22181, .T. ) ;
#9049=CIRCLE ( 'NONE', #6738, 0.1787899950787401049 ) ;
#9050=CARTESIAN_POINT ( 'NONE',  ( -0.9500414927467378812, 0.1787899950787401604, 0.5019685038832442103 ) ) ;
#9051=DIRECTION ( 'NONE',  ( 1.000000000000000000, 0.000000000000000000, -1.822029033848725275E-16 ) ) ;
#9052=ORIENTED_EDGE ( 'NONE', *, *, #2499, .T. ) ;
#9054=CARTESIAN_POINT ( 'NONE',  ( -0.9500414927467377701, 0.1787899950787401604, 1.530511810969859221 ) ) ;
#9058=CARTESIAN_POINT ( 'NONE',  ( -1.033464566929133799, 0.000000000000000000, 1.466535433070866201 ) ) ;
#9059=CARTESIAN_POINT ( 'NONE',  ( 0.7646288533564489232, 0.1113553986120547346, 0.4576771653543307283 ) ) ;
#9062=CARTESIAN_POINT ( 'NONE',  ( -1.033464566929134687, -0.06523048226347956391, 1.178641732175937040 ) ) ;
#9063=CARTESIAN_POINT ( 'NONE',  ( 0.6971942568897626646, 0.07405724077823318263, 0.6742125983714335469 ) ) ;
#9064=CARTESIAN_POINT ( 'NONE',  ( 0.8759842519685039353, 0.1787899950787401882, 0.07135826766277185429 ) ) ;
#9067=CARTESIAN_POINT ( 'NONE',  ( -0.7185039370078739607, 0.000000000000000000, -2.869337061179095023E-17 ) ) ;
#9070=CARTESIAN_POINT ( 'NONE',  ( 0.8759842519685039353, 0.1574803149606299191, 1.122047244094488194 ) ) ;
#9075=CARTESIAN_POINT ( 'NONE',  ( 0.9412147342319837628, -0.1574803149606297803, 1.685531495955465697 ) ) ;
#9077=FACE_OUTER_BOUND ( 'NONE', #23461, .T. ) ;
#9079=VERTEX_POINT ( 'NONE', #7157 ) ;
#9080=CARTESIAN_POINT ( 'NONE',  ( 0.8107537697050234415, -0.1574803149606297803, 0.2731299212598424231 ) ) ;
#9081=CARTESIAN_POINT ( 'NONE',  ( 0.6971942568897637749, 2.189545951927499583E-17, 0.8292322834108031282 ) ) ;
#9084=CARTESIAN_POINT ( 'NONE',  ( -1.033464566929133799, 1.928577636452524610E-17, 2.869337061179095023E-17 ) ) ;
#9089=CARTESIAN_POINT ( 'NONE',  ( 0.8759842519685039353, 0.1574803149606299191, 1.230314960522393752 ) ) ;
#9090=VERTEX_POINT ( 'NONE', #24904 ) ;
#9092=CARTESIAN_POINT ( 'NONE',  ( -0.9500414927467378812, -0.1787899950787401604, 1.948818897584033927 ) ) ;
#9093=CARTESIAN_POINT ( 'NONE',  ( 0.9500414927467378812, -0.1787899950787401604, 1.830708661363559253 ) ) ;
#9095=CARTESIAN_POINT ( 'NONE',  ( -0.9500414927467378812, -0.1787899950787401604, 0.8858267715997791836 ) ) ;
#9097=CARTESIAN_POINT ( 'NONE',  ( 0.9500414927467378812, -0.1787899950787401604, 0.4921259841982048577 ) ) ;
#9098=CARTESIAN_POINT ( 'NONE',  ( -1.054774247047244540, 0.07405724077823318263, 1.402559055064346971 ) ) ;
#9099=CARTESIAN_POINT ( 'NONE',  ( 0.8759842519685039353, 0.000000000000000000, 4.498031496062992574 ) ) ;
#9101=CARTESIAN_POINT ( 'NONE',  ( -1.002407869896990045, 0.1264236179284866091, 0.9719488188438739629 ) ) ;
#9102=CARTESIAN_POINT ( 'NONE',  ( -1.002407869896990045, 0.1264236179284866091, 0.07135826766277185429 ) ) ;
#9103=ADVANCED_FACE ( 'NONE', ( #35916 ), #17244, .T. ) ;
#9105=CARTESIAN_POINT ( 'NONE',  ( -0.8019270111902717657, 0.1787899950787401604, 1.811023621993480548 ) ) ;
#9106=CARTESIAN_POINT ( 'NONE',  ( -0.8759842519685039353, 0.1574803149606299191, 1.978346456585385882 ) ) ;
#9108=CARTESIAN_POINT ( 'NONE',  ( -0.8759842519685039353, -0.1574803149606299191, 1.771653543307086576 ) ) ;
#9109=CARTESIAN_POINT ( 'NONE',  ( -0.9873396505805591694, -0.1113553986120547346, 0.9498031496062993018 ) ) ;
#9110=CARTESIAN_POINT ( 'NONE',  ( 0.8019270111902716547, 0.1787899950787401604, 1.732283464513166615 ) ) ;
#9112=CARTESIAN_POINT ( 'NONE',  ( -0.9873396505805591694, -0.1113553986120547346, 0.7431102361129447997 ) ) ;
#9113=EDGE_CURVE ( 'NONE', #25448, #25968, #17465, .T. ) ;
#9116=ORIENTED_EDGE ( 'NONE', *, *, #33785, .T. ) ;
#9123=CARTESIAN_POINT ( 'NONE',  ( 0.9500414927467378812, -0.1787899950787401604, 1.825787401521040243 ) ) ;
#9125=CARTESIAN_POINT ( 'NONE',  ( -0.8759842519685039353, 0.1574803149606299191, 0.8759842518609765039 ) ) ;
#9127=CARTESIAN_POINT ( 'NONE',  ( 0.9500414927467378812, -0.1787899950787401604, 0.9596456692375764375 ) ) ;
#9128=CARTESIAN_POINT ( 'NONE',  ( 0.7646288533564489232, 0.1113553986120547346, 0.6151574803149606474 ) ) ;
#9130=CARTESIAN_POINT ( 'NONE',  ( 0.6971942568897648851, 0.07405724077823318263, 1.973425196796630088 ) ) ;
#9135=CARTESIAN_POINT ( 'NONE',  ( 0.6971942568897637749, 2.189545951927499583E-17, 0.3617125983714334359 ) ) ;
#9138=CARTESIAN_POINT ( 'NONE',  ( -1.002407869896990045, 0.1264236179284866091, 1.877460629867496067 ) ) ;
#9139=ORIENTED_EDGE ( 'NONE', *, *, #16095, .T. ) ;
#9140=CARTESIAN_POINT ( 'NONE',  ( -0.8759842519685039353, 0.1787899950787401882, 1.336122047190330786 ) ) ;
#9141=CARTESIAN_POINT ( 'NONE',  ( 0.8759842519685039353, 0.1787899950787401882, 1.414862204670645829 ) ) ;
#9142=CARTESIAN_POINT ( 'NONE',  ( 1.033464566929133799, 0.000000000000000000, 0.9448818896562519720 ) ) ;
#9143=CARTESIAN_POINT ( 'NONE',  ( 0.6971942568897626646, -0.07405724077823297447, 0.08858267711159097113 ) ) ;
#9144=CARTESIAN_POINT ( 'NONE',  ( -0.7495606340400177148, -0.1264236179284866091, 1.267224409395055096 ) ) ;
#9147=CARTESIAN_POINT ( 'NONE',  ( 0.8759842519685039353, -0.1787899950787401882, 0.6077755904974173617 ) ) ;
#9148=CARTESIAN_POINT ( 'NONE',  ( -0.8759842519685039353, -0.1787899950787401882, 0.5634842519147401640 ) ) ;
#9152=ORIENTED_EDGE ( 'NONE', *, *, #15833, .F. ) ;
#9153=CARTESIAN_POINT ( 'NONE',  ( -0.9873396505805591694, -0.1113553986120547346, 0.2805118110236220486 ) ) ;
#9154=CARTESIAN_POINT ( 'NONE',  ( 1.002407869896990045, 0.1264236179284866091, 1.213090551127338435 ) ) ;
#9157=ORIENTED_EDGE ( 'NONE', *, *, #40291, .T. ) ;
#9158=ADVANCED_FACE ( 'NONE', ( #14588 ), #43805, .T. ) ;
#9160=CARTESIAN_POINT ( 'NONE',  ( -0.8759842519685039353, -0.1787899950787401882, 0.9227362204186770889 ) ) ;
#9161=CARTESIAN_POINT ( 'NONE',  ( -0.8019270111902717657, -0.1787899950787401604, 0.2066929133320631329 ) ) ;
#9163=ORIENTED_EDGE ( 'NONE', *, *, #9953, .F. ) ;
#9164=CARTESIAN_POINT ( 'NONE',  ( 0.7185039370078739607, 1.928577636452523993E-17, 1.013779527559055094 ) ) ;
#9168=CARTESIAN_POINT ( 'NONE',  ( 0.9500414927467378812, -0.1787899950787401604, 1.353346456639149986 ) ) ;
#9171=CARTESIAN_POINT ( 'NONE',  ( 1.054774247047244096, 0.000000000000000000, 1.596948818843874074 ) ) ;
#9175=DIRECTION ( 'NONE',  ( 0.000000000000000000, 0.000000000000000000, 1.000000000000000000 ) ) ;
#9178=( BOUNDED_CURVE ( )  B_SPLINE_CURVE ( 2, ( #35069, #24743, #20668, #39106, #6280, #46536, #23801, #13034, #2686 ),
 .UNSPECIFIED., .F., .T. ) 
 B_SPLINE_CURVE_WITH_KNOTS ( ( 3, 2, 2, 2, 3 ),
 ( 0.6099999999999999867, 0.6125000000000000444, 0.6149999999999999911, 0.6175000000000000488, 0.6199999999999999956 ),
 .UNSPECIFIED. ) 
 CURVE ( )  GEOMETRIC_REPRESENTATION_ITEM ( )  RATIONAL_B_SPLINE_CURVE ( ( 1.000000000000000000, 0.9238795325112899581, 1.000000000000000000, 0.9238795325112869605, 1.000000000000000000, 0.9238795325112869605, 1.000000000000000000, 0.9238795325112869605, 1.000000000000000000 ) ) 
 REPRESENTATION_ITEM ( '' )  ) ;
#9179=CARTESIAN_POINT ( 'NONE',  ( -0.7495606340400177148, 0.1264236179284866091, 0.8292322834108031282 ) ) ;
#9183=CARTESIAN_POINT ( 'NONE',  ( -0.8092022386113262300, -0.1589064940435495621, 1.986942102874373228 ) ) ;
#9185=CARTESIAN_POINT ( 'NONE',  ( 0.6971942568897648851, 0.07405724077823318263, 1.500984251914741607 ) ) ;
#9186=CARTESIAN_POINT ( 'NONE',  ( 0.8019270111902716547, -0.1787899950787401604, 1.860236220418677089 ) ) ;
#9187=CARTESIAN_POINT ( 'NONE',  ( 1.054774247047244540, -0.07405724077823318263, 0.3740157479777325711 ) ) ;
#9188=LINE ( 'NONE', #1273, #10001 ) ;
#9189=LINE ( 'NONE', #19966, #28958 ) ;
#9192=CARTESIAN_POINT ( 'NONE',  ( 0.9500414927467378812, -0.1787899950787401604, 0.4084645668753704717 ) ) ;
#9193=CARTESIAN_POINT ( 'NONE',  ( 0.8084376188356441340, -0.1475773522112547032, 0.03937232269030457865 ) ) ;
#9194=CARTESIAN_POINT ( 'NONE',  ( -0.7185039370078746268, 0.06523048226347956391, 1.719980314960630086 ) ) ;
#9195=CARTESIAN_POINT ( 'NONE',  ( 0.8107537697050254399, 0.1574803149606300301, 0.8489173228346468258 ) ) ;
#9196=CARTESIAN_POINT ( 'NONE',  ( -0.7495606340400177148, -0.1264236179284866091, 1.503444881836000002 ) ) ;
#9197=CARTESIAN_POINT ( 'NONE',  ( 1.033464566929134687, -0.06523048226347956391, 0.8636811022546767580 ) ) ;
#9199=LINE ( 'NONE', #23817, #9249 ) ;
#9200=CARTESIAN_POINT ( 'NONE',  ( 0.8019270111902717657, -0.1787899950787401604, 1.077755905458048113 ) ) ;
#9204=CARTESIAN_POINT ( 'NONE',  ( -1.033464566929134687, -0.06523048226347956391, 0.6274606298137325178 ) ) ;
#9205=CARTESIAN_POINT ( 'NONE',  ( -1.033464566929134687, -0.06523048226347956391, 1.227854330708661124 ) ) ;
#9206=CARTESIAN_POINT ( 'NONE',  ( -0.9412147342319837628, -0.1574803149606297803, 1.380413385826771977 ) ) ;
#9207=CARTESIAN_POINT ( 'NONE',  ( 1.033464566929134687, 0.06523048226347956391, 0.2386811022546777294 ) ) ;
#9208=DIRECTION ( 'NONE',  ( 1.000000000000000000, 0.000000000000000000, -1.822029033848725275E-16 ) ) ;
#9209=CARTESIAN_POINT ( 'NONE',  ( 1.033464566929134687, 0.06523048226347956391, 1.941437007874014187 ) ) ;
#9210=CARTESIAN_POINT ( 'NONE',  ( 1.054774247047244540, -0.07405724077823318263, 0.1427165353793073133 ) ) ;
#9211=CARTESIAN_POINT ( 'NONE',  ( 0.8107537697050253289, -0.1574803149606297803, 1.483759842412158525 ) ) ;
#9212=ORIENTED_EDGE ( 'NONE', *, *, #11332, .F. ) ;
#9214=( BOUNDED_CURVE ( )  B_SPLINE_CURVE ( 2, ( #22699, #11698, #33285, #32805, #33763, #25611, #40642, #19093, #872 ),
 .UNSPECIFIED., .F., .F. ) 
 B_SPLINE_CURVE_WITH_KNOTS ( ( 3, 2, 2, 2, 3 ),
 ( 0.2999999999999999889, 0.3024999999999999911, 0.3049999999999999933, 0.3074999999999999956, 0.3099999999999999978 ),
 .UNSPECIFIED. ) 
 CURVE ( )  GEOMETRIC_REPRESENTATION_ITEM ( )  RATIONAL_B_SPLINE_CURVE ( ( 1.000000000000000000, 0.9238795325112869605, 1.000000000000000000, 0.9238795325112869605, 1.000000000000000000, 0.9238795325112869605, 1.000000000000000000, 0.9238795325112869605, 1.000000000000000000 ) ) 
 REPRESENTATION_ITEM ( '' )  ) ;
#9216=VECTOR ( 'NONE', #23052, 39.37007874015748143 ) ;
#9220=CARTESIAN_POINT ( 'NONE',  ( 0.8019270111902717657, 0.1787899950787401604, 0.7086614172690703928 ) ) ;
#9221=CARTESIAN_POINT ( 'NONE',  ( -1.054774247047244540, -0.07405724077823318263, 1.751968503883245987 ) ) ;
#9224=EDGE_CURVE ( 'NONE', #13621, #19295, #13423, .T. ) ;
#9225=AXIS2_PLACEMENT_3D ( 'NONE', #11768, #26141, #26387 ) ;
#9227=DIRECTION ( 'NONE',  ( 0.000000000000000000, 0.000000000000000000, -1.000000000000000000 ) ) ;
#9230=ORIENTED_EDGE ( 'NONE', *, *, #38271, .T. ) ;
#9232=ORIENTED_EDGE ( 'NONE', *, *, #12641, .T. ) ;
#9235=CARTESIAN_POINT ( 'NONE',  ( -0.7646288533564489232, -0.1113553986120547346, 1.451771653543306950 ) ) ;
#9236=CARTESIAN_POINT ( 'NONE',  ( 0.7185039370078739607, 1.928577636452523993E-17, 1.761811023622047223 ) ) ;
#9240=CARTESIAN_POINT ( 'NONE',  ( -0.6971942568897637749, 2.189545951927499583E-17, 0.4010826771115905687 ) ) ;
#9241=CARTESIAN_POINT ( 'NONE',  ( -0.8107537697050253289, -0.1574803149606297803, 1.060531496062992352 ) ) ;
#9244=CARTESIAN_POINT ( 'NONE',  ( 0.6971942568897648851, -0.07405724077823297447, 1.033464566875371027 ) ) ;
#9245=CARTESIAN_POINT ( 'NONE',  ( 0.8019270111902716547, 0.1787899950787401604, 0.2312992125446618197 ) ) ;
#9247=CARTESIAN_POINT ( 'NONE',  ( 0.7646288533564489232, -0.1113553986120547346, 1.609251968503937036 ) ) ;
#9248=CARTESIAN_POINT ( 'NONE',  ( 0.8759842519685039353, -0.1574803149606299191, 1.417322834645669216 ) ) ;
#9249=VECTOR ( 'NONE', #45372, 39.37007874015748143 ) ;
#9250=FACE_OUTER_BOUND ( 'NONE', #45613, .T. ) ;
#9253=CARTESIAN_POINT ( 'NONE',  ( 0.9500414927467377701, 0.1787899950787401604, 1.053149606245450176 ) ) ;
#9255=CARTESIAN_POINT ( 'NONE',  ( 0.7646288533564489232, -0.1113553986120547346, 0.3789370077664886427 ) ) ;
#9259=CARTESIAN_POINT ( 'NONE',  ( 0.7646288533564489232, -0.1113553986120547346, 1.245078740049952559 ) ) ;
#9260=ADVANCED_FACE ( 'NONE', ( #1130 ), #26336, .T. ) ;
#9262=CARTESIAN_POINT ( 'NONE',  ( -0.8107537697050234415, -0.1574803149606297803, 0.2239173227271187561 ) ) ;
#9263=ORIENTED_EDGE ( 'NONE', *, *, #32223, .T. ) ;
#9265=CARTESIAN_POINT ( 'NONE',  ( 0.8759842519685039353, 0.1787899950787401882, 1.252460629867496067 ) ) ;
#9266=CARTESIAN_POINT ( 'NONE',  ( 0.9873396505805591694, 0.1113553986120547346, 1.225393700679874076 ) ) ;
#9269=ADVANCED_FACE ( 'NONE', ( #26571 ), #37564, .T. ) ;
#9270=CARTESIAN_POINT ( 'NONE',  ( -0.8759842519685039353, -0.1787899950787401882, 0.6422244093950550958 ) ) ;
#9271=CARTESIAN_POINT ( 'NONE',  ( 0.9873396505805591694, -0.1113553986120547346, 1.373031495955464587 ) ) ;
#9273=ORIENTED_EDGE ( 'NONE', *, *, #10464, .F. ) ;
#9274=ORIENTED_EDGE ( 'NONE', *, *, #33152, .F. ) ;
#9276=CARTESIAN_POINT ( 'NONE',  ( -1.002407869896990045, 0.1264236179284866091, 0.9374999999462362288 ) ) ;
#9277=CARTESIAN_POINT ( 'NONE',  ( -0.8107537697050234415, -0.1574803149606297803, 0.03690944881889771101 ) ) ;
#9279=CARTESIAN_POINT ( 'NONE',  ( -0.7495606340400177148, 0.1264236179284866091, 0.6323818897100157432 ) ) ;
#9288=DIRECTION ( 'NONE',  ( 0.000000000000000000, 0.000000000000000000, -1.000000000000000000 ) ) ;
#9292=CARTESIAN_POINT ( 'NONE',  ( -1.033464566929134687, -0.06523048226347956391, 1.178641732175937040 ) ) ;
#9293=CARTESIAN_POINT ( 'NONE',  ( -0.9500414927467378812, 0.1787899950787401604, 0.4232283464029293896 ) ) ;
#9294=CARTESIAN_POINT ( 'NONE',  ( 0.7185039370078714072, 0.06523048226347728795, 1.355807086506647829 ) ) ;
#9296=CARTESIAN_POINT ( 'NONE',  ( -0.6971942568897648851, 0.07405724077823318263, 1.697834645615527771 ) ) ;
#9299=CARTESIAN_POINT ( 'NONE',  ( 1.033464566929134687, 0.06523048226347956391, 0.5634842519685042683 ) ) ;
#9301=CARTESIAN_POINT ( 'NONE',  ( 0.7646288533564489232, -0.1113553986120547346, 0.9399606299212598381 ) ) ;
#9302=CARTESIAN_POINT ( 'NONE',  ( -1.033464566929134687, 0.06523048226347956391, 1.301673228238930502 ) ) ;
#9304=CARTESIAN_POINT ( 'NONE',  ( 0.8759842519685039353, -0.1574803149606299191, 0.3543307086614173040 ) ) ;
#9305=CARTESIAN_POINT ( 'NONE',  ( -0.7185039370078739607, 1.928577636452523993E-17, 1.200787401467275695 ) ) ;
#9306=EDGE_LOOP ( 'NONE', ( #20771, #689, #35472, #31335 ) ) ;
#9309=CARTESIAN_POINT ( 'NONE',  ( -0.8019270111902716547, -0.1787899950787401604, 1.117125984198206412 ) ) ;
#9310=CARTESIAN_POINT ( 'NONE',  ( 0.7185039370078746268, -0.06523048226347956391, 1.055610236220473341 ) ) ;
#9314=DIRECTION ( 'NONE',  ( 0.000000000000000000, 0.000000000000000000, -1.000000000000000000 ) ) ;
#9318=CARTESIAN_POINT ( 'NONE',  ( -1.033464566929134687, -0.06523048226347956391, 1.966043306979087246 ) ) ;
#9326=CARTESIAN_POINT ( 'NONE',  ( 1.033464566929133799, 0.000000000000000000, 1.151574803149606474 ) ) ;
#9327=CARTESIAN_POINT ( 'NONE',  ( 1.002407869896990045, 0.1264236179284866091, 0.7750984251430865779 ) ) ;
#9329=CARTESIAN_POINT ( 'NONE',  ( 1.033464566929134687, -0.06523048226347956391, 1.306594488188977055 ) ) ;
#9330=CARTESIAN_POINT ( 'NONE',  ( -0.7185039370078739607, 1.928577636452523993E-17, 0.4527559054042842868 ) ) ;
#9336=CARTESIAN_POINT ( 'NONE',  ( 0.9412147342319837628, -0.1574803149606297803, 1.173720472333417586 ) ) ;
#9339=CARTESIAN_POINT ( 'NONE',  ( -0.6971942568897648851, -0.07405724077823297447, 1.978346456639149320 ) ) ;
#9340=CARTESIAN_POINT ( 'NONE',  ( 0.7495606340400177148, -0.1264236179284866091, 1.783956692859621995 ) ) ;
#9342=CARTESIAN_POINT ( 'NONE',  ( 0.7646288533564489232, -0.1113553986120547346, 1.766732283464566899 ) ) ;
#9343=CARTESIAN_POINT ( 'NONE',  ( -0.8759842519685039353, 0.1787899950787401882, 1.331200787347811110 ) ) ;
#9345=CARTESIAN_POINT ( 'NONE',  ( -0.8759842519685039353, -0.1787899950787401882, 0.9965551180564724554 ) ) ;
#9346=CARTESIAN_POINT ( 'NONE',  ( -0.6971942568897626646, 0.07405724077823318263, 0.2411417322297011168 ) ) ;
#9347=CARTESIAN_POINT ( 'NONE',  ( 1.033464566929133799, 0.000000000000000000, 1.584645669291338654 ) ) ;
#9348=CARTESIAN_POINT ( 'NONE',  ( -0.8019270111902717657, 0.1787899950787401604, 1.771653543253322249 ) ) ;
#9349=CARTESIAN_POINT ( 'NONE',  ( -0.7646288533564489232, 0.1113553986120547346, 1.796259842519684957 ) ) ;
#9350=CARTESIAN_POINT ( 'NONE',  ( -0.8107537697050254399, -0.1574803149606297803, 0.9424212598425207865 ) ) ;
#9352=CARTESIAN_POINT ( 'NONE',  ( 1.054774247047244540, -0.07405724077823318263, 1.717519684985606476 ) ) ;
#9354=DIRECTION ( 'NONE',  ( -1.000000000000000000, 0.000000000000000000, 0.000000000000000000 ) ) ;
#9355=ORIENTED_EDGE ( 'NONE', *, *, #38409, .T. ) ;
#9356=CARTESIAN_POINT ( 'NONE',  ( -0.7495606340400177148, 0.1264236179284866091, 1.262303149552535420 ) ) ;
#9357=EDGE_LOOP ( 'NONE', ( #42900, #18936, #1403, #37679 ) ) ;
#9363=CARTESIAN_POINT ( 'NONE',  ( 0.6971942568897637749, 2.189545951927499583E-17, 0.3961614172690708924 ) ) ;
#9366=CARTESIAN_POINT ( 'NONE',  ( -1.033464566929134687, -0.06523048226347956391, 0.7849409447743628254 ) ) ;
#9369=CARTESIAN_POINT ( 'NONE',  ( 0.7495606340400177148, -0.1264236179284866091, 0.8735236219934803259 ) ) ;
#9372=DIRECTION ( 'NONE',  ( -1.000000000000000000, 0.000000000000000000, 0.000000000000000000 ) ) ;
#9373=CARTESIAN_POINT ( 'NONE',  ( 1.033464566929133799, 0.000000000000000000, 0.07874015737278799998 ) ) ;
#9374=ADVANCED_FACE ( 'NONE', ( #16598 ), #27650, .T. ) ;
#9381=CARTESIAN_POINT ( 'NONE',  ( 0.9500414927467378812, -0.1787899950787401604, 0.3346456692375748831 ) ) ;
#9383=CARTESIAN_POINT ( 'NONE',  ( -0.9500414927467378812, 0.1787899950787401604, 1.919291338528913871 ) ) ;
#9386=CARTESIAN_POINT ( 'NONE',  ( -0.8759842519685039353, 0.1787899950787401882, 1.414862204670645829 ) ) ;
#9387=CARTESIAN_POINT ( 'NONE',  ( 1.054774247047244540, 0.07405724077823318263, 1.446850393647023614 ) ) ;
#9390=CARTESIAN_POINT ( 'NONE',  ( -1.054774247047244096, 0.000000000000000000, 1.242618110182456714 ) ) ;
#9392=CARTESIAN_POINT ( 'NONE',  ( 1.054774247047244540, 0.07405724077823318263, 0.5413385826234012876 ) ) ;
#9393=CARTESIAN_POINT ( 'NONE',  ( -0.8019270111902716547, -0.1787899950787401604, 0.5610236219934807700 ) ) ;
#9396=CARTESIAN_POINT ( 'NONE',  ( -0.8759842519685039353, 0.000000000000000000, 0.000000000000000000 ) ) ;
#9397=ORIENTED_EDGE ( 'NONE', *, *, #34588, .T. ) ;
#9398=PRODUCT ( 'U-Bolt', 'U-Bolt', '', ( #33198 ) ) ;
#9401=CARTESIAN_POINT ( 'NONE',  ( -0.7185039370078739607, 1.928577636452523993E-17, 0.3051181102362204856 ) ) ;
#9402=CARTESIAN_POINT ( 'NONE',  ( 1.054774247047244096, 0.000000000000000000, 1.247539370024976391 ) ) ;
#9405=CARTESIAN_POINT ( 'NONE',  ( -0.8019270111902717657, -0.1787899950787401604, 0.9596456692375764375 ) ) ;
#9408=CARTESIAN_POINT ( 'NONE',  ( -0.8759842519685039353, 0.1574803149606299191, 1.387795275483023616 ) ) ;
#9411=VERTEX_POINT ( 'NONE', #16818 ) ;
#9412=CARTESIAN_POINT ( 'NONE',  ( 0.6971942568897648851, -0.07405724077823297447, 1.382874015694268044 ) ) ;
#9420=CARTESIAN_POINT ( 'NONE',  ( 0.8759842519685039353, 0.1787899950787401882, 1.646161417269070837 ) ) ;
#9426=EDGE_CURVE ( 'NONE', #32512, #37199, #19834, .T. ) ;
#9427=CARTESIAN_POINT ( 'NONE',  ( -0.9500414927467377701, 0.1787899950787401604, 0.7824803149068668695 ) ) ;
#9429=CARTESIAN_POINT ( 'NONE',  ( 0.9873396505805591694, 0.1113553986120547346, 0.08366141721530767628 ) ) ;
#9431=CARTESIAN_POINT ( 'NONE',  ( -0.8003469732030862316, -0.1545552040134573757, 1.986757990405105145 ) ) ;
#9434=CARTESIAN_POINT ( 'NONE',  ( 0.6971942568897648851, -0.07405724077823297447, 1.505905511757261284 ) ) ;
#9436=CARTESIAN_POINT ( 'NONE',  ( 1.002407869896990045, 0.1264236179284866091, 0.3420275590013546751 ) ) ;
#9438=LINE ( 'NONE', #19497, #11544 ) ;
#9439=ORIENTED_EDGE ( 'NONE', *, *, #44066, .T. ) ;
#9440=EDGE_CURVE ( 'NONE', #36149, #20507, #24737, .T. ) ;
#9445=CARTESIAN_POINT ( 'NONE',  ( 1.002407869896990045, -0.1264236179284866091, 0.4109251967966299213 ) ) ;
#9447=CARTESIAN_POINT ( 'NONE',  ( 0.7609004089021561557, -0.1193751119366993352, 0.03937007863495575050 ) ) ;
#9448=CARTESIAN_POINT ( 'NONE',  ( 1.054774247047244096, 0.000000000000000000, 1.321358267662771757 ) ) ;
#9449=CARTESIAN_POINT ( 'NONE',  ( 1.033464566929134687, 0.06523048226347956391, 1.970964566821606034 ) ) ;
#9450=CARTESIAN_POINT ( 'NONE',  ( -0.6971942568897637749, 2.189545951927499583E-17, 1.380413385773007873 ) ) ;
#9451=CARTESIAN_POINT ( 'NONE',  ( 1.033464566929133799, 0.000000000000000000, 0.7480314959554645871 ) ) ;
#9454=CARTESIAN_POINT ( 'NONE',  ( 0.7495606340400177148, -0.1264236179284866091, 0.9571850393163149340 ) ) ;
#9455=EDGE_LOOP ( 'NONE', ( #17080, #1314, #13723, #45795 ) ) ;
#9456=CARTESIAN_POINT ( 'NONE',  ( -0.8107537697050253289, 0.1574803149606300301, 0.6422244093412926569 ) ) ;
#9457=CARTESIAN_POINT ( 'NONE',  ( -0.7185039370078746268, -0.06523048226347956391, 1.370570866141733291 ) ) ;
#9458=CARTESIAN_POINT ( 'NONE',  ( -0.7185039370078739607, 1.928577636452523993E-17, 0.5314960628845992741 ) ) ;
#9461=CARTESIAN_POINT ( 'NONE',  ( 0.8019270111902716547, 0.1787899950787401604, 0.07874015742655143812 ) ) ;
#9462=CARTESIAN_POINT ( 'NONE',  ( -0.9500414927467377701, 0.1787899950787401604, 0.1082677164816695514 ) ) ;
#9463=CARTESIAN_POINT ( 'NONE',  ( 0.9412147342319837628, -0.1574803149606297803, 1.409940944774363825 ) ) ;
#9465=ORIENTED_EDGE ( 'NONE', *, *, #40868, .F. ) ;
#9468=ORIENTED_EDGE ( 'NONE', *, *, #11817, .T. ) ;
#9469=CARTESIAN_POINT ( 'NONE',  ( -0.6971942568897648851, 0.07405724077823318263, 1.653543307032850462 ) ) ;
#9472=CARTESIAN_POINT ( 'NONE',  ( -1.033464566929133799, 0.000000000000000000, 1.899606299212598604 ) ) ;
#9474=CARTESIAN_POINT ( 'NONE',  ( 1.033464566929133799, 1.928577636452524610E-17, 4.498031496062992574 ) ) ;
#9480=CARTESIAN_POINT ( 'NONE',  ( 0.7185039370078714072, 0.06523048226347728795, 1.749507873908221045 ) ) ;
#9481=CARTESIAN_POINT ( 'NONE',  ( -1.033464566929134687, -0.06523048226347956391, 0.4306102361129448552 ) ) ;
#9482=( BOUNDED_CURVE ( )  B_SPLINE_CURVE ( 2, ( #45724, #17223, #13178, #16986, #12712, #24191, #13404, #5951, #34749 ),
 .UNSPECIFIED., .F., .T. ) 
 B_SPLINE_CURVE_WITH_KNOTS ( ( 3, 2, 2, 2, 3 ),
 ( 0.6999999999999999556, 0.7025000000000000133, 0.7049999999999999600, 0.7075000000000000178, 0.7099999999999999645 ),
 .UNSPECIFIED. ) 
 CURVE ( )  GEOMETRIC_REPRESENTATION_ITEM ( )  RATIONAL_B_SPLINE_CURVE ( ( 1.000000000000000000, 0.9238795325112899581, 1.000000000000000000, 0.9238795325112869605, 1.000000000000000000, 0.9238795325112869605, 1.000000000000000000, 0.9238795325112869605, 1.000000000000000000 ) ) 
 REPRESENTATION_ITEM ( '' )  ) ;
#9483=CARTESIAN_POINT ( 'NONE',  ( 0.9412147342319837628, 0.1574803149606300301, 1.788877952755905332 ) ) ;
#9486=CARTESIAN_POINT ( 'NONE',  ( -1.054774247047244540, 0.07405724077823318263, 0.3838582676627718127 ) ) ;
#9488=CARTESIAN_POINT ( 'NONE',  ( 0.7495606340400177148, -0.1264236179284866091, 1.114665354276944909 ) ) ;
#9489=CARTESIAN_POINT ( 'NONE',  ( 0.8019270111902716547, 0.1787899950787401604, 1.412401574749386990 ) ) ;
#9490=CARTESIAN_POINT ( 'NONE',  ( 1.002407869896990045, 0.1264236179284866091, 0.1845472440407248116 ) ) ;
#9492=CARTESIAN_POINT ( 'NONE',  ( 0.8107537697050253289, -0.1574803149606297803, 1.493602362204724754 ) ) ;
#9494=CARTESIAN_POINT ( 'NONE',  ( -0.7185039370078739607, 1.928577636452523993E-17, 0.7381889763779527769 ) ) ;
#9496=( BOUNDED_CURVE ( )  B_SPLINE_CURVE ( 2, ( #46978, #43858, #31918, #21102, #42885, #3378, #47226, #40251, #35969 ),
 .UNSPECIFIED., .F., .T. ) 
 B_SPLINE_CURVE_WITH_KNOTS ( ( 3, 2, 2, 2, 3 ),
 ( 0.5699999999999999512, 0.5725000000000000089, 0.5749999999999999556, 0.5775000000000000133, 0.5799999999999999600 ),
 .UNSPECIFIED. ) 
 CURVE ( )  GEOMETRIC_REPRESENTATION_ITEM ( )  RATIONAL_B_SPLINE_CURVE ( ( 1.000000000000000000, 0.9238795325112899581, 1.000000000000000000, 0.9238795325112869605, 1.000000000000000000, 0.9238795325112869605, 1.000000000000000000, 0.9238795325112869605, 1.000000000000000000 ) ) 
 REPRESENTATION_ITEM ( '' )  ) ;
#9497=CARTESIAN_POINT ( 'NONE',  ( -0.8759842519685039353, 0.1574803149606299191, 1.555118110236220597 ) ) ;
#9498=CARTESIAN_POINT ( 'NONE',  ( 0.6971942568897648851, -0.07405724077823297447, 0.9891732282926936071 ) ) ;
#9499=CARTESIAN_POINT ( 'NONE',  ( 1.054774247047244096, 0.000000000000000000, 1.916830708607653477 ) ) ;
#9500=CARTESIAN_POINT ( 'NONE',  ( 0.7646288533564489232, -0.1113553986120547346, 0.3001968502861740440 ) ) ;
#9501=ORIENTED_EDGE ( 'NONE', *, *, #17469, .T. ) ;
#9504=CARTESIAN_POINT ( 'NONE',  ( -0.9412147342319837628, 0.1574803149606300301, 0.3223425195775121432 ) ) ;
#9506=CARTESIAN_POINT ( 'NONE',  ( 0.8019270111902717657, -0.1787899950787401604, 1.348425196796630976 ) ) ;
#9510=DIRECTION ( 'NONE',  ( 0.000000000000000000, 0.000000000000000000, -1.000000000000000000 ) ) ;
#9511=CARTESIAN_POINT ( 'NONE',  ( -0.7495606340400177148, 0.1264236179284866091, 0.6274606298674959559 ) ) ;
#9512=CARTESIAN_POINT ( 'NONE',  ( 0.7185039370078739607, 1.928577636452523993E-17, 0.2657480314960630197 ) ) ;
#9514=ORIENTED_EDGE ( 'NONE', *, *, #37383, .F. ) ;
#9515=ORIENTED_EDGE ( 'NONE', *, *, #5867, .F. ) ;
#9516=CARTESIAN_POINT ( 'NONE',  ( -0.8019270111902716547, 0.1787899950787401604, 1.333661417269071281 ) ) ;
#9518=CARTESIAN_POINT ( 'NONE',  ( -0.6971942568897626646, 0.07405724077823318263, 0.9891732282926934960 ) ) ;
#9519=CARTESIAN_POINT ( 'NONE',  ( -0.7646288533564489232, 0.1113553986120547346, 0.06397637795275590289 ) ) ;
#9521=CARTESIAN_POINT ( 'NONE',  ( -0.6971942568897626646, -0.07405724077823297447, 0.6003937007336389575 ) ) ;
#9522=EDGE_CURVE ( 'NONE', #10631, #955, #39422, .T. ) ;
#9530=LINE ( 'NONE', #30886, #30281 ) ;
#9531=CARTESIAN_POINT ( 'NONE',  ( -1.033464566929133799, 0.000000000000000000, 1.181102362097196989 ) ) ;
#9532=CARTESIAN_POINT ( 'NONE',  ( -0.6971942568897626646, 0.07405724077823318263, 0.6299212597887560161 ) ) ;
#9534=CONICAL_SURFACE ( 'NONE', #37054, 0.1574803149606299191, 1.047197551196598297 ) ;
#9535=EDGE_CURVE ( 'NONE', #22060, #40552, #13007, .T. ) ;
#9536=CARTESIAN_POINT ( 'NONE',  ( -0.8019270111902716547, 0.1787899950787401604, 1.692913385773008539 ) ) ;
#9537=CARTESIAN_POINT ( 'NONE',  ( 0.7185039370078739607, 0.000000000000000000, 4.498031496062992574 ) ) ;
#9538=EDGE_CURVE ( 'NONE', #9783, #43175, #20880, .T. ) ;
#9539=CARTESIAN_POINT ( 'NONE',  ( -1.033464566929133799, 0.000000000000000000, 1.427165354330708569 ) ) ;
#9541=CARTESIAN_POINT ( 'NONE',  ( 0.8107537697050253289, 0.1574803149606300301, 0.5733267716535435099 ) ) ;
#9544=CARTESIAN_POINT ( 'NONE',  ( -0.7185039370078746268, 0.06523048226347956391, 1.237696850286174044 ) ) ;
#9549=ORIENTED_EDGE ( 'NONE', *, *, #13640, .T. ) ;
#9552=CARTESIAN_POINT ( 'NONE',  ( 1.033464566929134687, 0.06523048226347956391, 1.075295275590550048 ) ) ;
#9555=CYLINDRICAL_SURFACE ( 'NONE', #44220, 0.1574803149606299191 ) ;
#9556=EDGE_CURVE ( 'NONE', #40732, #23920, #11599, .T. ) ;
#9558=CARTESIAN_POINT ( 'NONE',  ( 0.5314960629921260393, 0.000000000000000000, 4.842519685039370358 ) ) ;
#9560=AXIS2_PLACEMENT_3D ( 'NONE', #34298, #1669, #15609 ) ;
#9562=ORIENTED_EDGE ( 'NONE', *, *, #14466, .F. ) ;
#9565=CARTESIAN_POINT ( 'NONE',  ( 0.9873396505805591694, -0.1113553986120547346, 0.8710629921259842590 ) ) ;
#9566=CARTESIAN_POINT ( 'NONE',  ( 0.8759842519685039353, 0.1787899950787401882, 0.7800196849856062542 ) ) ;
#9567=CARTESIAN_POINT ( 'NONE',  ( 0.9873396505805591694, -0.1113553986120547346, 1.304133858267716661 ) ) ;
#9568=CARTESIAN_POINT ( 'NONE',  ( 0.7185039370078746268, -0.06523048226347956391, 0.6914370077664891978 ) ) ;
#9572=CARTESIAN_POINT ( 'NONE',  ( 0.8759842519685039353, -0.1574803149606299191, 1.249999999892472236 ) ) ;
#9574=ORIENTED_EDGE ( 'NONE', *, *, #8812, .T. ) ;
#9575=CARTESIAN_POINT ( 'NONE',  ( -0.6971942568897648851, 0.07405724077823318263, 1.973425196796630088 ) ) ;
#9576=CARTESIAN_POINT ( 'NONE',  ( 1.002407869896990045, -0.1264236179284866091, 1.872539370024976391 ) ) ;
#9578=CARTESIAN_POINT ( 'NONE',  ( 0.8107537697050254399, -0.1574803149606297803, 0.5487204724409447953 ) ) ;
#9579=CARTESIAN_POINT ( 'NONE',  ( -0.9500414927467378812, -0.1787899950787401604, 1.510826771599780294 ) ) ;
#9581=CARTESIAN_POINT ( 'NONE',  ( -1.002407869896990045, -0.1264236179284866091, 0.9621062991588346103 ) ) ;
#9582=CARTESIAN_POINT ( 'NONE',  ( -0.8019270111902717657, 0.1787899950787401604, 0.2755905511273391006 ) ) ;
#9583=CARTESIAN_POINT ( 'NONE',  ( 0.9412147342319837628, -0.1574803149606297803, 1.577263779527559917 ) ) ;
#9584=CARTESIAN_POINT ( 'NONE',  ( -1.054774247047244096, 0.000000000000000000, 1.838090551127338657 ) ) ;
#9586=CARTESIAN_POINT ( 'NONE',  ( -0.8759842519685039353, 0.1574803149606299191, 1.751968503937007871 ) ) ;
#9591=DIRECTION ( 'NONE',  ( 1.822029033848725028E-16, 0.000000000000000000, 1.000000000000000000 ) ) ;
#9592=AXIS2_PLACEMENT_3D ( 'NONE', #3354, #17731, #47207 ) ;
#9596=CARTESIAN_POINT ( 'NONE',  ( -1.002407869896990045, -0.1264236179284866091, 1.242618110182456714 ) ) ;
#9601=CARTESIAN_POINT ( 'NONE',  ( 1.054774247047244540, 0.07405724077823318263, 0.4183070865604097133 ) ) ;
#9604=CARTESIAN_POINT ( 'NONE',  ( -1.033464566929134687, -0.06523048226347956391, 0.7160433070866151217 ) ) ;
#9606=CARTESIAN_POINT ( 'NONE',  ( -1.044119406988188947, 0.000000000000000000, 1.984498031469181134 ) ) ;
#9608=CARTESIAN_POINT ( 'NONE',  ( 1.054774247047244096, 0.000000000000000000, 0.8882874015210394658 ) ) ;
#9610=EDGE_CURVE ( 'NONE', #35682, #43583, #26307, .T. ) ;
#9613=CARTESIAN_POINT ( 'NONE',  ( 0.9500414927467378812, 0.1787899950787401604, 1.924212598371433325 ) ) ;
#9614=CARTESIAN_POINT ( 'NONE',  ( 1.033464566929133799, 0.000000000000000000, 0.7086614172153071767 ) ) ;
#9618=CARTESIAN_POINT ( 'NONE',  ( -0.8019270111902717657, -0.1787899950787401604, 1.899606299158834943 ) ) ;
#9619=VERTEX_POINT ( 'NONE', #8436 ) ;
#9620=VECTOR ( 'NONE', #45449, 39.37007874015748143 ) ;
#9621=CARTESIAN_POINT ( 'NONE',  ( -0.6971942568897648851, -0.07405724077823297447, 1.427165354276944687 ) ) ;
#9622=CARTESIAN_POINT ( 'NONE',  ( 0.6971942568897648851, 0.07405724077823318263, 1.343503936954111744 ) ) ;
#9623=AXIS2_PLACEMENT_3D ( 'NONE', #46288, #16605, #20183 ) ;
#9626=CARTESIAN_POINT ( 'NONE',  ( -0.8019270111902717657, 0.1787899950787401604, 0.5905511810485987167 ) ) ;
#9629=CARTESIAN_POINT ( 'NONE',  ( 0.9500414927467377701, -0.1787899950787401604, 0.6889763778989936860 ) ) ;
#9630=CARTESIAN_POINT ( 'NONE',  ( -0.8019270111902716547, -0.1787899950787401604, 0.6003937007336380693 ) ) ;
#9632=DIRECTION ( 'NONE',  ( 1.000000000000000000, 0.000000000000000000, 0.000000000000000000 ) ) ;
#9635=CARTESIAN_POINT ( 'NONE',  ( -0.7646288533564489232, -0.1113553986120547346, 0.3494094488188976277 ) ) ;
#9636=CARTESIAN_POINT ( 'NONE',  ( 0.9500414927467377701, 0.1787899950787401604, 1.333661417269071281 ) ) ;
#9640=CARTESIAN_POINT ( 'NONE',  ( -1.002407869896990045, 0.1264236179284866091, 0.9768700786863937502 ) ) ;
#9644=CARTESIAN_POINT ( 'NONE',  ( 1.033464566929133799, 0.000000000000000000, 0.9940944881889764995 ) ) ;
#9653=CARTESIAN_POINT ( 'NONE',  ( 0.7185039370078739607, 1.928577636452523993E-17, 1.879921259842519676 ) ) ;
#9654=CARTESIAN_POINT ( 'NONE',  ( 1.033464566929133799, 0.000000000000000000, 1.732283464459401623 ) ) ;
#9660=CARTESIAN_POINT ( 'NONE',  ( 0.7495606340400177148, -0.1264236179284866091, 0.5191929133320630774 ) ) ;
#9661=CARTESIAN_POINT ( 'NONE',  ( -0.8759842519685039353, -0.1787899950787401882, 0.8833661416785196785 ) ) ;
#9662=CARTESIAN_POINT ( 'NONE',  ( -0.9873396505805591694, -0.1113553986120547346, 1.294291338475149544 ) ) ;
#9666=CARTESIAN_POINT ( 'NONE',  ( -0.8102569175943972191, -0.1593853870594618694, 1.986963696465253726 ) ) ;
#9668=CARTESIAN_POINT ( 'NONE',  ( 1.002407869896990045, -0.1264236179284866091, 1.478838582623401399 ) ) ;
#9671=CARTESIAN_POINT ( 'NONE',  ( 0.6971942568897648851, -0.07405724077823297447, 0.3986220471903311746 ) ) ;
#9672=ORIENTED_EDGE ( 'NONE', *, *, #27582, .F. ) ;
#9674=CARTESIAN_POINT ( 'NONE',  ( 0.7185039370078760701, -0.06523048226348075740, 0.8489173227271181732 ) ) ;
#9678=CARTESIAN_POINT ( 'NONE',  ( 0.7495606340400177148, 0.1264236179284866091, 0.4699803149068661479 ) ) ;
#9680=CYLINDRICAL_SURFACE ( 'NONE', #26153, 0.1574803149606299191 ) ;
#9682=CARTESIAN_POINT ( 'NONE',  ( -0.8759842519685039353, -0.1787899950787401882, 1.468996062938362046 ) ) ;
#9684=CARTESIAN_POINT ( 'NONE',  ( 0.8019270111902717657, -0.1787899950787401604, 0.9596456692375764375 ) ) ;
#9685=ORIENTED_EDGE ( 'NONE', *, *, #34425, .F. ) ;
#9687=CARTESIAN_POINT ( 'NONE',  ( -0.8759842519685039353, 0.1574803149606299191, 0.5216535431995598104 ) ) ;
#9689=AXIS2_PLACEMENT_3D ( 'NONE', #5127, #15950, #9208 ) ;
#9690=CARTESIAN_POINT ( 'NONE',  ( -1.054774247047244540, -0.07405724077823318263, 0.9645669290800953366 ) ) ;
#9691=CARTESIAN_POINT ( 'NONE',  ( -0.8107537697050254399, 0.1574803149606300301, 0.5241141731208195376 ) ) ;
#9693=CARTESIAN_POINT ( 'NONE',  ( 0.9500414927467377701, 0.1787899950787401604, 0.1919291338045042705 ) ) ;
#9694=CARTESIAN_POINT ( 'NONE',  ( 0.9873396505805591694, 0.1113553986120547346, 1.461614173120818760 ) ) ;
#9697=CYLINDRICAL_SURFACE ( 'NONE', #33664, 0.1574803149606299191 ) ;
#9699=CARTESIAN_POINT ( 'NONE',  ( -0.8759842519685039353, 0.1787899950787401882, 1.685531496009228469 ) ) ;
#9702=EDGE_CURVE ( 'NONE', #3252, #29740, #31199, .T. ) ;
#9704=CARTESIAN_POINT ( 'NONE',  ( -0.9412147342319837628, 0.1574803149606300301, 0.6471456692913394315 ) ) ;
#9715=CARTESIAN_POINT ( 'NONE',  ( 0.9873396505805591694, -0.1113553986120547346, 1.815944881889763884 ) ) ;
#9717=CARTESIAN_POINT ( 'NONE',  ( -0.8759842519685039353, -0.1787899950787401882, 0.2928149605761578567 ) ) ;
#9718=CARTESIAN_POINT ( 'NONE',  ( -0.7185039370078739607, 1.928577636452523993E-17, 0.9744094488188976833 ) ) ;
#9721=CARTESIAN_POINT ( 'NONE',  ( 0.6971942568897648851, -0.07405724077823297447, 1.151574803095843036 ) ) ;
#9722=CARTESIAN_POINT ( 'NONE',  ( 0.7495606340400177148, 0.1264236179284866091, 1.454232283410803017 ) ) ;
#9723=CARTESIAN_POINT ( 'NONE',  ( 0.6971942568897626646, -0.07405724077823297447, 0.2411417322297010890 ) ) ;
#9727=LINE ( 'NONE', #24116, #21300 ) ;
#9728=CARTESIAN_POINT ( 'NONE',  ( -0.8107537697050254399, -0.1574803149606297803, 0.6963582676090083190 ) ) ;
#9729=CARTESIAN_POINT ( 'NONE',  ( 0.8019270111902716547, -0.1787899950787401604, 1.072834645615528659 ) ) ;
#9730=CARTESIAN_POINT ( 'NONE',  ( 0.7495606340400177148, -0.1264236179284866091, 1.941437007820252081 ) ) ;
#9731=CARTESIAN_POINT ( 'NONE',  ( 0.8759842519685039353, 0.1574803149606299191, 0.4035433069790866356 ) ) ;
#9732=ORIENTED_EDGE ( 'NONE', *, *, #46737, .T. ) ;
#9734=ORIENTED_EDGE ( 'NONE', *, *, #15700, .T. ) ;
#9735=CARTESIAN_POINT ( 'NONE',  ( -0.9873396505805591694, -0.1113553986120547346, 0.2312992124908980207 ) ) ;
#9737=CARTESIAN_POINT ( 'NONE',  ( 0.9500414927467378812, 0.1787899950787401604, 1.368110236166710125 ) ) ;
#9742=VECTOR ( 'NONE', #34745, 39.37007874015748143 ) ;
#9743=CARTESIAN_POINT ( 'NONE',  ( -0.8107537697050254399, 0.1574803149606300301, 1.872539370078740495 ) ) ;
#9747=ORIENTED_EDGE ( 'NONE', *, *, #4094, .T. ) ;
#9748=CARTESIAN_POINT ( 'NONE',  ( -0.8019270111902716547, -0.1787899950787401604, 1.387795275536786610 ) ) ;
#9749=EDGE_CURVE ( 'NONE', #7257, #5433, #43761, .T. ) ;
#9751=CARTESIAN_POINT ( 'NONE',  ( -0.6971942568897626646, 0.07405724077823318263, 0.9498031495525356416 ) ) ;
#9752=CARTESIAN_POINT ( 'NONE',  ( -1.033464566929133799, 0.000000000000000000, 0.009842519685039369942 ) ) ;
#9753=ORIENTED_EDGE ( 'NONE', *, *, #7218, .F. ) ;
#9754=CARTESIAN_POINT ( 'NONE',  ( -0.6971942568897648851, -0.07405724077823297447, 0.9891732282926936071 ) ) ;
#9755=CARTESIAN_POINT ( 'NONE',  ( -1.054774247047244540, -0.07405724077823318263, 0.6151574802611974313 ) ) ;
#9756=( BOUNDED_CURVE ( )  B_SPLINE_CURVE ( 2, ( #27490, #15504, #4681, #41088, #5163, #5394, #42041, #23398, #38002 ),
 .UNSPECIFIED., .F., .T. ) 
 B_SPLINE_CURVE_WITH_KNOTS ( ( 3, 2, 2, 2, 3 ),
 ( 0.2000000000000000111, 0.2025000000000000133, 0.2049999999999999878, 0.2074999999999999900, 0.2099999999999999922 ),
 .UNSPECIFIED. ) 
 CURVE ( )  GEOMETRIC_REPRESENTATION_ITEM ( )  RATIONAL_B_SPLINE_CURVE ( ( 1.000000000000000000, 0.9238795325112869605, 1.000000000000000000, 0.9238795325112869605, 1.000000000000000000, 0.9238795325112869605, 1.000000000000000000, 0.9238795325112869605, 1.000000000000000000 ) ) 
 REPRESENTATION_ITEM ( '' )  ) ;
#9765=CARTESIAN_POINT ( 'NONE',  ( -0.7185039370078739607, 1.928577636452523993E-17, 0.3346456691838114450 ) ) ;
#9766=EDGE_CURVE ( 'NONE', #5874, #15306, #1210, .T. ) ;
#9768=CARTESIAN_POINT ( 'NONE',  ( -1.054774247047244540, -0.07405724077823318263, 0.6889763778989935750 ) ) ;
#9770=CARTESIAN_POINT ( 'NONE',  ( -1.002407869896990045, 0.1264236179284866091, 1.724901574749385880 ) ) ;
#9772=VECTOR ( 'NONE', #7784, 39.37007874015748143 ) ;
#9773=( BOUNDED_CURVE ( )  B_SPLINE_CURVE ( 2, ( #44233, #26304, #33023, #40400, #18147, #32790, #15042, #47385, #14557 ),
 .UNSPECIFIED., .F., .F. ) 
 B_SPLINE_CURVE_WITH_KNOTS ( ( 3, 2, 2, 2, 3 ),
 ( 0.7700000000000000178, 0.7724999999999999645, 0.7750000000000000222, 0.7774999999999999689, 0.7800000000000000266 ),
 .UNSPECIFIED. ) 
 CURVE ( )  GEOMETRIC_REPRESENTATION_ITEM ( )  RATIONAL_B_SPLINE_CURVE ( ( 1.000000000000000000, 0.9238795325112899581, 1.000000000000000000, 0.9238795325112869605, 1.000000000000000000, 0.9238795325112869605, 1.000000000000000000, 0.9238795325112869605, 1.000000000000000000 ) ) 
 REPRESENTATION_ITEM ( '' )  ) ;
#9774=CARTESIAN_POINT ( 'NONE',  ( -1.033464566929134687, 0.06523048226347956391, 0.1205708660342053040 ) ) ;
#9775=CARTESIAN_POINT ( 'NONE',  ( 0.8759842519685039353, -0.1574803149606299191, 0.5511811023622047445 ) ) ;
#9778=( BOUNDED_CURVE ( )  B_SPLINE_CURVE ( 2, ( #24341, #39398, #16684, #21194, #2974, #43234, #13102, #5650, #2049 ),
 .UNSPECIFIED., .F., .T. ) 
 B_SPLINE_CURVE_WITH_KNOTS ( ( 3, 2, 2, 2, 3 ),
 ( 0.7099999999999999645, 0.7125000000000000222, 0.7149999999999999689, 0.7175000000000000266, 0.7199999999999999734 ),
 .UNSPECIFIED. ) 
 CURVE ( )  GEOMETRIC_REPRESENTATION_ITEM ( )  RATIONAL_B_SPLINE_CURVE ( ( 1.000000000000000000, 0.9238795325112939549, 1.000000000000000000, 0.9238795325112869605, 1.000000000000000000, 0.9238795325112869605, 1.000000000000000000, 0.9238795325112869605, 1.000000000000000000 ) ) 
 REPRESENTATION_ITEM ( '' )  ) ;
#9779=CARTESIAN_POINT ( 'NONE',  ( -0.8759842519685039353, -0.1574803149606299191, 1.249999999892472236 ) ) ;
#9783=VERTEX_POINT ( 'NONE', #7346 ) ;
#9784=CARTESIAN_POINT ( 'NONE',  ( 1.033464566929133799, 0.000000000000000000, 1.387795275590551158 ) ) ;
#9785=CARTESIAN_POINT ( 'NONE',  ( 0.8759842519685039353, 0.1574803149606299191, 1.279527559055118280 ) ) ;
#9789=ADVANCED_FACE ( 'NONE', ( #15899 ), #37687, .T. ) ;
#9791=CARTESIAN_POINT ( 'NONE',  ( 1.033464566929133799, 0.000000000000000000, 1.692913385719244213 ) ) ;
#9794=LINE ( 'NONE', #28022, #12413 ) ;
#9798=CARTESIAN_POINT ( 'NONE',  ( 0.6971942568897626646, -0.07405724077823297447, 0.8710629920722218200 ) ) ;
#9805=CARTESIAN_POINT ( 'NONE',  ( 0.8759842519685039353, -0.1574803149606299191, 1.289370078632629868 ) ) ;
#9808=CARTESIAN_POINT ( 'NONE',  ( -0.8759842519685039353, 0.1787899950787401882, 1.847933070812378009 ) ) ;
#9809=CARTESIAN_POINT ( 'NONE',  ( -0.7185039370078746268, -0.06523048226347956391, 0.8095472439869610959 ) ) ;
#9811=CARTESIAN_POINT ( 'NONE',  ( -0.9412147342319837628, 0.1574803149606300301, 0.4798228345381422288 ) ) ;
#9812=CARTESIAN_POINT ( 'NONE',  ( -1.054774247047244540, 0.07405724077823318263, 1.520669291284818758 ) ) ;
#9815=CARTESIAN_POINT ( 'NONE',  ( -0.6971942568897648851, -0.07405724077823297447, 1.028543307032851795 ) ) ;
#9818=CARTESIAN_POINT ( 'NONE',  ( -0.9500414927467378812, -0.1787899950787401604, 0.2952755904974176393 ) ) ;
#9821=CARTESIAN_POINT ( 'NONE',  ( -1.054774247047244096, 0.000000000000000000, 1.916830708607653477 ) ) ;
#9822=CARTESIAN_POINT ( 'NONE',  ( 0.9412147342319837628, -0.1574803149606297803, 1.409940944774363603 ) ) ;
#9823=CARTESIAN_POINT ( 'NONE',  ( -0.7185039370078746268, -0.06523048226347956391, 1.921751968503937480 ) ) ;
#9828=EDGE_CURVE ( 'NONE', #38514, #18242, #23912, .T. ) ;
#9835=CARTESIAN_POINT ( 'NONE',  ( -0.9873396505805591694, -0.1113553986120547346, 0.2411417322834645827 ) ) ;
#9836=CARTESIAN_POINT ( 'NONE',  ( -0.7646288533564489232, 0.1113553986120547346, 0.8415354329633386588 ) ) ;
#9838=CARTESIAN_POINT ( 'NONE',  ( 0.8759842519685039353, -0.1787899950787401882, 0.8784448818360000022 ) ) ;
#9841=CARTESIAN_POINT ( 'NONE',  ( -0.7185039370078746268, 0.06523048226347956391, 1.247539370078740273 ) ) ;
#9844=CARTESIAN_POINT ( 'NONE',  ( 1.033464566929134687, -0.06523048226347956391, 0.1943897636720004762 ) ) ;
#9846=CARTESIAN_POINT ( 'NONE',  ( 1.033464566929134687, -0.06523048226347956391, 0.3912401573727880555 ) ) ;
#9849=CARTESIAN_POINT ( 'NONE',  ( 0.9500414927467378812, -0.1787899950787401604, 0.3740157479777325711 ) ) ;
#9850=CARTESIAN_POINT ( 'NONE',  ( -1.002407869896990045, -0.1264236179284866091, 1.906988188922614125 ) ) ;
#9851=VERTEX_POINT ( 'NONE', #26122 ) ;
#9853=CARTESIAN_POINT ( 'NONE',  ( -1.054774247047244096, 0.000000000000000000, 1.483759842465921075 ) ) ;
#9855=CARTESIAN_POINT ( 'NONE',  ( 0.8759842519685039353, -0.1787899950787401882, 1.592027559001354398 ) ) ;
#9858=CARTESIAN_POINT ( 'NONE',  ( -0.8759842519685039353, -0.1787899950787401882, 0.6865157479777322935 ) ) ;
#9859=CARTESIAN_POINT ( 'NONE',  ( 0.8759842519685039353, -0.1787899950787401882, 0.1747047243556852092 ) ) ;
#9861=CARTESIAN_POINT ( 'NONE',  ( 0.9500414927467377701, 0.1787899950787401604, 0.5462598424659214080 ) ) ;
#9862=CARTESIAN_POINT ( 'NONE',  ( -0.6971942568897637749, 2.189545951927499583E-17, 0.5930118109698583329 ) ) ;
#9863=CYLINDRICAL_SURFACE ( 'NONE', #42946, 0.1574803149606299191 ) ;
#9868=CARTESIAN_POINT ( 'NONE',  ( -0.9500414927467378812, 0.1787899950787401604, 1.451771653489543290 ) ) ;
#9870=CARTESIAN_POINT ( 'NONE',  ( -0.8107537697050253289, -0.1574803149606297803, 0.4306102362204725642 ) ) ;
#9871=CARTESIAN_POINT ( 'NONE',  ( 0.9500414927467377701, 0.1787899950787401604, 1.373031496009229357 ) ) ;
#9874=DIRECTION ( 'NONE',  ( 1.822029033848725028E-16, 0.000000000000000000, 1.000000000000000000 ) ) ;
#9875=VECTOR ( 'NONE', #36098, 39.37007874015748143 ) ;
#9880=CARTESIAN_POINT ( 'NONE',  ( 0.7185039370078739607, 1.928577636452523993E-17, 0.8169291338582678197 ) ) ;
#9883=( BOUNDED_CURVE ( )  B_SPLINE_CURVE ( 2, ( #7238, #3639, #14201, #21858, #36485, #6275, #22554, #37400, #43886 ),
 .UNSPECIFIED., .F., .T. ) 
 B_SPLINE_CURVE_WITH_KNOTS ( ( 3, 2, 2, 2, 3 ),
 ( 0.5600000000000000533, 0.5625000000000000000, 0.5649999999999999467, 0.5675000000000000044, 0.5699999999999999512 ),
 .UNSPECIFIED. ) 
 CURVE ( )  GEOMETRIC_REPRESENTATION_ITEM ( )  RATIONAL_B_SPLINE_CURVE ( ( 1.000000000000000000, 0.9238795325112869605, 1.000000000000000000, 0.9238795325112869605, 1.000000000000000000, 0.9238795325112869605, 1.000000000000000000, 0.9238795325112829637, 1.000000000000000000 ) ) 
 REPRESENTATION_ITEM ( '' )  ) ;
#9886=CARTESIAN_POINT ( 'NONE',  ( 1.054774247047244096, 0.000000000000000000, 0.2977362204186775885 ) ) ;
#9890=FACE_OUTER_BOUND ( 'NONE', #21294, .T. ) ;
#9891=CARTESIAN_POINT ( 'NONE',  ( 0.6971942568897626646, -0.07405724077823297447, 0.4773622046706456068 ) ) ;
#9892=CARTESIAN_POINT ( 'NONE',  ( -1.054774247047244540, -0.07405724077823318263, 0.7726377952218266287 ) ) ;
#9896=CARTESIAN_POINT ( 'NONE',  ( -0.7701193937251510357, -0.1341754852037822243, 1.986078545504829984 ) ) ;
#9898=CARTESIAN_POINT ( 'NONE',  ( 0.8019270111902717657, -0.1787899950787401604, 1.668307086560410157 ) ) ;
#9899=CARTESIAN_POINT ( 'NONE',  ( 0.6971942568897648851, -0.07405724077823297447, 1.934055118056471567 ) ) ;
#9900=LINE ( 'NONE', #43410, #3250 ) ;
#9901=CARTESIAN_POINT ( 'NONE',  ( 1.054774247047244540, -0.07405724077823318263, 0.4133858267178901480 ) ) ;
#9909=CARTESIAN_POINT ( 'NONE',  ( 0.7495606340400177148, -0.1264236179284866091, 0.5979330708123780092 ) ) ;
#9910=CARTESIAN_POINT ( 'NONE',  ( 0.7704837865233213900, -0.1271003095796768290, 0.03936944523697429726 ) ) ;
#9912=CARTESIAN_POINT ( 'NONE',  ( -0.8759842519685039353, -0.1787899950787401882, 1.429625984198204858 ) ) ;
#9913=ORIENTED_EDGE ( 'NONE', *, *, #34116, .T. ) ;
#9917=CARTESIAN_POINT ( 'NONE',  ( 1.054774247047244540, -0.07405724077823318263, 1.048228346402930944 ) ) ;
#9919=CARTESIAN_POINT ( 'NONE',  ( -0.9412147342319837628, 0.1574803149606300301, 0.6766732282389293918 ) ) ;
#9921=CARTESIAN_POINT ( 'NONE',  ( 0.6971942568897648851, -0.07405724077823297447, 1.855314960576157635 ) ) ;
#9922=CARTESIAN_POINT ( 'NONE',  ( -0.8759842519685039353, -0.1574803149606299191, 1.456692913385826849 ) ) ;
#9923=CARTESIAN_POINT ( 'NONE',  ( -0.8019270111902717657, 0.1787899950787401604, 0.8218503936470251681 ) ) ;
#9925=CARTESIAN_POINT ( 'NONE',  ( -0.8081549416023995347, -0.1479449179857115215, 0.03937007874015843734 ) ) ;
#9926=CARTESIAN_POINT ( 'NONE',  ( 0.8019270111902716547, -0.1787899950787401604, 0.09350393695411057804 ) ) ;
#9927=CARTESIAN_POINT ( 'NONE',  ( -0.8759842519685039353, 0.1787899950787401882, 0.1500984251430870220 ) ) ;
#9928=EDGE_CURVE ( 'NONE', #6940, #40417, #30646, .T. ) ;
#9929=CARTESIAN_POINT ( 'NONE',  ( 0.7185039370078746268, 0.06523048226347956391, 1.513287401467275917 ) ) ;
#9933=CARTESIAN_POINT ( 'NONE',  ( -0.9500414927467377701, 0.1787899950787401604, 1.643700787347811998 ) ) ;
#9943=CARTESIAN_POINT ( 'NONE',  ( 1.033464566929134687, -0.06523048226347956391, 1.857775590551181244 ) ) ;
#9947=CARTESIAN_POINT ( 'NONE',  ( -1.002407869896990045, 0.1264236179284866091, 0.3469488188438744070 ) ) ;
#9950=CARTESIAN_POINT ( 'NONE',  ( 0.8019270111902717657, 0.1787899950787401604, 1.102362204670646495 ) ) ;
#9951=CARTESIAN_POINT ( 'NONE',  ( 0.8759842519685039353, -0.1787899950787401882, 1.547736220418677089 ) ) ;
#9952=FACE_OUTER_BOUND ( 'NONE', #13689, .T. ) ;
#9953=EDGE_CURVE ( 'NONE', #815, #45828, #29130, .T. ) ;
#9954=CARTESIAN_POINT ( 'NONE',  ( 0.9412147342319837628, -0.1574803149606297803, 1.695374015748031482 ) ) ;
#9955=CARTESIAN_POINT ( 'NONE',  ( 0.7612901950597569245, 0.1140645495863889802, 1.980815085937517317 ) ) ;
#9956=CARTESIAN_POINT ( 'NONE',  ( 0.7185039370078766252, -0.06523048226348168721, 1.518208661309796481 ) ) ;
#9958=CARTESIAN_POINT ( 'NONE',  ( -1.033464566929133799, 0.000000000000000000, 1.732283464459401623 ) ) ;
#9959=CARTESIAN_POINT ( 'NONE',  ( 1.054774247047244540, 0.07405724077823318263, 0.1820866141194649179 ) ) ;
#9961=CARTESIAN_POINT ( 'NONE',  ( -0.9412147342319837628, -0.1574803149606297803, 0.7012795274515276622 ) ) ;
#9962=CARTESIAN_POINT ( 'NONE',  ( 0.7495606340400177148, -0.1264236179284866091, 1.109744094434425232 ) ) ;
#9963=CYLINDRICAL_SURFACE ( 'NONE', #7018, 0.1574803149606299191 ) ;
#9965=CARTESIAN_POINT ( 'NONE',  ( -1.033464566929133799, 0.000000000000000000, 0.1574803148531029595 ) ) ;
#9966=CARTESIAN_POINT ( 'NONE',  ( 0.7185039370078746268, -0.06523048226347956391, 0.4945866140657015353 ) ) ;
#9968=CARTESIAN_POINT ( 'NONE',  ( -0.9873396505805591694, 0.1113553986120547346, 1.117125984251968518 ) ) ;
#9970=CARTESIAN_POINT ( 'NONE',  ( -0.8107537697050234415, -0.1574803149606297803, 0.3420275589475912925 ) ) ;
#9972=CARTESIAN_POINT ( 'NONE',  ( 0.8759842519685039353, 0.1787899950787401882, 1.331200787347811110 ) ) ;
#9973=EDGE_CURVE ( 'NONE', #38897, #13902, #35803, .T. ) ;
#9977=CARTESIAN_POINT ( 'NONE',  ( -0.8759842519685039353, 0.000000000000000000, 0.000000000000000000 ) ) ;
#9978=CARTESIAN_POINT ( 'NONE',  ( 1.033464566929133799, 0.000000000000000000, 0.5216535433070865757 ) ) ;
#9980=CARTESIAN_POINT ( 'NONE',  ( 1.002407869896990045, -0.1264236179284866091, 0.4158464566391496531 ) ) ;
#9982=CARTESIAN_POINT ( 'NONE',  ( -0.6971942568897648851, -0.07405724077823297447, 1.422244094434425898 ) ) ;
#9985=CARTESIAN_POINT ( 'NONE',  ( -0.7495606340400177148, -0.1264236179284866091, 1.897145669237574772 ) ) ;
#9987=CARTESIAN_POINT ( 'NONE',  ( -0.8759842519685039353, 0.1787899950787401882, 1.134350393647023614 ) ) ;
#9988=CARTESIAN_POINT ( 'NONE',  ( -0.8019270111902717657, -0.1787899950787401604, 0.6840551180564720113 ) ) ;
#9994=EDGE_LOOP ( 'NONE', ( #40118, #33466, #32292, #46814, #13595 ) ) ;
#9996=CARTESIAN_POINT ( 'NONE',  ( -0.9873396505805591694, 0.1113553986120547346, 0.5561023620971968784 ) ) ;
#9997=CARTESIAN_POINT ( 'NONE',  ( -1.054774247047244540, -0.07405724077823318263, 0.5708661416785201226 ) ) ;
#10000=CARTESIAN_POINT ( 'NONE',  ( -1.002407869896990045, 0.1264236179284866091, 1.685531496009228469 ) ) ;
#10001=VECTOR ( 'NONE', #5106, 39.37007874015748143 ) ;
#10004=ORIENTED_EDGE ( 'NONE', *, *, #45038, .T. ) ;
#10005=CARTESIAN_POINT ( 'NONE',  ( 0.7185039370078739607, 1.928577636452523993E-17, 0.5807086614173228023 ) ) ;
#10007=CARTESIAN_POINT ( 'NONE',  ( -0.8107537697050254399, 0.1574803149606300301, 0.9670275590551187239 ) ) ;
#10008=CARTESIAN_POINT ( 'NONE',  ( -0.8107537697050253289, -0.1574803149606297803, 1.405019684931842816 ) ) ;
#10009=CARTESIAN_POINT ( 'NONE',  ( 0.7495606340400177148, -0.1264236179284866091, 0.6422244093950550958 ) ) ;
#10013=CARTESIAN_POINT ( 'NONE',  ( 0.8759842519685039353, 0.1574803149606299191, 1.200787401574803237 ) ) ;
#10014=CARTESIAN_POINT ( 'NONE',  ( 0.7185039370078739607, 1.928577636452523993E-17, 1.830708661309795149 ) ) ;
#10016=EDGE_CURVE ( 'NONE', #22696, #29244, #19626, .T. ) ;
#10017=CARTESIAN_POINT ( 'NONE',  ( 1.002407869896990045, -0.1264236179284866091, 0.6077755904974173617 ) ) ;
#10020=CARTESIAN_POINT ( 'NONE',  ( 0.8759842519685039353, 0.1574803149606299191, 1.555118110236220597 ) ) ;
#10023=CARTESIAN_POINT ( 'NONE',  ( 0.6971942568897637749, 2.189545951927499583E-17, 0.7504921259304880854 ) ) ;
#10025=FACE_OUTER_BOUND ( 'NONE', #46277, .T. ) ;
#10026=CARTESIAN_POINT ( 'NONE',  ( -0.9412147342319837628, 0.1574803149606300301, 0.5290354330708663122 ) ) ;
#10030=CARTESIAN_POINT ( 'NONE',  ( 1.033464566929134687, 0.06523048226347956391, 1.262303149498772425 ) ) ;
#10034=CARTESIAN_POINT ( 'NONE',  ( -0.7495606340400177148, 0.1264236179284866091, 1.892224409395055096 ) ) ;
#10036=ORIENTED_EDGE ( 'NONE', *, *, #8331, .F. ) ;
#10038=CARTESIAN_POINT ( 'NONE',  ( -0.7495606340400177148, -0.1264236179284866091, 1.941437007820252081 ) ) ;
#10040=CARTESIAN_POINT ( 'NONE',  ( -0.7495606340400177148, 0.1264236179284866091, 1.532972440891118060 ) ) ;
#10042=CARTESIAN_POINT ( 'NONE',  ( -0.8759842519685039353, 0.1787899950787401882, 1.016240157426551161 ) ) ;
#10044=CARTESIAN_POINT ( 'NONE',  ( -0.8019270111902717657, -0.1787899950787401604, 0.1722440944344256208 ) ) ;
#10046=CARTESIAN_POINT ( 'NONE',  ( -1.002407869896990045, 0.1264236179284866091, 1.843011810969858333 ) ) ;
#10054=CARTESIAN_POINT ( 'NONE',  ( -0.6971942568897626646, 0.07405724077823318263, 0.1968503936470238913 ) ) ;
#10056=CARTESIAN_POINT ( 'NONE',  ( -0.6971942568897637749, 2.189545951927499583E-17, 1.267224409395055096 ) ) ;
#10061=CARTESIAN_POINT ( 'NONE',  ( -0.7185039370078746268, 0.06523048226347956391, 0.9621062991050720603 ) ) ;
#10062=CARTESIAN_POINT ( 'NONE',  ( -0.7185039370078739607, 1.928577636452523993E-17, 0.6988188976377952555 ) ) ;
#10066=CARTESIAN_POINT ( 'NONE',  ( 0.9873396505805591694, 0.1113553986120547346, 1.855314960522393530 ) ) ;
#10067=CARTESIAN_POINT ( 'NONE',  ( 0.8107537697050253289, 0.1574803149606300301, 0.7308070866141725963 ) ) ;
#10068=AXIS2_PLACEMENT_3D ( 'NONE', #34199, #41558, #19785 ) ;
#10074=CARTESIAN_POINT ( 'NONE',  ( 1.033464566929134687, -0.06523048226347956391, 1.099901574695623108 ) ) ;
#10075=CARTESIAN_POINT ( 'NONE',  ( 0.7646288533564489232, -0.1113553986120547346, 0.1427165353255439029 ) ) ;
#10077=EDGE_CURVE ( 'NONE', #1642, #35490, #37322, .T. ) ;
#10078=CARTESIAN_POINT ( 'NONE',  ( 0.7646288533564489232, -0.1113553986120547346, 0.2312992125984252023 ) ) ;
#10079=CARTESIAN_POINT ( 'NONE',  ( 1.033464566929133799, 1.928577636452524610E-17, 4.498031496062992574 ) ) ;
#10080=CARTESIAN_POINT ( 'NONE',  ( 0.8759842519685039353, 0.1574803149606299191, 0.7185039369003465293 ) ) ;
#10083=CARTESIAN_POINT ( 'NONE',  ( -1.002407869896990045, 0.1264236179284866091, 1.916830708607653477 ) ) ;
#10084=ORIENTED_EDGE ( 'NONE', *, *, #31884, .T. ) ;
#10085=CARTESIAN_POINT ( 'NONE',  ( -1.054774247047244096, 0.000000000000000000, 1.444389763725763665 ) ) ;
#10086=CARTESIAN_POINT ( 'NONE',  ( 0.7495606340400177148, 0.1264236179284866091, 1.498523621993480326 ) ) ;
#10087=ORIENTED_EDGE ( 'NONE', *, *, #15948, .F. ) ;
#10089=CARTESIAN_POINT ( 'NONE',  ( -0.9500414927467378812, 0.1787899950787401604, 0.5856299212060785964 ) ) ;
#10091=CARTESIAN_POINT ( 'NONE',  ( 0.9500414927467377701, -0.1787899950787401604, 0.7677165353793073965 ) ) ;
#10092=CARTESIAN_POINT ( 'NONE',  ( -1.002407869896990045, 0.1264236179284866091, 0.6176181101824566033 ) ) ;
#10096=CYLINDRICAL_SURFACE ( 'NONE', #36718, 0.1574803149606299191 ) ;
#10099=CARTESIAN_POINT ( 'NONE',  ( -0.8019270111902717657, -0.1787899950787401604, 1.392716535379308285 ) ) ;
#10100=CARTESIAN_POINT ( 'NONE',  ( -1.033464566929134687, 0.06523048226347956391, 1.508366141732284449 ) ) ;
#10101=CARTESIAN_POINT ( 'NONE',  ( -0.9873396505805591694, -0.1113553986120547346, 0.3986220472440945017 ) ) ;
#10102=CARTESIAN_POINT ( 'NONE',  ( 0.9500414927467377701, -0.1787899950787401604, 1.358267716481669662 ) ) ;
#10105=VERTEX_POINT ( 'NONE', #16056 ) ;
#10112=CARTESIAN_POINT ( 'NONE',  ( 0.8107537697050254399, 0.1574803149606300301, 0.4945866141732282451 ) ) ;
#10114=CYLINDRICAL_SURFACE ( 'NONE', #35396, 0.1574803149606299191 ) ;
#10119=CARTESIAN_POINT ( 'NONE',  ( 0.7495606340400177148, 0.1264236179284866091, 1.690452755851748146 ) ) ;
#10120=CARTESIAN_POINT ( 'NONE',  ( 0.8759842519685039353, -0.1787899950787401882, 0.2878937007336381804 ) ) ;
#10125=DIRECTION ( 'NONE',  ( -1.000000000000000000, 0.000000000000000000, 0.000000000000000000 ) ) ;
#10126=CARTESIAN_POINT ( 'NONE',  ( -0.7185039370078778465, -0.06523048226348396317, 1.478838582569639071 ) ) ;
#10127=CARTESIAN_POINT ( 'NONE',  ( 0.9500414927467378812, -0.1787899950787401604, 0.6053149605761579677 ) ) ;
#10128=AXIS2_PLACEMENT_3D ( 'NONE', #1388, #16047, #34031 ) ;
#10129=CARTESIAN_POINT ( 'NONE',  ( -1.054774247047244540, 0.07405724077823318263, 0.7775590550643457499 ) ) ;
#10130=EDGE_CURVE ( 'NONE', #28079, #2953, #12467, .T. ) ;
#10134=CARTESIAN_POINT ( 'NONE',  ( -0.8453766735112447916, -0.1708762415285247638, 1.987646152247962927 ) ) ;
#10135=CARTESIAN_POINT ( 'NONE',  ( 1.054774247047244540, -0.07405724077823318263, 1.638779527505292988 ) ) ;
#10136=CARTESIAN_POINT ( 'NONE',  ( 0.7495606340400177148, -0.1264236179284866091, 1.975885826717889815 ) ) ;
#10137=CARTESIAN_POINT ( 'NONE',  ( -0.9873396505805591694, -0.1113553986120547346, 1.815944881889763884 ) ) ;
#10138=CARTESIAN_POINT ( 'NONE',  ( 0.9500414927467377701, -0.1787899950787401604, 0.4084645668753704162 ) ) ;
#10144=CARTESIAN_POINT ( 'NONE',  ( 0.6971942568897626646, 0.07405724077823318263, 0.5905511810485987167 ) ) ;
#10146=CARTESIAN_POINT ( 'NONE',  ( 1.054774247047244540, 0.07405724077823318263, 0.1476377952218269618 ) ) ;
#10148=CARTESIAN_POINT ( 'NONE',  ( 0.8759842519685039353, 0.1787899950787401882, 0.5437992125446614589 ) ) ;
#10150=CARTESIAN_POINT ( 'NONE',  ( -1.002407869896990045, 0.1264236179284866091, 1.483759842465921075 ) ) ;
#10151=ORIENTED_EDGE ( 'NONE', *, *, #40985, .T. ) ;
#10154=CARTESIAN_POINT ( 'NONE',  ( 0.6971942568897637749, 2.189545951927499583E-17, 1.109744094434425232 ) ) ;
#10156=CARTESIAN_POINT ( 'NONE',  ( 1.054774247047244096, 0.000000000000000000, 1.754429133804503715 ) ) ;
#10157=CARTESIAN_POINT ( 'NONE',  ( -0.8759842519685039353, -0.1574803149606299191, 1.338582677165354395 ) ) ;
#10158=CARTESIAN_POINT ( 'NONE',  ( -0.6971942568897626646, -0.07405724077823297447, 0.9104330708123776761 ) ) ;
#10159=CARTESIAN_POINT ( 'NONE',  ( -0.7185039370078746268, 0.06523048226347956391, 0.5290354329633386588 ) ) ;
#10160=CARTESIAN_POINT ( 'NONE',  ( -0.7184511836828970655, -0.06596510897976094745, 0.03937007874015842346 ) ) ;
#10161=CARTESIAN_POINT ( 'NONE',  ( 0.6971942568897626646, 0.07405724077823318263, 0.2017716534895435399 ) ) ;
#10163=CARTESIAN_POINT ( 'NONE',  ( 1.033464566929134687, 0.06523048226347956391, 1.577263779420032153 ) ) ;
#10166=ORIENTED_EDGE ( 'NONE', *, *, #20083, .F. ) ;
#10167=CARTESIAN_POINT ( 'NONE',  ( 0.8759842519685039353, -0.1787899950787401882, 0.8046259841982047467 ) ) ;
#10168=CARTESIAN_POINT ( 'NONE',  ( -0.8019270111902716547, 0.1787899950787401604, 1.727362204670645385 ) ) ;
#10170=( BOUNDED_CURVE ( )  B_SPLINE_CURVE ( 2, ( #15431, #19714, #540, #22605, #41249, #4851, #15196, #30534, #45096 ),
 .UNSPECIFIED., .F., .F. ) 
 B_SPLINE_CURVE_WITH_KNOTS ( ( 3, 2, 2, 2, 3 ),
 ( 0.7199999999999999734, 0.7225000000000000311, 0.7249999999999999778, 0.7275000000000000355, 0.7299999999999999822 ),
 .UNSPECIFIED. ) 
 CURVE ( )  GEOMETRIC_REPRESENTATION_ITEM ( )  RATIONAL_B_SPLINE_CURVE ( ( 1.000000000000000000, 0.9238795325112869605, 1.000000000000000000, 0.9238795325112869605, 1.000000000000000000, 0.9238795325112869605, 1.000000000000000000, 0.9238795325112869605, 1.000000000000000000 ) ) 
 REPRESENTATION_ITEM ( '' )  ) ;
#10172=CARTESIAN_POINT ( 'NONE',  ( -1.033464566929134687, 0.06523048226347956391, 0.6422244094488180899 ) ) ;
#10173=CARTESIAN_POINT ( 'NONE',  ( -0.8107537697050254399, -0.1574803149606297803, 0.7849409448818904789 ) ) ;
#10175=ORIENTED_EDGE ( 'NONE', *, *, #3361, .T. ) ;
#10180=EDGE_CURVE ( 'NONE', #29530, #18116, #12708, .T. ) ;
#10182=CARTESIAN_POINT ( 'NONE',  ( 0.7646288533564489232, -0.1113553986120547346, 1.924212598425196985 ) ) ;
#10186=( BOUNDED_CURVE ( )  B_SPLINE_CURVE ( 2, ( #28728, #3035, #6638, #36598, #18378, #46418, #17666, #14083, #10498 ),
 .UNSPECIFIED., .F., .F. ) 
 B_SPLINE_CURVE_WITH_KNOTS ( ( 3, 2, 2, 2, 3 ),
 ( 0.05999999999999999778, 0.06250000000000000000, 0.06500000000000000222, 0.06750000000000000444, 0.07000000000000000666 ),
 .UNSPECIFIED. ) 
 CURVE ( )  GEOMETRIC_REPRESENTATION_ITEM ( )  RATIONAL_B_SPLINE_CURVE ( ( 1.000000000000000000, 0.9238795325112869605, 1.000000000000000000, 0.9238795325112869605, 1.000000000000000000, 0.9238795325112869605, 1.000000000000000000, 0.9238795325112869605, 1.000000000000000000 ) ) 
 REPRESENTATION_ITEM ( '' )  ) ;
#10187=CARTESIAN_POINT ( 'NONE',  ( -0.6971942568897626646, 0.07405724077823318263, 0.3198818897100159098 ) ) ;
#10190=CARTESIAN_POINT ( 'NONE',  ( 0.9500414927467378812, 0.1787899950787401604, 1.215551181048599272 ) ) ;
#10191=CARTESIAN_POINT ( 'NONE',  ( 0.7495606340400177148, 0.1264236179284866091, 1.493602362150960650 ) ) ;
#10195=CARTESIAN_POINT ( 'NONE',  ( 0.7646288533564489232, -0.1113553986120547346, 1.520669291231054876 ) ) ;
#10196=CARTESIAN_POINT ( 'NONE',  ( -1.033464566929134687, -0.06523048226347956391, 1.690452755797984929 ) ) ;
#10198=CARTESIAN_POINT ( 'NONE',  ( 0.9500414927467378812, 0.1787899950787401604, 0.2263779527021421711 ) ) ;
#10200=CARTESIAN_POINT ( 'NONE',  ( -0.9412147342319837628, 0.1574803149606300301, 1.552657480314961758 ) ) ;
#10201=CARTESIAN_POINT ( 'NONE',  ( 0.7495606340400177148, 0.1264236179284866091, 1.099901574749385880 ) ) ;
#10202=CARTESIAN_POINT ( 'NONE',  ( -0.9873396505805591694, -0.1113553986120547346, 0.5462598424121581919 ) ) ;
#10203=ADVANCED_FACE ( 'NONE', ( #45719 ), #12935, .T. ) ;
#10205=CARTESIAN_POINT ( 'NONE',  ( 0.7185039370078746268, 0.06523048226347956391, 0.5684055117034967353 ) ) ;
#10206=ORIENTED_EDGE ( 'NONE', *, *, #12485, .F. ) ;
#10207=CARTESIAN_POINT ( 'NONE',  ( 0.9652740342186406641, 0.1428087511534603948, 0.03937007787513571028 ) ) ;
#10210=CARTESIAN_POINT ( 'NONE',  ( -0.8759842519685039353, 0.1574803149606299191, 0.4429133857192448787 ) ) ;
#10212=CARTESIAN_POINT ( 'NONE',  ( 1.002407869896990045, -0.1264236179284866091, 1.513287401521039355 ) ) ;
#10213=CARTESIAN_POINT ( 'NONE',  ( -0.8759842519685039353, 0.1574803149606299191, 1.633858267716535639 ) ) ;
#10215=ORIENTED_EDGE ( 'NONE', *, *, #47297, .T. ) ;
#10221=CARTESIAN_POINT ( 'NONE',  ( 0.6971942568897637749, 2.189545951927499583E-17, 0.5979330708123780092 ) ) ;
#10224=CARTESIAN_POINT ( 'NONE',  ( -0.9500414927467378812, -0.1787899950787401604, 1.200787401521039355 ) ) ;
#10225=CARTESIAN_POINT ( 'NONE',  ( -0.8759842519685039353, -0.1787899950787401882, 1.941437007820252081 ) ) ;
#10227=CARTESIAN_POINT ( 'NONE',  ( -1.002407869896990045, 0.1264236179284866091, 1.129429133804503937 ) ) ;
#10228=CARTESIAN_POINT ( 'NONE',  ( -1.054774247047244540, 0.07405724077823318263, 0.7775590550643479704 ) ) ;
#10229=CARTESIAN_POINT ( 'NONE',  ( -0.8759842519685039353, 0.000000000000000000, 0.000000000000000000 ) ) ;
#10230=DIRECTION ( 'NONE',  ( 0.000000000000000000, 0.000000000000000000, -1.000000000000000000 ) ) ;
#10233=CARTESIAN_POINT ( 'NONE',  ( -1.033464566929134687, 0.06523048226347956391, 1.459153543199560144 ) ) ;
#10238=CARTESIAN_POINT ( 'NONE',  ( -1.033464566929133799, 0.000000000000000000, 0.5511811022546772021 ) ) ;
#10239=CARTESIAN_POINT ( 'NONE',  ( -0.9500414927467378812, 0.1787899950787401604, 0.6988188975840318173 ) ) ;
#10244=CARTESIAN_POINT ( 'NONE',  ( -0.8019270111902716547, 0.1787899950787401604, 1.653543307032850462 ) ) ;
#10245=AXIS2_PLACEMENT_3D ( 'NONE', #40673, #18652, #33310 ) ;
#10246=EDGE_CURVE ( 'NONE', #41905, #6896, #24201, .T. ) ;
#10252=VECTOR ( 'NONE', #11306, 39.37007874015748143 ) ;
#10253=CARTESIAN_POINT ( 'NONE',  ( 0.7495606340400177148, 0.1264236179284866091, 0.7504921259304880854 ) ) ;
#10258=CARTESIAN_POINT ( 'NONE',  ( 1.033464566929133799, 0.000000000000000000, 1.230314960629921295 ) ) ;
#10259=CARTESIAN_POINT ( 'NONE',  ( 0.9317429405948658427, -0.1672133690053895227, 1.989191746694990881 ) ) ;
#10261=CARTESIAN_POINT ( 'NONE',  ( 0.7646288533564489232, -0.1113553986120547346, 1.963582677165354395 ) ) ;
#10262=CARTESIAN_POINT ( 'NONE',  ( 0.7495606340400177148, -0.1264236179284866091, 0.6373031495525354195 ) ) ;
#10267=CARTESIAN_POINT ( 'NONE',  ( 0.6971942568897626646, -0.07405724077823297447, 0.9498031495525356416 ) ) ;
#10269=CARTESIAN_POINT ( 'NONE',  ( -1.033464566929133799, 1.928577636452524610E-17, 2.869337061179095023E-17 ) ) ;
#10276=CARTESIAN_POINT ( 'NONE',  ( -1.054774247047244096, 0.000000000000000000, 0.02214566923757503927 ) ) ;
#10282=CARTESIAN_POINT ( 'NONE',  ( -1.054774247047244540, -0.07405724077823318263, 1.874999999946236784 ) ) ;
#10283=CARTESIAN_POINT ( 'NONE',  ( -0.7495606340400177148, 0.1264236179284866091, 1.493602362150960650 ) ) ;
#10284=CARTESIAN_POINT ( 'NONE',  ( 1.002407869896990045, 0.1264236179284866091, 0.8193897637257637756 ) ) ;
#10285=CARTESIAN_POINT ( 'NONE',  ( -1.054774247047244540, -0.07405724077823318263, 1.082677165300567346 ) ) ;
#10286=ADVANCED_FACE ( 'NONE', ( #13611 ), #21031, .T. ) ;
#10287=CARTESIAN_POINT ( 'NONE',  ( -1.002407869896990045, -0.1264236179284866091, 0.2189960629383626012 ) ) ;
#10289=CARTESIAN_POINT ( 'NONE',  ( -0.6971942568897637749, 2.189545951927499583E-17, 1.975885826717889815 ) ) ;
#10290=CARTESIAN_POINT ( 'NONE',  ( -0.7185039370078739607, 1.928577636452523993E-17, 0.3051181102362204856 ) ) ;
#10291=CARTESIAN_POINT ( 'NONE',  ( -0.7646288533564489232, -0.1113553986120547346, 1.884842519685039353 ) ) ;
#10296=CARTESIAN_POINT ( 'NONE',  ( -0.9500414927467378812, 0.1787899950787401604, 0.1082677164816695514 ) ) ;
#10299=EDGE_CURVE ( 'NONE', #39650, #9619, #1486, .T. ) ;
#10300=CARTESIAN_POINT ( 'NONE',  ( -0.7495606340400177148, 0.1264236179284866091, 1.222933070812378009 ) ) ;
#10307=CARTESIAN_POINT ( 'NONE',  ( -0.7646288533564489232, -0.1113553986120547346, 0.8907480313885355327 ) ) ;
#10308=CARTESIAN_POINT ( 'NONE',  ( -0.9873396505805591694, 0.1113553986120547346, 0.7234251968503936370 ) ) ;
#10310=VECTOR ( 'NONE', #30547, 39.37007874015748143 ) ;
#10311=CARTESIAN_POINT ( 'NONE',  ( 0.7185039370078746268, -0.06523048226347956391, 1.793799212490897244 ) ) ;
#10314=CARTESIAN_POINT ( 'NONE',  ( 1.033464566929134687, 0.06523048226347956391, 0.8390748031496061410 ) ) ;
#10317=CARTESIAN_POINT ( 'NONE',  ( 1.033464566929133799, 0.000000000000000000, 0.2362204723334177248 ) ) ;
#10318=CARTESIAN_POINT ( 'NONE',  ( 0.8759842519685039353, 0.1574803149606299191, 1.515748031496062964 ) ) ;
#10319=CARTESIAN_POINT ( 'NONE',  ( 0.7185039370078739607, 1.928577636452523993E-17, 0.2165354329633393804 ) ) ;
#10320=ORIENTED_EDGE ( 'NONE', *, *, #36131, .T. ) ;
#10321=ADVANCED_FACE ( 'NONE', ( #14099 ), #31620, .T. ) ;
#10322=CARTESIAN_POINT ( 'NONE',  ( -0.9412147342319837628, -0.1574803149606297803, 0.6225393699712132856 ) ) ;
#10326=CARTESIAN_POINT ( 'NONE',  ( 0.7646288533564489232, 0.1113553986120547346, 0.9596456691838111119 ) ) ;
#10328=CARTESIAN_POINT ( 'NONE',  ( -0.7495606340400177148, -0.1264236179284866091, 0.4010826771115905687 ) ) ;
#10329=ORIENTED_EDGE ( 'NONE', *, *, #42294, .T. ) ;
#10331=CARTESIAN_POINT ( 'NONE',  ( -0.8019270111902717657, 0.1787899950787401604, 1.535433070812378675 ) ) ;
#10332=CARTESIAN_POINT ( 'NONE',  ( 0.8759842519685039353, 0.1787899950787401882, 1.493602362150960650 ) ) ;
#10334=CARTESIAN_POINT ( 'NONE',  ( 0.7185039370078739607, 1.928577636452523993E-17, 1.082677165246803241 ) ) ;
#10335=CARTESIAN_POINT ( 'NONE',  ( -1.054774247047244096, 0.000000000000000000, 0.6176181101824566033 ) ) ;
#10336=CARTESIAN_POINT ( 'NONE',  ( 0.7495606340400177148, -0.1264236179284866091, 0.2091535432533232486 ) ) ;
#10338=CARTESIAN_POINT ( 'NONE',  ( -0.8759842519685039353, 0.1574803149606299191, 0.2559055118110236116 ) ) ;
#10339=CARTESIAN_POINT ( 'NONE',  ( -0.6971942568897648851, 0.07405724077823318263, 0.7086614172690703928 ) ) ;
#10340=CARTESIAN_POINT ( 'NONE',  ( 0.8759842519685039353, -0.1574803149606299191, 0.6299212598425196763 ) ) ;
#10341=( BOUNDED_CURVE ( )  B_SPLINE_CURVE ( 2, ( #34464, #16264, #30898, #45454, #12676, #21004, #43040, #39452, #32055 ),
 .UNSPECIFIED., .F., .T. ) 
 B_SPLINE_CURVE_WITH_KNOTS ( ( 3, 2, 2, 2, 3 ),
 ( 0.5000000000000000000, 0.5024999999999999467, 0.5050000000000000044, 0.5074999999999999512, 0.5100000000000000089 ),
 .UNSPECIFIED. ) 
 CURVE ( )  GEOMETRIC_REPRESENTATION_ITEM ( )  RATIONAL_B_SPLINE_CURVE ( ( 1.000000000000000000, 0.9238795325112869605, 1.000000000000000000, 0.9238795325112869605, 1.000000000000000000, 0.9238795325112869605, 1.000000000000000000, 0.9238795325112869605, 1.000000000000000000 ) ) 
 REPRESENTATION_ITEM ( '' )  ) ;
#10342=FACE_OUTER_BOUND ( 'NONE', #17265, .T. ) ;
#10344=CARTESIAN_POINT ( 'NONE',  ( -1.054774247047244096, 0.000000000000000000, 1.365649606245448844 ) ) ;
#10345=AXIS2_PLACEMENT_3D ( 'NONE', #40477, #7661, #18917 ) ;
#10346=CARTESIAN_POINT ( 'NONE',  ( -0.8759842519685039353, -0.1574803149606299191, 0.5118110236220472231 ) ) ;
#10347=CARTESIAN_POINT ( 'NONE',  ( 0.7495606340400177148, 0.1264236179284866091, 1.341043307032850462 ) ) ;
#10352=CARTESIAN_POINT ( 'NONE',  ( -0.8107537697050254399, -0.1574803149606297803, 0.6274606299212601712 ) ) ;
#10355=ORIENTED_EDGE ( 'NONE', *, *, #5473, .F. ) ;
#10360=FACE_OUTER_BOUND ( 'NONE', #35417, .T. ) ;
#10363=DIRECTION ( 'NONE',  ( 0.000000000000000000, 0.000000000000000000, -1.000000000000000000 ) ) ;
#10365=CARTESIAN_POINT ( 'NONE',  ( 0.6971942568897648851, -0.07405724077823297447, 1.697834645615527771 ) ) ;
#10366=CARTESIAN_POINT ( 'NONE',  ( 1.002407869896990045, 0.1264236179284866091, 0.3026574802611972648 ) ) ;
#10370=CARTESIAN_POINT ( 'NONE',  ( 0.9412147342319837628, 0.1574803149606300301, 0.5585629920184573827 ) ) ;
#10371=CARTESIAN_POINT ( 'NONE',  ( -0.9500414927467377701, -0.1787899950787401604, 0.9645669290800954476 ) ) ;
#10372=CARTESIAN_POINT ( 'NONE',  ( -1.033464566929135131, 1.928577636452536319E-17, 0.03937007874015843040 ) ) ;
#10373=CARTESIAN_POINT ( 'NONE',  ( 0.8107537697050254399, 0.1574803149606300301, 1.705216535325545069 ) ) ;
#10376=CARTESIAN_POINT ( 'NONE',  ( 0.8759842519685039353, 0.1787899950787401882, 1.651082677111590513 ) ) ;
#10378=CARTESIAN_POINT ( 'NONE',  ( -1.033464566929133799, 1.928577636452524610E-17, 2.869337061179095023E-17 ) ) ;
#10379=CARTESIAN_POINT ( 'NONE',  ( 1.002407869896990045, -0.1264236179284866091, 0.5290354330171024300 ) ) ;
#10381=AXIS2_PLACEMENT_3D ( 'NONE', #4782, #5027, #19408 ) ;
#10386=CARTESIAN_POINT ( 'NONE',  ( 0.7495606340400177148, 0.1264236179284866091, 0.5487204723871811352 ) ) ;
#10389=CARTESIAN_POINT ( 'NONE',  ( 1.054774247047244540, 0.07405724077823318263, 0.02952755900135457801 ) ) ;
#10390=CARTESIAN_POINT ( 'NONE',  ( -0.7185039370078739607, 1.928577636452523993E-17, 0.9251968502861732668 ) ) ;
#10391=CARTESIAN_POINT ( 'NONE',  ( -0.6971942568897648851, 0.07405724077823318263, 1.574803149552536530 ) ) ;
#10392=EDGE_LOOP ( 'NONE', ( #41113, #47055, #6073, #18093 ) ) ;
#10393=CARTESIAN_POINT ( 'NONE',  ( -1.054774247047244540, 0.07405724077823318263, 1.092519684985605810 ) ) ;
#10394=CARTESIAN_POINT ( 'NONE',  ( 0.8759842519685039353, -0.1574803149606299191, 0.1574803149606299191 ) ) ;
#10395=CARTESIAN_POINT ( 'NONE',  ( 0.8019270111902717657, -0.1787899950787401604, 1.235236220418678199 ) ) ;
#10397=CARTESIAN_POINT ( 'NONE',  ( -0.9412147342319837628, -0.1574803149606297803, 0.6619094487113696967 ) ) ;
#10399=CARTESIAN_POINT ( 'NONE',  ( 0.8019270111902717657, 0.1787899950787401604, 1.806102362150961316 ) ) ;
#10400=CARTESIAN_POINT ( 'NONE',  ( -1.033464566929134687, 0.06523048226347956391, 0.6028543307086614567 ) ) ;
#10401=CARTESIAN_POINT ( 'NONE',  ( -0.8019270111902717657, -0.1787899950787401604, 0.8366141731745828647 ) ) ;
#10402=CARTESIAN_POINT ( 'NONE',  ( -0.8107537697050254399, -0.1574803149606297803, 1.611712598425196319 ) ) ;
#10403=CARTESIAN_POINT ( 'NONE',  ( -0.7412252283027040978, -0.1004855783171688804, 0.03937007874015844427 ) ) ;
#10404=CARTESIAN_POINT ( 'NONE',  ( 0.9500414927467377701, 0.1787899950787401604, 0.2706692912848194243 ) ) ;
#10405=CARTESIAN_POINT ( 'NONE',  ( -0.9500414927467377701, -0.1787899950787401604, 0.1722440944344254543 ) ) ;
#10406=CARTESIAN_POINT ( 'NONE',  ( -0.8759842519685039353, -0.1787899950787401882, 0.6028543306548976854 ) ) ;
#10407=CARTESIAN_POINT ( 'NONE',  ( 1.033464566929133799, 0.000000000000000000, 1.614173228238929170 ) ) ;
#10408=ORIENTED_EDGE ( 'NONE', *, *, #31937, .F. ) ;
#10410=LINE ( 'NONE', #6309, #7633 ) ;
#10411=CARTESIAN_POINT ( 'NONE',  ( 0.9500414927467378812, 0.1787899950787401604, 0.7824803149068669805 ) ) ;
#10412=CARTESIAN_POINT ( 'NONE',  ( -0.8019270111902716547, -0.1787899950787401604, 1.820866141678520789 ) ) ;
#10413=VECTOR ( 'NONE', #26784, 39.37007874015748143 ) ;
#10414=EDGE_CURVE ( 'NONE', #40492, #2870, #12602, .T. ) ;
#10416=CARTESIAN_POINT ( 'NONE',  ( -0.8107537697050254399, 0.1574803149606300301, 0.6520669291338587747 ) ) ;
#10417=CARTESIAN_POINT ( 'NONE',  ( 0.8107537697050254399, 0.1574803149606300301, 1.321358267716534751 ) ) ;
#10423=EDGE_CURVE ( 'NONE', #3332, #17493, #40356, .T. ) ;
#10425=CARTESIAN_POINT ( 'NONE',  ( -0.7185039370078739607, 1.928577636452523993E-17, 1.003937007766488199 ) ) ;
#10426=CARTESIAN_POINT ( 'NONE',  ( 0.7185039370078746268, 0.06523048226347956391, 1.916830708661418248 ) ) ;
#10429=CARTESIAN_POINT ( 'NONE',  ( -1.054774247047244540, 0.07405724077823318263, 0.5019685038832443214 ) ) ;
#10432=CARTESIAN_POINT ( 'NONE',  ( 0.9500414927467378812, -0.1787899950787401604, 1.200787401521039355 ) ) ;
#10433=CARTESIAN_POINT ( 'NONE',  ( 1.054774247047244540, -0.07405724077823318263, 1.555118110182457158 ) ) ;
#10434=CIRCLE ( 'NONE', #37206, 0.1574803149606299191 ) ;
#10435=CARTESIAN_POINT ( 'NONE',  ( -1.033464566929133799, 1.928577636452524610E-17, 2.869337061179095023E-17 ) ) ;
#10436=CARTESIAN_POINT ( 'NONE',  ( -0.7646288533564489232, -0.1113553986120547346, 1.097440944881889813 ) ) ;
#10437=CARTESIAN_POINT ( 'NONE',  ( 1.033464566929133799, 0.000000000000000000, 0.6692913384751496553 ) ) ;
#10439=CARTESIAN_POINT ( 'NONE',  ( -0.8759842519685039353, -0.1574803149606299191, 1.761811023514519459 ) ) ;
#10441=CARTESIAN_POINT ( 'NONE',  ( 0.8019270111902717657, -0.1787899950787401604, 0.2066929133320631329 ) ) ;
#10442=CARTESIAN_POINT ( 'NONE',  ( 0.7132454508862760001, -0.05294806947096847988, 0.03937007859770621371 ) ) ;
#10443=CARTESIAN_POINT ( 'NONE',  ( 1.054774247047244096, 0.000000000000000000, 1.124507873961984261 ) ) ;
#10445=CARTESIAN_POINT ( 'NONE',  ( -0.7185039370078739607, 1.928577636452523993E-17, 1.909448818790110192 ) ) ;
#10446=CARTESIAN_POINT ( 'NONE',  ( 0.8107537697050253289, 0.1574803149606300301, 0.5241141731208195376 ) ) ;
#10447=ORIENTED_EDGE ( 'NONE', *, *, #43269, .T. ) ;
#10449=CARTESIAN_POINT ( 'NONE',  ( 0.8755199539507505513, 0.1745681463551092827, 0.03936728564635524202 ) ) ;
#10450=CARTESIAN_POINT ( 'NONE',  ( -0.7646288533564489232, 0.1113553986120547346, 0.4084645668216063119 ) ) ;
#10451=CARTESIAN_POINT ( 'NONE',  ( -0.8759842519685039353, -0.1574803149606299191, 1.535433070866141669 ) ) ;
#10452=CARTESIAN_POINT ( 'NONE',  ( 0.9500414927467378812, 0.1787899950787401604, 1.525590551127340433 ) ) ;
#10458=( BOUNDED_CURVE ( )  B_SPLINE_CURVE ( 2, ( #32746, #26013, #7783, #25554, #22398, #33228, #37027, #26261, #108 ),
 .UNSPECIFIED., .F., .T. ) 
 B_SPLINE_CURVE_WITH_KNOTS ( ( 3, 2, 2, 2, 3 ),
 ( 0.8399999999999999689, 0.8425000000000000266, 0.8449999999999999734, 0.8475000000000000311, 0.8499999999999999778 ),
 .UNSPECIFIED. ) 
 CURVE ( )  GEOMETRIC_REPRESENTATION_ITEM ( )  RATIONAL_B_SPLINE_CURVE ( ( 1.000000000000000000, 0.9238795325112869605, 1.000000000000000000, 0.9238795325112869605, 1.000000000000000000, 0.9238795325112869605, 1.000000000000000000, 0.9238795325112869605, 1.000000000000000000 ) ) 
 REPRESENTATION_ITEM ( '' )  ) ;
#10459=VERTEX_POINT ( 'NONE', #23593 ) ;
#10462=CARTESIAN_POINT ( 'NONE',  ( 0.8019270111902717657, -0.1787899950787401604, 0.5659448818360001132 ) ) ;
#10464=EDGE_CURVE ( 'NONE', #1535, #15970, #17458, .T. ) ;
#10466=CARTESIAN_POINT ( 'NONE',  ( -0.6971942568897648851, -0.07405724077823297447, 1.382874015694267822 ) ) ;
#10468=CARTESIAN_POINT ( 'NONE',  ( -1.002407869896990045, 0.1264236179284866091, 1.094980314906866203 ) ) ;
#10469=CARTESIAN_POINT ( 'NONE',  ( -0.7185039370078746268, -0.06523048226347956391, 0.1107283464566929249 ) ) ;
#10471=CARTESIAN_POINT ( 'NONE',  ( -0.8019270111902716547, -0.1787899950787401604, 1.151574803095843036 ) ) ;
#10472=CARTESIAN_POINT ( 'NONE',  ( -0.9500414927467378812, 0.1787899950787401604, 0.8218503936470251681 ) ) ;
#10473=EDGE_CURVE ( 'NONE', #8877, #35682, #45293, .T. ) ;
#10474=CARTESIAN_POINT ( 'NONE',  ( -0.9500414927467378812, 0.1787899950787401604, 0.2312992125446618197 ) ) ;
#10475=CYLINDRICAL_SURFACE ( 'NONE', #40456, 0.1574803149606299191 ) ;
#10481=EDGE_CURVE ( 'NONE', #11244, #19795, #4654, .T. ) ;
#10482=DIRECTION ( 'NONE',  ( -1.000000000000000000, 0.000000000000000000, 0.000000000000000000 ) ) ;
#10483=( BOUNDED_CURVE ( )  B_SPLINE_CURVE ( 2, ( #15749, #12145, #18605, #610, #19316, #44930, #15508, #8288, #1092 ),
 .UNSPECIFIED., .F., .T. ) 
 B_SPLINE_CURVE_WITH_KNOTS ( ( 3, 2, 2, 2, 3 ),
 ( 0.2200000000000000011, 0.2225000000000000033, 0.2250000000000000056, 0.2275000000000000078, 0.2300000000000000100 ),
 .UNSPECIFIED. ) 
 CURVE ( )  GEOMETRIC_REPRESENTATION_ITEM ( )  RATIONAL_B_SPLINE_CURVE ( ( 1.000000000000000000, 0.9238795325112869605, 1.000000000000000000, 0.9238795325112869605, 1.000000000000000000, 0.9238795325112869605, 1.000000000000000000, 0.9238795325112869605, 1.000000000000000000 ) ) 
 REPRESENTATION_ITEM ( '' )  ) ;
#10484=CARTESIAN_POINT ( 'NONE',  ( -1.002407869896990045, -0.1264236179284866091, 0.6471456692375747721 ) ) ;
#10485=ORIENTED_EDGE ( 'NONE', *, *, #23784, .F. ) ;
#10486=CARTESIAN_POINT ( 'NONE',  ( -1.054774247047244096, 0.000000000000000000, 1.798720472387181024 ) ) ;
#10488=CARTESIAN_POINT ( 'NONE',  ( -0.8759842519685039353, 0.1787899950787401882, 0.1156496062454492185 ) ) ;
#10490=CARTESIAN_POINT ( 'NONE',  ( 0.7185039370078746268, -0.06523048226347956391, 0.6619094488188971281 ) ) ;
#10492=CARTESIAN_POINT ( 'NONE',  ( -1.033464566929134687, 0.06523048226347956391, 0.9571850393700783721 ) ) ;
#10493=CARTESIAN_POINT ( 'NONE',  ( -0.8107537697050253289, -0.1574803149606297803, 1.444389763672000671 ) ) ;
#10494=CARTESIAN_POINT ( 'NONE',  ( 1.002407869896990045, -0.1264236179284866091, 0.7308070865604093802 ) ) ;
#10498=CARTESIAN_POINT ( 'NONE',  ( 0.7185039370078739607, 1.928577636452523993E-17, 0.1771653542231816925 ) ) ;
#10499=CARTESIAN_POINT ( 'NONE',  ( 0.9412147342319837628, -0.1574803149606297803, 1.183562992125983593 ) ) ;
#10500=CARTESIAN_POINT ( 'NONE',  ( 0.8478354771968141801, -0.1713848073773632519, 1.987689202509897557 ) ) ;
#10504=CARTESIAN_POINT ( 'NONE',  ( 0.8759842519685039353, 0.1787899950787401882, 0.7012795275052913224 ) ) ;
#10507=CARTESIAN_POINT ( 'NONE',  ( 0.7185039370078739607, 1.928577636452523993E-17, 1.564960629921259949 ) ) ;
#10509=CARTESIAN_POINT ( 'NONE',  ( 0.8107537697050253289, -0.1574803149606297803, 1.729822834645670548 ) ) ;
#10510=CARTESIAN_POINT ( 'NONE',  ( 1.033464566929133799, 0.000000000000000000, 0.7185039370078739607 ) ) ;
#10511=CARTESIAN_POINT ( 'NONE',  ( 0.8019270111902717657, 0.1787899950787401604, 1.018700787347811110 ) ) ;
#10517=CARTESIAN_POINT ( 'NONE',  ( 0.7646288533564489232, 0.1113553986120547346, 1.245078740157480324 ) ) ;
#10518=ORIENTED_EDGE ( 'NONE', *, *, #47008, .T. ) ;
#10519=CARTESIAN_POINT ( 'NONE',  ( -1.054774247047244540, -0.07405724077823318263, 0.09842519679663024046 ) ) ;
#10520=EDGE_CURVE ( 'NONE', #2780, #43175, #39143, .T. ) ;
#10521=CARTESIAN_POINT ( 'NONE',  ( 1.002407869896990045, -0.1264236179284866091, 1.951279527505291433 ) ) ;
#10523=CARTESIAN_POINT ( 'NONE',  ( -0.9500414927467377701, 0.1787899950787401604, 1.884842519631275026 ) ) ;
#10524=CARTESIAN_POINT ( 'NONE',  ( -0.8019270111902717657, 0.1787899950787401604, 1.648622047190331230 ) ) ;
#10525=CARTESIAN_POINT ( 'NONE',  ( 0.6971942568897648851, -0.07405724077823297447, 0.8366141731745828647 ) ) ;
#10526=CARTESIAN_POINT ( 'NONE',  ( -1.002407869896990045, 0.1264236179284866091, 0.8144685038832440993 ) ) ;
#10527=CARTESIAN_POINT ( 'NONE',  ( -0.8759842519685039353, -0.1787899950787401882, 1.114665354276944909 ) ) ;
#10528=CARTESIAN_POINT ( 'NONE',  ( -0.8019270111902717657, -0.1787899950787401604, 0.4084645668753704717 ) ) ;
#10529=CARTESIAN_POINT ( 'NONE',  ( -0.8107537697050254399, -0.1574803149606297803, 1.798720472333418918 ) ) ;
#10530=CARTESIAN_POINT ( 'NONE',  ( -1.054774247047244540, -0.07405724077823318263, 1.874999999946236784 ) ) ;
#10532=CARTESIAN_POINT ( 'NONE',  ( -0.8107537697050253289, -0.1574803149606297803, 1.966043307086614567 ) ) ;
#10533=CARTESIAN_POINT ( 'NONE',  ( -0.8107537697050254399, -0.1574803149606297803, 1.887303149606298414 ) ) ;
#10537=CARTESIAN_POINT ( 'NONE',  ( 0.7646288533564489232, -0.1113553986120547346, 1.048228346349165507 ) ) ;
#10539=CARTESIAN_POINT ( 'NONE',  ( -0.6971942568897637749, 2.189545951927499583E-17, 0.08120078734781142893 ) ) ;
#10541=CARTESIAN_POINT ( 'NONE',  ( -0.6971942568897637749, 2.189545951927499583E-17, 1.345964566875370139 ) ) ;
#10545=CARTESIAN_POINT ( 'NONE',  ( -0.7185039370078714072, 0.06523048226347728795, 1.552657480207434659 ) ) ;
#10547=CARTESIAN_POINT ( 'NONE',  ( 0.7185039370078746268, 0.06523048226347956391, 0.3813976377952755237 ) ) ;
#10549=CARTESIAN_POINT ( 'NONE',  ( -1.033464566929134687, 0.06523048226347956391, 0.9473425195775121432 ) ) ;
#10550=CARTESIAN_POINT ( 'NONE',  ( -0.9412147342319837628, -0.1574803149606297803, 0.7898622047244097111 ) ) ;
#10551=CARTESIAN_POINT ( 'NONE',  ( 1.054774247047244540, 0.07405724077823318263, 0.3838582676627718127 ) ) ;
#10553=CARTESIAN_POINT ( 'NONE',  ( 0.8759842519685039353, -0.1574803149606299191, 1.879921259734992134 ) ) ;
#10555=CARTESIAN_POINT ( 'NONE',  ( -0.8107537697050254399, 0.1574803149606300301, 1.429625984144440531 ) ) ;
#10556=CARTESIAN_POINT ( 'NONE',  ( 0.8107537697050253289, -0.1574803149606297803, 0.8636811023622045225 ) ) ;
#10558=LINE ( 'NONE', #25157, #23309 ) ;
#10561=CARTESIAN_POINT ( 'NONE',  ( 0.8107537697050254399, 0.1574803149606300301, 1.518208661417322913 ) ) ;
#10562=CARTESIAN_POINT ( 'NONE',  ( 0.7646288533564489232, -0.1113553986120547346, 0.2608267715460165226 ) ) ;
#10571=CARTESIAN_POINT ( 'NONE',  ( 0.8759842519685039353, 0.1574803149606299191, 0.9153543306011338032 ) ) ;
#10574=CARTESIAN_POINT ( 'NONE',  ( -0.6971942568897626646, 0.07405724077823318263, 0.3937007873478115538 ) ) ;
#10575=ORIENTED_EDGE ( 'NONE', *, *, #20495, .T. ) ;
#10578=CARTESIAN_POINT ( 'NONE',  ( -0.6971942568897648851, 0.07405724077823318263, 1.658464566875369472 ) ) ;
#10581=CARTESIAN_POINT ( 'NONE',  ( 0.7495606340400177148, 0.1264236179284866091, 1.577263779473795369 ) ) ;
#10582=VERTEX_POINT ( 'NONE', #41292 ) ;
#10583=CARTESIAN_POINT ( 'NONE',  ( -0.8019270111902717657, -0.1787899950787401604, 0.7627952755367881643 ) ) ;
#10584=EDGE_CURVE ( 'NONE', #1283, #31809, #22351, .T. ) ;
#10586=CARTESIAN_POINT ( 'NONE',  ( 0.9500414927467377701, 0.1787899950787401604, 0.7824803149068668695 ) ) ;
#10587=CARTESIAN_POINT ( 'NONE',  ( -0.6971942568897648851, -0.07405724077823297447, 0.7135826771115916234 ) ) ;
#10588=CYLINDRICAL_SURFACE ( 'NONE', #24608, 0.1574803149606299191 ) ;
#10589=CYLINDRICAL_SURFACE ( 'NONE', #29892, 0.1574803149606299191 ) ;
#10591=CARTESIAN_POINT ( 'NONE',  ( -1.002407869896990045, -0.1264236179284866091, 1.360728346402929168 ) ) ;
#10592=CARTESIAN_POINT ( 'NONE',  ( -0.8759842519685039353, 0.1574803149606299191, 1.476377952755905554 ) ) ;
#10593=CARTESIAN_POINT ( 'NONE',  ( -0.7646288533564489232, 0.1113553986120547346, 0.4576771653543307283 ) ) ;
#10594=CARTESIAN_POINT ( 'NONE',  ( 0.8759842519685039353, 0.1787899950787401882, 1.454232283410803017 ) ) ;
#10596=CARTESIAN_POINT ( 'NONE',  ( -1.033464566929133799, 0.000000000000000000, 0.3149606298137326843 ) ) ;
#10600=VERTEX_POINT ( 'NONE', #24576 ) ;
#10601=CARTESIAN_POINT ( 'NONE',  ( 0.9873396505805591694, 0.1113553986120547346, 0.4872047244094488416 ) ) ;
#10604=AXIS2_PLACEMENT_3D ( 'NONE', #12008, #16314, #12490 ) ;
#10606=DIRECTION ( 'NONE',  ( 1.822029033848725028E-16, 0.000000000000000000, 1.000000000000000000 ) ) ;
#10607=CARTESIAN_POINT ( 'NONE',  ( 1.054774247047244096, 0.000000000000000000, 0.3371062991588349989 ) ) ;
#10612=CARTESIAN_POINT ( 'NONE',  ( 0.9500414927467378812, 0.1787899950787401604, 0.5807086613635594752 ) ) ;
#10613=CARTESIAN_POINT ( 'NONE',  ( -1.002407869896990045, -0.1264236179284866091, 0.8882874015210394658 ) ) ;
#10615=LINE ( 'NONE', #2909, #36919 ) ;
#10617=CARTESIAN_POINT ( 'NONE',  ( 0.7646288533564489232, -0.1113553986120547346, 1.687992125984252079 ) ) ;
#10618=CARTESIAN_POINT ( 'NONE',  ( 0.8019270111902717657, -0.1787899950787401604, 1.707677165300566235 ) ) ;
#10621=CARTESIAN_POINT ( 'NONE',  ( 0.7185039370078746268, 0.06523048226347956391, 0.02706692913385832025 ) ) ;
#10625=CARTESIAN_POINT ( 'NONE',  ( 0.7495606340400177148, -0.1264236179284866091, 0.5585629920722204877 ) ) ;
#10627=CARTESIAN_POINT ( 'NONE',  ( 1.054774247047244096, 0.000000000000000000, 0.1058070865604096300 ) ) ;
#10629=CARTESIAN_POINT ( 'NONE',  ( 0.6971942568897648851, 0.07405724077823318263, 0.5905511810485987167 ) ) ;
#10630=CARTESIAN_POINT ( 'NONE',  ( -1.002407869896990045, 0.1264236179284866091, 1.601870078686393750 ) ) ;
#10631=VERTEX_POINT ( 'NONE', #9965 ) ;
#10632=CARTESIAN_POINT ( 'NONE',  ( 0.8759842519685039353, -0.1787899950787401882, 1.158956692859621995 ) ) ;
#10634=CARTESIAN_POINT ( 'NONE',  ( -0.9412147342319837628, 0.1574803149606300301, 0.7160433069790875793 ) ) ;
#10636=CARTESIAN_POINT ( 'NONE',  ( 0.8019270111902717657, 0.1787899950787401604, 1.884842519631275026 ) ) ;
#10637=CARTESIAN_POINT ( 'NONE',  ( -0.8107537697050253289, 0.1574803149606300301, 0.6126968503937006982 ) ) ;
#10638=CARTESIAN_POINT ( 'NONE',  ( -0.7495606340400177148, 0.1264236179284866091, 0.9424212597887559051 ) ) ;
#10639=ADVANCED_FACE ( 'NONE', ( #35374 ), #17144, .T. ) ;
#10640=CARTESIAN_POINT ( 'NONE',  ( 0.6971942568897626646, 0.07405724077823318263, 0.2411417322297010890 ) ) ;
#10641=CARTESIAN_POINT ( 'NONE',  ( -0.7495606340400177148, -0.1264236179284866091, 0.2436023621509610382 ) ) ;
#10642=CARTESIAN_POINT ( 'NONE',  ( -0.8759842519685039353, -0.1787899950787401882, 0.7603346456155274380 ) ) ;
#10643=CARTESIAN_POINT ( 'NONE',  ( 0.8107537697050253289, 0.1574803149606300301, 1.626476377845228694 ) ) ;
#10644=ORIENTED_EDGE ( 'NONE', *, *, #4803, .F. ) ;
#10647=CARTESIAN_POINT ( 'NONE',  ( 0.8019270111902717657, 0.1787899950787401604, 0.7874015747493863238 ) ) ;
#10648=CARTESIAN_POINT ( 'NONE',  ( 1.054774247047244540, -0.07405724077823318263, 1.008858267662772423 ) ) ;
#10649=CARTESIAN_POINT ( 'NONE',  ( -0.8019270111902716547, 0.1787899950787401604, 1.924212598371433325 ) ) ;
#10650=CARTESIAN_POINT ( 'NONE',  ( 0.6971942568897648851, 0.07405724077823318263, 1.929133858213952335 ) ) ;
#10656=CARTESIAN_POINT ( 'NONE',  ( 0.9500414927467378812, 0.1787899950787401604, 1.053149606245450176 ) ) ;
#10659=CARTESIAN_POINT ( 'NONE',  ( -0.8107537697050254399, 0.1574803149606300301, 0.9965551180027086842 ) ) ;
#10661=CARTESIAN_POINT ( 'NONE',  ( 0.6971942568897626646, 0.07405724077823318263, 0.03937007868639404856 ) ) ;
#10662=AXIS2_PLACEMENT_3D ( 'NONE', #34606, #6049, #41506 ) ;
#10666=CARTESIAN_POINT ( 'NONE',  ( -0.9500414927467377701, -0.1787899950787401604, 0.4527559054580477249 ) ) ;
#10668=CARTESIAN_POINT ( 'NONE',  ( -0.7109468291419211994, -0.02418920431224856268, 1.983709381215293721 ) ) ;
#10670=CARTESIAN_POINT ( 'NONE',  ( 0.6971942568897637749, 2.189545951927499583E-17, 1.227854330654897685 ) ) ;
#10672=CARTESIAN_POINT ( 'NONE',  ( 0.7495606340400177148, 0.1264236179284866091, 1.572342519631275692 ) ) ;
#10673=DIRECTION ( 'NONE',  ( 0.000000000000000000, 0.000000000000000000, 1.000000000000000000 ) ) ;
#10678=CARTESIAN_POINT ( 'NONE',  ( -0.8107537697050253289, -0.1574803149606297803, 1.759350393593260842 ) ) ;
#10679=CARTESIAN_POINT ( 'NONE',  ( 0.7495606340400177148, -0.1264236179284866091, 0.1254921259304885850 ) ) ;
#10680=CARTESIAN_POINT ( 'NONE',  ( 0.7013878823978492161, 0.0007829370750213354322, 0.03936334417628854776 ) ) ;
#10682=CARTESIAN_POINT ( 'NONE',  ( 0.8019270111902716547, -0.1787899950787401604, 1.151574803095843036 ) ) ;
#10683=CARTESIAN_POINT ( 'NONE',  ( 0.8759842519685039353, 0.000000000000000000, 4.498031496062992574 ) ) ;
#10684=CARTESIAN_POINT ( 'NONE',  ( 0.7185039370078746268, -0.06523048226347956391, 1.213090551181103427 ) ) ;
#10685=CARTESIAN_POINT ( 'NONE',  ( -0.8759842519685039353, 0.1787899950787401882, 1.252460629867496067 ) ) ;
#10686=CARTESIAN_POINT ( 'NONE',  ( 0.8107537697050253289, 0.1574803149606300301, 0.4847440943806614055 ) ) ;
#10687=ORIENTED_EDGE ( 'NONE', *, *, #7218, .T. ) ;
#10689=CARTESIAN_POINT ( 'NONE',  ( 0.8898084847641706263, 0.1731449922679708653, 0.03937008185983620345 ) ) ;
#10690=VERTEX_POINT ( 'NONE', #2982 ) ;
#10691=CARTESIAN_POINT ( 'NONE',  ( -0.7646288533564489232, 0.1113553986120547346, 0.3690944880814492901 ) ) ;
#10693=CARTESIAN_POINT ( 'NONE',  ( 1.054774247047244540, 0.07405724077823318263, 1.402559055064346971 ) ) ;
#10695=CARTESIAN_POINT ( 'NONE',  ( -1.033464566929133799, 1.928577636452524610E-17, 2.869337061179095023E-17 ) ) ;
#10697=CARTESIAN_POINT ( 'NONE',  ( 0.7646288533564489232, 0.1113553986120547346, 1.914370078740157632 ) ) ;
#10700=CARTESIAN_POINT ( 'NONE',  ( 0.7185039370078739607, 1.928577636452523993E-17, 1.318897637687747926 ) ) ;
#10701=AXIS2_PLACEMENT_3D ( 'NONE', #2167, #28300, #46012 ) ;
#10702=ORIENTED_EDGE ( 'NONE', *, *, #2224, .T. ) ;
#10703=CARTESIAN_POINT ( 'NONE',  ( 0.7185039370078739607, 1.928577636452523993E-17, 1.279527558947590515 ) ) ;
#10706=CARTESIAN_POINT ( 'NONE',  ( 1.002407869896990045, -0.1264236179284866091, 0.5339566928596221063 ) ) ;
#10708=CARTESIAN_POINT ( 'NONE',  ( -0.6971942568897648851, 0.07405724077823318263, 1.456692913332062522 ) ) ;
#10710=CARTESIAN_POINT ( 'NONE',  ( -1.054774247047244540, -0.07405724077823318263, 1.126968503883244654 ) ) ;
#10711=CARTESIAN_POINT ( 'NONE',  ( -0.7185039370078746268, -0.06523048226347956391, 0.1500984251968505434 ) ) ;
#10713=CARTESIAN_POINT ( 'NONE',  ( -0.7495606340400177148, 0.1264236179284866091, 1.139271653489543290 ) ) ;
#10714=CARTESIAN_POINT ( 'NONE',  ( -1.002407869896990045, 0.1264236179284866091, 0.2682086613635594752 ) ) ;
#10718=EDGE_LOOP ( 'NONE', ( #6894, #42010, #16054, #42598 ) ) ;
#10721=CARTESIAN_POINT ( 'NONE',  ( 0.7931922328058882421, 0.1592273191109241925, 0.03937007863263045776 ) ) ;
#10723=CARTESIAN_POINT ( 'NONE',  ( 0.7185039370078739607, 0.000000000000000000, 4.498031496062992574 ) ) ;
#10726=CARTESIAN_POINT ( 'NONE',  ( -0.6971942568897637749, 2.189545951927499583E-17, 0.7504921259304880854 ) ) ;
#10727=CARTESIAN_POINT ( 'NONE',  ( -0.7185039370078746268, -0.06523048226347956391, 0.5733267715460159675 ) ) ;
#10728=ORIENTED_EDGE ( 'NONE', *, *, #22778, .F. ) ;
#10729=CARTESIAN_POINT ( 'NONE',  ( -0.6971942568897648851, -0.07405724077823297447, 1.742125984198204858 ) ) ;
#10731=CARTESIAN_POINT ( 'NONE',  ( -0.7646288533564489232, -0.1113553986120547346, 1.126968503829480328 ) ) ;
#10733=CARTESIAN_POINT ( 'NONE',  ( -0.7495606340400177148, 0.1264236179284866091, 0.1205708660879689087 ) ) ;
#10734=CARTESIAN_POINT ( 'NONE',  ( 0.9873396505805591694, -0.1113553986120547346, 0.6742125984251968740 ) ) ;
#10736=CARTESIAN_POINT ( 'NONE',  ( -0.7185039370078746268, 0.06523048226347956391, 0.4109251967428667052 ) ) ;
#10737=CARTESIAN_POINT ( 'NONE',  ( -1.033464566929134687, -0.06523048226347956391, 1.336122047136566904 ) ) ;
#10739=CARTESIAN_POINT ( 'NONE',  ( 1.002407869896990045, -0.1264236179284866091, 0.6914370078202519698 ) ) ;
#10744=CARTESIAN_POINT ( 'NONE',  ( 0.7646288533564489232, 0.1113553986120547346, 1.245078740157480324 ) ) ;
#10745=CARTESIAN_POINT ( 'NONE',  ( 0.8020464063513640385, -0.1557015648984066136, 1.986795982854316467 ) ) ;
#10748=CARTESIAN_POINT ( 'NONE',  ( 0.7185039370078746268, -0.06523048226347956391, 1.724901574803149540 ) ) ;
#10749=( BOUNDED_CURVE ( )  B_SPLINE_CURVE ( 2, ( #30675, #12460, #19617, #31380, #4752, #23470, #41153, #34482, #15813 ),
 .UNSPECIFIED., .F., .T. ) 
 B_SPLINE_CURVE_WITH_KNOTS ( ( 3, 2, 2, 2, 3 ),
 ( 0.6300000000000000044, 0.6324999999999999512, 0.6350000000000000089, 0.6374999999999999556, 0.6400000000000000133 ),
 .UNSPECIFIED. ) 
 CURVE ( )  GEOMETRIC_REPRESENTATION_ITEM ( )  RATIONAL_B_SPLINE_CURVE ( ( 1.000000000000000000, 0.9238795325112869605, 1.000000000000000000, 0.9238795325112869605, 1.000000000000000000, 0.9238795325112869605, 1.000000000000000000, 0.9238795325112869605, 1.000000000000000000 ) ) 
 REPRESENTATION_ITEM ( '' )  ) ;
#10751=CARTESIAN_POINT ( 'NONE',  ( 0.8759842519685039353, -0.1787899950787401882, 0.6028543306548976854 ) ) ;
#10756=CARTESIAN_POINT ( 'NONE',  ( 0.9873396505805591694, -0.1113553986120547346, 0.7135826771653542844 ) ) ;
#10757=CARTESIAN_POINT ( 'NONE',  ( 0.9500414927467378812, -0.1787899950787401604, 0.9202755904974182499 ) ) ;
#10763=CARTESIAN_POINT ( 'NONE',  ( -1.054774247047244540, 0.07405724077823318263, 0.1427165353793072855 ) ) ;
#10767=CARTESIAN_POINT ( 'NONE',  ( -0.6971942568897648851, 0.07405724077823318263, 1.973425196796630088 ) ) ;
#10768=CARTESIAN_POINT ( 'NONE',  ( -1.002407869896990045, -0.1264236179284866091, 1.710137795221826851 ) ) ;
#10769=CARTESIAN_POINT ( 'NONE',  ( -0.8019270111902717657, 0.1787899950787401604, 0.3937007873478115538 ) ) ;
#10770=( BOUNDED_CURVE ( )  B_SPLINE_CURVE ( 2, ( #11863, #44646, #18564, #15706, #33451, #4884, #800, #4639, #345 ),
 .UNSPECIFIED., .F., .T. ) 
 B_SPLINE_CURVE_WITH_KNOTS ( ( 3, 2, 2, 2, 3 ),
 ( 0.8800000000000000044, 0.8824999999999999512, 0.8850000000000000089, 0.8874999999999999556, 0.8900000000000000133 ),
 .UNSPECIFIED. ) 
 CURVE ( )  GEOMETRIC_REPRESENTATION_ITEM ( )  RATIONAL_B_SPLINE_CURVE ( ( 1.000000000000000000, 0.9238795325112869605, 1.000000000000000000, 0.9238795325112869605, 1.000000000000000000, 0.9238795325112869605, 1.000000000000000000, 0.9238795325112869605, 1.000000000000000000 ) ) 
 REPRESENTATION_ITEM ( '' )  ) ;
#10771=CARTESIAN_POINT ( 'NONE',  ( -0.7185039370078739607, 1.928577636452523993E-17, 0.6594488188976378451 ) ) ;
#10773=CARTESIAN_POINT ( 'NONE',  ( -1.033464566929134687, -0.06523048226347956391, 1.857775590551181244 ) ) ;
#10780=AXIS2_PLACEMENT_3D ( 'NONE', #6314, #2718, #6561 ) ;
#10781=CARTESIAN_POINT ( 'NONE',  ( -0.9500414927467378812, 0.1787899950787401604, 0.1870078739619845387 ) ) ;
#10782=ORIENTED_EDGE ( 'NONE', *, *, #6811, .F. ) ;
#10783=CARTESIAN_POINT ( 'NONE',  ( -1.002407869896990045, 0.1264236179284866091, 1.409940944828126153 ) ) ;
#10790=CARTESIAN_POINT ( 'NONE',  ( 0.9873396505805591694, 0.1113553986120547346, 0.3690944881889763884 ) ) ;
#10792=CARTESIAN_POINT ( 'NONE',  ( 0.8759842519685039353, 0.000000000000000000, 4.498031496062992574 ) ) ;
#10793=CARTESIAN_POINT ( 'NONE',  ( -0.8759842519685039353, -0.1574803149606299191, 0.9744094487113701408 ) ) ;
#10794=EDGE_CURVE ( 'NONE', #19295, #9411, #5861, .T. ) ;
#10796=CARTESIAN_POINT ( 'NONE',  ( 0.7185039370078746268, 0.06523048226347956391, 1.749507873908222155 ) ) ;
#10797=VERTEX_POINT ( 'NONE', #14274 ) ;
#10798=CARTESIAN_POINT ( 'NONE',  ( 0.7185039370078739607, 1.928577636452523993E-17, 0.2165354329633393804 ) ) ;
#10799=CARTESIAN_POINT ( 'NONE',  ( 0.8759842519685039353, -0.1574803149606299191, 0.7874015748031496509 ) ) ;
#10802=DIRECTION ( 'NONE',  ( -1.000000000000000000, 0.000000000000000000, 0.000000000000000000 ) ) ;
#10804=CARTESIAN_POINT ( 'NONE',  ( 0.8107537697050234415, -0.1574803149606297803, 0.1451771652468037688 ) ) ;
#10807=CARTESIAN_POINT ( 'NONE',  ( -0.7185039370078746268, -0.06523048226347956391, 0.7701771652468031304 ) ) ;
#10810=CARTESIAN_POINT ( 'NONE',  ( -0.8759842519685039353, 0.1574803149606299191, 0.08858267705782735257 ) ) ;
#10813=CARTESIAN_POINT ( 'NONE',  ( 0.9873396505805591694, -0.1113553986120547346, 0.9793307085538898171 ) ) ;
#10814=CARTESIAN_POINT ( 'NONE',  ( -0.7495606340400177148, 0.1264236179284866091, 0.4306102361667086820 ) ) ;
#10815=VERTEX_POINT ( 'NONE', #21440 ) ;
#10817=CARTESIAN_POINT ( 'NONE',  ( -0.7495606340400177148, -0.1264236179284866091, 1.626476377898992132 ) ) ;
#10820=CARTESIAN_POINT ( 'NONE',  ( -0.6971942568897626646, 0.07405724077823318263, 0.7923228345919055560 ) ) ;
#10822=CARTESIAN_POINT ( 'NONE',  ( -0.9500414927467377701, -0.1787899950787401604, 0.7627952755367883864 ) ) ;
#10824=CARTESIAN_POINT ( 'NONE',  ( -0.8759842519685039353, 0.000000000000000000, 0.000000000000000000 ) ) ;
#10826=CARTESIAN_POINT ( 'NONE',  ( -0.7646288533564489232, 0.1113553986120547346, 1.904527558947590515 ) ) ;
#10828=CARTESIAN_POINT ( 'NONE',  ( -0.9873396505805591694, -0.1113553986120547346, 1.500984251968503935 ) ) ;
#10829=CARTESIAN_POINT ( 'NONE',  ( -0.9873396505805591694, 0.1113553986120547346, 0.4478346456692913202 ) ) ;
#10830=CARTESIAN_POINT ( 'NONE',  ( 1.002407869896990045, 0.1264236179284866091, 1.409940944828126153 ) ) ;
#10835=DIRECTION ( 'NONE',  ( 1.000000000000000000, 0.000000000000000000, 0.000000000000000000 ) ) ;
#10837=AXIS2_PLACEMENT_3D ( 'NONE', #34188, #41795, #8994 ) ;
#10839=ADVANCED_FACE ( 'NONE', ( #21929 ), #14502, .T. ) ;
#10840=VECTOR ( 'NONE', #2796, 39.37007874015748143 ) ;
#10841=DIRECTION ( 'NONE',  ( 1.822029033848725028E-16, 0.000000000000000000, 1.000000000000000000 ) ) ;
#10844=CARTESIAN_POINT ( 'NONE',  ( 0.7185039370078739607, 1.928577636452523993E-17, 1.053149606299212504 ) ) ;
#10845=CARTESIAN_POINT ( 'NONE',  ( -1.033464566929133799, 1.928577636452524610E-17, 2.869337061179095023E-17 ) ) ;
#10846=CARTESIAN_POINT ( 'NONE',  ( 1.054774247047244096, 0.000000000000000000, 1.754429133804503715 ) ) ;
#10847=CARTESIAN_POINT ( 'NONE',  ( 0.7495606340400177148, -0.1264236179284866091, 0.3617125983714334359 ) ) ;
#10849=EDGE_CURVE ( 'NONE', #36693, #45011, #930, .T. ) ;
#10853=LINE ( 'NONE', #25466, #1977 ) ;
#10855=CARTESIAN_POINT ( 'NONE',  ( 0.8759842519685039353, 0.1787899950787401882, 0.5831692912848189803 ) ) ;
#10856=CARTESIAN_POINT ( 'NONE',  ( -0.9418700712360449367, 0.1575712691376264796, 0.03937007874015843734 ) ) ;
#10859=CARTESIAN_POINT ( 'NONE',  ( 0.7495606340400177148, 0.1264236179284866091, 1.734744094434425232 ) ) ;
#10861=CARTESIAN_POINT ( 'NONE',  ( 1.033464566929134687, 0.06523048226347956391, 0.1205708660342053040 ) ) ;
#10862=ORIENTED_EDGE ( 'NONE', *, *, #15795, .T. ) ;
#10863=CARTESIAN_POINT ( 'NONE',  ( 0.8759842519685039353, -0.1574803149606299191, 1.328740157372787278 ) ) ;
#10865=CARTESIAN_POINT ( 'NONE',  ( -1.054774247047244096, 0.000000000000000000, 0.4207677164816693294 ) ) ;
#10866=CARTESIAN_POINT ( 'NONE',  ( 0.9873396505805591694, 0.1113553986120547346, 0.4773622046168818911 ) ) ;
#10868=FACE_OUTER_BOUND ( 'NONE', #7726, .T. ) ;
#10871=CARTESIAN_POINT ( 'NONE',  ( -0.8759842519685039353, 0.1787899950787401882, 1.528051181048598384 ) ) ;
#10874=CARTESIAN_POINT ( 'NONE',  ( 1.054774247047244096, 0.000000000000000000, 1.090059055064346527 ) ) ;
#10876=VECTOR ( 'NONE', #14988, 39.37007874015748143 ) ;
#10877=CARTESIAN_POINT ( 'NONE',  ( 0.9500414927467378812, 0.1787899950787401604, 1.761811023568284007 ) ) ;
#10878=CARTESIAN_POINT ( 'NONE',  ( -0.7185039370078746268, -0.06523048226347956391, 0.6225393700787401619 ) ) ;
#10879=CARTESIAN_POINT ( 'NONE',  ( -0.8759842519685039353, 0.1787899950787401882, 1.094980314906866203 ) ) ;
#10882=CARTESIAN_POINT ( 'NONE',  ( 1.054774247047244540, 0.07405724077823318263, 0.2657480314422993595 ) ) ;
#10883=CARTESIAN_POINT ( 'NONE',  ( -0.6971942568897637749, 2.189545951927499583E-17, 0.2386811023084413619 ) ) ;
#10884=CARTESIAN_POINT ( 'NONE',  ( -1.054774247047244540, -0.07405724077823318263, 0.7283464566391493200 ) ) ;
#10885=CARTESIAN_POINT ( 'NONE',  ( 0.9412147342319837628, -0.1574803149606297803, 1.646161417215307843 ) ) ;
#10887=( BOUNDED_CURVE ( )  B_SPLINE_CURVE ( 2, ( #20483, #32237, #28895, #2956, #314, #10659, #71, #7509, #10425 ),
 .UNSPECIFIED., .F., .T. ) 
 B_SPLINE_CURVE_WITH_KNOTS ( ( 3, 2, 2, 2, 3 ),
 ( 0.4799999999999999822, 0.4824999999999999845, 0.4849999999999999867, 0.4874999999999999889, 0.4899999999999999911 ),
 .UNSPECIFIED. ) 
 CURVE ( )  GEOMETRIC_REPRESENTATION_ITEM ( )  RATIONAL_B_SPLINE_CURVE ( ( 1.000000000000000000, 0.9238795325112869605, 1.000000000000000000, 0.9238795325112869605, 1.000000000000000000, 0.9238795325112869605, 1.000000000000000000, 0.9238795325112869605, 1.000000000000000000 ) ) 
 REPRESENTATION_ITEM ( '' )  ) ;
#10889=CARTESIAN_POINT ( 'NONE',  ( 0.6971942568897626646, 0.07405724077823318263, 0.7923228345919055560 ) ) ;
#10890=CARTESIAN_POINT ( 'NONE',  ( 0.9500414927467377701, -0.1787899950787401604, 1.003937007820253413 ) ) ;
#10891=CARTESIAN_POINT ( 'NONE',  ( -0.6971942568897637749, 2.189545951927499583E-17, 1.813484251914740053 ) ) ;
#10892=CARTESIAN_POINT ( 'NONE',  ( 0.9500414927467378812, -0.1787899950787401604, 1.865157480261195877 ) ) ;
#10893=LINE ( 'NONE', #25259, #21384 ) ;
#10899=CARTESIAN_POINT ( 'NONE',  ( 0.9500414927467378812, 0.1787899950787401604, 1.171259842465921741 ) ) ;
#10901=CARTESIAN_POINT ( 'NONE',  ( -0.9873396505805591694, -0.1113553986120547346, 1.215551180994834723 ) ) ;
#10904=CIRCLE ( 'NONE', #7825, 0.1574803149606300579 ) ;
#10905=CARTESIAN_POINT ( 'NONE',  ( 0.8759842519685039353, -0.1787899950787401882, 1.508366141678519678 ) ) ;
#10906=CARTESIAN_POINT ( 'NONE',  ( 0.7495606340400177148, -0.1264236179284866091, 0.08612204719033110523 ) ) ;
#10909=EDGE_CURVE ( 'NONE', #38992, #6537, #19020, .T. ) ;
#10910=CARTESIAN_POINT ( 'NONE',  ( -0.7495606340400177148, -0.1264236179284866091, 0.5241141731745827537 ) ) ;
#10912=CARTESIAN_POINT ( 'NONE',  ( -0.7646288533564489232, 0.1113553986120547346, 1.205708661417322913 ) ) ;
#10913=CARTESIAN_POINT ( 'NONE',  ( 0.8019270111902717657, -0.1787899950787401604, 1.156496062938362046 ) ) ;
#10914=CARTESIAN_POINT ( 'NONE',  ( 0.9500414927467377701, -0.1787899950787401604, 1.668307086560410157 ) ) ;
#10915=CARTESIAN_POINT ( 'NONE',  ( -0.7646288533564489232, 0.1113553986120547346, 0.6446850392625511628 ) ) ;
#10916=CARTESIAN_POINT ( 'NONE',  ( -0.7185039370078746268, 0.06523048226347956391, 1.011318897637796033 ) ) ;
#10919=CARTESIAN_POINT ( 'NONE',  ( -0.8759842519685039353, 0.1574803149606299191, 1.781496062884598164 ) ) ;
#10920=CARTESIAN_POINT ( 'NONE',  ( 0.9500414927467378812, 0.1787899950787401604, 0.1476377952218271561 ) ) ;
#10921=CARTESIAN_POINT ( 'NONE',  ( 0.7125016681442003508, -0.05105472478026783223, 0.03937008547748529347 ) ) ;
#10923=CARTESIAN_POINT ( 'NONE',  ( 0.8759842519685039353, 0.000000000000000000, 4.498031496062992574 ) ) ;
#10924=CARTESIAN_POINT ( 'NONE',  ( -1.054774247047244096, 0.000000000000000000, 1.242618110182456714 ) ) ;
#10925=CARTESIAN_POINT ( 'NONE',  ( 0.7185039370078739607, 1.928577636452523993E-17, 0.4527559054042842868 ) ) ;
#10926=VERTEX_POINT ( 'NONE', #11626 ) ;
#10927=CARTESIAN_POINT ( 'NONE',  ( 0.8689611821192279040, 0.1748045417376594690, 0.03936951059370389500 ) ) ;
#10928=CARTESIAN_POINT ( 'NONE',  ( 0.8107537697050254399, 0.1574803149606300301, 0.8390748030420788206 ) ) ;
#10929=CARTESIAN_POINT ( 'NONE',  ( -0.8107537697050253289, 0.1574803149606300301, 0.4453740156405042727 ) ) ;
#10931=CARTESIAN_POINT ( 'NONE',  ( 1.002407869896990045, 0.1264236179284866091, 1.405019684985606476 ) ) ;
#10932=CARTESIAN_POINT ( 'NONE',  ( -1.033464566929133799, 0.000000000000000000, 1.151574803149606474 ) ) ;
#10933=CARTESIAN_POINT ( 'NONE',  ( -0.8759842519685039353, 0.1574803149606299191, 0.09842519685039370636 ) ) ;
#10934=CARTESIAN_POINT ( 'NONE',  ( -0.7646288533564489232, -0.1113553986120547346, 1.373031496062992352 ) ) ;
#10936=ORIENTED_EDGE ( 'NONE', *, *, #27522, .T. ) ;
#10938=VECTOR ( 'NONE', #5855, 39.37007874015748143 ) ;
#10940=LINE ( 'NONE', #25558, #45112 ) ;
#10942=CARTESIAN_POINT ( 'NONE',  ( 0.7495606340400177148, -0.1264236179284866091, 0.5634842519147401640 ) ) ;
#10944=CARTESIAN_POINT ( 'NONE',  ( -0.9500414927467377701, 0.1787899950787401604, 1.446850393647023836 ) ) ;
#10946=CARTESIAN_POINT ( 'NONE',  ( -0.6971942568897648851, -0.07405724077823297447, 1.151574803095843036 ) ) ;
#10948=CARTESIAN_POINT ( 'NONE',  ( -0.9500414927467378812, 0.1787899950787401604, 0.8612204723871809131 ) ) ;
#10949=CARTESIAN_POINT ( 'NONE',  ( -0.6971942568897626646, 0.07405724077823318263, 0.1624015747493861295 ) ) ;
#10950=CARTESIAN_POINT ( 'NONE',  ( 1.033464566929134687, 0.06523048226347956391, 0.7898622046168821687 ) ) ;
#10955=DIRECTION ( 'NONE',  ( 1.822029033848725028E-16, 0.000000000000000000, 1.000000000000000000 ) ) ;
#10956=ORIENTED_EDGE ( 'NONE', *, *, #429, .T. ) ;
#10959=CARTESIAN_POINT ( 'NONE',  ( -0.7495606340400177148, 0.1264236179284866091, 0.7849409448281259305 ) ) ;
#10961=ORIENTED_EDGE ( 'NONE', *, *, #7573, .F. ) ;
#10962=CARTESIAN_POINT ( 'NONE',  ( -0.6971942568897637749, 2.189545951927499583E-17, 1.857775590497417362 ) ) ;
#10963=EDGE_CURVE ( 'NONE', #44204, #47215, #32163, .T. ) ;
#10964=CIRCLE ( 'NONE', #16232, 0.1574803149606299191 ) ;
#10965=CARTESIAN_POINT ( 'NONE',  ( -1.054774247047244540, -0.07405724077823318263, 0.06397637789899228433 ) ) ;
#10966=CARTESIAN_POINT ( 'NONE',  ( 0.9412147342319837628, -0.1574803149606297803, 0.7111220472440957785 ) ) ;
#10969=CARTESIAN_POINT ( 'NONE',  ( -0.7185039370078739607, 1.928577636452523993E-17, 1.515748031388535200 ) ) ;
#10970=CARTESIAN_POINT ( 'NONE',  ( 0.6971942568897626646, 0.07405724077823318263, 0.8316929133320636325 ) ) ;
#10971=CARTESIAN_POINT ( 'NONE',  ( 1.002407869896990045, 0.1264236179284866091, 1.365649606245448844 ) ) ;
#10974=DIRECTION ( 'NONE',  ( 0.000000000000000000, 0.000000000000000000, -1.000000000000000000 ) ) ;
#10976=CARTESIAN_POINT ( 'NONE',  ( 0.9873396505805591694, 0.1113553986120547346, 1.471456692913385877 ) ) ;
#10977=CARTESIAN_POINT ( 'NONE',  ( 0.8206978720991248144, -0.1637064837517050730, 1.987174065507188780 ) ) ;
#10979=FACE_OUTER_BOUND ( 'NONE', #18165, .T. ) ;
#10981=CARTESIAN_POINT ( 'NONE',  ( 0.8759842519685039353, 0.1787899950787401882, 0.7406496062454487328 ) ) ;
#10984=VERTEX_POINT ( 'NONE', #22869 ) ;
#10987=CARTESIAN_POINT ( 'NONE',  ( 0.8759842519685039353, -0.1787899950787401882, 0.9965551180564724554 ) ) ;
#10988=DIRECTION ( 'NONE',  ( 1.000000000000000000, 0.000000000000000000, -1.822029033848725275E-16 ) ) ;
#10992=ORIENTED_EDGE ( 'NONE', *, *, #33424, .T. ) ;
#10993=CARTESIAN_POINT ( 'NONE',  ( -0.9500414927467378812, 0.1787899950787401604, 0.1082677164816695514 ) ) ;
#10995=ORIENTED_EDGE ( 'NONE', *, *, #5952, .T. ) ;
#10996=CARTESIAN_POINT ( 'NONE',  ( -0.8019270111902716547, 0.1787899950787401604, 1.968503936954110412 ) ) ;
#10997=CARTESIAN_POINT ( 'NONE',  ( -0.7495606340400177148, -0.1264236179284866091, 1.739665354276945131 ) ) ;
#10998=CARTESIAN_POINT ( 'NONE',  ( -0.9500414927467378812, 0.1787899950787401604, 1.092519684985605810 ) ) ;
#10999=CARTESIAN_POINT ( 'NONE',  ( -1.002407869896990045, 0.1264236179284866091, 0.3469488188438744070 ) ) ;
#11002=CARTESIAN_POINT ( 'NONE',  ( 1.002407869896990045, 0.1264236179284866091, 0.06643700782025216411 ) ) ;
#11003=CARTESIAN_POINT ( 'NONE',  ( -1.033464566929133799, 0.000000000000000000, 0.5610236220472440971 ) ) ;
#11006=CARTESIAN_POINT ( 'NONE',  ( 0.8759842519685039353, 0.000000000000000000, 4.498031496062992574 ) ) ;
#11007=CARTESIAN_POINT ( 'NONE',  ( -1.002407869896990045, -0.1264236179284866091, 0.2534448818360003908 ) ) ;
#11011=CARTESIAN_POINT ( 'NONE',  ( -1.054774247047244096, 0.000000000000000000, 1.405019684985606476 ) ) ;
#11012=ORIENTED_EDGE ( 'NONE', *, *, #9538, .T. ) ;
#11013=EDGE_CURVE ( 'NONE', #27525, #45154, #4176, .T. ) ;
#11016=( BOUNDED_CURVE ( )  B_SPLINE_CURVE ( 2, ( #1860, #27544, #9301, #12681, #45457, #23922, #2096, #23680, #38530 ),
 .UNSPECIFIED., .F., .F. ) 
 B_SPLINE_CURVE_WITH_KNOTS ( ( 3, 2, 2, 2, 3 ),
 ( 0.4699999999999999734, 0.4724999999999999756, 0.4749999999999999778, 0.4774999999999999800, 0.4799999999999999822 ),
 .UNSPECIFIED. ) 
 CURVE ( )  GEOMETRIC_REPRESENTATION_ITEM ( )  RATIONAL_B_SPLINE_CURVE ( ( 1.000000000000000000, 0.9238795325112879597, 1.000000000000000000, 0.9238795325112869605, 1.000000000000000000, 0.9238795325112869605, 1.000000000000000000, 0.9238795325112869605, 1.000000000000000000 ) ) 
 REPRESENTATION_ITEM ( '' )  ) ;
#11017=EDGE_CURVE ( 'NONE', #37016, #480, #2744, .T. ) ;
#11021=CARTESIAN_POINT ( 'NONE',  ( 1.002407869896990045, 0.1264236179284866091, 0.4256889763241890057 ) ) ;
#11024=CARTESIAN_POINT ( 'NONE',  ( 0.8107537697050253289, 0.1574803149606300301, 1.823326771546016856 ) ) ;
#11027=CARTESIAN_POINT ( 'NONE',  ( 0.7646288533564489232, -0.1113553986120547346, 0.2214566928058590567 ) ) ;
#11028=CARTESIAN_POINT ( 'NONE',  ( 0.9873396505805591694, -0.1113553986120547346, 0.7923228346456693272 ) ) ;
#11032=CARTESIAN_POINT ( 'NONE',  ( 0.9412147342319837628, -0.1574803149606297803, 0.7898622047244097111 ) ) ;
#11035=ORIENTED_EDGE ( 'NONE', *, *, #30144, .T. ) ;
#11036=VERTEX_POINT ( 'NONE', #7322 ) ;
#11038=CARTESIAN_POINT ( 'NONE',  ( 0.9873396505805591694, -0.1113553986120547346, 1.382874015748031704 ) ) ;
#11042=CARTESIAN_POINT ( 'NONE',  ( -0.7646288533564489232, -0.1113553986120547346, 0.06397637784522892945 ) ) ;
#11044=CARTESIAN_POINT ( 'NONE',  ( 0.8107537697050253289, 0.1574803149606300301, 0.9178149605223947516 ) ) ;
#11045=( BOUNDED_CURVE ( )  B_SPLINE_CURVE ( 2, ( #41426, #23261, #37876, #19651, #27357, #1420, #16079, #3320, #35913 ),
 .UNSPECIFIED., .F., .F. ) 
 B_SPLINE_CURVE_WITH_KNOTS ( ( 3, 2, 2, 2, 3 ),
 ( 0.1400000000000000133, 0.1424999999999999878, 0.1449999999999999900, 0.1474999999999999922, 0.1499999999999999944 ),
 .UNSPECIFIED. ) 
 CURVE ( )  GEOMETRIC_REPRESENTATION_ITEM ( )  RATIONAL_B_SPLINE_CURVE ( ( 1.000000000000000000, 0.9238795325112869605, 1.000000000000000000, 0.9238795325112869605, 1.000000000000000000, 0.9238795325112869605, 1.000000000000000000, 0.9238795325112869605, 1.000000000000000000 ) ) 
 REPRESENTATION_ITEM ( '' )  ) ;
#11047=CARTESIAN_POINT ( 'NONE',  ( -1.054774247047244540, -0.07405724077823318263, 0.4133858267178901480 ) ) ;
#11048=ORIENTED_EDGE ( 'NONE', *, *, #34881, .F. ) ;
#11051=COLOUR_RGB ( '', 0.40784314, 0.44705882, 0.49803922) ;
#11052=CARTESIAN_POINT ( 'NONE',  ( -0.9500414927467378812, -0.1787899950787401604, 1.555118110182455382 ) ) ;
#11053=CARTESIAN_POINT ( 'NONE',  ( 0.7495606340400177148, 0.1264236179284866091, 1.734744094434425232 ) ) ;
#11054=CARTESIAN_POINT ( 'NONE',  ( -1.054774247047244540, 0.07405724077823318263, 0.8562992125446617919 ) ) ;
#11055=CARTESIAN_POINT ( 'NONE',  ( 0.7495606340400177148, 0.1264236179284866091, 0.3174212597887562382 ) ) ;
#11056=CARTESIAN_POINT ( 'NONE',  ( -0.7646288533564489232, -0.1113553986120547346, 1.678149606191684962 ) ) ;
#11057=CARTESIAN_POINT ( 'NONE',  ( 0.8019270111902716547, -0.1787899950787401604, 0.7627952755367883864 ) ) ;
#11058=CARTESIAN_POINT ( 'NONE',  ( -1.054774247047244540, -0.07405724077823318263, 0.7283464566391492090 ) ) ;
#11060=CARTESIAN_POINT ( 'NONE',  ( -1.054774247047244540, -0.07405724077823318263, 1.520669291284818758 ) ) ;
#11061=CARTESIAN_POINT ( 'NONE',  ( -0.9412147342319837628, 0.1574803149606300301, 1.936515747923967856 ) ) ;
#11063=CARTESIAN_POINT ( 'NONE',  ( -0.7185039370078746268, -0.06523048226347956391, 1.606791338582677309 ) ) ;
#11066=CARTESIAN_POINT ( 'NONE',  ( 1.002407869896990045, -0.1264236179284866091, 1.518208661363559031 ) ) ;
#11067=CYLINDRICAL_SURFACE ( 'NONE', #17946, 0.1574803149606299191 ) ;
#11069=ORIENTED_EDGE ( 'NONE', *, *, #17254, .T. ) ;
#11071=ORIENTED_EDGE ( 'NONE', *, *, #45879, .F. ) ;
#11077=CARTESIAN_POINT ( 'NONE',  ( 0.9412147342319837628, 0.1574803149606300301, 1.040846456692913424 ) ) ;
#11084=CARTESIAN_POINT ( 'NONE',  ( 1.054774247047244540, -0.07405724077823318263, 0.6889763778989935750 ) ) ;
#11085=CARTESIAN_POINT ( 'NONE',  ( 0.8759842519685039353, 0.000000000000000000, 4.498031496062992574 ) ) ;
#11087=CARTESIAN_POINT ( 'NONE',  ( 0.8759842519685039353, 0.000000000000000000, 4.498031496062992574 ) ) ;
#11088=CARTESIAN_POINT ( 'NONE',  ( -0.8731188658399394731, -0.1744580357768550638, 1.988137801528226278 ) ) ;
#11089=CARTESIAN_POINT ( 'NONE',  ( -1.033464566929133799, 0.000000000000000000, 1.141732283357039357 ) ) ;
#11090=CARTESIAN_POINT ( 'NONE',  ( 1.054774247047244540, -0.07405724077823318263, 1.796259842465923073 ) ) ;
#11095=CARTESIAN_POINT ( 'NONE',  ( -0.7495606340400177148, 0.1264236179284866091, 0.4749015747493858242 ) ) ;
#11099=CARTESIAN_POINT ( 'NONE',  ( 1.002407869896990045, -0.1264236179284866091, 0.5684055117572598403 ) ) ;
#11100=CARTESIAN_POINT ( 'NONE',  ( -1.054774247047244540, 0.07405724077823318263, 1.560039370024977057 ) ) ;
#11103=CARTESIAN_POINT ( 'NONE',  ( -1.002407869896990045, -0.1264236179284866091, 1.203248031442299304 ) ) ;
#11104=CARTESIAN_POINT ( 'NONE',  ( -0.7185039370078739607, 1.928577636452523993E-17, 0.8956692913385826404 ) ) ;
#11105=CARTESIAN_POINT ( 'NONE',  ( 1.054774247047244540, -0.07405724077823318263, 1.126968503883244654 ) ) ;
#11107=CARTESIAN_POINT ( 'NONE',  ( 0.8019270111902717657, -0.1787899950787401604, 1.978346456639149320 ) ) ;
#11108=CARTESIAN_POINT ( 'NONE',  ( -1.033464566929134687, -0.06523048226347956391, 0.5585629921259840369 ) ) ;
#11109=CARTESIAN_POINT ( 'NONE',  ( -0.6971942568897648851, 0.07405724077823318263, 1.062992125930488418 ) ) ;
#11113=CARTESIAN_POINT ( 'NONE',  ( 1.002407869896990045, -0.1264236179284866091, 0.2583661416785200671 ) ) ;
#11114=CARTESIAN_POINT ( 'NONE',  ( -0.9500414927467377701, 0.1787899950787401604, 0.2263779527021421711 ) ) ;
#11116=CARTESIAN_POINT ( 'NONE',  ( -0.6971942568897626646, 0.07405724077823318263, 0.7086614172690703928 ) ) ;
#11117=VERTEX_POINT ( 'NONE', #11638 ) ;
#11121=CARTESIAN_POINT ( 'NONE',  ( 0.6971942568897626646, -0.07405724077823297447, 0.7972440944344250102 ) ) ;
#11123=CARTESIAN_POINT ( 'NONE',  ( 0.7495606340400177148, 0.1264236179284866091, 1.065452755851747924 ) ) ;
#11124=CARTESIAN_POINT ( 'NONE',  ( -1.002407869896990045, 0.1264236179284866091, 1.877460629867496067 ) ) ;
#11128=VERTEX_POINT ( 'NONE', #5126 ) ;
#11131=CARTESIAN_POINT ( 'NONE',  ( 0.8019270111902717657, 0.1787899950787401604, 1.215551181048599272 ) ) ;
#11134=CARTESIAN_POINT ( 'NONE',  ( 0.9500414927467378812, -0.1787899950787401604, 0.09350393695411057804 ) ) ;
#11139=CARTESIAN_POINT ( 'NONE',  ( -0.9500414927467377701, -0.1787899950787401604, 0.5708661416785200116 ) ) ;
#11143=CARTESIAN_POINT ( 'NONE',  ( 1.054774247047244540, -0.07405724077823318263, 1.284448818843874740 ) ) ;
#11144=CARTESIAN_POINT ( 'NONE',  ( 0.9500414927467377701, 0.1787899950787401604, 1.643700787347811998 ) ) ;
#11145=FACE_OUTER_BOUND ( 'NONE', #4052, .T. ) ;
#11146=CARTESIAN_POINT ( 'NONE',  ( 0.7185039370078739607, 1.928577636452523993E-17, 0.8858267715460158565 ) ) ;
#11148=CARTESIAN_POINT ( 'NONE',  ( -0.7185039370078739607, 1.928577636452523993E-17, 0.6496062991050708391 ) ) ;
#11150=CARTESIAN_POINT ( 'NONE',  ( 1.002407869896990045, 0.1264236179284866091, 0.2632874015210397434 ) ) ;
#11152=CARTESIAN_POINT ( 'NONE',  ( 0.7021184280059326044, 0.02911167292124897457, 0.03937009334504424501 ) ) ;
#11153=CARTESIAN_POINT ( 'NONE',  ( 0.6971942568897648851, 0.07405724077823318263, 1.259842519631276359 ) ) ;
#11156=CARTESIAN_POINT ( 'NONE',  ( -0.7185039370078739607, 1.928577636452523993E-17, 1.053149606299212504 ) ) ;
#11157=CARTESIAN_POINT ( 'NONE',  ( -0.9500414927467378812, 0.1787899950787401604, 1.249999999946235896 ) ) ;
#11158=CARTESIAN_POINT ( 'NONE',  ( 0.8759842519685039353, -0.1574803149606299191, 0.6200787400499527813 ) ) ;
#11161=CARTESIAN_POINT ( 'NONE',  ( 0.9647019635636798762, 0.1432196322012359857, 0.03937007870177667429 ) ) ;
#11162=CARTESIAN_POINT ( 'NONE',  ( 0.9412147342319837628, 0.1574803149606300301, 0.8341535431995593664 ) ) ;
#11163=CARTESIAN_POINT ( 'NONE',  ( -0.7646288533564489232, 0.1113553986120547346, 1.117125984144440975 ) ) ;
#11164=CARTESIAN_POINT ( 'NONE',  ( 0.6971942568897648851, -0.07405724077823297447, 1.500984251914741607 ) ) ;
#11165=CARTESIAN_POINT ( 'NONE',  ( -0.8759842519685039353, -0.1574803149606299191, 1.141732283464567121 ) ) ;
#11166=AXIS2_PLACEMENT_3D ( 'NONE', #16288, #27331, #10988 ) ;
#11167=EDGE_CURVE ( 'NONE', #31032, #13663, #4277, .T. ) ;
#11170=CARTESIAN_POINT ( 'NONE',  ( -0.7185039370078739607, 1.928577636452523993E-17, 0.1082677165354330728 ) ) ;
#11173=CARTESIAN_POINT ( 'NONE',  ( 0.7646288533564489232, -0.1113553986120547346, 0.6545275589475906264 ) ) ;
#11174=EDGE_CURVE ( 'NONE', #37198, #21900, #44042, .T. ) ;
#11175=CARTESIAN_POINT ( 'NONE',  ( -0.8759842519685039353, 0.000000000000000000, 0.000000000000000000 ) ) ;
#11177=CARTESIAN_POINT ( 'NONE',  ( 0.7495606340400177148, -0.1264236179284866091, 0.6028543306548976854 ) ) ;
#11178=ORIENTED_EDGE ( 'NONE', *, *, #19255, .T. ) ;
#11180=CARTESIAN_POINT ( 'NONE',  ( -0.8019270111902716547, -0.1787899950787401604, 1.466535433017102763 ) ) ;
#11182=CARTESIAN_POINT ( 'NONE',  ( -0.6971942568897648851, -0.07405724077823297447, 1.190944881836001112 ) ) ;
#11185=CARTESIAN_POINT ( 'NONE',  ( 0.7185039370078739607, 1.928577636452523993E-17, 1.318897637687747926 ) ) ;
#11187=CARTESIAN_POINT ( 'NONE',  ( -1.002407869896990045, 0.1264236179284866091, 0.8193897637257637756 ) ) ;
#11188=CARTESIAN_POINT ( 'NONE',  ( -0.6971942568897626646, -0.07405724077823297447, 0.2066929133320631329 ) ) ;
#11190=CARTESIAN_POINT ( 'NONE',  ( 0.8107537697050254399, 0.1574803149606300301, 0.7997047243019207441 ) ) ;
#11192=VERTEX_POINT ( 'NONE', #37494 ) ;
#11193=CARTESIAN_POINT ( 'NONE',  ( 0.8759842519685039353, -0.1574803149606299191, 1.062992125984252079 ) ) ;
#11196=CARTESIAN_POINT ( 'NONE',  ( 0.9873396505805591694, -0.1113553986120547346, 1.215551180994834723 ) ) ;
#11197=CARTESIAN_POINT ( 'NONE',  ( -1.002407869896990045, 0.1264236179284866091, 0.8144685038832440993 ) ) ;
#11200=CARTESIAN_POINT ( 'NONE',  ( -1.054774247047244096, 0.000000000000000000, 0.1058070865604096300 ) ) ;
#11203=CARTESIAN_POINT ( 'NONE',  ( -0.9873396505805591694, 0.1113553986120547346, 1.579724409341291214 ) ) ;
#11204=CARTESIAN_POINT ( 'NONE',  ( 1.054774247047244540, 0.07405724077823318263, 0.6988188975840318173 ) ) ;
#11205=CARTESIAN_POINT ( 'NONE',  ( 0.9500414927467377701, 0.1787899950787401604, 1.328740157426552049 ) ) ;
#11207=CARTESIAN_POINT ( 'NONE',  ( 0.9873396505805591694, -0.1113553986120547346, 1.382874015748031704 ) ) ;
#11208=CARTESIAN_POINT ( 'NONE',  ( 0.8128431167288246995, -0.1605282852710551433, 1.987016390083011785 ) ) ;
#11210=CARTESIAN_POINT ( 'NONE',  ( 0.7646288533564489232, 0.1113553986120547346, 0.3297244093412917687 ) ) ;
#11212=CARTESIAN_POINT ( 'NONE',  ( 0.8019270111902716547, -0.1787899950787401604, 0.8759842519147408302 ) ) ;
#11217=CARTESIAN_POINT ( 'NONE',  ( 1.054774247047244540, -0.07405724077823318263, 0.9645669290800953366 ) ) ;
#11222=ORIENTED_EDGE ( 'NONE', *, *, #39112, .T. ) ;
#11223=DIRECTION ( 'NONE',  ( -1.000000000000000000, 0.000000000000000000, 0.000000000000000000 ) ) ;
#11224=CARTESIAN_POINT ( 'NONE',  ( -0.8759842519685039353, -0.1787899950787401882, 0.1304133857730082613 ) ) ;
#11226=CARTESIAN_POINT ( 'NONE',  ( 1.033464566929134687, 0.06523048226347956391, 0.3272637795275590289 ) ) ;
#11229=CARTESIAN_POINT ( 'NONE',  ( -0.9500414927467378812, -0.1787899950787401604, 1.668307086560410157 ) ) ;
#11230=CARTESIAN_POINT ( 'NONE',  ( -0.9500414927467377701, 0.1787899950787401604, 0.8956692912848198684 ) ) ;
#11231=EDGE_CURVE ( 'NONE', #33230, #22586, #27294, .T. ) ;
#11232=CARTESIAN_POINT ( 'NONE',  ( -1.054774247047244096, 0.000000000000000000, 0.3813976377415121966 ) ) ;
#11233=CARTESIAN_POINT ( 'NONE',  ( -0.8759842519685039353, -0.1574803149606299191, 0.1574803149606299191 ) ) ;
#11241=CARTESIAN_POINT ( 'NONE',  ( -0.8019270111902717657, 0.1787899950787401604, 0.2706692912848194243 ) ) ;
#11243=CARTESIAN_POINT ( 'NONE',  ( 0.8759842519685039353, 0.1574803149606299191, 0.8070866141732283561 ) ) ;
#11244=VERTEX_POINT ( 'NONE', #1293 ) ;
#11245=CARTESIAN_POINT ( 'NONE',  ( -0.7495606340400177148, 0.1264236179284866091, 1.419783464513165505 ) ) ;
#11248=EDGE_CURVE ( 'NONE', #30530, #1000, #6106, .T. ) ;
#11251=CARTESIAN_POINT ( 'NONE',  ( 1.033464566929134687, 0.06523048226347956391, 0.4060039370078741272 ) ) ;
#11254=CARTESIAN_POINT ( 'NONE',  ( -0.7185039370078739607, 1.928577636452523993E-17, 1.003937007766488199 ) ) ;
#11255=DIRECTION ( 'NONE',  ( 0.000000000000000000, 0.000000000000000000, -1.000000000000000000 ) ) ;
#11257=CARTESIAN_POINT ( 'NONE',  ( 0.8759842519685039353, -0.1574803149606299191, 1.919291338475149544 ) ) ;
#11258=ORIENTED_EDGE ( 'NONE', *, *, #40650, .T. ) ;
#11260=CARTESIAN_POINT ( 'NONE',  ( -0.7185039370078692977, 0.06523048226347515077, 1.434547243986962428 ) ) ;
#11261=CARTESIAN_POINT ( 'NONE',  ( 0.9412147342319837628, 0.1574803149606300301, 0.9621062992125994917 ) ) ;
#11263=CARTESIAN_POINT ( 'NONE',  ( -0.7185039370078739607, 1.928577636452523993E-17, 0.4625984251968504046 ) ) ;
#11266=EDGE_LOOP ( 'NONE', ( #34335, #4281, #26980, #17591 ) ) ;
#11273=CARTESIAN_POINT ( 'NONE',  ( 0.9873396505805591694, -0.1113553986120547346, 0.9005905510735748853 ) ) ;
#11276=CARTESIAN_POINT ( 'NONE',  ( -0.8759842519685039353, -0.1787899950787401882, 0.3666338582139531677 ) ) ;
#11280=CARTESIAN_POINT ( 'NONE',  ( -0.7495606340400177148, 0.1264236179284866091, 1.616633858213952779 ) ) ;
#11281=CARTESIAN_POINT ( 'NONE',  ( 0.8759842519685039353, 0.1787899950787401882, 1.651082677111590513 ) ) ;
#11284=CARTESIAN_POINT ( 'NONE',  ( -0.6971942568897626646, -0.07405724077823297447, 0.8759842519147408302 ) ) ;
#11285=DIRECTION ( 'NONE',  ( -1.000000000000000000, 0.000000000000000000, 0.000000000000000000 ) ) ;
#11286=CARTESIAN_POINT ( 'NONE',  ( -0.8759842519685039353, -0.1787899950787401882, 1.272145669237574772 ) ) ;
#11287=CARTESIAN_POINT ( 'NONE',  ( -1.002407869896990045, 0.1264236179284866091, 0.7750984251430865779 ) ) ;
#11288=CARTESIAN_POINT ( 'NONE',  ( 1.033464566929134687, 0.06523048226347956391, 0.9079724408373541777 ) ) ;
#11290=CARTESIAN_POINT ( 'NONE',  ( -0.9500414927467378812, -0.1787899950787401604, 1.594488188922613237 ) ) ;
#11291=CARTESIAN_POINT ( 'NONE',  ( -0.7185039370078739607, 1.928577636452523993E-17, 1.830708661309795149 ) ) ;
#11293=CARTESIAN_POINT ( 'NONE',  ( -0.9873396505805591694, 0.1113553986120547346, 1.628937007874015963 ) ) ;
#11295=CARTESIAN_POINT ( 'NONE',  ( 0.6971942568897648851, -0.07405724077823297447, 1.387795275536786610 ) ) ;
#11297=ORIENTED_EDGE ( 'NONE', *, *, #46777, .F. ) ;
#11298=( BOUNDED_CURVE ( )  B_SPLINE_CURVE ( 2, ( #23091, #37709, #26943, #34137, #43588, #35941, #17958, #28542, #2850 ),
 .UNSPECIFIED., .F., .T. ) 
 B_SPLINE_CURVE_WITH_KNOTS ( ( 3, 2, 2, 2, 3 ),
 ( 0.7900000000000000355, 0.7924999999999999822, 0.7950000000000000400, 0.7974999999999999867, 0.8000000000000000444 ),
 .UNSPECIFIED. ) 
 CURVE ( )  GEOMETRIC_REPRESENTATION_ITEM ( )  RATIONAL_B_SPLINE_CURVE ( ( 1.000000000000000000, 0.9238795325112899581, 1.000000000000000000, 0.9238795325112869605, 1.000000000000000000, 0.9238795325112869605, 1.000000000000000000, 0.9238795325112869605, 1.000000000000000000 ) ) 
 REPRESENTATION_ITEM ( '' )  ) ;
#11306=DIRECTION ( 'NONE',  ( 1.822029033848725028E-16, 0.000000000000000000, 1.000000000000000000 ) ) ;
#11312=CARTESIAN_POINT ( 'NONE',  ( 0.9500414927467378812, 0.1787899950787401604, 0.7381889763241898939 ) ) ;
#11314=( BOUNDED_CURVE ( )  B_SPLINE_CURVE ( 2, ( #6198, #13634, #28761, #10533, #24902, #25130, #6906, #36166, #13873 ),
 .UNSPECIFIED., .F., .T. ) 
 B_SPLINE_CURVE_WITH_KNOTS ( ( 3, 2, 2, 2, 3 ),
 ( 0.9499999999999999556, 0.9525000000000000133, 0.9549999999999999600, 0.9575000000000000178, 0.9599999999999999645 ),
 .UNSPECIFIED. ) 
 CURVE ( )  GEOMETRIC_REPRESENTATION_ITEM ( )  RATIONAL_B_SPLINE_CURVE ( ( 1.000000000000000000, 0.9238795325112899581, 1.000000000000000000, 0.9238795325112869605, 1.000000000000000000, 0.9238795325112869605, 1.000000000000000000, 0.9238795325112869605, 1.000000000000000000 ) ) 
 REPRESENTATION_ITEM ( '' )  ) ;
#11315=FACE_OUTER_BOUND ( 'NONE', #43752, .T. ) ;
#11316=CARTESIAN_POINT ( 'NONE',  ( 1.033464566929133799, 0.000000000000000000, 1.338582677057826853 ) ) ;
#11319=CARTESIAN_POINT ( 'NONE',  ( -0.7185039370078739607, 1.928577636452523993E-17, 1.043307086506645831 ) ) ;
#11320=CARTESIAN_POINT ( 'NONE',  ( 0.7495606340400177148, -0.1264236179284866091, 1.902066929080094448 ) ) ;
#11321=CYLINDRICAL_SURFACE ( 'NONE', #23775, 0.1574803149606299191 ) ;
#11322=CARTESIAN_POINT ( 'NONE',  ( 0.9412147342319837628, -0.1574803149606297803, 1.882381889656251639 ) ) ;
#11323=EDGE_CURVE ( 'NONE', #15970, #40728, #4554, .T. ) ;
#11324=VERTEX_POINT ( 'NONE', #34867 ) ;
#11325=CARTESIAN_POINT ( 'NONE',  ( -1.033464566929133799, 1.928577636452524610E-17, 2.869337061179095023E-17 ) ) ;
#11327=FACE_OUTER_BOUND ( 'NONE', #35326, .T. ) ;
#11329=CARTESIAN_POINT ( 'NONE',  ( 0.9500414927467378812, -0.1787899950787401604, 0.2559055117572600624 ) ) ;
#11331=CARTESIAN_POINT ( 'NONE',  ( 1.054774247047244096, 0.000000000000000000, 0.5733267715997795166 ) ) ;
#11332=EDGE_CURVE ( 'NONE', #2870, #35775, #2242, .T. ) ;
#11333=CARTESIAN_POINT ( 'NONE',  ( -1.054774247047244540, -0.07405724077823318263, 1.555118110182455382 ) ) ;
#11337=CARTESIAN_POINT ( 'NONE',  ( 0.8759842519685039353, -0.1787899950787401882, 1.277066929080094448 ) ) ;
#11338=CARTESIAN_POINT ( 'NONE',  ( 0.8759842519685039353, 0.1787899950787401882, 0.03690944876513417572 ) ) ;
#11339=CARTESIAN_POINT ( 'NONE',  ( -1.054774247047244540, -0.07405724077823318263, 1.043307086560409269 ) ) ;
#11341=CARTESIAN_POINT ( 'NONE',  ( 0.7495606340400177148, 0.1264236179284866091, 0.4355314960092284138 ) ) ;
#11342=CARTESIAN_POINT ( 'NONE',  ( -0.6971942568897626646, -0.07405724077823297447, 0.2411417322297010890 ) ) ;
#11343=EDGE_CURVE ( 'NONE', #7779, #20929, #43474, .T. ) ;
#11344=CARTESIAN_POINT ( 'NONE',  ( -0.7495606340400177148, -0.1264236179284866091, 0.7160433070328504623 ) ) ;
#11345=CARTESIAN_POINT ( 'NONE',  ( 0.8759842519685039353, -0.1574803149606299191, 1.722440944774362270 ) ) ;
#11346=ORIENTED_EDGE ( 'NONE', *, *, #38952, .T. ) ;
#11349=CARTESIAN_POINT ( 'NONE',  ( -0.7646288533564489232, 0.1113553986120547346, 1.363188976377952999 ) ) ;
#11350=CARTESIAN_POINT ( 'NONE',  ( 1.054774247047244096, 0.000000000000000000, 1.129429133804503937 ) ) ;
#11351=CARTESIAN_POINT ( 'NONE',  ( -0.8019270111902716547, 0.1787899950787401604, 1.845472440891119392 ) ) ;
#11353=CARTESIAN_POINT ( 'NONE',  ( 1.002407869896990045, 0.1264236179284866091, 1.916830708607653477 ) ) ;
#11355=DIRECTION ( 'NONE',  ( 1.822029033848725028E-16, 0.000000000000000000, 1.000000000000000000 ) ) ;
#11361=CARTESIAN_POINT ( 'NONE',  ( 0.8759842519685039353, 0.1787899950787401882, 1.252460629867496067 ) ) ;
#11364=CARTESIAN_POINT ( 'NONE',  ( 0.9500414927467378812, 0.1787899950787401604, 1.486220472387181690 ) ) ;
#11365=CARTESIAN_POINT ( 'NONE',  ( 1.054774247047244096, 0.000000000000000000, 0.1796259841982051075 ) ) ;
#11369=CARTESIAN_POINT ( 'NONE',  ( -1.002407869896990045, -0.1264236179284866091, 0.4552165353793071745 ) ) ;
#11372=CARTESIAN_POINT ( 'NONE',  ( -0.7119983469427643152, -0.03169511975089377848, 1.983853482814432745 ) ) ;
#11373=CARTESIAN_POINT ( 'NONE',  ( 0.7495606340400177148, -0.1264236179284866091, 1.429625984198204858 ) ) ;
#11374=CARTESIAN_POINT ( 'NONE',  ( 1.002407869896990045, -0.1264236179284866091, 1.749507873961984483 ) ) ;
#11375=ADVANCED_FACE ( 'NONE', ( #46330 ), #16862, .T. ) ;
#11376=FACE_OUTER_BOUND ( 'NONE', #16173, .T. ) ;
#11378=CARTESIAN_POINT ( 'NONE',  ( -1.033464566929133799, 0.000000000000000000, 1.505905511811023612 ) ) ;
#11379=CARTESIAN_POINT ( 'NONE',  ( -0.8084482433127401224, 0.1455052200007756480, 1.979717192799555825 ) ) ;
#11380=CARTESIAN_POINT ( 'NONE',  ( 0.8759842519685039353, -0.1574803149606299191, 0.8169291337507401662 ) ) ;
#11381=CARTESIAN_POINT ( 'NONE',  ( -0.7185039370078746268, -0.06523048226347956391, 1.921751968503937480 ) ) ;
#11383=CARTESIAN_POINT ( 'NONE',  ( 0.9500414927467378812, 0.1787899950787401604, 0.2657480314422993595 ) ) ;
#11384=CARTESIAN_POINT ( 'NONE',  ( -1.033464566929133799, 0.000000000000000000, 1.702755905511810885 ) ) ;
#11387=CARTESIAN_POINT ( 'NONE',  ( 1.033464566929133799, 0.000000000000000000, 0.7086614172153071767 ) ) ;
#11389=CARTESIAN_POINT ( 'NONE',  ( 0.9873396505805591694, 0.1113553986120547346, 1.392716535433070835 ) ) ;
#11392=CARTESIAN_POINT ( 'NONE',  ( 0.7185039370078746268, -0.06523048226347956391, 0.2682086614173231909 ) ) ;
#11394=CARTESIAN_POINT ( 'NONE',  ( 1.054774247047244540, -0.07405724077823318263, 1.555118110182455382 ) ) ;
#11401=DIRECTION ( 'NONE',  ( 1.822029033848725028E-16, 0.000000000000000000, 1.000000000000000000 ) ) ;
#11404=CARTESIAN_POINT ( 'NONE',  ( 0.6971942568897637749, 2.189545951927499583E-17, 0.9128937007336377363 ) ) ;
#11406=CARTESIAN_POINT ( 'NONE',  ( -1.054774247047244096, 0.000000000000000000, 1.286909448765133801 ) ) ;
#11410=DIRECTION ( 'NONE',  ( -1.000000000000000000, 0.000000000000000000, 0.000000000000000000 ) ) ;
#11417=DIRECTION ( 'NONE',  ( 1.822029033848725028E-16, 0.000000000000000000, 1.000000000000000000 ) ) ;
#11419=CARTESIAN_POINT ( 'NONE',  ( -1.054774247047244540, -0.07405724077823318263, 0.8070866141194653620 ) ) ;
#11422=CARTESIAN_POINT ( 'NONE',  ( -0.9500414927467377701, -0.1787899950787401604, 1.830708661363559253 ) ) ;
#11428=CARTESIAN_POINT ( 'NONE',  ( -0.7185039370078739607, 1.928577636452523993E-17, 0.9350393700787401619 ) ) ;
#11431=DIRECTION ( 'NONE',  ( 1.000000000000000000, 0.000000000000000000, -1.822029033848725275E-16 ) ) ;
#11432=CARTESIAN_POINT ( 'NONE',  ( 1.002407869896990045, 0.1264236179284866091, 0.8981299212060788184 ) ) ;
#11433=CARTESIAN_POINT ( 'NONE',  ( 0.8759842519685039353, 0.1787899950787401882, 1.331200787347811110 ) ) ;
#11434=EDGE_CURVE ( 'NONE', #15222, #11894, #14114, .T. ) ;
#11436=CARTESIAN_POINT ( 'NONE',  ( 0.8107537697050254399, 0.1574803149606300301, 0.5241141731208195376 ) ) ;
#11437=CARTESIAN_POINT ( 'NONE',  ( 0.9412147342319837628, 0.1574803149606300301, 1.395177165354331672 ) ) ;
#11438=CARTESIAN_POINT ( 'NONE',  ( 0.7351878293081982596, 0.08236403197891215000, 1.981599075499917095 ) ) ;
#11440=CARTESIAN_POINT ( 'NONE',  ( 0.7185039370078739607, 1.928577636452523993E-17, 0.4527559054042842868 ) ) ;
#11441=CARTESIAN_POINT ( 'NONE',  ( 0.6971942568897648851, 0.07405724077823318263, 0.7874015747493863238 ) ) ;
#11444=ORIENTED_EDGE ( 'NONE', *, *, #251, .T. ) ;
#11445=CARTESIAN_POINT ( 'NONE',  ( -0.9873396505805591694, 0.1113553986120547346, 0.8415354330708662012 ) ) ;
#11447=CARTESIAN_POINT ( 'NONE',  ( 0.8019270111902717657, -0.1787899950787401604, 1.190944881836001112 ) ) ;
#11451=CARTESIAN_POINT ( 'NONE',  ( -0.9873396505805591694, -0.1113553986120547346, 0.5167322834645668994 ) ) ;
#11454=CARTESIAN_POINT ( 'NONE',  ( -1.002407869896990045, -0.1264236179284866091, 0.2928149605761578567 ) ) ;
#11455=EDGE_LOOP ( 'NONE', ( #10728, #14213, #44849, #19890 ) ) ;
#11456=CARTESIAN_POINT ( 'NONE',  ( 1.033464566929133799, 0.000000000000000000, 1.742125984251968518 ) ) ;
#11457=CARTESIAN_POINT ( 'NONE',  ( -0.8019270111902717657, 0.1787899950787401604, 1.609251968450173376 ) ) ;
#11458=CARTESIAN_POINT ( 'NONE',  ( -0.7495606340400177148, 0.1264236179284866091, 0.3961614172690708924 ) ) ;
#11466=CARTESIAN_POINT ( 'NONE',  ( -0.9412147342319837628, 0.1574803149606300301, 1.975885826664125711 ) ) ;
#11467=CARTESIAN_POINT ( 'NONE',  ( -0.9500414927467378812, 0.1787899950787401604, 0.3444881889226146243 ) ) ;
#11469=ORIENTED_EDGE ( 'NONE', *, *, #28714, .T. ) ;
#11470=CARTESIAN_POINT ( 'NONE',  ( -1.002407869896990045, -0.1264236179284866091, 1.360728346402929168 ) ) ;
#11471=VERTEX_POINT ( 'NONE', #39602 ) ;
#11478=CARTESIAN_POINT ( 'NONE',  ( 0.7646288533564489232, -0.1113553986120547346, 0.4281496062992125595 ) ) ;
#11480=CARTESIAN_POINT ( 'NONE',  ( -1.033464566929133799, 0.000000000000000000, 1.102362204616881947 ) ) ;
#11481=CARTESIAN_POINT ( 'NONE',  ( 0.9500414927467378812, 0.1787899950787401604, 0.4281496062454490659 ) ) ;
#11482=CARTESIAN_POINT ( 'NONE',  ( 1.033464566929133799, 0.000000000000000000, 1.456692913278299084 ) ) ;
#11484=VERTEX_POINT ( 'NONE', #22337 ) ;
#11485=CARTESIAN_POINT ( 'NONE',  ( 0.8107537697050253289, -0.1574803149606297803, 1.995570866034207080 ) ) ;
#11486=ORIENTED_EDGE ( 'NONE', *, *, #6811, .T. ) ;
#11489=CARTESIAN_POINT ( 'NONE',  ( -1.054774247047244540, 0.07405724077823318263, 1.013779527505291878 ) ) ;
#11490=CARTESIAN_POINT ( 'NONE',  ( 0.9873396505805591694, -0.1113553986120547346, 0.9891732283464568232 ) ) ;
#11494=CARTESIAN_POINT ( 'NONE',  ( 0.8759842519685039353, -0.1574803149606299191, 0.7480314960629921295 ) ) ;
#11496=CARTESIAN_POINT ( 'NONE',  ( 0.7185039370078739607, 1.928577636452523993E-17, 1.437007873908220601 ) ) ;
#11497=ORIENTED_EDGE ( 'NONE', *, *, #33595, .T. ) ;
#11498=CARTESIAN_POINT ( 'NONE',  ( 0.9500414927467378812, -0.1787899950787401604, 0.6446850393163160442 ) ) ;
#11505=CARTESIAN_POINT ( 'NONE',  ( 0.8107537697050253289, 0.1574803149606300301, 1.075295275483024504 ) ) ;
#11508=ORIENTED_EDGE ( 'NONE', *, *, #30710, .F. ) ;
#11509=ORIENTED_EDGE ( 'NONE', *, *, #44983, .F. ) ;
#11511=CARTESIAN_POINT ( 'NONE',  ( -0.8019270111902717657, 0.1787899950787401604, 1.732283464513166615 ) ) ;
#11512=CARTESIAN_POINT ( 'NONE',  ( 0.9500414927467378812, -0.1787899950787401604, 1.712598425143087688 ) ) ;
#11513=CARTESIAN_POINT ( 'NONE',  ( -1.054774247047244540, -0.07405724077823318263, 0.7332677164816707727 ) ) ;
#11514=CARTESIAN_POINT ( 'NONE',  ( 1.033464566929133799, 0.000000000000000000, 1.781496062992125928 ) ) ;
#11515=CARTESIAN_POINT ( 'NONE',  ( 0.8759842519685039353, 0.1787899950787401882, 0.3518700786863940833 ) ) ;
#11516=AXIS2_PLACEMENT_3D ( 'NONE', #8468, #46071, #20439 ) ;
#11518=CARTESIAN_POINT ( 'NONE',  ( -1.054774247047244096, 0.000000000000000000, 1.242618110182456714 ) ) ;
#11519=CARTESIAN_POINT ( 'NONE',  ( -1.054774247047244096, 0.000000000000000000, 0.8095472440407244230 ) ) ;
#11523=CARTESIAN_POINT ( 'NONE',  ( -1.002407869896990045, -0.1264236179284866091, 1.596948818843874074 ) ) ;
#11524=CARTESIAN_POINT ( 'NONE',  ( -0.7185039370078739607, 1.928577636452523993E-17, 1.909448818790110192 ) ) ;
#11526=CARTESIAN_POINT ( 'NONE',  ( -0.8107537697050253289, -0.1574803149606297803, 1.611712598425196319 ) ) ;
#11528=CARTESIAN_POINT ( 'NONE',  ( 0.6971942568897648851, 0.07405724077823318263, 1.461614173174583753 ) ) ;
#11532=ORIENTED_EDGE ( 'NONE', *, *, #220, .F. ) ;
#11540=CARTESIAN_POINT ( 'NONE',  ( 1.002407869896990045, -0.1264236179284866091, 1.710137795221826851 ) ) ;
#11544=VECTOR ( 'NONE', #19730, 39.37007874015748143 ) ;
#11547=CARTESIAN_POINT ( 'NONE',  ( -0.7185039370078746268, 0.06523048226347956391, 1.080216535325543958 ) ) ;
#11548=CARTESIAN_POINT ( 'NONE',  ( 0.7495606340400177148, 0.1264236179284866091, 0.7849409448281259305 ) ) ;
#11549=AXIS2_PLACEMENT_3D ( 'NONE', #3198, #46809, #32472 ) ;
#11551=DIRECTION ( 'NONE',  ( -1.000000000000000000, 0.000000000000000000, 0.000000000000000000 ) ) ;
#11554=CARTESIAN_POINT ( 'NONE',  ( 1.002407869896990045, -0.1264236179284866091, 1.833169291284818758 ) ) ;
#11557=ORIENTED_EDGE ( 'NONE', *, *, #38937, .F. ) ;
#11559=CARTESIAN_POINT ( 'NONE',  ( -0.6971942568897626646, -0.07405724077823297447, 0.4035433070328508509 ) ) ;
#11560=CARTESIAN_POINT ( 'NONE',  ( -0.7185039370078739607, 1.928577636452523993E-17, 1.683070866141732402 ) ) ;
#11562=CARTESIAN_POINT ( 'NONE',  ( 0.7495606340400177148, 0.1264236179284866091, 0.2386811023084413619 ) ) ;
#11563=CYLINDRICAL_SURFACE ( 'NONE', #27765, 0.1574803149606299191 ) ;
#11564=CARTESIAN_POINT ( 'NONE',  ( -0.9500414927467378812, 0.1787899950787401604, 1.801181102308441861 ) ) ;
#11565=VERTEX_POINT ( 'NONE', #18742 ) ;
#11566=CARTESIAN_POINT ( 'NONE',  ( -1.054774247047244540, 0.07405724077823318263, 1.210629921206079818 ) ) ;
#11567=CARTESIAN_POINT ( 'NONE',  ( -1.033464566929133799, 0.000000000000000000, 0.7086614172153071767 ) ) ;
#11568=CARTESIAN_POINT ( 'NONE',  ( 0.6971942568897637749, 2.189545951927499583E-17, 1.267224409395055096 ) ) ;
#11569=CARTESIAN_POINT ( 'NONE',  ( 0.6971942568897648851, -0.07405724077823297447, 1.934055118056471567 ) ) ;
#11570=CARTESIAN_POINT ( 'NONE',  ( -1.054774247047244540, -0.07405724077823318263, 1.082677165300567346 ) ) ;
#11573=CARTESIAN_POINT ( 'NONE',  ( 0.8759842519685039353, 0.1787899950787401882, 0.4699803149068661479 ) ) ;
#11574=CARTESIAN_POINT ( 'NONE',  ( -0.8759842519685039353, -0.1787899950787401882, 0.4060039369541102450 ) ) ;
#11575=CARTESIAN_POINT ( 'NONE',  ( -0.7495606340400177148, -0.1264236179284866091, 0.7947834645131652831 ) ) ;
#11580=CARTESIAN_POINT ( 'NONE',  ( -1.033464566929134687, 0.06523048226347956391, 0.2091535433070865757 ) ) ;
#11581=CARTESIAN_POINT ( 'NONE',  ( 0.6971942568897648851, -0.07405724077823297447, 1.072834645615528659 ) ) ;
#11582=CARTESIAN_POINT ( 'NONE',  ( 0.8107537697050254399, 0.1574803149606300301, 1.941437007766490863 ) ) ;
#11586=CARTESIAN_POINT ( 'NONE',  ( 0.8759842519685039353, -0.1787899950787401882, 1.941437007820252081 ) ) ;
#11594=EDGE_CURVE ( 'NONE', #9411, #37983, #24009, .T. ) ;
#11595=ORIENTED_EDGE ( 'NONE', *, *, #4400, .T. ) ;
#11596=CARTESIAN_POINT ( 'NONE',  ( 1.002407869896990045, 0.1264236179284866091, 1.129429133804503937 ) ) ;
#11599=( BOUNDED_CURVE ( )  B_SPLINE_CURVE ( 2, ( #47418, #16062, #28441, #43254, #18104, #26015, #44426, #26263, #29183, #40825, #28926, #25303, #21941, #36561, #7547, #29424, #39134, #46560, #13295, #34871, #20694, #42487, #6549, #21161, #13062, #5615, #46332, #20464, #31509, #9462, #35336, #17573, #20222, #27699, #24080, #42709, #35099, #42007, #38688, #2477, #5857, #32213, #13516, #2246, #17103, #28149, #9927, #18745, #520, #28636, #47284, #43672, #40071, #25007, #33172, #10405, #294, #29372, #33403, #21650, #18520, #39605, #25246, #32930, #44143, #21401, #36735, #14461, #7723, #43193, #3187, #28875, #3434, #14940, #17815, #25734, #32462, #11114, #40305, #39833, #7488, #29602, #10883, #11342, #10641, #29121, #47041, #22340, #25503, #25955, #36026, #36283, #40534, #7271, #36968, #43912, #32693, #4121, #51, #43433, #6782, #14233, #21889, #7025, #14698, #18048, #36510, #22107, #3665, #3893, #18288, #12287, #19688, #22582, #19217, #15178, #4828, #15652, #45072, #37917, #33876, #19923, #5072, #995, #12535, #34332, #33635, #29821, #19451, #41002, #37428, #15410, #12052, #8910, #44367, #749, #7963, #15887, #26906, #5306, #30290, #26674, #34106, #1233, #1462, #26201, #30057, #16122, #41466, #40767, #11574, #4582, #44599, #37196, #4340, #18973, #23300, #11815, #30744, #44842, #41224, #27155, #8428, #23056, #26439, #8664, #37676, #45317, #41710, #23541, #34555, #30511, #8190, #38142, #22814, #24011, #45543, #46264, #31684, #5549, #35507, #12766, #6479, #21100, #17280, #20159, #42422, #20630, #39069, #1707, #20395, #6239, #16584, #31212, #13459, #45785, #1953, #46025, #34809, #16354, #30977, #2182, #46497, #20864, #12993, #27397, #6010, #27635, #38612, #42188, #13237, #42882, #41941, #9393, #9148, #2412, #28089, #39305, #16804, #31444, #42650, #38843, #2647, #23766, #5790, #31916, #9862, #38375, #27865, #9630, #24247, #35275, #17043, #24474, #13676, #28314, #10092, #24704, #25183, #14168, #40481, #39547, #7206, #33110, #234, #25435, #7436, #17984, #39770, #43375, #25899, #7666, #35738, #6961, #3375, #47224, #32144, #40248, #17510, #22055, #36455, #46735, #21581, #36223, #13920, #32399, #40011, #3838, #28567, #43855, #32637, #14880, #43135, #10339, #35966, #10587, #36679, #24949, #32870, #6720, #18228, #11058, #29307, #3123, #18461, #14407, #23205, #29540, #21335, #29057, #17751, #21828, #43613, #14638, #25673, #10822, #46976, #3609, #44091, #28813, #11287, #7908, #33345, #1181, #941, #30464, #22524, #12234, #45263, #15122, #37140, #44315, #1413, #22282, #11519, #43325, #10526, #29252, #43080, #14351, #3064, #17693, #46923, #26563, #40423, #29484, #4231, #26074, #4007, #25841, #36854, #37553, #7607, #30409, #33518, #18860, #7847, #34227, #18628, #11701, #44027, #26794, #19099, #15780, #40887, #631, #15289, #19583, #1355, #11230, #29940, #44485, #8081, #412, #33993, #15063, #44958, #44724, #29710, #22460, #19342, #44256, #40647, #33766, #12170, #22703, #4716, #37309, #8555, #4458, #877, #15538, #11941, #41351, #41121, #8315, #22945, #23189, #37802, #4955, #42326, #13354, #42076, #42551, #23658, #1836, #34445, #9754, #20286, #38966, #8795, #34693, #6131, #20528, #35401, #30637, #45199, #38034, #16247, #2774, #21718, #36350, #21228, #40138, #36094, #39905, #35633, #47109, #3504, #28942, #46626, #24834, #7338, #39437, #46395, #14299, #32522, #6372, #18117, #35853, #21951, #2542, #32761, #20984, #43270, #21464, #47357, #17170, #3004, #29196, #17397, #32036, #43502, #13811, #28452, #14051, #43021, #13572, #28207, #43743, #17639, #32285, #25566, #42771, #10227, #28699, #9987, #24597, #10713, #25318, #39196, #6614, #17878, #10471, #25068, #39660, #6842, #3253, #30002, #37368, #8139, #15121, #15600, #37617, #34055, #26620, #44787, #26384, #41175, #4289, #4523, #44314, #7665, #694, #22281, #19404, #8375, #44546, #33109, #30463, #36918, #233, #11764, #40480, #4776, #12000, #14879, #1180, #15841, #45021, #11518, #37139, #30236, #29539, #33579, #23005, #37869, #12233, #4072, #29767, #44090, #18920, #11286, #26139, #22762, #26858, #25898, #41417, #15350, #8614, #18685, #33344, #468, #40707, #23253, #7907, #18460, #22523, #940, #40943, #19161, #33822, #24827, #35393, #21222, #35158, #38961, #9516, #32280, #2538, #3001, #45262, #27977, #39430, #6125, #17393, #17635, #20750, #13567, #38743, #32031, #17166, #28694, #27108, #42545, #6608, #31805, #10466, #6365, #9748, #19642, #39190, #20523, #34287, #46389, #24140, #16073, #1412, #2301, #16929, #28203, #42765, #46622, #9982, #2769, #13806, #28448, #43014, #39655, #29433, #36570, #22164, #15013, #10944, #47103, #116, #25563, #10708, #14763, #22408, #587, #11180, #40365, #3956, #7088, #44205, #15243, #21459, #25313, #14293, #7791, #37034, #44433, #36090, #28937, #36345, #3499, #1305, #22889, #23376, #45390, #19763, #4413, #26271, #1064, #4660, #819, #19043, #33710, #34396, #15481, #27226, #44906, #15722, #19287, #31052, #44665, #8500, #40834, #19523, #26506, #12605, #23130, #12119, #33941, #16424, #41066, #4902, #30580, #45144, #12364, #26982, #30820, #41533, #41779, #8740, #1536, #8980, #23601, #38213, #5373, #19994, #34633, #1783, #20934, #31517, #39373, #27467, #34879, #13071, #35107, #17348, #2024, #9933, #16654, #42717, #24539, #9469, #39142, #2484, #27708, #17110, #13300, #6311, #35574, #46100, #5622, #27929, #42492, #31281, #9699, #42960, #6557, #45858, #24313, #46568, #24776, #2717, #31980, #13751, #21167, #20230, #13520, #28392, #2946, #38913, #6074, #10168, #42268, #20699, #24086, #35801, #17581, #32224, #12835, #42015, #35341, #9221, #31752, #46335, #38694, #23839, #38451, #5866, #16873, #2253, #20471, #28154, #25014, #29128, #13993, #40081, #21407, #33180, #40314, #28643, #18525, #29610, #44151, #39843, #18055, #14472, #10891, #43201, #3900, #10412, #301, #58, #36974, #7032, #36742, #25511, #14947, #7497, #14704, #11351, #3196, #22348, #39612, #32702, #6789, #47049, #21659, #25960, #36034, #43919, #17823, #29379, #11124, #43444, #25741, #36518, #22117, #40541, #47292, #7278, #32470, #7731, #21896, #4129, #18753, #36291, #46808, #43682, #14242, #28883, #3443, #10649, #18296, #25254, #3673, #32937, #37204, #44374, #38148, #5313, #1470, #4347, #26682, #4836, #23306, #30518, #37923, #40774, #45081, #19697, #12292, #41009, #26915, #5077, #7970, #37440, #33411, #23065, #33882 ),
 .UNSPECIFIED., .F., .T. ) 
 B_SPLINE_CURVE_WITH_KNOTS ( ( 3, 2, 2, 2, 2, 2, 2, 2, 2, 2, 2, 2, 2, 2, 2, 2, 2, 2, 2, 2, 2, 2, 2, 2, 2, 2, 2, 2, 2, 2, 2, 2, 2, 2, 2, 2, 2, 2, 2, 2, 2, 2, 2, 2, 2, 2, 2, 2, 2, 2, 2, 2, 2, 2, 2, 2, 2, 2, 2, 2, 2, 2, 2, 2, 2, 2, 2, 2, 2, 2, 2, 2, 2, 2, 2, 2, 2, 2, 2, 2, 2, 2, 2, 2, 2, 2, 2, 2, 2, 2, 2, 2, 2, 2, 2, 2, 2, 2, 2, 2, 2, 2, 2, 2, 2, 2, 2, 2, 2, 2, 2, 2, 2, 2, 2, 2, 2, 2, 2, 2, 2, 2, 2, 2, 2, 2, 2, 2, 2, 2, 2, 2, 2, 2, 2, 2, 2, 2, 2, 2, 2, 2, 2, 2, 2, 2, 2, 2, 2, 2, 2, 2, 2, 2, 2, 2, 2, 2, 2, 2, 2, 2, 2, 2, 2, 2, 2, 2, 2, 2, 2, 2, 2, 2, 2, 2, 2, 2, 2, 2, 2, 2, 2, 2, 2, 2, 2, 2, 2, 2, 2, 2, 2, 2, 2, 2, 2, 2, 2, 2, 2, 2, 2, 2, 2, 2, 2, 2, 2, 2, 2, 2, 2, 2, 2, 2, 2, 2, 2, 2, 2, 2, 2, 2, 2, 2, 2, 2, 2, 2, 2, 2, 2, 2, 2, 2, 2, 2, 2, 2, 2, 2, 2, 2, 2, 2, 2, 2, 2, 2, 2, 2, 2, 2, 2, 2, 2, 2, 2, 2, 2, 2, 2, 2, 2, 2, 2, 2, 2, 2, 2, 2, 2, 2, 2, 2, 2, 2, 2, 2, 2, 2, 2, 2, 2, 2, 2, 2, 2, 2, 2, 2, 2, 2, 2, 2, 2, 2, 2, 2, 2, 2, 2, 2, 2, 2, 2, 2, 2, 2, 2, 2, 2, 2, 2, 2, 2, 2, 2, 2, 2, 2, 2, 2, 2, 2, 2, 2, 2, 2, 2, 2, 2, 2, 2, 2, 2, 2, 2, 2, 2, 2, 2, 2, 2, 2, 2, 2, 2, 2, 2, 2, 2, 2, 2, 2, 2, 2, 2, 2, 2, 2, 2, 2, 2, 2, 2, 2, 2, 2, 2, 2, 2, 2, 2, 2, 2, 2, 2, 2, 2, 2, 2, 2, 2, 2, 2, 2, 2, 2, 2, 2, 2, 2, 2, 2, 2, 3 ),
 ( 0.008750000026272800741, 0.01000000000000000021, 0.01250000000000000069, 0.01499999999999999944, 0.01750000000000000167, 0.02000000000000000042, 0.02249999999999999917, 0.02500000000000000139, 0.02750000000000000014, 0.02999999999999999889, 0.03250000000000000111, 0.03500000000000000333, 0.03749999999999999861, 0.04000000000000000083, 0.04249999999999999611, 0.04499999999999999833, 0.04750000000000000056, 0.05000000000000000278, 0.05249999999999999112, 0.05499999999999999334, 0.05749999999999999556, 0.05999999999999999778, 0.06250000000000000000, 0.06500000000000000222, 0.06750000000000000444, 0.07000000000000000666, 0.07249999999999999500, 0.07499999999999999722, 0.07749999999999999944, 0.08000000000000000167, 0.08250000000000000389, 0.08500000000000000611, 0.08749999999999999445, 0.08999999999999999667, 0.09249999999999999889, 0.09500000000000000111, 0.09750000000000000333, 0.1000000000000000056, 0.1024999999999999939, 0.1049999999999999961, 0.1074999999999999983, 0.1100000000000000006, 0.1125000000000000028, 0.1150000000000000050, 0.1174999999999999933, 0.1199999999999999956, 0.1224999999999999978, 0.1250000000000000000, 0.1275000000000000300, 0.1300000000000000044, 0.1325000000000000067, 0.1350000000000000089, 0.1375000000000000111, 0.1400000000000000133, 0.1424999999999999878, 0.1449999999999999900, 0.1474999999999999922, 0.1499999999999999944, 0.1524999999999999967, 0.1549999999999999989, 0.1575000000000000011, 0.1600000000000000033, 0.1625000000000000056, 0.1650000000000000078, 0.1675000000000000100, 0.1700000000000000122, 0.1724999999999999867, 0.1749999999999999889, 0.1774999999999999911, 0.1799999999999999933, 0.1824999999999999956, 0.1849999999999999978, 0.1875000000000000000, 0.1900000000000000022, 0.1925000000000000044, 0.1950000000000000067, 0.1975000000000000089, 0.2000000000000000111, 0.2025000000000000133, 0.2049999999999999878, 0.2074999999999999900, 0.2099999999999999922, 0.2124999999999999944, 0.2149999999999999967, 0.2174999999999999989, 0.2200000000000000011, 0.2225000000000000033, 0.2250000000000000056, 0.2275000000000000078, 0.2300000000000000100, 0.2325000000000000122, 0.2349999999999999867, 0.2374999999999999889, 0.2399999999999999911, 0.2424999999999999933, 0.2449999999999999956, 0.2474999999999999978, 0.2500000000000000000, 0.2525000000000000022, 0.2550000000000000044, 0.2575000000000000067, 0.2600000000000000089, 0.2625000000000000111, 0.2650000000000000133, 0.2675000000000000155, 0.2700000000000000178, 0.2725000000000000755, 0.2750000000000000222, 0.2775000000000000244, 0.2800000000000000266, 0.2824999999999999734, 0.2849999999999999756, 0.2874999999999999778, 0.2899999999999999800, 0.2924999999999999822, 0.2949999999999999845, 0.2974999999999999867, 0.2999999999999999889, 0.3024999999999999911, 0.3049999999999999933, 0.3074999999999999956, 0.3099999999999999978, 0.3125000000000000000, 0.3150000000000000022, 0.3175000000000000044, 0.3200000000000000067, 0.3225000000000000089, 0.3250000000000000111, 0.3275000000000000133, 0.3300000000000000155, 0.3325000000000000178, 0.3350000000000000200, 0.3375000000000000222, 0.3400000000000000244, 0.3425000000000000266, 0.3449999999999999734, 0.3474999999999999756, 0.3499999999999999778, 0.3524999999999999800, 0.3549999999999999822, 0.3574999999999999845, 0.3599999999999999867, 0.3624999999999999889, 0.3649999999999999911, 0.3674999999999999933, 0.3699999999999999956, 0.3724999999999999978, 0.3750000000000000000, 0.3775000000000000022, 0.3800000000000000044, 0.3825000000000000067, 0.3850000000000000089, 0.3875000000000000111, 0.3900000000000000133, 0.3925000000000000155, 0.3950000000000000178, 0.3975000000000000755, 0.4000000000000000222, 0.4025000000000000244, 0.4050000000000000266, 0.4074999999999999734, 0.4099999999999999756, 0.4124999999999999778, 0.4149999999999999800, 0.4174999999999999822, 0.4199999999999999845, 0.4224999999999999867, 0.4249999999999999889, 0.4274999999999999911, 0.4299999999999999933, 0.4324999999999999956, 0.4349999999999999978, 0.4375000000000000000, 0.4400000000000000022, 0.4425000000000000044, 0.4450000000000000067, 0.4475000000000000089, 0.4500000000000000111, 0.4525000000000000133, 0.4550000000000000155, 0.4575000000000000178, 0.4600000000000000200, 0.4625000000000000222, 0.4650000000000000244, 0.4675000000000000266, 0.4699999999999999734, 0.4724999999999999756, 0.4749999999999999778, 0.4774999999999999800, 0.4799999999999999822, 0.4824999999999999845, 0.4849999999999999867, 0.4874999999999999889, 0.4899999999999999911, 0.4924999999999999933, 0.4949999999999999956, 0.4974999999999999978, 0.5000000000000000000, 0.5024999999999999467, 0.5050000000000000044, 0.5074999999999999512, 0.5100000000000000089, 0.5124999999999999556, 0.5150000000000000133, 0.5174999999999999600, 0.5200000000000000178, 0.5224999999999999645, 0.5250000000000000222, 0.5274999999999999689, 0.5300000000000000266, 0.5324999999999999734, 0.5350000000000000311, 0.5374999999999999778, 0.5400000000000000355, 0.5424999999999999822, 0.5450000000000000400, 0.5474999999999999867, 0.5500000000000000444, 0.5524999999999999911, 0.5550000000000000488, 0.5574999999999999956, 0.5600000000000000533, 0.5625000000000000000, 0.5649999999999999467, 0.5675000000000000044, 0.5699999999999999512, 0.5725000000000000089, 0.5749999999999999556, 0.5775000000000000133, 0.5799999999999999600, 0.5825000000000000178, 0.5849999999999999645, 0.5875000000000000222, 0.5899999999999999689, 0.5925000000000000266, 0.5949999999999999734, 0.5975000000000000311, 0.5999999999999999778, 0.6025000000000000355, 0.6049999999999999822, 0.6075000000000000400, 0.6099999999999999867, 0.6125000000000000444, 0.6149999999999999911, 0.6175000000000000488, 0.6199999999999999956, 0.6225000000000000533, 0.6250000000000000000, 0.6274999999999999467, 0.6300000000000000044, 0.6324999999999999512, 0.6350000000000000089, 0.6374999999999999556, 0.6400000000000000133, 0.6424999999999999600, 0.6450000000000000178, 0.6474999999999999645, 0.6500000000000000222, 0.6524999999999999689, 0.6550000000000000266, 0.6574999999999999734, 0.6600000000000000311, 0.6624999999999999778, 0.6650000000000000355, 0.6674999999999999822, 0.6700000000000000400, 0.6724999999999999867, 0.6750000000000000444, 0.6774999999999999911, 0.6800000000000000488, 0.6824999999999999956, 0.6850000000000000533, 0.6875000000000000000, 0.6899999999999999467, 0.6925000000000000044, 0.6949999999999999512, 0.6975000000000000089, 0.6999999999999999556, 0.7025000000000000133, 0.7049999999999999600, 0.7075000000000000178, 0.7099999999999999645, 0.7125000000000000222, 0.7149999999999999689, 0.7175000000000000266, 0.7199999999999999734, 0.7225000000000000311, 0.7249999999999999778, 0.7275000000000000355, 0.7299999999999999822, 0.7325000000000000400, 0.7349999999999999867, 0.7375000000000000444, 0.7399999999999999911, 0.7425000000000000488, 0.7449999999999999956, 0.7475000000000000533, 0.7500000000000000000, 0.7524999999999999467, 0.7550000000000000044, 0.7574999999999999512, 0.7600000000000000089, 0.7624999999999999556, 0.7650000000000000133, 0.7674999999999999600, 0.7700000000000000178, 0.7724999999999999645, 0.7750000000000000222, 0.7774999999999999689, 0.7800000000000000266, 0.7824999999999999734, 0.7850000000000000311, 0.7874999999999999778, 0.7900000000000000355, 0.7924999999999999822, 0.7950000000000000400, 0.7974999999999999867, 0.8000000000000000444, 0.8024999999999999911, 0.8050000000000000488, 0.8074999999999999956, 0.8100000000000000533, 0.8125000000000000000, 0.8149999999999999467, 0.8175000000000000044, 0.8199999999999999512, 0.8225000000000000089, 0.8249999999999999556, 0.8275000000000000133, 0.8299999999999999600, 0.8325000000000000178, 0.8349999999999999645, 0.8375000000000000222, 0.8399999999999999689, 0.8425000000000000266, 0.8449999999999999734, 0.8475000000000000311, 0.8499999999999999778, 0.8525000000000000355, 0.8549999999999999822, 0.8575000000000000400, 0.8599999999999999867, 0.8625000000000000444, 0.8649999999999999911, 0.8675000000000000488, 0.8699999999999999956, 0.8725000000000000533, 0.8750000000000000000, 0.8774999999999999467, 0.8800000000000000044, 0.8824999999999999512, 0.8850000000000000089, 0.8874999999999999556, 0.8900000000000000133, 0.8924999999999999600, 0.8950000000000000178, 0.8974999999999999645, 0.9000000000000000222, 0.9024999999999999689, 0.9050000000000000266, 0.9074999999999999734, 0.9100000000000000311, 0.9124999999999999778, 0.9150000000000000355, 0.9174999999999999822, 0.9200000000000000400, 0.9224999999999999867, 0.9250000000000000444, 0.9274999999999999911, 0.9300000000000000488, 0.9324999999999999956, 0.9350000000000000533, 0.9375000000000000000, 0.9399999999999999467, 0.9425000000000000044, 0.9449999999999999512, 0.9475000000000000089, 0.9499999999999999556, 0.9525000000000000133, 0.9549999999999999600, 0.9575000000000000178, 0.9599999999999999645, 0.9625000000000000222, 0.9649999999999999689, 0.9675000000000000266, 0.9699999999999999734, 0.9725000000000000311, 0.9749999999999999778, 0.9775000000000000355, 0.9799999999999999822, 0.9825000000000000400, 0.9849999999999999867, 0.9875000000000000444, 0.9899999999999999911, 0.9925000000000000488, 0.9949999999999999956, 0.9975000000000000533, 1.000000000000000000 ),
 .UNSPECIFIED. ) 
 CURVE ( )  GEOMETRIC_REPRESENTATION_ITEM ( )  RATIONAL_B_SPLINE_CURVE ( ( 0.9619397662556429252, 0.9619397670556029123, 1.000000000000000000, 0.9238795325112869605, 1.000000000000000000, 0.9238795325112869605, 1.000000000000000000, 0.9238795325112869605, 1.000000000000000000, 0.9238795325112869605, 1.000000000000000000, 0.9238795325112869605, 1.000000000000000000, 0.9238795325112869605, 1.000000000000000000, 0.9238795325112869605, 1.000000000000000000, 0.9238795325112869605, 1.000000000000000000, 0.9238795325112869605, 1.000000000000000000, 0.9238795325112869605, 1.000000000000000000, 0.9238795325112869605, 1.000000000000000000, 0.9238795325112869605, 1.000000000000000000, 0.9238795325112869605, 1.000000000000000000, 0.9238795325112869605, 1.000000000000000000, 0.9238795325112869605, 1.000000000000000000, 0.9238795325112869605, 1.000000000000000000, 0.9238795325112869605, 1.000000000000000000, 0.9238795325112869605, 1.000000000000000000, 0.9238795325112869605, 1.000000000000000000, 0.9238795325112869605, 1.000000000000000000, 0.9238795325112869605, 1.000000000000000000, 0.9238795325112869605, 1.000000000000000000, 0.9238795325112869605, 1.000000000000000000, 0.9238795325112869605, 1.000000000000000000, 0.9238795325112869605, 1.000000000000000000, 0.9238795325112869605, 1.000000000000000000, 0.9238795325112869605, 1.000000000000000000, 0.9238795325112869605, 1.000000000000000000, 0.9238795325112869605, 1.000000000000000000, 0.9238795325112869605, 1.000000000000000000, 0.9238795325112869605, 1.000000000000000000, 0.9238795325112869605, 1.000000000000000000, 0.9238795325112869605, 1.000000000000000000, 0.9238795325112869605, 1.000000000000000000, 0.9238795325112869605, 1.000000000000000000, 0.9238795325112869605, 1.000000000000000000, 0.9238795325112869605, 1.000000000000000000, 0.9238795325112869605, 1.000000000000000000, 0.9238795325112869605, 1.000000000000000000, 0.9238795325112869605, 1.000000000000000000, 0.9238795325112869605, 1.000000000000000000, 0.9238795325112869605, 1.000000000000000000, 0.9238795325112869605, 1.000000000000000000, 0.9238795325112869605, 1.000000000000000000, 0.9238795325112869605, 1.000000000000000000, 0.9238795325112869605, 1.000000000000000000, 0.9238795325112869605, 1.000000000000000000, 0.9238795325112869605, 1.000000000000000000, 0.9238795325112869605, 1.000000000000000000, 0.9238795325112869605, 1.000000000000000000, 0.9238795325112869605, 1.000000000000000000, 0.9238795325112869605, 1.000000000000000000, 0.9238795325112869605, 1.000000000000000000, 0.9238795325112869605, 1.000000000000000000, 0.9238795325112869605, 1.000000000000000000, 0.9238795325112869605, 1.000000000000000000, 0.9238795325112869605, 1.000000000000000000, 0.9238795325112869605, 1.000000000000000000, 0.9238795325112869605, 1.000000000000000000, 0.9238795325112869605, 1.000000000000000000, 0.9238795325112869605, 1.000000000000000000, 0.9238795325112869605, 1.000000000000000000, 0.9238795325112869605, 1.000000000000000000, 0.9238795325112869605, 1.000000000000000000, 0.9238795325112869605, 1.000000000000000000, 0.9238795325112869605, 1.000000000000000000, 0.9238795325112869605, 1.000000000000000000, 0.9238795325112869605, 1.000000000000000000, 0.9238795325112869605, 1.000000000000000000, 0.9238795325112869605, 1.000000000000000000, 0.9238795325112869605, 1.000000000000000000, 0.9238795325112869605, 1.000000000000000000, 0.9238795325112869605, 1.000000000000000000, 0.9238795325112869605, 1.000000000000000000, 0.9238795325112869605, 1.000000000000000000, 0.9238795325112869605, 1.000000000000000000, 0.9238795325112869605, 1.000000000000000000, 0.9238795325112869605, 1.000000000000000000, 0.9238795325112869605, 1.000000000000000000, 0.9238795325112869605, 1.000000000000000000, 0.9238795325112869605, 1.000000000000000000, 0.9238795325112869605, 1.000000000000000000, 0.9238795325112869605, 1.000000000000000000, 0.9238795325112869605, 1.000000000000000000, 0.9238795325112869605, 1.000000000000000000, 0.9238795325112869605, 1.000000000000000000, 0.9238795325112869605, 1.000000000000000000, 0.9238795325112869605, 1.000000000000000000, 0.9238795325112869605, 1.000000000000000000, 0.9238795325112869605, 1.000000000000000000, 0.9238795325112869605, 1.000000000000000000, 0.9238795325112869605, 1.000000000000000000, 0.9238795325112869605, 1.000000000000000000, 0.9238795325112869605, 1.000000000000000000, 0.9238795325112869605, 1.000000000000000000, 0.9238795325112869605, 1.000000000000000000, 0.9238795325112869605, 1.000000000000000000, 0.9238795325112869605, 1.000000000000000000, 0.9238795325112869605, 1.000000000000000000, 0.9238795325112869605, 1.000000000000000000, 0.9238795325112869605, 1.000000000000000000, 0.9238795325112869605, 1.000000000000000000, 0.9238795325112869605, 1.000000000000000000, 0.9238795325112869605, 1.000000000000000000, 0.9238795325112869605, 1.000000000000000000, 0.9238795325112869605, 1.000000000000000000, 0.9238795325112869605, 1.000000000000000000, 0.9238795325112869605, 1.000000000000000000, 0.9238795325112869605, 1.000000000000000000, 0.9238795325112869605, 1.000000000000000000, 0.9238795325112869605, 1.000000000000000000, 0.9238795325112869605, 1.000000000000000000, 0.9238795325112869605, 1.000000000000000000, 0.9238795325112869605, 1.000000000000000000, 0.9238795325112869605, 1.000000000000000000, 0.9238795325112869605, 1.000000000000000000, 0.9238795325112869605, 1.000000000000000000, 0.9238795325112869605, 1.000000000000000000, 0.9238795325112869605, 1.000000000000000000, 0.9238795325112869605, 1.000000000000000000, 0.9238795325112869605, 1.000000000000000000, 0.9238795325112869605, 1.000000000000000000, 0.9238795325112869605, 1.000000000000000000, 0.9238795325112869605, 1.000000000000000000, 0.9238795325112869605, 1.000000000000000000, 0.9238795325112869605, 1.000000000000000000, 0.9238795325112869605, 1.000000000000000000, 0.9238795325112869605, 1.000000000000000000, 0.9238795325112869605, 1.000000000000000000, 0.9238795325112869605, 1.000000000000000000, 0.9238795325112869605, 1.000000000000000000, 0.9238795325112869605, 1.000000000000000000, 0.9238795325112869605, 1.000000000000000000, 0.9238795325112869605, 1.000000000000000000, 0.9238795325112869605, 1.000000000000000000, 0.9238795325112869605, 1.000000000000000000, 0.9238795325112869605, 1.000000000000000000, 0.9238795325112869605, 1.000000000000000000, 0.9238795325112869605, 1.000000000000000000, 0.9238795325112869605, 1.000000000000000000, 0.9238795325112869605, 1.000000000000000000, 0.9238795325112869605, 1.000000000000000000, 0.9238795325112869605, 1.000000000000000000, 0.9238795325112869605, 1.000000000000000000, 0.9238795325112869605, 1.000000000000000000, 0.9238795325112869605, 1.000000000000000000, 0.9238795325112869605, 1.000000000000000000, 0.9238795325112869605, 1.000000000000000000, 0.9238795325112869605, 1.000000000000000000, 0.9238795325112869605, 1.000000000000000000, 0.9238795325112869605, 1.000000000000000000, 0.9238795325112869605, 1.000000000000000000, 0.9238795325112869605, 1.000000000000000000, 0.9238795325112869605, 1.000000000000000000, 0.9238795325112869605, 1.000000000000000000, 0.9238795325112869605, 1.000000000000000000, 0.9238795325112869605, 1.000000000000000000, 0.9238795325112869605, 1.000000000000000000, 0.9238795325112869605, 1.000000000000000000, 0.9238795325112869605, 1.000000000000000000, 0.9238795325112869605, 1.000000000000000000, 0.9238795325112869605, 1.000000000000000000, 0.9238795325112869605, 1.000000000000000000, 0.9238795325112869605, 1.000000000000000000, 0.9238795325112869605, 1.000000000000000000, 0.9238795325112869605, 1.000000000000000000, 0.9238795325112869605, 1.000000000000000000, 0.9238795325112869605, 1.000000000000000000, 0.9238795325112869605, 1.000000000000000000, 0.9238795325112869605, 1.000000000000000000, 0.9238795325112869605, 1.000000000000000000, 0.9238795325112869605, 1.000000000000000000, 0.9238795325112869605, 1.000000000000000000, 0.9238795325112869605, 1.000000000000000000, 0.9238795325112869605, 1.000000000000000000, 0.9238795325112869605, 1.000000000000000000, 0.9238795325112869605, 1.000000000000000000, 0.9238795325112869605, 1.000000000000000000, 0.9238795325112869605, 1.000000000000000000, 0.9238795325112869605, 1.000000000000000000, 0.9238795325112869605, 1.000000000000000000, 0.9238795325112869605, 1.000000000000000000, 0.9238795325112869605, 1.000000000000000000, 0.9238795325112869605, 1.000000000000000000, 0.9238795325112869605, 1.000000000000000000, 0.9238795325112869605, 1.000000000000000000, 0.9238795325112869605, 1.000000000000000000, 0.9238795325112869605, 1.000000000000000000, 0.9238795325112869605, 1.000000000000000000, 0.9238795325112869605, 1.000000000000000000, 0.9238795325112869605, 1.000000000000000000, 0.9238795325112869605, 1.000000000000000000, 0.9238795325112869605, 1.000000000000000000, 0.9238795325112869605, 1.000000000000000000, 0.9238795325112869605, 1.000000000000000000, 0.9238795325112869605, 1.000000000000000000, 0.9238795325112869605, 1.000000000000000000, 0.9238795325112869605, 1.000000000000000000, 0.9238795325112869605, 1.000000000000000000, 0.9238795325112869605, 1.000000000000000000, 0.9238795325112869605, 1.000000000000000000, 0.9238795325112869605, 1.000000000000000000, 0.9238795325112869605, 1.000000000000000000, 0.9238795325112869605, 1.000000000000000000, 0.9238795325112869605, 1.000000000000000000, 0.9238795325112869605, 1.000000000000000000, 0.9238795325112869605, 1.000000000000000000, 0.9238795325112869605, 1.000000000000000000, 0.9238795325112869605, 1.000000000000000000, 0.9238795325112869605, 1.000000000000000000, 0.9238795325112869605, 1.000000000000000000, 0.9238795325112869605, 1.000000000000000000, 0.9238795325112869605, 1.000000000000000000, 0.9238795325112869605, 1.000000000000000000, 0.9238795325112869605, 1.000000000000000000, 0.9238795325112869605, 1.000000000000000000, 0.9238795325112869605, 1.000000000000000000, 0.9238795325112869605, 1.000000000000000000, 0.9238795325112869605, 1.000000000000000000, 0.9238795325112869605, 1.000000000000000000, 0.9238795325112869605, 1.000000000000000000, 0.9238795325112869605, 1.000000000000000000, 0.9238795325112869605, 1.000000000000000000, 0.9238795325112869605, 1.000000000000000000, 0.9238795325112869605, 1.000000000000000000, 0.9238795325112869605, 1.000000000000000000, 0.9238795325112869605, 1.000000000000000000, 0.9238795325112869605, 1.000000000000000000, 0.9238795325112869605, 1.000000000000000000, 0.9238795325112869605, 1.000000000000000000, 0.9238795325112869605, 1.000000000000000000, 0.9238795325112869605, 1.000000000000000000, 0.9238795325112869605, 1.000000000000000000, 0.9238795325112869605, 1.000000000000000000, 0.9238795325112869605, 1.000000000000000000, 0.9238795325112869605, 1.000000000000000000, 0.9238795325112869605, 1.000000000000000000, 0.9238795325112869605, 1.000000000000000000, 0.9238795325112869605, 1.000000000000000000, 0.9238795325112869605, 1.000000000000000000, 0.9238795325112869605, 1.000000000000000000, 0.9238795325112869605, 1.000000000000000000, 0.9238795325112869605, 1.000000000000000000, 0.9238795325112869605, 1.000000000000000000, 0.9238795325112869605, 1.000000000000000000, 0.9238795325112869605, 1.000000000000000000, 0.9238795325112869605, 1.000000000000000000, 0.9238795325112869605, 1.000000000000000000, 0.9238795325112869605, 1.000000000000000000, 0.9238795325112869605, 1.000000000000000000, 0.9238795325112869605, 1.000000000000000000, 0.9238795325112869605, 1.000000000000000000, 0.9238795325112869605, 1.000000000000000000, 0.9238795325112869605, 1.000000000000000000, 0.9238795325112869605, 1.000000000000000000, 0.9238795325112869605, 1.000000000000000000, 0.9238795325112869605, 1.000000000000000000, 0.9238795325112869605, 1.000000000000000000, 0.9238795325112869605, 1.000000000000000000, 0.9238795325112869605, 1.000000000000000000, 0.9238795325112869605, 1.000000000000000000, 0.9238795325112869605, 1.000000000000000000, 0.9238795325112869605, 1.000000000000000000, 0.9238795325112869605, 1.000000000000000000, 0.9238795325112869605, 1.000000000000000000, 0.9238795325112869605, 1.000000000000000000, 0.9238795325112869605, 1.000000000000000000, 0.9238795325112869605, 1.000000000000000000, 0.9238795325112869605, 1.000000000000000000, 0.9238795325112869605, 1.000000000000000000, 0.9238795325112869605, 1.000000000000000000, 0.9238795325112869605, 1.000000000000000000, 0.9238795325112869605, 1.000000000000000000, 0.9238795325112869605, 1.000000000000000000, 0.9238795325112869605, 1.000000000000000000, 0.9238795325112869605, 1.000000000000000000, 0.9238795325112869605, 1.000000000000000000, 0.9238795325112869605, 1.000000000000000000, 0.9238795325112869605, 1.000000000000000000, 0.9238795325112869605, 1.000000000000000000, 0.9238795325112869605, 1.000000000000000000, 0.9238795325112869605, 1.000000000000000000, 0.9238795325112869605, 1.000000000000000000, 0.9238795325112869605, 1.000000000000000000, 0.9238795325112869605, 1.000000000000000000, 0.9238795325112869605, 1.000000000000000000, 0.9238795325112869605, 1.000000000000000000, 0.9238795325112869605, 1.000000000000000000, 0.9238795325112869605, 1.000000000000000000, 0.9238795325112869605, 1.000000000000000000, 0.9238795325112869605, 1.000000000000000000, 0.9238795325112869605, 1.000000000000000000, 0.9238795325112869605, 1.000000000000000000, 0.9238795325112869605, 1.000000000000000000, 0.9238795325112869605, 1.000000000000000000, 0.9238795325112869605, 1.000000000000000000, 0.9238795325112869605, 1.000000000000000000, 0.9238795325112869605, 1.000000000000000000, 0.9238795325112869605, 1.000000000000000000, 0.9238795325112869605, 1.000000000000000000, 0.9238795325112869605, 1.000000000000000000, 0.9238795325112869605, 1.000000000000000000, 0.9238795325112869605, 1.000000000000000000, 0.9238795325112869605, 1.000000000000000000, 0.9238795325112869605, 1.000000000000000000, 0.9238795325112869605, 1.000000000000000000, 0.9238795325112869605, 1.000000000000000000, 0.9238795325112869605, 1.000000000000000000, 0.9238795325112869605, 1.000000000000000000, 0.9238795325112869605, 1.000000000000000000, 0.9238795325112869605, 1.000000000000000000, 0.9238795325112869605, 1.000000000000000000, 0.9238795325112869605, 1.000000000000000000, 0.9238795325112869605, 1.000000000000000000, 0.9238795325112869605, 1.000000000000000000, 0.9238795325112869605, 1.000000000000000000, 0.9238795325112869605, 1.000000000000000000, 0.9238795325112869605, 1.000000000000000000, 0.9238795325112869605, 1.000000000000000000, 0.9238795325112869605, 1.000000000000000000, 0.9238795325112869605, 1.000000000000000000, 0.9238795325112869605, 1.000000000000000000, 0.9238795325112869605, 1.000000000000000000, 0.9238795325112869605, 1.000000000000000000, 0.9238795325112869605, 1.000000000000000000, 0.9238795325112869605, 1.000000000000000000, 0.9238795325112869605, 1.000000000000000000, 0.9238795325112869605, 1.000000000000000000, 0.9238795325112869605, 1.000000000000000000, 0.9238795325112869605, 1.000000000000000000, 0.9238795325112869605, 1.000000000000000000, 0.9238795325112869605, 1.000000000000000000, 0.9238795325112869605, 1.000000000000000000, 0.9238795325112869605, 1.000000000000000000, 0.9238795325112869605, 1.000000000000000000, 0.9238795325112869605, 1.000000000000000000, 0.9238795325112869605, 1.000000000000000000, 0.9238795325112869605, 1.000000000000000000, 0.9238795325112869605, 1.000000000000000000, 0.9238795325112869605, 1.000000000000000000, 0.9238795325112869605, 1.000000000000000000, 0.9238795325112869605, 1.000000000000000000, 0.9238795325112869605, 1.000000000000000000, 0.9238795325112869605, 1.000000000000000000, 0.9238795325112869605, 1.000000000000000000, 0.9238795325112869605, 1.000000000000000000, 0.9238795325112869605, 1.000000000000000000, 0.9238795325112869605, 1.000000000000000000, 0.9238795325112869605, 1.000000000000000000, 0.9238795325112869605, 1.000000000000000000, 0.9238795325112869605, 1.000000000000000000, 0.9238795325112869605, 1.000000000000000000, 0.9238795325112869605, 1.000000000000000000, 0.9238795325112869605, 1.000000000000000000, 0.9238795325112869605, 1.000000000000000000, 0.9238795325112869605, 1.000000000000000000, 0.9238795325112869605, 1.000000000000000000, 0.9238795325112869605, 1.000000000000000000, 0.9238795325112869605, 1.000000000000000000, 0.9238795325112869605, 1.000000000000000000, 0.9238795325112869605, 1.000000000000000000, 0.9238795325112869605, 1.000000000000000000, 0.9238795325112869605, 1.000000000000000000, 0.9238795325112869605, 1.000000000000000000, 0.9238795325112869605, 1.000000000000000000, 0.9238795325112869605, 1.000000000000000000, 0.9238795325112869605, 1.000000000000000000, 0.9238795325112869605, 1.000000000000000000, 0.9238795325112869605, 1.000000000000000000, 0.9238795325112869605, 1.000000000000000000, 0.9238795325112869605, 1.000000000000000000, 0.9238795325112869605, 1.000000000000000000, 0.9238795325112869605, 1.000000000000000000, 0.9238795325112869605, 1.000000000000000000, 0.9238795325112869605, 1.000000000000000000, 0.9238795325112869605, 1.000000000000000000, 0.9238795325112869605, 1.000000000000000000, 0.9238795325112869605, 1.000000000000000000, 0.9238795325112869605, 1.000000000000000000, 0.9238795325112869605, 1.000000000000000000, 0.9238795325112869605, 1.000000000000000000, 0.9238795325112869605, 1.000000000000000000, 0.9238795325112869605, 1.000000000000000000, 0.9238795325112869605, 1.000000000000000000, 0.9238795325112869605, 1.000000000000000000, 0.9238795325112869605, 1.000000000000000000, 0.9238795325112869605, 1.000000000000000000, 0.9238795325112869605, 1.000000000000000000, 0.9238795325112869605, 1.000000000000000000, 0.9238795325112869605, 1.000000000000000000, 0.9238795325112869605, 1.000000000000000000, 0.9238795325112869605, 1.000000000000000000, 0.9238795325112869605, 1.000000000000000000, 0.9238795325112869605, 1.000000000000000000, 0.9238795325112869605, 1.000000000000000000, 0.9238795325112869605, 1.000000000000000000 ) ) 
 REPRESENTATION_ITEM ( '' )  ) ;
#11600=EDGE_CURVE ( 'NONE', #28962, #18481, #46022, .T. ) ;
#11602=CARTESIAN_POINT ( 'NONE',  ( 0.9500414927467378812, -0.1787899950787401604, 1.510826771599780294 ) ) ;
#11603=CARTESIAN_POINT ( 'NONE',  ( 1.054774247047244540, 0.07405724077823318263, 0.1427165353793072855 ) ) ;
#11609=CARTESIAN_POINT ( 'NONE',  ( -0.8019270111902716547, -0.1787899950787401604, 0.6446850393163160442 ) ) ;
#11614=CARTESIAN_POINT ( 'NONE',  ( 0.8019270111902717657, -0.1787899950787401604, 1.432086614119464141 ) ) ;
#11615=CARTESIAN_POINT ( 'NONE',  ( 1.002407869896990045, -0.1264236179284866091, 1.710137795221826851 ) ) ;
#11617=VECTOR ( 'NONE', #17985, 39.37007874015748143 ) ;
#11618=CARTESIAN_POINT ( 'NONE',  ( 0.8107537697050254399, 0.1574803149606300301, 0.1402559055118110520 ) ) ;
#11619=CARTESIAN_POINT ( 'NONE',  ( -0.9412147342319837628, -0.1574803149606297803, 1.449311023514519681 ) ) ;
#11623=CARTESIAN_POINT ( 'NONE',  ( -1.033464566929133799, 0.000000000000000000, 1.230314960629921295 ) ) ;
#11624=CARTESIAN_POINT ( 'NONE',  ( 0.7495606340400177148, 0.1264236179284866091, 0.3124999999462365619 ) ) ;
#11625=CARTESIAN_POINT ( 'NONE',  ( -0.9873396505805591694, -0.1113553986120547346, 1.727362204616881947 ) ) ;
#11626=CARTESIAN_POINT ( 'NONE',  ( 0.7185039370078739607, 1.928577636452523993E-17, 0.5413385826771653919 ) ) ;
#11628=CARTESIAN_POINT ( 'NONE',  ( -0.7495606340400177148, 0.1264236179284866091, 1.257381889710015743 ) ) ;
#11629=CARTESIAN_POINT ( 'NONE',  ( 0.7185039370078739607, 1.928577636452523993E-17, 0.6496062991050708391 ) ) ;
#11633=ORIENTED_EDGE ( 'NONE', *, *, #9113, .F. ) ;
#11636=CARTESIAN_POINT ( 'NONE',  ( -0.8759842519685039353, -0.1574803149606299191, 0.03937007874015843040 ) ) ;
#11637=CARTESIAN_POINT ( 'NONE',  ( 0.6971942568897637749, 2.189545951927499583E-17, 1.656003936954110412 ) ) ;
#11638=CARTESIAN_POINT ( 'NONE',  ( 1.033464566929133799, 0.000000000000000000, 0.5905511809948347235 ) ) ;
#11640=CARTESIAN_POINT ( 'NONE',  ( 0.9412147342319837628, 0.1574803149606300301, 1.906988188976377563 ) ) ;
#11641=CARTESIAN_POINT ( 'NONE',  ( 0.7185039370078739607, 1.928577636452523993E-17, 1.909448818790110192 ) ) ;
#11643=CARTESIAN_POINT ( 'NONE',  ( 0.9873396505805591694, 0.1113553986120547346, 1.304133858160188897 ) ) ;
#11645=CARTESIAN_POINT ( 'NONE',  ( -0.8759842519685039353, 0.000000000000000000, 0.000000000000000000 ) ) ;
#11647=CARTESIAN_POINT ( 'NONE',  ( 0.8019270111902717657, 0.1787899950787401604, 0.6692913385289144257 ) ) ;
#11648=CARTESIAN_POINT ( 'NONE',  ( 0.8759842519685039353, -0.1787899950787401882, 0.8833661416785196785 ) ) ;
#11650=CARTESIAN_POINT ( 'NONE',  ( -0.6971942568897637749, 2.189545951927499583E-17, 1.345964566875370139 ) ) ;
#11651=VERTEX_POINT ( 'NONE', #41938 ) ;
#11652=ADVANCED_FACE ( 'NONE', ( #20392 ), #42420, .T. ) ;
#11656=CARTESIAN_POINT ( 'NONE',  ( -1.054774247047244540, 0.07405724077823318263, 0.3051181101824569919 ) ) ;
#11666=CARTESIAN_POINT ( 'NONE',  ( -0.8107537697050234415, -0.1574803149606297803, 0.2632874014672759722 ) ) ;
#11668=CARTESIAN_POINT ( 'NONE',  ( 0.7185039370078739607, 1.928577636452523993E-17, 1.830708661309795149 ) ) ;
#11669=CARTESIAN_POINT ( 'NONE',  ( -0.8759842519685039353, 0.1787899950787401882, 0.1943897637257641919 ) ) ;
#11670=CARTESIAN_POINT ( 'NONE',  ( -0.8107537697050253289, 0.1574803149606300301, 0.8489173228346468258 ) ) ;
#11673=CARTESIAN_POINT ( 'NONE',  ( 1.033464566929133799, 0.000000000000000000, 1.545275590551181244 ) ) ;
#11674=CARTESIAN_POINT ( 'NONE',  ( -0.7185039370078746268, -0.06523048226347956391, 1.596948818790111080 ) ) ;
#11675=CARTESIAN_POINT ( 'NONE',  ( 1.054774247047244096, 0.000000000000000000, 0.9719488188438739629 ) ) ;
#11676=CARTESIAN_POINT ( 'NONE',  ( 0.7495606340400177148, 0.1264236179284866091, 0.1156496062454492185 ) ) ;
#11677=CARTESIAN_POINT ( 'NONE',  ( 0.9412147342319837628, 0.1574803149606300301, 1.473917322834645605 ) ) ;
#11678=CARTESIAN_POINT ( 'NONE',  ( 0.7126071576447854383, -0.03525399196628299647, 1.983921887778285376 ) ) ;
#11679=DIRECTION ( 'NONE',  ( -1.000000000000000000, 0.000000000000000000, 0.000000000000000000 ) ) ;
#11680=CARTESIAN_POINT ( 'NONE',  ( 0.9873396505805591694, 0.1113553986120547346, 0.3198818896562523606 ) ) ;
#11683=CARTESIAN_POINT ( 'NONE',  ( 0.7495606340400177148, 0.1264236179284866091, 0.8636811023084409733 ) ) ;
#11686=ORIENTED_EDGE ( 'NONE', *, *, #33675, .T. ) ;
#11690=CARTESIAN_POINT ( 'NONE',  ( 0.9500414927467378812, 0.1787899950787401604, 1.210629921206079818 ) ) ;
#11695=CARTESIAN_POINT ( 'NONE',  ( -1.054774247047244096, 0.000000000000000000, 0.1796259841982051075 ) ) ;
#11698=CARTESIAN_POINT ( 'NONE',  ( -1.033464566929134687, 0.06523048226347956391, 0.6028543307086614567 ) ) ;
#11699=CARTESIAN_POINT ( 'NONE',  ( -1.054774247047244540, 0.07405724077823318263, 1.796259842465923073 ) ) ;
#11701=CARTESIAN_POINT ( 'NONE',  ( -0.6971942568897648851, -0.07405724077823297447, 0.8710629920722218200 ) ) ;
#11702=CARTESIAN_POINT ( 'NONE',  ( -0.7495606340400177148, -0.1264236179284866091, 0.5241141731745827537 ) ) ;
#11703=EDGE_CURVE ( 'NONE', #7899, #36581, #2409, .T. ) ;
#11705=CARTESIAN_POINT ( 'NONE',  ( 1.033464566929133799, 0.000000000000000000, 0.3937007872940480047 ) ) ;
#11707=CARTESIAN_POINT ( 'NONE',  ( 1.054774247047244096, 0.000000000000000000, 0.02214566923757503927 ) ) ;
#11713=EDGE_CURVE ( 'NONE', #13468, #3727, #37048, .T. ) ;
#11716=CARTESIAN_POINT ( 'NONE',  ( -1.002407869896990045, -0.1264236179284866091, 0.2928149605761578567 ) ) ;
#11720=ORIENTED_EDGE ( 'NONE', *, *, #43269, .F. ) ;
#11729=CARTESIAN_POINT ( 'NONE',  ( 1.033464566929133799, 0.000000000000000000, 0.5216535433070865757 ) ) ;
#11731=CARTESIAN_POINT ( 'NONE',  ( -0.8107537697050253289, 0.1574803149606300301, 1.114665354223180804 ) ) ;
#11732=CARTESIAN_POINT ( 'NONE',  ( 0.8759842519685039353, 0.1787899950787401882, 0.5093503936470236138 ) ) ;
#11735=CARTESIAN_POINT ( 'NONE',  ( 0.7185039370078739607, 1.928577636452523993E-17, 1.909448818790110192 ) ) ;
#11737=DIRECTION ( 'NONE',  ( -1.000000000000000000, 0.000000000000000000, 0.000000000000000000 ) ) ;
#11738=CARTESIAN_POINT ( 'NONE',  ( -0.9500414927467377701, -0.1787899950787401604, 0.9251968503399373711 ) ) ;
#11739=CARTESIAN_POINT ( 'NONE',  ( 0.9873396505805591694, 0.1113553986120547346, 0.8809055118110236116 ) ) ;
#11741=CARTESIAN_POINT ( 'NONE',  ( 0.9873396505805591694, -0.1113553986120547346, 0.7529527559055118058 ) ) ;
#11746=ORIENTED_EDGE ( 'NONE', *, *, #44785, .F. ) ;
#11747=CARTESIAN_POINT ( 'NONE',  ( -0.9412147342319837628, 0.1574803149606300301, 1.779035432963339769 ) ) ;
#11748=CARTESIAN_POINT ( 'NONE',  ( 0.7185039370078739607, 1.928577636452523993E-17, 1.161417322727118284 ) ) ;
#11752=CARTESIAN_POINT ( 'NONE',  ( 1.033464566929134687, -0.06523048226347956391, 1.060531495955465031 ) ) ;
#11756=CARTESIAN_POINT ( 'NONE',  ( -0.6971942568897648851, 0.07405724077823318263, 1.697834645615527771 ) ) ;
#11757=CARTESIAN_POINT ( 'NONE',  ( 0.9500414927467378812, -0.1787899950787401604, 1.633858267662771313 ) ) ;
#11760=FACE_OUTER_BOUND ( 'NONE', #20047, .T. ) ;
#11761=CARTESIAN_POINT ( 'NONE',  ( -0.8759842519685039353, 0.000000000000000000, 0.000000000000000000 ) ) ;
#11762=CARTESIAN_POINT ( 'NONE',  ( 0.6971942568897637749, 2.189545951927499583E-17, 0.2436023621509610382 ) ) ;
#11764=CARTESIAN_POINT ( 'NONE',  ( -0.6971942568897637749, 2.189545951927499583E-17, 1.222933070812378009 ) ) ;
#11765=CARTESIAN_POINT ( 'NONE',  ( -0.7495606340400177148, 0.1264236179284866091, 0.9424212597887559051 ) ) ;
#11766=CARTESIAN_POINT ( 'NONE',  ( -1.054774247047244540, -0.07405724077823318263, 0.06397637789899228433 ) ) ;
#11767=ADVANCED_FACE ( 'NONE', ( #24948 ), #28811, .T. ) ;
#11768=CARTESIAN_POINT ( 'NONE',  ( -0.8759842519685039353, 0.000000000000000000, 0.000000000000000000 ) ) ;
#11769=CARTESIAN_POINT ( 'NONE',  ( -0.7495606340400177148, 0.1264236179284866091, 1.577263779473795369 ) ) ;
#11770=CARTESIAN_POINT ( 'NONE',  ( -1.033464566929133799, 0.000000000000000000, 1.811023621939716444 ) ) ;
#11773=CARTESIAN_POINT ( 'NONE',  ( -1.033464566929134687, 0.06523048226347956391, 1.665846456692914312 ) ) ;
#11774=CYLINDRICAL_SURFACE ( 'NONE', #42713, 0.1574803149606299191 ) ;
#11775=CARTESIAN_POINT ( 'NONE',  ( 0.8019270111902716547, -0.1787899950787401604, 1.628937007820252303 ) ) ;
#11778=EDGE_CURVE ( 'NONE', #8150, #22180, #32635, .T. ) ;
#11780=ORIENTED_EDGE ( 'NONE', *, *, #40396, .F. ) ;
#11781=EDGE_CURVE ( 'NONE', #13902, #20455, #19283, .T. ) ;
#11782=ORIENTED_EDGE ( 'NONE', *, *, #16203, .F. ) ;
#11788=CARTESIAN_POINT ( 'NONE',  ( 0.6971942568897637749, 2.189545951927499583E-17, 1.774114173174582643 ) ) ;
#11791=CARTESIAN_POINT ( 'NONE',  ( -1.033464566929133799, 0.000000000000000000, 0.9055118109160944506 ) ) ;
#11793=CARTESIAN_POINT ( 'NONE',  ( 0.8019270111902717657, -0.1787899950787401604, 0.8366141731745828647 ) ) ;
#11796=CYLINDRICAL_SURFACE ( 'NONE', #8885, 0.1574803149606299191 ) ;
#11798=CARTESIAN_POINT ( 'NONE',  ( 0.8759842519685039353, -0.1787899950787401882, 1.867618110182456714 ) ) ;
#11799=CARTESIAN_POINT ( 'NONE',  ( 0.9873396505805591694, 0.1113553986120547346, 0.09350393700787401619 ) ) ;
#11804=CARTESIAN_POINT ( 'NONE',  ( 1.054774247047244540, 0.07405724077823318263, 0.2657480314422993595 ) ) ;
#11806=CARTESIAN_POINT ( 'NONE',  ( -0.8759842519685039353, 0.1787899950787401882, 1.803641732229700700 ) ) ;
#11808=CARTESIAN_POINT ( 'NONE',  ( -0.9500414927467378812, -0.1787899950787401604, 1.358267716481669662 ) ) ;
#11809=CARTESIAN_POINT ( 'NONE',  ( -0.8107537697050254399, 0.1574803149606300301, 0.8882874015748026819 ) ) ;
#11810=CARTESIAN_POINT ( 'NONE',  ( 0.7495606340400177148, 0.1264236179284866091, 0.04183070860765386589 ) ) ;
#11811=CARTESIAN_POINT ( 'NONE',  ( -0.6971942568897648851, -0.07405724077823297447, 1.067913385773007651 ) ) ;
#11814=CARTESIAN_POINT ( 'NONE',  ( 0.6971942568897637749, 2.189545951927499583E-17, 0.5191929133320630774 ) ) ;
#11815=CARTESIAN_POINT ( 'NONE',  ( -0.9500414927467377701, 0.1787899950787401604, 0.4232283464029293896 ) ) ;
#11817=EDGE_CURVE ( 'NONE', #18659, #6785, #32471, .T. ) ;
#11818=CARTESIAN_POINT ( 'NONE',  ( -0.9412147342319837628, 0.1574803149606300301, 0.8735236219397174429 ) ) ;
#11819=CARTESIAN_POINT ( 'NONE',  ( -0.8759842519685039353, 0.1574803149606299191, 0.1377952755905511861 ) ) ;
#11821=VERTEX_POINT ( 'NONE', #46734 ) ;
#11823=CARTESIAN_POINT ( 'NONE',  ( -0.7185039370078746268, -0.06523048226347956391, 1.291830708661417360 ) ) ;
#11825=CARTESIAN_POINT ( 'NONE',  ( -0.8759842519685039353, -0.1787899950787401882, 0.05167322829269314910 ) ) ;
#11831=CARTESIAN_POINT ( 'NONE',  ( 0.7495606340400177148, -0.1264236179284866091, 1.188484251914740275 ) ) ;
#11832=CARTESIAN_POINT ( 'NONE',  ( 0.9873396505805591694, 0.1113553986120547346, 1.589566929133858331 ) ) ;
#11835=CARTESIAN_POINT ( 'NONE',  ( 0.6971942568897648851, -0.07405724077823297447, 1.500984251914741607 ) ) ;
#11840=EDGE_CURVE ( 'NONE', #32303, #47141, #17982, .T. ) ;
#11841=CARTESIAN_POINT ( 'NONE',  ( -0.8759842519685039353, -0.1787899950787401882, 0.6471456692375747721 ) ) ;
#11843=CARTESIAN_POINT ( 'NONE',  ( 0.8107537697050234415, -0.1574803149606297803, 0.3026574802074336046 ) ) ;
#11847=CARTESIAN_POINT ( 'NONE',  ( 0.7495606340400177148, 0.1264236179284866091, 1.769192913332062966 ) ) ;
#11850=CARTESIAN_POINT ( 'NONE',  ( -1.033464566929133799, 0.000000000000000000, 0.6791338582677166613 ) ) ;
#11852=CARTESIAN_POINT ( 'NONE',  ( 0.9873396505805591694, -0.1113553986120547346, 0.9005905510735748853 ) ) ;
#11855=CARTESIAN_POINT ( 'NONE',  ( 1.054774247047244096, 0.000000000000000000, 0.2977362204186775885 ) ) ;
#11856=CARTESIAN_POINT ( 'NONE',  ( 0.9500414927467377701, -0.1787899950787401604, 1.235236220418678199 ) ) ;
#11860=CARTESIAN_POINT ( 'NONE',  ( -0.7495606340400177148, 0.1264236179284866091, 1.375492125930488196 ) ) ;
#11861=CARTESIAN_POINT ( 'NONE',  ( 0.7185039370078746268, -0.06523048226347956391, 0.6520669290263312323 ) ) ;
#11862=ORIENTED_EDGE ( 'NONE', *, *, #8528, .T. ) ;
#11863=CARTESIAN_POINT ( 'NONE',  ( -1.033464566929133799, 0.000000000000000000, 1.742125984251968518 ) ) ;
#11864=CARTESIAN_POINT ( 'NONE',  ( 0.8107537697050254399, 0.1574803149606300301, 0.6914370078740148529 ) ) ;
#11865=ORIENTED_EDGE ( 'NONE', *, *, #9224, .F. ) ;
#11869=CARTESIAN_POINT ( 'NONE',  ( 0.8019270111902717657, 0.1787899950787401604, 1.569881889710015299 ) ) ;
#11870=CARTESIAN_POINT ( 'NONE',  ( -0.7185039370078746268, -0.06523048226347956391, 1.291830708661417360 ) ) ;
#11871=CARTESIAN_POINT ( 'NONE',  ( 0.7646288533564489232, 0.1113553986120547346, 0.2509842518609771700 ) ) ;
#11874=CARTESIAN_POINT ( 'NONE',  ( 0.6971942568897626646, 0.07405724077823318263, 0.04429133852891373180 ) ) ;
#11880=EDGE_LOOP ( 'NONE', ( #27529, #10084, #19052, #35979 ) ) ;
#11881=CARTESIAN_POINT ( 'NONE',  ( 1.002407869896990045, 0.1264236179284866091, 0.9768700786863937502 ) ) ;
#11883=CARTESIAN_POINT ( 'NONE',  ( -0.7495606340400177148, 0.1264236179284866091, 1.262303149552535420 ) ) ;
#11884=ORIENTED_EDGE ( 'NONE', *, *, #1730, .T. ) ;
#11886=( BOUNDED_CURVE ( )  B_SPLINE_CURVE ( 2, ( #24918, #2380, #24678, #42623, #39508, #28776, #43344, #10545, #25143 ),
 .UNSPECIFIED., .F., .F. ) 
 B_SPLINE_CURVE_WITH_KNOTS ( ( 3, 2, 2, 2, 3 ),
 ( 0.7600000000000000089, 0.7624999999999999556, 0.7650000000000000133, 0.7674999999999999600, 0.7700000000000000178 ),
 .UNSPECIFIED. ) 
 CURVE ( )  GEOMETRIC_REPRESENTATION_ITEM ( )  RATIONAL_B_SPLINE_CURVE ( ( 1.000000000000000000, 0.9238795325112869605, 1.000000000000000000, 0.9238795325112869605, 1.000000000000000000, 0.9238795325112869605, 1.000000000000000000, 0.9238795325112829637, 1.000000000000000000 ) ) 
 REPRESENTATION_ITEM ( '' )  ) ;
#11887=CARTESIAN_POINT ( 'NONE',  ( -0.9500414927467378812, 0.1787899950787401604, 0.3100393700249766682 ) ) ;
#11890=CIRCLE ( 'NONE', #9560, 0.1574803149606299191 ) ;
#11891=CYLINDRICAL_SURFACE ( 'NONE', #20598, 0.1574803149606299191 ) ;
#11893=EDGE_LOOP ( 'NONE', ( #11720, #31674, #22413, #1819 ) ) ;
#11894=VERTEX_POINT ( 'NONE', #8861 ) ;
#11897=ORIENTED_EDGE ( 'NONE', *, *, #13562, .T. ) ;
#11900=CARTESIAN_POINT ( 'NONE',  ( 0.7185039370078692977, 0.06523048226347515077, 1.434547243986962428 ) ) ;
#11901=CARTESIAN_POINT ( 'NONE',  ( -0.7495606340400177148, -0.1264236179284866091, 0.2485236219934806867 ) ) ;
#11902=CARTESIAN_POINT ( 'NONE',  ( -0.9412147342319837628, 0.1574803149606300301, 0.9621062992125994917 ) ) ;
#11905=CARTESIAN_POINT ( 'NONE',  ( 0.7185039370078739607, 1.928577636452523993E-17, 1.092519685039370136 ) ) ;
#11906=CARTESIAN_POINT ( 'NONE',  ( -0.8759842519685039353, -0.1574803149606299191, 1.525590551073574774 ) ) ;
#11907=CARTESIAN_POINT ( 'NONE',  ( 0.8019270111902717657, -0.1787899950787401604, 0.9202755904974182499 ) ) ;
#11908=CARTESIAN_POINT ( 'NONE',  ( 0.8019270111902716547, -0.1787899950787401604, 1.348425196796630976 ) ) ;
#11910=CARTESIAN_POINT ( 'NONE',  ( 0.7646288533564489232, 0.1113553986120547346, 0.5265748030420794867 ) ) ;
#11911=CARTESIAN_POINT ( 'NONE',  ( 0.8107537697050253289, 0.1574803149606300301, 1.360728346456693050 ) ) ;
#11912=CARTESIAN_POINT ( 'NONE',  ( 0.7171850904892348444, -0.05464115389802457617, 1.984299705265581304 ) ) ;
#11914=CARTESIAN_POINT ( 'NONE',  ( 0.7185039370078739607, 1.928577636452523993E-17, 1.476377952648377789 ) ) ;
#11917=CARTESIAN_POINT ( 'NONE',  ( 0.9500414927467377701, -0.1787899950787401604, 0.8021653542769462408 ) ) ;
#11918=CARTESIAN_POINT ( 'NONE',  ( 0.6971942568897648851, 0.07405724077823318263, 1.776574803095843702 ) ) ;
#11920=AXIS2_PLACEMENT_3D ( 'NONE', #29616, #22355, #7741 ) ;
#11924=CARTESIAN_POINT ( 'NONE',  ( 1.033464566929133355, -0.06523048226348075740, 0.4306102361129452438 ) ) ;
#11928=CARTESIAN_POINT ( 'NONE',  ( -0.8759842519685039353, -0.1574803149606299191, 0.06889763768774861963 ) ) ;
#11929=CARTESIAN_POINT ( 'NONE',  ( 1.054774247047244540, 0.07405724077823318263, 1.126968503883244654 ) ) ;
#11933=ADVANCED_FACE ( 'NONE', ( #22761 ), #1411, .T. ) ;
#11936=CARTESIAN_POINT ( 'NONE',  ( -0.9500414927467378812, -0.1787899950787401604, 0.2903543306548980185 ) ) ;
#11937=ORIENTED_EDGE ( 'NONE', *, *, #32102, .F. ) ;
#11938=CARTESIAN_POINT ( 'NONE',  ( 0.8107537697050254399, 0.1574803149606300301, 1.754429133858266932 ) ) ;
#11940=CARTESIAN_POINT ( 'NONE',  ( -0.6971942568897648851, 0.07405724077823318263, 1.771653543253322249 ) ) ;
#11941=CARTESIAN_POINT ( 'NONE',  ( -0.7495606340400177148, -0.1264236179284866091, 0.9522637794737952577 ) ) ;
#11942=CARTESIAN_POINT ( 'NONE',  ( -1.002407869896990045, -0.1264236179284866091, 0.4552165353793071745 ) ) ;
#11946=CARTESIAN_POINT ( 'NONE',  ( -1.033464566929133799, 0.000000000000000000, 0.3149606298137326843 ) ) ;
#11950=DIRECTION ( 'NONE',  ( -1.000000000000000000, 0.000000000000000000, 0.000000000000000000 ) ) ;
#11951=CARTESIAN_POINT ( 'NONE',  ( 0.8759842519685039353, -0.1574803149606299191, 1.929133858267716661 ) ) ;
#11954=CARTESIAN_POINT ( 'NONE',  ( -0.8759842491179902213, 0.1574803149606299191, 1.978346456692913646 ) ) ;
#11955=CARTESIAN_POINT ( 'NONE',  ( -1.002407869896990045, 0.1264236179284866091, 0.3026574802611972648 ) ) ;
#11956=CARTESIAN_POINT ( 'NONE',  ( -1.033464566929133799, 1.928577636452524610E-17, 2.869337061179095023E-17 ) ) ;
#11957=VERTEX_POINT ( 'NONE', #23252 ) ;
#11960=CARTESIAN_POINT ( 'NONE',  ( -1.002407869896990045, 0.1264236179284866091, 1.488681102308440751 ) ) ;
#11966=CARTESIAN_POINT ( 'NONE',  ( 1.033464566929134687, 0.06523048226347956391, 0.5241141732283461918 ) ) ;
#11968=CARTESIAN_POINT ( 'NONE',  ( -0.8107537697050253289, 0.1574803149606300301, 1.154035432963338659 ) ) ;
#11969=CARTESIAN_POINT ( 'NONE',  ( 1.054774247047244096, 0.000000000000000000, 0.06151574797773248782 ) ) ;
#11972=CARTESIAN_POINT ( 'NONE',  ( 0.9412147342319837628, 0.1574803149606300301, 1.936515747923967856 ) ) ;
#11974=EDGE_CURVE ( 'NONE', #461, #33076, #30936, .T. ) ;
#11977=DIRECTION ( 'NONE',  ( 1.822029033848725028E-16, 0.000000000000000000, 1.000000000000000000 ) ) ;
#11978=CARTESIAN_POINT ( 'NONE',  ( 0.9412147342319837628, -0.1574803149606297803, 1.537893700787401841 ) ) ;
#11980=ORIENTED_EDGE ( 'NONE', *, *, #43584, .F. ) ;
#11988=CARTESIAN_POINT ( 'NONE',  ( 0.9412147342319837628, 0.1574803149606300301, 1.149114173120819427 ) ) ;
#11989=CARTESIAN_POINT ( 'NONE',  ( 0.8759842519685039353, 0.000000000000000000, 4.498031496062992574 ) ) ;
#11993=CARTESIAN_POINT ( 'NONE',  ( -0.9500414927467378812, 0.1787899950787401604, 1.766732283410803461 ) ) ;
#11994=CARTESIAN_POINT ( 'NONE',  ( -0.9873396505805591694, -0.1113553986120547346, 0.5954724409448819422 ) ) ;
#11995=CARTESIAN_POINT ( 'NONE',  ( 0.6971942568897648851, -0.07405724077823297447, 1.702755905458047003 ) ) ;
#11996=CARTESIAN_POINT ( 'NONE',  ( 0.7185039370078739607, 1.928577636452523993E-17, 1.791338582569637738 ) ) ;
#11997=CARTESIAN_POINT ( 'NONE',  ( 0.6971942568897626646, 0.07405724077823318263, 0.3198818897100162983 ) ) ;
#11998=CARTESIAN_POINT ( 'NONE',  ( -1.002407869896990045, 0.1264236179284866091, 1.444389763725763665 ) ) ;
#11999=DIRECTION ( 'NONE',  ( 0.000000000000000000, 0.000000000000000000, -1.000000000000000000 ) ) ;
#12000=CARTESIAN_POINT ( 'NONE',  ( -0.8019270111902716547, -0.1787899950787401604, 1.230314960576158967 ) ) ;
#12001=CARTESIAN_POINT ( 'NONE',  ( -0.8019270111902717657, 0.1787899950787401604, 0.9005905511273389896 ) ) ;
#12002=CARTESIAN_POINT ( 'NONE',  ( -0.6971942568897637749, 2.189545951927499583E-17, 0.04675196845017354913 ) ) ;
#12003=( BOUNDED_CURVE ( )  B_SPLINE_CURVE ( 2, ( #12828, #23125, #12597, #19986, #22883, #34166, #15474, #5128, #15951 ),
 .UNSPECIFIED., .F., .T. ) 
 B_SPLINE_CURVE_WITH_KNOTS ( ( 3, 2, 2, 2, 3 ),
 ( 0.3599999999999999867, 0.3624999999999999889, 0.3649999999999999911, 0.3674999999999999933, 0.3699999999999999956 ),
 .UNSPECIFIED. ) 
 CURVE ( )  GEOMETRIC_REPRESENTATION_ITEM ( )  RATIONAL_B_SPLINE_CURVE ( ( 1.000000000000000000, 0.9238795325112869605, 1.000000000000000000, 0.9238795325112869605, 1.000000000000000000, 0.9238795325112869605, 1.000000000000000000, 0.9238795325112869605, 1.000000000000000000 ) ) 
 REPRESENTATION_ITEM ( '' )  ) ;
#12005=CARTESIAN_POINT ( 'NONE',  ( -1.054774247047244540, -0.07405724077823318263, 1.599409448765135133 ) ) ;
#12006=CARTESIAN_POINT ( 'NONE',  ( -1.054774247047244096, 0.000000000000000000, 0.02706692908009476414 ) ) ;
#12008=CARTESIAN_POINT ( 'NONE',  ( -0.8759842519685039353, 0.000000000000000000, 2.007874015640504162 ) ) ;
#12009=CARTESIAN_POINT ( 'NONE',  ( 0.7495606340400177148, -0.1264236179284866091, 1.547736220418677089 ) ) ;
#12013=EDGE_LOOP ( 'NONE', ( #5149, #43314, #19935, #17708 ) ) ;
#12014=CARTESIAN_POINT ( 'NONE',  ( -0.9500414927467377701, 0.1787899950787401604, 1.176181102308441195 ) ) ;
#12017=( BOUNDED_CURVE ( )  B_SPLINE_CURVE ( 2, ( #26430, #25726, #12044, #14689, #7716, #36502, #26666, #15644, #18279 ),
 .UNSPECIFIED., .F., .T. ) 
 B_SPLINE_CURVE_WITH_KNOTS ( ( 3, 2, 2, 2, 3 ),
 ( 0.5100000000000000089, 0.5124999999999999556, 0.5150000000000000133, 0.5174999999999999600, 0.5200000000000000178 ),
 .UNSPECIFIED. ) 
 CURVE ( )  GEOMETRIC_REPRESENTATION_ITEM ( )  RATIONAL_B_SPLINE_CURVE ( ( 1.000000000000000000, 0.9238795325112869605, 1.000000000000000000, 0.9238795325112869605, 1.000000000000000000, 0.9238795325112869605, 1.000000000000000000, 0.9238795325112869605, 1.000000000000000000 ) ) 
 REPRESENTATION_ITEM ( '' )  ) ;
#12019=DIRECTION ( 'NONE',  ( 0.000000000000000000, 0.000000000000000000, -1.000000000000000000 ) ) ;
#12020=CARTESIAN_POINT ( 'NONE',  ( 0.8107537697050234415, -0.1574803149606297803, 0.3125000000000000000 ) ) ;
#12024=CARTESIAN_POINT ( 'NONE',  ( -1.033464566929134687, 0.06523048226347956391, 0.1304133858267717272 ) ) ;
#12025=CARTESIAN_POINT ( 'NONE',  ( 0.6971942568897626646, -0.07405724077823297447, 0.7529527558517473684 ) ) ;
#12030=DIRECTION ( 'NONE',  ( -1.000000000000000000, 0.000000000000000000, 0.000000000000000000 ) ) ;
#12031=CARTESIAN_POINT ( 'NONE',  ( 1.054774247047244540, 0.07405724077823318263, 1.761811023568284007 ) ) ;
#12034=CARTESIAN_POINT ( 'NONE',  ( 0.9412147342319837628, 0.1574803149606300301, 0.09596456692913378494 ) ) ;
#12040=CARTESIAN_POINT ( 'NONE',  ( 0.6971942568897626646, 0.07405724077823318263, 0.2805118109698587214 ) ) ;
#12041=CARTESIAN_POINT ( 'NONE',  ( -0.6971942568897648851, -0.07405724077823297447, 1.776574803095843924 ) ) ;
#12042=VERTEX_POINT ( 'NONE', #16072 ) ;
#12043=CARTESIAN_POINT ( 'NONE',  ( -1.002407869896990045, 0.1264236179284866091, 1.331200787347811110 ) ) ;
#12044=CARTESIAN_POINT ( 'NONE',  ( 0.7646288533564489232, -0.1113553986120547346, 1.018700787401574770 ) ) ;
#12046=CARTESIAN_POINT ( 'NONE',  ( 1.002407869896990045, 0.1264236179284866091, 0.03198818892261445085 ) ) ;
#12047=CARTESIAN_POINT ( 'NONE',  ( -0.9500414927467378812, 0.1787899950787401604, 1.171259842465921741 ) ) ;
#12048=CARTESIAN_POINT ( 'NONE',  ( 1.033464566929134687, 0.06523048226347956391, 1.537893700679874076 ) ) ;
#12051=CARTESIAN_POINT ( 'NONE',  ( 1.002407869896990045, -0.1264236179284866091, 0.4552165353793071745 ) ) ;
#12052=CARTESIAN_POINT ( 'NONE',  ( -0.7495606340400177148, -0.1264236179284866091, 0.3617125983714334359 ) ) ;
#12053=VERTEX_POINT ( 'NONE', #15599 ) ;
#12054=VERTEX_POINT ( 'NONE', #30697 ) ;
#12055=CARTESIAN_POINT ( 'NONE',  ( 0.9500414927467378812, -0.1787899950787401604, 0.9251968503399374821 ) ) ;
#12056=CARTESIAN_POINT ( 'NONE',  ( -0.7185039370078746268, 0.06523048226347956391, 0.1451771653543309226 ) ) ;
#12057=CARTESIAN_POINT ( 'NONE',  ( 0.9500414927467377701, 0.1787899950787401604, 1.176181102308441195 ) ) ;
#12058=CARTESIAN_POINT ( 'NONE',  ( 1.033464566929134687, 0.06523048226347956391, 1.931594488081448180 ) ) ;
#12061=CARTESIAN_POINT ( 'NONE',  ( -1.033464566929133799, 0.000000000000000000, 0.3248031496062992463 ) ) ;
#12062=CARTESIAN_POINT ( 'NONE',  ( 0.8759842519685039353, -0.1574803149606299191, 0.3149606299212598381 ) ) ;
#12067=VERTEX_POINT ( 'NONE', #19641 ) ;
#12068=CARTESIAN_POINT ( 'NONE',  ( 1.054774247047244540, -0.07405724077823318263, 1.279527559001355286 ) ) ;
#12070=LINE ( 'NONE', #26693, #2423 ) ;
#12072=CARTESIAN_POINT ( 'NONE',  ( 0.8759842519685039353, 0.1787899950787401882, 0.1894685038832444879 ) ) ;
#12078=EDGE_CURVE ( 'NONE', #3940, #3727, #4775, .T. ) ;
#12079=CARTESIAN_POINT ( 'NONE',  ( -0.7495606340400177148, 0.1264236179284866091, 0.7111220471903307860 ) ) ;
#12080=DIRECTION ( 'NONE',  ( -1.000000000000000000, 0.000000000000000000, 0.000000000000000000 ) ) ;
#12082=CARTESIAN_POINT ( 'NONE',  ( 0.9873396505805591694, -0.1113553986120547346, 0.3100393699712130080 ) ) ;
#12086=CARTESIAN_POINT ( 'NONE',  ( 0.8759842519685039353, 0.1787899950787401882, 1.375492125930488196 ) ) ;
#12087=CARTESIAN_POINT ( 'NONE',  ( 1.054774247047244540, 0.07405724077823318263, 1.914370078686394860 ) ) ;
#12088=CARTESIAN_POINT ( 'NONE',  ( 1.033464566929134687, 0.06523048226347956391, 1.498523621939716444 ) ) ;
#12092=CARTESIAN_POINT ( 'NONE',  ( -0.7533556175591157311, 0.1062596105467954882, 1.981019962422237990 ) ) ;
#12095=CARTESIAN_POINT ( 'NONE',  ( 0.7185039370078732945, -0.06523048226347899492, 0.5339566928058584461 ) ) ;
#12096=CARTESIAN_POINT ( 'NONE',  ( 0.9500414927467378812, 0.1787899950787401604, 0.3051181101824569919 ) ) ;
#12099=CARTESIAN_POINT ( 'NONE',  ( -0.7185039370078739607, 1.928577636452523993E-17, 0.9645669290263307882 ) ) ;
#12100=CARTESIAN_POINT ( 'NONE',  ( -1.002407869896990045, -0.1264236179284866091, 1.277066929080094448 ) ) ;
#12101=CARTESIAN_POINT ( 'NONE',  ( 1.033464566929134687, -0.06523048226347956391, 0.7062007872940467834 ) ) ;
#12102=VERTEX_POINT ( 'NONE', #42602 ) ;
#12103=CARTESIAN_POINT ( 'NONE',  ( 0.7646288533564489232, 0.1113553986120547346, 1.402559055118110187 ) ) ;
#12109=CARTESIAN_POINT ( 'NONE',  ( 0.6971942568897648851, 0.07405724077823318263, 1.614173228292692386 ) ) ;
#12110=CARTESIAN_POINT ( 'NONE',  ( -1.033464566929134687, -0.06523048226347956391, 1.267224409448818978 ) ) ;
#12111=CARTESIAN_POINT ( 'NONE',  ( -0.7185039370078739607, 1.928577636452523993E-17, 1.161417322727118284 ) ) ;
#12112=CARTESIAN_POINT ( 'NONE',  ( -1.033464566929133799, 0.000000000000000000, 1.820866141732283561 ) ) ;
#12113=DIRECTION ( 'NONE',  ( 1.000000000000000000, 0.000000000000000000, 0.000000000000000000 ) ) ;
#12114=CARTESIAN_POINT ( 'NONE',  ( -0.7185039370078746268, -0.06523048226347956391, 0.4945866140657015353 ) ) ;
#12115=CARTESIAN_POINT ( 'NONE',  ( 0.7185039370078746268, 0.06523048226347956391, 1.316437007766489975 ) ) ;
#12118=CARTESIAN_POINT ( 'NONE',  ( 1.054774247047244540, -0.07405724077823318263, 0.9301181101824563813 ) ) ;
#12119=CARTESIAN_POINT ( 'NONE',  ( -0.8019270111902716547, 0.1787899950787401604, 1.569881889710015299 ) ) ;
#12121=CARTESIAN_POINT ( 'NONE',  ( -0.7495606340400177148, -0.1264236179284866091, 1.350885826717889815 ) ) ;
#12123=ADVANCED_FACE ( 'NONE', ( #2596 ), #28264, .T. ) ;
#12124=CARTESIAN_POINT ( 'NONE',  ( -1.002407869896990045, 0.1264236179284866091, 0.3863188975840318173 ) ) ;
#12126=CARTESIAN_POINT ( 'NONE',  ( -1.033464566929133799, 0.000000000000000000, 1.889763779420031486 ) ) ;
#12128=ORIENTED_EDGE ( 'NONE', *, *, #24040, .T. ) ;
#12132=CARTESIAN_POINT ( 'NONE',  ( 1.033464566929133799, 0.000000000000000000, 1.141732283357039357 ) ) ;
#12134=CARTESIAN_POINT ( 'NONE',  ( 0.8107537697050254399, 0.1574803149606300301, 1.429625984144440531 ) ) ;
#12135=VECTOR ( 'NONE', #27592, 39.37007874015748143 ) ;
#12137=CARTESIAN_POINT ( 'NONE',  ( -0.9500414927467377701, 0.1787899950787401604, 0.2312992125446618197 ) ) ;
#12138=CARTESIAN_POINT ( 'NONE',  ( -0.7646288533564489232, 0.1113553986120547346, 0.8120078740157481434 ) ) ;
#12141=CARTESIAN_POINT ( 'NONE',  ( -1.033464566929133799, 0.000000000000000000, 1.663385826771653697 ) ) ;
#12142=CARTESIAN_POINT ( 'NONE',  ( 0.6971942568897626646, 0.07405724077823318263, 0.9891732282926934960 ) ) ;
#12143=CARTESIAN_POINT ( 'NONE',  ( 1.054774247047244096, 0.000000000000000000, 1.439468503883244210 ) ) ;
#12144=CARTESIAN_POINT ( 'NONE',  ( 0.6971942568897637749, 2.189545951927499583E-17, 0.1205708660879689087 ) ) ;
#12145=CARTESIAN_POINT ( 'NONE',  ( -1.033464566929134687, 0.06523048226347956391, 0.4453740157480309270 ) ) ;
#12146=CARTESIAN_POINT ( 'NONE',  ( 0.9412147342319837628, 0.1574803149606300301, 1.552657480314961536 ) ) ;
#12147=CARTESIAN_POINT ( 'NONE',  ( 0.7101756151665713501, 0.004432158464400415970, 1.983187800286568381 ) ) ;
#12151=CARTESIAN_POINT ( 'NONE',  ( 0.8019270111902716547, 0.1787899950787401604, 0.7824803149068668695 ) ) ;
#12152=CARTESIAN_POINT ( 'NONE',  ( -0.8107537697050254399, -0.1574803149606297803, 1.414862204724410377 ) ) ;
#12153=CARTESIAN_POINT ( 'NONE',  ( 0.8019270111902716547, -0.1787899950787401604, 1.865157480261198097 ) ) ;
#12156=CARTESIAN_POINT ( 'NONE',  ( 1.033464566929133799, 0.000000000000000000, 0.9153543307086614567 ) ) ;
#12158=CARTESIAN_POINT ( 'NONE',  ( -1.033464566929134687, 0.06523048226347956391, 0.04183070855389029591 ) ) ;
#12159=CARTESIAN_POINT ( 'NONE',  ( 0.8019270111902717657, -0.1787899950787401604, 1.072834645615528659 ) ) ;
#12165=CARTESIAN_POINT ( 'NONE',  ( -0.8019270111902717657, -0.1787899950787401604, 0.3248031495525355306 ) ) ;
#12166=ORIENTED_EDGE ( 'NONE', *, *, #28263, .F. ) ;
#12169=CARTESIAN_POINT ( 'NONE',  ( -0.7495606340400177148, -0.1264236179284866091, 1.779035433017102319 ) ) ;
#12170=CARTESIAN_POINT ( 'NONE',  ( -1.002407869896990045, 0.1264236179284866091, 0.9325787401037164415 ) ) ;
#12172=CARTESIAN_POINT ( 'NONE',  ( -0.8759842519685039353, 0.1787899950787401882, 0.5880905511273386566 ) ) ;
#12179=CARTESIAN_POINT ( 'NONE',  ( -1.033464566929133799, 0.000000000000000000, 1.574803149498771537 ) ) ;
#12182=CARTESIAN_POINT ( 'NONE',  ( -0.8759842519685039353, 0.1787899950787401882, 0.4256889763241890057 ) ) ;
#12183=CARTESIAN_POINT ( 'NONE',  ( -1.033464566929134687, -0.06523048226347956391, 0.4010826771653545619 ) ) ;
#12184=VERTEX_POINT ( 'NONE', #1659 ) ;
#12185=EDGE_CURVE ( 'NONE', #17885, #20293, #38094, .T. ) ;
#12186=CARTESIAN_POINT ( 'NONE',  ( -0.8759842519685039353, 0.1787899950787401882, 1.493602362150960650 ) ) ;
#12194=CARTESIAN_POINT ( 'NONE',  ( -0.8759842519685039353, 0.1574803149606299191, 1.151574803042078710 ) ) ;
#12195=CARTESIAN_POINT ( 'NONE',  ( 1.054774247047244540, -0.07405724077823318263, 0.5364173227808821665 ) ) ;
#12198=CARTESIAN_POINT ( 'NONE',  ( 0.7185039370078739607, 1.928577636452523993E-17, 1.988188976270425234 ) ) ;
#12202=CARTESIAN_POINT ( 'NONE',  ( -0.6971942568897648851, 0.07405724077823318263, 1.107283464513165727 ) ) ;
#12203=CARTESIAN_POINT ( 'NONE',  ( 0.9412147342319837628, 0.1574803149606300301, 1.040846456692913424 ) ) ;
#12204=AXIS2_PLACEMENT_3D ( 'NONE', #35577, #31522, #5627 ) ;
#12205=DIRECTION ( 'NONE',  ( 1.822029033848725028E-16, 0.000000000000000000, 1.000000000000000000 ) ) ;
#12208=DIRECTION ( 'NONE',  ( -1.000000000000000000, 0.000000000000000000, 0.000000000000000000 ) ) ;
#12209=CARTESIAN_POINT ( 'NONE',  ( 1.033464566929133799, 0.000000000000000000, 1.259842519577511810 ) ) ;
#12212=VECTOR ( 'NONE', #20033, 39.37007874015748143 ) ;
#12213=CARTESIAN_POINT ( 'NONE',  ( -1.033464566929133799, 1.928577636452524610E-17, 2.869337061179095023E-17 ) ) ;
#12214=CARTESIAN_POINT ( 'NONE',  ( 0.6971942568897626646, -0.07405724077823297447, 0.7135826771115916234 ) ) ;
#12216=CARTESIAN_POINT ( 'NONE',  ( 0.9873396505805591694, -0.1113553986120547346, 0.8316929133858268486 ) ) ;
#12221=CARTESIAN_POINT ( 'NONE',  ( 1.033464566929134687, 0.06523048226347956391, 1.183562992018456272 ) ) ;
#12222=CARTESIAN_POINT ( 'NONE',  ( 0.7185039370078739607, 1.928577636452523993E-17, 1.840551181102362266 ) ) ;
#12223=CARTESIAN_POINT ( 'NONE',  ( -1.054774247047244540, 0.07405724077823318263, 0.4576771653005669016 ) ) ;
#12225=CARTESIAN_POINT ( 'NONE',  ( -0.6971942568897637749, 2.189545951927499583E-17, 1.818405511757259729 ) ) ;
#12226=CARTESIAN_POINT ( 'NONE',  ( 0.7495606340400177148, 0.1264236179284866091, 1.892224409395055096 ) ) ;
#12229=CARTESIAN_POINT ( 'NONE',  ( -0.8019270111902717657, -0.1787899950787401604, 0.9202755904974182499 ) ) ;
#12231=CARTESIAN_POINT ( 'NONE',  ( 0.6971942568897637749, 2.189545951927499583E-17, 0.4010826771115905687 ) ) ;
#12232=CARTESIAN_POINT ( 'NONE',  ( -0.6971942568897648851, -0.07405724077823297447, 1.422244094434426120 ) ) ;
#12233=CARTESIAN_POINT ( 'NONE',  ( -0.6971942568897648851, 0.07405724077823318263, 1.259842519631276359 ) ) ;
#12234=CARTESIAN_POINT ( 'NONE',  ( -0.6971942568897648851, -0.07405724077823297447, 0.7923228345919055560 ) ) ;
#12235=CARTESIAN_POINT ( 'NONE',  ( -0.6971942568897637749, 2.189545951927499583E-17, 0.1254921259304885850 ) ) ;
#12237=CARTESIAN_POINT ( 'NONE',  ( -0.8107537697050254399, 0.1574803149606300301, 1.665846456585386548 ) ) ;
#12238=CARTESIAN_POINT ( 'NONE',  ( -0.8759842519685039353, 0.1787899950787401882, 1.690452755851748146 ) ) ;
#12239=CARTESIAN_POINT ( 'NONE',  ( -0.8107537697050253289, -0.1574803149606297803, 1.995570866034207080 ) ) ;
#12241=CARTESIAN_POINT ( 'NONE',  ( -1.033464566929133799, 0.000000000000000000, 1.742125984251968518 ) ) ;
#12242=FACE_OUTER_BOUND ( 'NONE', #35117, .T. ) ;
#12243=CARTESIAN_POINT ( 'NONE',  ( 0.6971942568897637749, 2.189545951927499583E-17, 1.660925196796630088 ) ) ;
#12250=AXIS2_PLACEMENT_3D ( 'NONE', #30871, #41587, #15772 ) ;
#12251=ADVANCED_FACE ( 'NONE', ( #24199 ), #41891, .T. ) ;
#12260=CARTESIAN_POINT ( 'NONE',  ( 1.002407869896990045, -0.1264236179284866091, 0.8439960629383622681 ) ) ;
#12262=CARTESIAN_POINT ( 'NONE',  ( -1.033464566929133799, 0.000000000000000000, 1.535433070758614127 ) ) ;
#12263=CARTESIAN_POINT ( 'NONE',  ( -0.9873396505805591694, -0.1113553986120547346, 0.07381889753026830980 ) ) ;
#12264=CARTESIAN_POINT ( 'NONE',  ( 0.8107537697050234415, -0.1574803149606297803, 0.06643700776648873985 ) ) ;
#12265=CARTESIAN_POINT ( 'NONE',  ( 1.033464566929134687, 0.06523048226347956391, 0.1697834645669291653 ) ) ;
#12273=CARTESIAN_POINT ( 'NONE',  ( 1.054774247047244096, 0.000000000000000000, 0.3026574802611972648 ) ) ;
#12274=( BOUNDED_CURVE ( )  B_SPLINE_CURVE ( 2, ( #38417, #27670, #20194, #1988, #42230, #24052, #38655, #5828, #11319 ),
 .UNSPECIFIED., .F., .T. ) 
 B_SPLINE_CURVE_WITH_KNOTS ( ( 3, 2, 2, 2, 3 ),
 ( 0.5000000000000000000, 0.5024999999999999467, 0.5050000000000000044, 0.5074999999999999512, 0.5100000000000000089 ),
 .UNSPECIFIED. ) 
 CURVE ( )  GEOMETRIC_REPRESENTATION_ITEM ( )  RATIONAL_B_SPLINE_CURVE ( ( 1.000000000000000000, 0.9238795325112869605, 1.000000000000000000, 0.9238795325112869605, 1.000000000000000000, 0.9238795325112869605, 1.000000000000000000, 0.9238795325112869605, 1.000000000000000000 ) ) 
 REPRESENTATION_ITEM ( '' )  ) ;
#12276=CARTESIAN_POINT ( 'NONE',  ( -1.054774247047244096, 0.000000000000000000, 1.675688976324189117 ) ) ;
#12278=CARTESIAN_POINT ( 'NONE',  ( -1.054774247047244540, -0.07405724077823318263, 1.363188976324188895 ) ) ;
#12281=CARTESIAN_POINT ( 'NONE',  ( 0.8019270111902717657, -0.1787899950787401604, 1.274606299158834277 ) ) ;
#12282=CARTESIAN_POINT ( 'NONE',  ( -0.9500414927467378812, 0.1787899950787401604, 1.249999999946235896 ) ) ;
#12285=CARTESIAN_POINT ( 'NONE',  ( -0.7185039370078739607, 1.928577636452523993E-17, 1.358267716427907779 ) ) ;
#12286=CARTESIAN_POINT ( 'NONE',  ( 0.7495606340400177148, 0.1264236179284866091, 0.3961614172690708924 ) ) ;
#12287=CARTESIAN_POINT ( 'NONE',  ( -0.8019270111902716547, 0.1787899950787401604, 0.3100393700249766682 ) ) ;
#12289=CARTESIAN_POINT ( 'NONE',  ( -0.9412147342319837628, 0.1574803149606300301, 1.355807086614173596 ) ) ;
#12290=CARTESIAN_POINT ( 'NONE',  ( -1.033464566929134687, -0.06523048226347956391, 0.3617125984251968740 ) ) ;
#12291=CARTESIAN_POINT ( 'NONE',  ( 1.054774247047244096, 0.000000000000000000, 1.208169291284818980 ) ) ;
#12292=CARTESIAN_POINT ( 'NONE',  ( -0.6971942568897637749, 2.189545951927499583E-17, 1.970964566875370139 ) ) ;
#12293=CARTESIAN_POINT ( 'NONE',  ( -0.8759842519685039353, -0.1574803149606299191, 1.968503937007874072 ) ) ;
#12294=ORIENTED_EDGE ( 'NONE', *, *, #46313, .F. ) ;
#12296=CARTESIAN_POINT ( 'NONE',  ( 0.9500414927467378812, -0.1787899950787401604, 1.983267716481667886 ) ) ;
#12297=( BOUNDED_CURVE ( )  B_SPLINE_CURVE ( 2, ( #20332, #24183, #24638, #5942, #20563, #17212, #31848, #13606, #28246 ),
 .UNSPECIFIED., .F., .T. ) 
 B_SPLINE_CURVE_WITH_KNOTS ( ( 3, 2, 2, 2, 3 ),
 ( 0.5300000000000000266, 0.5324999999999999734, 0.5350000000000000311, 0.5374999999999999778, 0.5400000000000000355 ),
 .UNSPECIFIED. ) 
 CURVE ( )  GEOMETRIC_REPRESENTATION_ITEM ( )  RATIONAL_B_SPLINE_CURVE ( ( 1.000000000000000000, 0.9238795325112869605, 1.000000000000000000, 0.9238795325112869605, 1.000000000000000000, 0.9238795325112869605, 1.000000000000000000, 0.9238795325112869605, 1.000000000000000000 ) ) 
 REPRESENTATION_ITEM ( '' )  ) ;
#12298=EDGE_CURVE ( 'NONE', #17885, #38458, #47130, .T. ) ;
#12300=CARTESIAN_POINT ( 'NONE',  ( -0.9412147342319837628, 0.1574803149606300301, 1.464074803042079376 ) ) ;
#12301=FACE_OUTER_BOUND ( 'NONE', #16874, .T. ) ;
#12304=DIRECTION ( 'NONE',  ( 0.000000000000000000, 0.000000000000000000, -1.000000000000000000 ) ) ;
#12306=ADVANCED_FACE ( 'NONE', ( #29775 ), #11774, .T. ) ;
#12308=DIRECTION ( 'NONE',  ( 1.822029033848725028E-16, 0.000000000000000000, 1.000000000000000000 ) ) ;
#12309=ORIENTED_EDGE ( 'NONE', *, *, #34408, .F. ) ;
#12310=CARTESIAN_POINT ( 'NONE',  ( 0.6971942568897648851, -0.07405724077823297447, 1.304133858213953667 ) ) ;
#12313=CARTESIAN_POINT ( 'NONE',  ( 1.033464566929134687, 0.06523048226347956391, 1.459153543199560144 ) ) ;
#12314=VECTOR ( 'NONE', #4333, 39.37007874015748143 ) ;
#12317=CARTESIAN_POINT ( 'NONE',  ( 1.002407869896990045, 0.1264236179284866091, 1.562499999946236118 ) ) ;
#12322=VERTEX_POINT ( 'NONE', #22769 ) ;
#12323=CARTESIAN_POINT ( 'NONE',  ( -0.9500414927467377701, 0.1787899950787401604, 0.5856299212060785964 ) ) ;
#12325=DIRECTION ( 'NONE',  ( 0.000000000000000000, 0.000000000000000000, 1.000000000000000000 ) ) ;
#12329=CARTESIAN_POINT ( 'NONE',  ( 1.033464566929133799, 0.000000000000000000, 1.653543306979086580 ) ) ;
#12330=CARTESIAN_POINT ( 'NONE',  ( 1.054774247047244096, 0.000000000000000000, 1.405019684985606476 ) ) ;
#12331=CARTESIAN_POINT ( 'NONE',  ( 1.054774247047244096, 0.000000000000000000, 1.872539370024976391 ) ) ;
#12332=CARTESIAN_POINT ( 'NONE',  ( 0.8759842519685039353, 0.1787899950787401882, 0.3075787401037169411 ) ) ;
#12334=ORIENTED_EDGE ( 'NONE', *, *, #4094, .F. ) ;
#12335=DIRECTION ( 'NONE',  ( -1.000000000000000000, 0.000000000000000000, 0.000000000000000000 ) ) ;
#12338=CARTESIAN_POINT ( 'NONE',  ( 0.6971942568897637749, 2.189545951927499583E-17, 0.5142716534895434011 ) ) ;
#12342=CARTESIAN_POINT ( 'NONE',  ( 0.8107537697050253289, 0.1574803149606300301, 0.8390748030420787096 ) ) ;
#12344=CARTESIAN_POINT ( 'NONE',  ( -0.8759842519685039353, 0.000000000000000000, 0.000000000000000000 ) ) ;
#12345=CARTESIAN_POINT ( 'NONE',  ( -1.033464566929133799, 0.000000000000000000, 0.1673228346456692994 ) ) ;
#12346=VERTEX_POINT ( 'NONE', #4297 ) ;
#12347=CARTESIAN_POINT ( 'NONE',  ( -0.8759842519685039353, -0.1574803149606299191, 0.5413385825696385156 ) ) ;
#12350=CARTESIAN_POINT ( 'NONE',  ( 0.8759842519685039353, -0.1787899950787401882, 1.587106299158834721 ) ) ;
#12351=CARTESIAN_POINT ( 'NONE',  ( -0.9412147342319837628, -0.1574803149606297803, 1.301673228346455602 ) ) ;
#12353=CARTESIAN_POINT ( 'NONE',  ( -0.7646288533564489232, 0.1113553986120547346, 0.7332677165354331006 ) ) ;
#12355=CARTESIAN_POINT ( 'NONE',  ( 0.7185039370078778465, -0.06523048226348396317, 1.911909448711369697 ) ) ;
#12357=CARTESIAN_POINT ( 'NONE',  ( 1.033464566929134687, 0.06523048226347956391, 1.380413385719244213 ) ) ;
#12361=ORIENTED_EDGE ( 'NONE', *, *, #24040, .F. ) ;
#12362=CARTESIAN_POINT ( 'NONE',  ( 0.6971942568897637749, 2.189545951927499583E-17, 0.6766732282926929409 ) ) ;
#12364=CARTESIAN_POINT ( 'NONE',  ( -0.8759842519685039353, -0.1787899950787401882, 1.587106299158834721 ) ) ;
#12366=CARTESIAN_POINT ( 'NONE',  ( -0.8019270111902717657, -0.1787899950787401604, 1.313976377898992132 ) ) ;
#12371=ORIENTED_EDGE ( 'NONE', *, *, #6974, .F. ) ;
#12374=ORIENTED_EDGE ( 'NONE', *, *, #14798, .T. ) ;
#12383=CARTESIAN_POINT ( 'NONE',  ( -0.6971942568897626646, 0.07405724077823318263, 0.2017716534895435399 ) ) ;
#12384=CARTESIAN_POINT ( 'NONE',  ( -1.033464566929134687, -0.06523048226347956391, 1.070374015748031038 ) ) ;
#12385=CARTESIAN_POINT ( 'NONE',  ( 0.7185039370078739607, 1.928577636452523993E-17, 0.6594488188976378451 ) ) ;
#12386=CARTESIAN_POINT ( 'NONE',  ( -0.8759842519685039353, 0.000000000000000000, 0.000000000000000000 ) ) ;
#12388=FACE_OUTER_BOUND ( 'NONE', #25118, .T. ) ;
#12389=CARTESIAN_POINT ( 'NONE',  ( 1.002407869896990045, 0.1264236179284866091, 0.9374999999462362288 ) ) ;
#12390=CARTESIAN_POINT ( 'NONE',  ( 0.7495606340400177148, 0.1264236179284866091, 1.414862204670645829 ) ) ;
#12391=CARTESIAN_POINT ( 'NONE',  ( 0.8019270111902716547, 0.1787899950787401604, 0.1131889763241894220 ) ) ;
#12393=CARTESIAN_POINT ( 'NONE',  ( 0.7185039370078746268, -0.06523048226347956391, 1.567421259842519676 ) ) ;
#12394=CARTESIAN_POINT ( 'NONE',  ( 0.7290331858934718801, -0.08312163584841733566, 1.984889472013028566 ) ) ;
#12395=CARTESIAN_POINT ( 'NONE',  ( 1.033464566929133799, 0.000000000000000000, 0.6397637795275591399 ) ) ;
#12396=CARTESIAN_POINT ( 'NONE',  ( -0.7185039370078739607, 1.928577636452523993E-17, 1.633858267609007875 ) ) ;
#12398=CARTESIAN_POINT ( 'NONE',  ( 0.8759842519685039353, -0.1574803149606299191, 0.7874015748031496509 ) ) ;
#12399=CARTESIAN_POINT ( 'NONE',  ( 0.9500414927467377701, -0.1787899950787401604, 1.038385826717890259 ) ) ;
#12400=CARTESIAN_POINT ( 'NONE',  ( 0.9500414927467377701, -0.1787899950787401604, 1.751968503883245987 ) ) ;
#12402=CARTESIAN_POINT ( 'NONE',  ( 0.7185039370078739607, 1.928577636452523993E-17, 0.4133858266641267654 ) ) ;
#12405=CARTESIAN_POINT ( 'NONE',  ( -0.7185039370078739607, 1.928577636452523993E-17, 0.1771653542231816925 ) ) ;
#12408=CARTESIAN_POINT ( 'NONE',  ( -0.9412147342319837628, 0.1574803149606300301, 0.1254921258767249526 ) ) ;
#12410=CARTESIAN_POINT ( 'NONE',  ( 0.9500414927467378812, -0.1787899950787401604, 1.156496062938362046 ) ) ;
#12411=ORIENTED_EDGE ( 'NONE', *, *, #14434, .F. ) ;
#12413=VECTOR ( 'NONE', #27563, 39.37007874015748143 ) ;
#12414=CARTESIAN_POINT ( 'NONE',  ( -0.8759842519685039353, 0.1787899950787401882, 0.5437992125446614589 ) ) ;
#12415=CARTESIAN_POINT ( 'NONE',  ( -0.8107537697050234415, -0.1574803149606297803, 0.2731299212598424231 ) ) ;
#12416=CARTESIAN_POINT ( 'NONE',  ( -0.6971942568897626646, -0.07405724077823297447, 0.3198818897100162983 ) ) ;
#12422=CARTESIAN_POINT ( 'NONE',  ( -0.8019270111902717657, 0.1787899950787401604, 0.5511811023084406402 ) ) ;
#12425=CARTESIAN_POINT ( 'NONE',  ( -0.7185039370078739607, 1.928577636452523993E-17, 1.683070866141732402 ) ) ;
#12428=CARTESIAN_POINT ( 'NONE',  ( 1.033464566929134687, -0.06523048226347956391, 0.4798228346456689386 ) ) ;
#12431=CARTESIAN_POINT ( 'NONE',  ( -0.8107537697050254399, -0.1574803149606297803, 1.168799212490898576 ) ) ;
#12432=CARTESIAN_POINT ( 'NONE',  ( -0.6971942568897626646, -0.07405724077823297447, 0.4379921259304882519 ) ) ;
#12441=CARTESIAN_POINT ( 'NONE',  ( 0.9412147342319837628, 0.1574803149606300301, 0.5290354330708663122 ) ) ;
#12442=FACE_OUTER_BOUND ( 'NONE', #38742, .T. ) ;
#12443=CARTESIAN_POINT ( 'NONE',  ( -0.9873396505805591694, 0.1113553986120547346, 1.186023621939716666 ) ) ;
#12444=CARTESIAN_POINT ( 'NONE',  ( 1.002407869896990045, 0.1264236179284866091, 0.5437992125446614589 ) ) ;
#12447=CARTESIAN_POINT ( 'NONE',  ( -0.7185039370078739607, 1.928577636452523993E-17, 1.633858267609007875 ) ) ;
#12449=VECTOR ( 'NONE', #39580, 39.37007874015748143 ) ;
#12453=CARTESIAN_POINT ( 'NONE',  ( -0.8019270111902716547, -0.1787899950787401604, 1.077755905458048113 ) ) ;
#12454=CARTESIAN_POINT ( 'NONE',  ( 1.033464566929134687, -0.06523048226347956391, 1.149114173228346969 ) ) ;
#12455=CARTESIAN_POINT ( 'NONE',  ( -0.9287573551135129835, -0.1680815725407091843, 1.989135227375367743 ) ) ;
#12456=FACE_OUTER_BOUND ( 'NONE', #25051, .T. ) ;
#12457=EDGE_CURVE ( 'NONE', #6796, #39036, #41918, .T. ) ;
#12458=CARTESIAN_POINT ( 'NONE',  ( 0.9412147342319837628, 0.1574803149606300301, 0.1747047244094490082 ) ) ;
#12460=CARTESIAN_POINT ( 'NONE',  ( -0.7185039370078746268, -0.06523048226347956391, 1.252460629921259061 ) ) ;
#12464=CARTESIAN_POINT ( 'NONE',  ( 0.9412147342319837628, -0.1574803149606297803, 0.8686023622047237547 ) ) ;
#12466=CARTESIAN_POINT ( 'NONE',  ( 1.033464566929134687, 0.06523048226347956391, 1.272145669291338432 ) ) ;
#12467=LINE ( 'NONE', #8843, #14331 ) ;
#12471=CARTESIAN_POINT ( 'NONE',  ( 0.7185039370078746268, -0.06523048226347956391, 1.124507873908221489 ) ) ;
#12474=VERTEX_POINT ( 'NONE', #947 ) ;
#12475=CARTESIAN_POINT ( 'NONE',  ( -1.054774247047244540, 0.07405724077823318263, 1.801181102308441861 ) ) ;
#12476=CARTESIAN_POINT ( 'NONE',  ( 0.7495606340400177148, 0.1264236179284866091, 1.852854330654897685 ) ) ;
#12480=CARTESIAN_POINT ( 'NONE',  ( 0.8019270111902717657, 0.1787899950787401604, 0.4724409448281262636 ) ) ;
#12481=CARTESIAN_POINT ( 'NONE',  ( -0.7495606340400177148, 0.1264236179284866091, 1.454232283410803017 ) ) ;
#12483=CARTESIAN_POINT ( 'NONE',  ( -0.9500414927467378812, -0.1787899950787401604, 0.09842519679663024046 ) ) ;
#12485=EDGE_CURVE ( 'NONE', #44026, #2780, #32878, .T. ) ;
#12486=CARTESIAN_POINT ( 'NONE',  ( -1.033464566929134687, 0.06523048226347956391, 0.5634842519685042683 ) ) ;
#12487=CARTESIAN_POINT ( 'NONE',  ( -0.7495606340400177148, -0.1264236179284866091, 1.783956692859621995 ) ) ;
#12488=CARTESIAN_POINT ( 'NONE',  ( -0.6971942568897637749, 2.189545951927499583E-17, 0.1254921259304885850 ) ) ;
#12489=CARTESIAN_POINT ( 'NONE',  ( -0.7646288533564489232, -0.1113553986120547346, 1.687992125984252079 ) ) ;
#12490=DIRECTION ( 'NONE',  ( 1.000000000000000000, 0.000000000000000000, 0.000000000000000000 ) ) ;
#12491=CARTESIAN_POINT ( 'NONE',  ( 0.9500414927467377701, 0.1787899950787401604, 1.648622047190331230 ) ) ;
#12493=CARTESIAN_POINT ( 'NONE',  ( 0.9412147342319837628, 0.1574803149606300301, 0.2042322833570397733 ) ) ;
#12498=EDGE_LOOP ( 'NONE', ( #14816, #12601, #30015, #22010 ) ) ;
#12503=CARTESIAN_POINT ( 'NONE',  ( 0.7495606340400177148, 0.1264236179284866091, 0.3912401574265515491 ) ) ;
#12505=CARTESIAN_POINT ( 'NONE',  ( -0.7185039370078746268, -0.06523048226347956391, 0.7701771652468031304 ) ) ;
#12508=CARTESIAN_POINT ( 'NONE',  ( 0.6971942568897626646, 0.07405724077823318263, 0.8661417322297003674 ) ) ;
#12512=CARTESIAN_POINT ( 'NONE',  ( -1.033464566929134687, -0.06523048226347956391, 0.07627952745152805081 ) ) ;
#12513=CARTESIAN_POINT ( 'NONE',  ( 1.054774247047244096, 0.000000000000000000, 1.916830708607653477 ) ) ;
#12516=CARTESIAN_POINT ( 'NONE',  ( 1.033464566929134687, 0.06523048226347956391, 0.2091535433070865757 ) ) ;
#12517=FACE_OUTER_BOUND ( 'NONE', #27166, .T. ) ;
#12523=CARTESIAN_POINT ( 'NONE',  ( -1.054774247047244540, 0.07405724077823318263, 1.756889763725764553 ) ) ;
#12525=CARTESIAN_POINT ( 'NONE',  ( -0.7495606340400177148, -0.1264236179284866091, 1.272145669237574772 ) ) ;
#12526=CYLINDRICAL_SURFACE ( 'NONE', #61, 0.1574803149606299191 ) ;
#12528=CARTESIAN_POINT ( 'NONE',  ( 0.9500414927467378812, 0.1787899950787401604, 1.373031496009229135 ) ) ;
#12529=CARTESIAN_POINT ( 'NONE',  ( -0.8759842519685039353, -0.1787899950787401882, 0.5684055117572598403 ) ) ;
#12530=CARTESIAN_POINT ( 'NONE',  ( -0.8759842519685039353, -0.1787899950787401882, 1.154035433017102319 ) ) ;
#12534=CARTESIAN_POINT ( 'NONE',  ( 1.002407869896990045, 0.1264236179284866091, 0.5437992125446614589 ) ) ;
#12535=CARTESIAN_POINT ( 'NONE',  ( -1.002407869896990045, 0.1264236179284866091, 0.3420275590013546751 ) ) ;
#12536=CARTESIAN_POINT ( 'NONE',  ( -0.6971942568897626646, 0.07405724077823318263, 0.8267716534895444003 ) ) ;
#12539=CARTESIAN_POINT ( 'NONE',  ( -0.9412147342319837628, -0.1574803149606297803, 0.3567913385826772532 ) ) ;
#12540=CARTESIAN_POINT ( 'NONE',  ( 0.8759842519685039353, 0.1787899950787401882, 1.139271653489543290 ) ) ;
#12542=CARTESIAN_POINT ( 'NONE',  ( -1.033464566929133799, 1.928577636452524610E-17, 2.869337061179095023E-17 ) ) ;
#12544=CARTESIAN_POINT ( 'NONE',  ( -1.054774247047244540, -0.07405724077823318263, 0.9694881889226144578 ) ) ;
#12554=DIRECTION ( 'NONE',  ( 1.000000000000000000, 0.000000000000000000, -1.822029033848725275E-16 ) ) ;
#12559=CARTESIAN_POINT ( 'NONE',  ( 1.054774247047244540, 0.07405724077823318263, 0.5364173227808821665 ) ) ;
#12561=CARTESIAN_POINT ( 'NONE',  ( -1.054774247047244540, -0.07405724077823318263, 0.6545275590013546196 ) ) ;
#12567=CARTESIAN_POINT ( 'NONE',  ( 1.054774247047244540, -0.07405724077823318263, 1.560039370024977057 ) ) ;
#12568=CARTESIAN_POINT ( 'NONE',  ( 1.002407869896990045, -0.1264236179284866091, 1.788877952702141672 ) ) ;
#12571=EDGE_CURVE ( 'NONE', #13201, #35449, #6392, .T. ) ;
#12576=CARTESIAN_POINT ( 'NONE',  ( -0.8759842519685039353, 0.1574803149606299191, 0.1771653543307086520 ) ) ;
#12577=CARTESIAN_POINT ( 'NONE',  ( 0.6971942568897626646, 0.07405724077823318263, 0.4330708660879683536 ) ) ;
#12578=ADVANCED_FACE ( 'NONE', ( #38333 ), #32812, .T. ) ;
#12579=CARTESIAN_POINT ( 'NONE',  ( 0.7654444006328559036, -0.1232301103881700693, 0.03937007855823598801 ) ) ;
#12580=CARTESIAN_POINT ( 'NONE',  ( 0.8107537697050254399, -0.1574803149606297803, 1.956200787294048338 ) ) ;
#12581=CARTESIAN_POINT ( 'NONE',  ( -0.7185039370078739607, 1.928577636452523993E-17, 1.318897637687747926 ) ) ;
#12582=DIRECTION ( 'NONE',  ( 0.000000000000000000, 0.000000000000000000, -1.000000000000000000 ) ) ;
#12583=CARTESIAN_POINT ( 'NONE',  ( -1.054774247047244096, 0.000000000000000000, 1.360728346402929168 ) ) ;
#12584=CARTESIAN_POINT ( 'NONE',  ( 0.9412147342319837628, -0.1574803149606297803, 0.8193897636719996713 ) ) ;
#12587=CARTESIAN_POINT ( 'NONE',  ( 0.8759842519685039353, 0.1787899950787401882, 1.060531496009228247 ) ) ;
#12588=ORIENTED_EDGE ( 'NONE', *, *, #3411, .F. ) ;
#12589=AXIS2_PLACEMENT_3D ( 'NONE', #5459, #16498, #15801 ) ;
#12592=CARTESIAN_POINT ( 'NONE',  ( -0.9873396505805591694, 0.1113553986120547346, 0.5561023620971968784 ) ) ;
#12594=CARTESIAN_POINT ( 'NONE',  ( -0.9873396505805591694, -0.1113553986120547346, 1.225393700787401619 ) ) ;
#12595=CARTESIAN_POINT ( 'NONE',  ( 0.7185039370078739607, 1.928577636452523993E-17, 0.2559055117034968463 ) ) ;
#12597=CARTESIAN_POINT ( 'NONE',  ( -0.9873396505805591694, 0.1113553986120547346, 0.7529527557979842634 ) ) ;
#12599=CARTESIAN_POINT ( 'NONE',  ( 0.8759842519685039353, -0.1574803149606299191, 1.407480314853102321 ) ) ;
#12601=ORIENTED_EDGE ( 'NONE', *, *, #21771, .T. ) ;
#12602=( BOUNDED_CURVE ( )  B_SPLINE_CURVE ( 2, ( #47344, #3235, #355, #3947, #29182, #46849, #29657, #39893, #14753 ),
 .UNSPECIFIED., .F., .F. ) 
 B_SPLINE_CURVE_WITH_KNOTS ( ( 3, 2, 2, 2, 3 ),
 ( 0.5899999999999999689, 0.5925000000000000266, 0.5949999999999999734, 0.5975000000000000311, 0.5999999999999999778 ),
 .UNSPECIFIED. ) 
 CURVE ( )  GEOMETRIC_REPRESENTATION_ITEM ( )  RATIONAL_B_SPLINE_CURVE ( ( 1.000000000000000000, 0.9238795325112869605, 1.000000000000000000, 0.9238795325112869605, 1.000000000000000000, 0.9238795325112869605, 1.000000000000000000, 0.9238795325112869605, 1.000000000000000000 ) ) 
 REPRESENTATION_ITEM ( '' )  ) ;
#12605=CARTESIAN_POINT ( 'NONE',  ( -0.9500414927467377701, 0.1787899950787401604, 1.564960629867495845 ) ) ;
#12607=CARTESIAN_POINT ( 'NONE',  ( -1.054774247047244096, 0.000000000000000000, 1.405019684985606476 ) ) ;
#12608=DIRECTION ( 'NONE',  ( -1.000000000000000000, 0.000000000000000000, 0.000000000000000000 ) ) ;
#12609=DIRECTION ( 'NONE',  ( -1.000000000000000000, 0.000000000000000000, 0.000000000000000000 ) ) ;
#12613=ORIENTED_EDGE ( 'NONE', *, *, #6260, .T. ) ;
#12614=ORIENTED_EDGE ( 'NONE', *, *, #31630, .F. ) ;
#12615=CARTESIAN_POINT ( 'NONE',  ( 0.7185039370078739607, 0.000000000000000000, 4.498031496062992574 ) ) ;
#12617=CARTESIAN_POINT ( 'NONE',  ( 0.9873396505805591694, 0.1113553986120547346, 1.786417322834645605 ) ) ;
#12622=CARTESIAN_POINT ( 'NONE',  ( -0.8019270111902716547, 0.1787899950787401604, 0.2362204723871814682 ) ) ;
#12623=CARTESIAN_POINT ( 'NONE',  ( -0.8107537697050253289, 0.1574803149606300301, 1.045767716535432879 ) ) ;
#12626=CARTESIAN_POINT ( 'NONE',  ( 0.8019270111902717657, 0.1787899950787401604, 1.141732283410804349 ) ) ;
#12628=ADVANCED_FACE ( 'NONE', ( #1189 ), #45269, .T. ) ;
#12629=CARTESIAN_POINT ( 'NONE',  ( 0.9412147342319837628, 0.1574803149606300301, 1.592027559055119390 ) ) ;
#12630=CARTESIAN_POINT ( 'NONE',  ( 0.7609548656500562114, 0.1137474223536875800, 1.980823507184093391 ) ) ;
#12633=CARTESIAN_POINT ( 'NONE',  ( -0.9873396505805591694, -0.1113553986120547346, 1.609251968396409493 ) ) ;
#12636=CARTESIAN_POINT ( 'NONE',  ( 0.7495606340400177148, -0.1264236179284866091, 0.9522637794737952577 ) ) ;
#12637=CARTESIAN_POINT ( 'NONE',  ( 1.054774247047244540, 0.07405724077823318263, 1.840551181048599938 ) ) ;
#12638=CARTESIAN_POINT ( 'NONE',  ( 1.033464566929134687, -0.06523048226347956391, 0.2731299211523157133 ) ) ;
#12639=ORIENTED_EDGE ( 'NONE', *, *, #17859, .F. ) ;
#12640=CARTESIAN_POINT ( 'NONE',  ( 0.9873396505805591694, -0.1113553986120547346, 1.254921259734991912 ) ) ;
#12641=EDGE_CURVE ( 'NONE', #6061, #12053, #23501, .T. ) ;
#12643=CARTESIAN_POINT ( 'NONE',  ( -0.7185039370078739607, 1.928577636452523993E-17, 0.2559055117034968463 ) ) ;
#12645=CARTESIAN_POINT ( 'NONE',  ( 1.054774247047244096, 0.000000000000000000, 1.281988188922614125 ) ) ;
#12647=FACE_OUTER_BOUND ( 'NONE', #20908, .T. ) ;
#12649=DIRECTION ( 'NONE',  ( 1.000000000000000000, 0.000000000000000000, -1.822029033848725275E-16 ) ) ;
#12651=VECTOR ( 'NONE', #16760, 39.37007874015748143 ) ;
#12656=CARTESIAN_POINT ( 'NONE',  ( -0.6971942568897637749, 2.189545951927499583E-17, 0.9916338582139527791 ) ) ;
#12657=VECTOR ( 'NONE', #5200, 39.37007874015748143 ) ;
#12659=CARTESIAN_POINT ( 'NONE',  ( -0.9500414927467378812, 0.1787899950787401604, 1.840551181048599938 ) ) ;
#12661=CARTESIAN_POINT ( 'NONE',  ( -0.8759842519685039353, 0.1787899950787401882, 0.7062007873478109987 ) ) ;
#12667=CARTESIAN_POINT ( 'NONE',  ( 0.9873396505805591694, -0.1113553986120547346, 0.4773622047244094890 ) ) ;
#12668=CARTESIAN_POINT ( 'NONE',  ( -0.7495606340400177148, 0.1264236179284866091, 0.4306102361667086820 ) ) ;
#12670=ORIENTED_EDGE ( 'NONE', *, *, #36261, .F. ) ;
#12672=CARTESIAN_POINT ( 'NONE',  ( -0.7495606340400177148, -0.1264236179284866091, 1.508366141678519678 ) ) ;
#12676=CARTESIAN_POINT ( 'NONE',  ( 0.8759842519685039353, 0.1574803149606299191, 1.033464566821606478 ) ) ;
#12681=CARTESIAN_POINT ( 'NONE',  ( 0.8107537697050254399, -0.1574803149606297803, 0.9424212598425207865 ) ) ;
#12682=CARTESIAN_POINT ( 'NONE',  ( -0.9412147342319837628, 0.1574803149606300301, 1.188484251860977503 ) ) ;
#12684=CARTESIAN_POINT ( 'NONE',  ( 0.8759842519685039353, -0.1787899950787401882, 0.6077755904974173617 ) ) ;
#12685=CARTESIAN_POINT ( 'NONE',  ( 1.054774247047244540, -0.07405724077823318263, 0.05905511805647267048 ) ) ;
#12687=CARTESIAN_POINT ( 'NONE',  ( -0.7646288533564489232, 0.1113553986120547346, 1.628937007766488199 ) ) ;
#12689=AXIS2_PLACEMENT_3D ( 'NONE', #31521, #9227, #12608 ) ;
#12692=CARTESIAN_POINT ( 'NONE',  ( 1.033464566929133799, 0.000000000000000000, 1.574803149498771537 ) ) ;
#12693=CARTESIAN_POINT ( 'NONE',  ( 0.9873396505805591694, 0.1113553986120547346, 1.077755905511811108 ) ) ;
#12696=ADVANCED_FACE ( 'NONE', ( #12242 ), #16767, .T. ) ;
#12698=CARTESIAN_POINT ( 'NONE',  ( 0.7185039370078739607, 1.928577636452523993E-17, 1.673228346349165285 ) ) ;
#12699=CARTESIAN_POINT ( 'NONE',  ( 0.7185039370078746268, 0.06523048226347956391, 0.6077755904436539236 ) ) ;
#12703=CARTESIAN_POINT ( 'NONE',  ( 0.7185039370078746268, 0.06523048226347956391, 1.168799212598425896 ) ) ;
#12704=CARTESIAN_POINT ( 'NONE',  ( 0.8019270111902717657, 0.1787899950787401604, 0.7037401574265510495 ) ) ;
#12708=LINE ( 'NONE', #9084, #9742 ) ;
#12712=CARTESIAN_POINT ( 'NONE',  ( -0.8759842519685039353, 0.1574803149606299191, 1.397637795275590511 ) ) ;
#12715=CARTESIAN_POINT ( 'NONE',  ( -0.7495606340400177148, 0.1264236179284866091, 1.970964566875370139 ) ) ;
#12716=CARTESIAN_POINT ( 'NONE',  ( 0.8759842519685039353, -0.1787899950787401882, 1.906988188922614125 ) ) ;
#12717=ORIENTED_EDGE ( 'NONE', *, *, #1611, .T. ) ;
#12718=FACE_OUTER_BOUND ( 'NONE', #1394, .T. ) ;
#12719=CARTESIAN_POINT ( 'NONE',  ( 0.7495606340400177148, -0.1264236179284866091, 0.4847440944344252323 ) ) ;
#12720=CARTESIAN_POINT ( 'NONE',  ( -0.8759842519685039353, 0.1787899950787401882, 1.370570866087968520 ) ) ;
#12722=CARTESIAN_POINT ( 'NONE',  ( -0.8759842519685039353, -0.1787899950787401882, 0.05659448813521291560 ) ) ;
#12723=CARTESIAN_POINT ( 'NONE',  ( -0.5314960629921260393, 0.000000000000000000, 4.498031496062992574 ) ) ;
#12724=CARTESIAN_POINT ( 'NONE',  ( -0.9500414927467378812, -0.1787899950787401604, 1.751968503883245765 ) ) ;
#12725=CARTESIAN_POINT ( 'NONE',  ( -0.6971942568897626646, -0.07405724077823297447, 0.04921259837143338034 ) ) ;
#12726=CARTESIAN_POINT ( 'NONE',  ( -0.8759842519685039353, -0.1574803149606299191, 1.692913385826771533 ) ) ;
#12728=CARTESIAN_POINT ( 'NONE',  ( 1.054774247047244096, 0.000000000000000000, 1.680610236166708793 ) ) ;
#12730=CARTESIAN_POINT ( 'NONE',  ( -0.8107537697050254399, -0.1574803149606297803, 0.7357283463491665065 ) ) ;
#12731=AXIS2_PLACEMENT_3D ( 'NONE', #28600, #24275, #39097 ) ;
#12733=EDGE_CURVE ( 'NONE', #47141, #5874, #11045, .T. ) ;
#12734=ORIENTED_EDGE ( 'NONE', *, *, #19039, .T. ) ;
#12739=CARTESIAN_POINT ( 'NONE',  ( 1.002407869896990045, 0.1264236179284866091, 0.3813976377415121966 ) ) ;
#12741=CARTESIAN_POINT ( 'NONE',  ( -0.7185039370078746268, 0.06523048226347956391, 0.8439960628845977197 ) ) ;
#12744=AXIS2_PLACEMENT_3D ( 'NONE', #47090, #18341, #32983 ) ;
#12745=CARTESIAN_POINT ( 'NONE',  ( 0.7495606340400177148, -0.1264236179284866091, 0.9522637794737952577 ) ) ;
#12746=EDGE_CURVE ( 'NONE', #758, #43833, #9049, .T. ) ;
#12749=CARTESIAN_POINT ( 'NONE',  ( 1.002407869896990045, -0.1264236179284866091, 1.911909448765133801 ) ) ;
#12751=CARTESIAN_POINT ( 'NONE',  ( 0.7646288533564489232, -0.1113553986120547346, 0.1919291338582677087 ) ) ;
#12752=CARTESIAN_POINT ( 'NONE',  ( -1.033464566929133799, 0.000000000000000000, 0.7578740157480314821 ) ) ;
#12755=CARTESIAN_POINT ( 'NONE',  ( 1.054774247047244540, 0.07405724077823318263, 0.3444881889226146243 ) ) ;
#12756=CARTESIAN_POINT ( 'NONE',  ( -1.054774247047244540, -0.07405724077823318263, 1.870078740103715331 ) ) ;
#12757=ORIENTED_EDGE ( 'NONE', *, *, #19453, .T. ) ;
#12758=CARTESIAN_POINT ( 'NONE',  ( -1.002407869896990045, -0.1264236179284866091, 1.242618110182456714 ) ) ;
#12759=FACE_OUTER_BOUND ( 'NONE', #28139, .T. ) ;
#12760=CARTESIAN_POINT ( 'NONE',  ( 0.7495606340400177148, -0.1264236179284866091, 1.350885826717889815 ) ) ;
#12761=CARTESIAN_POINT ( 'NONE',  ( -1.054774247047244096, 0.000000000000000000, 0.4995078739619842612 ) ) ;
#12762=CARTESIAN_POINT ( 'NONE',  ( -0.6971942568897648851, -0.07405724077823297447, 1.264763779473795813 ) ) ;
#12763=CARTESIAN_POINT ( 'NONE',  ( -1.033464566929133799, 0.000000000000000000, 0.2460629921259842590 ) ) ;
#12764=CARTESIAN_POINT ( 'NONE',  ( 0.8107537697050254399, 0.1574803149606300301, 0.05167322823892971789 ) ) ;
#12765=CARTESIAN_POINT ( 'NONE',  ( 0.8019270111902716547, -0.1787899950787401604, 0.6446850393163160442 ) ) ;
#12766=CARTESIAN_POINT ( 'NONE',  ( -0.8019270111902716547, -0.1787899950787401604, 0.4822834645131655606 ) ) ;
#12768=ORIENTED_EDGE ( 'NONE', *, *, #30555, .T. ) ;
#12769=CARTESIAN_POINT ( 'NONE',  ( -0.8759842519685039353, 0.1574803149606299191, 0.3346456692913385988 ) ) ;
#12770=CARTESIAN_POINT ( 'NONE',  ( 1.002407869896990045, 0.1264236179284866091, 1.173720472387181246 ) ) ;
#12773=CARTESIAN_POINT ( 'NONE',  ( -1.033464566929134687, -0.06523048226347956391, 1.306594488188977055 ) ) ;
#12774=CARTESIAN_POINT ( 'NONE',  ( -0.6971942568897637749, 2.189545951927499583E-17, 0.1205708660879689087 ) ) ;
#12781=CARTESIAN_POINT ( 'NONE',  ( 0.9500414927467378812, -0.1787899950787401604, 1.274606299158834277 ) ) ;
#12782=CARTESIAN_POINT ( 'NONE',  ( 1.033464566929133799, 0.000000000000000000, 1.456692913278299084 ) ) ;
#12785=CARTESIAN_POINT ( 'NONE',  ( 0.9873396505805591694, -0.1113553986120547346, 0.1919291337507405548 ) ) ;
#12786=CARTESIAN_POINT ( 'NONE',  ( 0.8019270111902717657, -0.1787899950787401604, 1.545275590497416696 ) ) ;
#12787=CARTESIAN_POINT ( 'NONE',  ( 0.6971942568897637749, 2.189545951927499583E-17, 0.2386811023084413619 ) ) ;
#12792=DIRECTION ( 'NONE',  ( 0.000000000000000000, 1.000000000000000000, 0.000000000000000000 ) ) ;
#12794=CARTESIAN_POINT ( 'NONE',  ( -0.8019270111902716547, -0.1787899950787401604, 0.7627952755367883864 ) ) ;
#12796=CARTESIAN_POINT ( 'NONE',  ( -1.033464566929134687, -0.06523048226347956391, 1.296751968396409049 ) ) ;
#12803=CARTESIAN_POINT ( 'NONE',  ( 0.8019270111902717657, 0.1787899950787401604, 1.496062992072220821 ) ) ;
#12804=CARTESIAN_POINT ( 'NONE',  ( 1.002407869896990045, 0.1264236179284866091, 1.838090551127338657 ) ) ;
#12805=CARTESIAN_POINT ( 'NONE',  ( 0.7495606340400177148, 0.1264236179284866091, 0.4699803149068661479 ) ) ;
#12814=CARTESIAN_POINT ( 'NONE',  ( 1.054774247047244540, 0.07405724077823318263, 0.4970472440407249226 ) ) ;
#12816=CARTESIAN_POINT ( 'NONE',  ( 0.7495606340400177148, -0.1264236179284866091, 0.5585629920722204877 ) ) ;
#12817=CARTESIAN_POINT ( 'NONE',  ( 0.8107537697050254399, 0.1574803149606300301, 0.2189960629921262614 ) ) ;
#12818=CARTESIAN_POINT ( 'NONE',  ( 0.7185039370078739607, 1.928577636452523993E-17, 0.8070866140657008136 ) ) ;
#12820=CARTESIAN_POINT ( 'NONE',  ( 1.002407869896990045, -0.1264236179284866091, 0.9670275590013542866 ) ) ;
#12823=CARTESIAN_POINT ( 'NONE',  ( -0.7185039370078739607, 1.928577636452523993E-17, 0.5314960628845992741 ) ) ;
#12824=CARTESIAN_POINT ( 'NONE',  ( -0.9873396505805591694, 0.1113553986120547346, 0.8021653543307086798 ) ) ;
#12825=CARTESIAN_POINT ( 'NONE',  ( -0.8759842519685039353, -0.1574803149606299191, 1.299212598425196985 ) ) ;
#12826=CARTESIAN_POINT ( 'NONE',  ( -1.033464566929134687, -0.06523048226347956391, 1.060531495955465031 ) ) ;
#12828=CARTESIAN_POINT ( 'NONE',  ( -1.033464566929133799, 0.000000000000000000, 0.7480314959554645871 ) ) ;
#12829=CARTESIAN_POINT ( 'NONE',  ( 0.9500414927467377701, -0.1787899950787401604, 0.1377952755367876370 ) ) ;
#12830=CARTESIAN_POINT ( 'NONE',  ( 1.033464566929134687, 0.06523048226347956391, 1.341043306979086136 ) ) ;
#12831=ORIENTED_EDGE ( 'NONE', *, *, #45094, .T. ) ;
#12835=CARTESIAN_POINT ( 'NONE',  ( -0.8759842519685039353, -0.1787899950787401882, 1.744586614119464807 ) ) ;
#12837=ORIENTED_EDGE ( 'NONE', *, *, #25392, .T. ) ;
#12839=CARTESIAN_POINT ( 'NONE',  ( 0.7185039370078739607, 1.928577636452523993E-17, 1.870078740049952559 ) ) ;
#12842=ORIENTED_EDGE ( 'NONE', *, *, #20127, .T. ) ;
#12846=CARTESIAN_POINT ( 'NONE',  ( 1.033464566929133799, 0.000000000000000000, 1.732283464459401623 ) ) ;
#12847=CARTESIAN_POINT ( 'NONE',  ( -0.9412147342319837628, -0.1574803149606297803, 0.4256889762704256230 ) ) ;
#12848=( BOUNDED_CURVE ( )  B_SPLINE_CURVE ( 2, ( #24398, #20555, #10261, #31839, #28239, #6168, #2800, #47146, #35197 ),
 .UNSPECIFIED., .F., .F. ) 
 B_SPLINE_CURVE_WITH_KNOTS ( ( 3, 2, 2, 2, 3 ),
 ( 0.9899999999999999911, 0.9925000000000000488, 0.9949999999999999956, 0.9975000000000000533, 1.000000000000000000 ),
 .UNSPECIFIED. ) 
 CURVE ( )  GEOMETRIC_REPRESENTATION_ITEM ( )  RATIONAL_B_SPLINE_CURVE ( ( 1.000000000000000000, 0.9238795325112869605, 1.000000000000000000, 0.9238795325112869605, 1.000000000000000000, 0.9238795325112869605, 1.000000000000000000, 0.9238795325112869605, 1.000000000000000000 ) ) 
 REPRESENTATION_ITEM ( '' )  ) ;
#12850=CARTESIAN_POINT ( 'NONE',  ( 1.033464566929134687, 0.06523048226347956391, 1.783956692913386766 ) ) ;
#12851=ADVANCED_FACE ( 'NONE', ( #35234 ), #35460, .T. ) ;
#12854=CARTESIAN_POINT ( 'NONE',  ( -0.7646288533564489232, -0.1113553986120547346, 1.018700787401574770 ) ) ;
#12857=CARTESIAN_POINT ( 'NONE',  ( 1.054774247047244540, 0.07405724077823318263, 1.131889763725763665 ) ) ;
#12858=CARTESIAN_POINT ( 'NONE',  ( 0.8019270111902716547, 0.1787899950787401604, 0.1525590550643468324 ) ) ;
#12859=LINE ( 'NONE', #2278, #42202 ) ;
#12860=CARTESIAN_POINT ( 'NONE',  ( 0.7185039370078739607, 1.928577636452523993E-17, 1.525590551181102317 ) ) ;
#12861=CARTESIAN_POINT ( 'NONE',  ( 0.7801209693189999905, 0.1293481257666107553, 1.980357471351750442 ) ) ;
#12863=CARTESIAN_POINT ( 'NONE',  ( 0.8759842519685039353, -0.1574803149606299191, 0.4625984250893235838 ) ) ;
#12864=CARTESIAN_POINT ( 'NONE',  ( -0.7185039370078746268, -0.06523048226347956391, 1.636318897530269156 ) ) ;
#12867=( BOUNDED_CURVE ( )  B_SPLINE_CURVE ( 2, ( #42597, #9809, #13862, #24418, #28507, #20809, #2590, #28751, #17226 ),
 .UNSPECIFIED., .F., .T. ) 
 B_SPLINE_CURVE_WITH_KNOTS ( ( 3, 2, 2, 2, 3 ),
 ( 0.3900000000000000133, 0.3925000000000000155, 0.3950000000000000178, 0.3975000000000000200, 0.4000000000000000222 ),
 .UNSPECIFIED. ) 
 CURVE ( )  GEOMETRIC_REPRESENTATION_ITEM ( )  RATIONAL_B_SPLINE_CURVE ( ( 1.000000000000000000, 0.9238795325112869605, 1.000000000000000000, 0.9238795325112869605, 1.000000000000000000, 0.9238795325112869605, 1.000000000000000000, 0.9238795325112869605, 1.000000000000000000 ) ) 
 REPRESENTATION_ITEM ( '' )  ) ;
#12868=CARTESIAN_POINT ( 'NONE',  ( 0.8019270111902716547, -0.1787899950787401604, 0.9547244093950545407 ) ) ;
#12869=CARTESIAN_POINT ( 'NONE',  ( 0.8759842519685039353, 0.1787899950787401882, 1.769192913332062966 ) ) ;
#12870=CARTESIAN_POINT ( 'NONE',  ( 0.7185039370078739607, 1.928577636452523993E-17, 0.2952755904436539236 ) ) ;
#12871=ORIENTED_EDGE ( 'NONE', *, *, #12571, .T. ) ;
#12872=CARTESIAN_POINT ( 'NONE',  ( -0.7185039370078739607, 0.000000000000000000, -2.869337061179095023E-17 ) ) ;
#12874=CARTESIAN_POINT ( 'NONE',  ( -0.7185039370078739607, 1.928577636452523993E-17, 0.2165354329633393804 ) ) ;
#12875=CARTESIAN_POINT ( 'NONE',  ( 0.6971942568897637749, 2.189545951927499583E-17, 1.262303149552535420 ) ) ;
#12877=EDGE_CURVE ( 'NONE', #32389, #16635, #11314, .T. ) ;
#12879=DIRECTION ( 'NONE',  ( 0.000000000000000000, 0.000000000000000000, -1.000000000000000000 ) ) ;
#12880=CARTESIAN_POINT ( 'NONE',  ( -1.002407869896990045, -0.1264236179284866091, 0.5290354330171024300 ) ) ;
#12881=CARTESIAN_POINT ( 'NONE',  ( 0.7185039370078739607, 1.928577636452523993E-17, 0.8956692913385826404 ) ) ;
#12882=CARTESIAN_POINT ( 'NONE',  ( 0.7185039370078739607, 0.000000000000000000, 4.498031496062992574 ) ) ;
#12886=CARTESIAN_POINT ( 'NONE',  ( -1.054774247047244540, -0.07405724077823318263, 0.9694881889226144578 ) ) ;
#12887=CARTESIAN_POINT ( 'NONE',  ( -0.8107537697050253289, 0.1574803149606300301, 0.02214566929133862661 ) ) ;
#12888=ORIENTED_EDGE ( 'NONE', *, *, #15774, .T. ) ;
#12889=CARTESIAN_POINT ( 'NONE',  ( -1.002407869896990045, 0.1264236179284866091, 0.7406496062454487328 ) ) ;
#12890=ORIENTED_EDGE ( 'NONE', *, *, #44920, .F. ) ;
#12896=DIRECTION ( 'NONE',  ( 1.822029033848725028E-16, 0.000000000000000000, 1.000000000000000000 ) ) ;
#12901=CARTESIAN_POINT ( 'NONE',  ( -0.7495606340400177148, -0.1264236179284866091, 0.4404527558517480901 ) ) ;
#12906=CARTESIAN_POINT ( 'NONE',  ( -1.054774247047244096, 0.000000000000000000, 1.680610236166708793 ) ) ;
#12910=CARTESIAN_POINT ( 'NONE',  ( 1.033464566929133799, 0.000000000000000000, 1.535433070758614127 ) ) ;
#12912=CARTESIAN_POINT ( 'NONE',  ( 0.7185039370078746268, -0.06523048226347956391, 0.5437992125984247860 ) ) ;
#12914=CARTESIAN_POINT ( 'NONE',  ( 0.7185039370078739607, 0.000000000000000000, 4.498031496062992574 ) ) ;
#12915=CARTESIAN_POINT ( 'NONE',  ( -0.8759842519685039353, 0.1574803149606299191, 1.190944881782236342 ) ) ;
#12917=CARTESIAN_POINT ( 'NONE',  ( -0.7185039370078739607, 1.928577636452523993E-17, 0.05905511800270921846 ) ) ;
#12919=ORIENTED_EDGE ( 'NONE', *, *, #29391, .T. ) ;
#12921=CARTESIAN_POINT ( 'NONE',  ( -1.002407869896990045, -0.1264236179284866091, 1.045767716481669440 ) ) ;
#12922=CARTESIAN_POINT ( 'NONE',  ( 0.8759842519685039353, -0.1574803149606299191, 1.141732283464567121 ) ) ;
#12926=CARTESIAN_POINT ( 'NONE',  ( 0.8107537697050254399, -0.1574803149606297803, 0.5782480313885360879 ) ) ;
#12927=CARTESIAN_POINT ( 'NONE',  ( -0.9412147342319837628, -0.1574803149606297803, 1.961122047136568014 ) ) ;
#12928=CARTESIAN_POINT ( 'NONE',  ( 1.033464566929133799, 0.000000000000000000, 0.1279527559055118058 ) ) ;
#12932=CARTESIAN_POINT ( 'NONE',  ( 0.7495606340400177148, -0.1264236179284866091, 0.7947834645131652831 ) ) ;
#12934=CARTESIAN_POINT ( 'NONE',  ( 0.9412147342319837628, -0.1574803149606297803, 1.301673228346455602 ) ) ;
#12935=CYLINDRICAL_SURFACE ( 'NONE', #18151, 0.1574803149606299191 ) ;
#12940=CARTESIAN_POINT ( 'NONE',  ( -0.8759842519685039353, 0.1574803149606299191, 1.860236220364913207 ) ) ;
#12941=ORIENTED_EDGE ( 'NONE', *, *, #29609, .F. ) ;
#12943=CARTESIAN_POINT ( 'NONE',  ( -1.054774247047244096, 0.000000000000000000, 1.956200787347811110 ) ) ;
#12944=CARTESIAN_POINT ( 'NONE',  ( 0.7495606340400177148, 0.1264236179284866091, 1.813484251914740053 ) ) ;
#12946=CARTESIAN_POINT ( 'NONE',  ( 1.054774247047244096, 0.000000000000000000, 0.4601377952218267953 ) ) ;
#12947=CARTESIAN_POINT ( 'NONE',  ( -0.6971942568897648851, 0.07405724077823318263, 1.417322834591906222 ) ) ;
#12948=CARTESIAN_POINT ( 'NONE',  ( -0.8759842519685039353, 0.1787899950787401882, 0.2731299212060791515 ) ) ;
#12950=CARTESIAN_POINT ( 'NONE',  ( -1.054774247047244540, 0.07405724077823318263, 1.683070866087970074 ) ) ;
#12951=CARTESIAN_POINT ( 'NONE',  ( -0.9412147342319837628, -0.1574803149606297803, 2.000492125876725424 ) ) ;
#12953=CARTESIAN_POINT ( 'NONE',  ( -1.033464566929134687, 0.06523048226347956391, 1.783956692913386766 ) ) ;
#12957=EDGE_CURVE ( 'NONE', #34176, #43833, #47174, .T. ) ;
#12964=DIRECTION ( 'NONE',  ( 1.000000000000000000, 0.000000000000000000, -1.822029033848725275E-16 ) ) ;
#12967=CARTESIAN_POINT ( 'NONE',  ( -0.9873396505805591694, -0.1113553986120547346, 0.7431102361129447997 ) ) ;
#12972=CARTESIAN_POINT ( 'NONE',  ( 0.9500414927467378812, 0.1787899950787401604, 0.9744094487651340231 ) ) ;
#12973=( BOUNDED_CURVE ( )  B_SPLINE_CURVE ( 2, ( #6101, #24113, #38938, #42045, #9248, #34420, #45416, #5648, #31309 ),
 .UNSPECIFIED., .F., .T. ) 
 B_SPLINE_CURVE_WITH_KNOTS ( ( 3, 2, 2, 2, 3 ),
 ( 0.7099999999999999645, 0.7125000000000000222, 0.7149999999999999689, 0.7175000000000000266, 0.7199999999999999734 ),
 .UNSPECIFIED. ) 
 CURVE ( )  GEOMETRIC_REPRESENTATION_ITEM ( )  RATIONAL_B_SPLINE_CURVE ( ( 1.000000000000000000, 0.9238795325112869605, 1.000000000000000000, 0.9238795325112869605, 1.000000000000000000, 0.9238795325112869605, 1.000000000000000000, 0.9238795325112869605, 1.000000000000000000 ) ) 
 REPRESENTATION_ITEM ( '' )  ) ;
#12976=CARTESIAN_POINT ( 'NONE',  ( 0.6971942568897648851, -0.07405724077823297447, 1.938976377898990799 ) ) ;
#12977=CARTESIAN_POINT ( 'NONE',  ( 0.9873396505805591694, 0.1113553986120547346, 0.7135826770578268530 ) ) ;
#12981=DIRECTION ( 'NONE',  ( 1.822029033848725028E-16, 0.000000000000000000, 1.000000000000000000 ) ) ;
#12983=CARTESIAN_POINT ( 'NONE',  ( -0.8759842519685039353, -0.1787899950787401882, 1.941437007820252081 ) ) ;
#12985=CARTESIAN_POINT ( 'NONE',  ( -1.002407869896990045, 0.1264236179284866091, 1.488681102308440751 ) ) ;
#12986=CARTESIAN_POINT ( 'NONE',  ( 0.8759842519685039353, -0.1787899950787401882, 1.473917322780881722 ) ) ;
#12989=CARTESIAN_POINT ( 'NONE',  ( -0.7495606340400177148, -0.1264236179284866091, 0.6815944881352126172 ) ) ;
#12990=CARTESIAN_POINT ( 'NONE',  ( -0.7495606340400177148, -0.1264236179284866091, 1.188484251914740275 ) ) ;
#12991=DIRECTION ( 'NONE',  ( 1.822029033848725028E-16, 0.000000000000000000, 1.000000000000000000 ) ) ;
#12992=CARTESIAN_POINT ( 'NONE',  ( 1.002407869896990045, 0.1264236179284866091, 0.5831692912848189803 ) ) ;
#12993=CARTESIAN_POINT ( 'NONE',  ( -1.002407869896990045, 0.1264236179284866091, 0.5388779527021417826 ) ) ;
#12995=CARTESIAN_POINT ( 'NONE',  ( 0.9412147342319837628, 0.1574803149606300301, 1.660925196742867982 ) ) ;
#12997=CARTESIAN_POINT ( 'NONE',  ( -1.033464566929134687, 0.06523048226347956391, 0.2878937007874017295 ) ) ;
#12998=VECTOR ( 'NONE', #359, 39.37007874015748143 ) ;
#12999=CARTESIAN_POINT ( 'NONE',  ( 0.8759842519685039353, -0.1787899950787401882, 1.277066929080094448 ) ) ;
#13001=CARTESIAN_POINT ( 'NONE',  ( -0.7185039370078739607, 1.928577636452523993E-17, 1.830708661309795149 ) ) ;
#13003=CARTESIAN_POINT ( 'NONE',  ( -1.033464566929134687, -0.06523048226347956391, 0.6373031496062994128 ) ) ;
#13007=LINE ( 'NONE', #30768, #37263 ) ;
#13011=CARTESIAN_POINT ( 'NONE',  ( 0.6971942568897637749, 2.189545951927499583E-17, 1.459153543253322693 ) ) ;
#13019=CARTESIAN_POINT ( 'NONE',  ( 0.8759842519685039353, 0.1787899950787401882, 1.606791338528913426 ) ) ;
#13024=CARTESIAN_POINT ( 'NONE',  ( 0.9500414927467378812, 0.1787899950787401604, 0.5019685038832442103 ) ) ;
#13027=CARTESIAN_POINT ( 'NONE',  ( -0.8019270111902716547, -0.1787899950787401604, 0.8809055117572600624 ) ) ;
#13032=CARTESIAN_POINT ( 'NONE',  ( -0.8493927667999465747, -0.1716682518494001275, 1.987719807708568709 ) ) ;
#13034=CARTESIAN_POINT ( 'NONE',  ( -1.033464566929134687, -0.06523048226347956391, 1.257381889656253193 ) ) ;
#13035=CARTESIAN_POINT ( 'NONE',  ( 1.002407869896990045, 0.1264236179284866091, 1.449311023568283341 ) ) ;
#13037=CARTESIAN_POINT ( 'NONE',  ( 0.9500414927467377701, 0.1787899950787401604, 0.4232283464029293896 ) ) ;
#13038=DIRECTION ( 'NONE',  ( 1.822029033848725028E-16, 0.000000000000000000, 1.000000000000000000 ) ) ;
#13039=CARTESIAN_POINT ( 'NONE',  ( 0.8107537697050254399, -0.1574803149606297803, 0.8538385825696385156 ) ) ;
#13042=CARTESIAN_POINT ( 'NONE',  ( 0.8107537697050254399, -0.1574803149606297803, 0.4995078739082208230 ) ) ;
#13043=CARTESIAN_POINT ( 'NONE',  ( 0.8019270111902717657, 0.1787899950787401604, 0.3887795275052913224 ) ) ;
#13044=CARTESIAN_POINT ( 'NONE',  ( 0.8314340917992454338, -0.1542392197562734157, 0.03937235152828252871 ) ) ;
#13045=CARTESIAN_POINT ( 'NONE',  ( 1.054774247047244540, -0.07405724077823318263, 1.318897637741511364 ) ) ;
#13048=CARTESIAN_POINT ( 'NONE',  ( -1.054774247047244540, 0.07405724077823318263, 1.481299212544662680 ) ) ;
#13049=CARTESIAN_POINT ( 'NONE',  ( 0.9873396505805591694, -0.1113553986120547346, 0.7431102361129447997 ) ) ;
#13051=CYLINDRICAL_SURFACE ( 'NONE', #25305, 0.1574803149606299191 ) ;
#13052=CARTESIAN_POINT ( 'NONE',  ( 0.8019270111902717657, 0.1787899950787401604, 1.023622047190330342 ) ) ;
#13054=CARTESIAN_POINT ( 'NONE',  ( -0.7185039370078746268, 0.06523048226347956391, 0.6077755904436538126 ) ) ;
#13055=DIRECTION ( 'NONE',  ( 1.822029033848725028E-16, 0.000000000000000000, 1.000000000000000000 ) ) ;
#13056=CARTESIAN_POINT ( 'NONE',  ( 1.054774247047244540, 0.07405724077823318263, 1.678149606245448622 ) ) ;
#13057=CARTESIAN_POINT ( 'NONE',  ( -0.9873396505805591694, -0.1113553986120547346, 1.422244094488188892 ) ) ;
#13058=CARTESIAN_POINT ( 'NONE',  ( 0.7646288533564489232, -0.1113553986120547346, 1.796259842412157415 ) ) ;
#13059=CYLINDRICAL_SURFACE ( 'NONE', #9689, 0.1574803149606299191 ) ;
#13060=CARTESIAN_POINT ( 'NONE',  ( -0.7504702239987475210, -0.1105241597664997355, 0.03937007874015843734 ) ) ;
#13061=CARTESIAN_POINT ( 'NONE',  ( 0.6971942568897626646, -0.07405724077823297447, 0.2066929133320631329 ) ) ;
#13062=CARTESIAN_POINT ( 'NONE',  ( -1.002407869896990045, -0.1264236179284866091, 0.09596456687537027741 ) ) ;
#13063=CARTESIAN_POINT ( 'NONE',  ( 0.8107537697050253289, 0.1574803149606300301, 1.390255905404285119 ) ) ;
#13064=VERTEX_POINT ( 'NONE', #11003 ) ;
#13065=EDGE_LOOP ( 'NONE', ( #14869, #20884, #13252, #10151 ) ) ;
#13069=CARTESIAN_POINT ( 'NONE',  ( 0.9500414927467378812, 0.1787899950787401604, 0.7037401574265510495 ) ) ;
#13071=CARTESIAN_POINT ( 'NONE',  ( -1.054774247047244540, -0.07405724077823318263, 1.633858267662771091 ) ) ;
#13079=CARTESIAN_POINT ( 'NONE',  ( -0.9873396505805591694, -0.1113553986120547346, 0.7923228346456693272 ) ) ;
#13086=CARTESIAN_POINT ( 'NONE',  ( -1.033464566929133799, 0.000000000000000000, 1.417322834538141674 ) ) ;
#13088=CARTESIAN_POINT ( 'NONE',  ( 1.033464566929133799, 0.000000000000000000, 1.820866141732283561 ) ) ;
#13091=CARTESIAN_POINT ( 'NONE',  ( -1.054774247047244096, 0.000000000000000000, 0.3026574802611972648 ) ) ;
#13092=CARTESIAN_POINT ( 'NONE',  ( -0.8107537697050253289, -0.1574803149606297803, 1.021161417322834497 ) ) ;
#13094=CARTESIAN_POINT ( 'NONE',  ( 0.8759842519685039353, 0.000000000000000000, 4.498031496062992574 ) ) ;
#13095=CARTESIAN_POINT ( 'NONE',  ( 0.6971942568897637749, 2.189545951927499583E-17, 1.070374015694267600 ) ) ;
#13098=CARTESIAN_POINT ( 'NONE',  ( 1.033464566929133799, 0.000000000000000000, 1.584645669291338654 ) ) ;
#13100=CARTESIAN_POINT ( 'NONE',  ( -0.8418157620803491392, 0.1549362366669437274, 1.979014853567908627 ) ) ;
#13102=CARTESIAN_POINT ( 'NONE',  ( 0.9873396505805591694, -0.1113553986120547346, 1.451771653435779408 ) ) ;
#13106=CARTESIAN_POINT ( 'NONE',  ( 0.6971942568897648851, 0.07405724077823318263, 0.9055118109698584439 ) ) ;
#13107=CARTESIAN_POINT ( 'NONE',  ( 0.8759842519685039353, 0.1787899950787401882, 1.926673228292693052 ) ) ;
#13108=CARTESIAN_POINT ( 'NONE',  ( -0.6971942568897637749, 2.189545951927499583E-17, 1.144192913332062966 ) ) ;
#13109=CARTESIAN_POINT ( 'NONE',  ( 1.033464566929134687, 0.06523048226347956391, 0.3961614172153076763 ) ) ;
#13112=CARTESIAN_POINT ( 'NONE',  ( 0.9412147342319837628, -0.1574803149606297803, 1.892224409448819866 ) ) ;
#13114=CARTESIAN_POINT ( 'NONE',  ( -1.033464566929134687, -0.06523048226347956391, 0.3124999998924728462 ) ) ;
#13120=CARTESIAN_POINT ( 'NONE',  ( 0.8759842519685039353, 0.000000000000000000, 4.498031496062992574 ) ) ;
#13122=CARTESIAN_POINT ( 'NONE',  ( -0.8019270111902717657, 0.1787899950787401604, 0.6249999999462366729 ) ) ;
#13129=CARTESIAN_POINT ( 'NONE',  ( -0.8759842519685039353, 0.1574803149606299191, 0.05905511811023622659 ) ) ;
#13130=VERTEX_POINT ( 'NONE', #19106 ) ;
#13131=CARTESIAN_POINT ( 'NONE',  ( -1.002407869896990045, -0.1264236179284866091, 0.6520669290800944484 ) ) ;
#13133=( BOUNDED_CURVE ( )  B_SPLINE_CURVE ( 2, ( #11384, #25997, #33445, #560, #22632, #45837, #8960, #9194, #1512 ),
 .UNSPECIFIED., .F., .F. ) 
 B_SPLINE_CURVE_WITH_KNOTS ( ( 3, 2, 2, 2, 3 ),
 ( 0.8599999999999999867, 0.8625000000000000444, 0.8649999999999999911, 0.8675000000000000488, 0.8699999999999999956 ),
 .UNSPECIFIED. ) 
 CURVE ( )  GEOMETRIC_REPRESENTATION_ITEM ( )  RATIONAL_B_SPLINE_CURVE ( ( 1.000000000000000000, 0.9238795325112869605, 1.000000000000000000, 0.9238795325112869605, 1.000000000000000000, 0.9238795325112869605, 1.000000000000000000, 0.9238795325112869605, 1.000000000000000000 ) ) 
 REPRESENTATION_ITEM ( '' )  ) ;
#13134=VECTOR ( 'NONE', #34138, 39.37007874015748143 ) ;
#13137=ORIENTED_EDGE ( 'NONE', *, *, #40601, .F. ) ;
#13141=CARTESIAN_POINT ( 'NONE',  ( -1.002407869896990045, 0.1264236179284866091, 0.4207677164816693294 ) ) ;
#13145=CARTESIAN_POINT ( 'NONE',  ( -1.054774247047244540, -0.07405724077823318263, 1.717519684985606476 ) ) ;
#13147=( BOUNDED_CURVE ( )  B_SPLINE_CURVE ( 2, ( #45157, #5154, #16435, #34893, #31066, #35118, #27715, #34406, #13086 ),
 .UNSPECIFIED., .F., .F. ) 
 B_SPLINE_CURVE_WITH_KNOTS ( ( 3, 2, 2, 2, 3 ),
 ( 0.6899999999999999467, 0.6925000000000000044, 0.6949999999999999512, 0.6975000000000000089, 0.6999999999999999556 ),
 .UNSPECIFIED. ) 
 CURVE ( )  GEOMETRIC_REPRESENTATION_ITEM ( )  RATIONAL_B_SPLINE_CURVE ( ( 1.000000000000000000, 0.9238795325112939549, 1.000000000000000000, 0.9238795325112869605, 1.000000000000000000, 0.9238795325112869605, 1.000000000000000000, 0.9238795325112829637, 1.000000000000000000 ) ) 
 REPRESENTATION_ITEM ( '' )  ) ;
#13148=CARTESIAN_POINT ( 'NONE',  ( -0.7185039370078746268, 0.06523048226347977208, 0.1353346455617644717 ) ) ;
#13150=CARTESIAN_POINT ( 'NONE',  ( 0.7646288533564489232, 0.1113553986120547346, 0.5757874015748032370 ) ) ;
#13153=( BOUNDED_CURVE ( )  B_SPLINE_CURVE ( 2, ( #40579, #44887, #4167, #8478, #4391, #8245, #22634, #14742, #12099 ),
 .UNSPECIFIED., .F., .F. ) 
 B_SPLINE_CURVE_WITH_KNOTS ( ( 3, 2, 2, 2, 3 ),
 ( 0.4600000000000000200, 0.4625000000000000222, 0.4650000000000000244, 0.4675000000000000266, 0.4699999999999999734 ),
 .UNSPECIFIED. ) 
 CURVE ( )  GEOMETRIC_REPRESENTATION_ITEM ( )  RATIONAL_B_SPLINE_CURVE ( ( 1.000000000000000000, 0.9238795325112869605, 1.000000000000000000, 0.9238795325112869605, 1.000000000000000000, 0.9238795325112869605, 1.000000000000000000, 0.9238795325112849621, 1.000000000000000000 ) ) 
 REPRESENTATION_ITEM ( '' )  ) ;
#13154=CARTESIAN_POINT ( 'NONE',  ( -0.9873396505805591694, -0.1113553986120547346, 1.215551180994834723 ) ) ;
#13156=CARTESIAN_POINT ( 'NONE',  ( -0.8759842519685039353, 0.1574803149606299191, 0.6791338581601890079 ) ) ;
#13157=CARTESIAN_POINT ( 'NONE',  ( -0.9873396505805591694, 0.1113553986120547346, 0.4084645669291339098 ) ) ;
#13160=CARTESIAN_POINT ( 'NONE',  ( 0.7185039370078746268, -0.06523048226347956391, 1.094980314960628975 ) ) ;
#13162=CARTESIAN_POINT ( 'NONE',  ( -0.7185039370078739607, 1.928577636452523993E-17, 1.328740157480315043 ) ) ;
#13171=CARTESIAN_POINT ( 'NONE',  ( 1.054774247047244540, -0.07405724077823318263, 0.8070866141194653620 ) ) ;
#13173=DIRECTION ( 'NONE',  ( 1.822029033848725028E-16, 0.000000000000000000, 1.000000000000000000 ) ) ;
#13178=CARTESIAN_POINT ( 'NONE',  ( -0.9873396505805591694, 0.1113553986120547346, 1.392716535433070835 ) ) ;
#13179=ORIENTED_EDGE ( 'NONE', *, *, #37662, .T. ) ;
#13180=CARTESIAN_POINT ( 'NONE',  ( -0.8759842519685039353, 0.1787899950787401882, 1.887303149552535420 ) ) ;
#13181=EDGE_CURVE ( 'NONE', #25968, #23819, #18987, .T. ) ;
#13182=CARTESIAN_POINT ( 'NONE',  ( 1.002407869896990045, 0.1264236179284866091, 1.843011810969858333 ) ) ;
#13185=CARTESIAN_POINT ( 'NONE',  ( -0.8019270111902717657, -0.1787899950787401604, 1.584645669237574994 ) ) ;
#13187=CARTESIAN_POINT ( 'NONE',  ( -1.054774247047244540, 0.07405724077823318263, 0.2657480314422993595 ) ) ;
#13188=CARTESIAN_POINT ( 'NONE',  ( -0.9412147342319837628, 0.1574803149606300301, 0.5684055118110233895 ) ) ;
#13189=CARTESIAN_POINT ( 'NONE',  ( -0.6971942568897637749, 2.189545951927499583E-17, 1.779035433017102319 ) ) ;
#13191=CARTESIAN_POINT ( 'NONE',  ( -1.033464566929134687, 0.06523048226347956391, 1.705216535433070613 ) ) ;
#13194=CARTESIAN_POINT ( 'NONE',  ( 0.9500414927467377701, 0.1787899950787401604, 1.727362204670645385 ) ) ;
#13197=CYLINDRICAL_SURFACE ( 'NONE', #46376, 0.1574803149606299191 ) ;
#13198=CIRCLE ( 'NONE', #23883, 0.1574803149606299191 ) ;
#13200=ORIENTED_EDGE ( 'NONE', *, *, #1287, .F. ) ;
#13201=VERTEX_POINT ( 'NONE', #41593 ) ;
#13202=AXIS2_PLACEMENT_3D ( 'NONE', #6257, #43389, #24264 ) ;
#13206=CARTESIAN_POINT ( 'NONE',  ( -1.033464566929133799, 0.000000000000000000, 1.181102362097196989 ) ) ;
#13208=CARTESIAN_POINT ( 'NONE',  ( -0.9873396505805591694, -0.1113553986120547346, 0.8612204723334173639 ) ) ;
#13211=CARTESIAN_POINT ( 'NONE',  ( 0.8759842519685039353, -0.1787899950787401882, 0.9965551180564724554 ) ) ;
#13212=CARTESIAN_POINT ( 'NONE',  ( 0.7185039370078746268, -0.06523048226347956391, 1.085137795168063191 ) ) ;
#13213=CARTESIAN_POINT ( 'NONE',  ( 0.8019270111902717657, 0.1787899950787401604, 1.929133858213952335 ) ) ;
#13214=ORIENTED_EDGE ( 'NONE', *, *, #30555, .F. ) ;
#13216=CYLINDRICAL_SURFACE ( 'NONE', #42020, 0.1574803149606299191 ) ;
#13220=CARTESIAN_POINT ( 'NONE',  ( 0.8759842519685039353, -0.1787899950787401882, 0.3715551180564728440 ) ) ;
#13223=CARTESIAN_POINT ( 'NONE',  ( -0.9500414927467378812, 0.1787899950787401604, 1.958661417269071947 ) ) ;
#13226=CARTESIAN_POINT ( 'NONE',  ( -1.002407869896990045, 0.1264236179284866091, 1.528051181048598384 ) ) ;
#13228=CARTESIAN_POINT ( 'NONE',  ( 1.054774247047244096, 0.000000000000000000, 1.405019684985606476 ) ) ;
#13230=CARTESIAN_POINT ( 'NONE',  ( -1.054774247047244540, 0.07405724077823318263, 0.6594488188438737408 ) ) ;
#13232=CARTESIAN_POINT ( 'NONE',  ( 1.002407869896990045, 0.1264236179284866091, 0.07135826766277185429 ) ) ;
#13236=CARTESIAN_POINT ( 'NONE',  ( 0.7495606340400177148, -0.1264236179284866091, 0.6815944881352126172 ) ) ;
#13237=CARTESIAN_POINT ( 'NONE',  ( -0.6971942568897637749, 2.189545951927499583E-17, 0.5536417322297008115 ) ) ;
#13240=ORIENTED_EDGE ( 'NONE', *, *, #2963, .T. ) ;
#13242=CARTESIAN_POINT ( 'NONE',  ( -0.7646288533564489232, 0.1113553986120547346, 0.3395669291338583307 ) ) ;
#13244=LINE ( 'NONE', #479, #18735 ) ;
#13246=CARTESIAN_POINT ( 'NONE',  ( -0.6971942568897637749, 2.189545951927499583E-17, 0.9522637794737952577 ) ) ;
#13248=ORIENTED_EDGE ( 'NONE', *, *, #6648, .T. ) ;
#13249=CARTESIAN_POINT ( 'NONE',  ( -1.033464566929133799, 0.000000000000000000, 1.377952755797984263 ) ) ;
#13251=FACE_OUTER_BOUND ( 'NONE', #4397, .T. ) ;
#13252=ORIENTED_EDGE ( 'NONE', *, *, #43149, .T. ) ;
#13254=( BOUNDED_CURVE ( )  B_SPLINE_CURVE ( 2, ( #44799, #34517, #16318, #30946, #45508, #19414, #23733, #33831, #38337 ),
 .UNSPECIFIED., .F., .T. ) 
 B_SPLINE_CURVE_WITH_KNOTS ( ( 3, 2, 2, 2, 3 ),
 ( 0.9000000000000000222, 0.9024999999999999689, 0.9050000000000000266, 0.9074999999999999734, 0.9100000000000000311 ),
 .UNSPECIFIED. ) 
 CURVE ( )  GEOMETRIC_REPRESENTATION_ITEM ( )  RATIONAL_B_SPLINE_CURVE ( ( 1.000000000000000000, 0.9238795325112869605, 1.000000000000000000, 0.9238795325112869605, 1.000000000000000000, 0.9238795325112869605, 1.000000000000000000, 0.9238795325112869605, 1.000000000000000000 ) ) 
 REPRESENTATION_ITEM ( '' )  ) ;
#13258=CARTESIAN_POINT ( 'NONE',  ( 0.7646288533564489232, 0.1113553986120547346, 1.432086614065700925 ) ) ;
#13259=CARTESIAN_POINT ( 'NONE',  ( 0.8019270111902717657, -0.1787899950787401604, 0.2460629920722207375 ) ) ;
#13264=CARTESIAN_POINT ( 'NONE',  ( 0.6971942568897637749, 2.189545951927499583E-17, 0.5142716534895434011 ) ) ;
#13266=CARTESIAN_POINT ( 'NONE',  ( -0.6971942568897648851, -0.07405724077823297447, 0.8759842519147408302 ) ) ;
#13268=DIRECTION ( 'NONE',  ( -6.938893903907229955E-15, 0.000000000000000000, -1.000000000000000000 ) ) ;
#13270=CARTESIAN_POINT ( 'NONE',  ( 0.9500414927467378812, -0.1787899950787401604, 1.594488188922613237 ) ) ;
#13273=CARTESIAN_POINT ( 'NONE',  ( 0.7495606340400177148, 0.1264236179284866091, 0.3518700786863940833 ) ) ;
#13274=CARTESIAN_POINT ( 'NONE',  ( -1.033464566929133799, 0.000000000000000000, 1.456692913278299084 ) ) ;
#13277=CARTESIAN_POINT ( 'NONE',  ( 1.002407869896990045, 0.1264236179284866091, 0.4601377952218267953 ) ) ;
#13279=CARTESIAN_POINT ( 'NONE',  ( 1.033464566929133799, 0.000000000000000000, 1.889763779420031486 ) ) ;
#13282=CARTESIAN_POINT ( 'NONE',  ( -0.6971942568897648851, 0.07405724077823318263, 1.496062992072220821 ) ) ;
#13284=CARTESIAN_POINT ( 'NONE',  ( 0.8759842519685039353, 0.000000000000000000, 4.498031496062992574 ) ) ;
#13285=CARTESIAN_POINT ( 'NONE',  ( 0.6971942568897626646, -0.07405724077823297447, 0.9547244093950547628 ) ) ;
#13287=CARTESIAN_POINT ( 'NONE',  ( -0.9412147342319837628, -0.1574803149606297803, 0.5044291337507409434 ) ) ;
#13289=CARTESIAN_POINT ( 'NONE',  ( 0.8019270111902717657, 0.1787899950787401604, 1.687992125930489307 ) ) ;
#13290=CARTESIAN_POINT ( 'NONE',  ( -0.7646288533564489232, 0.1113553986120547346, 1.402559055118110187 ) ) ;
#13292=DIRECTION ( 'NONE',  ( 0.000000000000000000, 0.000000000000000000, -1.000000000000000000 ) ) ;
#13294=CARTESIAN_POINT ( 'NONE',  ( 1.054774247047244096, 0.000000000000000000, 0.2239173227808822775 ) ) ;
#13295=CARTESIAN_POINT ( 'NONE',  ( -0.6971942568897637749, 2.189545951927499583E-17, 0.08120078734781142893 ) ) ;
#13296=CARTESIAN_POINT ( 'NONE',  ( 0.7185039370078746268, 0.06523048226347956391, 1.355807086506646275 ) ) ;
#13298=VERTEX_POINT ( 'NONE', #43024 ) ;
#13300=CARTESIAN_POINT ( 'NONE',  ( -0.8759842519685039353, -0.1787899950787401882, 1.665846456639149764 ) ) ;
#13301=CARTESIAN_POINT ( 'NONE',  ( 1.033836350893150957, 0.005690288880516385442, 0.03937007863263045776 ) ) ;
#13310=CARTESIAN_POINT ( 'NONE',  ( 0.9500414927467378812, -0.1787899950787401604, 1.117125984198206412 ) ) ;
#13311=ADVANCED_FACE ( 'NONE', ( #28455 ), #10475, .T. ) ;
#13312=CARTESIAN_POINT ( 'NONE',  ( -0.8759842519685039353, 0.1574803149606299191, 0.9153543306011338032 ) ) ;
#13313=CARTESIAN_POINT ( 'NONE',  ( 0.7646288533564489232, -0.1113553986120547346, 1.766732283464566899 ) ) ;
#13316=CARTESIAN_POINT ( 'NONE',  ( -1.002407869896990045, 0.1264236179284866091, 0.3075787401037169411 ) ) ;
#13317=CARTESIAN_POINT ( 'NONE',  ( -1.033464566929133799, 0.000000000000000000, 1.033464566929133799 ) ) ;
#13320=CARTESIAN_POINT ( 'NONE',  ( 0.9500414927467378812, -0.1787899950787401604, 1.043307086560409269 ) ) ;
#13321=CARTESIAN_POINT ( 'NONE',  ( 0.8759842519685039353, 0.1787899950787401882, 1.606791338528913426 ) ) ;
#13322=CARTESIAN_POINT ( 'NONE',  ( 1.002407869896990045, -0.1264236179284866091, 0.1747047243556852092 ) ) ;
#13331=CARTESIAN_POINT ( 'NONE',  ( 0.7495606340400177148, -0.1264236179284866091, 1.149114173174582643 ) ) ;
#13332=CARTESIAN_POINT ( 'NONE',  ( 0.7495606340400177148, -0.1264236179284866091, 1.902066929080094448 ) ) ;
#13333=CARTESIAN_POINT ( 'NONE',  ( 0.9412147342319837628, 0.1574803149606300301, 0.3223425195775121432 ) ) ;
#13335=VECTOR ( 'NONE', #18648, 39.37007874015748143 ) ;
#13337=CARTESIAN_POINT ( 'NONE',  ( 1.033464566929133799, 0.000000000000000000, 0.2460629921259842590 ) ) ;
#13338=CARTESIAN_POINT ( 'NONE',  ( -0.8759842519685039353, 0.1574803149606299191, 0.2066929132782996115 ) ) ;
#13339=CARTESIAN_POINT ( 'NONE',  ( 1.054774247047244540, 0.07405724077823318263, 1.363188976324188895 ) ) ;
#13340=ADVANCED_FACE ( 'NONE', ( #43274 ), #46630, .T. ) ;
#13344=CYLINDRICAL_SURFACE ( 'NONE', #22960, 0.1574803149606299191 ) ;
#13346=CARTESIAN_POINT ( 'NONE',  ( 1.033464566929134687, -0.06523048226347956391, 0.5191929133858269596 ) ) ;
#13347=CARTESIAN_POINT ( 'NONE',  ( -0.8107537697050254399, 0.1574803149606300301, 0.2091535431995598104 ) ) ;
#13349=ORIENTED_EDGE ( 'NONE', *, *, #10520, .F. ) ;
#13351=CARTESIAN_POINT ( 'NONE',  ( -0.7495606340400177148, 0.1264236179284866091, 1.026082677111590513 ) ) ;
#13352=CARTESIAN_POINT ( 'NONE',  ( -0.7495606340400177148, -0.1264236179284866091, 1.936515747977732405 ) ) ;
#13353=ORIENTED_EDGE ( 'NONE', *, *, #20766, .F. ) ;
#13354=CARTESIAN_POINT ( 'NONE',  ( -0.9500414927467377701, 0.1787899950787401604, 0.9744094487651340231 ) ) ;
#13356=CARTESIAN_POINT ( 'NONE',  ( -1.002407869896990045, -0.1264236179284866091, 0.6126968503399370380 ) ) ;
#13365=CARTESIAN_POINT ( 'NONE',  ( -1.033464566929133799, 0.000000000000000000, 0.3543307085538902057 ) ) ;
#13366=CARTESIAN_POINT ( 'NONE',  ( -0.7185039370078766252, -0.06523048226348168721, 1.754429133750741832 ) ) ;
#13367=CARTESIAN_POINT ( 'NONE',  ( -1.002407869896990045, 0.1264236179284866091, 0.6569881889226141247 ) ) ;
#13370=CARTESIAN_POINT ( 'NONE',  ( -1.002407869896990045, -0.1264236179284866091, 1.596948818843874074 ) ) ;
#13372=CARTESIAN_POINT ( 'NONE',  ( -0.8107537697050234415, -0.1574803149606297803, 0.1845472439869611792 ) ) ;
#13373=CARTESIAN_POINT ( 'NONE',  ( 0.7185039370078739607, 0.000000000000000000, 4.498031496062992574 ) ) ;
#13374=CARTESIAN_POINT ( 'NONE',  ( 0.8107537697050253289, 0.1574803149606300301, 0.5339566929133855444 ) ) ;
#13375=CARTESIAN_POINT ( 'NONE',  ( 0.7185039370078739607, 1.928577636452523993E-17, 0.6496062991050708391 ) ) ;
#13376=CARTESIAN_POINT ( 'NONE',  ( -0.8107537697050253289, 0.1574803149606300301, 1.193405511703496957 ) ) ;
#13379=CARTESIAN_POINT ( 'NONE',  ( -1.033464566929134687, 0.06523048226347956391, 0.6717519683964101596 ) ) ;
#13380=CARTESIAN_POINT ( 'NONE',  ( -0.7185039370078739607, 1.928577636452523993E-17, 0.4232283464566928832 ) ) ;
#13383=CARTESIAN_POINT ( 'NONE',  ( 0.9873396505805591694, -0.1113553986120547346, 1.264763779527559029 ) ) ;
#13386=DIRECTION ( 'NONE',  ( 0.000000000000000000, 0.000000000000000000, -1.000000000000000000 ) ) ;
#13389=CARTESIAN_POINT ( 'NONE',  ( 1.002407869896990045, -0.1264236179284866091, 1.990649606245448844 ) ) ;
#13391=CARTESIAN_POINT ( 'NONE',  ( -0.7185039370078741827, 0.06523048226347841205, 0.6963582677165353063 ) ) ;
#13396=CARTESIAN_POINT ( 'NONE',  ( 0.8759842519685039353, -0.1787899950787401882, 0.7997047243556849594 ) ) ;
#13403=CARTESIAN_POINT ( 'NONE',  ( 0.7646288533564489232, -0.1113553986120547346, 1.284448818790110192 ) ) ;
#13404=CARTESIAN_POINT ( 'NONE',  ( -0.7646288533564489232, 0.1113553986120547346, 1.402559055118110187 ) ) ;
#13407=CARTESIAN_POINT ( 'NONE',  ( -0.9500414927467378812, -0.1787899950787401604, 1.870078740103715331 ) ) ;
#13408=CARTESIAN_POINT ( 'NONE',  ( 1.054774247047244540, -0.07405724077823318263, 1.993110236166711013 ) ) ;
#13409=EDGE_LOOP ( 'NONE', ( #22047, #34109, #8250, #4883 ) ) ;
#13411=CARTESIAN_POINT ( 'NONE',  ( -0.6971942568897648851, 0.07405724077823318263, 1.574803149552536530 ) ) ;
#13413=CARTESIAN_POINT ( 'NONE',  ( -0.6971942568897626646, 0.07405724077823318263, 0.2017716534895435399 ) ) ;
#13414=CARTESIAN_POINT ( 'NONE',  ( 1.033464566929134687, -0.06523048226347956391, 1.582185039370079149 ) ) ;
#13415=CARTESIAN_POINT ( 'NONE',  ( -0.6971942568897648851, -0.07405724077823297447, 1.860236220418677089 ) ) ;
#13416=CARTESIAN_POINT ( 'NONE',  ( 1.033464566929133799, 0.000000000000000000, 1.417322834538141674 ) ) ;
#13417=CARTESIAN_POINT ( 'NONE',  ( -0.9412147342319837628, -0.1574803149606297803, 1.892224409448819644 ) ) ;
#13422=CARTESIAN_POINT ( 'NONE',  ( 0.7185039370078739607, 1.928577636452523993E-17, 1.043307086506645831 ) ) ;
#13423=( BOUNDED_CURVE ( )  B_SPLINE_CURVE ( 2, ( #23434, #26083, #26802, #4468, #18637, #420, #40658, #19109, #8323 ),
 .UNSPECIFIED., .F., .T. ) 
 B_SPLINE_CURVE_WITH_KNOTS ( ( 3, 2, 2, 2, 3 ),
 ( 0.9399999999999999467, 0.9425000000000000044, 0.9449999999999999512, 0.9475000000000000089, 0.9499999999999999556 ),
 .UNSPECIFIED. ) 
 CURVE ( )  GEOMETRIC_REPRESENTATION_ITEM ( )  RATIONAL_B_SPLINE_CURVE ( ( 1.000000000000000000, 0.9238795325112899581, 1.000000000000000000, 0.9238795325112869605, 1.000000000000000000, 0.9238795325112869605, 1.000000000000000000, 0.9238795325112799661, 1.000000000000000000 ) ) 
 REPRESENTATION_ITEM ( '' )  ) ;
#13426=( BOUNDED_CURVE ( )  B_SPLINE_CURVE ( 2, ( #11636, #33697, #32980, #4648, #21938 ),
 .UNSPECIFIED., .F., .F. ) 
 B_SPLINE_CURVE_WITH_KNOTS ( ( 3, 2, 3 ),
 ( 0.01500000000000034986, 0.01750000000000000167, 0.02000000000000000042 ),
 .UNSPECIFIED. ) 
 CURVE ( )  GEOMETRIC_REPRESENTATION_ITEM ( )  RATIONAL_B_SPLINE_CURVE ( ( 0.9999999999999880096, 0.9238795325112979517, 1.000000000000000000, 0.9238795325112869605, 1.000000000000000000 ) ) 
 REPRESENTATION_ITEM ( '' )  ) ;
#13427=ORIENTED_EDGE ( 'NONE', *, *, #44066, .F. ) ;
#13433=CARTESIAN_POINT ( 'NONE',  ( -0.7185039370078739607, 1.928577636452523993E-17, 0.2263779527559055260 ) ) ;
#13434=CARTESIAN_POINT ( 'NONE',  ( -0.8759842519685039353, 0.1574803149606299191, 0.7972440943806614611 ) ) ;
#13435=CARTESIAN_POINT ( 'NONE',  ( -0.9873396505805591694, 0.1113553986120547346, 0.6840551181102363376 ) ) ;
#13436=EDGE_CURVE ( 'NONE', #4424, #39085, #15958, .T. ) ;
#13438=CARTESIAN_POINT ( 'NONE',  ( 1.054774247047244540, 0.07405724077823318263, 0.9694881889226144578 ) ) ;
#13441=CARTESIAN_POINT ( 'NONE',  ( 0.8759842519685039353, -0.1574803149606299191, 0.1870078739082208508 ) ) ;
#13444=CARTESIAN_POINT ( 'NONE',  ( -0.9873396505805591694, -0.1113553986120547346, 0.7824803148531023211 ) ) ;
#13448=CARTESIAN_POINT ( 'NONE',  ( 0.8759842519685039353, -0.1787899950787401882, 0.3321850393163153226 ) ) ;
#13449=CARTESIAN_POINT ( 'NONE',  ( -0.6971942568897648851, -0.07405724077823297447, 1.855314960576157635 ) ) ;
#13451=CARTESIAN_POINT ( 'NONE',  ( -0.9500414927467378812, -0.1787899950787401604, 1.476377952702141449 ) ) ;
#13452=CARTESIAN_POINT ( 'NONE',  ( 1.054774247047244096, 0.000000000000000000, 1.444389763725763665 ) ) ;
#13455=VECTOR ( 'NONE', #22174, 39.37007874015748143 ) ;
#13456=CARTESIAN_POINT ( 'NONE',  ( -0.9500414927467378812, 0.1787899950787401604, 0.6249999999462356737 ) ) ;
#13458=CARTESIAN_POINT ( 'NONE',  ( 0.8019270111902716547, 0.1787899950787401604, 0.5905511810485987167 ) ) ;
#13459=CARTESIAN_POINT ( 'NONE',  ( -0.6971942568897637749, 2.189545951927499583E-17, 0.5142716534895434011 ) ) ;
#13463=CARTESIAN_POINT ( 'NONE',  ( -1.054774247047244096, 0.000000000000000000, 1.444389763725763665 ) ) ;
#13464=ORIENTED_EDGE ( 'NONE', *, *, #3532, .T. ) ;
#13465=CARTESIAN_POINT ( 'NONE',  ( -1.033464566929133799, 0.000000000000000000, 0.5216535433070865757 ) ) ;
#13466=CARTESIAN_POINT ( 'NONE',  ( 0.8759842519685039353, 0.1787899950787401882, 1.296751968450173154 ) ) ;
#13468=VERTEX_POINT ( 'NONE', #13574 ) ;
#13469=CARTESIAN_POINT ( 'NONE',  ( -0.8107537697050254399, -0.1574803149606297803, 0.5487204724409447953 ) ) ;
#13473=ORIENTED_EDGE ( 'NONE', *, *, #27252, .T. ) ;
#13474=CARTESIAN_POINT ( 'NONE',  ( 1.054774247047244540, 0.07405724077823318263, 1.402559055064346971 ) ) ;
#13480=CYLINDRICAL_SURFACE ( 'NONE', #37910, 0.1574803149606299191 ) ;
#13487=CARTESIAN_POINT ( 'NONE',  ( 1.054774247047244540, 0.07405724077823318263, 0.4576771653005669016 ) ) ;
#13488=CARTESIAN_POINT ( 'NONE',  ( -1.054774247047244096, 0.000000000000000000, 0.8144685038832440993 ) ) ;
#13490=CARTESIAN_POINT ( 'NONE',  ( 0.8759842519685039353, 0.1574803149606299191, 0.9940944880814488460 ) ) ;
#13492=CARTESIAN_POINT ( 'NONE',  ( -0.7744514135987524694, -0.1376688215221703315, 1.986184949705119385 ) ) ;
#13493=CARTESIAN_POINT ( 'NONE',  ( 1.002407869896990045, 0.1264236179284866091, 1.488681102308440751 ) ) ;
#13494=CARTESIAN_POINT ( 'NONE',  ( 0.8759842519685039353, -0.1787899950787401882, 1.941437007820252081 ) ) ;
#13496=CARTESIAN_POINT ( 'NONE',  ( 1.054774247047244540, 0.07405724077823318263, 0.3789370078202520253 ) ) ;
#13500=DIRECTION ( 'NONE',  ( 1.822029033848725028E-16, 0.000000000000000000, 1.000000000000000000 ) ) ;
#13502=CARTESIAN_POINT ( 'NONE',  ( 0.8759842519685039353, 0.1787899950787401882, 0.5831692912848189803 ) ) ;
#13504=CARTESIAN_POINT ( 'NONE',  ( 0.8624158387615522559, -0.1583668281930513955, 0.03937007853128456775 ) ) ;
#13505=CARTESIAN_POINT ( 'NONE',  ( 1.033464566929134687, -0.06523048226347956391, 1.966043306979087246 ) ) ;
#13506=CARTESIAN_POINT ( 'NONE',  ( -0.9500414927467378812, 0.1787899950787401604, 1.407480314906865981 ) ) ;
#13507=CARTESIAN_POINT ( 'NONE',  ( 0.8107537697050254399, -0.1574803149606297803, 0.4306102362204725642 ) ) ;
#13508=CARTESIAN_POINT ( 'NONE',  ( 0.7495606340400177148, -0.1264236179284866091, 0.9965551180564724554 ) ) ;
#13510=CARTESIAN_POINT ( 'NONE',  ( 0.7646288533564489232, -0.1113553986120547346, 1.491141732283464583 ) ) ;
#13511=CARTESIAN_POINT ( 'NONE',  ( -0.7185039370078746268, -0.06523048226347956391, 1.449311023622047445 ) ) ;
#13512=CARTESIAN_POINT ( 'NONE',  ( -0.8019270111902717657, -0.1787899950787401604, 0.9153543306548987957 ) ) ;
#13515=CARTESIAN_POINT ( 'NONE',  ( 0.8019270111902716547, 0.1787899950787401604, 0.1574803149068664809 ) ) ;
#13516=CARTESIAN_POINT ( 'NONE',  ( -1.054774247047244096, 0.000000000000000000, 0.1402559054580474474 ) ) ;
#13517=CARTESIAN_POINT ( 'NONE',  ( 0.7646288533564489232, -0.1113553986120547346, 1.599409448711369919 ) ) ;
#13519=CARTESIAN_POINT ( 'NONE',  ( 0.8107537697050254399, 0.1574803149606300301, 1.783956692805859001 ) ) ;
#13520=CARTESIAN_POINT ( 'NONE',  ( -1.054774247047244096, 0.000000000000000000, 1.715059055064346527 ) ) ;
#13522=FACE_OUTER_BOUND ( 'NONE', #4258, .T. ) ;
#13523=LINE ( 'NONE', #9474, #669 ) ;
#13529=CARTESIAN_POINT ( 'NONE',  ( 0.6971942568897648851, 0.07405724077823318263, 1.062992125930488418 ) ) ;
#13533=CARTESIAN_POINT ( 'NONE',  ( 0.7646288533564489232, -0.1113553986120547346, 1.845472440944881942 ) ) ;
#13535=EDGE_CURVE ( 'NONE', #28682, #7400, #16222, .T. ) ;
#13536=( BOUNDED_CURVE ( )  B_SPLINE_CURVE ( 2, ( #46324, #42698, #43423, #13507, #3425, #39357, #24760, #13734, #40060 ),
 .UNSPECIFIED., .F., .F. ) 
 B_SPLINE_CURVE_WITH_KNOTS ( ( 3, 2, 2, 2, 3 ),
 ( 0.2099999999999999922, 0.2124999999999999944, 0.2149999999999999967, 0.2174999999999999989, 0.2200000000000000011 ),
 .UNSPECIFIED. ) 
 CURVE ( )  GEOMETRIC_REPRESENTATION_ITEM ( )  RATIONAL_B_SPLINE_CURVE ( ( 1.000000000000000000, 0.9238795325112869605, 1.000000000000000000, 0.9238795325112869605, 1.000000000000000000, 0.9238795325112869605, 1.000000000000000000, 0.9238795325112869605, 1.000000000000000000 ) ) 
 REPRESENTATION_ITEM ( '' )  ) ;
#13537=CARTESIAN_POINT ( 'NONE',  ( -0.9500414927467377701, 0.1787899950787401604, 0.3494094487651343006 ) ) ;
#13540=CARTESIAN_POINT ( 'NONE',  ( 0.8019270111902717657, -0.1787899950787401604, 1.038385826717890259 ) ) ;
#13541=CARTESIAN_POINT ( 'NONE',  ( 0.6971942568897648851, 0.07405724077823318263, 1.574803149552536530 ) ) ;
#13542=CARTESIAN_POINT ( 'NONE',  ( 0.8019270111902716547, -0.1787899950787401604, 0.2066929133320631329 ) ) ;
#13544=CARTESIAN_POINT ( 'NONE',  ( -0.8501570456612310700, 0.1562720023928429736, 1.978846797534572044 ) ) ;
#13546=CARTESIAN_POINT ( 'NONE',  ( -0.7185039370078746268, -0.06523048226347956391, 1.715059055010583311 ) ) ;
#13548=CARTESIAN_POINT ( 'NONE',  ( 0.9500414927467378812, -0.1787899950787401604, 0.1722440944344254266 ) ) ;
#13550=CARTESIAN_POINT ( 'NONE',  ( 0.9500414927467377701, 0.1787899950787401604, 1.171259842465921741 ) ) ;
#13551=CARTESIAN_POINT ( 'NONE',  ( -0.7185039370078746268, 0.06523048226347956391, 1.956200787401576102 ) ) ;
#13552=CARTESIAN_POINT ( 'NONE',  ( 0.8759842519685039353, 0.000000000000000000, 4.498031496062992574 ) ) ;
#13553=CARTESIAN_POINT ( 'NONE',  ( 0.8107537697050253289, 0.1574803149606300301, 0.4453740156405042727 ) ) ;
#13556=CARTESIAN_POINT ( 'NONE',  ( 1.029575913376797658, 0.04788448113887518870, 0.03937007987371889811 ) ) ;
#13557=CARTESIAN_POINT ( 'NONE',  ( -0.9412147342319837628, -0.1574803149606297803, 0.2288385825696384601 ) ) ;
#13559=CARTESIAN_POINT ( 'NONE',  ( 0.8107537697050254399, 0.1574803149606300301, 1.232775590443654812 ) ) ;
#13560=CARTESIAN_POINT ( 'NONE',  ( -0.7185039370078739607, 1.928577636452523993E-17, 0.2165354329633393804 ) ) ;
#13562=EDGE_CURVE ( 'NONE', #14046, #32938, #40663, .T. ) ;
#13565=CARTESIAN_POINT ( 'NONE',  ( 0.7185039370078739607, 0.000000000000000000, 4.498031496062992574 ) ) ;
#13566=VERTEX_POINT ( 'NONE', #21723 ) ;
#13567=CARTESIAN_POINT ( 'NONE',  ( -1.054774247047244096, 0.000000000000000000, 1.360728346402929168 ) ) ;
#13569=CARTESIAN_POINT ( 'NONE',  ( -1.054774247047244540, 0.07405724077823318263, 0.9744094487651340231 ) ) ;
#13570=CARTESIAN_POINT ( 'NONE',  ( -0.9500414927467378812, 0.1787899950787401604, 1.919291338528913871 ) ) ;
#13572=CARTESIAN_POINT ( 'NONE',  ( -0.8019270111902716547, -0.1787899950787401604, 1.112204724355684959 ) ) ;
#13573=CARTESIAN_POINT ( 'NONE',  ( -0.8759842519685039353, 0.1787899950787401882, 0.6668307086076534773 ) ) ;
#13574=CARTESIAN_POINT ( 'NONE',  ( -1.033464566929133799, 0.000000000000000000, 0.2460629921259842590 ) ) ;
#13579=CARTESIAN_POINT ( 'NONE',  ( -0.9412147342319837628, -0.1574803149606297803, 1.734744094488190003 ) ) ;
#13580=CARTESIAN_POINT ( 'NONE',  ( -0.8019270111902717657, -0.1787899950787401604, 0.5610236219934807700 ) ) ;
#13583=ORIENTED_EDGE ( 'NONE', *, *, #13181, .T. ) ;
#13584=CARTESIAN_POINT ( 'NONE',  ( -0.6971942568897648851, -0.07405724077823297447, 1.663385826717890925 ) ) ;
#13587=CARTESIAN_POINT ( 'NONE',  ( -1.033464566929133799, 0.000000000000000000, 0.4822834645669291653 ) ) ;
#13589=CARTESIAN_POINT ( 'NONE',  ( 0.9873396505805591694, 0.1113553986120547346, 0.5659448818897637734 ) ) ;
#13591=CARTESIAN_POINT ( 'NONE',  ( -0.9873396505805591694, 0.1113553986120547346, 0.9596456692913386544 ) ) ;
#13592=CARTESIAN_POINT ( 'NONE',  ( -0.7185039370078746268, -0.06523048226347956391, 1.400098425089323140 ) ) ;
#13595=ORIENTED_EDGE ( 'NONE', *, *, #38353, .F. ) ;
#13597=CARTESIAN_POINT ( 'NONE',  ( 0.7185039370078746268, 0.06523048226347956391, 1.326279527559055982 ) ) ;
#13600=CARTESIAN_POINT ( 'NONE',  ( 1.033464566929133799, 0.000000000000000000, 1.742125984251968518 ) ) ;
#13601=CARTESIAN_POINT ( 'NONE',  ( 0.6971942568897648851, -0.07405724077823297447, 0.6348425196312760255 ) ) ;
#13602=CARTESIAN_POINT ( 'NONE',  ( 0.7646288533564489232, -0.1113553986120547346, 1.678149606191684962 ) ) ;
#13603=CARTESIAN_POINT ( 'NONE',  ( -0.8759842519685039353, 0.1574803149606299191, 0.6889763779527560139 ) ) ;
#13606=CARTESIAN_POINT ( 'NONE',  ( -1.033464566929134687, -0.06523048226347956391, 1.070374015748031038 ) ) ;
#13607=CARTESIAN_POINT ( 'NONE',  ( 1.033464566929134687, -0.06523048226347956391, 0.7160433070866151217 ) ) ;
#13608=CARTESIAN_POINT ( 'NONE',  ( 0.8019270111902717657, -0.1787899950787401604, 0.7578740156942689321 ) ) ;
#13610=CARTESIAN_POINT ( 'NONE',  ( 0.7185039370078739607, 1.928577636452523993E-17, 1.289370078740157632 ) ) ;
#13611=FACE_OUTER_BOUND ( 'NONE', #20479, .T. ) ;
#13615=CARTESIAN_POINT ( 'NONE',  ( 0.8107537697050253289, -0.1574803149606297803, 1.247539369971212508 ) ) ;
#13620=CARTESIAN_POINT ( 'NONE',  ( -0.8019270111902717657, 0.1787899950787401604, 1.889763779473794258 ) ) ;
#13621=VERTEX_POINT ( 'NONE', #36576 ) ;
#13622=CARTESIAN_POINT ( 'NONE',  ( -0.8759842519685039353, 0.000000000000000000, 0.000000000000000000 ) ) ;
#13624=CARTESIAN_POINT ( 'NONE',  ( -1.002407869896990045, -0.1264236179284866091, 1.951279527505291433 ) ) ;
#13625=CARTESIAN_POINT ( 'NONE',  ( -1.054774247047244540, 0.07405724077823318263, 1.599409448765135133 ) ) ;
#13629=CARTESIAN_POINT ( 'NONE',  ( -0.7495606340400177148, 0.1264236179284866091, 0.2386811023084413619 ) ) ;
#13631=CARTESIAN_POINT ( 'NONE',  ( -1.054774247047244540, -0.07405724077823318263, 1.835629921206078485 ) ) ;
#13633=CARTESIAN_POINT ( 'NONE',  ( -1.033464566929133799, 0.000000000000000000, 1.938976377952756014 ) ) ;
#13634=CARTESIAN_POINT ( 'NONE',  ( -0.7185039370078766252, -0.06523048226348168721, 1.882381889763779625 ) ) ;
#13637=CARTESIAN_POINT ( 'NONE',  ( -0.8107537697050254399, -0.1574803149606297803, 1.493602362204724754 ) ) ;
#13638=CARTESIAN_POINT ( 'NONE',  ( 0.9873396505805591694, -0.1113553986120547346, 1.058070866034204860 ) ) ;
#13639=CARTESIAN_POINT ( 'NONE',  ( -0.6971942568897637749, 2.189545951927499583E-17, 0.1599409448281264023 ) ) ;
#13640=EDGE_CURVE ( 'NONE', #46242, #32499, #14774, .T. ) ;
#13642=ORIENTED_EDGE ( 'NONE', *, *, #33323, .F. ) ;
#13643=CARTESIAN_POINT ( 'NONE',  ( -1.054774247047244540, -0.07405724077823318263, 1.205708661363558365 ) ) ;
#13652=CARTESIAN_POINT ( 'NONE',  ( -0.9873396505805591694, -0.1113553986120547346, 0.9399606298137322957 ) ) ;
#13653=CARTESIAN_POINT ( 'NONE',  ( -1.033464566929134687, 0.06523048226347956391, 0.7603346456692923194 ) ) ;
#13656=CARTESIAN_POINT ( 'NONE',  ( 0.9873396505805591694, 0.1113553986120547346, 1.815944881782236120 ) ) ;
#13657=CARTESIAN_POINT ( 'NONE',  ( 1.033464566929133799, 0.000000000000000000, 0.8366141732283465249 ) ) ;
#13658=CARTESIAN_POINT ( 'NONE',  ( -0.9873396505805591694, 0.1113553986120547346, 1.235236220472440971 ) ) ;
#13660=CARTESIAN_POINT ( 'NONE',  ( 0.7646288533564489232, 0.1113553986120547346, 1.520669291338582640 ) ) ;
#13661=CARTESIAN_POINT ( 'NONE',  ( 0.9412147342319837628, -0.1574803149606297803, 0.2288385825696384601 ) ) ;
#13663=VERTEX_POINT ( 'NONE', #44914 ) ;
#13664=CARTESIAN_POINT ( 'NONE',  ( 0.7185039370078741827, -0.06523048226347841205, 0.3764763778452291376 ) ) ;
#13668=ORIENTED_EDGE ( 'NONE', *, *, #6617, .T. ) ;
#13669=CARTESIAN_POINT ( 'NONE',  ( -0.6971942568897648851, 0.07405724077823318263, 1.382874015694268044 ) ) ;
#13670=CARTESIAN_POINT ( 'NONE',  ( 0.9500414927467378812, -0.1787899950787401604, 1.555118110182455382 ) ) ;
#13673=CARTESIAN_POINT ( 'NONE',  ( -0.8759842519685039353, 0.1787899950787401882, 0.7062007873478109987 ) ) ;
#13674=EDGE_CURVE ( 'NONE', #14505, #13621, #21086, .T. ) ;
#13676=CARTESIAN_POINT ( 'NONE',  ( -1.054774247047244096, 0.000000000000000000, 0.6126968503399370380 ) ) ;
#13678=CARTESIAN_POINT ( 'NONE',  ( -1.033464566929134687, -0.06523048226347956391, 0.8735236220472449853 ) ) ;
#13682=CARTESIAN_POINT ( 'NONE',  ( -0.8107537697050253289, -0.1574803149606297803, 1.493602362204724754 ) ) ;
#13683=( BOUNDED_CURVE ( )  B_SPLINE_CURVE ( 2, ( #31038, #45605, #42001, #23825, #46085, #42947, #28144, #25240, #39597 ),
 .UNSPECIFIED., .F., .T. ) 
 B_SPLINE_CURVE_WITH_KNOTS ( ( 3, 2, 2, 2, 3 ),
 ( 0.04000000000000000083, 0.04250000000000000305, 0.04499999999999999833, 0.04750000000000000056, 0.05000000000000000278 ),
 .UNSPECIFIED. ) 
 CURVE ( )  GEOMETRIC_REPRESENTATION_ITEM ( )  RATIONAL_B_SPLINE_CURVE ( ( 1.000000000000000000, 0.9238795325112869605, 1.000000000000000000, 0.9238795325112869605, 1.000000000000000000, 0.9238795325112869605, 1.000000000000000000, 0.9238795325112869605, 1.000000000000000000 ) ) 
 REPRESENTATION_ITEM ( '' )  ) ;
#13684=CARTESIAN_POINT ( 'NONE',  ( -0.9873396505805591694, 0.1113553986120547346, 0.5265748031496062520 ) ) ;
#13687=CARTESIAN_POINT ( 'NONE',  ( 0.6971942568897648851, -0.07405724077823297447, 1.309055118056473122 ) ) ;
#13689=EDGE_LOOP ( 'NONE', ( #9501, #44712, #46621, #5691 ) ) ;
#13690=CARTESIAN_POINT ( 'NONE',  ( -1.033464566929133799, 0.000000000000000000, 0.9448818896562519720 ) ) ;
#13693=VERTEX_POINT ( 'NONE', #30829 ) ;
#13696=CARTESIAN_POINT ( 'NONE',  ( 0.9873396505805591694, 0.1113553986120547346, 0.8021653543307086798 ) ) ;
#13697=DIRECTION ( 'NONE',  ( 1.822029033848725028E-16, 0.000000000000000000, 1.000000000000000000 ) ) ;
#13699=CARTESIAN_POINT ( 'NONE',  ( 0.9500414927467378812, -0.1787899950787401604, 1.432086614119464141 ) ) ;
#13703=CARTESIAN_POINT ( 'NONE',  ( -0.7185039370078760701, -0.06523048226348075740, 0.9670275589475921807 ) ) ;
#13704=CARTESIAN_POINT ( 'NONE',  ( 1.054774247047244540, 0.07405724077823318263, 1.678149606245448622 ) ) ;
#13705=CARTESIAN_POINT ( 'NONE',  ( 0.8759842519685039353, -0.1787899950787401882, 0.2485236219934806867 ) ) ;
#13708=CARTESIAN_POINT ( 'NONE',  ( 0.8759842519685039353, 0.000000000000000000, 4.498031496062992574 ) ) ;
#13711=CARTESIAN_POINT ( 'NONE',  ( 0.8019270111902717657, 0.1787899950787401604, 0.5856299212060785964 ) ) ;
#13712=CARTESIAN_POINT ( 'NONE',  ( -0.8759842519685039353, 0.1787899950787401882, 0.8243110235682834519 ) ) ;
#13715=CARTESIAN_POINT ( 'NONE',  ( 0.9873396505805591694, 0.1113553986120547346, 1.697834645561763889 ) ) ;
#13719=CARTESIAN_POINT ( 'NONE',  ( 1.054774247047244540, -0.07405724077823318263, 1.599409448765135133 ) ) ;
#13721=CARTESIAN_POINT ( 'NONE',  ( -0.7185039370078739607, 1.928577636452523993E-17, 1.801181102362204633 ) ) ;
#13722=CARTESIAN_POINT ( 'NONE',  ( 0.6971942568897637749, 2.189545951927499583E-17, 0.3174212597887562382 ) ) ;
#13723=ORIENTED_EDGE ( 'NONE', *, *, #10246, .T. ) ;
#13727=CARTESIAN_POINT ( 'NONE',  ( 1.054774247047244540, -0.07405724077823318263, 0.5314960629383620461 ) ) ;
#13730=CARTESIAN_POINT ( 'NONE',  ( -0.9412147342319837628, -0.1574803149606297803, 1.528051180994836056 ) ) ;
#13731=CARTESIAN_POINT ( 'NONE',  ( 1.054774247047244540, 0.07405724077823318263, 0.5364173227808820554 ) ) ;
#13732=CARTESIAN_POINT ( 'NONE',  ( -0.8019270111902717657, -0.1787899950787401604, 1.466535433017102763 ) ) ;
#13733=ORIENTED_EDGE ( 'NONE', *, *, #40721, .T. ) ;
#13734=CARTESIAN_POINT ( 'NONE',  ( 1.033464566929134687, -0.06523048226347956391, 0.4404527559055117503 ) ) ;
#13735=CARTESIAN_POINT ( 'NONE',  ( 1.054774247047244540, 0.07405724077823318263, 1.171259842465921741 ) ) ;
#13738=CARTESIAN_POINT ( 'NONE',  ( 0.8019270111902717657, -0.1787899950787401604, 1.820866141678520789 ) ) ;
#13739=CARTESIAN_POINT ( 'NONE',  ( -0.7185039370078746268, 0.06523048226347956391, 1.365649606299211838 ) ) ;
#13740=CARTESIAN_POINT ( 'NONE',  ( -1.054774247047244540, 0.07405724077823318263, 0.8907480314422986378 ) ) ;
#13741=ADVANCED_FACE ( 'NONE', ( #40840 ), #11891, .T. ) ;
#13742=CARTESIAN_POINT ( 'NONE',  ( -0.8759842519685039353, 0.1574803149606299191, 0.5216535431995598104 ) ) ;
#13744=CARTESIAN_POINT ( 'NONE',  ( 0.7495606340400177148, 0.1264236179284866091, 0.1205708660879689087 ) ) ;
#13745=CARTESIAN_POINT ( 'NONE',  ( 0.9873396505805591694, -0.1113553986120547346, 1.648622047136566904 ) ) ;
#13746=ORIENTED_EDGE ( 'NONE', *, *, #34263, .F. ) ;
#13749=CARTESIAN_POINT ( 'NONE',  ( 0.9500414927467378812, -0.1787899950787401604, 0.7677165353793073965 ) ) ;
#13751=CARTESIAN_POINT ( 'NONE',  ( -0.9500414927467377701, -0.1787899950787401604, 1.707677165300568456 ) ) ;
#13752=EDGE_CURVE ( 'NONE', #22068, #12322, #28834, .T. ) ;
#13764=CARTESIAN_POINT ( 'NONE',  ( 0.8759842519685039353, -0.1787899950787401882, 0.09104330703285078152 ) ) ;
#13767=VERTEX_POINT ( 'NONE', #37754 ) ;
#13768=CARTESIAN_POINT ( 'NONE',  ( -0.6971942568897626646, -0.07405724077823297447, 0.3248031495525359746 ) ) ;
#13769=CARTESIAN_POINT ( 'NONE',  ( -0.7185039370078739607, 1.928577636452523993E-17, 1.948818897530267602 ) ) ;
#13770=CARTESIAN_POINT ( 'NONE',  ( 0.6971942568897648851, -0.07405724077823297447, 1.190944881836001112 ) ) ;
#13771=CARTESIAN_POINT ( 'NONE',  ( 1.054774247047244096, 0.000000000000000000, 1.518208661363559031 ) ) ;
#13772=CARTESIAN_POINT ( 'NONE',  ( 0.7495606340400177148, -0.1264236179284866091, 0.1648622046706460786 ) ) ;
#13774=CARTESIAN_POINT ( 'NONE',  ( 0.8107537697050254399, -0.1574803149606297803, 0.8932086613097963701 ) ) ;
#13776=CARTESIAN_POINT ( 'NONE',  ( -0.7185039370078739607, 1.928577636452523993E-17, 1.279527558947590515 ) ) ;
#13777=CARTESIAN_POINT ( 'NONE',  ( -0.9412147342319837628, 0.1574803149606300301, 1.739665354223181470 ) ) ;
#13778=CARTESIAN_POINT ( 'NONE',  ( 0.6971942568897626646, -0.07405724077823297447, 0.1624015747493861295 ) ) ;
#13779=CARTESIAN_POINT ( 'NONE',  ( 0.7185039370078766252, -0.06523048226348168721, 1.646161417322834497 ) ) ;
#13780=CARTESIAN_POINT ( 'NONE',  ( 0.7495606340400177148, 0.1264236179284866091, 1.139271653489543290 ) ) ;
#13781=CYLINDRICAL_SURFACE ( 'NONE', #42201, 0.1574803149606299191 ) ;
#13783=CARTESIAN_POINT ( 'NONE',  ( 1.054774247047244096, 0.000000000000000000, 1.956200787347811110 ) ) ;
#13784=CARTESIAN_POINT ( 'NONE',  ( 0.7185039370078739607, 1.928577636452523993E-17, 0.4921259841444416971 ) ) ;
#13786=LINE ( 'NONE', #32501, #45971 ) ;
#13788=CARTESIAN_POINT ( 'NONE',  ( -1.033464566929134687, -0.06523048226347956391, 0.3912401573727880555 ) ) ;
#13791=CARTESIAN_POINT ( 'NONE',  ( 0.8019270111902717657, -0.1787899950787401604, 1.505905511757261284 ) ) ;
#13792=CARTESIAN_POINT ( 'NONE',  ( -1.033464566929133799, 0.000000000000000000, 0.4330708660342047489 ) ) ;
#13794=VECTOR ( 'NONE', #1416, 39.37007874015748143 ) ;
#13796=CARTESIAN_POINT ( 'NONE',  ( 0.9873396505805591694, 0.1113553986120547346, 0.7234251968503936370 ) ) ;
#13797=( BOUNDED_CURVE ( )  B_SPLINE_CURVE ( 2, ( #33667, #780, #44628, #11843, #25760, #22137, #12082, #26470, #4861 ),
 .UNSPECIFIED., .F., .T. ) 
 B_SPLINE_CURVE_WITH_KNOTS ( ( 3, 2, 2, 2, 3 ),
 ( 0.1300000000000000044, 0.1325000000000000067, 0.1350000000000000089, 0.1375000000000000111, 0.1400000000000000133 ),
 .UNSPECIFIED. ) 
 CURVE ( )  GEOMETRIC_REPRESENTATION_ITEM ( )  RATIONAL_B_SPLINE_CURVE ( ( 1.000000000000000000, 0.9238795325112869605, 1.000000000000000000, 0.9238795325112869605, 1.000000000000000000, 0.9238795325112869605, 1.000000000000000000, 0.9238795325112869605, 1.000000000000000000 ) ) 
 REPRESENTATION_ITEM ( '' )  ) ;
#13798=ADVANCED_FACE ( 'NONE', ( #41542 ), #38227, .T. ) ;
#13799=VERTEX_POINT ( 'NONE', #4909 ) ;
#13801=DIRECTION ( 'NONE',  ( 1.822029033848725028E-16, 0.000000000000000000, 1.000000000000000000 ) ) ;
#13803=CARTESIAN_POINT ( 'NONE',  ( 0.8759842519685039353, 0.1787899950787401882, 0.5093503936470236138 ) ) ;
#13806=CARTESIAN_POINT ( 'NONE',  ( -0.8019270111902716547, -0.1787899950787401604, 1.427165354276944687 ) ) ;
#13808=CARTESIAN_POINT ( 'NONE',  ( -0.7495606340400177148, -0.1264236179284866091, 1.114665354276944909 ) ) ;
#13809=CARTESIAN_POINT ( 'NONE',  ( -0.8019270111902717657, -0.1787899950787401604, 1.938976377898990799 ) ) ;
#13810=ORIENTED_EDGE ( 'NONE', *, *, #37885, .F. ) ;
#13811=CARTESIAN_POINT ( 'NONE',  ( -0.6971942568897648851, 0.07405724077823318263, 1.102362204670646495 ) ) ;
#13813=CARTESIAN_POINT ( 'NONE',  ( -0.9412147342319837628, -0.1574803149606297803, 0.3567913385826773087 ) ) ;
#13819=ORIENTED_EDGE ( 'NONE', *, *, #45806, .F. ) ;
#13820=CARTESIAN_POINT ( 'NONE',  ( 0.9873396505805591694, 0.1113553986120547346, 0.7627952755905511584 ) ) ;
#13822=( BOUNDED_CURVE ( )  B_SPLINE_CURVE ( 2, ( #19258, #37001, #44401, #25764, #19010, #11618, #33674, #33913, #26475 ),
 .UNSPECIFIED., .F., .F. ) 
 B_SPLINE_CURVE_WITH_KNOTS ( ( 3, 2, 2, 2, 3 ),
 ( 0.05999999999999999778, 0.06250000000000000000, 0.06500000000000000222, 0.06750000000000000444, 0.07000000000000000666 ),
 .UNSPECIFIED. ) 
 CURVE ( )  GEOMETRIC_REPRESENTATION_ITEM ( )  RATIONAL_B_SPLINE_CURVE ( ( 1.000000000000000000, 0.9238795325112869605, 1.000000000000000000, 0.9238795325112869605, 1.000000000000000000, 0.9238795325112869605, 1.000000000000000000, 0.9238795325112869605, 1.000000000000000000 ) ) 
 REPRESENTATION_ITEM ( '' )  ) ;
#13823=CARTESIAN_POINT ( 'NONE',  ( -0.8759842519685039353, -0.1787899950787401882, 0.5634842519147401640 ) ) ;
#13825=EDGE_LOOP ( 'NONE', ( #33422, #23805, #23782, #27229 ) ) ;
#13826=CARTESIAN_POINT ( 'NONE',  ( -1.054774247047244096, 0.000000000000000000, 1.601870078686393750 ) ) ;
#13828=AXIS2_PLACEMENT_3D ( 'NONE', #45149, #44911, #38217 ) ;
#13831=CARTESIAN_POINT ( 'NONE',  ( 0.9873396505805591694, -0.1113553986120547346, 0.5954724409448819422 ) ) ;
#13833=CARTESIAN_POINT ( 'NONE',  ( -0.7185039370078746268, 0.06523048226347956391, 0.9719488188976379561 ) ) ;
#13835=DIRECTION ( 'NONE',  ( 0.000000000000000000, 0.000000000000000000, 1.000000000000000000 ) ) ;
#13837=CARTESIAN_POINT ( 'NONE',  ( 1.033464566929133799, 0.000000000000000000, 1.269685039370078705 ) ) ;
#13838=CARTESIAN_POINT ( 'NONE',  ( 0.7790738941308391619, -0.1411882674591699027, 1.986291969488682252 ) ) ;
#13840=CARTESIAN_POINT ( 'NONE',  ( 0.7185039370078746268, -0.06523048226347956391, 1.843011811023621327 ) ) ;
#13842=CARTESIAN_POINT ( 'NONE',  ( 1.054774247047244540, 0.07405724077823318263, 0.6151574802611965431 ) ) ;
#13843=CARTESIAN_POINT ( 'NONE',  ( 0.8107537697050234415, -0.1574803149606297803, 0.2632874014672759722 ) ) ;
#13844=DIRECTION ( 'NONE',  ( 1.822029033848725028E-16, 0.000000000000000000, 1.000000000000000000 ) ) ;
#13847=ORIENTED_EDGE ( 'NONE', *, *, #1262, .T. ) ;
#13848=CARTESIAN_POINT ( 'NONE',  ( 0.7185039370078739607, 1.928577636452523993E-17, 0.6102362203649134287 ) ) ;
#13850=CARTESIAN_POINT ( 'NONE',  ( 0.6971942568897637749, 2.189545951927499583E-17, 0.7898622046706456068 ) ) ;
#13851=ORIENTED_EDGE ( 'NONE', *, *, #4362, .F. ) ;
#13852=CARTESIAN_POINT ( 'NONE',  ( 1.033464566929134687, 0.06523048226347956391, 1.468996062992126150 ) ) ;
#13853=DIRECTION ( 'NONE',  ( -1.000000000000000000, 0.000000000000000000, 0.000000000000000000 ) ) ;
#13860=CARTESIAN_POINT ( 'NONE',  ( -0.6971942568897626646, -0.07405724077823297447, 0.08366141726907129483 ) ) ;
#13862=CARTESIAN_POINT ( 'NONE',  ( -0.7646288533564489232, -0.1113553986120547346, 0.8120078739082204899 ) ) ;
#13863=ORIENTED_EDGE ( 'NONE', *, *, #9426, .F. ) ;
#13864=CARTESIAN_POINT ( 'NONE',  ( -1.054774247047244540, -0.07405724077823318263, 1.953740157426552715 ) ) ;
#13865=VECTOR ( 'NONE', #40632, 39.37007874015748143 ) ;
#13866=CARTESIAN_POINT ( 'NONE',  ( -0.7495606340400177148, -0.1264236179284866091, 1.464074803095842370 ) ) ;
#13867=CARTESIAN_POINT ( 'NONE',  ( 0.9500414927467377701, -0.1787899950787401604, 0.8858267715997791836 ) ) ;
#13868=EDGE_CURVE ( 'NONE', #480, #10797, #15965, .T. ) ;
#13870=CARTESIAN_POINT ( 'NONE',  ( -1.002407869896990045, 0.1264236179284866091, 0.2682086613635594752 ) ) ;
#13871=CARTESIAN_POINT ( 'NONE',  ( -0.9500414927467378812, -0.1787899950787401604, 1.909448818843873186 ) ) ;
#13872=CARTESIAN_POINT ( 'NONE',  ( -0.8107537697050253289, 0.1574803149606300301, 1.833169291338582418 ) ) ;
#13873=CARTESIAN_POINT ( 'NONE',  ( -1.033464566929133799, 0.000000000000000000, 1.899606299212598604 ) ) ;
#13875=VECTOR ( 'NONE', #29642, 39.37007874015748143 ) ;
#13878=CARTESIAN_POINT ( 'NONE',  ( 1.033464566929133799, 0.000000000000000000, 0.1574803148531029595 ) ) ;
#13879=CARTESIAN_POINT ( 'NONE',  ( -0.8019270111902717657, 0.1787899950787401604, 0.2312992125446618197 ) ) ;
#13881=VERTEX_POINT ( 'NONE', #15489 ) ;
#13882=CARTESIAN_POINT ( 'NONE',  ( -0.6971942568897648851, -0.07405724077823297447, 1.190944881836001112 ) ) ;
#13890=CARTESIAN_POINT ( 'NONE',  ( -0.8107537697050253289, -0.1574803149606297803, 0.7062007874015745479 ) ) ;
#13891=VECTOR ( 'NONE', #37761, 39.37007874015748143 ) ;
#13893=CARTESIAN_POINT ( 'NONE',  ( 0.8107537697050253289, -0.1574803149606297803, 1.877460629813732407 ) ) ;
#13896=CARTESIAN_POINT ( 'NONE',  ( 0.7646288533564489232, -0.1113553986120547346, 0.8218503937007874960 ) ) ;
#13900=CARTESIAN_POINT ( 'NONE',  ( 0.7646288533564489232, 0.1113553986120547346, 0.2116141731208196763 ) ) ;
#13901=ORIENTED_EDGE ( 'NONE', *, *, #25577, .T. ) ;
#13902=VERTEX_POINT ( 'NONE', #38220 ) ;
#13903=DIRECTION ( 'NONE',  ( 0.000000000000000000, 0.000000000000000000, -1.000000000000000000 ) ) ;
#13907=CARTESIAN_POINT ( 'NONE',  ( 0.8107537697050253289, -0.1574803149606297803, 0.7750984250893222516 ) ) ;
#13910=CARTESIAN_POINT ( 'NONE',  ( -0.6971942568897626646, 0.07405724077823318263, 0.4330708660879683536 ) ) ;
#13911=ORIENTED_EDGE ( 'NONE', *, *, #4049, .T. ) ;
#13912=ORIENTED_EDGE ( 'NONE', *, *, #35276, .F. ) ;
#13913=CARTESIAN_POINT ( 'NONE',  ( -0.6971942568897637749, 2.189545951927499583E-17, 1.424704724355685181 ) ) ;
#13914=CARTESIAN_POINT ( 'NONE',  ( 0.6971942568897648851, 0.07405724077823318263, 1.500984251914741607 ) ) ;
#13916=CARTESIAN_POINT ( 'NONE',  ( -1.054774247047244096, 0.000000000000000000, 0.6569881889226141247 ) ) ;
#13917=CARTESIAN_POINT ( 'NONE',  ( 0.6971942568897626646, -0.07405724077823297447, 0.1673228345919059168 ) ) ;
#13918=CARTESIAN_POINT ( 'NONE',  ( -1.033464566929133799, 0.000000000000000000, 1.692913385719244213 ) ) ;
#13919=CARTESIAN_POINT ( 'NONE',  ( 1.054774247047244540, -0.07405724077823318263, 0.7332677164816705506 ) ) ;
#13920=CARTESIAN_POINT ( 'NONE',  ( -1.002407869896990045, -0.1264236179284866091, 0.6865157479777322935 ) ) ;
#13925=CARTESIAN_POINT ( 'NONE',  ( 1.033464566929134687, 0.06523048226347956391, 1.065452755797984041 ) ) ;
#13927=CARTESIAN_POINT ( 'NONE',  ( -0.8019270111902717657, -0.1787899950787401604, 1.432086614119464141 ) ) ;
#13929=CARTESIAN_POINT ( 'NONE',  ( -0.9412147342319837628, -0.1574803149606297803, 1.498523622047243764 ) ) ;
#13930=CARTESIAN_POINT ( 'NONE',  ( -0.9873396505805591694, 0.1113553986120547346, 0.4084645669291339098 ) ) ;
#13931=CARTESIAN_POINT ( 'NONE',  ( 1.054774247047244540, -0.07405724077823318263, 1.363188976324188673 ) ) ;
#13932=AXIS2_PLACEMENT_3D ( 'NONE', #45338, #44620, #12554 ) ;
#13935=CARTESIAN_POINT ( 'NONE',  ( -0.7185039370078739607, 1.928577636452523993E-17, 0.6200787401574803237 ) ) ;
#13939=CARTESIAN_POINT ( 'NONE',  ( 0.7646288533564489232, -0.1113553986120547346, 0.3887795275590551491 ) ) ;
#13940=ORIENTED_EDGE ( 'NONE', *, *, #5348, .T. ) ;
#13941=CARTESIAN_POINT ( 'NONE',  ( 0.8759842519685039353, 0.1787899950787401882, 1.370570866087968520 ) ) ;
#13942=LINE ( 'NONE', #36239, #6250 ) ;
#13944=CARTESIAN_POINT ( 'NONE',  ( 0.8759842519685039353, 0.000000000000000000, 4.498031496062992574 ) ) ;
#13945=CARTESIAN_POINT ( 'NONE',  ( -0.9412147342319837628, -0.1574803149606297803, 0.9768700786326298680 ) ) ;
#13946=CARTESIAN_POINT ( 'NONE',  ( 1.002407869896990045, -0.1264236179284866091, 0.3321850393163153226 ) ) ;
#13950=CARTESIAN_POINT ( 'NONE',  ( 0.8019270111902717657, 0.1787899950787401604, 0.5462598424659214080 ) ) ;
#13952=CARTESIAN_POINT ( 'NONE',  ( -1.054774247047244096, 0.000000000000000000, 1.011318897584031484 ) ) ;
#13953=FACE_OUTER_BOUND ( 'NONE', #11880, .T. ) ;
#13954=CARTESIAN_POINT ( 'NONE',  ( 0.9412147342319837628, 0.1574803149606300301, 0.9916338581601894520 ) ) ;
#13958=CARTESIAN_POINT ( 'NONE',  ( 1.054774247047244540, 0.07405724077823318263, 1.683070866087970074 ) ) ;
#13959=CARTESIAN_POINT ( 'NONE',  ( 0.7495606340400177148, -0.1264236179284866091, 1.936515747977732405 ) ) ;
#13960=CARTESIAN_POINT ( 'NONE',  ( -1.033464566929134687, -0.06523048226347956391, 1.818405511811023167 ) ) ;
#13968=CARTESIAN_POINT ( 'NONE',  ( 0.9500414927467378812, -0.1787899950787401604, 0.6053149605761579677 ) ) ;
#13970=CARTESIAN_POINT ( 'NONE',  ( 0.8759842519685039353, 0.1787899950787401882, 0.1156496062454492185 ) ) ;
#13971=CARTESIAN_POINT ( 'NONE',  ( 1.033464566929133799, 0.000000000000000000, 1.968503936900346529 ) ) ;
#13972=CARTESIAN_POINT ( 'NONE',  ( 0.8759842519685039353, 0.1787899950787401882, 0.5831692912848189803 ) ) ;
#13974=CARTESIAN_POINT ( 'NONE',  ( -0.8019270111902717657, -0.1787899950787401604, 1.387795275536786610 ) ) ;
#13977=CARTESIAN_POINT ( 'NONE',  ( 1.054774247047244540, 0.07405724077823318263, 1.210629921206079818 ) ) ;
#13978=CARTESIAN_POINT ( 'NONE',  ( -0.8759842519685039353, -0.1574803149606299191, 0.7381889762704251234 ) ) ;
#13980=CARTESIAN_POINT ( 'NONE',  ( 1.054774247047244096, 0.000000000000000000, 1.833169291284818758 ) ) ;
#13981=CARTESIAN_POINT ( 'NONE',  ( -0.8019270111902717657, 0.1787899950787401604, 0.9005905511273389896 ) ) ;
#13984=CARTESIAN_POINT ( 'NONE',  ( 1.002407869896990045, -0.1264236179284866091, 0.3764763778989925203 ) ) ;
#13985=EDGE_CURVE ( 'NONE', #25810, #5177, #13523, .T. ) ;
#13987=CARTESIAN_POINT ( 'NONE',  ( -0.7495606340400177148, 0.1264236179284866091, 0.5487204723871811352 ) ) ;
#13988=CARTESIAN_POINT ( 'NONE',  ( 0.8107537697050253289, 0.1574803149606300301, 1.547736220364914983 ) ) ;
#13992=CARTESIAN_POINT ( 'NONE',  ( 0.8759842519685039353, -0.1787899950787401882, 0.8439960629383622681 ) ) ;
#13993=CARTESIAN_POINT ( 'NONE',  ( -0.8759842519685039353, -0.1787899950787401882, 1.783956692859621995 ) ) ;
#13996=CARTESIAN_POINT ( 'NONE',  ( -0.9873396505805591694, 0.1113553986120547346, 0.6446850393700788162 ) ) ;
#13999=ORIENTED_EDGE ( 'NONE', *, *, #14257, .F. ) ;
#14004=CARTESIAN_POINT ( 'NONE',  ( -0.9412147342319837628, -0.1574803149606297803, 1.213090551073575662 ) ) ;
#14006=CARTESIAN_POINT ( 'NONE',  ( 0.6971942568897637749, 2.189545951927499583E-17, 0.04183070860765386589 ) ) ;
#14010=ADVANCED_FACE ( 'NONE', ( #45864 ), #42720, .T. ) ;
#14011=CARTESIAN_POINT ( 'NONE',  ( -1.002407869896990045, -0.1264236179284866091, 0.4945866141194645849 ) ) ;
#14014=CARTESIAN_POINT ( 'NONE',  ( 1.002407869896990045, 0.1264236179284866091, 1.252460629867496067 ) ) ;
#14015=CARTESIAN_POINT ( 'NONE',  ( 1.054774247047244540, -0.07405724077823318263, 1.515748031442299526 ) ) ;
#14017=CARTESIAN_POINT ( 'NONE',  ( 0.9873396505805591694, 0.1113553986120547346, 1.707677165354330562 ) ) ;
#14020=CARTESIAN_POINT ( 'NONE',  ( 0.7185039370078739607, 1.928577636452523993E-17, 1.250000000000000000 ) ) ;
#14022=CARTESIAN_POINT ( 'NONE',  ( -0.7185039370078746268, -0.06523048226347956391, 1.754429133750741387 ) ) ;
#14024=CARTESIAN_POINT ( 'NONE',  ( 0.9500414927467378812, 0.1787899950787401604, 0.1082677164816695514 ) ) ;
#14025=CARTESIAN_POINT ( 'NONE',  ( 0.7022289528609824139, 0.03015070893300095256, 0.03937013461078139875 ) ) ;
#14026=CARTESIAN_POINT ( 'NONE',  ( 0.8759842519685039353, 0.1787899950787401882, 1.213090551127338435 ) ) ;
#14029=CARTESIAN_POINT ( 'NONE',  ( 1.033464566929134687, -0.06523048226347956391, 0.5487204723334181411 ) ) ;
#14030=ORIENTED_EDGE ( 'NONE', *, *, #11713, .F. ) ;
#14031=CARTESIAN_POINT ( 'NONE',  ( -0.7185039370078739607, 1.928577636452523993E-17, 1.131889763779527547 ) ) ;
#14032=CARTESIAN_POINT ( 'NONE',  ( 0.8685850549921918518, 0.1748108619810979925, 0.03936985974487598045 ) ) ;
#14033=CARTESIAN_POINT ( 'NONE',  ( -0.7185039370078746268, -0.06523048226347956391, 1.488681102362205300 ) ) ;
#14035=CARTESIAN_POINT ( 'NONE',  ( -0.8107537697050253289, 0.1574803149606300301, 0.3272637794200322636 ) ) ;
#14036=CARTESIAN_POINT ( 'NONE',  ( -0.8107537697050254399, -0.1574803149606297803, 1.532972440944882386 ) ) ;
#14037=CARTESIAN_POINT ( 'NONE',  ( 0.8019270111902717657, 0.1787899950787401604, 1.412401574749386990 ) ) ;
#14043=CARTESIAN_POINT ( 'NONE',  ( 0.7646288533564489232, -0.1113553986120547346, 1.284448818790110192 ) ) ;
#14045=CARTESIAN_POINT ( 'NONE',  ( 1.054774247047244540, -0.07405724077823318263, 0.5757874015210394658 ) ) ;
#14046=VERTEX_POINT ( 'NONE', #16880 ) ;
#14048=CARTESIAN_POINT ( 'NONE',  ( -0.8759842519685039353, -0.1787899950787401882, 1.080216535379306952 ) ) ;
#14049=CARTESIAN_POINT ( 'NONE',  ( -0.8107537697050234415, -0.1574803149606297803, 0.1943897637795276023 ) ) ;
#14050=ORIENTED_EDGE ( 'NONE', *, *, #17851, .T. ) ;
#14051=CARTESIAN_POINT ( 'NONE',  ( -0.6971942568897648851, -0.07405724077823297447, 1.107283464513165727 ) ) ;
#14052=CARTESIAN_POINT ( 'NONE',  ( -0.8759842519685039353, 0.1787899950787401882, 0.7849409448281259305 ) ) ;
#14053=CARTESIAN_POINT ( 'NONE',  ( -1.054774247047244096, 0.000000000000000000, 0.2239173227808822775 ) ) ;
#14056=ORIENTED_EDGE ( 'NONE', *, *, #44105, .F. ) ;
#14059=ORIENTED_EDGE ( 'NONE', *, *, #8941, .F. ) ;
#14060=ORIENTED_EDGE ( 'NONE', *, *, #35926, .F. ) ;
#14061=DIRECTION ( 'NONE',  ( 1.822029033848725028E-16, 0.000000000000000000, 1.000000000000000000 ) ) ;
#14062=CARTESIAN_POINT ( 'NONE',  ( 0.7185039370078739607, 1.928577636452523993E-17, 0.1870078740157480324 ) ) ;
#14063=CARTESIAN_POINT ( 'NONE',  ( -0.6971942568897637749, 2.189545951927499583E-17, 0.6323818897100157432 ) ) ;
#14066=CARTESIAN_POINT ( 'NONE',  ( -0.8759842519685039353, -0.1787899950787401882, 1.788877952702141672 ) ) ;
#14073=CARTESIAN_POINT ( 'NONE',  ( 0.9873396505805591694, -0.1113553986120547346, 0.6348425196850393526 ) ) ;
#14076=CARTESIAN_POINT ( 'NONE',  ( -0.9412147342319837628, -0.1574803149606297803, 1.370570866034205970 ) ) ;
#14078=CARTESIAN_POINT ( 'NONE',  ( 0.8759842519685039353, 0.1787899950787401882, 0.7455708660879684091 ) ) ;
#14083=CARTESIAN_POINT ( 'NONE',  ( 0.7185039370078746268, 0.06523048226347956391, 0.1747047243019218821 ) ) ;
#14084=CARTESIAN_POINT ( 'NONE',  ( 0.7646288533564489232, 0.1113553986120547346, 1.284448818897637956 ) ) ;
#14085=CARTESIAN_POINT ( 'NONE',  ( 0.8586096885590351890, -0.1731299321688159754, 1.987893929421542305 ) ) ;
#14087=FACE_OUTER_BOUND ( 'NONE', #5895, .T. ) ;
#14088=( BOUNDED_CURVE ( )  B_SPLINE_CURVE ( 2, ( #25473, #14673, #21862, #18260, #23, #40981, #30726, #44818, #4806 ),
 .UNSPECIFIED., .F., .T. ) 
 B_SPLINE_CURVE_WITH_KNOTS ( ( 3, 2, 2, 2, 3 ),
 ( 0.6400000000000000133, 0.6424999999999999600, 0.6450000000000000178, 0.6474999999999999645, 0.6500000000000000222 ),
 .UNSPECIFIED. ) 
 CURVE ( )  GEOMETRIC_REPRESENTATION_ITEM ( )  RATIONAL_B_SPLINE_CURVE ( ( 1.000000000000000000, 0.9238795325112869605, 1.000000000000000000, 0.9238795325112869605, 1.000000000000000000, 0.9238795325112869605, 1.000000000000000000, 0.9238795325112829637, 1.000000000000000000 ) ) 
 REPRESENTATION_ITEM ( '' )  ) ;
#14089=CARTESIAN_POINT ( 'NONE',  ( 0.8019270111902716547, 0.1787899950787401604, 0.6643700786863951935 ) ) ;
#14090=CARTESIAN_POINT ( 'NONE',  ( -1.054774247047244096, 0.000000000000000000, 1.990649606245448844 ) ) ;
#14093=CARTESIAN_POINT ( 'NONE',  ( -0.8107537697050254399, 0.1574803149606300301, 1.163877952755904666 ) ) ;
#14095=CARTESIAN_POINT ( 'NONE',  ( 0.6971942568897648851, -0.07405724077823297447, 0.9891732282926934960 ) ) ;
#14096=VECTOR ( 'NONE', #29284, 39.37007874015748143 ) ;
#14097=ORIENTED_EDGE ( 'NONE', *, *, #15392, .F. ) ;
#14098=CARTESIAN_POINT ( 'NONE',  ( 0.8759842519685039353, 0.000000000000000000, 1.990649606245448844 ) ) ;
#14099=FACE_OUTER_BOUND ( 'NONE', #26638, .T. ) ;
#14103=CARTESIAN_POINT ( 'NONE',  ( 0.9873396505805591694, 0.1113553986120547346, 1.235236220472440971 ) ) ;
#14104=CARTESIAN_POINT ( 'NONE',  ( -1.002407869896990045, -0.1264236179284866091, 0.05659448813521283234 ) ) ;
#14107=ORIENTED_EDGE ( 'NONE', *, *, #5880, .F. ) ;
#14109=CARTESIAN_POINT ( 'NONE',  ( -0.9500414927467377701, -0.1787899950787401604, 1.988188976324191781 ) ) ;
#14110=CARTESIAN_POINT ( 'NONE',  ( -1.054774247047244540, 0.07405724077823318263, 1.560039370024977057 ) ) ;
#14111=CARTESIAN_POINT ( 'NONE',  ( 0.8019270111902716547, 0.1787899950787401604, 0.9055118109698584439 ) ) ;
#14112=CARTESIAN_POINT ( 'NONE',  ( -0.6971942568897637749, 2.189545951927499583E-17, 1.104822834591905556 ) ) ;
#14113=CARTESIAN_POINT ( 'NONE',  ( -0.9500414927467378812, -0.1787899950787401604, 0.3740157479777325711 ) ) ;
#14114=( BOUNDED_CURVE ( )  B_SPLINE_CURVE ( 2, ( #291, #7485, #21398, #10402, #32690, #36280, #47038, #36023, #14230 ),
 .UNSPECIFIED., .F., .T. ) 
 B_SPLINE_CURVE_WITH_KNOTS ( ( 3, 2, 2, 2, 3 ),
 ( 0.8100000000000000533, 0.8125000000000000000, 0.8149999999999999467, 0.8175000000000000044, 0.8199999999999999512 ),
 .UNSPECIFIED. ) 
 CURVE ( )  GEOMETRIC_REPRESENTATION_ITEM ( )  RATIONAL_B_SPLINE_CURVE ( ( 1.000000000000000000, 0.9238795325112869605, 1.000000000000000000, 0.9238795325112869605, 1.000000000000000000, 0.9238795325112869605, 1.000000000000000000, 0.9238795325112829637, 1.000000000000000000 ) ) 
 REPRESENTATION_ITEM ( '' )  ) ;
#14116=CARTESIAN_POINT ( 'NONE',  ( -0.9500414927467378812, -0.1787899950787401604, 1.830708661363559253 ) ) ;
#14118=CARTESIAN_POINT ( 'NONE',  ( -0.7646288533564489232, 0.1113553986120547346, 1.953740157480315043 ) ) ;
#14123=DIRECTION ( 'NONE',  ( 0.000000000000000000, 0.000000000000000000, -1.000000000000000000 ) ) ;
#14125=CARTESIAN_POINT ( 'NONE',  ( -0.9500414927467378812, 0.1787899950787401604, 0.1476377952218271561 ) ) ;
#14126=ORIENTED_EDGE ( 'NONE', *, *, #45532, .T. ) ;
#14127=CARTESIAN_POINT ( 'NONE',  ( -0.8019270111902716547, -0.1787899950787401604, 1.235236220418678199 ) ) ;
#14131=EDGE_CURVE ( 'NONE', #31452, #8537, #26019, .T. ) ;
#14133=CARTESIAN_POINT ( 'NONE',  ( 1.033464566929133799, 0.000000000000000000, 0.3641732283464567121 ) ) ;
#14136=CARTESIAN_POINT ( 'NONE',  ( -0.7185039370078746268, -0.06523048226347956391, 0.9276574802074333270 ) ) ;
#14137=CARTESIAN_POINT ( 'NONE',  ( -0.8759842519685039353, -0.1574803149606299191, 0.7874015748031496509 ) ) ;
#14138=CARTESIAN_POINT ( 'NONE',  ( 0.8019270111902717657, 0.1787899950787401604, 0.4724409448281262636 ) ) ;
#14142=CARTESIAN_POINT ( 'NONE',  ( 0.9873396505805591694, -0.1113553986120547346, 1.845472440837354178 ) ) ;
#14146=CARTESIAN_POINT ( 'NONE',  ( 0.7646288533564489232, -0.1113553986120547346, 0.8612204724409449064 ) ) ;
#14147=CARTESIAN_POINT ( 'NONE',  ( -1.033464566929134687, 0.06523048226347956391, 1.232775590551180134 ) ) ;
#14148=CARTESIAN_POINT ( 'NONE',  ( 0.7646288533564489232, 0.1113553986120547346, 0.1722440943806619884 ) ) ;
#14151=CARTESIAN_POINT ( 'NONE',  ( 0.7646288533564489232, -0.1113553986120547346, 1.835629921152314825 ) ) ;
#14155=CARTESIAN_POINT ( 'NONE',  ( 1.033464566929133799, 0.000000000000000000, 0.9448818896562519720 ) ) ;
#14157=CARTESIAN_POINT ( 'NONE',  ( -0.8759842519685039353, -0.1787899950787401882, 0.4453740156942677664 ) ) ;
#14161=CARTESIAN_POINT ( 'NONE',  ( -0.7495606340400177148, 0.1264236179284866091, 1.577263779473795369 ) ) ;
#14163=CARTESIAN_POINT ( 'NONE',  ( 1.054774247047244540, -0.07405724077823318263, 1.560039370024977057 ) ) ;
#14165=CARTESIAN_POINT ( 'NONE',  ( -1.054774247047244096, 0.000000000000000000, 0.8144685038832440993 ) ) ;
#14166=CARTESIAN_POINT ( 'NONE',  ( 1.054774247047244096, 0.000000000000000000, 0.2239173227808822775 ) ) ;
#14168=CARTESIAN_POINT ( 'NONE',  ( -0.8019270111902716547, 0.1787899950787401604, 0.6249999999462366729 ) ) ;
#14170=CARTESIAN_POINT ( 'NONE',  ( 0.7185039370078739607, 1.928577636452523993E-17, 0.9251968502861732668 ) ) ;
#14173=CARTESIAN_POINT ( 'NONE',  ( -1.002407869896990045, -0.1264236179284866091, 1.439468503883244210 ) ) ;
#14176=CARTESIAN_POINT ( 'NONE',  ( -1.033464566929133799, 1.928577636452524610E-17, 2.869337061179095023E-17 ) ) ;
#14177=CARTESIAN_POINT ( 'NONE',  ( -0.9412147342319837628, -0.1574803149606297803, 0.4355314960629916299 ) ) ;
#14178=CARTESIAN_POINT ( 'NONE',  ( 0.6971942568897648851, 0.07405724077823318263, 1.500984251914741829 ) ) ;
#14180=CARTESIAN_POINT ( 'NONE',  ( -0.9873396505805591694, 0.1113553986120547346, 0.3592519683964098820 ) ) ;
#14185=ORIENTED_EDGE ( 'NONE', *, *, #11778, .F. ) ;
#14189=EDGE_CURVE ( 'NONE', #3331, #20293, #45564, .T. ) ;
#14192=CARTESIAN_POINT ( 'NONE',  ( 1.054774247047244096, 0.000000000000000000, 1.675688976324189117 ) ) ;
#14196=CARTESIAN_POINT ( 'NONE',  ( 1.033464566929134687, -0.06523048226347956391, 0.1550196849318430659 ) ) ;
#14198=CARTESIAN_POINT ( 'NONE',  ( 1.002407869896990045, -0.1264236179284866091, 0.6471456692375747721 ) ) ;
#14199=CARTESIAN_POINT ( 'NONE',  ( -0.6971942568897637749, 2.189545951927499583E-17, 1.031003936954110189 ) ) ;
#14201=CARTESIAN_POINT ( 'NONE',  ( 0.9873396505805591694, 0.1113553986120547346, 1.117125984251968518 ) ) ;
#14203=CARTESIAN_POINT ( 'NONE',  ( -0.8901995480705489072, -0.1743753279471531581, 1.988434009720291273 ) ) ;
#14207=CARTESIAN_POINT ( 'NONE',  ( 0.6971942568897637749, 2.189545951927499583E-17, 1.700295275536787498 ) ) ;
#14208=CARTESIAN_POINT ( 'NONE',  ( -0.7185039370078739607, 1.928577636452523993E-17, 0.7775590551181102983 ) ) ;
#14210=CARTESIAN_POINT ( 'NONE',  ( 0.7495606340400177148, -0.1264236179284866091, 0.4798228345919055560 ) ) ;
#14211=AXIS2_PLACEMENT_3D ( 'NONE', #43874, #10606, #25204 ) ;
#14212=VECTOR ( 'NONE', #37567, 39.37007874015748143 ) ;
#14213=ORIENTED_EDGE ( 'NONE', *, *, #34408, .T. ) ;
#14217=CARTESIAN_POINT ( 'NONE',  ( 1.054774247047244096, 0.000000000000000000, 0.6126968503399370380 ) ) ;
#14219=CARTESIAN_POINT ( 'NONE',  ( 0.7495606340400177148, 0.1264236179284866091, 0.1205708660879689087 ) ) ;
#14221=CARTESIAN_POINT ( 'NONE',  ( -0.8019270111902717657, -0.1787899950787401604, 1.584645669237574994 ) ) ;
#14223=CARTESIAN_POINT ( 'NONE',  ( 0.8019270111902717657, 0.1787899950787401604, 1.181102362150960428 ) ) ;
#14225=CARTESIAN_POINT ( 'NONE',  ( -0.7646288533564489232, -0.1113553986120547346, 0.6938976376877481478 ) ) ;
#14226=CARTESIAN_POINT ( 'NONE',  ( 0.9873396505805591694, -0.1113553986120547346, 1.500984251968503935 ) ) ;
#14227=CARTESIAN_POINT ( 'NONE',  ( 0.9500414927467378812, -0.1787899950787401604, 1.825787401521040243 ) ) ;
#14228=CARTESIAN_POINT ( 'NONE',  ( -0.9873396505805591694, -0.1113553986120547346, 0.5561023622047244208 ) ) ;
#14229=CARTESIAN_POINT ( 'NONE',  ( -1.054774247047244540, -0.07405724077823318263, 0.9251968503399374821 ) ) ;
#14230=CARTESIAN_POINT ( 'NONE',  ( -1.033464566929133799, 0.000000000000000000, 1.624015748031496287 ) ) ;
#14232=CARTESIAN_POINT ( 'NONE',  ( 0.6971942568897626646, 0.07405724077823318263, 0.3198818897100159098 ) ) ;
#14233=CARTESIAN_POINT ( 'NONE',  ( -0.8019270111902716547, -0.1787899950787401604, 0.2854330708123783977 ) ) ;
#14234=CARTESIAN_POINT ( 'NONE',  ( -1.002407869896990045, 0.1264236179284866091, 0.7357283464029290565 ) ) ;
#14235=CARTESIAN_POINT ( 'NONE',  ( 0.7185039370078739607, 1.928577636452523993E-17, 1.594488188868850242 ) ) ;
#14240=CARTESIAN_POINT ( 'NONE',  ( 0.6971942568897626646, 0.07405724077823318263, 0.8316929133320636325 ) ) ;
#14241=CARTESIAN_POINT ( 'NONE',  ( 1.054774247047244096, 0.000000000000000000, 1.050688976324189117 ) ) ;
#14242=CARTESIAN_POINT ( 'NONE',  ( -1.002407869896990045, 0.1264236179284866091, 1.916830708607653477 ) ) ;
#14243=CARTESIAN_POINT ( 'NONE',  ( 1.054774247047244096, 0.000000000000000000, 1.911909448765133801 ) ) ;
#14245=CARTESIAN_POINT ( 'NONE',  ( -1.033464566929133799, 0.000000000000000000, 0.6397637795275591399 ) ) ;
#14246=CARTESIAN_POINT ( 'NONE',  ( 0.9412147342319837628, -0.1574803149606297803, 1.606791338475149766 ) ) ;
#14255=CARTESIAN_POINT ( 'NONE',  ( 0.9500414927467378812, 0.1787899950787401604, 0.02952755900135462311 ) ) ;
#14257=EDGE_CURVE ( 'NONE', #38897, #11192, #10893, .T. ) ;
#14258=CARTESIAN_POINT ( 'NONE',  ( -1.054774247047244540, 0.07405724077823318263, 0.5413385826234012876 ) ) ;
#14260=CARTESIAN_POINT ( 'NONE',  ( -0.7128900651292061630, -0.03685103854907906956, 1.983952560205947568 ) ) ;
#14262=CARTESIAN_POINT ( 'NONE',  ( 0.6971942568897648851, 0.07405724077823318263, 1.264763779473795813 ) ) ;
#14263=CARTESIAN_POINT ( 'NONE',  ( 1.054774247047244540, 0.07405724077823318263, 1.520669291284818758 ) ) ;
#14264=VECTOR ( 'NONE', #33610, 39.37007874015748143 ) ;
#14266=CARTESIAN_POINT ( 'NONE',  ( 0.7185039370078739607, 1.928577636452523993E-17, 1.722440944881889813 ) ) ;
#14267=CYLINDRICAL_SURFACE ( 'NONE', #36587, 0.1574803149606299191 ) ;
#14269=CARTESIAN_POINT ( 'NONE',  ( -0.7646288533564489232, 0.1113553986120547346, 1.747047243986960652 ) ) ;
#14270=CARTESIAN_POINT ( 'NONE',  ( 0.8019270111902717657, -0.1787899950787401604, 0.2460629920722207375 ) ) ;
#14271=CARTESIAN_POINT ( 'NONE',  ( 0.7078001474992028363, 0.05966467328708899981, 0.03937007863263041613 ) ) ;
#14272=CARTESIAN_POINT ( 'NONE',  ( 0.8759842519685039353, 0.1787899950787401882, 1.134350393647023614 ) ) ;
#14273=CARTESIAN_POINT ( 'NONE',  ( -0.8759842519685039353, 0.000000000000000000, 0.000000000000000000 ) ) ;
#14274=CARTESIAN_POINT ( 'NONE',  ( -1.033464566929133799, 0.000000000000000000, 1.112204724409448842 ) ) ;
#14275=CARTESIAN_POINT ( 'NONE',  ( -1.002407869896990045, 0.1264236179284866091, 1.208169291284818980 ) ) ;
#14276=CARTESIAN_POINT ( 'NONE',  ( 1.033464566929134687, -0.06523048226347956391, 0.4699803148531029318 ) ) ;
#14278=CARTESIAN_POINT ( 'NONE',  ( 0.7646288533564489232, 0.1113553986120547346, 0.2608267716535432879 ) ) ;
#14279=CARTESIAN_POINT ( 'NONE',  ( 0.9873396505805591694, 0.1113553986120547346, 0.8316929132782993062 ) ) ;
#14280=CARTESIAN_POINT ( 'NONE',  ( -0.9873396505805591694, 0.1113553986120547346, 0.4379921258767252024 ) ) ;
#14282=CARTESIAN_POINT ( 'NONE',  ( 0.8019270111902717657, -0.1787899950787401604, 1.466535433017102763 ) ) ;
#14283=CARTESIAN_POINT ( 'NONE',  ( -0.9412147342319837628, -0.1574803149606297803, 1.144192913385827737 ) ) ;
#14291=CARTESIAN_POINT ( 'NONE',  ( 1.054774247047244540, -0.07405724077823318263, 0.6151574802611974313 ) ) ;
#14292=ORIENTED_EDGE ( 'NONE', *, *, #3669, .F. ) ;
#14293=CARTESIAN_POINT ( 'NONE',  ( -0.9500414927467377701, 0.1787899950787401604, 1.486220472387181912 ) ) ;
#14295=CARTESIAN_POINT ( 'NONE',  ( -0.6971942568897637749, 2.189545951927499583E-17, 1.149114173174582643 ) ) ;
#14296=CARTESIAN_POINT ( 'NONE',  ( -1.033464566929134687, -0.06523048226347956391, 0.2042322834645668717 ) ) ;
#14297=ORIENTED_EDGE ( 'NONE', *, *, #25666, .T. ) ;
#14298=ADVANCED_FACE ( 'NONE', ( #3199 ), #29132, .T. ) ;
#14299=CARTESIAN_POINT ( 'NONE',  ( -0.8019270111902716547, 0.1787899950787401604, 1.058070866087969186 ) ) ;
#14300=CARTESIAN_POINT ( 'NONE',  ( -0.6971942568897626646, -0.07405724077823297447, 0.7972440944344250102 ) ) ;
#14301=CARTESIAN_POINT ( 'NONE',  ( -0.6971942568897637749, 2.189545951927499583E-17, 0.2042322834108035723 ) ) ;
#14302=CYLINDRICAL_SURFACE ( 'NONE', #36415, 0.1574803149606299191 ) ;
#14303=CARTESIAN_POINT ( 'NONE',  ( 0.7185039370078746268, 0.06523048226347956391, 0.8046259841444418637 ) ) ;
#14305=ORIENTED_EDGE ( 'NONE', *, *, #41431, .T. ) ;
#14307=CARTESIAN_POINT ( 'NONE',  ( -0.7185039370078760701, -0.06523048226348075740, 0.8489173227271181732 ) ) ;
#14308=ORIENTED_EDGE ( 'NONE', *, *, #6070, .T. ) ;
#14311=CARTESIAN_POINT ( 'NONE',  ( 0.8759842519685039353, 0.1574803149606299191, 0.7677165354330708347 ) ) ;
#14312=DIRECTION ( 'NONE',  ( 1.000000000000000000, 0.000000000000000000, -1.822029033848725275E-16 ) ) ;
#14313=CARTESIAN_POINT ( 'NONE',  ( -1.054774247047244096, 0.000000000000000000, 0.7701771653005669016 ) ) ;
#14314=CARTESIAN_POINT ( 'NONE',  ( -0.8107537697050254399, -0.1574803149606297803, 0.5782480313885360879 ) ) ;
#14315=CARTESIAN_POINT ( 'NONE',  ( -0.6971942568897637749, 2.189545951927499583E-17, 1.739665354276945131 ) ) ;
#14316=ORIENTED_EDGE ( 'NONE', *, *, #16492, .T. ) ;
#14318=CARTESIAN_POINT ( 'NONE',  ( -0.8759842519685039353, 0.1787899950787401882, 0.07627952750529173875 ) ) ;
#14319=ORIENTED_EDGE ( 'NONE', *, *, #12078, .T. ) ;
#14321=CARTESIAN_POINT ( 'NONE',  ( -1.033464566929134687, 0.06523048226347956391, 1.380413385719244213 ) ) ;
#14322=CARTESIAN_POINT ( 'NONE',  ( 0.8759842519685039353, -0.1787899950787401882, 0.7258858267178898149 ) ) ;
#14325=EDGE_LOOP ( 'NONE', ( #5799, #15889, #28057, #12890 ) ) ;
#14327=CARTESIAN_POINT ( 'NONE',  ( 0.9412147342319837628, 0.1574803149606300301, 1.277066929133857442 ) ) ;
#14328=CARTESIAN_POINT ( 'NONE',  ( 0.8497971692482408912, -0.1717431688695388314, 1.987727230376266974 ) ) ;
#14330=CARTESIAN_POINT ( 'NONE',  ( 0.9412147342319837628, -0.1574803149606297803, 1.852854330708662012 ) ) ;
#14331=VECTOR ( 'NONE', #41159, 39.37007874015748143 ) ;
#14332=CARTESIAN_POINT ( 'NONE',  ( 0.6971942568897637749, 2.189545951927499583E-17, 0.7111220471903307860 ) ) ;
#14335=CARTESIAN_POINT ( 'NONE',  ( -0.9412147342319837628, -0.1574803149606297803, 0.3863188975302684347 ) ) ;
#14339=CARTESIAN_POINT ( 'NONE',  ( 0.6971942568897626646, -0.07405724077823297447, 0.9104330708123776761 ) ) ;
#14340=CARTESIAN_POINT ( 'NONE',  ( 0.7185039370078739607, 1.928577636452523993E-17, 0.3051181102362204856 ) ) ;
#14344=CARTESIAN_POINT ( 'NONE',  ( -0.6971942568897626646, 0.07405724077823318263, 0.1574803149068664809 ) ) ;
#14345=CARTESIAN_POINT ( 'NONE',  ( 0.6971942568897637749, 2.189545951927499583E-17, 1.936515747977732405 ) ) ;
#14348=CARTESIAN_POINT ( 'NONE',  ( -0.7495606340400177148, 0.1264236179284866091, 1.892224409395055096 ) ) ;
#14349=CARTESIAN_POINT ( 'NONE',  ( -0.8759842519685039353, 0.1787899950787401882, 1.606791338528913426 ) ) ;
#14351=CARTESIAN_POINT ( 'NONE',  ( -0.8019270111902716547, 0.1787899950787401604, 0.8218503936470251681 ) ) ;
#14352=CARTESIAN_POINT ( 'NONE',  ( -0.8019270111902717657, -0.1787899950787401604, 0.3690944881352128393 ) ) ;
#14355=CARTESIAN_POINT ( 'NONE',  ( -0.6971942568897637749, 2.189545951927499583E-17, 1.897145669237574772 ) ) ;
#14356=CARTESIAN_POINT ( 'NONE',  ( -0.9873396505805591694, 0.1113553986120547346, 1.904527559055118280 ) ) ;
#14361=DIRECTION ( 'NONE',  ( -1.000000000000000000, 0.000000000000000000, 0.000000000000000000 ) ) ;
#14366=CARTESIAN_POINT ( 'NONE',  ( -0.7495606340400177148, 0.1264236179284866091, 0.1550196849856066983 ) ) ;
#14368=CARTESIAN_POINT ( 'NONE',  ( -0.6971942568897648851, -0.07405724077823297447, 1.387795275536786610 ) ) ;
#14372=( BOUNDED_CURVE ( )  B_SPLINE_CURVE ( 2, ( #7528, #11381, #43951, #4627, #7765, #41043, #18328, #37005, #22145 ),
 .UNSPECIFIED., .F., .T. ) 
 B_SPLINE_CURVE_WITH_KNOTS ( ( 3, 2, 2, 2, 3 ),
 ( 0.9699999999999999734, 0.9725000000000000311, 0.9749999999999999778, 0.9775000000000000355, 0.9799999999999999822 ),
 .UNSPECIFIED. ) 
 CURVE ( )  GEOMETRIC_REPRESENTATION_ITEM ( )  RATIONAL_B_SPLINE_CURVE ( ( 1.000000000000000000, 0.9238795325112869605, 1.000000000000000000, 0.9238795325112869605, 1.000000000000000000, 0.9238795325112869605, 1.000000000000000000, 0.9238795325112869605, 1.000000000000000000 ) ) 
 REPRESENTATION_ITEM ( '' )  ) ;
#14373=CARTESIAN_POINT ( 'NONE',  ( 0.7646288533564489232, 0.1113553986120547346, 0.3395669291338583307 ) ) ;
#14375=CARTESIAN_POINT ( 'NONE',  ( -0.8107537697050253289, 0.1574803149606300301, 0.9965551180027087952 ) ) ;
#14377=CARTESIAN_POINT ( 'NONE',  ( 0.8759842519685039353, 0.1574803149606299191, 1.742125984144440975 ) ) ;
#14380=CARTESIAN_POINT ( 'NONE',  ( 0.8759842519685039353, -0.1574803149606299191, 0.7480314960629921295 ) ) ;
#14382=DIRECTION ( 'NONE',  ( 1.000000000000000000, 0.000000000000000000, -4.336808689942014778E-16 ) ) ;
#14385=CARTESIAN_POINT ( 'NONE',  ( 0.9873396505805591694, -0.1113553986120547346, 0.1525590550105832555 ) ) ;
#14390=CARTESIAN_POINT ( 'NONE',  ( -0.7185039370078746268, -0.06523048226347956391, 0.06151574792396910518 ) ) ;
#14393=CARTESIAN_POINT ( 'NONE',  ( 0.7646288533564489232, -0.1113553986120547346, 0.8907480313885355327 ) ) ;
#14395=CARTESIAN_POINT ( 'NONE',  ( -1.033464566929133799, 0.000000000000000000, 1.259842519577511810 ) ) ;
#14396=CARTESIAN_POINT ( 'NONE',  ( -0.6971942568897626646, 0.07405724077823318263, 0.3543307086076538659 ) ) ;
#14398=ORIENTED_EDGE ( 'NONE', *, *, #24160, .T. ) ;
#14399=ORIENTED_EDGE ( 'NONE', *, *, #8109, .T. ) ;
#14400=CARTESIAN_POINT ( 'NONE',  ( -0.9500414927467378812, -0.1787899950787401604, 1.673228346402929834 ) ) ;
#14401=VERTEX_POINT ( 'NONE', #44155 ) ;
#14403=CARTESIAN_POINT ( 'NONE',  ( -1.002407869896990045, -0.1264236179284866091, 0.7701771653005669016 ) ) ;
#14404=CARTESIAN_POINT ( 'NONE',  ( 1.054774247047244540, 0.07405724077823318263, 0.1476377952218269618 ) ) ;
#14405=CARTESIAN_POINT ( 'NONE',  ( -1.033464566929133799, 1.928577636452524610E-17, 2.869337061179095023E-17 ) ) ;
#14406=CARTESIAN_POINT ( 'NONE',  ( 1.054774247047244540, 0.07405724077823318263, 0.6988188975840318173 ) ) ;
#14407=CARTESIAN_POINT ( 'NONE',  ( -0.9500414927467377701, 0.1787899950787401604, 0.7381889763241898939 ) ) ;
#14412=CARTESIAN_POINT ( 'NONE',  ( -0.7185039370078746268, 0.06523048226347956391, 1.867618110128693720 ) ) ;
#14413=ORIENTED_EDGE ( 'NONE', *, *, #7127, .T. ) ;
#14415=CARTESIAN_POINT ( 'NONE',  ( -0.9873396505805591694, 0.1113553986120547346, 0.4872047244094488416 ) ) ;
#14416=CARTESIAN_POINT ( 'NONE',  ( 0.8759842519685039353, -0.1787899950787401882, 1.473917322780881722 ) ) ;
#14417=CARTESIAN_POINT ( 'NONE',  ( -1.033464566929134687, -0.06523048226347956391, 1.582185039370079149 ) ) ;
#14423=CARTESIAN_POINT ( 'NONE',  ( -1.033464566929133799, 0.000000000000000000, 1.151574803149606474 ) ) ;
#14425=CARTESIAN_POINT ( 'NONE',  ( 1.033464566929133799, 0.000000000000000000, 1.033464566929133799 ) ) ;
#14427=CARTESIAN_POINT ( 'NONE',  ( 0.6971942568897637749, 2.189545951927499583E-17, 1.734744094434425232 ) ) ;
#14428=CARTESIAN_POINT ( 'NONE',  ( 1.054774247047244540, 0.07405724077823318263, 0.3001968503399373711 ) ) ;
#14433=CARTESIAN_POINT ( 'NONE',  ( 0.8759842519685039353, 0.1787899950787401882, 0.5437992125446614589 ) ) ;
#14434=EDGE_CURVE ( 'NONE', #47261, #14468, #20817, .T. ) ;
#14435=CARTESIAN_POINT ( 'NONE',  ( -0.8019270111902716547, 0.1787899950787401604, 0.9448818897100165204 ) ) ;
#14438=DIRECTION ( 'NONE',  ( 0.000000000000000000, 0.000000000000000000, -1.000000000000000000 ) ) ;
#14439=CARTESIAN_POINT ( 'NONE',  ( 0.9500414927467378812, -0.1787899950787401604, 1.673228346402929834 ) ) ;
#14442=VERTEX_POINT ( 'NONE', #40316 ) ;
#14446=CARTESIAN_POINT ( 'NONE',  ( 0.9412147342319837628, 0.1574803149606300301, 0.4798228345381422288 ) ) ;
#14447=CARTESIAN_POINT ( 'NONE',  ( 0.7495606340400177148, 0.1264236179284866091, 0.6274606298674959559 ) ) ;
#14449=CARTESIAN_POINT ( 'NONE',  ( 0.9500414927467378812, -0.1787899950787401604, 0.05905511805647267048 ) ) ;
#14451=CARTESIAN_POINT ( 'NONE',  ( -0.9500414927467378812, 0.1787899950787401604, 1.525590551127340433 ) ) ;
#14453=CARTESIAN_POINT ( 'NONE',  ( -1.054774247047244096, 0.000000000000000000, 1.208169291284818980 ) ) ;
#14455=CARTESIAN_POINT ( 'NONE',  ( 1.054774247047244540, 0.07405724077823318263, 1.092519684985605810 ) ) ;
#14456=CARTESIAN_POINT ( 'NONE',  ( 1.054774247047244540, 0.07405724077823318263, 1.756889763725764553 ) ) ;
#14457=CARTESIAN_POINT ( 'NONE',  ( -0.9500414927467378812, -0.1787899950787401604, 0.9596456692375764375 ) ) ;
#14460=CARTESIAN_POINT ( 'NONE',  ( 0.6971942568897648851, -0.07405724077823297447, 0.3641732282926931630 ) ) ;
#14461=CARTESIAN_POINT ( 'NONE',  ( -0.6971942568897626646, -0.07405724077823297447, 0.2017716534895435399 ) ) ;
#14463=CARTESIAN_POINT ( 'NONE',  ( -0.7495606340400177148, 0.1264236179284866091, 0.6668307086076534773 ) ) ;
#14464=CARTESIAN_POINT ( 'NONE',  ( 1.033464566929134687, -0.06523048226347956391, 1.572342519577513142 ) ) ;
#14466=EDGE_CURVE ( 'NONE', #43835, #40552, #33728, .T. ) ;
#14468=VERTEX_POINT ( 'NONE', #19231 ) ;
#14469=ORIENTED_EDGE ( 'NONE', *, *, #41793, .F. ) ;
#14470=CARTESIAN_POINT ( 'NONE',  ( 0.9500414927467378812, 0.1787899950787401604, 0.8612204723871809131 ) ) ;
#14471=CARTESIAN_POINT ( 'NONE',  ( 0.6971942568897648851, 0.07405724077823318263, 1.107283464513165727 ) ) ;
#14472=CARTESIAN_POINT ( 'NONE',  ( -0.6971942568897648851, 0.07405724077823318263, 1.811023621993480548 ) ) ;
#14473=EDGE_CURVE ( 'NONE', #38318, #39969, #3023, .T. ) ;
#14474=CARTESIAN_POINT ( 'NONE',  ( 0.6971942568897648851, 0.07405724077823318263, 1.968503936954110189 ) ) ;
#14483=CARTESIAN_POINT ( 'NONE',  ( 0.8019270111902717657, 0.1787899950787401604, 0.03444881884387430981 ) ) ;
#14486=VECTOR ( 'NONE', #1008, 39.37007874015748143 ) ;
#14487=CARTESIAN_POINT ( 'NONE',  ( -0.9500414927467377701, -0.1787899950787401604, 0.5314960629383620461 ) ) ;
#14488=CARTESIAN_POINT ( 'NONE',  ( -0.9873396505805591694, 0.1113553986120547346, 0.6742125983176693316 ) ) ;
#14490=CARTESIAN_POINT ( 'NONE',  ( -0.7108390435763994875, 0.01258011831628214061, 1.983038464472898221 ) ) ;
#14491=CARTESIAN_POINT ( 'NONE',  ( -0.9873396505805591694, 0.1113553986120547346, 1.195866141732283561 ) ) ;
#14492=CARTESIAN_POINT ( 'NONE',  ( 0.8019270111902717657, -0.1787899950787401604, 1.235236220418678199 ) ) ;
#14493=CARTESIAN_POINT ( 'NONE',  ( 0.6971942568897648851, 0.07405724077823318263, 1.692913385773008539 ) ) ;
#14494=CARTESIAN_POINT ( 'NONE',  ( -0.7185039370078739607, 1.928577636452523993E-17, 0.6102362203649134287 ) ) ;
#14497=CARTESIAN_POINT ( 'NONE',  ( -0.7185039370078746268, 0.06523048226347956391, 1.788877952648378233 ) ) ;
#14498=CARTESIAN_POINT ( 'NONE',  ( 0.8759842519685039353, -0.1787899950787401882, 0.1304133857730082613 ) ) ;
#14499=CARTESIAN_POINT ( 'NONE',  ( 0.7039992537011210416, -0.02173256458483645986, 0.03937460100240990774 ) ) ;
#14500=CARTESIAN_POINT ( 'NONE',  ( 0.8759842519685039353, -0.1787899950787401882, 1.232775590497417362 ) ) ;
#14501=CARTESIAN_POINT ( 'NONE',  ( -0.7185039370078746268, -0.06523048226347956391, 0.5339566928058587791 ) ) ;
#14502=CYLINDRICAL_SURFACE ( 'NONE', #5171, 0.1574803149606299191 ) ;
#14503=CARTESIAN_POINT ( 'NONE',  ( -0.8019270111902717657, -0.1787899950787401604, 1.190944881836001112 ) ) ;
#14504=CARTESIAN_POINT ( 'NONE',  ( 0.7185039370078739607, 1.928577636452523993E-17, 0.5314960628845992741 ) ) ;
#14505=VERTEX_POINT ( 'NONE', #4353 ) ;
#14507=CARTESIAN_POINT ( 'NONE',  ( 0.9303600321982549159, 0.1621629823367503609, 0.03937005601395735660 ) ) ;
#14508=CARTESIAN_POINT ( 'NONE',  ( 0.8107537697050253289, 0.1574803149606300301, 0.2583661417322835052 ) ) ;
#14510=CARTESIAN_POINT ( 'NONE',  ( -0.9412147342319837628, -0.1574803149606297803, 0.4256889762704256230 ) ) ;
#14513=CARTESIAN_POINT ( 'NONE',  ( 1.054774247047244096, 0.000000000000000000, 1.400098425143086800 ) ) ;
#14514=CARTESIAN_POINT ( 'NONE',  ( -0.7185039370078746268, -0.06523048226347956391, 1.764271653543307616 ) ) ;
#14515=CARTESIAN_POINT ( 'NONE',  ( -1.033464566929136907, -0.06523048226347749612, 1.385334645669292541 ) ) ;
#14519=FACE_OUTER_BOUND ( 'NONE', #45402, .T. ) ;
#14521=VECTOR ( 'NONE', #15394, 39.37007874015748143 ) ;
#14525=CARTESIAN_POINT ( 'NONE',  ( 0.7495606340400177148, -0.1264236179284866091, 0.6422244093950550958 ) ) ;
#14528=CARTESIAN_POINT ( 'NONE',  ( -0.8019270111902717657, 0.1787899950787401604, 1.181102362150960428 ) ) ;
#14529=VERTEX_POINT ( 'NONE', #22830 ) ;
#14532=CARTESIAN_POINT ( 'NONE',  ( -0.8019270111902717657, 0.1787899950787401604, 0.8267716534895444003 ) ) ;
#14534=CARTESIAN_POINT ( 'NONE',  ( -0.8759842519685039353, -0.1574803149606299191, 0.3543307086614173040 ) ) ;
#14538=AXIS2_PLACEMENT_3D ( 'NONE', #44250, #28561, #7600 ) ;
#14541=CARTESIAN_POINT ( 'NONE',  ( -0.9412147342319837628, 0.1574803149606300301, 0.5585629920184573827 ) ) ;
#14542=CARTESIAN_POINT ( 'NONE',  ( -1.054774247047244540, 0.07405724077823318263, 0.7332677164816707727 ) ) ;
#14545=CARTESIAN_POINT ( 'NONE',  ( -0.8019270111902716547, 0.1787899950787401604, 0.1181102361667090567 ) ) ;
#14546=CARTESIAN_POINT ( 'NONE',  ( 0.8107537697050253289, 0.1574803149606300301, 0.6914370078740167402 ) ) ;
#14549=CARTESIAN_POINT ( 'NONE',  ( -0.7646288533564489232, -0.1113553986120547346, 1.441929133750740277 ) ) ;
#14550=CARTESIAN_POINT ( 'NONE',  ( 0.6971942568897626646, 0.07405724077823318263, 0.7135826771115916234 ) ) ;
#14551=CARTESIAN_POINT ( 'NONE',  ( 0.8019270111902716547, 0.1787899950787401604, 1.333661417269071281 ) ) ;
#14553=CYLINDRICAL_SURFACE ( 'NONE', #16204, 0.1574803149606299191 ) ;
#14555=CARTESIAN_POINT ( 'NONE',  ( 1.033464566929134687, -0.06523048226347956391, 1.464074803149607140 ) ) ;
#14556=CARTESIAN_POINT ( 'NONE',  ( 0.7949805117774454422, -0.1517228856934477454, 1.986644361401757930 ) ) ;
#14557=CARTESIAN_POINT ( 'NONE',  ( 1.033464566929133799, 0.000000000000000000, 1.574803149498771537 ) ) ;
#14558=AXIS2_PLACEMENT_3D ( 'NONE', #44094, #44789, #238 ) ;
#14559=CARTESIAN_POINT ( 'NONE',  ( 1.033464566929134687, -0.06523048226347956391, 1.729822834538142784 ) ) ;
#14561=CARTESIAN_POINT ( 'NONE',  ( 1.002407869896990045, -0.1264236179284866091, 0.7258858267178898149 ) ) ;
#14563=EDGE_CURVE ( 'NONE', #2430, #31278, #30071, .T. ) ;
#14564=CARTESIAN_POINT ( 'NONE',  ( 1.033464566929134687, 0.06523048226347956391, 1.547736220472440305 ) ) ;
#14566=ADVANCED_FACE ( 'NONE', ( #12301 ), #7936, .F. ) ;
#14569=CARTESIAN_POINT ( 'NONE',  ( 0.7495606340400177148, -0.1264236179284866091, 0.9128937007336377363 ) ) ;
#14570=CARTESIAN_POINT ( 'NONE',  ( 0.7185039370078739607, 1.928577636452523993E-17, 1.368110236220472675 ) ) ;
#14573=CARTESIAN_POINT ( 'NONE',  ( -0.7495606340400177148, -0.1264236179284866091, 0.04675196845017354913 ) ) ;
#14577=CARTESIAN_POINT ( 'NONE',  ( -1.054774247047244540, 0.07405724077823318263, 1.638779527505292988 ) ) ;
#14579=CARTESIAN_POINT ( 'NONE',  ( -0.6971942568897626646, 0.07405724077823318263, 0.4379921259304882519 ) ) ;
#14583=CARTESIAN_POINT ( 'NONE',  ( 1.033464566929134687, 0.06523048226347956391, 0.2878937007874017850 ) ) ;
#14588=FACE_OUTER_BOUND ( 'NONE', #18894, .T. ) ;
#14592=CARTESIAN_POINT ( 'NONE',  ( -1.054774247047244540, 0.07405724077823318263, 0.3395669290800945039 ) ) ;
#14595=CARTESIAN_POINT ( 'NONE',  ( -0.8019270111902716547, 0.1787899950787401604, 1.338582677111590069 ) ) ;
#14599=FILL_AREA_STYLE_COLOUR ( '', #11051 ) ;
#14601=CARTESIAN_POINT ( 'NONE',  ( 0.7185039370078746268, 0.06523048226347956391, 0.3420275590551182798 ) ) ;
#14603=CARTESIAN_POINT ( 'NONE',  ( -0.8107537697050253289, 0.1574803149606300301, 0.9178149605223947516 ) ) ;
#14605=CARTESIAN_POINT ( 'NONE',  ( 0.7185039370078746268, 0.06523048226347956391, 1.828248031388536310 ) ) ;
#14606=ADVANCED_FACE ( 'NONE', ( #7392 ), #46835, .F. ) ;
#14608=CARTESIAN_POINT ( 'NONE',  ( 0.8107537697050253289, 0.1574803149606300301, 0.8489173228346468258 ) ) ;
#14609=CARTESIAN_POINT ( 'NONE',  ( 0.7646288533564489232, 0.1113553986120547346, 1.363188976377952999 ) ) ;
#14612=CARTESIAN_POINT ( 'NONE',  ( 1.044119406988188947, 0.000000000000000000, 1.984498031469181134 ) ) ;
#14613=CARTESIAN_POINT ( 'NONE',  ( 0.7185039370078746268, -0.06523048226347956391, 1.528051181102361378 ) ) ;
#14623=CARTESIAN_POINT ( 'NONE',  ( -0.7646288533564489232, 0.1113553986120547346, 0.05413385816018952829 ) ) ;
#14626=CARTESIAN_POINT ( 'NONE',  ( 0.8759842519685039353, -0.1574803149606299191, 1.013779527451527551 ) ) ;
#14628=CARTESIAN_POINT ( 'NONE',  ( -0.8759842519685039353, 0.1787899950787401882, 0.3863188975840318173 ) ) ;
#14630=CARTESIAN_POINT ( 'NONE',  ( -1.054774247047244540, -0.07405724077823318263, 1.599409448765135133 ) ) ;
#14632=CARTESIAN_POINT ( 'NONE',  ( 1.002407869896990045, 0.1264236179284866091, 1.724901574749385880 ) ) ;
#14634=CARTESIAN_POINT ( 'NONE',  ( -0.7495606340400177148, -0.1264236179284866091, 0.7997047243556849594 ) ) ;
#14635=CARTESIAN_POINT ( 'NONE',  ( 1.054774247047244540, 0.07405724077823318263, 0.3051181101824569919 ) ) ;
#14636=CARTESIAN_POINT ( 'NONE',  ( 0.8759842519685039353, 0.000000000000000000, 4.498031496062992574 ) ) ;
#14637=CARTESIAN_POINT ( 'NONE',  ( 0.6971942568897637749, 2.189545951927499583E-17, 0.7554133857730077617 ) ) ;
#14638=CARTESIAN_POINT ( 'NONE',  ( -0.8019270111902716547, -0.1787899950787401604, 0.7578740156942688211 ) ) ;
#14641=CARTESIAN_POINT ( 'NONE',  ( -0.8019270111902717657, -0.1787899950787401604, 1.510826771599780294 ) ) ;
#14642=CARTESIAN_POINT ( 'NONE',  ( -0.8759842519685039353, 0.1574803149606299191, 1.938976377845228249 ) ) ;
#14644=CARTESIAN_POINT ( 'NONE',  ( 1.033464566929133799, 1.928577636452524610E-17, 4.498031496062992574 ) ) ;
#14645=CARTESIAN_POINT ( 'NONE',  ( 0.8019270111902716547, -0.1787899950787401604, 1.510826771599780294 ) ) ;
#14647=FACE_OUTER_BOUND ( 'NONE', #4504, .T. ) ;
#14649=( BOUNDED_CURVE ( )  B_SPLINE_CURVE ( 2, ( #36310, #325, #3465, #40331, #22140, #36766, #3926, #14976, #33910 ),
 .UNSPECIFIED., .F., .F. ) 
 B_SPLINE_CURVE_WITH_KNOTS ( ( 3, 2, 2, 2, 3 ),
 ( 0.7199999999999999734, 0.7225000000000000311, 0.7249999999999999778, 0.7275000000000000355, 0.7299999999999999822 ),
 .UNSPECIFIED. ) 
 CURVE ( )  GEOMETRIC_REPRESENTATION_ITEM ( )  RATIONAL_B_SPLINE_CURVE ( ( 1.000000000000000000, 0.9238795325112869605, 1.000000000000000000, 0.9238795325112869605, 1.000000000000000000, 0.9238795325112869605, 1.000000000000000000, 0.9238795325112869605, 1.000000000000000000 ) ) 
 REPRESENTATION_ITEM ( '' )  ) ;
#14660=CARTESIAN_POINT ( 'NONE',  ( 0.8019270111902717657, 0.1787899950787401604, 0.2706692912848194243 ) ) ;
#14666=EDGE_CURVE ( 'NONE', #7011, #5868, #24655, .T. ) ;
#14667=CARTESIAN_POINT ( 'NONE',  ( 0.6971942568897626646, 0.07405724077823318263, 0.6692913385289144257 ) ) ;
#14668=( BOUNDED_CURVE ( )  B_SPLINE_CURVE ( 2, ( #11946, #1126, #26567, #44033, #29944, #15785, #29488, #30414, #4013 ),
 .UNSPECIFIED., .F., .T. ) 
 B_SPLINE_CURVE_WITH_KNOTS ( ( 3, 2, 2, 2, 3 ),
 ( 0.1400000000000000133, 0.1424999999999999878, 0.1449999999999999900, 0.1474999999999999922, 0.1499999999999999944 ),
 .UNSPECIFIED. ) 
 CURVE ( )  GEOMETRIC_REPRESENTATION_ITEM ( )  RATIONAL_B_SPLINE_CURVE ( ( 1.000000000000000000, 0.9238795325112869605, 1.000000000000000000, 0.9238795325112869605, 1.000000000000000000, 0.9238795325112869605, 1.000000000000000000, 0.9238795325112869605, 1.000000000000000000 ) ) 
 REPRESENTATION_ITEM ( '' )  ) ;
#14669=EDGE_CURVE ( 'NONE', #20105, #3237, #12867, .T. ) ;
#14670=CARTESIAN_POINT ( 'NONE',  ( -0.8075642815980649258, 0.1651804164989427171, 0.03937007874015843040 ) ) ;
#14673=CARTESIAN_POINT ( 'NONE',  ( -1.033464566929134687, 0.06523048226347956391, 1.301673228238930502 ) ) ;
#14674=CARTESIAN_POINT ( 'NONE',  ( 0.6971942568897637749, 2.189545951927499583E-17, 1.621555118056472455 ) ) ;
#14677=CARTESIAN_POINT ( 'NONE',  ( 0.7495606340400177148, 0.1264236179284866091, 0.5093503936470236138 ) ) ;
#14678=ADVANCED_FACE ( 'NONE', ( #31861 ), #46440, .T. ) ;
#14681=CARTESIAN_POINT ( 'NONE',  ( -0.8019270111902717657, 0.1787899950787401604, 0.4330708660879683536 ) ) ;
#14682=CARTESIAN_POINT ( 'NONE',  ( -1.054774247047244096, 0.000000000000000000, 1.990649606245448844 ) ) ;
#14684=CARTESIAN_POINT ( 'NONE',  ( 0.8019270111902717657, 0.1787899950787401604, 0.07874015742655145200 ) ) ;
#14686=CARTESIAN_POINT ( 'NONE',  ( -1.002407869896990045, 0.1264236179284866091, 1.641240157426551161 ) ) ;
#14688=CARTESIAN_POINT ( 'NONE',  ( -0.7495606340400177148, -0.1264236179284866091, 1.114665354276944909 ) ) ;
#14689=CARTESIAN_POINT ( 'NONE',  ( 0.8107537697050254399, -0.1574803149606297803, 1.021161417322834497 ) ) ;
#14690=CARTESIAN_POINT ( 'NONE',  ( 0.7495606340400177148, 0.1264236179284866091, 1.183562992072220599 ) ) ;
#14692=CARTESIAN_POINT ( 'NONE',  ( 0.6971942568897648851, -0.07405724077823297447, 1.815944881835999558 ) ) ;
#14693=CARTESIAN_POINT ( 'NONE',  ( -1.033464566929133799, 0.000000000000000000, 0.6397637795275591399 ) ) ;
#14694=CARTESIAN_POINT ( 'NONE',  ( -0.6971942568897626646, 0.07405724077823318263, 0.9842519684501742638 ) ) ;
#14697=CARTESIAN_POINT ( 'NONE',  ( 1.002407869896990045, 0.1264236179284866091, 0.2682086613635594752 ) ) ;
#14698=CARTESIAN_POINT ( 'NONE',  ( -1.002407869896990045, -0.1264236179284866091, 0.2928149605761578567 ) ) ;
#14699=CARTESIAN_POINT ( 'NONE',  ( -0.8019270111902717657, 0.1787899950787401604, 0.7037401574265510495 ) ) ;
#14700=CARTESIAN_POINT ( 'NONE',  ( 0.9412147342319837628, 0.1574803149606300301, 1.700295275483023172 ) ) ;
#14702=CARTESIAN_POINT ( 'NONE',  ( 1.054774247047244096, 0.000000000000000000, 0.7357283464029290565 ) ) ;
#14703=CARTESIAN_POINT ( 'NONE',  ( 1.054774247047244096, 0.000000000000000000, 1.011318897584031484 ) ) ;
#14704=CARTESIAN_POINT ( 'NONE',  ( -0.8759842519685039353, 0.1787899950787401882, 1.843011810969858333 ) ) ;
#14705=ORIENTED_EDGE ( 'NONE', *, *, #17009, .F. ) ;
#14706=CARTESIAN_POINT ( 'NONE',  ( 1.054774247047244096, 0.000000000000000000, 1.951279527505291433 ) ) ;
#14707=CARTESIAN_POINT ( 'NONE',  ( -0.8107537697050234415, -0.1574803149606297803, 0.1943897637795276023 ) ) ;
#14711=CARTESIAN_POINT ( 'NONE',  ( -0.7185039370078739607, 1.928577636452523993E-17, 1.948818897530267602 ) ) ;
#14712=ORIENTED_EDGE ( 'NONE', *, *, #18645, .F. ) ;
#14713=CARTESIAN_POINT ( 'NONE',  ( 1.002407869896990045, -0.1264236179284866091, 1.237696850339937038 ) ) ;
#14718=CARTESIAN_POINT ( 'NONE',  ( 1.002407869896990045, 0.1264236179284866091, 1.483759842465921075 ) ) ;
#14719=CARTESIAN_POINT ( 'NONE',  ( 1.033464566929133799, 0.000000000000000000, 1.978346456692913646 ) ) ;
#14723=EDGE_CURVE ( 'NONE', #22721, #6712, #42212, .T. ) ;
#14724=CARTESIAN_POINT ( 'NONE',  ( -0.7495606340400177148, -0.1264236179284866091, 0.5634842519147401640 ) ) ;
#14728=VECTOR ( 'NONE', #7586, 39.37007874015748143 ) ;
#14729=CARTESIAN_POINT ( 'NONE',  ( 0.8019270111902717657, -0.1787899950787401604, 1.274606299158834277 ) ) ;
#14730=CARTESIAN_POINT ( 'NONE',  ( 0.6971942568897637749, 2.189545951927499583E-17, 1.734744094434425232 ) ) ;
#14732=EDGE_CURVE ( 'NONE', #16491, #13799, #9214, .T. ) ;
#14736=CARTESIAN_POINT ( 'NONE',  ( 1.033464566929133799, 0.000000000000000000, 0.1574803148531029595 ) ) ;
#14737=LINE ( 'NONE', #29408, #26275 ) ;
#14738=CARTESIAN_POINT ( 'NONE',  ( 0.7017793196824928526, -0.004420539869511170769, 0.03936223978338515561 ) ) ;
#14739=CARTESIAN_POINT ( 'NONE',  ( 0.9500414927467377701, -0.1787899950787401604, 1.274606299158834277 ) ) ;
#14740=CARTESIAN_POINT ( 'NONE',  ( 1.033464566929133799, 0.000000000000000000, 0.07874015737278799998 ) ) ;
#14741=CARTESIAN_POINT ( 'NONE',  ( 0.9873396505805591694, -0.1113553986120547346, 1.225393700787401619 ) ) ;
#14742=CARTESIAN_POINT ( 'NONE',  ( -0.7185039370078741827, 0.06523048226347841205, 0.9621062991050717272 ) ) ;
#14743=CARTESIAN_POINT ( 'NONE',  ( -1.002407869896990045, 0.1264236179284866091, 1.247539370024976391 ) ) ;
#14744=CARTESIAN_POINT ( 'NONE',  ( 0.7646288533564489232, -0.1113553986120547346, 0.6938976376877481478 ) ) ;
#14746=CARTESIAN_POINT ( 'NONE',  ( 0.9363197608943458761, 0.1595975290736699748, 0.03936943479083548914 ) ) ;
#14747=CARTESIAN_POINT ( 'NONE',  ( 0.8107537697050234415, -0.1574803149606297803, 0.2731299212598424231 ) ) ;
#14750=CARTESIAN_POINT ( 'NONE',  ( 1.054774247047244540, 0.07405724077823318263, 1.441929133804504604 ) ) ;
#14753=CARTESIAN_POINT ( 'NONE',  ( 1.033464566929133799, 0.000000000000000000, 1.190944881889763884 ) ) ;
#14756=CARTESIAN_POINT ( 'NONE',  ( -1.033464566929133799, 1.928577636452524610E-17, 2.869337061179095023E-17 ) ) ;
#14761=CARTESIAN_POINT ( 'NONE',  ( 0.9500414927467378812, -0.1787899950787401604, 0.5708661416785201226 ) ) ;
#14763=CARTESIAN_POINT ( 'NONE',  ( -0.6971942568897637749, 2.189545951927499583E-17, 1.459153543253322693 ) ) ;
#14765=CARTESIAN_POINT ( 'NONE',  ( -0.8759842519685039353, 0.1787899950787401882, 1.060531496009228247 ) ) ;
#14769=CARTESIAN_POINT ( 'NONE',  ( -0.9412147342319837628, -0.1574803149606297803, 1.970964566929134021 ) ) ;
#14770=CARTESIAN_POINT ( 'NONE',  ( -0.6971942568897626646, 0.07405724077823318263, 0.7923228345919055560 ) ) ;
#14772=CARTESIAN_POINT ( 'NONE',  ( -0.8759842519685039353, -0.1787899950787401882, 0.2140748030958428971 ) ) ;
#14774=LINE ( 'NONE', #29438, #9875 ) ;
#14779=VERTEX_POINT ( 'NONE', #40185 ) ;
#14781=CARTESIAN_POINT ( 'NONE',  ( -1.002407869896990045, -0.1264236179284866091, 0.7652559054580472253 ) ) ;
#14782=CARTESIAN_POINT ( 'NONE',  ( 0.7185039370078739607, 0.000000000000000000, 4.498031496062992574 ) ) ;
#14783=ORIENTED_EDGE ( 'NONE', *, *, #45990, .F. ) ;
#14784=CARTESIAN_POINT ( 'NONE',  ( -0.8759842519685039353, -0.1787899950787401882, 1.867618110182456714 ) ) ;
#14785=( BOUNDED_CURVE ( )  B_SPLINE_CURVE ( 2, ( #5599, #31030, #20207, #19739, #16404, #12817, #34375, #2003, #41991 ),
 .UNSPECIFIED., .F., .F. ) 
 B_SPLINE_CURVE_WITH_KNOTS ( ( 3, 2, 2, 2, 3 ),
 ( 0.1000000000000000056, 0.1024999999999999939, 0.1049999999999999961, 0.1074999999999999983, 0.1100000000000000006 ),
 .UNSPECIFIED. ) 
 CURVE ( )  GEOMETRIC_REPRESENTATION_ITEM ( )  RATIONAL_B_SPLINE_CURVE ( ( 1.000000000000000000, 0.9238795325112869605, 1.000000000000000000, 0.9238795325112869605, 1.000000000000000000, 0.9238795325112869605, 1.000000000000000000, 0.9238795325112869605, 1.000000000000000000 ) ) 
 REPRESENTATION_ITEM ( '' )  ) ;
#14788=EDGE_CURVE ( 'NONE', #34008, #38222, #29428, .T. ) ;
#14789=CARTESIAN_POINT ( 'NONE',  ( -0.6971942568897626646, 0.07405724077823318263, 0.04429133852891373180 ) ) ;
#14790=CARTESIAN_POINT ( 'NONE',  ( 0.8759842519685039353, 0.1574803149606299191, 0.6496062992125984925 ) ) ;
#14792=FACE_OUTER_BOUND ( 'NONE', #5492, .T. ) ;
#14793=CARTESIAN_POINT ( 'NONE',  ( -1.033464566929134687, 0.06523048226347956391, 1.537893700679874298 ) ) ;
#14794=CARTESIAN_POINT ( 'NONE',  ( 0.6971942568897626646, 0.07405724077823318263, 0.7529527558517473684 ) ) ;
#14797=CYLINDRICAL_SURFACE ( 'NONE', #22301, 0.1574803149606299191 ) ;
#14798=EDGE_CURVE ( 'NONE', #26252, #24091, #36620, .T. ) ;
#14799=CARTESIAN_POINT ( 'NONE',  ( 0.9873396505805591694, 0.1113553986120547346, 1.353346456692913424 ) ) ;
#14801=CARTESIAN_POINT ( 'NONE',  ( 0.9373987626270909868, -0.1654231709439420162, 1.989299970918606331 ) ) ;
#14802=CARTESIAN_POINT ( 'NONE',  ( 1.033464566929133799, 0.000000000000000000, 0.5216535433070865757 ) ) ;
#14803=CARTESIAN_POINT ( 'NONE',  ( 1.033464566929133799, 0.000000000000000000, 1.732283464459401623 ) ) ;
#14805=CARTESIAN_POINT ( 'NONE',  ( -1.002407869896990045, -0.1264236179284866091, 1.985728346402929168 ) ) ;
#14807=LINE ( 'NONE', #46663, #2322 ) ;
#14809=CARTESIAN_POINT ( 'NONE',  ( 0.7495606340400177148, 0.1264236179284866091, 1.021161417269070837 ) ) ;
#14813=VERTEX_POINT ( 'NONE', #3779 ) ;
#14815=CARTESIAN_POINT ( 'NONE',  ( -0.8759842519685039353, 0.1787899950787401882, 0.1500984251430870220 ) ) ;
#14816=ORIENTED_EDGE ( 'NONE', *, *, #36498, .F. ) ;
#14818=CARTESIAN_POINT ( 'NONE',  ( -1.054774247047244540, -0.07405724077823318263, 1.712598425143087688 ) ) ;
#14819=CARTESIAN_POINT ( 'NONE',  ( -0.6971942568897637749, 2.189545951927499583E-17, 0.3223425196312759144 ) ) ;
#14820=CARTESIAN_POINT ( 'NONE',  ( -0.8759842519685039353, -0.1574803149606299191, 0.1082677164279060994 ) ) ;
#14821=CARTESIAN_POINT ( 'NONE',  ( 0.9412147342319837628, 0.1574803149606300301, 0.4010826770578274081 ) ) ;
#14822=CARTESIAN_POINT ( 'NONE',  ( 0.8759842519685039353, 0.000000000000000000, 4.498031496062992574 ) ) ;
#14823=CARTESIAN_POINT ( 'NONE',  ( 1.054774247047244096, 0.000000000000000000, 0.06151574797773248782 ) ) ;
#14830=CARTESIAN_POINT ( 'NONE',  ( -0.7495606340400177148, 0.1264236179284866091, 0.2731299212060791515 ) ) ;
#14832=AXIS2_PLACEMENT_3D ( 'NONE', #3861, #14902, #7927 ) ;
#14833=EDGE_CURVE ( 'NONE', #39969, #46991, #17736, .T. ) ;
#14834=CARTESIAN_POINT ( 'NONE',  ( -0.7495606340400177148, 0.1264236179284866091, 1.341043307032850462 ) ) ;
#14835=ORIENTED_EDGE ( 'NONE', *, *, #24269, .T. ) ;
#14838=ADVANCED_FACE ( 'NONE', ( #44718 ), #9697, .T. ) ;
#14839=DIRECTION ( 'NONE',  ( 0.000000000000000000, 0.000000000000000000, -1.000000000000000000 ) ) ;
#14841=CARTESIAN_POINT ( 'NONE',  ( 0.8107537697050253289, -0.1574803149606297803, 0.3912401574803148763 ) ) ;
#14844=CARTESIAN_POINT ( 'NONE',  ( -0.8107537697050253289, 0.1574803149606300301, 1.075295275483024504 ) ) ;
#14845=CARTESIAN_POINT ( 'NONE',  ( 0.6971942568897626646, 0.07405724077823318263, 0.4379921259304882519 ) ) ;
#14848=ORIENTED_EDGE ( 'NONE', *, *, #19906, .T. ) ;
#14849=CARTESIAN_POINT ( 'NONE',  ( 1.033464566929134687, -0.06523048226347956391, 1.926673228238929170 ) ) ;
#14851=VECTOR ( 'NONE', #11977, 39.37007874015748143 ) ;
#14852=CARTESIAN_POINT ( 'NONE',  ( -0.9412147342319837628, 0.1574803149606300301, 1.424704724301921521 ) ) ;
#14853=CARTESIAN_POINT ( 'NONE',  ( 0.9412147342319837628, 0.1574803149606300301, 0.9227362204724416372 ) ) ;
#14856=CYLINDRICAL_SURFACE ( 'NONE', #26356, 0.1574803149606299191 ) ;
#14857=CARTESIAN_POINT ( 'NONE',  ( -1.033464566929133799, 1.928577636452524610E-17, 2.869337061179095023E-17 ) ) ;
#14862=CARTESIAN_POINT ( 'NONE',  ( 1.033464566929133799, 0.000000000000000000, 1.387795275590551158 ) ) ;
#14867=CARTESIAN_POINT ( 'NONE',  ( 0.8107537697050253289, 0.1574803149606300301, 0.9965551180027087952 ) ) ;
#14869=ORIENTED_EDGE ( 'NONE', *, *, #10423, .F. ) ;
#14872=VECTOR ( 'NONE', #46942, 39.37007874015748143 ) ;
#14873=CARTESIAN_POINT ( 'NONE',  ( -0.7495606340400177148, -0.1264236179284866091, 1.547736220418677089 ) ) ;
#14874=CARTESIAN_POINT ( 'NONE',  ( 1.054774247047244096, 0.000000000000000000, 1.759350393647023614 ) ) ;
#14875=CARTESIAN_POINT ( 'NONE',  ( -0.6971942568897637749, 2.189545951927499583E-17, 0.8735236219934803259 ) ) ;
#14877=CARTESIAN_POINT ( 'NONE',  ( 1.002407869896990045, -0.1264236179284866091, 0.2583661416785200671 ) ) ;
#14878=CARTESIAN_POINT ( 'NONE',  ( -0.7185039370078739607, 1.928577636452523993E-17, 0.2657480314960630197 ) ) ;
#14879=CARTESIAN_POINT ( 'NONE',  ( -0.8759842519685039353, -0.1787899950787401882, 1.232775590497417362 ) ) ;
#14880=CARTESIAN_POINT ( 'NONE',  ( -0.8019270111902716547, 0.1787899950787401604, 0.7037401574265510495 ) ) ;
#14883=CARTESIAN_POINT ( 'NONE',  ( -0.6971942568897648851, -0.07405724077823297447, 1.505905511757261284 ) ) ;
#14884=CARTESIAN_POINT ( 'NONE',  ( -0.7185039370078739607, 1.928577636452523993E-17, 1.870078740049952559 ) ) ;
#14885=ORIENTED_EDGE ( 'NONE', *, *, #33957, .T. ) ;
#14886=CARTESIAN_POINT ( 'NONE',  ( -0.7646288533564489232, -0.1113553986120547346, 1.569881889763779625 ) ) ;
#14888=CARTESIAN_POINT ( 'NONE',  ( 0.9500414927467377701, -0.1787899950787401604, 1.476377952702141449 ) ) ;
#14889=CARTESIAN_POINT ( 'NONE',  ( -0.9412147342319837628, -0.1574803149606297803, 1.577263779527559917 ) ) ;
#14891=VERTEX_POINT ( 'NONE', #27464 ) ;
#14896=ORIENTED_EDGE ( 'NONE', *, *, #11013, .F. ) ;
#14899=CARTESIAN_POINT ( 'NONE',  ( -0.7185039370078739607, 1.928577636452523993E-17, 1.131889763779527547 ) ) ;
#14902=DIRECTION ( 'NONE',  ( 0.000000000000000000, 0.000000000000000000, 1.000000000000000000 ) ) ;
#14904=CARTESIAN_POINT ( 'NONE',  ( 0.7495606340400177148, 0.1264236179284866091, 1.808562992072220377 ) ) ;
#14909=CARTESIAN_POINT ( 'NONE',  ( 1.054774247047244540, 0.07405724077823318263, 0.7332677164816707727 ) ) ;
#14912=CARTESIAN_POINT ( 'NONE',  ( 1.033464566929134687, 0.06523048226347956391, 0.9473425195775121432 ) ) ;
#14913=CARTESIAN_POINT ( 'NONE',  ( 1.054774247047244540, 0.07405724077823318263, 1.801181102308441861 ) ) ;
#14916=CARTESIAN_POINT ( 'NONE',  ( 0.6971942568897648851, -0.07405724077823297447, 0.5167322834108035723 ) ) ;
#14918=CARTESIAN_POINT ( 'NONE',  ( 0.8759842519685039353, 0.1574803149606299191, 0.09842519685039370636 ) ) ;
#14922=CARTESIAN_POINT ( 'NONE',  ( -0.7495606340400177148, -0.1264236179284866091, 0.4847440944344252323 ) ) ;
#14925=CARTESIAN_POINT ( 'NONE',  ( 0.8019270111902717657, -0.1787899950787401604, 0.2509842519147403861 ) ) ;
#14927=CARTESIAN_POINT ( 'NONE',  ( -0.6971942568897648851, -0.07405724077823297447, 1.540354330654897685 ) ) ;
#14930=CARTESIAN_POINT ( 'NONE',  ( -0.7495606340400177148, 0.1264236179284866091, 1.222933070812378009 ) ) ;
#14931=CARTESIAN_POINT ( 'NONE',  ( -1.033464566929133799, 0.000000000000000000, 0.8759842519685039353 ) ) ;
#14932=CARTESIAN_POINT ( 'NONE',  ( 0.8759842519685039353, 0.1787899950787401882, 1.257381889710015743 ) ) ;
#14935=CARTESIAN_POINT ( 'NONE',  ( 0.7495606340400177148, -0.1264236179284866091, 0.05167322829269323931 ) ) ;
#14936=CARTESIAN_POINT ( 'NONE',  ( -0.9500414927467378812, -0.1787899950787401604, 0.9990157479777320715 ) ) ;
#14939=CARTESIAN_POINT ( 'NONE',  ( 0.6971942568897637749, 2.189545951927499583E-17, 0.2436023621509610382 ) ) ;
#14940=CARTESIAN_POINT ( 'NONE',  ( -1.054774247047244540, -0.07405724077823318263, 0.2165354330171024577 ) ) ;
#14941=CARTESIAN_POINT ( 'NONE',  ( -0.8019270111902717657, -0.1787899950787401604, 0.6791338582139527791 ) ) ;
#14942=CARTESIAN_POINT ( 'NONE',  ( 1.033464566929133799, 0.000000000000000000, 1.692913385719244213 ) ) ;
#14946=CARTESIAN_POINT ( 'NONE',  ( 0.8759842519685039353, 0.1787899950787401882, 1.099901574749385880 ) ) ;
#14947=CARTESIAN_POINT ( 'NONE',  ( -1.002407869896990045, 0.1264236179284866091, 1.838090551127338657 ) ) ;
#14948=ORIENTED_EDGE ( 'NONE', *, *, #18881, .T. ) ;
#14950=CARTESIAN_POINT ( 'NONE',  ( 0.9500414927467378812, 0.1787899950787401604, 1.958661417269071947 ) ) ;
#14959=CARTESIAN_POINT ( 'NONE',  ( 0.8759842519685039353, -0.1787899950787401882, 1.272145669237574772 ) ) ;
#14960=VECTOR ( 'NONE', #26368, 39.37007874015748143 ) ;
#14964=( BOUNDED_CURVE ( )  B_SPLINE_CURVE ( 2, ( #21287, #3069, #17699, #6904, #21526, #36164, #3318, #47172, #29003 ),
 .UNSPECIFIED., .F., .F. ) 
 B_SPLINE_CURVE_WITH_KNOTS ( ( 3, 2, 2, 2, 3 ),
 ( 0.7399999999999999911, 0.7425000000000000488, 0.7449999999999999956, 0.7475000000000000533, 0.7500000000000000000 ),
 .UNSPECIFIED. ) 
 CURVE ( )  GEOMETRIC_REPRESENTATION_ITEM ( )  RATIONAL_B_SPLINE_CURVE ( ( 1.000000000000000000, 0.9238795325112869605, 1.000000000000000000, 0.9238795325112869605, 1.000000000000000000, 0.9238795325112869605, 1.000000000000000000, 0.9238795325112869605, 1.000000000000000000 ) ) 
 REPRESENTATION_ITEM ( '' )  ) ;
#14965=CARTESIAN_POINT ( 'NONE',  ( 0.6971942568897626646, -0.07405724077823297447, 0.2017716534895435399 ) ) ;
#14967=VECTOR ( 'NONE', #39723, 39.37007874015748143 ) ;
#14972=CARTESIAN_POINT ( 'NONE',  ( -1.054774247047244540, 0.07405724077823318263, 0.4625984251430869665 ) ) ;
#14975=CARTESIAN_POINT ( 'NONE',  ( -0.7115070055584155062, -0.02845177017965971542, 1.983791088683289017 ) ) ;
#14976=CARTESIAN_POINT ( 'NONE',  ( 0.7185039370078746268, 0.06523048226347956391, 1.444389763779527991 ) ) ;
#14977=CARTESIAN_POINT ( 'NONE',  ( 0.6971942568897648851, -0.07405724077823297447, 1.427165354276944687 ) ) ;
#14978=CARTESIAN_POINT ( 'NONE',  ( 0.8759842519685039353, -0.1787899950787401882, 1.626476377898992132 ) ) ;
#14979=CARTESIAN_POINT ( 'NONE',  ( 0.7185039370078739607, 1.928577636452523993E-17, 1.515748031388535200 ) ) ;
#14984=CARTESIAN_POINT ( 'NONE',  ( 1.033464566929134687, -0.06523048226347956391, 0.5487204723334181411 ) ) ;
#14985=CARTESIAN_POINT ( 'NONE',  ( 0.8759842519685039353, -0.1787899950787401882, 0.2878937007336381804 ) ) ;
#14986=CARTESIAN_POINT ( 'NONE',  ( 0.7233020866430639462, -0.07417860294387490505, 0.03937367257947978899 ) ) ;
#14987=CARTESIAN_POINT ( 'NONE',  ( 0.8759842519685039353, -0.1787899950787401882, 1.272145669237574772 ) ) ;
#14988=DIRECTION ( 'NONE',  ( 1.822029033848725028E-16, 0.000000000000000000, 1.000000000000000000 ) ) ;
#14990=CARTESIAN_POINT ( 'NONE',  ( -0.7185039370078746268, 0.06523048226347956391, 0.7750984251968497940 ) ) ;
#14991=CARTESIAN_POINT ( 'NONE',  ( -0.8019270111902717657, -0.1787899950787401604, 1.269685039316314601 ) ) ;
#14992=CARTESIAN_POINT ( 'NONE',  ( 0.7185039370078746268, 0.06523048226347956391, 0.6865157479239701876 ) ) ;
#14994=LINE ( 'NONE', #15465, #39844 ) ;
#14995=CARTESIAN_POINT ( 'NONE',  ( 0.9412147342319837628, 0.1574803149606300301, 0.6865157480314956207 ) ) ;
#14996=ORIENTED_EDGE ( 'NONE', *, *, #2487, .F. ) ;
#14997=CARTESIAN_POINT ( 'NONE',  ( 1.033464566929134687, 0.06523048226347956391, 0.2878937007874017295 ) ) ;
#15000=CARTESIAN_POINT ( 'NONE',  ( -0.9873396505805591694, 0.1113553986120547346, 1.589566929133858331 ) ) ;
#15001=CARTESIAN_POINT ( 'NONE',  ( 0.6971942568897648851, -0.07405724077823297447, 1.579724409395055318 ) ) ;
#15003=CARTESIAN_POINT ( 'NONE',  ( -0.9412147342319837628, -0.1574803149606297803, 1.094980314853103653 ) ) ;
#15005=CARTESIAN_POINT ( 'NONE',  ( -0.9412147342319837628, -0.1574803149606297803, 0.1205708661417322358 ) ) ;
#15008=FACE_OUTER_BOUND ( 'NONE', #25978, .T. ) ;
#15010=CARTESIAN_POINT ( 'NONE',  ( 1.054774247047244540, 0.07405724077823318263, 0.5807086613635594752 ) ) ;
#15012=CARTESIAN_POINT ( 'NONE',  ( 0.9500414927467377701, -0.1787899950787401604, 0.8070866141194653620 ) ) ;
#15013=CARTESIAN_POINT ( 'NONE',  ( -1.002407869896990045, 0.1264236179284866091, 1.444389763725763665 ) ) ;
#15015=CARTESIAN_POINT ( 'NONE',  ( -1.054774247047244096, 0.000000000000000000, 1.247539370024976391 ) ) ;
#15020=CARTESIAN_POINT ( 'NONE',  ( -0.9500414927467378812, -0.1787899950787401604, 0.2559055117572600624 ) ) ;
#15023=EDGE_LOOP ( 'NONE', ( #12941, #41951, #4898, #37019 ) ) ;
#15024=CARTESIAN_POINT ( 'NONE',  ( 0.7521669337840648506, 0.1290358749737920141, 0.03937007777616036847 ) ) ;
#15026=ADVANCED_FACE ( 'NONE', ( #4831 ), #22587, .T. ) ;
#15027=CARTESIAN_POINT ( 'NONE',  ( -0.7646288533564489232, -0.1113553986120547346, 0.2608267715460161340 ) ) ;
#15028=CARTESIAN_POINT ( 'NONE',  ( -0.8019270111902717657, -0.1787899950787401604, 0.7578740156942689321 ) ) ;
#15031=CARTESIAN_POINT ( 'NONE',  ( -0.6971942568897648851, -0.07405724077823297447, 1.820866141678520789 ) ) ;
#15034=CARTESIAN_POINT ( 'NONE',  ( -0.7646288533564489232, 0.1113553986120547346, 0.9301181102362204856 ) ) ;
#15037=CARTESIAN_POINT ( 'NONE',  ( -0.7185039370078746268, 0.06523048226347956391, 1.473917322727117840 ) ) ;
#15038=CARTESIAN_POINT ( 'NONE',  ( 1.054774247047244096, 0.000000000000000000, 0.6963582676627716461 ) ) ;
#15040=CARTESIAN_POINT ( 'NONE',  ( 1.033464566929133799, 0.000000000000000000, 1.348425196850393748 ) ) ;
#15041=CARTESIAN_POINT ( 'NONE',  ( 0.7291528398006205114, 0.07205607647759287859, 1.981831347760247164 ) ) ;
#15042=CARTESIAN_POINT ( 'NONE',  ( 0.9873396505805591694, -0.1113553986120547346, 1.569881889656251861 ) ) ;
#15044=EDGE_CURVE ( 'NONE', #32278, #10690, #34290, .T. ) ;
#15045=CARTESIAN_POINT ( 'NONE',  ( 0.8759842519685039353, -0.1787899950787401882, 0.8390748030958424808 ) ) ;
#15049=CARTESIAN_POINT ( 'NONE',  ( 1.033464566929133799, 0.000000000000000000, 1.072834645669291431 ) ) ;
#15051=CARTESIAN_POINT ( 'NONE',  ( 0.9500414927467378812, 0.1787899950787401604, 1.092519684985605810 ) ) ;
#15058=CARTESIAN_POINT ( 'NONE',  ( -0.8759842519685039353, -0.1787899950787401882, 0.2091535432533232486 ) ) ;
#15060=CARTESIAN_POINT ( 'NONE',  ( 0.9412147342319837628, 0.1574803149606300301, 0.3321850393700786497 ) ) ;
#15062=CARTESIAN_POINT ( 'NONE',  ( -0.7495606340400177148, -0.1264236179284866091, 1.660925196796630088 ) ) ;
#15063=CARTESIAN_POINT ( 'NONE',  ( -0.6971942568897648851, -0.07405724077823297447, 0.9104330708123777871 ) ) ;
#15064=CARTESIAN_POINT ( 'NONE',  ( -0.8759842519685039353, -0.1787899950787401882, 0.4109251967966299213 ) ) ;
#15066=CARTESIAN_POINT ( 'NONE',  ( -0.9873396505805591694, -0.1113553986120547346, 0.1624015748031496231 ) ) ;
#15076=CARTESIAN_POINT ( 'NONE',  ( -0.8019270111902717657, 0.1787899950787401604, 0.3494094487651343006 ) ) ;
#15077=( BOUNDED_CURVE ( )  B_SPLINE_CURVE ( 2, ( #15916, #19485, #30543, #41493, #23335, #3922, #9662, #12796, #20662 ),
 .UNSPECIFIED., .F., .F. ) 
 B_SPLINE_CURVE_WITH_KNOTS ( ( 3, 2, 2, 2, 3 ),
 ( 0.6300000000000000044, 0.6324999999999999512, 0.6350000000000000089, 0.6374999999999999556, 0.6400000000000000133 ),
 .UNSPECIFIED. ) 
 CURVE ( )  GEOMETRIC_REPRESENTATION_ITEM ( )  RATIONAL_B_SPLINE_CURVE ( ( 1.000000000000000000, 0.9238795325112899581, 1.000000000000000000, 0.9238795325112869605, 1.000000000000000000, 0.9238795325112869605, 1.000000000000000000, 0.9238795325112869605, 1.000000000000000000 ) ) 
 REPRESENTATION_ITEM ( '' )  ) ;
#15078=CARTESIAN_POINT ( 'NONE',  ( 1.033464566929134687, 0.06523048226347956391, 0.7997047244094481755 ) ) ;
#15080=CARTESIAN_POINT ( 'NONE',  ( -1.054774247047244540, -0.07405724077823318263, 1.402559055064346749 ) ) ;
#15086=CARTESIAN_POINT ( 'NONE',  ( 0.7185039370078746268, 0.06523048226347956391, 0.4207677165354331561 ) ) ;
#15088=CARTESIAN_POINT ( 'NONE',  ( -0.9412147342319837628, -0.1574803149606297803, 1.055610236112945799 ) ) ;
#15089=CARTESIAN_POINT ( 'NONE',  ( 0.7495606340400177148, 0.1264236179284866091, 0.3961614172690708924 ) ) ;
#15090=CARTESIAN_POINT ( 'NONE',  ( -0.7646288533564489232, -0.1113553986120547346, 1.687992125984252079 ) ) ;
#15092=CARTESIAN_POINT ( 'NONE',  ( 0.7646288533564489232, 0.1113553986120547346, 1.904527558947590515 ) ) ;
#15095=CARTESIAN_POINT ( 'NONE',  ( 0.9412147342319837628, -0.1574803149606297803, 0.04183070866141735261 ) ) ;
#15096=CARTESIAN_POINT ( 'NONE',  ( 1.033464566929133799, 0.000000000000000000, 0.9547244094488189781 ) ) ;
#15098=( BOUNDED_CURVE ( )  B_SPLINE_CURVE ( 2, ( #12156, #18614, #7831, #44944, #4697, #33275, #7594, #29927, #4220 ),
 .UNSPECIFIED., .F., .T. ) 
 B_SPLINE_CURVE_WITH_KNOTS ( ( 3, 2, 2, 2, 3 ),
 ( 0.4600000000000000200, 0.4625000000000000222, 0.4650000000000000244, 0.4675000000000000266, 0.4699999999999999734 ),
 .UNSPECIFIED. ) 
 CURVE ( )  GEOMETRIC_REPRESENTATION_ITEM ( )  RATIONAL_B_SPLINE_CURVE ( ( 1.000000000000000000, 0.9238795325112869605, 1.000000000000000000, 0.9238795325112869605, 1.000000000000000000, 0.9238795325112869605, 1.000000000000000000, 0.9238795325112849621, 1.000000000000000000 ) ) 
 REPRESENTATION_ITEM ( '' )  ) ;
#15099=EDGE_CURVE ( 'NONE', #44104, #31513, #27585, .T. ) ;
#15100=CARTESIAN_POINT ( 'NONE',  ( -0.7185039370078739607, 0.000000000000000000, 2.007874015640504162 ) ) ;
#15109=CARTESIAN_POINT ( 'NONE',  ( 1.033464566929134687, 0.06523048226347956391, 1.065452755797984041 ) ) ;
#15114=CARTESIAN_POINT ( 'NONE',  ( -0.8019270111902717657, -0.1787899950787401604, 1.589566929080094448 ) ) ;
#15116=CARTESIAN_POINT ( 'NONE',  ( 0.8759842519685039353, -0.1787899950787401882, 1.670767716481669440 ) ) ;
#15117=CARTESIAN_POINT ( 'NONE',  ( -1.002407869896990045, 0.1264236179284866091, 0.8193897637257637756 ) ) ;
#15118=CARTESIAN_POINT ( 'NONE',  ( -1.033464566929133799, 0.000000000000000000, 0.7480314959554645871 ) ) ;
#15119=CARTESIAN_POINT ( 'NONE',  ( 0.8019270111902717657, 0.1787899950787401604, 0.3149606298674962890 ) ) ;
#15120=CARTESIAN_POINT ( 'NONE',  ( -1.033464566929133799, 0.000000000000000000, 1.496062992018456494 ) ) ;
#15121=CARTESIAN_POINT ( 'NONE',  ( -0.9500414927467377701, 0.1787899950787401604, 1.171259842465921741 ) ) ;
#15122=CARTESIAN_POINT ( 'NONE',  ( -0.8019270111902716547, -0.1787899950787401604, 0.7972440944344248992 ) ) ;
#15126=CARTESIAN_POINT ( 'NONE',  ( -0.9500414927467378812, 0.1787899950787401604, 1.648622047190331230 ) ) ;
#15127=CARTESIAN_POINT ( 'NONE',  ( -0.9412147342319837628, -0.1574803149606297803, 1.882381889656251861 ) ) ;
#15129=CARTESIAN_POINT ( 'NONE',  ( -0.7185039370078739607, 1.928577636452523993E-17, 1.604330708661417360 ) ) ;
#15130=CARTESIAN_POINT ( 'NONE',  ( 1.033464566929133355, 0.06523048226348168721, 1.626476377952755570 ) ) ;
#15131=CARTESIAN_POINT ( 'NONE',  ( 1.002407869896990045, -0.1264236179284866091, 1.478838582623401399 ) ) ;
#15133=DIRECTION ( 'NONE',  ( 0.000000000000000000, 0.000000000000000000, -1.000000000000000000 ) ) ;
#15137=EDGE_LOOP ( 'NONE', ( #13819, #20209, #9040, #1 ) ) ;
#15142=CARTESIAN_POINT ( 'NONE',  ( 1.002407869896990045, -0.1264236179284866091, 1.749507873961984483 ) ) ;
#15143=CARTESIAN_POINT ( 'NONE',  ( 0.8107537697050253289, 0.1574803149606300301, 0.2977362204724410821 ) ) ;
#15145=CARTESIAN_POINT ( 'NONE',  ( 0.7185039370078739607, 1.928577636452523993E-17, 0.1082677165354330728 ) ) ;
#15148=CARTESIAN_POINT ( 'NONE',  ( 0.8759842519685039353, -0.1787899950787401882, 0.7603346456155274380 ) ) ;
#15151=CARTESIAN_POINT ( 'NONE',  ( 0.9412147342319837628, -0.1574803149606297803, 1.134350393593259732 ) ) ;
#15153=CARTESIAN_POINT ( 'NONE',  ( -0.8989048142471400826, -0.1738438585959865001, 1.988589590799940687 ) ) ;
#15154=FACE_OUTER_BOUND ( 'NONE', #1074, .T. ) ;
#15155=CARTESIAN_POINT ( 'NONE',  ( 0.9500414927467378812, -0.1787899950787401604, 1.830708661363559253 ) ) ;
#15158=CARTESIAN_POINT ( 'NONE',  ( 0.9873396505805591694, 0.1113553986120547346, 0.05413385826771653642 ) ) ;
#15163=CARTESIAN_POINT ( 'NONE',  ( 0.6971942568897626646, -0.07405724077823297447, 0.2066929133320631329 ) ) ;
#15166=CARTESIAN_POINT ( 'NONE',  ( -1.054774247047244540, 0.07405724077823318263, 1.520669291284818758 ) ) ;
#15168=CARTESIAN_POINT ( 'NONE',  ( -1.054774247047244096, 0.000000000000000000, 1.168799212544661348 ) ) ;
#15171=CARTESIAN_POINT ( 'NONE',  ( 1.002407869896990045, -0.1264236179284866091, 1.321358267662771757 ) ) ;
#15173=CARTESIAN_POINT ( 'NONE',  ( 0.8019270111902717657, 0.1787899950787401604, 1.924212598371433325 ) ) ;
#15174=CARTESIAN_POINT ( 'NONE',  ( -0.7495606340400177148, 0.1264236179284866091, 1.099901574749385880 ) ) ;
#15176=CARTESIAN_POINT ( 'NONE',  ( -1.033464566929133799, 0.000000000000000000, 0.3641732283464567121 ) ) ;
#15177=CARTESIAN_POINT ( 'NONE',  ( 0.8759842519685039353, -0.1787899950787401882, 0.4502952755367874427 ) ) ;
#15178=CARTESIAN_POINT ( 'NONE',  ( -0.6971942568897626646, -0.07405724077823297447, 0.3198818897100159098 ) ) ;
#15179=CARTESIAN_POINT ( 'NONE',  ( -1.002407869896990045, -0.1264236179284866091, 0.7258858267178898149 ) ) ;
#15180=CARTESIAN_POINT ( 'NONE',  ( 1.033464566929133799, 0.000000000000000000, 1.732283464459401623 ) ) ;
#15181=ORIENTED_EDGE ( 'NONE', *, *, #14833, .F. ) ;
#15183=CARTESIAN_POINT ( 'NONE',  ( -1.033464566929134687, 0.06523048226347956391, 0.1304133858267717272 ) ) ;
#15184=CARTESIAN_POINT ( 'NONE',  ( 0.8019270111902716547, 0.1787899950787401604, 1.062992125930488418 ) ) ;
#15187=CARTESIAN_POINT ( 'NONE',  ( 0.7185039370078739607, 1.928577636452523993E-17, 0.3051181102362204856 ) ) ;
#15191=CARTESIAN_POINT ( 'NONE',  ( -1.033464566929133799, 0.000000000000000000, 1.692913385719244213 ) ) ;
#15192=ORIENTED_EDGE ( 'NONE', *, *, #11778, .T. ) ;
#15193=CARTESIAN_POINT ( 'NONE',  ( 0.6971942568897637749, 2.189545951927499583E-17, 1.262303149552535420 ) ) ;
#15195=CYLINDRICAL_SURFACE ( 'NONE', #31534, 0.1574803149606299191 ) ;
#15196=CARTESIAN_POINT ( 'NONE',  ( -0.7646288533564489232, 0.1113553986120547346, 1.441929133858267598 ) ) ;
#15197=CARTESIAN_POINT ( 'NONE',  ( 0.6971942568897626646, -0.07405724077823297447, 0.1624015747493861295 ) ) ;
#15202=CARTESIAN_POINT ( 'NONE',  ( -0.6971942568897637749, 2.189545951927499583E-17, 0.6766732282926929409 ) ) ;
#15206=CARTESIAN_POINT ( 'NONE',  ( -0.9412147342319837628, 0.1574803149606300301, 1.198326771653543732 ) ) ;
#15207=CARTESIAN_POINT ( 'NONE',  ( 0.8019270111902717657, -0.1787899950787401604, 1.353346456639149986 ) ) ;
#15208=CARTESIAN_POINT ( 'NONE',  ( 0.9500414927467377701, -0.1787899950787401604, 1.707677165300568456 ) ) ;
#15211=CYLINDRICAL_SURFACE ( 'NONE', #39698, 0.1574803149606299191 ) ;
#15217=CARTESIAN_POINT ( 'NONE',  ( 1.002407869896990045, 0.1264236179284866091, 1.247539370024976391 ) ) ;
#15220=CARTESIAN_POINT ( 'NONE',  ( -1.002407869896990045, 0.1264236179284866091, 1.168799212544661348 ) ) ;
#15221=CARTESIAN_POINT ( 'NONE',  ( 0.9873396505805591694, -0.1113553986120547346, 0.5856299211523157133 ) ) ;
#15222=VERTEX_POINT ( 'NONE', #38144 ) ;
#15224=EDGE_CURVE ( 'NONE', #32938, #33816, #22653, .T. ) ;
#15225=CARTESIAN_POINT ( 'NONE',  ( 0.8376409825901903750, 0.1727894281041914559, 0.03936911855021455603 ) ) ;
#15228=CARTESIAN_POINT ( 'NONE',  ( -0.8107537697050234415, -0.1574803149606297803, 0.3026574802074336046 ) ) ;
#15232=CARTESIAN_POINT ( 'NONE',  ( 0.7495606340400177148, 0.1264236179284866091, 1.651082677111590513 ) ) ;
#15236=CARTESIAN_POINT ( 'NONE',  ( -0.7185039370078739607, 1.928577636452523993E-17, 1.368110236220472675 ) ) ;
#15237=CARTESIAN_POINT ( 'NONE',  ( 0.6971942568897637749, 2.189545951927499583E-17, 0.04675196845017354913 ) ) ;
#15239=ORIENTED_EDGE ( 'NONE', *, *, #8941, .T. ) ;
#15242=CARTESIAN_POINT ( 'NONE',  ( 0.9500414927467377701, 0.1787899950787401604, 0.9005905511273391006 ) ) ;
#15243=CARTESIAN_POINT ( 'NONE',  ( -1.054774247047244096, 0.000000000000000000, 1.478838582623401399 ) ) ;
#15246=( BOUNDED_CURVE ( )  B_SPLINE_CURVE ( 2, ( #1919, #5041, #19661, #34524, #19893, #1680, #16327, #41911, #38585 ),
 .UNSPECIFIED., .F., .F. ) 
 B_SPLINE_CURVE_WITH_KNOTS ( ( 3, 2, 2, 2, 3 ),
 ( 0.2899999999999999800, 0.2924999999999999822, 0.2949999999999999845, 0.2974999999999999867, 0.2999999999999999889 ),
 .UNSPECIFIED. ) 
 CURVE ( )  GEOMETRIC_REPRESENTATION_ITEM ( )  RATIONAL_B_SPLINE_CURVE ( ( 1.000000000000000000, 0.9238795325112869605, 1.000000000000000000, 0.9238795325112869605, 1.000000000000000000, 0.9238795325112869605, 1.000000000000000000, 0.9238795325112869605, 1.000000000000000000 ) ) 
 REPRESENTATION_ITEM ( '' )  ) ;
#15247=AXIS2_PLACEMENT_3D ( 'NONE', #45360, #41507, #16162 ) ;
#15248=CARTESIAN_POINT ( 'NONE',  ( -1.002407869896990045, -0.1264236179284866091, 0.3764763778989925203 ) ) ;
#15253=CARTESIAN_POINT ( 'NONE',  ( -0.7185039370078739607, 0.000000000000000000, -2.869337061179095023E-17 ) ) ;
#15254=ORIENTED_EDGE ( 'NONE', *, *, #21878, .F. ) ;
#15255=CARTESIAN_POINT ( 'NONE',  ( 1.054774247047244540, 0.07405724077823318263, 1.008858267662772423 ) ) ;
#15257=CARTESIAN_POINT ( 'NONE',  ( -0.9412147342319837628, -0.1574803149606297803, 0.5831692912310552090 ) ) ;
#15259=CARTESIAN_POINT ( 'NONE',  ( -0.7185039370078739607, 1.928577636452523993E-17, 0.6594488188976378451 ) ) ;
#15260=CARTESIAN_POINT ( 'NONE',  ( -0.9873396505805591694, 0.1113553986120547346, 0.9202755905511811330 ) ) ;
#15261=FACE_OUTER_BOUND ( 'NONE', #35123, .T. ) ;
#15264=CARTESIAN_POINT ( 'NONE',  ( -0.8107537697050253289, 0.1574803149606300301, 1.587106299105073060 ) ) ;
#15265=CARTESIAN_POINT ( 'NONE',  ( 0.6971942568897626646, 0.07405724077823318263, 0.9498031495525356416 ) ) ;
#15267=CARTESIAN_POINT ( 'NONE',  ( 0.8107537697050253289, -0.1574803149606297803, 1.375492125984252523 ) ) ;
#15268=CARTESIAN_POINT ( 'NONE',  ( 0.7102373793000918978, 0.005418808439761009510, 1.983169977139155993 ) ) ;
#15272=CARTESIAN_POINT ( 'NONE',  ( 0.9500414927467377701, -0.1787899950787401604, 0.8415354330171020969 ) ) ;
#15278=CARTESIAN_POINT ( 'NONE',  ( 0.9500414927467378812, 0.1787899950787401604, 1.171259842465921741 ) ) ;
#15279=ADVANCED_FACE ( 'NONE', ( #16357 ), #20866, .F. ) ;
#15283=ORIENTED_EDGE ( 'NONE', *, *, #3073, .F. ) ;
#15285=CARTESIAN_POINT ( 'NONE',  ( -0.8759842519685039353, 0.1787899950787401882, 0.1894685038832444879 ) ) ;
#15287=CARTESIAN_POINT ( 'NONE',  ( 0.7185039370078739607, 1.928577636452523993E-17, 0.3444881889763780070 ) ) ;
#15288=CARTESIAN_POINT ( 'NONE',  ( -1.002407869896990045, -0.1264236179284866091, 1.670767716481669440 ) ) ;
#15289=CARTESIAN_POINT ( 'NONE',  ( -1.054774247047244096, 0.000000000000000000, 0.8882874015210394658 ) ) ;
#15290=CARTESIAN_POINT ( 'NONE',  ( -0.7495606340400177148, -0.1264236179284866091, 0.4453740156942677664 ) ) ;
#15291=CARTESIAN_POINT ( 'NONE',  ( -1.033464566929133799, 1.928577636452524610E-17, 2.869337061179095023E-17 ) ) ;
#15299=CARTESIAN_POINT ( 'NONE',  ( -0.8759842519685039353, -0.1574803149606299191, 1.171259842412157637 ) ) ;
#15300=CARTESIAN_POINT ( 'NONE',  ( -0.6971942568897637749, 2.189545951927499583E-17, 0.3567913385289137596 ) ) ;
#15303=ORIENTED_EDGE ( 'NONE', *, *, #22, .T. ) ;
#15305=CARTESIAN_POINT ( 'NONE',  ( -0.6971942568897648851, 0.07405724077823318263, 1.500984251914741829 ) ) ;
#15306=VERTEX_POINT ( 'NONE', #35278 ) ;
#15311=CARTESIAN_POINT ( 'NONE',  ( 1.033464566929134687, -0.06523048226347956391, 0.5191929133858269596 ) ) ;
#15312=DIRECTION ( 'NONE',  ( -1.000000000000000000, 0.000000000000000000, 0.000000000000000000 ) ) ;
#15313=CARTESIAN_POINT ( 'NONE',  ( -0.7185039370078746268, -0.06523048226347956391, 1.045767716427905114 ) ) ;
#15314=CARTESIAN_POINT ( 'NONE',  ( 0.8759842519685039353, 0.1787899950787401882, 0.5487204723871811352 ) ) ;
#15322=CARTESIAN_POINT ( 'NONE',  ( -0.8019270111902716547, 0.1787899950787401604, 1.023622047190330342 ) ) ;
#15323=CARTESIAN_POINT ( 'NONE',  ( 1.033464566929134687, -0.06523048226347956391, 0.9128937007874008414 ) ) ;
#15325=ADVANCED_FACE ( 'NONE', ( #5550 ), #31686, .T. ) ;
#15326=CARTESIAN_POINT ( 'NONE',  ( -0.9873396505805591694, -0.1113553986120547346, 0.8316929133858268486 ) ) ;
#15331=ORIENTED_EDGE ( 'NONE', *, *, #41846, .T. ) ;
#15334=CARTESIAN_POINT ( 'NONE',  ( 0.8759842519685039353, -0.1574803149606299191, 0.8267716535433071723 ) ) ;
#15335=CARTESIAN_POINT ( 'NONE',  ( 0.7185039370078766252, -0.06523048226348168721, 1.370570866141733068 ) ) ;
#15339=CARTESIAN_POINT ( 'NONE',  ( 0.9412147342319837628, 0.1574803149606300301, 1.188484251860977503 ) ) ;
#15340=CARTESIAN_POINT ( 'NONE',  ( -1.002407869896990045, -0.1264236179284866091, 0.4896653542769449086 ) ) ;
#15343=CARTESIAN_POINT ( 'NONE',  ( -0.9500414927467378812, -0.1787899950787401604, 1.712598425143087688 ) ) ;
#15344=CARTESIAN_POINT ( 'NONE',  ( 0.8759842519685039353, -0.1787899950787401882, 1.631397637741511808 ) ) ;
#15346=DIRECTION ( 'NONE',  ( 0.000000000000000000, 0.000000000000000000, -1.000000000000000000 ) ) ;
#15347=CARTESIAN_POINT ( 'NONE',  ( 0.6971942568897626646, -0.07405724077823297447, 0.2460629920722207375 ) ) ;
#15350=CARTESIAN_POINT ( 'NONE',  ( -1.002407869896990045, 0.1264236179284866091, 1.286909448765133801 ) ) ;
#15351=CARTESIAN_POINT ( 'NONE',  ( -0.8759842519685039353, -0.1787899950787401882, 0.9178149605761574126 ) ) ;
#15353=CARTESIAN_POINT ( 'NONE',  ( -0.6971942568897626646, -0.07405724077823297447, 0.1279527558517483676 ) ) ;
#15354=( BOUNDED_CURVE ( )  B_SPLINE_CURVE ( 2, ( #35388, #25557, #13796, #40128, #2531, #2762, #46615, #31800, #46383 ),
 .UNSPECIFIED., .F., .T. ) 
 B_SPLINE_CURVE_WITH_KNOTS ( ( 3, 2, 2, 2, 3 ),
 ( 0.3599999999999999867, 0.3624999999999999889, 0.3649999999999999911, 0.3674999999999999933, 0.3699999999999999956 ),
 .UNSPECIFIED. ) 
 CURVE ( )  GEOMETRIC_REPRESENTATION_ITEM ( )  RATIONAL_B_SPLINE_CURVE ( ( 1.000000000000000000, 0.9238795325112869605, 1.000000000000000000, 0.9238795325112869605, 1.000000000000000000, 0.9238795325112869605, 1.000000000000000000, 0.9238795325112869605, 1.000000000000000000 ) ) 
 REPRESENTATION_ITEM ( '' )  ) ;
#15356=CARTESIAN_POINT ( 'NONE',  ( -0.8759842519685039353, 0.1787899950787401882, 1.611712598371433103 ) ) ;
#15357=CARTESIAN_POINT ( 'NONE',  ( -1.033464566929134687, -0.06523048226347956391, 1.926673228238929170 ) ) ;
#15359=CARTESIAN_POINT ( 'NONE',  ( -0.8759842519685039353, -0.1574803149606299191, 1.653543307086614345 ) ) ;
#15361=CARTESIAN_POINT ( 'NONE',  ( 0.6971942568897648851, -0.07405724077823297447, 1.584645669237574994 ) ) ;
#15364=CARTESIAN_POINT ( 'NONE',  ( 0.7646288533564489232, 0.1113553986120547346, 0.2903543306011346359 ) ) ;
#15371=( BOUNDED_CURVE ( )  B_SPLINE_CURVE ( 2, ( #15693, #12088, #33206, #3700, #40107, #18324, #84, #332, #14979 ),
 .UNSPECIFIED., .F., .T. ) 
 B_SPLINE_CURVE_WITH_KNOTS ( ( 3, 2, 2, 2, 3 ),
 ( 0.7399999999999999911, 0.7425000000000000488, 0.7449999999999999956, 0.7475000000000000533, 0.7500000000000000000 ),
 .UNSPECIFIED. ) 
 CURVE ( )  GEOMETRIC_REPRESENTATION_ITEM ( )  RATIONAL_B_SPLINE_CURVE ( ( 1.000000000000000000, 0.9238795325112869605, 1.000000000000000000, 0.9238795325112869605, 1.000000000000000000, 0.9238795325112869605, 1.000000000000000000, 0.9238795325112829637, 1.000000000000000000 ) ) 
 REPRESENTATION_ITEM ( '' )  ) ;
#15373=ORIENTED_EDGE ( 'NONE', *, *, #35190, .T. ) ;
#15377=CARTESIAN_POINT ( 'NONE',  ( 0.6971942568897648851, 0.07405724077823318263, 1.811023621993480548 ) ) ;
#15381=CARTESIAN_POINT ( 'NONE',  ( -0.9873396505805591694, 0.1113553986120547346, 1.067913385719243990 ) ) ;
#15383=CARTESIAN_POINT ( 'NONE',  ( 1.054774247047244540, -0.07405724077823318263, 0.8070866141194653620 ) ) ;
#15385=LINE ( 'NONE', #41199, #33894 ) ;
#15388=CARTESIAN_POINT ( 'NONE',  ( 0.7185039370078739607, 1.928577636452523993E-17, 0.4625984251968504046 ) ) ;
#15389=CARTESIAN_POINT ( 'NONE',  ( 1.002407869896990045, 0.1264236179284866091, 1.803641732229700700 ) ) ;
#15390=AXIS2_PLACEMENT_3D ( 'NONE', #37483, #33921, #26484 ) ;
#15392=EDGE_CURVE ( 'NONE', #7011, #37113, #9496, .T. ) ;
#15393=CARTESIAN_POINT ( 'NONE',  ( 0.9412147342319837628, -0.1574803149606297803, 0.1205708661417322497 ) ) ;
#15394=DIRECTION ( 'NONE',  ( 0.000000000000000000, 0.000000000000000000, -1.000000000000000000 ) ) ;
#15398=CARTESIAN_POINT ( 'NONE',  ( 1.002407869896990045, 0.1264236179284866091, 0.1894685038832444879 ) ) ;
#15400=CARTESIAN_POINT ( 'NONE',  ( -0.6971942568897648851, -0.07405724077823297447, 1.697834645615527771 ) ) ;
#15401=ORIENTED_EDGE ( 'NONE', *, *, #27999, .F. ) ;
#15402=CARTESIAN_POINT ( 'NONE',  ( -0.8019270111902717657, -0.1787899950787401604, 1.353346456639149986 ) ) ;
#15403=CARTESIAN_POINT ( 'NONE',  ( -0.8759842519685039353, 0.000000000000000000, 0.000000000000000000 ) ) ;
#15404=CARTESIAN_POINT ( 'NONE',  ( 1.002407869896990045, 0.1264236179284866091, 1.331200787347811110 ) ) ;
#15405=CARTESIAN_POINT ( 'NONE',  ( 0.7495606340400177148, 0.1264236179284866091, 1.926673228292693052 ) ) ;
#15406=CARTESIAN_POINT ( 'NONE',  ( -0.8019270111902717657, -0.1787899950787401604, 1.072834645615528659 ) ) ;
#15408=CARTESIAN_POINT ( 'NONE',  ( 1.033464566929134687, 0.06523048226347956391, 1.193405511811024278 ) ) ;
#15409=CARTESIAN_POINT ( 'NONE',  ( 0.6971942568897648851, 0.07405724077823318263, 0.3986220471903311746 ) ) ;
#15410=CARTESIAN_POINT ( 'NONE',  ( -0.6971942568897648851, -0.07405724077823297447, 0.3592519684501735422 ) ) ;
#15411=CARTESIAN_POINT ( 'NONE',  ( -1.002407869896990045, 0.1264236179284866091, 0.8538385826234016207 ) ) ;
#15412=ORIENTED_EDGE ( 'NONE', *, *, #5787, .F. ) ;
#15414=CARTESIAN_POINT ( 'NONE',  ( -0.7185039370078739607, 1.928577636452523993E-17, 1.368110236220472675 ) ) ;
#15415=CARTESIAN_POINT ( 'NONE',  ( -0.8107537697050234415, -0.1574803149606297803, 0.07627952755905517690 ) ) ;
#15419=CARTESIAN_POINT ( 'NONE',  ( -0.7185039370078739607, 1.928577636452523993E-17, 1.289370078740157632 ) ) ;
#15421=CARTESIAN_POINT ( 'NONE',  ( -1.002407869896990045, -0.1264236179284866091, 0.8882874015210394658 ) ) ;
#15428=CARTESIAN_POINT ( 'NONE',  ( 0.6971942568897648851, -0.07405724077823297447, 1.146653543253323582 ) ) ;
#15429=CARTESIAN_POINT ( 'NONE',  ( 0.9412147342319837628, 0.1574803149606300301, 1.592027559055119612 ) ) ;
#15430=FACE_OUTER_BOUND ( 'NONE', #31986, .T. ) ;
#15431=CARTESIAN_POINT ( 'NONE',  ( -1.033464566929133799, 0.000000000000000000, 1.427165354330708569 ) ) ;
#15432=CARTESIAN_POINT ( 'NONE',  ( 1.002407869896990045, 0.1264236179284866091, 0.1845472440407248116 ) ) ;
#15439=CARTESIAN_POINT ( 'NONE',  ( -0.7495606340400177148, -0.1264236179284866091, 0.7209645668753701386 ) ) ;
#15440=ADVANCED_FACE ( 'NONE', ( #39773 ), #10096, .T. ) ;
#15442=CARTESIAN_POINT ( 'NONE',  ( -0.7185039370078739607, 1.928577636452523993E-17, 1.564960629921259949 ) ) ;
#15446=CARTESIAN_POINT ( 'NONE',  ( 0.8759842519685039353, -0.1787899950787401882, 1.355807086560409491 ) ) ;
#15447=CARTESIAN_POINT ( 'NONE',  ( 0.9500414927467377701, 0.1787899950787401604, 1.683070866087970074 ) ) ;
#15448=CARTESIAN_POINT ( 'NONE',  ( 0.9500414927467377701, -0.1787899950787401604, 0.2509842519147403861 ) ) ;
#15451=CARTESIAN_POINT ( 'NONE',  ( -1.033464566929133799, 0.000000000000000000, 1.653543306979086580 ) ) ;
#15452=CARTESIAN_POINT ( 'NONE',  ( -0.7185039370078739607, 1.928577636452523993E-17, 1.525590551181102317 ) ) ;
#15455=CARTESIAN_POINT ( 'NONE',  ( -0.7646288533564489232, -0.1113553986120547346, 1.018700787401574770 ) ) ;
#15456=CARTESIAN_POINT ( 'NONE',  ( 0.7185039370078746268, 0.06523048226347956391, 0.7652559054042838982 ) ) ;
#15457=CARTESIAN_POINT ( 'NONE',  ( 0.6971942568897637749, 2.189545951927499583E-17, 0.3567913385289137596 ) ) ;
#15458=CARTESIAN_POINT ( 'NONE',  ( 0.7368992853545974775, -0.09446756238934114758, 0.03937007758462267998 ) ) ;
#15459=CARTESIAN_POINT ( 'NONE',  ( 0.6971942568897648851, -0.07405724077823297447, 1.225393700733637514 ) ) ;
#15460=DIRECTION ( 'NONE',  ( 0.000000000000000000, 0.000000000000000000, -1.000000000000000000 ) ) ;
#15462=CARTESIAN_POINT ( 'NONE',  ( -0.8759842519685039353, 0.1787899950787401882, 1.291830708607653477 ) ) ;
#15463=CARTESIAN_POINT ( 'NONE',  ( 0.9412147342319837628, 0.1574803149606300301, 0.5979330707586145710 ) ) ;
#15464=VERTEX_POINT ( 'NONE', #25440 ) ;
#15465=CARTESIAN_POINT ( 'NONE',  ( 0.7185039370078739607, 0.000000000000000000, 4.498031496062992574 ) ) ;
#15471=CARTESIAN_POINT ( 'NONE',  ( -0.7646288533564489232, -0.1113553986120547346, 1.176181102362204633 ) ) ;
#15472=CARTESIAN_POINT ( 'NONE',  ( 0.7185039370078739607, 1.928577636452523993E-17, 0.5807086614173228023 ) ) ;
#15474=CARTESIAN_POINT ( 'NONE',  ( -0.7646288533564489232, 0.1113553986120547346, 0.7627952754830236159 ) ) ;
#15475=CARTESIAN_POINT ( 'NONE',  ( 1.054774247047244540, 0.07405724077823318263, 0.06889763774151215492 ) ) ;
#15477=CARTESIAN_POINT ( 'NONE',  ( 0.8107537697050253289, 0.1574803149606300301, 1.311515747923968744 ) ) ;
#15479=CARTESIAN_POINT ( 'NONE',  ( 1.002407869896990045, -0.1264236179284866091, 0.6914370078202519698 ) ) ;
#15480=CARTESIAN_POINT ( 'NONE',  ( 1.002407869896990045, -0.1264236179284866091, 0.9276574802611967652 ) ) ;
#15481=CARTESIAN_POINT ( 'NONE',  ( -0.6971942568897637749, 2.189545951927499583E-17, 1.537893700733637736 ) ) ;
#15483=CARTESIAN_POINT ( 'NONE',  ( -0.8019270111902717657, 0.1787899950787401604, 1.220472440891118504 ) ) ;
#15487=CARTESIAN_POINT ( 'NONE',  ( -0.9500414927467378812, 0.1787899950787401604, 0.3494094487651343006 ) ) ;
#15489=CARTESIAN_POINT ( 'NONE',  ( 0.7185039370078739607, 1.928577636452523993E-17, 1.683070866141732402 ) ) ;
#15491=ORIENTED_EDGE ( 'NONE', *, *, #43402, .T. ) ;
#15494=EDGE_CURVE ( 'NONE', #8469, #1467, #38864, .T. ) ;
#15497=EDGE_CURVE ( 'NONE', #18901, #10582, #8632, .T. ) ;
#15499=CARTESIAN_POINT ( 'NONE',  ( -0.7495606340400177148, 0.1264236179284866091, 0.2386811023084413619 ) ) ;
#15500=CARTESIAN_POINT ( 'NONE',  ( -0.9873396505805591694, -0.1113553986120547346, 0.8316929133858268486 ) ) ;
#15504=CARTESIAN_POINT ( 'NONE',  ( 1.033464566929134687, 0.06523048226347956391, 0.4060039370078741827 ) ) ;
#15505=CARTESIAN_POINT ( 'NONE',  ( -0.8107537697050253289, 0.1574803149606300301, 1.508366141624757129 ) ) ;
#15506=CARTESIAN_POINT ( 'NONE',  ( 0.7495606340400177148, -0.1264236179284866091, 0.9178149605761574126 ) ) ;
#15507=CARTESIAN_POINT ( 'NONE',  ( 0.6971942568897648851, -0.07405724077823297447, 1.343503936954111966 ) ) ;
#15508=CARTESIAN_POINT ( 'NONE',  ( -0.7646288533564489232, 0.1113553986120547346, 0.4576771653543307283 ) ) ;
#15509=AXIS2_PLACEMENT_3D ( 'NONE', #47255, #36252, #43648 ) ;
#15510=CARTESIAN_POINT ( 'NONE',  ( 0.7185039370078746268, 0.06523048226347956391, 1.365649606299211838 ) ) ;
#15511=CARTESIAN_POINT ( 'NONE',  ( 0.7459936014081097744, -0.1092670104579866602, 1.985467488891498045 ) ) ;
#15512=CARTESIAN_POINT ( 'NONE',  ( 1.033464566929133799, 0.000000000000000000, 1.860236220472440971 ) ) ;
#15514=CARTESIAN_POINT ( 'NONE',  ( 0.6971942568897648851, 0.07405724077823318263, 0.8661417322297002563 ) ) ;
#15516=CARTESIAN_POINT ( 'NONE',  ( 1.054774247047244540, 0.07405724077823318263, 1.761811023568284229 ) ) ;
#15519=CARTESIAN_POINT ( 'NONE',  ( 0.9412147342319837628, 0.1574803149606300301, 1.080216535433071501 ) ) ;
#15520=( GEOMETRIC_REPRESENTATION_CONTEXT ( 3 ) GLOBAL_UNCERTAINTY_ASSIGNED_CONTEXT ( ( #7724 ) ) GLOBAL_UNIT_ASSIGNED_CONTEXT ( ( #39041, #2614, #2841 ) ) REPRESENTATION_CONTEXT ( 'NONE', 'WORKASPACE' ) ) ;
#15523=CARTESIAN_POINT ( 'NONE',  ( -0.7646288533564489232, 0.1113553986120547346, 0.1328740156405045225 ) ) ;
#15524=CARTESIAN_POINT ( 'NONE',  ( 0.8019270111902717657, 0.1787899950787401604, 1.097440944828127041 ) ) ;
#15525=FACE_OUTER_BOUND ( 'NONE', #39289, .T. ) ;
#15530=CARTESIAN_POINT ( 'NONE',  ( -0.6971942568897626646, -0.07405724077823297447, 0.2805118109698587214 ) ) ;
#15534=CARTESIAN_POINT ( 'NONE',  ( -0.8759842519685039353, -0.1574803149606299191, 0.7086614173228346081 ) ) ;
#15537=CARTESIAN_POINT ( 'NONE',  ( -0.8019270111902717657, -0.1787899950787401604, 1.781496062938362934 ) ) ;
#15538=CARTESIAN_POINT ( 'NONE',  ( -0.6971942568897648851, -0.07405724077823297447, 0.9498031495525356416 ) ) ;
#15539=CARTESIAN_POINT ( 'NONE',  ( -0.6971942568897626646, -0.07405724077823297447, 0.5610236219934807700 ) ) ;
#15540=CARTESIAN_POINT ( 'NONE',  ( -1.033464566929133799, 0.000000000000000000, 0.1673228346456692994 ) ) ;
#15542=CARTESIAN_POINT ( 'NONE',  ( -0.8107537697050254399, 0.1574803149606300301, 1.675688976377952999 ) ) ;
#15545=CARTESIAN_POINT ( 'NONE',  ( 0.7185039370078746268, 0.06523048226347956391, 1.798720472440944240 ) ) ;
#15548=CARTESIAN_POINT ( 'NONE',  ( -1.054774247047244096, 0.000000000000000000, 0.3371062991588349989 ) ) ;
#15549=CARTESIAN_POINT ( 'NONE',  ( 0.7185039370078739607, 1.928577636452523993E-17, 1.200787401467275695 ) ) ;
#15551=AXIS2_PLACEMENT_3D ( 'NONE', #8426, #34330, #26437 ) ;
#15552=ORIENTED_EDGE ( 'NONE', *, *, #45320, .T. ) ;
#15555=CARTESIAN_POINT ( 'NONE',  ( -0.9500414927467377701, 0.1787899950787401604, 1.491141732229701145 ) ) ;
#15556=ORIENTED_EDGE ( 'NONE', *, *, #19453, .F. ) ;
#15559=ADVANCED_FACE ( 'NONE', ( #10342 ), #10589, .T. ) ;
#15562=SURFACE_STYLE_FILL_AREA ( #1856 ) ;
#15564=CARTESIAN_POINT ( 'NONE',  ( 0.8759842519685039353, -0.1574803149606299191, 0.4330708661417322913 ) ) ;
#15566=CARTESIAN_POINT ( 'NONE',  ( -0.9873396505805591694, 0.1113553986120547346, 1.146653543199559033 ) ) ;
#15567=CARTESIAN_POINT ( 'NONE',  ( 0.8759842519685039353, 0.1787899950787401882, 0.5880905511273386566 ) ) ;
#15568=CARTESIAN_POINT ( 'NONE',  ( 0.6971942568897644410, 0.03556354196195587319, 0.04064907242275180022 ) ) ;
#15571=CARTESIAN_POINT ( 'NONE',  ( 0.7185039370078739607, 1.928577636452523993E-17, 1.948818897530267602 ) ) ;
#15574=CARTESIAN_POINT ( 'NONE',  ( -0.8759842519685039353, -0.1787899950787401882, 1.001476377898992132 ) ) ;
#15575=CARTESIAN_POINT ( 'NONE',  ( 0.8759842519685039353, -0.1574803149606299191, 0.9842519685039370358 ) ) ;
#15580=ORIENTED_EDGE ( 'NONE', *, *, #17261, .T. ) ;
#15587=CARTESIAN_POINT ( 'NONE',  ( 0.7646288533564489232, -0.1113553986120547346, 1.126968503829480328 ) ) ;
#15588=CARTESIAN_POINT ( 'NONE',  ( -0.7185039370078766252, -0.06523048226348168721, 1.646161417322834497 ) ) ;
#15591=CARTESIAN_POINT ( 'NONE',  ( -0.8019270111902717657, 0.1787899950787401604, 1.692913385773008539 ) ) ;
#15592=CARTESIAN_POINT ( 'NONE',  ( -0.7646288533564489232, 0.1113553986120547346, 0.6545275590551181688 ) ) ;
#15593=CARTESIAN_POINT ( 'NONE',  ( 1.002407869896990045, 0.1264236179284866091, 1.685531496009228469 ) ) ;
#15596=CARTESIAN_POINT ( 'NONE',  ( 0.7646288533564489232, 0.1113553986120547346, 1.471456692805858113 ) ) ;
#15597=CARTESIAN_POINT ( 'NONE',  ( 0.6971942568897626646, -0.07405724077823297447, 0.2854330708123783422 ) ) ;
#15598=CARTESIAN_POINT ( 'NONE',  ( -1.054774247047244540, 0.07405724077823318263, 1.441929133804504604 ) ) ;
#15599=CARTESIAN_POINT ( 'NONE',  ( 1.033464566929133799, 0.000000000000000000, 1.259842519577511810 ) ) ;
#15600=CARTESIAN_POINT ( 'NONE',  ( -0.8759842519685039353, 0.1787899950787401882, 1.173720472387181246 ) ) ;
#15601=CARTESIAN_POINT ( 'NONE',  ( -0.6971942568897637749, 2.189545951927499583E-17, 0.08612204719033110523 ) ) ;
#15603=CARTESIAN_POINT ( 'NONE',  ( -0.7495606340400177148, -0.1264236179284866091, 1.587106299158834721 ) ) ;
#15604=CARTESIAN_POINT ( 'NONE',  ( -0.6971942568897626646, 0.07405724077823318263, 0.08366141726907129483 ) ) ;
#15605=CARTESIAN_POINT ( 'NONE',  ( -0.8107537697050253289, 0.1574803149606300301, 1.596948818897636402 ) ) ;
#15606=CARTESIAN_POINT ( 'NONE',  ( 0.7646288533564489232, 0.1113553986120547346, 1.638779527559055316 ) ) ;
#15607=CARTESIAN_POINT ( 'NONE',  ( 1.002407869896990045, -0.1264236179284866091, 1.596948818843874074 ) ) ;
#15609=DIRECTION ( 'NONE',  ( -1.000000000000000000, 0.000000000000000000, 0.000000000000000000 ) ) ;
#15613=ORIENTED_EDGE ( 'NONE', *, *, #44105, .T. ) ;
#15615=ADVANCED_FACE ( 'NONE', ( #4292 ), #33113, .T. ) ;
#15618=ORIENTED_EDGE ( 'NONE', *, *, #13674, .T. ) ;
#15620=CARTESIAN_POINT ( 'NONE',  ( 1.002407869896990045, 0.1264236179284866091, 1.838090551127338657 ) ) ;
#15624=CARTESIAN_POINT ( 'NONE',  ( -0.8759842519685039353, 0.1574803149606299191, 1.072834645561763889 ) ) ;
#15625=CARTESIAN_POINT ( 'NONE',  ( 1.002407869896990045, -0.1264236179284866091, 0.8046259841982047467 ) ) ;
#15627=CARTESIAN_POINT ( 'NONE',  ( -0.8759842491179902213, 0.1574803149606299191, 1.978346456692913646 ) ) ;
#15629=VECTOR ( 'NONE', #37392, 39.37007874015748143 ) ;
#15630=CARTESIAN_POINT ( 'NONE',  ( 0.7646288533564489232, -0.1113553986120547346, 1.254921259842519676 ) ) ;
#15631=CARTESIAN_POINT ( 'NONE',  ( 1.054774247047244096, 0.000000000000000000, 1.759350393647023614 ) ) ;
#15632=CARTESIAN_POINT ( 'NONE',  ( 0.9412147342319837628, 0.1574803149606300301, 0.05659448818897635375 ) ) ;
#15638=CARTESIAN_POINT ( 'NONE',  ( 1.054774247047244540, -0.07405724077823318263, 0.2608267715997796832 ) ) ;
#15639=( BOUNDED_CURVE ( )  B_SPLINE_CURVE ( 2, ( #34249, #1865, #1147, #37832, #41144, #31131, #16037, #16501, #44753 ),
 .UNSPECIFIED., .F., .T. ) 
 B_SPLINE_CURVE_WITH_KNOTS ( ( 3, 2, 2, 2, 3 ),
 ( 0.8699999999999999956, 0.8725000000000000533, 0.8750000000000000000, 0.8774999999999999467, 0.8800000000000000044 ),
 .UNSPECIFIED. ) 
 CURVE ( )  GEOMETRIC_REPRESENTATION_ITEM ( )  RATIONAL_B_SPLINE_CURVE ( ( 1.000000000000000000, 0.9238795325112899581, 1.000000000000000000, 0.9238795325112869605, 1.000000000000000000, 0.9238795325112869605, 1.000000000000000000, 0.9238795325112869605, 1.000000000000000000 ) ) 
 REPRESENTATION_ITEM ( '' )  ) ;
#15640=CARTESIAN_POINT ( 'NONE',  ( 0.7185039370078746268, 0.06523048226347956391, 0.06643700787401589369 ) ) ;
#15641=CARTESIAN_POINT ( 'NONE',  ( -1.002407869896990045, 0.1264236179284866091, 1.719980314906866203 ) ) ;
#15643=CARTESIAN_POINT ( 'NONE',  ( -0.8759842519685039353, -0.1787899950787401882, 1.316437007820252081 ) ) ;
#15644=CARTESIAN_POINT ( 'NONE',  ( 1.033464566929134687, -0.06523048226347956391, 1.031003937007875182 ) ) ;
#15645=B_SPLINE_CURVE_WITH_KNOTS ( 'NONE', 3,
 ( #16790, #38359, #2858, #17495, #5530, #20145 ),
 .UNSPECIFIED., .F., .F.,
 ( 4, 2, 4 ),
 ( 0.000000000000000000, 0.5000000000000000000, 1.000000000000000000 ),
 .UNSPECIFIED. ) ;
#15646=CARTESIAN_POINT ( 'NONE',  ( 0.8019270111902717657, 0.1787899950787401604, 1.963582677111591401 ) ) ;
#15647=CARTESIAN_POINT ( 'NONE',  ( -1.002407869896990045, 0.1264236179284866091, 1.090059055064346527 ) ) ;
#15648=CARTESIAN_POINT ( 'NONE',  ( 0.7185039370078739607, 1.928577636452523993E-17, 0.6496062991050708391 ) ) ;
#15650=CARTESIAN_POINT ( 'NONE',  ( -1.033464566929134687, 0.06523048226347956391, 1.341043306979086358 ) ) ;
#15651=CARTESIAN_POINT ( 'NONE',  ( 0.7495606340400177148, -0.1264236179284866091, 0.5241141731745827537 ) ) ;
#15652=CARTESIAN_POINT ( 'NONE',  ( -0.8019270111902716547, -0.1787899950787401604, 0.3248031495525355861 ) ) ;
#15656=CARTESIAN_POINT ( 'NONE',  ( -0.9412147342319837628, -0.1574803149606297803, 0.1599409448818898405 ) ) ;
#15657=CARTESIAN_POINT ( 'NONE',  ( 0.9500414927467377701, 0.1787899950787401604, 1.136811023568283119 ) ) ;
#15660=CYLINDRICAL_SURFACE ( 'NONE', #45476, 0.1787899950787401049 ) ;
#15662=EDGE_CURVE ( 'NONE', #25448, #18659, #20537, .T. ) ;
#15663=CARTESIAN_POINT ( 'NONE',  ( -0.9873396505805591694, 0.1113553986120547346, 1.461614173120818760 ) ) ;
#15664=CARTESIAN_POINT ( 'NONE',  ( -0.8019270111902717657, -0.1787899950787401604, 0.04921259837143338034 ) ) ;
#15676=CARTESIAN_POINT ( 'NONE',  ( 0.6971942568897648851, 0.07405724077823318263, 1.653543307032850462 ) ) ;
#15677=CARTESIAN_POINT ( 'NONE',  ( 0.8019270111902717657, 0.1787899950787401604, 0.2312992125446618197 ) ) ;
#15680=FACE_OUTER_BOUND ( 'NONE', #5084, .T. ) ;
#15683=CARTESIAN_POINT ( 'NONE',  ( -1.002407869896990045, -0.1264236179284866091, 0.5733267715997795166 ) ) ;
#15685=CARTESIAN_POINT ( 'NONE',  ( 1.033464566929133799, 0.000000000000000000, 0.3641732283464567121 ) ) ;
#15689=CARTESIAN_POINT ( 'NONE',  ( 1.054774247047244096, 0.000000000000000000, 1.326279527505291433 ) ) ;
#15690=CARTESIAN_POINT ( 'NONE',  ( 0.7495606340400177148, -0.1264236179284866091, 1.897145669237574772 ) ) ;
#15693=CARTESIAN_POINT ( 'NONE',  ( 1.033464566929133799, 0.000000000000000000, 1.496062992018456494 ) ) ;
#15698=CARTESIAN_POINT ( 'NONE',  ( -0.7646288533564489232, 0.1113553986120547346, 1.235236220364913207 ) ) ;
#15699=CARTESIAN_POINT ( 'NONE',  ( 0.8759842519685039353, -0.1787899950787401882, 0.2485236219934806867 ) ) ;
#15700=EDGE_CURVE ( 'NONE', #16187, #10690, #22285, .T. ) ;
#15703=CARTESIAN_POINT ( 'NONE',  ( -1.054774247047244540, 0.07405724077823318263, 1.323818897584032817 ) ) ;
#15704=CARTESIAN_POINT ( 'NONE',  ( 0.9873396505805591694, -0.1113553986120547346, 0.7037401573727875004 ) ) ;
#15706=CARTESIAN_POINT ( 'NONE',  ( -0.9412147342319837628, 0.1574803149606300301, 1.749507874015747699 ) ) ;
#15712=CARTESIAN_POINT ( 'NONE',  ( -1.033464566929133799, 0.000000000000000000, 0.7972440944881890035 ) ) ;
#15713=CARTESIAN_POINT ( 'NONE',  ( 0.6971942568897637749, 2.189545951927499583E-17, 1.537893700733637736 ) ) ;
#15714=CARTESIAN_POINT ( 'NONE',  ( -0.8107537697050253289, 0.1574803149606300301, 1.242618110236220819 ) ) ;
#15715=CARTESIAN_POINT ( 'NONE',  ( 0.7646288533564489232, 0.1113553986120547346, 0.5757874015748032370 ) ) ;
#15719=ORIENTED_EDGE ( 'NONE', *, *, #19544, .T. ) ;
#15722=CARTESIAN_POINT ( 'NONE',  ( -0.8019270111902716547, -0.1787899950787401604, 1.545275590497419138 ) ) ;
#15724=CARTESIAN_POINT ( 'NONE',  ( -1.002407869896990045, 0.1264236179284866091, 1.331200787347811110 ) ) ;
#15728=CARTESIAN_POINT ( 'NONE',  ( -1.054774247047244540, -0.07405724077823318263, 0.3001968503399373711 ) ) ;
#15729=DIRECTION ( 'NONE',  ( 0.000000000000000000, 0.000000000000000000, -1.000000000000000000 ) ) ;
#15730=VECTOR ( 'NONE', #45030, 39.37007874015748143 ) ;
#15738=ORIENTED_EDGE ( 'NONE', *, *, #14434, .T. ) ;
#15739=ADVANCED_FACE ( 'NONE', ( #36682 ), #29770, .T. ) ;
#15743=CARTESIAN_POINT ( 'NONE',  ( -0.9500414927467377701, -0.1787899950787401604, 0.2165354330171024577 ) ) ;
#15744=CARTESIAN_POINT ( 'NONE',  ( -1.033464566929134687, -0.06523048226347956391, 0.8735236220472449853 ) ) ;
#15747=CARTESIAN_POINT ( 'NONE',  ( -1.033464566929134687, -0.06523048226347956391, 1.572342519577513142 ) ) ;
#15748=CARTESIAN_POINT ( 'NONE',  ( 0.8759842519685039353, -0.1787899950787401882, 0.9227362204186770889 ) ) ;
#15749=CARTESIAN_POINT ( 'NONE',  ( -1.033464566929133799, 0.000000000000000000, 0.4429133858267716439 ) ) ;
#15750=CARTESIAN_POINT ( 'NONE',  ( 0.7646288533564489232, 0.1113553986120547346, 1.520669291338582640 ) ) ;
#15751=CARTESIAN_POINT ( 'NONE',  ( 0.7440012176947153888, -0.1067469361137101808, 1.985406665012090510 ) ) ;
#15753=CARTESIAN_POINT ( 'NONE',  ( 0.7185039370078739607, 1.928577636452523993E-17, 1.870078740049952559 ) ) ;
#15757=CARTESIAN_POINT ( 'NONE',  ( 1.002407869896990045, -0.1264236179284866091, 0.8439960629383622681 ) ) ;
#15758=CARTESIAN_POINT ( 'NONE',  ( 0.6971942568897637749, 2.189545951927499583E-17, 1.818405511757259729 ) ) ;
#15761=ORIENTED_EDGE ( 'NONE', *, *, #32638, .T. ) ;
#15764=DIRECTION ( 'NONE',  ( 0.000000000000000000, 0.000000000000000000, -1.000000000000000000 ) ) ;
#15766=CARTESIAN_POINT ( 'NONE',  ( -0.8759842519685039353, -0.1574803149606299191, 0.1082677164279060994 ) ) ;
#15767=CARTESIAN_POINT ( 'NONE',  ( 0.6971942568897648851, 0.07405724077823318263, 1.220472440891118504 ) ) ;
#15771=CARTESIAN_POINT ( 'NONE',  ( -0.8759842519685039353, -0.1574803149606299191, 0.5118110236220472231 ) ) ;
#15772=DIRECTION ( 'NONE',  ( 1.000000000000000000, 0.000000000000000000, -1.822029033848725275E-16 ) ) ;
#15773=CARTESIAN_POINT ( 'NONE',  ( -0.8759842519685039353, 0.1787899950787401882, 0.3075787401037169411 ) ) ;
#15774=EDGE_CURVE ( 'NONE', #36149, #24840, #34509, .T. ) ;
#15778=CARTESIAN_POINT ( 'NONE',  ( -1.033464566929136907, -0.06523048226347749612, 1.857775590551182798 ) ) ;
#15779=CARTESIAN_POINT ( 'NONE',  ( -1.054774247047244540, -0.07405724077823318263, 1.791338582623401177 ) ) ;
#15780=CARTESIAN_POINT ( 'NONE',  ( -0.9500414927467377701, -0.1787899950787401604, 0.8809055117572600624 ) ) ;
#15781=CARTESIAN_POINT ( 'NONE',  ( -0.9500414927467378812, 0.1787899950787401604, 0.5068897637257642197 ) ) ;
#15782=( BOUNDED_CURVE ( )  B_SPLINE_CURVE ( 2, ( #46348, #28403, #35585, #21178, #13312, #42508, #24325, #31067, #16665 ),
 .UNSPECIFIED., .F., .T. ) 
 B_SPLINE_CURVE_WITH_KNOTS ( ( 3, 2, 2, 2, 3 ),
 ( 0.4400000000000000022, 0.4425000000000000044, 0.4450000000000000067, 0.4475000000000000089, 0.4500000000000000111 ),
 .UNSPECIFIED. ) 
 CURVE ( )  GEOMETRIC_REPRESENTATION_ITEM ( )  RATIONAL_B_SPLINE_CURVE ( ( 1.000000000000000000, 0.9238795325112869605, 1.000000000000000000, 0.9238795325112869605, 1.000000000000000000, 0.9238795325112869605, 1.000000000000000000, 0.9238795325112869605, 1.000000000000000000 ) ) 
 REPRESENTATION_ITEM ( '' )  ) ;
#15783=CARTESIAN_POINT ( 'NONE',  ( 0.7185039370078739607, 1.928577636452523993E-17, 0.4921259841444416971 ) ) ;
#15785=CARTESIAN_POINT ( 'NONE',  ( -0.8107537697050254399, 0.1574803149606300301, 0.3272637794200322636 ) ) ;
#15792=CARTESIAN_POINT ( 'NONE',  ( -1.054774247047244540, 0.07405724077823318263, 0.5364173227808821665 ) ) ;
#15793=CARTESIAN_POINT ( 'NONE',  ( 0.8107537697050254399, 0.1574803149606300301, 1.193405511703496957 ) ) ;
#15795=EDGE_CURVE ( 'NONE', #38992, #28962, #33175, .T. ) ;
#15797=CARTESIAN_POINT ( 'NONE',  ( -0.7495606340400177148, 0.1264236179284866091, 1.577263779473795369 ) ) ;
#15800=CARTESIAN_POINT ( 'NONE',  ( 1.033464566929134687, 0.06523048226347956391, 0.9571850393700783721 ) ) ;
#15801=DIRECTION ( 'NONE',  ( -1.000000000000000000, 0.000000000000000000, 0.000000000000000000 ) ) ;
#15802=CARTESIAN_POINT ( 'NONE',  ( -0.8107537697050253289, -0.1574803149606297803, 1.129429133750740277 ) ) ;
#15803=CARTESIAN_POINT ( 'NONE',  ( 0.8759842519685039353, -0.1787899950787401882, 0.5684055117572598403 ) ) ;
#15806=CARTESIAN_POINT ( 'NONE',  ( 1.033464566929133799, 0.000000000000000000, 1.968503936900346529 ) ) ;
#15809=CARTESIAN_POINT ( 'NONE',  ( 0.9412147342319837628, -0.1574803149606297803, 0.9867125984251976512 ) ) ;
#15812=DIRECTION ( 'NONE',  ( 0.000000000000000000, 0.000000000000000000, -1.000000000000000000 ) ) ;
#15813=CARTESIAN_POINT ( 'NONE',  ( -1.033464566929133799, 0.000000000000000000, 1.269685039370078705 ) ) ;
#15819=CARTESIAN_POINT ( 'NONE',  ( 0.9500414927467378812, 0.1787899950787401604, 0.7381889763241898939 ) ) ;
#15827=CARTESIAN_POINT ( 'NONE',  ( 0.7185039370078746268, -0.06523048226347956391, 1.085137795168063413 ) ) ;
#15832=CARTESIAN_POINT ( 'NONE',  ( -1.002407869896990045, -0.1264236179284866091, 1.793799212544661348 ) ) ;
#15833=EDGE_CURVE ( 'NONE', #13064, #11651, #36514, .T. ) ;
#15834=CARTESIAN_POINT ( 'NONE',  ( 0.9500414927467378812, -0.1787899950787401604, 1.791338582623401177 ) ) ;
#15836=CARTESIAN_POINT ( 'NONE',  ( -1.002407869896990045, -0.1264236179284866091, 0.8882874015210394658 ) ) ;
#15838=CARTESIAN_POINT ( 'NONE',  ( 0.8759842519685039353, -0.1787899950787401882, 0.4109251967966299213 ) ) ;
#15839=CARTESIAN_POINT ( 'NONE',  ( -0.8759842519685039353, 0.1787899950787401882, 1.449311023568283341 ) ) ;
#15840=EDGE_CURVE ( 'NONE', #47099, #16198, #38099, .T. ) ;
#15841=CARTESIAN_POINT ( 'NONE',  ( -1.002407869896990045, -0.1264236179284866091, 1.237696850339937038 ) ) ;
#15842=CARTESIAN_POINT ( 'NONE',  ( -0.6971942568897626646, -0.07405724077823297447, 0.9498031495525356416 ) ) ;
#15843=CARTESIAN_POINT ( 'NONE',  ( -0.8019270111902717657, -0.1787899950787401604, 0.05413385821395302888 ) ) ;
#15845=CARTESIAN_POINT ( 'NONE',  ( -0.8019270111902717657, -0.1787899950787401604, 1.707677165300566235 ) ) ;
#15846=CARTESIAN_POINT ( 'NONE',  ( -1.002407869896990045, -0.1264236179284866091, 0.06151574797773248782 ) ) ;
#15847=CARTESIAN_POINT ( 'NONE',  ( -1.033464566929134687, 0.06523048226347956391, 1.547736220472440749 ) ) ;
#15849=CARTESIAN_POINT ( 'NONE',  ( 0.8019270111902716547, 0.1787899950787401604, 1.614173228292692386 ) ) ;
#15853=VERTEX_POINT ( 'NONE', #16309 ) ;
#15858=CARTESIAN_POINT ( 'NONE',  ( -0.8107537697050254399, 0.1574803149606300301, 1.281988188976378895 ) ) ;
#15861=CARTESIAN_POINT ( 'NONE',  ( -1.033464566929134687, 0.06523048226347956391, 1.065452755797984041 ) ) ;
#15862=CARTESIAN_POINT ( 'NONE',  ( 0.6971942568897626646, 0.07405724077823318263, 0.7086614172690703928 ) ) ;
#15864=CARTESIAN_POINT ( 'NONE',  ( -0.7185039370078746268, -0.06523048226347956391, 0.06151574792396910518 ) ) ;
#15865=CARTESIAN_POINT ( 'NONE',  ( 0.8019270111902717657, -0.1787899950787401604, 1.825787401521040243 ) ) ;
#15866=CARTESIAN_POINT ( 'NONE',  ( 0.8759842519685039353, -0.1574803149606299191, 0.03937007874015747977 ) ) ;
#15867=LINE ( 'NONE', #45299, #14521 ) ;
#15872=CARTESIAN_POINT ( 'NONE',  ( 1.054774247047244540, 0.07405724077823318263, 0.2263779527021421711 ) ) ;
#15875=CARTESIAN_POINT ( 'NONE',  ( -0.8759842519685039353, -0.1787899950787401882, 1.744586614119464807 ) ) ;
#15877=CARTESIAN_POINT ( 'NONE',  ( -0.6971942568897637749, 2.189545951927499583E-17, 1.267224409395055096 ) ) ;
#15879=CARTESIAN_POINT ( 'NONE',  ( 0.7495606340400177148, 0.1264236179284866091, 1.301673228292692830 ) ) ;
#15880=CARTESIAN_POINT ( 'NONE',  ( -1.054774247047244540, 0.07405724077823318263, 0.5413385826234012876 ) ) ;
#15881=CARTESIAN_POINT ( 'NONE',  ( -0.9500414927467378812, -0.1787899950787401604, 1.235236220418678199 ) ) ;
#15885=FACE_OUTER_BOUND ( 'NONE', #7083, .T. ) ;
#15886=CARTESIAN_POINT ( 'NONE',  ( 0.8019270111902716547, -0.1787899950787401604, 0.4478346456155276045 ) ) ;
#15887=CARTESIAN_POINT ( 'NONE',  ( -1.054774247047244540, -0.07405724077823318263, 0.3740157479777325711 ) ) ;
#15888=CARTESIAN_POINT ( 'NONE',  ( -0.8759842519685039353, -0.1787899950787401882, 0.8390748030958424808 ) ) ;
#15889=ORIENTED_EDGE ( 'NONE', *, *, #8504, .F. ) ;
#15892=CARTESIAN_POINT ( 'NONE',  ( 1.054774247047244540, 0.07405724077823318263, 0.9350393700249758355 ) ) ;
#15893=CARTESIAN_POINT ( 'NONE',  ( -0.8759842519685039353, -0.1574803149606299191, 0.2755905511811023723 ) ) ;
#15894=CARTESIAN_POINT ( 'NONE',  ( 0.6971942568897648851, 0.07405724077823318263, 1.225393700733637514 ) ) ;
#15899=FACE_OUTER_BOUND ( 'NONE', #29823, .T. ) ;
#15906=ORIENTED_EDGE ( 'NONE', *, *, #16997, .F. ) ;
#15908=DIRECTION ( 'NONE',  ( 0.000000000000000000, 0.000000000000000000, -1.000000000000000000 ) ) ;
#15911=CARTESIAN_POINT ( 'NONE',  ( 1.002407869896990045, -0.1264236179284866091, 0.1747047243556852092 ) ) ;
#15914=( BOUNDED_CURVE ( )  B_SPLINE_CURVE ( 2, ( #444, #26598, #4749, #41150, #36654, #29517, #14609, #36890, #33321 ),
 .UNSPECIFIED., .F., .T. ) 
 B_SPLINE_CURVE_WITH_KNOTS ( ( 3, 2, 2, 2, 3 ),
 ( 0.6800000000000000488, 0.6824999999999999956, 0.6850000000000000533, 0.6875000000000000000, 0.6899999999999999467 ),
 .UNSPECIFIED. ) 
 CURVE ( )  GEOMETRIC_REPRESENTATION_ITEM ( )  RATIONAL_B_SPLINE_CURVE ( ( 1.000000000000000000, 0.9238795325112869605, 1.000000000000000000, 0.9238795325112869605, 1.000000000000000000, 0.9238795325112869605, 1.000000000000000000, 0.9238795325112829637, 1.000000000000000000 ) ) 
 REPRESENTATION_ITEM ( '' )  ) ;
#15915=CARTESIAN_POINT ( 'NONE',  ( -1.054774247047244540, -0.07405724077823318263, 0.6151574802611973203 ) ) ;
#15916=CARTESIAN_POINT ( 'NONE',  ( -0.7185039370078739607, 1.928577636452523993E-17, 1.279527558947590515 ) ) ;
#15921=CARTESIAN_POINT ( 'NONE',  ( 0.7495606340400177148, 0.1264236179284866091, 1.341043307032850462 ) ) ;
#15922=CARTESIAN_POINT ( 'NONE',  ( 1.002407869896990045, -0.1264236179284866091, 1.867618110182456714 ) ) ;
#15925=ORIENTED_EDGE ( 'NONE', *, *, #31630, .T. ) ;
#15926=CARTESIAN_POINT ( 'NONE',  ( -0.9873396505805591694, -0.1113553986120547346, 1.451771653435779408 ) ) ;
#15927=CARTESIAN_POINT ( 'NONE',  ( -0.8759842519685039353, 0.000000000000000000, 0.000000000000000000 ) ) ;
#15930=CARTESIAN_POINT ( 'NONE',  ( 0.7646288533564489232, -0.1113553986120547346, 0.4970472439869613734 ) ) ;
#15931=CARTESIAN_POINT ( 'NONE',  ( 0.9500414927467378812, -0.1787899950787401604, 0.4872047243556847929 ) ) ;
#15937=CARTESIAN_POINT ( 'NONE',  ( -0.6971942568897637749, 2.189545951927499583E-17, 1.341043307032850462 ) ) ;
#15938=CARTESIAN_POINT ( 'NONE',  ( 0.7185039370078746268, -0.06523048226347956391, 0.8882874014672753615 ) ) ;
#15939=ORIENTED_EDGE ( 'NONE', *, *, #21878, .T. ) ;
#15940=FACE_OUTER_BOUND ( 'NONE', #36114, .T. ) ;
#15945=CARTESIAN_POINT ( 'NONE',  ( -0.8759842519685039353, -0.1574803149606299191, 0.5807086613097960370 ) ) ;
#15946=CARTESIAN_POINT ( 'NONE',  ( 0.7495606340400177148, 0.1264236179284866091, 1.572342519631275692 ) ) ;
#15947=CARTESIAN_POINT ( 'NONE',  ( -0.8759842519685039353, -0.1574803149606299191, 1.220472440944881942 ) ) ;
#15948=EDGE_CURVE ( 'NONE', #20413, #42967, #7667, .T. ) ;
#15950=DIRECTION ( 'NONE',  ( 1.822029033848725028E-16, 0.000000000000000000, 1.000000000000000000 ) ) ;
#15951=CARTESIAN_POINT ( 'NONE',  ( -0.7185039370078739607, 1.928577636452523993E-17, 0.7677165353255432922 ) ) ;
#15952=CARTESIAN_POINT ( 'NONE',  ( -0.7185039370078739607, 1.928577636452523993E-17, 0.4921259841444416971 ) ) ;
#15954=CARTESIAN_POINT ( 'NONE',  ( 0.7185039370078746268, -0.06523048226347956391, 1.478838582569637294 ) ) ;
#15956=ORIENTED_EDGE ( 'NONE', *, *, #5961, .F. ) ;
#15958=( BOUNDED_CURVE ( )  B_SPLINE_CURVE ( 2, ( #38969, #35637, #6134, #20758, #2544, #38752, #20291, #34934, #42329 ),
 .UNSPECIFIED., .F., .T. ) 
 B_SPLINE_CURVE_WITH_KNOTS ( ( 3, 2, 2, 2, 3 ),
 ( 0.02000000000000000042, 0.02249999999999999917, 0.02500000000000000139, 0.02750000000000000014, 0.02999999999999999889 ),
 .UNSPECIFIED. ) 
 CURVE ( )  GEOMETRIC_REPRESENTATION_ITEM ( )  RATIONAL_B_SPLINE_CURVE ( ( 1.000000000000000000, 0.9238795325112869605, 1.000000000000000000, 0.9238795325112869605, 1.000000000000000000, 0.9238795325112869605, 1.000000000000000000, 0.9238795325112869605, 1.000000000000000000 ) ) 
 REPRESENTATION_ITEM ( '' )  ) ;
#15959=CARTESIAN_POINT ( 'NONE',  ( 0.9873396505805591694, -0.1113553986120547346, 0.5954724409448819422 ) ) ;
#15960=CARTESIAN_POINT ( 'NONE',  ( 0.8759842519685039353, 0.1787899950787401882, 0.9817913385289134265 ) ) ;
#15962=CARTESIAN_POINT ( 'NONE',  ( -0.8019270111902717657, -0.1787899950787401604, 1.274606299158834277 ) ) ;
#15964=CARTESIAN_POINT ( 'NONE',  ( 0.8759842519685039353, 0.1574803149606299191, 1.860236220364913207 ) ) ;
#15965=LINE ( 'NONE', #8986, #26754 ) ;
#15970=VERTEX_POINT ( 'NONE', #1904 ) ;
#15977=CARTESIAN_POINT ( 'NONE',  ( -1.054774247047244540, 0.07405724077823318263, 0.1476377952218269340 ) ) ;
#15978=CARTESIAN_POINT ( 'NONE',  ( -0.7185039370078746268, 0.06523048226347956391, 0.9325787401574799906 ) ) ;
#15981=CARTESIAN_POINT ( 'NONE',  ( 0.7646288533564489232, -0.1113553986120547346, 1.097440944881889813 ) ) ;
#15982=CARTESIAN_POINT ( 'NONE',  ( 1.054774247047244540, 0.07405724077823318263, 0.8956692912848198684 ) ) ;
#15984=CARTESIAN_POINT ( 'NONE',  ( 0.8107537697050253289, 0.1574803149606300301, 1.557578740157481212 ) ) ;
#15985=CARTESIAN_POINT ( 'NONE',  ( 0.7100035458928386500, 0.0008589249953504293073, 1.983251210439181067 ) ) ;
#15987=CARTESIAN_POINT ( 'NONE',  ( -0.8759842519685039353, 0.000000000000000000, 0.000000000000000000 ) ) ;
#15988=CARTESIAN_POINT ( 'NONE',  ( -1.033464566929133799, 0.000000000000000000, 1.614173228238929170 ) ) ;
#15991=CARTESIAN_POINT ( 'NONE',  ( 0.9500414927467377701, -0.1787899950787401604, 0.9596456692375763264 ) ) ;
#15992=CARTESIAN_POINT ( 'NONE',  ( 1.054774247047244096, 0.000000000000000000, 1.877460629867496067 ) ) ;
#15994=CARTESIAN_POINT ( 'NONE',  ( 0.7646288533564489232, 0.1113553986120547346, 0.4084645668216063119 ) ) ;
#15996=CARTESIAN_POINT ( 'NONE',  ( 0.7185039370078739607, 1.928577636452523993E-17, 1.092519685039370136 ) ) ;
#15998=CARTESIAN_POINT ( 'NONE',  ( -1.033464566929134687, -0.06523048226347956391, 0.1156496061916856694 ) ) ;
#15999=DIRECTION ( 'NONE',  ( -1.000000000000000000, 0.000000000000000000, 0.000000000000000000 ) ) ;
#16000=CARTESIAN_POINT ( 'NONE',  ( 1.002407869896990045, 0.1264236179284866091, 1.129429133804503937 ) ) ;
#16007=CARTESIAN_POINT ( 'NONE',  ( -1.002407869896990045, 0.1264236179284866091, 0.2632874015210397434 ) ) ;
#16011=CARTESIAN_POINT ( 'NONE',  ( -0.6971942568897648851, -0.07405724077823297447, 1.894685039316315489 ) ) ;
#16013=CARTESIAN_POINT ( 'NONE',  ( -1.002407869896990045, 0.1264236179284866091, 0.5437992125446614589 ) ) ;
#16024=CARTESIAN_POINT ( 'NONE',  ( -0.6971942568897637749, 2.189545951927499583E-17, 0.4749015747493858242 ) ) ;
#16025=CARTESIAN_POINT ( 'NONE',  ( -0.9412147342319837628, -0.1574803149606297803, 0.3961614173228344415 ) ) ;
#16027=CARTESIAN_POINT ( 'NONE',  ( -0.6971942568897648851, 0.07405724077823318263, 1.579724409395055318 ) ) ;
#16033=CARTESIAN_POINT ( 'NONE',  ( -0.9412147342319837628, -0.1574803149606297803, 1.291830708553889817 ) ) ;
#16034=ADVANCED_FACE ( 'NONE', ( #28512 ), #39958, .T. ) ;
#16035=CARTESIAN_POINT ( 'NONE',  ( 1.054774247047244540, 0.07405724077823318263, 0.5413385826234012876 ) ) ;
#16037=CARTESIAN_POINT ( 'NONE',  ( 0.9873396505805591694, -0.1113553986120547346, 1.766732283357039135 ) ) ;
#16038=CARTESIAN_POINT ( 'NONE',  ( -0.7646288533564489232, 0.1113553986120547346, 0.4183070866141732624 ) ) ;
#16040=DIRECTION ( 'NONE',  ( 0.000000000000000000, 0.000000000000000000, -1.000000000000000000 ) ) ;
#16041=CARTESIAN_POINT ( 'NONE',  ( 0.7646288533564489232, -0.1113553986120547346, 1.058070866141732402 ) ) ;
#16047=DIRECTION ( 'NONE',  ( 0.000000000000000000, 0.000000000000000000, -1.000000000000000000 ) ) ;
#16050=ORIENTED_EDGE ( 'NONE', *, *, #23236, .T. ) ;
#16052=CARTESIAN_POINT ( 'NONE',  ( 0.7185039370078746268, -0.06523048226347956391, 0.8587598425196851792 ) ) ;
#16053=CARTESIAN_POINT ( 'NONE',  ( -1.033464566929134687, 0.06523048226347956391, 1.114665354330708125 ) ) ;
#16054=ORIENTED_EDGE ( 'NONE', *, *, #45091, .T. ) ;
#16055=CARTESIAN_POINT ( 'NONE',  ( 0.7185039370078739607, 1.928577636452523993E-17, 1.289370078740157632 ) ) ;
#16056=CARTESIAN_POINT ( 'NONE',  ( 1.033464566929133799, 0.000000000000000000, 1.505905511811023612 ) ) ;
#16060=CARTESIAN_POINT ( 'NONE',  ( 0.7185039370078739607, 1.928577636452523993E-17, 1.082677165246803241 ) ) ;
#16061=CARTESIAN_POINT ( 'NONE',  ( -0.8107537697050254399, -0.1574803149606297803, 1.651082677165354839 ) ) ;
#16062=CARTESIAN_POINT ( 'NONE',  ( -0.6971942568897635528, 0.03556354040785144471, 0.04064907247438850901 ) ) ;
#16066=CARTESIAN_POINT ( 'NONE',  ( 0.9500414927467378812, -0.1787899950787401604, 1.870078740103715331 ) ) ;
#16067=ORIENTED_EDGE ( 'NONE', *, *, #38250, .T. ) ;
#16070=CARTESIAN_POINT ( 'NONE',  ( 0.9500414927467378812, -0.1787899950787401604, 0.4527559054580477249 ) ) ;
#16071=CARTESIAN_POINT ( 'NONE',  ( -0.7495606340400177148, -0.1264236179284866091, 1.385334645615527549 ) ) ;
#16072=CARTESIAN_POINT ( 'NONE',  ( -1.033464566929133799, 0.000000000000000000, 0.4035433070866141780 ) ) ;
#16073=CARTESIAN_POINT ( 'NONE',  ( -1.002407869896990045, 0.1264236179284866091, 1.405019684985606476 ) ) ;
#16074=CARTESIAN_POINT ( 'NONE',  ( -1.054774247047244540, 0.07405724077823318263, 0.06889763774151215492 ) ) ;
#16076=CARTESIAN_POINT ( 'NONE',  ( -0.8759842519685039353, -0.1787899950787401882, 1.670767716481669440 ) ) ;
#16077=CARTESIAN_POINT ( 'NONE',  ( -0.7495606340400177148, 0.1264236179284866091, 0.1205708660879689087 ) ) ;
#16078=CARTESIAN_POINT ( 'NONE',  ( -0.9873396505805591694, 0.1113553986120547346, 1.707677165354330562 ) ) ;
#16079=CARTESIAN_POINT ( 'NONE',  ( -0.7646288533564489232, 0.1113553986120547346, 0.3001968503937008093 ) ) ;
#16080=CARTESIAN_POINT ( 'NONE',  ( 1.054774247047244540, 0.07405724077823318263, 1.564960629867495845 ) ) ;
#16082=DIRECTION ( 'NONE',  ( 1.000000000000000000, 0.000000000000000000, -1.822029033848725275E-16 ) ) ;
#16083=CARTESIAN_POINT ( 'NONE',  ( 0.9873396505805591694, 0.1113553986120547346, 0.2805118109160948947 ) ) ;
#16085=ORIENTED_EDGE ( 'NONE', *, *, #18503, .T. ) ;
#16092=CYLINDRICAL_SURFACE ( 'NONE', #20965, 0.1574803149606299191 ) ;
#16093=CARTESIAN_POINT ( 'NONE',  ( 0.6971942568897637749, 2.189545951927499583E-17, 1.852854330654897685 ) ) ;
#16095=EDGE_CURVE ( 'NONE', #12054, #23661, #4009, .T. ) ;
#16098=CARTESIAN_POINT ( 'NONE',  ( -0.8107537697050254399, -0.1574803149606297803, 0.8932086613097963701 ) ) ;
#16099=CARTESIAN_POINT ( 'NONE',  ( 0.9500414927467378812, -0.1787899950787401604, 0.9990157479777320715 ) ) ;
#16100=AXIS2_PLACEMENT_3D ( 'NONE', #19806, #45430, #12649 ) ;
#16102=CARTESIAN_POINT ( 'NONE',  ( 0.7185039370078739607, 1.928577636452523993E-17, 1.250000000000000000 ) ) ;
#16103=CARTESIAN_POINT ( 'NONE',  ( 1.033464566929134687, 0.06523048226347956391, 0.04183070855389029591 ) ) ;
#16110=CARTESIAN_POINT ( 'NONE',  ( -1.002407869896990045, -0.1264236179284866091, 1.710137795221826851 ) ) ;
#16112=CARTESIAN_POINT ( 'NONE',  ( -0.8019270111902717657, 0.1787899950787401604, 1.377952755851748146 ) ) ;
#16113=CARTESIAN_POINT ( 'NONE',  ( -0.8759842519685039353, 0.000000000000000000, 4.498031496062992574 ) ) ;
#16115=CARTESIAN_POINT ( 'NONE',  ( 0.9500414927467378812, -0.1787899950787401604, 1.358267716481669662 ) ) ;
#16116=CARTESIAN_POINT ( 'NONE',  ( 0.7495606340400177148, 0.1264236179284866091, 0.08120078734781142893 ) ) ;
#16117=CARTESIAN_POINT ( 'NONE',  ( -0.9500414927467378812, -0.1787899950787401604, 1.195866141678520345 ) ) ;
#16121=CARTESIAN_POINT ( 'NONE',  ( 0.7495606340400177148, -0.1264236179284866091, 0.4060039369541102450 ) ) ;
#16122=CARTESIAN_POINT ( 'NONE',  ( -0.6971942568897648851, -0.07405724077823297447, 0.3986220471903311746 ) ) ;
#16126=CARTESIAN_POINT ( 'NONE',  ( -0.9412147342319837628, -0.1574803149606297803, 0.2780511811023620439 ) ) ;
#16127=CARTESIAN_POINT ( 'NONE',  ( 0.7185039370078692977, 0.06523048226347515077, 1.946358267609008097 ) ) ;
#16128=CARTESIAN_POINT ( 'NONE',  ( 0.7185039370078739607, 1.928577636452523993E-17, 1.279527558947590515 ) ) ;
#16130=CARTESIAN_POINT ( 'NONE',  ( 1.054774247047244540, -0.07405724077823318263, 1.988188976324187562 ) ) ;
#16131=CARTESIAN_POINT ( 'NONE',  ( -0.8019270111902717657, -0.1787899950787401604, 1.038385826717890259 ) ) ;
#16134=CARTESIAN_POINT ( 'NONE',  ( -0.6971942568897626646, -0.07405724077823297447, 0.04429133852891373180 ) ) ;
#16135=ORIENTED_EDGE ( 'NONE', *, *, #42244, .F. ) ;
#16136=CARTESIAN_POINT ( 'NONE',  ( -0.7646288533564489232, 0.1113553986120547346, 0.1722440943806619884 ) ) ;
#16139=VERTEX_POINT ( 'NONE', #21524 ) ;
#16140=EDGE_CURVE ( 'NONE', #4083, #19285, #38315, .T. ) ;
#16141=CARTESIAN_POINT ( 'NONE',  ( 0.8107537697050254399, 0.1574803149606300301, 1.468996062884598830 ) ) ;
#16142=CARTESIAN_POINT ( 'NONE',  ( 0.8107537697050254399, -0.1574803149606297803, 0.7357283463491665065 ) ) ;
#16144=DIRECTION ( 'NONE',  ( 1.000000000000000000, 0.000000000000000000, -1.822029033848725275E-16 ) ) ;
#16145=CARTESIAN_POINT ( 'NONE',  ( 0.7495606340400177148, 0.1264236179284866091, 1.651082677111590513 ) ) ;
#16148=CYLINDRICAL_SURFACE ( 'NONE', #27266, 0.1574803149606299191 ) ;
#16149=EDGE_CURVE ( 'NONE', #39085, #17112, #43198, .T. ) ;
#16150=CARTESIAN_POINT ( 'NONE',  ( -0.7495606340400177148, -0.1264236179284866091, 0.6422244093950550958 ) ) ;
#16152=CARTESIAN_POINT ( 'NONE',  ( 1.033464566929133799, 0.000000000000000000, 0.9842519683964094934 ) ) ;
#16154=CARTESIAN_POINT ( 'NONE',  ( 0.5314960629921260393, -1.928577636452524610E-17, 4.498031496062992574 ) ) ;
#16156=CARTESIAN_POINT ( 'NONE',  ( 0.9500414927467378812, 0.1787899950787401604, 1.569881889710015299 ) ) ;
#16157=CARTESIAN_POINT ( 'NONE',  ( 0.7495606340400177148, 0.1264236179284866091, 1.808562992072220377 ) ) ;
#16158=CARTESIAN_POINT ( 'NONE',  ( 0.8019270111902716547, -0.1787899950787401604, 0.2854330708123783977 ) ) ;
#16162=DIRECTION ( 'NONE',  ( -1.000000000000000000, 0.000000000000000000, 0.000000000000000000 ) ) ;
#16164=CARTESIAN_POINT ( 'NONE',  ( 1.002407869896990045, 0.1264236179284866091, 0.4995078739619842612 ) ) ;
#16166=AXIS2_PLACEMENT_3D ( 'NONE', #30911, #45952, #2110 ) ;
#16167=CARTESIAN_POINT ( 'NONE',  ( 0.7185039370078739607, 0.000000000000000000, 4.498031496062992574 ) ) ;
#16168=CARTESIAN_POINT ( 'NONE',  ( -1.002407869896990045, -0.1264236179284866091, 1.316437007820252081 ) ) ;
#16169=CARTESIAN_POINT ( 'NONE',  ( 0.7185039370078746268, -0.06523048226347956391, 0.8095472439869610959 ) ) ;
#16172=CARTESIAN_POINT ( 'NONE',  ( 0.6971942568897637749, 2.189545951927499583E-17, 1.031003936954110189 ) ) ;
#16173=EDGE_LOOP ( 'NONE', ( #25575, #23822, #39678, #5013 ) ) ;
#16175=CARTESIAN_POINT ( 'NONE',  ( -0.8107537697050253289, 0.1574803149606300301, 0.5634842518609766149 ) ) ;
#16177=CARTESIAN_POINT ( 'NONE',  ( -0.7185039370078739607, 1.928577636452523993E-17, 0.8169291338582678197 ) ) ;
#16178=CARTESIAN_POINT ( 'NONE',  ( 0.8019270111902717657, 0.1787899950787401604, 1.727362204670645385 ) ) ;
#16179=CARTESIAN_POINT ( 'NONE',  ( -1.033464566929133799, 0.000000000000000000, 1.309055118110236338 ) ) ;
#16181=CARTESIAN_POINT ( 'NONE',  ( -0.8107537697050254399, 0.1574803149606300301, 0.7308070866141727073 ) ) ;
#16183=CARTESIAN_POINT ( 'NONE',  ( -0.8107537697050254399, -0.1574803149606297803, 0.4995078739082208230 ) ) ;
#16185=CARTESIAN_POINT ( 'NONE',  ( 1.033464566929133799, 0.000000000000000000, 1.338582677057826853 ) ) ;
#16186=ORIENTED_EDGE ( 'NONE', *, *, #22560, .T. ) ;
#16187=VERTEX_POINT ( 'NONE', #19103 ) ;
#16191=CARTESIAN_POINT ( 'NONE',  ( -1.002407869896990045, 0.1264236179284866091, 1.488681102308440751 ) ) ;
#16192=CARTESIAN_POINT ( 'NONE',  ( 0.9873396505805591694, 0.1113553986120547346, 1.855314960522393530 ) ) ;
#16193=CARTESIAN_POINT ( 'NONE',  ( -1.033464566929136907, -0.06523048226347749612, 1.887303149498772425 ) ) ;
#16195=ORIENTED_EDGE ( 'NONE', *, *, #15224, .T. ) ;
#16198=VERTEX_POINT ( 'NONE', #15783 ) ;
#16200=DIRECTION ( 'NONE',  ( 0.000000000000000000, 0.000000000000000000, -1.000000000000000000 ) ) ;
#16201=CARTESIAN_POINT ( 'NONE',  ( 1.033464566929133799, 0.000000000000000000, 0.1181102361129454797 ) ) ;
#16202=( BOUNDED_CURVE ( )  B_SPLINE_CURVE ( 2, ( #45124, #9449, #16628, #37724, #24063 ),
 .UNSPECIFIED., .F., .F. ) 
 B_SPLINE_CURVE_WITH_KNOTS ( ( 3, 2, 3 ),
 ( 0.9799999999999999822, 0.9825000000000000400, 0.9850000000591240257 ),
 .UNSPECIFIED. ) 
 CURVE ( )  GEOMETRIC_REPRESENTATION_ITEM ( )  RATIONAL_B_SPLINE_CURVE ( ( 1.000000000000000000, 0.9238795325112869605, 1.000000000000000000, 0.9238795325112869605, 1.000000000000000000 ) ) 
 REPRESENTATION_ITEM ( '' )  ) ;
#16203=EDGE_CURVE ( 'NONE', #30928, #44478, #37311, .T. ) ;
#16204=AXIS2_PLACEMENT_3D ( 'NONE', #2562, #17195, #46416 ) ;
#16205=CARTESIAN_POINT ( 'NONE',  ( 0.9873396505805591694, -0.1113553986120547346, 1.776574803149606252 ) ) ;
#16209=EDGE_CURVE ( 'NONE', #398, #7779, #3787, .T. ) ;
#16211=CARTESIAN_POINT ( 'NONE',  ( -1.002407869896990045, 0.1264236179284866091, 0.1894685038832444879 ) ) ;
#16214=CARTESIAN_POINT ( 'NONE',  ( -1.033464566929133799, 0.000000000000000000, 1.033464566929133799 ) ) ;
#16215=CARTESIAN_POINT ( 'NONE',  ( 0.7495606340400177148, -0.1264236179284866091, 1.035925196796629866 ) ) ;
#16216=CARTESIAN_POINT ( 'NONE',  ( 1.054774247047244096, 0.000000000000000000, 0.1402559054580474474 ) ) ;
#16218=CARTESIAN_POINT ( 'NONE',  ( 1.033464566929134687, 0.06523048226347956391, 1.547736220472440749 ) ) ;
#16219=CARTESIAN_POINT ( 'NONE',  ( 0.7599549351170132860, 0.1127937001634502223, 1.980848792121916668 ) ) ;
#16220=CARTESIAN_POINT ( 'NONE',  ( -0.7185039370078739607, 0.000000000000000000, -2.869337061179095023E-17 ) ) ;
#16221=DIRECTION ( 'NONE',  ( 1.822029033848725028E-16, 0.000000000000000000, 1.000000000000000000 ) ) ;
#16222=( BOUNDED_CURVE ( )  B_SPLINE_CURVE ( 2, ( #21466, #10950, #25570, #3256, #3508, #11190, #4191, #14303, #18819 ),
 .UNSPECIFIED., .F., .F. ) 
 B_SPLINE_CURVE_WITH_KNOTS ( ( 3, 2, 2, 2, 3 ),
 ( 0.3800000000000000044, 0.3825000000000000067, 0.3850000000000000089, 0.3875000000000000111, 0.3900000000000000133 ),
 .UNSPECIFIED. ) 
 CURVE ( )  GEOMETRIC_REPRESENTATION_ITEM ( )  RATIONAL_B_SPLINE_CURVE ( ( 1.000000000000000000, 0.9238795325112869605, 1.000000000000000000, 0.9238795325112869605, 1.000000000000000000, 0.9238795325112869605, 1.000000000000000000, 0.9238795325112869605, 1.000000000000000000 ) ) 
 REPRESENTATION_ITEM ( '' )  ) ;
#16224=CARTESIAN_POINT ( 'NONE',  ( 0.6971942568897648851, -0.07405724077823297447, 1.028543307032851573 ) ) ;
#16225=CARTESIAN_POINT ( 'NONE',  ( 1.054774247047244096, 0.000000000000000000, 1.759350393647023614 ) ) ;
#16226=CARTESIAN_POINT ( 'NONE',  ( 1.033464566929133799, 0.000000000000000000, 0.3149606298137326843 ) ) ;
#16227=ORIENTED_EDGE ( 'NONE', *, *, #39049, .F. ) ;
#16228=CARTESIAN_POINT ( 'NONE',  ( 1.033464566929133799, 0.000000000000000000, 1.614173228238929170 ) ) ;
#16230=CARTESIAN_POINT ( 'NONE',  ( -1.033464566929133799, 0.000000000000000000, 0.1968503935932602311 ) ) ;
#16231=CARTESIAN_POINT ( 'NONE',  ( 0.8019270111902717657, -0.1787899950787401604, 1.230314960576156746 ) ) ;
#16232=AXIS2_PLACEMENT_3D ( 'NONE', #31007, #13268, #23566 ) ;
#16237=CARTESIAN_POINT ( 'NONE',  ( -0.6971942568897637749, -2.189545951927502049E-17, 1.978346456692913646 ) ) ;
#16239=CARTESIAN_POINT ( 'NONE',  ( -1.002407869896990045, -0.1264236179284866091, 0.6077755904974173617 ) ) ;
#16245=CARTESIAN_POINT ( 'NONE',  ( -1.054774247047244540, 0.07405724077823318263, 1.756889763725764553 ) ) ;
#16247=CARTESIAN_POINT ( 'NONE',  ( -0.8759842519685039353, 0.1787899950787401882, 1.016240157426551161 ) ) ;
#16254=CARTESIAN_POINT ( 'NONE',  ( -0.7495606340400177148, -0.1264236179284866091, 0.5191929133320630774 ) ) ;
#16256=EDGE_CURVE ( 'NONE', #42055, #16808, #376, .T. ) ;
#16258=CARTESIAN_POINT ( 'NONE',  ( -0.8019270111902716547, -0.1787899950787401604, 1.510826771599780294 ) ) ;
#16263=AXIS2_PLACEMENT_3D ( 'NONE', #42316, #6118, #20743 ) ;
#16264=CARTESIAN_POINT ( 'NONE',  ( 1.033464566929134687, 0.06523048226347956391, 1.026082677057828185 ) ) ;
#16266=CARTESIAN_POINT ( 'NONE',  ( 0.8759842519685039353, 0.1574803149606299191, 0.4921259842519685179 ) ) ;
#16268=CARTESIAN_POINT ( 'NONE',  ( -1.033464566929133799, 0.000000000000000000, 1.653543306979086580 ) ) ;
#16269=CARTESIAN_POINT ( 'NONE',  ( -0.9873396505805591694, -0.1113553986120547346, 1.254921259734991912 ) ) ;
#16270=CARTESIAN_POINT ( 'NONE',  ( 1.002407869896990045, 0.1264236179284866091, 0.5831692912848189803 ) ) ;
#16277=CARTESIAN_POINT ( 'NONE',  ( 0.9412147342319837628, 0.1574803149606300301, 1.582185039262551607 ) ) ;
#16278=CARTESIAN_POINT ( 'NONE',  ( 1.033464566929134687, 0.06523048226347956391, 1.114665354330708125 ) ) ;
#16279=CARTESIAN_POINT ( 'NONE',  ( -0.9263122037349271753, -0.1687466150977034174, 1.989089231315331885 ) ) ;
#16280=CARTESIAN_POINT ( 'NONE',  ( 0.8107537697050254399, 0.1574803149606300301, 0.1796259842519686567 ) ) ;
#16281=CARTESIAN_POINT ( 'NONE',  ( -0.7185039370078778465, -0.06523048226348396317, 1.951279527451527329 ) ) ;
#16286=CARTESIAN_POINT ( 'NONE',  ( 0.7495606340400177148, 0.1264236179284866091, 0.7062007873478109987 ) ) ;
#16287=ORIENTED_EDGE ( 'NONE', *, *, #6443, .F. ) ;
#16288=CARTESIAN_POINT ( 'NONE',  ( -0.8759842519685039353, 0.000000000000000000, 0.000000000000000000 ) ) ;
#16289=CARTESIAN_POINT ( 'NONE',  ( 0.9873396505805591694, -0.1113553986120547346, 0.9104330708661417804 ) ) ;
#16293=CARTESIAN_POINT ( 'NONE',  ( 1.033464566929134687, -0.06523048226347956391, 1.296751968396409049 ) ) ;
#16298=CARTESIAN_POINT ( 'NONE',  ( -1.002407869896990045, -0.1264236179284866091, 1.715059055064346527 ) ) ;
#16299=CARTESIAN_POINT ( 'NONE',  ( 0.8019270111902717657, 0.1787899950787401604, 1.850393700733638624 ) ) ;
#16303=CARTESIAN_POINT ( 'NONE',  ( 1.002407869896990045, -0.1264236179284866091, 0.4552165353793071745 ) ) ;
#16304=CARTESIAN_POINT ( 'NONE',  ( -0.7495606340400177148, -0.1264236179284866091, 1.345964566875370139 ) ) ;
#16306=CARTESIAN_POINT ( 'NONE',  ( -1.002407869896990045, -0.1264236179284866091, 0.9227362204186770889 ) ) ;
#16307=CARTESIAN_POINT ( 'NONE',  ( -0.9500414927467378812, 0.1787899950787401604, 0.03444881884387430981 ) ) ;
#16309=CARTESIAN_POINT ( 'NONE',  ( 0.6971942568897643300, 0.000000000000000000, 1.995570866087968520 ) ) ;
#16310=CARTESIAN_POINT ( 'NONE',  ( -1.002407869896990045, -0.1264236179284866091, 1.793799212544661348 ) ) ;
#16311=CARTESIAN_POINT ( 'NONE',  ( -0.7495606340400177148, 0.1264236179284866091, 0.08120078734781142893 ) ) ;
#16313=CARTESIAN_POINT ( 'NONE',  ( -0.7185039370078746268, 0.06523048226347956391, 1.719980314960629864 ) ) ;
#16314=DIRECTION ( 'NONE',  ( 0.000000000000000000, 0.000000000000000000, -1.000000000000000000 ) ) ;
#16317=CARTESIAN_POINT ( 'NONE',  ( 0.7185039370078746268, -0.06523048226347956391, 1.006397637687749258 ) ) ;
#16318=CARTESIAN_POINT ( 'NONE',  ( -0.9873396505805591694, 0.1113553986120547346, 1.786417322834645605 ) ) ;
#16323=ORIENTED_EDGE ( 'NONE', *, *, #3852, .T. ) ;
#16327=CARTESIAN_POINT ( 'NONE',  ( -0.9873396505805591694, -0.1113553986120547346, 0.5954724409448819422 ) ) ;
#16330=CARTESIAN_POINT ( 'NONE',  ( -0.9873396505805591694, -0.1113553986120547346, 0.8218503935932598425 ) ) ;
#16331=B_SPLINE_CURVE_WITH_KNOTS ( 'NONE', 3,
 ( #28973, #18146, #29460, #3986, #39688, #47384, #32316, #18380, #32789, #14801, #146, #21259, #46894, #39936, #10259, #36600, #7365, #28730, #33022, #43530, #44005, #21747, #14085, #25593, #36378, #43774, #25821, #3758, #18607, #14328, #10500, #47144, #33266, #43300, #25098, #10977, #40165, #17668, #11208, #40399, #7585, #21495, #10745, #14556, #6875, #22199, #25354, #13838, #7124, #36835, #36129, #3284, #21977, #17906, #3535, #29227, #28482, #43053, #24863, #39465, #6640, #35884, #3037, #27015, #18841, #15511, #15751, #33967, #34201, #4212, #1328, #12394, #30386, #40861, #41561, #5168, #8056, #45172, #11912, #19318, #37530, #44465, #29691, #26055, #23404, #11678, #22439, #390, #41328, #1094, #44932, #26303, #37059, #30155, #33496, #15985, #37777, #26534, #12147, #15268, #29919, #23158, #19069, #40626, #44694, #33740, #22682, #851, #30607, #8768, #37284, #41094, #26770, #8529, #38007, #4438, #15041, #44232, #4930, #8289, #11438, #7822, #22917, #4688, #19554, #27255, #42297, #31080, #16219, #12630, #9955, #45644, #9006, #39167, #27955, #20496, #35137, #12861, #23631, #16682, #38241, #38478, #23866, #28179, #42523, #20023, #27494, #1566, #27732, #5399, #20724, #2047, #30849, #6338 ),
 .UNSPECIFIED., .F., .F.,
 ( 4, 2, 2, 2, 2, 1, 1, 1, 2, 2, 2, 2, 2, 1, 1, 1, 1, 2, 2, 2, 2, 2, 1, 1, 2, 2, 2, 2, 2, 1, 1, 2, 2, 2, 2, 1, 1, 1, 1, 2, 2, 2, 2, 2, 1, 2, 2, 2, 2, 2, 1, 1, 2, 2, 2, 2, 2, 2, 1, 1, 2, 2, 2, 2, 1, 1, 2, 2, 2, 2, 1, 2, 2, 2, 2, 1, 2, 2, 2, 2, 2, 2, 1, 1, 2, 2, 2, 2, 2, 4 ),
 ( 0.000000000000000000, 0.06249999999999325540, 0.09374999999998989697, 0.1093749999999879818, 0.1171874999999868022, 0.1210937499999859834, 0.1230468749999855532, 0.1240234374999851508, 0.1245117187499849426, 0.1249999999999847344, 0.1874999999999227007, 0.2187499999998916977, 0.2343749999998764877, 0.2421874999998691880, 0.2460937499998655520, 0.2480468749998637756, 0.2490234374998628597, 0.2495117187498623879, 0.2499999999998619160, 0.2812499999998631650, 0.2968749999998637756, 0.3046874999998641087, 0.3085937499998644418, 0.3105468749998647748, 0.3115234374998647748, 0.3124999999998648303, 0.3437499999998624989, 0.3593749999998612776, 0.3671874999998610001, 0.3710937499998608891, 0.3730468749998611111, 0.3740234374998612221, 0.3749999999998613331, 0.4062499999998746558, 0.4218749999998813172, 0.4296874999998846478, 0.4335937499998864242, 0.4355468749998873124, 0.4365234374998879230, 0.4370117187498884226, 0.4374999999998889777, 0.4687499999998933076, 0.4843749999998955835, 0.4921874999998967493, 0.4960937499998973599, 0.4980468749998976374, 0.4999999999998979150, 0.5312499999999020783, 0.5468749999999039657, 0.5546874999999050759, 0.5585937499999054090, 0.5605468749999055200, 0.5615234374999057421, 0.5624999999999059641, 0.5937499999999119593, 0.6093749999999149569, 0.6171874999999164002, 0.6210937499999171774, 0.6230468749999175104, 0.6240234374999177325, 0.6245117187499178435, 0.6249999999999179545, 0.6562499999999251710, 0.6718749999999289457, 0.6796874999999307221, 0.6835937499999317213, 0.6855468749999321654, 0.6874999999999326095, 0.7187499999999397149, 0.7343749999999433786, 0.7421874999999452660, 0.7460937499999461542, 0.7499999999999470424, 0.7812499999999529265, 0.7968749999999555911, 0.8046874999999568123, 0.8085937499999573674, 0.8105468749999575895, 0.8115234374999577005, 0.8124999999999578115, 0.8437499999999675815, 0.8593749999999722444, 0.8671874999999742428, 0.8710937499999750200, 0.8730468749999753530, 0.8749999999999756861, 0.9062499999999810152, 0.9218749999999840128, 0.9374999999999870104, 1.000000000000000000 ),
 .UNSPECIFIED. ) ;
#16333=CARTESIAN_POINT ( 'NONE',  ( 0.6971942568897626646, -0.07405724077823297447, 0.9498031495525356416 ) ) ;
#16334=( BOUNDED_CURVE ( )  B_SPLINE_CURVE ( 2, ( #11146, #32001, #46594, #13774, #25989, #22144, #11852, #33438, #33676 ),
 .UNSPECIFIED., .F., .T. ) 
 B_SPLINE_CURVE_WITH_KNOTS ( ( 3, 2, 2, 2, 3 ),
 ( 0.4299999999999999933, 0.4324999999999999956, 0.4349999999999999978, 0.4375000000000000000, 0.4400000000000000022 ),
 .UNSPECIFIED. ) 
 CURVE ( )  GEOMETRIC_REPRESENTATION_ITEM ( )  RATIONAL_B_SPLINE_CURVE ( ( 1.000000000000000000, 0.9238795325112869605, 1.000000000000000000, 0.9238795325112869605, 1.000000000000000000, 0.9238795325112869605, 1.000000000000000000, 0.9238795325112869605, 1.000000000000000000 ) ) 
 REPRESENTATION_ITEM ( '' )  ) ;
#16337=CARTESIAN_POINT ( 'NONE',  ( 1.054774247047244540, 0.07405724077823318263, 1.919291338528913871 ) ) ;
#16340=DIRECTION ( 'NONE',  ( 0.000000000000000000, 0.000000000000000000, -1.000000000000000000 ) ) ;
#16344=CARTESIAN_POINT ( 'NONE',  ( 0.6971942568897626646, -0.07405724077823297447, 0.3248031495525359746 ) ) ;
#16345=CARTESIAN_POINT ( 'NONE',  ( -0.8019270111902717657, -0.1787899950787401604, 1.860236220418677089 ) ) ;
#16347=CARTESIAN_POINT ( 'NONE',  ( -0.9500414927467378812, 0.1787899950787401604, 1.294291338528912982 ) ) ;
#16348=CYLINDRICAL_SURFACE ( 'NONE', #31463, 0.1574803149606299191 ) ;
#16349=CARTESIAN_POINT ( 'NONE',  ( -1.054774247047244096, 0.000000000000000000, 1.281988188922614125 ) ) ;
#16352=CARTESIAN_POINT ( 'NONE',  ( -1.033464566929133799, 0.000000000000000000, 0.9547244094488189781 ) ) ;
#16353=CARTESIAN_POINT ( 'NONE',  ( 0.7495606340400177148, 0.1264236179284866091, 0.6323818897100157432 ) ) ;
#16354=CARTESIAN_POINT ( 'NONE',  ( -0.9500414927467377701, -0.1787899950787401604, 0.5265748030958428139 ) ) ;
#16355=CARTESIAN_POINT ( 'NONE',  ( -0.6971942568897626646, -0.07405724077823297447, 0.8316929133320636325 ) ) ;
#16357=FACE_OUTER_BOUND ( 'NONE', #14325, .T. ) ;
#16359=VERTEX_POINT ( 'NONE', #23191 ) ;
#16361=CARTESIAN_POINT ( 'NONE',  ( -0.9873396505805591694, -0.1113553986120547346, 0.3592519685039369803 ) ) ;
#16365=ORIENTED_EDGE ( 'NONE', *, *, #26695, .F. ) ;
#16366=CARTESIAN_POINT ( 'NONE',  ( -0.7495606340400177148, 0.1264236179284866091, 0.9867125983714331028 ) ) ;
#16367=CARTESIAN_POINT ( 'NONE',  ( -0.7495606340400177148, -0.1264236179284866091, 0.2042322834108035723 ) ) ;
#16369=ORIENTED_EDGE ( 'NONE', *, *, #9535, .T. ) ;
#16373=CARTESIAN_POINT ( 'NONE',  ( 0.8759842519685039353, -0.1787899950787401882, 1.350885826717889815 ) ) ;
#16378=CARTESIAN_POINT ( 'NONE',  ( 0.7185039370078714072, 0.06523048226347728795, 1.877460629921259727 ) ) ;
#16383=CARTESIAN_POINT ( 'NONE',  ( -1.033464566929134687, 0.06523048226347956391, 1.734744094380662904 ) ) ;
#16384=CARTESIAN_POINT ( 'NONE',  ( 0.8019270111902717657, 0.1787899950787401604, 0.4281496062454490659 ) ) ;
#16386=CARTESIAN_POINT ( 'NONE',  ( -0.6971942568897648851, 0.07405724077823318263, 0.7529527558517473684 ) ) ;
#16394=CARTESIAN_POINT ( 'NONE',  ( 0.7495606340400177148, 0.1264236179284866091, 1.459153543253322693 ) ) ;
#16395=CARTESIAN_POINT ( 'NONE',  ( 0.8019270111902716547, -0.1787899950787401604, 1.781496062938362934 ) ) ;
#16396=CARTESIAN_POINT ( 'NONE',  ( 0.8759842519685039353, 0.1787899950787401882, 0.4650590550643464716 ) ) ;
#16398=CARTESIAN_POINT ( 'NONE',  ( -0.7185039370078739607, 1.928577636452523993E-17, 0.5314960628845992741 ) ) ;
#16401=CARTESIAN_POINT ( 'NONE',  ( 0.8019270111902717657, -0.1787899950787401604, 0.4822834645131655606 ) ) ;
#16404=CARTESIAN_POINT ( 'NONE',  ( 0.8759842519685039353, 0.1574803149606299191, 0.2165354330708661457 ) ) ;
#16405=CARTESIAN_POINT ( 'NONE',  ( 0.9412147342319837628, 0.1574803149606300301, 0.8341535431995593664 ) ) ;
#16407=CARTESIAN_POINT ( 'NONE',  ( -0.7185039370078746268, 0.06523048226347956391, 0.8046259841444418637 ) ) ;
#16408=CARTESIAN_POINT ( 'NONE',  ( 0.6971942568897648851, -0.07405724077823297447, 1.072834645615528659 ) ) ;
#16410=EDGE_LOOP ( 'NONE', ( #32697, #31577, #41167, #40348 ) ) ;
#16411=CARTESIAN_POINT ( 'NONE',  ( -0.8107537697050253289, -0.1574803149606297803, 0.4995078739082208230 ) ) ;
#16412=CARTESIAN_POINT ( 'NONE',  ( -0.7646288533564489232, 0.1113553986120547346, 1.284448818897637956 ) ) ;
#16414=CARTESIAN_POINT ( 'NONE',  ( -0.9412147342319837628, 0.1574803149606300301, 1.149114173120819427 ) ) ;
#16416=CARTESIAN_POINT ( 'NONE',  ( 1.002407869896990045, -0.1264236179284866091, 0.1796259841982051075 ) ) ;
#16417=CARTESIAN_POINT ( 'NONE',  ( 0.8759842519685039353, 0.1574803149606299191, 1.427165354223181248 ) ) ;
#16418=ORIENTED_EDGE ( 'NONE', *, *, #33149, .F. ) ;
#16424=CARTESIAN_POINT ( 'NONE',  ( -0.6971942568897648851, 0.07405724077823318263, 1.574803149552536530 ) ) ;
#16428=CARTESIAN_POINT ( 'NONE',  ( -0.9412147342319837628, 0.1574803149606300301, 0.2436023620971973780 ) ) ;
#16430=CARTESIAN_POINT ( 'NONE',  ( 0.8107537697050254399, 0.1574803149606300301, 0.8784448817822366751 ) ) ;
#16435=CARTESIAN_POINT ( 'NONE',  ( -0.7646288533564489232, -0.1113553986120547346, 1.402559055010582645 ) ) ;
#16436=CARTESIAN_POINT ( 'NONE',  ( -0.9412147342319837628, -0.1574803149606297803, 1.459153543307085688 ) ) ;
#16437=CARTESIAN_POINT ( 'NONE',  ( 0.8759842519685039353, -0.1574803149606299191, 1.889763779527559251 ) ) ;
#16440=AXIS2_PLACEMENT_3D ( 'NONE', #37952, #5336, #41744 ) ;
#16442=CARTESIAN_POINT ( 'NONE',  ( -1.054774247047244096, 0.000000000000000000, 0.2239173227808822775 ) ) ;
#16443=CARTESIAN_POINT ( 'NONE',  ( -0.8759842519685039353, 0.1574803149606299191, 1.003937007874015741 ) ) ;
#16446=CARTESIAN_POINT ( 'NONE',  ( 1.002407869896990045, -0.1264236179284866091, 1.006397637741511808 ) ) ;
#16448=CARTESIAN_POINT ( 'NONE',  ( 0.9412147342319837628, -0.1574803149606297803, 1.616633858267715551 ) ) ;
#16452=CYLINDRICAL_SURFACE ( 'NONE', #7727, 0.1574803149606299191 ) ;
#16453=CARTESIAN_POINT ( 'NONE',  ( 0.8019270111902716547, -0.1787899950787401604, 1.033464566875371027 ) ) ;
#16454=CARTESIAN_POINT ( 'NONE',  ( 0.9500414927467377701, -0.1787899950787401604, 1.870078740103715331 ) ) ;
#16455=CARTESIAN_POINT ( 'NONE',  ( 0.9873396505805591694, -0.1113553986120547346, 0.3100393699712130080 ) ) ;
#16456=ORIENTED_EDGE ( 'NONE', *, *, #8155, .F. ) ;
#16459=CARTESIAN_POINT ( 'NONE',  ( -0.9873396505805591694, 0.1113553986120547346, 0.2411417321759374011 ) ) ;
#16460=CARTESIAN_POINT ( 'NONE',  ( 0.8759842519685039353, -0.1787899950787401882, 1.272145669237574772 ) ) ;
#16463=CARTESIAN_POINT ( 'NONE',  ( -0.8759842519685039353, -0.1574803149606299191, 1.013779527451527551 ) ) ;
#16465=CARTESIAN_POINT ( 'NONE',  ( -0.9500414927467378812, 0.1787899950787401604, 0.5807086613635594752 ) ) ;
#16467=CARTESIAN_POINT ( 'NONE',  ( 0.7185039370078739607, 1.928577636452523993E-17, 1.358267716427907779 ) ) ;
#16470=DIRECTION ( 'NONE',  ( 1.822029033848725028E-16, 0.000000000000000000, 1.000000000000000000 ) ) ;
#16475=CARTESIAN_POINT ( 'NONE',  ( -0.9500414927467378812, -0.1787899950787401604, 1.786417322780882388 ) ) ;
#16478=CARTESIAN_POINT ( 'NONE',  ( -0.9500414927467378812, 0.1787899950787401604, 0.6643700786863929730 ) ) ;
#16484=FACE_OUTER_BOUND ( 'NONE', #41476, .T. ) ;
#16486=CARTESIAN_POINT ( 'NONE',  ( -0.7185039370078739607, 1.928577636452523993E-17, 1.751968503829480106 ) ) ;
#16487=CARTESIAN_POINT ( 'NONE',  ( -1.002407869896990045, 0.1264236179284866091, 0.5388779527021417826 ) ) ;
#16489=CARTESIAN_POINT ( 'NONE',  ( -1.054774247047244540, -0.07405724077823318263, 1.599409448765134911 ) ) ;
#16491=VERTEX_POINT ( 'NONE', #40372 ) ;
#16492=EDGE_CURVE ( 'NONE', #22349, #35290, #8450, .T. ) ;
#16493=CARTESIAN_POINT ( 'NONE',  ( -0.7185039370078739607, 1.928577636452523993E-17, 1.122047243986960652 ) ) ;
#16494=( BOUNDED_CURVE ( )  B_SPLINE_CURVE ( 2, ( #40848, #22669, #46050, #30141, #44682, #12134, #13258, #11900, #26521 ),
 .UNSPECIFIED., .F., .F. ) 
 B_SPLINE_CURVE_WITH_KNOTS ( ( 3, 2, 2, 2, 3 ),
 ( 0.6999999999999999556, 0.7025000000000000133, 0.7049999999999999600, 0.7075000000000000178, 0.7099999999999999645 ),
 .UNSPECIFIED. ) 
 CURVE ( )  GEOMETRIC_REPRESENTATION_ITEM ( )  RATIONAL_B_SPLINE_CURVE ( ( 1.000000000000000000, 0.9238795325112899581, 1.000000000000000000, 0.9238795325112869605, 1.000000000000000000, 0.9238795325112869605, 1.000000000000000000, 0.9238795325112799661, 1.000000000000000000 ) ) 
 REPRESENTATION_ITEM ( '' )  ) ;
#16498=DIRECTION ( 'NONE',  ( 0.000000000000000000, 0.000000000000000000, -1.000000000000000000 ) ) ;
#16499=CARTESIAN_POINT ( 'NONE',  ( -0.9412147342319837628, 0.1574803149606300301, 1.267224409341291436 ) ) ;
#16501=CARTESIAN_POINT ( 'NONE',  ( 1.033464566929134687, -0.06523048226347956391, 1.769192913278299084 ) ) ;
#16502=VECTOR ( 'NONE', #34716, 39.37007874015748143 ) ;
#16506=CARTESIAN_POINT ( 'NONE',  ( 0.7185039370078739607, 0.000000000000000000, 4.498031496062992574 ) ) ;
#16507=CARTESIAN_POINT ( 'NONE',  ( 1.033464566929134687, -0.06523048226347956391, 1.070374015748031038 ) ) ;
#16508=CARTESIAN_POINT ( 'NONE',  ( -0.7185039370078714072, 0.06523048226347728795, 1.277066929026331232 ) ) ;
#16509=CARTESIAN_POINT ( 'NONE',  ( -0.8938872902679191323, -0.1741726370573033755, 1.988501741345521712 ) ) ;
#16510=CARTESIAN_POINT ( 'NONE',  ( 1.033464566929133799, 0.000000000000000000, 0.3149606298137326843 ) ) ;
#16511=CARTESIAN_POINT ( 'NONE',  ( 0.9873396505805591694, -0.1113553986120547346, 0.5856299211523157133 ) ) ;
#16513=CARTESIAN_POINT ( 'NONE',  ( 0.9873396505805591694, 0.1113553986120547346, 1.264763779420031486 ) ) ;
#16517=CARTESIAN_POINT ( 'NONE',  ( 0.7185039370078739607, 1.928577636452523993E-17, 0.8562992125984251190 ) ) ;
#16518=CARTESIAN_POINT ( 'NONE',  ( 1.054774247047244540, -0.07405724077823318263, 0.8858267715997791836 ) ) ;
#16520=DIRECTION ( 'NONE',  ( 1.000000000000000000, 0.000000000000000000, -1.822029033848725275E-16 ) ) ;
#16525=CARTESIAN_POINT ( 'NONE',  ( 0.8107537697050253289, 0.1574803149606300301, 1.232775590443654812 ) ) ;
#16526=CARTESIAN_POINT ( 'NONE',  ( 0.7646288533564489232, -0.1113553986120547346, 1.166338582569637961 ) ) ;
#16530=CARTESIAN_POINT ( 'NONE',  ( -1.054774247047244540, 0.07405724077823318263, 1.840551181048599938 ) ) ;
#16531=CARTESIAN_POINT ( 'NONE',  ( 1.054774247047244540, 0.07405724077823318263, 1.879921259788756016 ) ) ;
#16534=CARTESIAN_POINT ( 'NONE',  ( 1.054774247047244540, 0.07405724077823318263, 0.3838582676627718127 ) ) ;
#16535=CARTESIAN_POINT ( 'NONE',  ( -0.8759842519685039353, -0.1787899950787401882, 1.390255905458047447 ) ) ;
#16536=VECTOR ( 'NONE', #40409, 39.37007874015748143 ) ;
#16537=CARTESIAN_POINT ( 'NONE',  ( 1.033464566929133799, 0.000000000000000000, 1.624015748031496287 ) ) ;
#16538=EDGE_CURVE ( 'NONE', #8711, #3940, #5277, .T. ) ;
#16539=CARTESIAN_POINT ( 'NONE',  ( -0.6971942568897626646, -0.07405724077823297447, 0.2854330708123783422 ) ) ;
#16541=CARTESIAN_POINT ( 'NONE',  ( -0.8759842519685039353, -0.1787899950787401882, 1.749507873961984483 ) ) ;
#16542=CARTESIAN_POINT ( 'NONE',  ( -0.9500414927467378812, 0.1787899950787401604, 0.1131889763241892138 ) ) ;
#16544=CARTESIAN_POINT ( 'NONE',  ( -0.8759842519685039353, 0.1574803149606299191, 1.712598425196850238 ) ) ;
#16546=CARTESIAN_POINT ( 'NONE',  ( 0.8759842519685039353, -0.1787899950787401882, 1.710137795221826851 ) ) ;
#16548=AXIS2_PLACEMENT_3D ( 'NONE', #13708, #42915, #10125 ) ;
#16553=FACE_OUTER_BOUND ( 'NONE', #1778, .T. ) ;
#16555=CARTESIAN_POINT ( 'NONE',  ( -0.9412147342319837628, -0.1574803149606297803, 0.7800196849318438153 ) ) ;
#16558=CARTESIAN_POINT ( 'NONE',  ( 0.8019270111902717657, 0.1787899950787401604, 0.9399606298674970661 ) ) ;
#16560=CARTESIAN_POINT ( 'NONE',  ( 0.8759842519685039353, -0.1787899950787401882, 1.985728346402929168 ) ) ;
#16563=CARTESIAN_POINT ( 'NONE',  ( 0.8759842519685039353, -0.1574803149606299191, 0.1968503937007874127 ) ) ;
#16564=DIRECTION ( 'NONE',  ( 1.000000000000000000, 0.000000000000000000, -1.822029033848725275E-16 ) ) ;
#16568=CARTESIAN_POINT ( 'NONE',  ( 0.6971942568897626646, 0.07405724077823318263, 0.3592519684501735977 ) ) ;
#16569=CARTESIAN_POINT ( 'NONE',  ( -0.8759842519685039353, 0.000000000000000000, 0.000000000000000000 ) ) ;
#16571=CARTESIAN_POINT ( 'NONE',  ( -0.6971942568897648851, 0.07405724077823318263, 1.850393700733638624 ) ) ;
#16573=CARTESIAN_POINT ( 'NONE',  ( -0.8019270111902717657, 0.1787899950787401604, 1.417322834591906222 ) ) ;
#16574=DIRECTION ( 'NONE',  ( 1.000000000000000000, 0.000000000000000000, 0.000000000000000000 ) ) ;
#16575=CARTESIAN_POINT ( 'NONE',  ( 1.054774247047244540, -0.07405724077823318263, 1.402559055064346971 ) ) ;
#16578=CARTESIAN_POINT ( 'NONE',  ( -0.7495606340400177148, -0.1264236179284866091, 0.5634842519147401640 ) ) ;
#16579=CARTESIAN_POINT ( 'NONE',  ( 0.8019270111902717657, 0.1787899950787401604, 0.07874015742655145200 ) ) ;
#16580=CARTESIAN_POINT ( 'NONE',  ( -0.7495606340400177148, 0.1264236179284866091, 1.178641732229700922 ) ) ;
#16583=CARTESIAN_POINT ( 'NONE',  ( 1.054774247047244096, 0.000000000000000000, 0.5782480314422993040 ) ) ;
#16584=CARTESIAN_POINT ( 'NONE',  ( -0.7495606340400177148, 0.1264236179284866091, 0.5093503936470236138 ) ) ;
#16589=DIRECTION ( 'NONE',  ( 1.822029033848725028E-16, 0.000000000000000000, 1.000000000000000000 ) ) ;
#16590=CARTESIAN_POINT ( 'NONE',  ( -0.7646288533564489232, -0.1113553986120547346, 0.3100393700787401619 ) ) ;
#16591=CARTESIAN_POINT ( 'NONE',  ( 1.054774247047244540, 0.07405724077823318263, 1.328740157426552049 ) ) ;
#16594=CARTESIAN_POINT ( 'NONE',  ( -0.7646288533564489232, -0.1113553986120547346, 0.5462598425196850682 ) ) ;
#16595=CARTESIAN_POINT ( 'NONE',  ( -0.8759842519685039353, -0.1787899950787401882, 1.001476377898992132 ) ) ;
#16596=CARTESIAN_POINT ( 'NONE',  ( -1.054774247047244540, -0.07405724077823318263, 0.2165354330171024577 ) ) ;
#16598=FACE_OUTER_BOUND ( 'NONE', #32707, .T. ) ;
#16600=ORIENTED_EDGE ( 'NONE', *, *, #1017, .F. ) ;
#16602=DIRECTION ( 'NONE',  ( 1.000000000000000000, 0.000000000000000000, -1.822029033848725275E-16 ) ) ;
#16603=( BOUNDED_CURVE ( )  B_SPLINE_CURVE ( 2, ( #46278, #27646, #16594, #13469, #38387, #2884, #35519, #17290, #42895 ),
 .UNSPECIFIED., .F., .T. ) 
 B_SPLINE_CURVE_WITH_KNOTS ( ( 3, 2, 2, 2, 3 ),
 ( 0.2700000000000000178, 0.2725000000000000200, 0.2750000000000000222, 0.2775000000000000244, 0.2800000000000000266 ),
 .UNSPECIFIED. ) 
 CURVE ( )  GEOMETRIC_REPRESENTATION_ITEM ( )  RATIONAL_B_SPLINE_CURVE ( ( 1.000000000000000000, 0.9238795325112869605, 1.000000000000000000, 0.9238795325112869605, 1.000000000000000000, 0.9238795325112869605, 1.000000000000000000, 0.9238795325112869605, 1.000000000000000000 ) ) 
 REPRESENTATION_ITEM ( '' )  ) ;
#16605=DIRECTION ( 'NONE',  ( 0.000000000000000000, 0.000000000000000000, -1.000000000000000000 ) ) ;
#16607=CARTESIAN_POINT ( 'NONE',  ( 0.7495606340400177148, 0.1264236179284866091, 1.611712598371433103 ) ) ;
#16614=CARTESIAN_POINT ( 'NONE',  ( -0.8019270111902716547, 0.1787899950787401604, 0.7480314960092282472 ) ) ;
#16616=LINE ( 'NONE', #37950, #7795 ) ;
#16618=CARTESIAN_POINT ( 'NONE',  ( 1.002407869896990045, -0.1264236179284866091, 1.557578740103716441 ) ) ;
#16619=CARTESIAN_POINT ( 'NONE',  ( 0.6971942568897648851, 0.07405724077823318263, 1.811023621993480548 ) ) ;
#16620=CARTESIAN_POINT ( 'NONE',  ( 1.054774247047244096, 0.000000000000000000, 0.3764763778989925203 ) ) ;
#16621=ADVANCED_FACE ( 'NONE', ( #30365 ), #37751, .T. ) ;
#16622=CARTESIAN_POINT ( 'NONE',  ( -0.7185039370078732945, -0.06523048226347920309, 0.1402559054042840370 ) ) ;
#16626=CARTESIAN_POINT ( 'NONE',  ( 1.002407869896990045, 0.1264236179284866091, 0.3813976377415121966 ) ) ;
#16627=CARTESIAN_POINT ( 'NONE',  ( 0.9500414927467377701, -0.1787899950787401604, 1.313976377898992132 ) ) ;
#16628=CARTESIAN_POINT ( 'NONE',  ( 0.9873396505805591694, 0.1113553986120547346, 1.973425196742866206 ) ) ;
#16629=CARTESIAN_POINT ( 'NONE',  ( -0.7646288533564489232, 0.1113553986120547346, 1.589566929026330566 ) ) ;
#16630=CARTESIAN_POINT ( 'NONE',  ( -1.002407869896990045, 0.1264236179284866091, 1.444389763725763665 ) ) ;
#16631=CARTESIAN_POINT ( 'NONE',  ( 0.8107537697050253289, -0.1574803149606297803, 0.7357283463491665065 ) ) ;
#16633=DIRECTION ( 'NONE',  ( 1.822029033848725028E-16, 0.000000000000000000, 1.000000000000000000 ) ) ;
#16634=CARTESIAN_POINT ( 'NONE',  ( 1.054774247047244096, 0.000000000000000000, 0.9719488188438739629 ) ) ;
#16635=VERTEX_POINT ( 'NONE', #9472 ) ;
#16638=CARTESIAN_POINT ( 'NONE',  ( -0.9873396505805591694, 0.1113553986120547346, 0.5167322833570401341 ) ) ;
#16639=CYLINDRICAL_SURFACE ( 'NONE', #29490, 0.1574803149606299191 ) ;
#16640=CARTESIAN_POINT ( 'NONE',  ( 0.8019270111902717657, -0.1787899950787401604, 1.663385826717890925 ) ) ;
#16641=CARTESIAN_POINT ( 'NONE',  ( -0.9873396505805591694, 0.1113553986120547346, 1.392716535433070835 ) ) ;
#16644=LINE ( 'NONE', #6780, #10938 ) ;
#16645=CARTESIAN_POINT ( 'NONE',  ( 0.7495606340400177148, 0.1264236179284866091, 0.1993110235682838682 ) ) ;
#16647=CARTESIAN_POINT ( 'NONE',  ( 0.8759842519685039353, 0.1574803149606299191, 1.387795275483023616 ) ) ;
#16652=CARTESIAN_POINT ( 'NONE',  ( 0.7185039370078746268, -0.06523048226347956391, 0.5831692913385827515 ) ) ;
#16653=CARTESIAN_POINT ( 'NONE',  ( 0.6971942568897648851, 0.07405724077823318263, 0.9498031495525356416 ) ) ;
#16654=CARTESIAN_POINT ( 'NONE',  ( -0.8759842519685039353, 0.1787899950787401882, 1.646161417269070837 ) ) ;
#16660=ORIENTED_EDGE ( 'NONE', *, *, #15497, .F. ) ;
#16665=CARTESIAN_POINT ( 'NONE',  ( -0.7185039370078739607, 1.928577636452523993E-17, 0.9251968502861732668 ) ) ;
#16666=CARTESIAN_POINT ( 'NONE',  ( 0.9873396505805591694, 0.1113553986120547346, 1.825787401574803237 ) ) ;
#16668=EDGE_CURVE ( 'NONE', #22426, #4083, #8923, .T. ) ;
#16670=CARTESIAN_POINT ( 'NONE',  ( -0.8019270111902716547, -0.1787899950787401604, 0.2903543306548980185 ) ) ;
#16671=CARTESIAN_POINT ( 'NONE',  ( -0.9873396505805591694, 0.1113553986120547346, 1.077755905511811108 ) ) ;
#16675=CARTESIAN_POINT ( 'NONE',  ( 0.7495606340400177148, 0.1264236179284866091, 1.026082677111590513 ) ) ;
#16676=CARTESIAN_POINT ( 'NONE',  ( 0.7495606340400177148, -0.1264236179284866091, 1.385334645615527549 ) ) ;
#16677=CARTESIAN_POINT ( 'NONE',  ( 0.8759842519685039353, 0.1787899950787401882, 0.2288385826234019815 ) ) ;
#16680=CARTESIAN_POINT ( 'NONE',  ( 0.7185039370078739607, 1.928577636452523993E-17, 0.2263779527559055260 ) ) ;
#16681=CARTESIAN_POINT ( 'NONE',  ( 0.9873396505805591694, 0.1113553986120547346, 1.550196850393700920 ) ) ;
#16682=CARTESIAN_POINT ( 'NONE',  ( 0.7878339515481005417, 0.1343209511212810070, 1.980178066860823760 ) ) ;
#16683=CARTESIAN_POINT ( 'NONE',  ( -0.8702779046212122394, 0.1576667313500946244, 1.978454084305184990 ) ) ;
#16684=CARTESIAN_POINT ( 'NONE',  ( 0.7646288533564489232, -0.1113553986120547346, 1.441929133750740277 ) ) ;
#16686=CARTESIAN_POINT ( 'NONE',  ( 1.033464566929134687, -0.06523048226347956391, 1.660925196850393526 ) ) ;
#16687=CARTESIAN_POINT ( 'NONE',  ( 1.054774247047244540, 0.07405724077823318263, 0.9694881889226145688 ) ) ;
#16688=CARTESIAN_POINT ( 'NONE',  ( 0.7495606340400177148, 0.1264236179284866091, 1.970964566875370139 ) ) ;
#16689=CARTESIAN_POINT ( 'NONE',  ( -0.7495606340400177148, -0.1264236179284866091, 1.149114173174582643 ) ) ;
#16690=CARTESIAN_POINT ( 'NONE',  ( 0.7185039370078746268, -0.06523048226347956391, 0.3371062991050715607 ) ) ;
#16692=CARTESIAN_POINT ( 'NONE',  ( 0.9998624034419133499, 0.1095613300894844738, 0.03936950506162378849 ) ) ;
#16694=CARTESIAN_POINT ( 'NONE',  ( -0.7646288533564489232, -0.1113553986120547346, 0.3001968502861740440 ) ) ;
#16695=CARTESIAN_POINT ( 'NONE',  ( 1.002407869896990045, -0.1264236179284866091, 1.277066929080094448 ) ) ;
#16700=CARTESIAN_POINT ( 'NONE',  ( 0.7646288533564489232, 0.1113553986120547346, 0.2608267716535432879 ) ) ;
#16701=CARTESIAN_POINT ( 'NONE',  ( 0.5314960629921260393, 0.000000000000000000, 4.498031496062992574 ) ) ;
#16703=CARTESIAN_POINT ( 'NONE',  ( -0.9873396505805591694, 0.1113553986120547346, 0.05413385826771653642 ) ) ;
#16705=CARTESIAN_POINT ( 'NONE',  ( -1.054774247047244096, 0.000000000000000000, 0.6963582676627716461 ) ) ;
#16706=EDGE_LOOP ( 'NONE', ( #32041, #31812, #25869, #23374, #4745, #6319, #16869, #3085, #13810, #44738, #16287, #20065, #40168, #34887, #40260, #39914, #22819, #22118, #7803, #45440, #45032, #2186, #3949, #23769, #18762, #18815, #29500, #14292, #7067, #9672, #33945, #40936, #19522, #15412, #53, #43341, #1797, #34391, #16456, #32105, #13746, #33062, #42586, #17056, #34501, #2082, #23596, #32796, #31794, #28538, #44756, #22598, #8444, #36212, #25010, #23022, #9274, #39847, #23876, #29190, #24322, #9465, #17925, #12166, #952, #26092, #22035, #17519, #26130, #29234, #15401, #6774, #37636, #36608, #29049, #12614, #24888, #47460, #16987, #43441, #39537, #42776, #43125, #25257, #43861, #29432, #13349, #10355, #37155, #36029, #32592, #169, #26095, #12639, #34025, #29773, #1724, #13427, #24145, #35025, #28941, #3496 ) ) ;
#16710=ORIENTED_EDGE ( 'NONE', *, *, #15840, .T. ) ;
#16716=AXIS2_PLACEMENT_3D ( 'NONE', #32349, #39029, #43088 ) ;
#16717=CARTESIAN_POINT ( 'NONE',  ( -0.7495606340400177148, 0.1264236179284866091, 0.5487204723871811352 ) ) ;
#16718=CARTESIAN_POINT ( 'NONE',  ( 0.7185039370078739607, 0.000000000000000000, 4.498031496062992574 ) ) ;
#16720=CARTESIAN_POINT ( 'NONE',  ( -0.7495606340400177148, -0.1264236179284866091, 1.705216535379307174 ) ) ;
#16726=DIRECTION ( 'NONE',  ( 0.000000000000000000, 0.000000000000000000, 1.000000000000000000 ) ) ;
#16727=CARTESIAN_POINT ( 'NONE',  ( -0.7185039370078746268, 0.06523048226347956391, 1.198326771546015967 ) ) ;
#16728=ADVANCED_FACE ( 'NONE', ( #13522 ), #39614, .T. ) ;
#16735=CARTESIAN_POINT ( 'NONE',  ( 1.033464566929133799, 0.000000000000000000, 1.072834645669291431 ) ) ;
#16736=CARTESIAN_POINT ( 'NONE',  ( 0.8759842519685039353, 0.000000000000000000, 4.498031496062992574 ) ) ;
#16737=CARTESIAN_POINT ( 'NONE',  ( -0.9498231833118063738, -0.1609423499385754242, 1.989542384547356324 ) ) ;
#16739=CARTESIAN_POINT ( 'NONE',  ( 0.7646288533564489232, 0.1113553986120547346, 0.1820866141732283561 ) ) ;
#16742=CARTESIAN_POINT ( 'NONE',  ( 0.8107537697050254399, 0.1574803149606300301, 0.6028543306011346914 ) ) ;
#16744=ORIENTED_EDGE ( 'NONE', *, *, #20661, .T. ) ;
#16745=CARTESIAN_POINT ( 'NONE',  ( 0.7646288533564489232, 0.1113553986120547346, 1.166338582677165281 ) ) ;
#16746=CARTESIAN_POINT ( 'NONE',  ( 0.8019270111902717657, 0.1787899950787401604, 0.8218503936470251681 ) ) ;
#16748=CARTESIAN_POINT ( 'NONE',  ( 0.9412147342319837628, -0.1574803149606297803, 1.459153543307085688 ) ) ;
#16754=CARTESIAN_POINT ( 'NONE',  ( 0.7646288533564489232, 0.1113553986120547346, 1.274606299105070839 ) ) ;
#16757=CARTESIAN_POINT ( 'NONE',  ( -1.002407869896990045, 0.1264236179284866091, 1.882381889710015743 ) ) ;
#16758=CARTESIAN_POINT ( 'NONE',  ( 0.8019270111902717657, -0.1787899950787401604, 1.865157480261195877 ) ) ;
#16760=DIRECTION ( 'NONE',  ( 1.822029033848725028E-16, 0.000000000000000000, 1.000000000000000000 ) ) ;
#16761=CARTESIAN_POINT ( 'NONE',  ( -1.002407869896990045, -0.1264236179284866091, 1.552657480261196765 ) ) ;
#16763=CARTESIAN_POINT ( 'NONE',  ( -0.8759842519685039353, 0.1787899950787401882, 0.2337598424659216578 ) ) ;
#16765=CARTESIAN_POINT ( 'NONE',  ( -0.7495606340400177148, 0.1264236179284866091, 1.774114173174582643 ) ) ;
#16766=CARTESIAN_POINT ( 'NONE',  ( -0.9412147342319837628, 0.1574803149606300301, 1.670767716535433545 ) ) ;
#16767=CYLINDRICAL_SURFACE ( 'NONE', #23621, 0.1574803149606299191 ) ;
#16769=CARTESIAN_POINT ( 'NONE',  ( 0.6971942568897648851, -0.07405724077823297447, 1.742125984198204858 ) ) ;
#16771=CARTESIAN_POINT ( 'NONE',  ( -0.8759842519685039353, -0.1574803149606299191, 0.7381889762704251234 ) ) ;
#16772=( BOUNDED_CURVE ( )  B_SPLINE_CURVE ( 2, ( #12846, #27239, #5386, #20711, #20005, #27000, #42280, #9480, #1551 ),
 .UNSPECIFIED., .F., .T. ) 
 B_SPLINE_CURVE_WITH_KNOTS ( ( 3, 2, 2, 2, 3 ),
 ( 0.8599999999999999867, 0.8625000000000000444, 0.8649999999999999911, 0.8675000000000000488, 0.8699999999999999956 ),
 .UNSPECIFIED. ) 
 CURVE ( )  GEOMETRIC_REPRESENTATION_ITEM ( )  RATIONAL_B_SPLINE_CURVE ( ( 1.000000000000000000, 0.9238795325112869605, 1.000000000000000000, 0.9238795325112869605, 1.000000000000000000, 0.9238795325112869605, 1.000000000000000000, 0.9238795325112829637, 1.000000000000000000 ) ) 
 REPRESENTATION_ITEM ( '' )  ) ;
#16776=CARTESIAN_POINT ( 'NONE',  ( -0.8019270111902716547, 0.1787899950787401604, 1.299212598371434435 ) ) ;
#16777=ORIENTED_EDGE ( 'NONE', *, *, #37506, .T. ) ;
#16781=CARTESIAN_POINT ( 'NONE',  ( -1.033464566929133799, 0.000000000000000000, 1.377952755797984263 ) ) ;
#16782=CARTESIAN_POINT ( 'NONE',  ( 0.8019270111902717657, 0.1787899950787401604, 0.3887795275052913224 ) ) ;
#16784=CARTESIAN_POINT ( 'NONE',  ( -0.7185039370078739607, 1.928577636452523993E-17, 0.8464566928058583350 ) ) ;
#16785=CARTESIAN_POINT ( 'NONE',  ( -0.7646288533564489232, 0.1113553986120547346, 0.6938976377952755792 ) ) ;
#16787=ADVANCED_FACE ( 'NONE', ( #47050 ), #46572, .T. ) ;
#16788=CARTESIAN_POINT ( 'NONE',  ( 0.6971942568897648851, -0.07405724077823297447, 0.9891732282926934960 ) ) ;
#16789=CARTESIAN_POINT ( 'NONE',  ( 1.002407869896990045, -0.1264236179284866091, 1.990649606245448844 ) ) ;
#16790=CARTESIAN_POINT ( 'NONE',  ( -0.8075642815980649258, 0.1651804164989427171, 0.03937007874015843040 ) ) ;
#16793=CARTESIAN_POINT ( 'NONE',  ( 1.054774247047244540, -0.07405724077823318263, 0.3395669290800945039 ) ) ;
#16794=AXIS2_PLACEMENT_3D ( 'NONE', #4563, #19673, #33857 ) ;
#16795=CARTESIAN_POINT ( 'NONE',  ( -1.054774247047244540, -0.07405724077823318263, 1.948818897584033927 ) ) ;
#16797=EDGE_LOOP ( 'NONE', ( #5315, #546, #6445, #25308 ) ) ;
#16798=CARTESIAN_POINT ( 'NONE',  ( 0.6971942568897648851, -0.07405724077823297447, 1.387795275536786610 ) ) ;
#16799=CARTESIAN_POINT ( 'NONE',  ( -0.7185039370078739607, 0.000000000000000000, -2.869337061179095023E-17 ) ) ;
#16800=CARTESIAN_POINT ( 'NONE',  ( -0.6971942568897626646, 0.07405724077823318263, 0.6348425196312760255 ) ) ;
#16801=CARTESIAN_POINT ( 'NONE',  ( 0.8019270111902717657, 0.1787899950787401604, 0.1181102361667090567 ) ) ;
#16803=CARTESIAN_POINT ( 'NONE',  ( 0.8019270111902716547, 0.1787899950787401604, 0.5511811023084406402 ) ) ;
#16804=CARTESIAN_POINT ( 'NONE',  ( -1.054774247047244096, 0.000000000000000000, 0.5733267715997795166 ) ) ;
#16805=EDGE_CURVE ( 'NONE', #10984, #1283, #36816, .T. ) ;
#16807=ORIENTED_EDGE ( 'NONE', *, *, #30075, .T. ) ;
#16808=VERTEX_POINT ( 'NONE', #12345 ) ;
#16809=CARTESIAN_POINT ( 'NONE',  ( -1.033464566929134687, -0.06523048226347956391, 0.2829724409448821643 ) ) ;
#16811=CARTESIAN_POINT ( 'NONE',  ( 0.7495606340400177148, 0.1264236179284866091, 1.380413385773007873 ) ) ;
#16815=CARTESIAN_POINT ( 'NONE',  ( -0.8019270111902717657, 0.1787899950787401604, 0.9448818897100165204 ) ) ;
#16817=ORIENTED_EDGE ( 'NONE', *, *, #20169, .T. ) ;
#16818=CARTESIAN_POINT ( 'NONE',  ( -1.033464566929133799, 0.000000000000000000, 1.929133858160188897 ) ) ;
#16820=CARTESIAN_POINT ( 'NONE',  ( 1.002407869896990045, 0.1264236179284866091, 1.444389763725763665 ) ) ;
#16826=CARTESIAN_POINT ( 'NONE',  ( 0.7185039370078746268, -0.06523048226347956391, 0.1796259841444415029 ) ) ;
#16827=LINE ( 'NONE', #41081, #40758 ) ;
#16831=DIRECTION ( 'NONE',  ( 1.000000000000000000, 0.000000000000000000, -1.822029033848725275E-16 ) ) ;
#16833=VECTOR ( 'NONE', #8141, 39.37007874015748143 ) ;
#16834=CARTESIAN_POINT ( 'NONE',  ( -1.002407869896990045, -0.1264236179284866091, 0.8095472440407244230 ) ) ;
#16836=CARTESIAN_POINT ( 'NONE',  ( -1.033464566929133799, 0.000000000000000000, 1.377952755797984263 ) ) ;
#16839=CARTESIAN_POINT ( 'NONE',  ( 0.6971942568897637749, 2.189545951927499583E-17, 1.542814960576157413 ) ) ;
#16840=CARTESIAN_POINT ( 'NONE',  ( 1.002407869896990045, 0.1264236179284866091, 1.956200787347811110 ) ) ;
#16842=CARTESIAN_POINT ( 'NONE',  ( 0.8759842519685039353, -0.1787899950787401882, 0.4060039369541102450 ) ) ;
#16845=CARTESIAN_POINT ( 'NONE',  ( -0.7108038343253642033, 0.06841996760810098444, 0.03937007874015843040 ) ) ;
#16848=CARTESIAN_POINT ( 'NONE',  ( -0.7185039370078739607, 1.928577636452523993E-17, 1.240157480207432883 ) ) ;
#16850=CARTESIAN_POINT ( 'NONE',  ( 1.054774247047244540, 0.07405724077823318263, 0.4576771653005669016 ) ) ;
#16852=CARTESIAN_POINT ( 'NONE',  ( 0.7821658433489714346, -0.1347180231840020004, 0.03936951888585819848 ) ) ;
#16854=CARTESIAN_POINT ( 'NONE',  ( -0.8759842519685039353, 0.1787899950787401882, 1.409940944828126153 ) ) ;
#16856=CARTESIAN_POINT ( 'NONE',  ( 1.002407869896990045, -0.1264236179284866091, 1.085137795221826629 ) ) ;
#16860=CARTESIAN_POINT ( 'NONE',  ( 1.002407869896990045, -0.1264236179284866091, 1.710137795221826851 ) ) ;
#16861=CARTESIAN_POINT ( 'NONE',  ( -0.9873396505805591694, 0.1113553986120547346, 1.353346456692913424 ) ) ;
#16862=CYLINDRICAL_SURFACE ( 'NONE', #24343, 0.1574803149606299191 ) ;
#16864=CARTESIAN_POINT ( 'NONE',  ( -0.7018081390872378256, -0.006340216279131547818, 0.03937007874015843734 ) ) ;
#16865=CARTESIAN_POINT ( 'NONE',  ( 0.8019270111902716547, 0.1787899950787401604, 0.1968503936470238636 ) ) ;
#16867=CARTESIAN_POINT ( 'NONE',  ( 0.7646288533564489232, -0.1113553986120547346, 1.441929133750740277 ) ) ;
#16869=ORIENTED_EDGE ( 'NONE', *, *, #9610, .F. ) ;
#16873=CARTESIAN_POINT ( 'NONE',  ( -0.7495606340400177148, 0.1264236179284866091, 1.769192913332062966 ) ) ;
#16874=EDGE_LOOP ( 'NONE', ( #32104, #34969, #17418, #27305, #15254, #35581, #20165, #17161, #47367, #17665, #25576, #25312, #34183, #26948, #20213, #19024, #28161, #34635, #1014, #17616, #11557, #23909, #6763, #10036, #11937, #19811, #11780, #37742, #14107, #25508, #46164, #19939, #41688, #46405, #34474, #21843, #38216, #18533, #45127, #22241, #40368, #20783, #33350, #6230, #24832, #28216, #8263, #32628, #38509, #22343, #7914, #44916, #8309, #9163, #44971, #4452, #16227, #29071, #19496, #16660, #8100, #6288, #11532, #22272, #17385, #59, #17246, #40377, #23302, #6364, #3481, #14469, #23140, #46183, #9152, #36467, #3601, #30516, #34394, #4515, #14712, #8234, #30211, #42493, #28651, #22389, #2553, #20762, #23359, #45254, #14030, #2916, #34260, #9562, #10485, #39993, #2296, #33646, #17563, #34402, #18473, #17886 ) ) ;
#16877=( BOUNDED_CURVE ( )  B_SPLINE_CURVE ( 2, ( #46262, #20628, #35274, #2410, #23684, #20079, #12687, #30903, #12447 ),
 .UNSPECIFIED., .F., .F. ) 
 B_SPLINE_CURVE_WITH_KNOTS ( ( 3, 2, 2, 2, 3 ),
 ( 0.8000000000000000444, 0.8024999999999999911, 0.8050000000000000488, 0.8074999999999999956, 0.8100000000000000533 ),
 .UNSPECIFIED. ) 
 CURVE ( )  GEOMETRIC_REPRESENTATION_ITEM ( )  RATIONAL_B_SPLINE_CURVE ( ( 1.000000000000000000, 0.9238795325112869605, 1.000000000000000000, 0.9238795325112869605, 1.000000000000000000, 0.9238795325112869605, 1.000000000000000000, 0.9238795325112829637, 1.000000000000000000 ) ) 
 REPRESENTATION_ITEM ( '' )  ) ;
#16880=CARTESIAN_POINT ( 'NONE',  ( 0.7185039370078739607, 1.928577636452523993E-17, 1.633858267609007875 ) ) ;
#16887=CARTESIAN_POINT ( 'NONE',  ( 0.6971942568897648851, -0.07405724077823297447, 1.107283464513165949 ) ) ;
#16889=EDGE_CURVE ( 'NONE', #42069, #12184, #27003, .T. ) ;
#16890=CARTESIAN_POINT ( 'NONE',  ( 1.033464566929134687, 0.06523048226347956391, 1.902066929133858775 ) ) ;
#16892=ORIENTED_EDGE ( 'NONE', *, *, #32223, .F. ) ;
#16893=( BOUNDED_CURVE ( )  B_SPLINE_CURVE ( 2, ( #7178, #43826, #43107, #14852, #32118, #10555, #6456, #11260, #33080 ),
 .UNSPECIFIED., .F., .T. ) 
 B_SPLINE_CURVE_WITH_KNOTS ( ( 3, 2, 2, 2, 3 ),
 ( 0.6999999999999999556, 0.7025000000000000133, 0.7049999999999999600, 0.7075000000000000178, 0.7099999999999999645 ),
 .UNSPECIFIED. ) 
 CURVE ( )  GEOMETRIC_REPRESENTATION_ITEM ( )  RATIONAL_B_SPLINE_CURVE ( ( 1.000000000000000000, 0.9238795325112899581, 1.000000000000000000, 0.9238795325112869605, 1.000000000000000000, 0.9238795325112869605, 1.000000000000000000, 0.9238795325112799661, 1.000000000000000000 ) ) 
 REPRESENTATION_ITEM ( '' )  ) ;
#16895=CARTESIAN_POINT ( 'NONE',  ( -0.8019270111902716547, 0.1787899950787401604, 0.3149606298674962890 ) ) ;
#16896=CARTESIAN_POINT ( 'NONE',  ( -1.033464566929134687, 0.06523048226347956391, 1.035925196850394192 ) ) ;
#16898=CARTESIAN_POINT ( 'NONE',  ( 0.8759842519685039353, 0.000000000000000000, 4.498031496062992574 ) ) ;
#16900=CARTESIAN_POINT ( 'NONE',  ( -0.7118405396259548379, 0.02030376831657693462, 1.982893094199861483 ) ) ;
#16902=CARTESIAN_POINT ( 'NONE',  ( 0.9500414927467378812, -0.1787899950787401604, 1.003937007820251193 ) ) ;
#16903=CARTESIAN_POINT ( 'NONE',  ( 0.9500414927467377701, -0.1787899950787401604, 1.510826771599780294 ) ) ;
#16904=CARTESIAN_POINT ( 'NONE',  ( 0.6971942568897637749, 2.189545951927499583E-17, 0.1993110235682838682 ) ) ;
#16907=CARTESIAN_POINT ( 'NONE',  ( 1.033464566929133799, 0.000000000000000000, 1.663385826771653697 ) ) ;
#16909=CARTESIAN_POINT ( 'NONE',  ( 0.9412147342319837628, -0.1574803149606297803, 1.528051180994836056 ) ) ;
#16911=CARTESIAN_POINT ( 'NONE',  ( 0.7185039370078739607, 1.928577636452523993E-17, 0.7677165353255432922 ) ) ;
#16912=CARTESIAN_POINT ( 'NONE',  ( -0.7646288533564489232, -0.1113553986120547346, 0.6938976376877481478 ) ) ;
#16913=CARTESIAN_POINT ( 'NONE',  ( 0.6971942568897637749, 2.189545951927499583E-17, 1.026082677111590513 ) ) ;
#16915=CARTESIAN_POINT ( 'NONE',  ( 1.054774247047244540, -0.07405724077823318263, 1.914370078686394860 ) ) ;
#16916=CARTESIAN_POINT ( 'NONE',  ( 1.033464566929134687, -0.06523048226347956391, 0.3124999998924728462 ) ) ;
#16918=DIRECTION ( 'NONE',  ( 1.822029033848725028E-16, 0.000000000000000000, 1.000000000000000000 ) ) ;
#16919=CARTESIAN_POINT ( 'NONE',  ( -0.8759842519685039353, 0.1574803149606299191, 0.2854330707586145710 ) ) ;
#16920=CARTESIAN_POINT ( 'NONE',  ( 1.054774247047244096, 0.000000000000000000, 1.360728346402929168 ) ) ;
#16921=CARTESIAN_POINT ( 'NONE',  ( -0.5314960629921260393, 0.000000000000000000, 4.842519685039370358 ) ) ;
#16922=CARTESIAN_POINT ( 'NONE',  ( 0.7646288533564489232, -0.1113553986120547346, 0.06397637784522892945 ) ) ;
#16926=CARTESIAN_POINT ( 'NONE',  ( 0.9873396505805591694, -0.1113553986120547346, 1.294291338475149544 ) ) ;
#16927=CARTESIAN_POINT ( 'NONE',  ( -0.7185039370078739607, 1.928577636452523993E-17, 0.1082677165354330728 ) ) ;
#16928=EDGE_LOOP ( 'NONE', ( #19914, #43553, #46441, #31283 ) ) ;
#16929=CARTESIAN_POINT ( 'NONE',  ( -0.8019270111902716547, 0.1787899950787401604, 1.412401574749386990 ) ) ;
#16932=CARTESIAN_POINT ( 'NONE',  ( -1.002407869896990045, 0.1264236179284866091, 1.016240157426551161 ) ) ;
#16933=CARTESIAN_POINT ( 'NONE',  ( -0.6971942568897637749, 2.189545951927499583E-17, 1.931594488135212728 ) ) ;
#16936=CARTESIAN_POINT ( 'NONE',  ( -0.7495606340400177148, 0.1264236179284866091, 0.7111220471903307860 ) ) ;
#16943=CARTESIAN_POINT ( 'NONE',  ( -0.9412147342319837628, -0.1574803149606297803, 0.6619094487113718062 ) ) ;
#16944=EDGE_CURVE ( 'NONE', #4710, #31350, #37968, .T. ) ;
#16950=CARTESIAN_POINT ( 'NONE',  ( -1.002407869896990045, -0.1264236179284866091, 0.5684055117572598403 ) ) ;
#16953=CARTESIAN_POINT ( 'NONE',  ( -1.054774247047244540, -0.07405724077823318263, 1.638779527505292766 ) ) ;
#16956=CARTESIAN_POINT ( 'NONE',  ( 0.8759842519685039353, -0.1574803149606299191, 0.5905511811023621549 ) ) ;
#16957=CARTESIAN_POINT ( 'NONE',  ( 1.033464566929133799, 0.000000000000000000, 0.6299212597349921339 ) ) ;
#16958=CARTESIAN_POINT ( 'NONE',  ( -1.033464566929133799, 0.000000000000000000, 1.181102362097196989 ) ) ;
#16962=ORIENTED_EDGE ( 'NONE', *, *, #23720, .F. ) ;
#16963=CARTESIAN_POINT ( 'NONE',  ( 1.033464566929134687, 0.06523048226347956391, 1.577263779420032153 ) ) ;
#16964=CARTESIAN_POINT ( 'NONE',  ( 1.033464566929134687, 0.06523048226347956391, 1.154035433070866423 ) ) ;
#16966=CARTESIAN_POINT ( 'NONE',  ( 1.033464566929133799, 0.000000000000000000, 0.3248031496062992463 ) ) ;
#16970=VECTOR ( 'NONE', #5052, 39.37007874015748143 ) ;
#16979=CARTESIAN_POINT ( 'NONE',  ( 0.8759842519685039353, -0.1787899950787401882, 0.8784448818360000022 ) ) ;
#16981=DIRECTION ( 'NONE',  ( 1.000000000000000000, 0.000000000000000000, -1.822029033848725275E-16 ) ) ;
#16985=CARTESIAN_POINT ( 'NONE',  ( 0.8107537697050253289, 0.1574803149606300301, 1.272145669183810668 ) ) ;
#16986=CARTESIAN_POINT ( 'NONE',  ( -0.9412147342319837628, 0.1574803149606300301, 1.395177165354331672 ) ) ;
#16987=ORIENTED_EDGE ( 'NONE', *, *, #18710, .F. ) ;
#16988=CARTESIAN_POINT ( 'NONE',  ( -1.002407869896990045, -0.1264236179284866091, 1.990649606245448844 ) ) ;
#16989=CARTESIAN_POINT ( 'NONE',  ( 0.7185039370078739607, 0.000000000000000000, 4.498031496062992574 ) ) ;
#16991=CARTESIAN_POINT ( 'NONE',  ( 0.9412147342319837628, -0.1574803149606297803, 0.5536417322834641386 ) ) ;
#16992=CARTESIAN_POINT ( 'NONE',  ( -0.6971942568897648851, -0.07405724077823297447, 1.540354330654897685 ) ) ;
#16995=CARTESIAN_POINT ( 'NONE',  ( -1.054774247047244540, -0.07405724077823318263, 0.9645669290800953366 ) ) ;
#16996=CARTESIAN_POINT ( 'NONE',  ( -0.6971942568897626646, -0.07405724077823297447, 0.1673228345919059168 ) ) ;
#16997=EDGE_CURVE ( 'NONE', #18349, #20105, #30377, .T. ) ;
#16999=CARTESIAN_POINT ( 'NONE',  ( -1.002407869896990045, -0.1264236179284866091, 1.833169291284818758 ) ) ;
#17000=CARTESIAN_POINT ( 'NONE',  ( 1.033464566929133799, 1.928577636452524610E-17, 4.498031496062992574 ) ) ;
#17001=DIRECTION ( 'NONE',  ( 0.000000000000000000, 0.000000000000000000, -1.000000000000000000 ) ) ;
#17002=CARTESIAN_POINT ( 'NONE',  ( -1.033464566929133799, 0.000000000000000000, 1.702755905511810885 ) ) ;
#17006=CARTESIAN_POINT ( 'NONE',  ( -1.033464566929133799, 0.000000000000000000, 0.7480314959554645871 ) ) ;
#17007=CARTESIAN_POINT ( 'NONE',  ( -0.7646288533564489232, 0.1113553986120547346, 0.05413385816018952829 ) ) ;
#17009=EDGE_CURVE ( 'NONE', #31513, #3955, #9199, .T. ) ;
#17012=CARTESIAN_POINT ( 'NONE',  ( -1.002407869896990045, 0.1264236179284866091, 1.252460629867496067 ) ) ;
#17014=AXIS2_PLACEMENT_3D ( 'NONE', #24963, #13697, #38860 ) ;
#17020=CARTESIAN_POINT ( 'NONE',  ( -0.7646288533564489232, -0.1113553986120547346, 0.7726377951680629685 ) ) ;
#17021=CARTESIAN_POINT ( 'NONE',  ( -0.7185039370078739607, 1.928577636452523993E-17, 0.7381889763779527769 ) ) ;
#17023=CARTESIAN_POINT ( 'NONE',  ( 0.9500414927467378812, 0.1787899950787401604, 0.9350393700249758355 ) ) ;
#17027=CARTESIAN_POINT ( 'NONE',  ( 0.7185039370078739607, 1.928577636452523993E-17, 0.1771653542231816925 ) ) ;
#17028=ORIENTED_EDGE ( 'NONE', *, *, #44668, .F. ) ;
#17029=CARTESIAN_POINT ( 'NONE',  ( 0.7185039370078746268, 0.06523048226347956391, 0.1845472440944883052 ) ) ;
#17030=CARTESIAN_POINT ( 'NONE',  ( 0.9873396505805591694, -0.1113553986120547346, 1.845472440837354178 ) ) ;
#17031=CARTESIAN_POINT ( 'NONE',  ( -1.033464566929134687, -0.06523048226347956391, 1.188484251968505268 ) ) ;
#17034=VECTOR ( 'NONE', #37194, 39.37007874015748143 ) ;
#17035=CARTESIAN_POINT ( 'NONE',  ( -0.6971942568897637749, 2.189545951927499583E-17, 1.970964566875370139 ) ) ;
#17037=CARTESIAN_POINT ( 'NONE',  ( -1.054774247047244096, 0.000000000000000000, 1.523129921206078707 ) ) ;
#17038=CARTESIAN_POINT ( 'NONE',  ( 1.054774247047244540, -0.07405724077823318263, 1.441929133804504604 ) ) ;
#17041=CARTESIAN_POINT ( 'NONE',  ( 1.033464566929133799, 1.928577636452524610E-17, 4.498031496062992574 ) ) ;
#17042=CARTESIAN_POINT ( 'NONE',  ( 0.6971942568897648851, -0.07405724077823297447, 0.5610236219934807700 ) ) ;
#17043=CARTESIAN_POINT ( 'NONE',  ( -1.002407869896990045, -0.1264236179284866091, 0.6077755904974173617 ) ) ;
#17045=EDGE_CURVE ( 'NONE', #41784, #3252, #20211, .T. ) ;
#17046=ORIENTED_EDGE ( 'NONE', *, *, #27476, .F. ) ;
#17047=CARTESIAN_POINT ( 'NONE',  ( -0.8019270111902717657, 0.1787899950787401604, 1.496062992072220821 ) ) ;
#17049=CARTESIAN_POINT ( 'NONE',  ( -1.033464566929134687, -0.06523048226347956391, 0.5191929133858269596 ) ) ;
#17050=CARTESIAN_POINT ( 'NONE',  ( 1.054774247047244540, 0.07405724077823318263, 1.289370078686393750 ) ) ;
#17052=ORIENTED_EDGE ( 'NONE', *, *, #14563, .F. ) ;
#17053=ADVANCED_FACE ( 'NONE', ( #15940 ), #13051, .T. ) ;
#17054=CARTESIAN_POINT ( 'NONE',  ( -0.8759842519685039353, 0.000000000000000000, 0.000000000000000000 ) ) ;
#17055=CARTESIAN_POINT ( 'NONE',  ( -0.9500414927467378812, 0.1787899950787401604, 1.018700787347811110 ) ) ;
#17056=ORIENTED_EDGE ( 'NONE', *, *, #6978, .F. ) ;
#17058=CARTESIAN_POINT ( 'NONE',  ( 0.7185039370078739607, 1.928577636452523993E-17, 0.5019685039370078705 ) ) ;
#17059=ORIENTED_EDGE ( 'NONE', *, *, #29711, .F. ) ;
#17062=CARTESIAN_POINT ( 'NONE',  ( 0.7646288533564489232, -0.1113553986120547346, 0.1820866140657015630 ) ) ;
#17065=AXIS2_PLACEMENT_3D ( 'NONE', #2843, #39736, #46944 ) ;
#17071=CARTESIAN_POINT ( 'NONE',  ( -1.054774247047244540, 0.07405724077823318263, 0.8562992125446617919 ) ) ;
#17075=CARTESIAN_POINT ( 'NONE',  ( -0.7680718972492022178, -0.1324197970153654924, 1.986028192752562482 ) ) ;
#17076=CARTESIAN_POINT ( 'NONE',  ( 0.7495606340400177148, -0.1264236179284866091, 1.547736220418677089 ) ) ;
#17077=CARTESIAN_POINT ( 'NONE',  ( 1.054774247047244096, 0.000000000000000000, 1.990649606245448844 ) ) ;
#17078=CARTESIAN_POINT ( 'NONE',  ( -0.7646288533564489232, -0.1113553986120547346, 1.806102362204724532 ) ) ;
#17079=CARTESIAN_POINT ( 'NONE',  ( 1.054774247047244096, 0.000000000000000000, 0.3371062991588349989 ) ) ;
#17080=ORIENTED_EDGE ( 'NONE', *, *, #11323, .F. ) ;
#17082=ORIENTED_EDGE ( 'NONE', *, *, #23019, .F. ) ;
#17087=CARTESIAN_POINT ( 'NONE',  ( 1.054774247047244540, 0.07405724077823318263, 0.5757874015210394658 ) ) ;
#17089=CARTESIAN_POINT ( 'NONE',  ( 0.7938769800658418418, -0.1410816750883244208, 0.03937005840330796980 ) ) ;
#17091=CARTESIAN_POINT ( 'NONE',  ( -0.9500414927467378812, 0.1787899950787401604, 1.446850393647023614 ) ) ;
#17094=CARTESIAN_POINT ( 'NONE',  ( 0.6971942568897648851, 0.07405724077823318263, 1.028543307032851795 ) ) ;
#17095=ORIENTED_EDGE ( 'NONE', *, *, #16209, .T. ) ;
#17098=CARTESIAN_POINT ( 'NONE',  ( -0.9412147342319837628, -0.1574803149606297803, 1.419783464566930276 ) ) ;
#17099=CARTESIAN_POINT ( 'NONE',  ( -0.6971942568897626646, 0.07405724077823318263, 0.9055118109698585549 ) ) ;
#17100=CARTESIAN_POINT ( 'NONE',  ( 0.9412147342319837628, -0.1574803149606297803, 1.803641732175937706 ) ) ;
#17102=CARTESIAN_POINT ( 'NONE',  ( 1.054774247047244540, 0.07405724077823318263, 0.1476377952218269340 ) ) ;
#17103=CARTESIAN_POINT ( 'NONE',  ( -1.002407869896990045, 0.1264236179284866091, 0.1451771653005673179 ) ) ;
#17104=CARTESIAN_POINT ( 'NONE',  ( 1.033464566929134687, -0.06523048226347956391, 1.611712598317668999 ) ) ;
#17105=EDGE_LOOP ( 'NONE', ( #45774, #3554, #20980, #9574 ) ) ;
#17106=ADVANCED_FACE ( 'NONE', ( #27212 ), #20452, .T. ) ;
#17108=CARTESIAN_POINT ( 'NONE',  ( 1.033464566929134687, -0.06523048226347956391, 0.5979330708661413363 ) ) ;
#17109=EDGE_LOOP ( 'NONE', ( #38678, #32027, #29051, #5843 ) ) ;
#17110=CARTESIAN_POINT ( 'NONE',  ( -0.8019270111902716547, -0.1787899950787401604, 1.663385826717890925 ) ) ;
#17111=AXIS2_PLACEMENT_3D ( 'NONE', #19605, #34952, #16726 ) ;
#17112=VERTEX_POINT ( 'NONE', #42249 ) ;
#17115=CARTESIAN_POINT ( 'NONE',  ( -0.7185039370078746268, -0.06523048226347956391, 0.7800196850393691372 ) ) ;
#17124=CARTESIAN_POINT ( 'NONE',  ( 0.7185039370078739607, 1.928577636452523993E-17, 1.840551181102362266 ) ) ;
#17128=CARTESIAN_POINT ( 'NONE',  ( -0.6971942568897637749, 2.189545951927499583E-17, 0.3617125983714334359 ) ) ;
#17129=CARTESIAN_POINT ( 'NONE',  ( -0.7185039370078746268, 0.06523048226347956391, 1.090059055118109965 ) ) ;
#17132=CARTESIAN_POINT ( 'NONE',  ( 0.8759842519685039353, 0.1787899950787401882, 1.021161417269070837 ) ) ;
#17133=CARTESIAN_POINT ( 'NONE',  ( 0.6971942568897648851, -0.07405724077823297447, 1.461614173174583753 ) ) ;
#17134=CARTESIAN_POINT ( 'NONE',  ( 1.054774247047244540, -0.07405724077823318263, 0.2165354330171024577 ) ) ;
#17139=CARTESIAN_POINT ( 'NONE',  ( -1.033464566929134687, 0.06523048226347956391, 1.695374015640504828 ) ) ;
#17141=CARTESIAN_POINT ( 'NONE',  ( 1.033464566929133799, 0.000000000000000000, 1.663385826771653697 ) ) ;
#17142=CARTESIAN_POINT ( 'NONE',  ( 1.002407869896990045, 0.1264236179284866091, 1.129429133804503937 ) ) ;
#17143=CARTESIAN_POINT ( 'NONE',  ( -1.033464566929133799, 0.000000000000000000, 1.938976377952756014 ) ) ;
#17144=CYLINDRICAL_SURFACE ( 'NONE', #44200, 0.1574803149606299191 ) ;
#17145=CARTESIAN_POINT ( 'NONE',  ( -0.8019270111902717657, -0.1787899950787401604, 1.151574803095843036 ) ) ;
#17146=CARTESIAN_POINT ( 'NONE',  ( 0.9412147342319837628, 0.1574803149606300301, 0.4404527557979849850 ) ) ;
#17151=EDGE_CURVE ( 'NONE', #22900, #20097, #13536, .T. ) ;
#17152=CARTESIAN_POINT ( 'NONE',  ( -0.7185039370078739607, 1.928577636452523993E-17, 0.2952755904436539236 ) ) ;
#17154=CARTESIAN_POINT ( 'NONE',  ( 0.9500414927467378812, 0.1787899950787401604, 1.289370078686393750 ) ) ;
#17155=DIRECTION ( 'NONE',  ( 1.000000000000000000, 0.000000000000000000, -4.336808689942015271E-16 ) ) ;
#17156=FACE_OUTER_BOUND ( 'NONE', #17109, .T. ) ;
#17158=FACE_OUTER_BOUND ( 'NONE', #47183, .T. ) ;
#17159=( BOUNDED_CURVE ( )  B_SPLINE_CURVE ( 2, ( #18491, #14912, #7466, #25708, #7241, #22086, #32669, #32906, #25216 ),
 .UNSPECIFIED., .F., .T. ) 
 B_SPLINE_CURVE_WITH_KNOTS ( ( 3, 2, 2, 2, 3 ),
 ( 0.4600000000000000200, 0.4625000000000000222, 0.4650000000000000244, 0.4675000000000000266, 0.4699999999999999734 ),
 .UNSPECIFIED. ) 
 CURVE ( )  GEOMETRIC_REPRESENTATION_ITEM ( )  RATIONAL_B_SPLINE_CURVE ( ( 1.000000000000000000, 0.9238795325112869605, 1.000000000000000000, 0.9238795325112869605, 1.000000000000000000, 0.9238795325112869605, 1.000000000000000000, 0.9238795325112849621, 1.000000000000000000 ) ) 
 REPRESENTATION_ITEM ( '' )  ) ;
#17161=ORIENTED_EDGE ( 'NONE', *, *, #12877, .F. ) ;
#17163=CARTESIAN_POINT ( 'NONE',  ( -0.7185039370078746268, 0.06523048226347956391, 0.2140748030420794590 ) ) ;
#17165=ORIENTED_EDGE ( 'NONE', *, *, #9702, .T. ) ;
#17166=CARTESIAN_POINT ( 'NONE',  ( -0.9500414927467377701, 0.1787899950787401604, 1.368110236166710125 ) ) ;
#17168=CARTESIAN_POINT ( 'NONE',  ( -0.7185039370078739607, 1.928577636452523993E-17, 0.02952755905511811330 ) ) ;
#17169=EDGE_LOOP ( 'NONE', ( #17654, #24845, #45475, #10936 ) ) ;
#17170=CARTESIAN_POINT ( 'NONE',  ( -1.054774247047244540, 0.07405724077823318263, 1.087598425143086578 ) ) ;
#17171=EDGE_CURVE ( 'NONE', #39764, #7863, #26719, .T. ) ;
#17172=CARTESIAN_POINT ( 'NONE',  ( -0.6971942568897626646, -0.07405724077823297447, 0.7185039369541108556 ) ) ;
#17178=CARTESIAN_POINT ( 'NONE',  ( -1.033464566929133799, 0.000000000000000000, 0.04921259842519685318 ) ) ;
#17179=CARTESIAN_POINT ( 'NONE',  ( -0.8759842519685039353, -0.1574803149606299191, 0.6594488187901103027 ) ) ;
#17180=VECTOR ( 'NONE', #28795, 39.37007874015748143 ) ;
#17181=ORIENTED_EDGE ( 'NONE', *, *, #16492, .F. ) ;
#17182=( BOUNDED_CURVE ( )  B_SPLINE_CURVE ( 2, ( #26488, #41050, #11389, #8248, #4395, #22874, #12103, #567, #22638 ),
 .UNSPECIFIED., .F., .T. ) 
 B_SPLINE_CURVE_WITH_KNOTS ( ( 3, 2, 2, 2, 3 ),
 ( 0.6999999999999999556, 0.7025000000000000133, 0.7049999999999999600, 0.7075000000000000178, 0.7099999999999999645 ),
 .UNSPECIFIED. ) 
 CURVE ( )  GEOMETRIC_REPRESENTATION_ITEM ( )  RATIONAL_B_SPLINE_CURVE ( ( 1.000000000000000000, 0.9238795325112899581, 1.000000000000000000, 0.9238795325112869605, 1.000000000000000000, 0.9238795325112869605, 1.000000000000000000, 0.9238795325112869605, 1.000000000000000000 ) ) 
 REPRESENTATION_ITEM ( '' )  ) ;
#17183=CARTESIAN_POINT ( 'NONE',  ( -0.8019270111902717657, 0.1787899950787401604, 0.7037401574265510495 ) ) ;
#17187=CARTESIAN_POINT ( 'NONE',  ( -0.7495606340400177148, 0.1264236179284866091, 1.656003936954110412 ) ) ;
#17191=CARTESIAN_POINT ( 'NONE',  ( 0.8107537697050253289, 0.1574803149606300301, 0.6126968503937006982 ) ) ;
#17195=DIRECTION ( 'NONE',  ( 0.000000000000000000, 0.000000000000000000, -1.000000000000000000 ) ) ;
#17196=VERTEX_POINT ( 'NONE', #37416 ) ;
#17197=EDGE_CURVE ( 'NONE', #10582, #3955, #2481, .T. ) ;
#17199=CARTESIAN_POINT ( 'NONE',  ( 0.8107537697050254399, 0.1574803149606300301, 1.587106299105070839 ) ) ;
#17200=CARTESIAN_POINT ( 'NONE',  ( 0.8107537697050253289, -0.1574803149606297803, 1.296751968503936370 ) ) ;
#17203=CARTESIAN_POINT ( 'NONE',  ( -0.7185039370078746268, -0.06523048226347956391, 1.331200787401575436 ) ) ;
#17204=CARTESIAN_POINT ( 'NONE',  ( 0.8759842519685039353, 0.000000000000000000, 4.498031496062992574 ) ) ;
#17205=CARTESIAN_POINT ( 'NONE',  ( 1.002407869896990045, 0.1264236179284866091, 0.7357283464029290565 ) ) ;
#17211=EDGE_CURVE ( 'NONE', #37199, #18156, #12017, .T. ) ;
#17212=CARTESIAN_POINT ( 'NONE',  ( -0.9412147342319837628, -0.1574803149606297803, 1.065452755905511806 ) ) ;
#17216=CARTESIAN_POINT ( 'NONE',  ( 0.7495606340400177148, 0.1264236179284866091, 0.9030511810485984947 ) ) ;
#17217=CARTESIAN_POINT ( 'NONE',  ( 1.033464566929134687, -0.06523048226347956391, 1.464074803149607140 ) ) ;
#17218=CARTESIAN_POINT ( 'NONE',  ( 0.7185039370078739607, 1.928577636452523993E-17, 0.6889763778452283605 ) ) ;
#17222=CARTESIAN_POINT ( 'NONE',  ( 0.8107537697050253289, -0.1574803149606297803, 1.208169291231056430 ) ) ;
#17223=CARTESIAN_POINT ( 'NONE',  ( -1.033464566929131356, 0.06523048226348168721, 1.390255905511812218 ) ) ;
#17225=CARTESIAN_POINT ( 'NONE',  ( -0.9500414927467378812, 0.1787899950787401604, 1.845472440891119392 ) ) ;
#17226=CARTESIAN_POINT ( 'NONE',  ( -1.033464566929133799, 0.000000000000000000, 0.8267716534357796299 ) ) ;
#17227=VERTEX_POINT ( 'NONE', #22100 ) ;
#17228=CARTESIAN_POINT ( 'NONE',  ( -1.054774247047244540, 0.07405724077823318263, 1.879921259788756016 ) ) ;
#17229=CARTESIAN_POINT ( 'NONE',  ( -1.054774247047244540, 0.07405724077823318263, 1.481299212544662680 ) ) ;
#17231=CARTESIAN_POINT ( 'NONE',  ( -0.8759842519685039353, 0.1787899950787401882, 0.9768700786863937502 ) ) ;
#17233=CARTESIAN_POINT ( 'NONE',  ( -0.8019270111902717657, -0.1787899950787401604, 1.825787401521040243 ) ) ;
#17235=CARTESIAN_POINT ( 'NONE',  ( -0.7185039370078739607, 1.928577636452523993E-17, 1.919291338582677309 ) ) ;
#17240=LINE ( 'NONE', #31876, #47139 ) ;
#17243=EDGE_LOOP ( 'NONE', ( #6370, #1048, #31339, #16135 ) ) ;
#17244=CONICAL_SURFACE ( 'NONE', #34094, 0.1787899950787401049, 1.047197551196598297 ) ;
#17245=CARTESIAN_POINT ( 'NONE',  ( -0.8759842519685039353, -0.1787899950787401882, 1.237696850339937038 ) ) ;
#17246=ORIENTED_EDGE ( 'NONE', *, *, #39211, .F. ) ;
#17252=CARTESIAN_POINT ( 'NONE',  ( -0.9873396505805591694, -0.1113553986120547346, 0.7923228346456693272 ) ) ;
#17254=EDGE_CURVE ( 'NONE', #34930, #35290, #36726, .T. ) ;
#17255=CARTESIAN_POINT ( 'NONE',  ( 0.9873396505805591694, 0.1113553986120547346, 0.8415354330708662012 ) ) ;
#17256=CARTESIAN_POINT ( 'NONE',  ( -0.9873396505805591694, 0.1113553986120547346, 1.077755905511811108 ) ) ;
#17260=CARTESIAN_POINT ( 'NONE',  ( 0.8759842519685039353, 0.1574803149606299191, 0.1673228345381423399 ) ) ;
#17261=EDGE_CURVE ( 'NONE', #15306, #1625, #18431, .T. ) ;
#17265=EDGE_LOOP ( 'NONE', ( #2468, #33953, #43339, #20477 ) ) ;
#17266=DIRECTION ( 'NONE',  ( -1.000000000000000000, 0.000000000000000000, 0.000000000000000000 ) ) ;
#17269=CARTESIAN_POINT ( 'NONE',  ( -0.9500414927467378812, 0.1787899950787401604, 1.879921259788756016 ) ) ;
#17271=CARTESIAN_POINT ( 'NONE',  ( -0.9500414927467378812, 0.1787899950787401604, 1.451771653489543290 ) ) ;
#17272=CARTESIAN_POINT ( 'NONE',  ( 0.6971942568897637749, 2.189545951927499583E-17, 1.503444881836000002 ) ) ;
#17275=AXIS2_PLACEMENT_3D ( 'NONE', #43283, #28952, #10482 ) ;
#17276=CARTESIAN_POINT ( 'NONE',  ( -0.8019270111902717657, -0.1787899950787401604, 0.6840551180564720113 ) ) ;
#17277=CARTESIAN_POINT ( 'NONE',  ( 0.6971942568897637749, 2.189545951927499583E-17, 0.1648622046706460786 ) ) ;
#17279=CARTESIAN_POINT ( 'NONE',  ( 1.002407869896990045, -0.1264236179284866091, 0.5733267715997795166 ) ) ;
#17280=CARTESIAN_POINT ( 'NONE',  ( -1.002407869896990045, -0.1264236179284866091, 0.4896653542769449086 ) ) ;
#17281=CARTESIAN_POINT ( 'NONE',  ( 0.8759842519685039353, 0.000000000000000000, 4.498031496062992574 ) ) ;
#17284=CARTESIAN_POINT ( 'NONE',  ( -0.8759842519685039353, 0.1787899950787401882, 1.414862204670645829 ) ) ;
#17285=CARTESIAN_POINT ( 'NONE',  ( -0.7646288533564489232, 0.1113553986120547346, 1.481299212598425230 ) ) ;
#17286=CARTESIAN_POINT ( 'NONE',  ( -0.8759842519685039353, -0.1574803149606299191, 0.4330708661417322913 ) ) ;
#17287=CARTESIAN_POINT ( 'NONE',  ( 1.002407869896990045, 0.1264236179284866091, 1.291830708607653477 ) ) ;
#17290=CARTESIAN_POINT ( 'NONE',  ( -1.033464566929134687, -0.06523048226347956391, 0.5585629921259840369 ) ) ;
#17293=ORIENTED_EDGE ( 'NONE', *, *, #33374, .F. ) ;
#17296=ORIENTED_EDGE ( 'NONE', *, *, #34682, .T. ) ;
#17297=CARTESIAN_POINT ( 'NONE',  ( 1.002407869896990045, -0.1264236179284866091, 1.434547244040724534 ) ) ;
#17299=CARTESIAN_POINT ( 'NONE',  ( -0.5314960629921260393, 1.928577636452522761E-17, 5.000000000000000000 ) ) ;
#17301=CARTESIAN_POINT ( 'NONE',  ( 0.8019270111902717657, -0.1787899950787401604, 1.663385826717890925 ) ) ;
#17302=CARTESIAN_POINT ( 'NONE',  ( 0.9500414927467378812, 0.1787899950787401604, 0.3444881889226146243 ) ) ;
#17306=CARTESIAN_POINT ( 'NONE',  ( 0.9873396505805591694, 0.1113553986120547346, 0.5561023620971968784 ) ) ;
#17307=CARTESIAN_POINT ( 'NONE',  ( 1.002407869896990045, -0.1264236179284866091, 0.4896653542769449086 ) ) ;
#17309=CARTESIAN_POINT ( 'NONE',  ( -0.8019270111902716547, 0.1787899950787401604, 0.8267716534895444003 ) ) ;
#17314=CARTESIAN_POINT ( 'NONE',  ( 0.8019270111902717657, -0.1787899950787401604, 1.747047244040724312 ) ) ;
#17317=CARTESIAN_POINT ( 'NONE',  ( 0.8759842519685039353, -0.1787899950787401882, 0.4453740156942677664 ) ) ;
#17318=ORIENTED_EDGE ( 'NONE', *, *, #28485, .T. ) ;
#17319=ADVANCED_FACE ( 'NONE', ( #30280 ), #41, .T. ) ;
#17323=CARTESIAN_POINT ( 'NONE',  ( 0.9500414927467378812, 0.1787899950787401604, 0.6594488188438737408 ) ) ;
#17325=CARTESIAN_POINT ( 'NONE',  ( 0.8182746624668372215, -0.1508186042162177609, 0.03937399344056087547 ) ) ;
#17326=CARTESIAN_POINT ( 'NONE',  ( -1.033464566929133799, 0.000000000000000000, 0.6397637795275591399 ) ) ;
#17327=CARTESIAN_POINT ( 'NONE',  ( 0.7646288533564489232, 0.1113553986120547346, 1.156496062884598608 ) ) ;
#17328=CARTESIAN_POINT ( 'NONE',  ( -0.6971942568897637749, 2.189545951927499583E-17, 1.459153543253322693 ) ) ;
#17330=CARTESIAN_POINT ( 'NONE',  ( 0.7185039370078732945, -0.06523048226347920309, 0.1500984251968504879 ) ) ;
#17331=CARTESIAN_POINT ( 'NONE',  ( 1.054774247047244540, -0.07405724077823318263, 1.205708661363558365 ) ) ;
#17333=ORIENTED_EDGE ( 'NONE', *, *, #29161, .F. ) ;
#17334=CARTESIAN_POINT ( 'NONE',  ( -0.9873396505805591694, 0.1113553986120547346, 0.7135826770578268530 ) ) ;
#17335=CARTESIAN_POINT ( 'NONE',  ( 0.8019270111902717657, -0.1787899950787401604, 1.899606299158834943 ) ) ;
#17336=CARTESIAN_POINT ( 'NONE',  ( -0.9412147342319837628, 0.1574803149606300301, 1.395177165354331672 ) ) ;
#17337=CARTESIAN_POINT ( 'NONE',  ( -0.8019270111902717657, 0.1787899950787401604, 0.9399606298674970661 ) ) ;
#17340=CARTESIAN_POINT ( 'NONE',  ( 0.6971942568897626646, -0.07405724077823297447, 0.1673228345919059168 ) ) ;
#17341=CARTESIAN_POINT ( 'NONE',  ( 0.7646288533564489232, 0.1113553986120547346, 1.628937007766488199 ) ) ;
#17345=VERTEX_POINT ( 'NONE', #11567 ) ;
#17346=CARTESIAN_POINT ( 'NONE',  ( 1.033464566929133799, 1.928577636452524610E-17, 4.498031496062992574 ) ) ;
#17347=CARTESIAN_POINT ( 'NONE',  ( 0.6971942568897626646, -0.07405724077823297447, 0.7578740156942689321 ) ) ;
#17348=CARTESIAN_POINT ( 'NONE',  ( -1.054774247047244540, 0.07405724077823318263, 1.638779527505292766 ) ) ;
#17355=CARTESIAN_POINT ( 'NONE',  ( -0.8759842519685039353, -0.1574803149606299191, 1.210629921152315047 ) ) ;
#17358=CARTESIAN_POINT ( 'NONE',  ( 0.8759842519685039353, -0.1574803149606299191, 1.929133858267716661 ) ) ;
#17360=EDGE_CURVE ( 'NONE', #29380, #36821, #33627, .T. ) ;
#17361=CARTESIAN_POINT ( 'NONE',  ( -1.033464566929133799, 0.000000000000000000, 0.2066929133858267931 ) ) ;
#17362=CARTESIAN_POINT ( 'NONE',  ( 0.7495606340400177148, -0.1264236179284866091, 1.464074803095842370 ) ) ;
#17363=CARTESIAN_POINT ( 'NONE',  ( 0.8759842519685039353, 0.1787899950787401882, 0.1500984251430870220 ) ) ;
#17367=CARTESIAN_POINT ( 'NONE',  ( -1.033464566929133799, 0.000000000000000000, 1.112204724409448842 ) ) ;
#17368=CARTESIAN_POINT ( 'NONE',  ( 0.9873396505805591694, 0.1113553986120547346, 0.6742125983176693316 ) ) ;
#17369=CARTESIAN_POINT ( 'NONE',  ( -0.9873396505805591694, 0.1113553986120547346, 1.697834645561763889 ) ) ;
#17371=CARTESIAN_POINT ( 'NONE',  ( 1.002407869896990045, 0.1264236179284866091, 0.1058070865604098382 ) ) ;
#17373=CARTESIAN_POINT ( 'NONE',  ( 1.054774247047244096, 0.000000000000000000, 1.163877952702141672 ) ) ;
#17374=CARTESIAN_POINT ( 'NONE',  ( -0.7185039370078739607, 1.928577636452523993E-17, 1.830708661309795149 ) ) ;
#17375=DIRECTION ( 'NONE',  ( -1.000000000000000000, 0.000000000000000000, 0.000000000000000000 ) ) ;
#17376=CARTESIAN_POINT ( 'NONE',  ( 0.9873396505805591694, -0.1113553986120547346, 0.4675196849318432601 ) ) ;
#17378=CARTESIAN_POINT ( 'NONE',  ( 1.033121824622407647, 0.02587047616005715145, 0.03936947535289492955 ) ) ;
#17379=CARTESIAN_POINT ( 'NONE',  ( -0.9412147342319837628, -0.1574803149606297803, 0.4650590550105836440 ) ) ;
#17381=CARTESIAN_POINT ( 'NONE',  ( 1.054774247047244540, -0.07405724077823318263, 1.476377952702141449 ) ) ;
#17382=CARTESIAN_POINT ( 'NONE',  ( -1.033464566929133799, 0.000000000000000000, 0.9153543307086614567 ) ) ;
#17383=CARTESIAN_POINT ( 'NONE',  ( -0.7185039370078746268, -0.06523048226347956391, 0.2189960628845991353 ) ) ;
#17385=ORIENTED_EDGE ( 'NONE', *, *, #2963, .F. ) ;
#17389=CARTESIAN_POINT ( 'NONE',  ( 0.7185039370078739607, 1.928577636452523993E-17, 0.5019685039370078705 ) ) ;
#17391=CARTESIAN_POINT ( 'NONE',  ( 0.6971942568897626646, -0.07405724077823297447, 0.3641732282926931630 ) ) ;
#17393=CARTESIAN_POINT ( 'NONE',  ( -0.9500414927467377701, -0.1787899950787401604, 1.353346456639149986 ) ) ;
#17395=CARTESIAN_POINT ( 'NONE',  ( -0.8759842519685039353, 0.1787899950787401882, 0.9424212597887559051 ) ) ;
#17396=CARTESIAN_POINT ( 'NONE',  ( -1.054774247047244540, -0.07405724077823318263, 1.948818897584033927 ) ) ;
#17397=CARTESIAN_POINT ( 'NONE',  ( -0.8759842519685039353, 0.1787899950787401882, 1.094980314906866203 ) ) ;
#17398=CARTESIAN_POINT ( 'NONE',  ( -1.002407869896990045, 0.1264236179284866091, 0.7012795275052913224 ) ) ;
#17407=ORIENTED_EDGE ( 'NONE', *, *, #35349, .T. ) ;
#17408=CARTESIAN_POINT ( 'NONE',  ( -1.033464566929134687, -0.06523048226347956391, 0.3518700786326304231 ) ) ;
#17410=CARTESIAN_POINT ( 'NONE',  ( -0.7495606340400177148, -0.1264236179284866091, 0.5979330708123780092 ) ) ;
#17411=LINE ( 'NONE', #16718, #31502 ) ;
#17414=CARTESIAN_POINT ( 'NONE',  ( -1.002407869896990045, 0.1264236179284866091, 1.646161417269070837 ) ) ;
#17416=EDGE_CURVE ( 'NONE', #38075, #33479, #23350, .T. ) ;
#17418=ORIENTED_EDGE ( 'NONE', *, *, #17793, .F. ) ;
#17419=CARTESIAN_POINT ( 'NONE',  ( 0.7185039370078746268, 0.06523048226347956391, 0.5782480314960627421 ) ) ;
#17421=DIRECTION ( 'NONE',  ( 0.000000000000000000, 0.000000000000000000, -1.000000000000000000 ) ) ;
#17422=CARTESIAN_POINT ( 'NONE',  ( -0.7646288533564489232, 0.1113553986120547346, 1.353346456585388102 ) ) ;
#17423=CARTESIAN_POINT ( 'NONE',  ( 0.7495606340400177148, -0.1264236179284866091, 0.6815944881352126172 ) ) ;
#17425=CARTESIAN_POINT ( 'NONE',  ( 0.8107537697050254399, 0.1574803149606300301, 1.626476377845228916 ) ) ;
#17427=ADVANCED_FACE ( 'NONE', ( #1940 ), #16348, .T. ) ;
#17428=CARTESIAN_POINT ( 'NONE',  ( 1.033464566929134687, -0.06523048226347956391, 1.267224409448818978 ) ) ;
#17434=( BOUNDED_CURVE ( )  B_SPLINE_CURVE ( 2, ( #20377, #39292, #32126, #35016, #24691, #38831, #46246, #17031, #31902 ),
 .UNSPECIFIED., .F., .T. ) 
 B_SPLINE_CURVE_WITH_KNOTS ( ( 3, 2, 2, 2, 3 ),
 ( 0.5899999999999999689, 0.5925000000000000266, 0.5949999999999999734, 0.5975000000000000311, 0.5999999999999999778 ),
 .UNSPECIFIED. ) 
 CURVE ( )  GEOMETRIC_REPRESENTATION_ITEM ( )  RATIONAL_B_SPLINE_CURVE ( ( 1.000000000000000000, 0.9238795325112869605, 1.000000000000000000, 0.9238795325112869605, 1.000000000000000000, 0.9238795325112869605, 1.000000000000000000, 0.9238795325112869605, 1.000000000000000000 ) ) 
 REPRESENTATION_ITEM ( '' )  ) ;
#17435=CARTESIAN_POINT ( 'NONE',  ( 0.6971942568897648851, -0.07405724077823297447, 0.7135826771115916234 ) ) ;
#17439=ORIENTED_EDGE ( 'NONE', *, *, #20241, .T. ) ;
#17442=CARTESIAN_POINT ( 'NONE',  ( 0.8759842519685039353, 0.1787899950787401882, 0.8981299212060788184 ) ) ;
#17443=DIRECTION ( 'NONE',  ( 0.000000000000000000, 0.000000000000000000, 1.000000000000000000 ) ) ;
#17448=LINE ( 'NONE', #28749, #33706 ) ;
#17449=AXIS2_PLACEMENT_3D ( 'NONE', #44992, #23692, #26830 ) ;
#17450=CARTESIAN_POINT ( 'NONE',  ( -0.8019270111902717657, 0.1787899950787401604, 0.07381889758403178958 ) ) ;
#17452=CARTESIAN_POINT ( 'NONE',  ( 0.7495606340400177148, -0.1264236179284866091, 1.941437007820252081 ) ) ;
#17454=CARTESIAN_POINT ( 'NONE',  ( -0.6971942568897637749, 2.189545951927499583E-17, 1.975885826717889815 ) ) ;
#17455=CARTESIAN_POINT ( 'NONE',  ( -1.002407869896990045, -0.1264236179284866091, 1.040846456639149764 ) ) ;
#17456=VECTOR ( 'NONE', #45783, 39.37007874015748143 ) ;
#17457=CARTESIAN_POINT ( 'NONE',  ( -0.8759842519685039353, -0.1787899950787401882, 0.2140748030958428971 ) ) ;
#17458=( BOUNDED_CURVE ( )  B_SPLINE_CURVE ( 2, ( #15952, #12114, #34167, #16183, #37977, #8974, #19280, #811, #26501 ),
 .UNSPECIFIED., .F., .T. ) 
 B_SPLINE_CURVE_WITH_KNOTS ( ( 3, 2, 2, 2, 3 ),
 ( 0.2300000000000000100, 0.2325000000000000122, 0.2349999999999999867, 0.2374999999999999889, 0.2399999999999999911 ),
 .UNSPECIFIED. ) 
 CURVE ( )  GEOMETRIC_REPRESENTATION_ITEM ( )  RATIONAL_B_SPLINE_CURVE ( ( 1.000000000000000000, 0.9238795325112869605, 1.000000000000000000, 0.9238795325112869605, 1.000000000000000000, 0.9238795325112869605, 1.000000000000000000, 0.9238795325112869605, 1.000000000000000000 ) ) 
 REPRESENTATION_ITEM ( '' )  ) ;
#17459=CARTESIAN_POINT ( 'NONE',  ( -0.7185039370078746268, -0.06523048226347956391, 0.6619094488188971281 ) ) ;
#17460=CARTESIAN_POINT ( 'NONE',  ( -1.002407869896990045, 0.1264236179284866091, 1.961122047190330786 ) ) ;
#17461=CARTESIAN_POINT ( 'NONE',  ( -0.7185039370078739607, 1.928577636452523993E-17, 1.879921259842519676 ) ) ;
#17465=LINE ( 'NONE', #32099, #14967 ) ;
#17467=CARTESIAN_POINT ( 'NONE',  ( -1.054774247047244096, 0.000000000000000000, 0.1402559054580474474 ) ) ;
#17469=EDGE_CURVE ( 'NONE', #33274, #20413, #39872, .T. ) ;
#17470=CARTESIAN_POINT ( 'NONE',  ( -1.054774247047244096, 0.000000000000000000, 1.286909448765133801 ) ) ;
#17474=AXIS2_PLACEMENT_3D ( 'NONE', #15987, #1569, #30609 ) ;
#17477=CARTESIAN_POINT ( 'NONE',  ( 0.8759842519685039353, -0.1574803149606299191, 0.3149606299212598381 ) ) ;
#17480=CARTESIAN_POINT ( 'NONE',  ( -0.7185039370078746268, 0.06523048226347956391, 0.7357283464566919395 ) ) ;
#17482=CARTESIAN_POINT ( 'NONE',  ( 0.9412147342319837628, -0.1574803149606297803, 1.764271653435779630 ) ) ;
#17483=ORIENTED_EDGE ( 'NONE', *, *, #18969, .T. ) ;
#17484=CARTESIAN_POINT ( 'NONE',  ( 0.8107537697050234415, -0.1574803149606297803, 0.2239173227271187561 ) ) ;
#17485=CARTESIAN_POINT ( 'NONE',  ( 1.033464566929133799, 0.000000000000000000, 0.7578740157480314821 ) ) ;
#17490=CARTESIAN_POINT ( 'NONE',  ( -0.9873396505805591694, -0.1113553986120547346, 0.4773622047244094890 ) ) ;
#17491=CARTESIAN_POINT ( 'NONE',  ( -0.8759842519685039353, 0.000000000000000000, 0.000000000000000000 ) ) ;
#17492=CARTESIAN_POINT ( 'NONE',  ( 1.033464566929133799, 0.000000000000000000, 0.2362204723334177248 ) ) ;
#17493=VERTEX_POINT ( 'NONE', #41701 ) ;
#17495=CARTESIAN_POINT ( 'NONE',  ( -0.7330379983016587220, 0.1099100077093767003, 0.03937007874015843040 ) ) ;
#17498=CARTESIAN_POINT ( 'NONE',  ( 0.7185039370078746268, 0.06523048226347956391, 0.8833661416247557963 ) ) ;
#17500=CARTESIAN_POINT ( 'NONE',  ( -0.6971942568897637749, 2.189545951927499583E-17, 0.3567913385289137596 ) ) ;
#17503=CARTESIAN_POINT ( 'NONE',  ( -1.002407869896990045, 0.1264236179284866091, 1.409940944828126153 ) ) ;
#17504=CARTESIAN_POINT ( 'NONE',  ( 0.8019270111902717657, 0.1787899950787401604, 1.574803149552536530 ) ) ;
#17505=CARTESIAN_POINT ( 'NONE',  ( -0.8107537697050254399, -0.1574803149606297803, 0.9030511811023625990 ) ) ;
#17507=CARTESIAN_POINT ( 'NONE',  ( -0.6971942568897626646, -0.07405724077823297447, 0.6397637794737947026 ) ) ;
#17508=CARTESIAN_POINT ( 'NONE',  ( -0.8759842519685039353, -0.1574803149606299191, 1.683070866034204638 ) ) ;
#17509=CARTESIAN_POINT ( 'NONE',  ( 0.6971942568897637749, 2.189545951927499583E-17, 0.7160433070328504623 ) ) ;
#17510=CARTESIAN_POINT ( 'NONE',  ( -0.6971942568897637749, 2.189545951927499583E-17, 0.6717519684501732646 ) ) ;
#17512=CARTESIAN_POINT ( 'NONE',  ( 0.8107537697050254399, 0.1574803149606300301, 1.075295275483024726 ) ) ;
#17514=CARTESIAN_POINT ( 'NONE',  ( -1.002407869896990045, 0.1264236179284866091, 1.370570866087968520 ) ) ;
#17516=CARTESIAN_POINT ( 'NONE',  ( -0.7646288533564489232, 0.1113553986120547346, 0.4970472440944882497 ) ) ;
#17517=CARTESIAN_POINT ( 'NONE',  ( 0.6971942568897648851, 0.07405724077823318263, 1.264763779473795813 ) ) ;
#17519=ORIENTED_EDGE ( 'NONE', *, *, #46159, .F. ) ;
#17523=ADVANCED_FACE ( 'NONE', ( #12759 ), #12526, .T. ) ;
#17528=CARTESIAN_POINT ( 'NONE',  ( 0.9873396505805591694, -0.1113553986120547346, 0.3986220472440945017 ) ) ;
#17530=CARTESIAN_POINT ( 'NONE',  ( 1.054774247047244096, 0.000000000000000000, 1.439468503883244210 ) ) ;
#17535=CARTESIAN_POINT ( 'NONE',  ( 0.6971942568897648851, 0.07405724077823318263, 1.692913385773008539 ) ) ;
#17536=CARTESIAN_POINT ( 'NONE',  ( 1.054774247047244540, -0.07405724077823318263, 0.2559055117572600624 ) ) ;
#17540=CARTESIAN_POINT ( 'NONE',  ( -0.7185039370078739607, 1.928577636452523993E-17, 1.683070866141732402 ) ) ;
#17541=CARTESIAN_POINT ( 'NONE',  ( 1.054774247047244540, -0.07405724077823318263, 0.5708661416785201226 ) ) ;
#17542=CARTESIAN_POINT ( 'NONE',  ( -0.7495606340400177148, -0.1264236179284866091, 0.9571850393163149340 ) ) ;
#17548=CARTESIAN_POINT ( 'NONE',  ( 1.002407869896990045, 0.1264236179284866091, 1.606791338528913426 ) ) ;
#17553=CARTESIAN_POINT ( 'NONE',  ( 0.8107537697050253289, 0.1574803149606300301, 0.02214566929133862661 ) ) ;
#17558=CARTESIAN_POINT ( 'NONE',  ( 0.6971942568897626646, -0.07405724077823297447, 0.08858267711159097113 ) ) ;
#17560=CARTESIAN_POINT ( 'NONE',  ( 0.6971942568897637749, 2.189545951927499583E-17, 0.5536417322297008115 ) ) ;
#17562=CARTESIAN_POINT ( 'NONE',  ( -0.6971942568897637749, 2.189545951927499583E-17, 1.419783464513165505 ) ) ;
#17563=ORIENTED_EDGE ( 'NONE', *, *, #38952, .F. ) ;
#17565=CARTESIAN_POINT ( 'NONE',  ( 0.6971942568897637749, 2.189545951927499583E-17, 1.188484251914740275 ) ) ;
#17566=CARTESIAN_POINT ( 'NONE',  ( -0.8759842519685039353, 0.1574803149606299191, 0.6791338581601890079 ) ) ;
#17567=CARTESIAN_POINT ( 'NONE',  ( 0.9500414927467378812, 0.1787899950787401604, 1.840551181048599938 ) ) ;
#17568=CARTESIAN_POINT ( 'NONE',  ( -1.033464566929133799, 0.000000000000000000, 1.348425196850393748 ) ) ;
#17569=CARTESIAN_POINT ( 'NONE',  ( -0.8019270111902717657, -0.1787899950787401604, 0.9547244093950547628 ) ) ;
#17572=CARTESIAN_POINT ( 'NONE',  ( 0.9500414927467377701, 0.1787899950787401604, 0.2312992125446618197 ) ) ;
#17573=CARTESIAN_POINT ( 'NONE',  ( -0.8019270111902716547, 0.1787899950787401604, 0.1131889763241894220 ) ) ;
#17574=CARTESIAN_POINT ( 'NONE',  ( -1.002407869896990045, 0.1264236179284866091, 0.5388779527021417826 ) ) ;
#17575=CARTESIAN_POINT ( 'NONE',  ( 0.7185039370078746268, -0.06523048226347956391, 1.518208661309795149 ) ) ;
#17577=( BOUNDED_CURVE ( )  B_SPLINE_CURVE ( 2, ( #30885, #23908, #23197, #41597, #45445, #4965, #12667, #12428, #27292 ),
 .UNSPECIFIED., .F., .T. ) 
 B_SPLINE_CURVE_WITH_KNOTS ( ( 3, 2, 2, 2, 3 ),
 ( 0.2300000000000000100, 0.2325000000000000122, 0.2349999999999999867, 0.2374999999999999889, 0.2399999999999999911 ),
 .UNSPECIFIED. ) 
 CURVE ( )  GEOMETRIC_REPRESENTATION_ITEM ( )  RATIONAL_B_SPLINE_CURVE ( ( 1.000000000000000000, 0.9238795325112869605, 1.000000000000000000, 0.9238795325112869605, 1.000000000000000000, 0.9238795325112869605, 1.000000000000000000, 0.9238795325112869605, 1.000000000000000000 ) ) 
 REPRESENTATION_ITEM ( '' )  ) ;
#17579=CARTESIAN_POINT ( 'NONE',  ( 0.9873396505805591694, 0.1113553986120547346, 1.776574803042078488 ) ) ;
#17580=CARTESIAN_POINT ( 'NONE',  ( 0.8759842519685039353, 0.1787899950787401882, 0.8243110235682834519 ) ) ;
#17581=CARTESIAN_POINT ( 'NONE',  ( -0.7495606340400177148, -0.1264236179284866091, 1.739665354276945131 ) ) ;
#17582=EDGE_CURVE ( 'NONE', #31513, #27525, #31896, .T. ) ;
#17590=EDGE_CURVE ( 'NONE', #1000, #37016, #25158, .T. ) ;
#17591=ORIENTED_EDGE ( 'NONE', *, *, #26379, .F. ) ;
#17592=CARTESIAN_POINT ( 'NONE',  ( 0.7495606340400177148, -0.1264236179284866091, 1.109744094434425232 ) ) ;
#17593=EDGE_CURVE ( 'NONE', #42069, #10600, #26409, .T. ) ;
#17596=CARTESIAN_POINT ( 'NONE',  ( 0.9500414927467378812, 0.1787899950787401604, 0.06889763774151215492 ) ) ;
#17599=CARTESIAN_POINT ( 'NONE',  ( -0.7495606340400177148, -0.1264236179284866091, 0.4847440944344252323 ) ) ;
#17600=CARTESIAN_POINT ( 'NONE',  ( -0.7124824329870323991, -0.03455856718743761241, 1.983908545787091082 ) ) ;
#17602=CARTESIAN_POINT ( 'NONE',  ( 0.7495606340400177148, 0.1264236179284866091, 1.532972440891118060 ) ) ;
#17603=CARTESIAN_POINT ( 'NONE',  ( 0.8759842519685039353, 0.1574803149606299191, 1.673228346456693050 ) ) ;
#17606=CARTESIAN_POINT ( 'NONE',  ( -0.8759842491179902213, 0.1574803149606299191, 1.978346456692913646 ) ) ;
#17609=CARTESIAN_POINT ( 'NONE',  ( -1.033464566929134687, 0.06523048226347956391, 1.774114173120818316 ) ) ;
#17611=CARTESIAN_POINT ( 'NONE',  ( 0.7495606340400177148, 0.1264236179284866091, 0.1943897637257641919 ) ) ;
#17612=CARTESIAN_POINT ( 'NONE',  ( 0.7032143776996268025, -0.01662162624712908501, 0.03937554043527696085 ) ) ;
#17613=CARTESIAN_POINT ( 'NONE',  ( 1.002407869896990045, -0.1264236179284866091, 1.198326771599779628 ) ) ;
#17614=CARTESIAN_POINT ( 'NONE',  ( -0.9412147342319837628, 0.1574803149606300301, 1.818405511703497845 ) ) ;
#17615=CARTESIAN_POINT ( 'NONE',  ( 0.9873396505805591694, -0.1113553986120547346, 0.5462598424121581919 ) ) ;
#17616=ORIENTED_EDGE ( 'NONE', *, *, #29850, .F. ) ;
#17617=CARTESIAN_POINT ( 'NONE',  ( -1.054774247047244540, -0.07405724077823318263, 1.048228346402930944 ) ) ;
#17619=CARTESIAN_POINT ( 'NONE',  ( 0.8940612688331117663, 0.1724986514511060165, 0.03937022261624964492 ) ) ;
#17620=CARTESIAN_POINT ( 'NONE',  ( -0.7185039370078739607, 1.928577636452523993E-17, 0.4527559054042842868 ) ) ;
#17622=CARTESIAN_POINT ( 'NONE',  ( 1.054774247047244540, 0.07405724077823318263, 1.520669291284818758 ) ) ;
#17623=CARTESIAN_POINT ( 'NONE',  ( -0.7185039370078746268, 0.06523048226347977208, 0.1058070866141732902 ) ) ;
#17624=CARTESIAN_POINT ( 'NONE',  ( -0.8107537697050254399, 0.1574803149606300301, 0.2878937006798746312 ) ) ;
#17629=CARTESIAN_POINT ( 'NONE',  ( 0.7646288533564489232, 0.1113553986120547346, 0.4478346455617645550 ) ) ;
#17631=CARTESIAN_POINT ( 'NONE',  ( 0.7185039370078766252, -0.06523048226348168721, 1.281988188868851353 ) ) ;
#17632=CARTESIAN_POINT ( 'NONE',  ( 1.033464566929133799, 0.000000000000000000, 1.112204724409448842 ) ) ;
#17633=CARTESIAN_POINT ( 'NONE',  ( 0.6971942568897626646, -0.07405724077823297447, 0.6397637794737947026 ) ) ;
#17634=ORIENTED_EDGE ( 'NONE', *, *, #20766, .T. ) ;
#17635=CARTESIAN_POINT ( 'NONE',  ( -1.002407869896990045, -0.1264236179284866091, 1.355807086560409491 ) ) ;
#17637=CARTESIAN_POINT ( 'NONE',  ( -0.8019270111902717657, 0.1787899950787401604, 1.062992125930488418 ) ) ;
#17638=CARTESIAN_POINT ( 'NONE',  ( -0.9412147342319837628, 0.1574803149606300301, 0.09596456692913378494 ) ) ;
#17639=CARTESIAN_POINT ( 'NONE',  ( -1.002407869896990045, -0.1264236179284866091, 1.119586614119464585 ) ) ;
#17640=CARTESIAN_POINT ( 'NONE',  ( -0.6971942568897637749, 2.189545951927499583E-17, 0.8341535432533228045 ) ) ;
#17642=CARTESIAN_POINT ( 'NONE',  ( -1.002407869896990045, 0.1264236179284866091, 0.1894685038832444879 ) ) ;
#17649=ORIENTED_EDGE ( 'NONE', *, *, #38353, .T. ) ;
#17650=CARTESIAN_POINT ( 'NONE',  ( 1.033464566929134687, 0.06523048226347956391, 0.7603346456692923194 ) ) ;
#17652=CARTESIAN_POINT ( 'NONE',  ( -1.002407869896990045, 0.1264236179284866091, 0.5782480314422993040 ) ) ;
#17653=CARTESIAN_POINT ( 'NONE',  ( 0.8107537697050254399, 0.1574803149606300301, 1.350885826664126821 ) ) ;
#17654=ORIENTED_EDGE ( 'NONE', *, *, #5795, .F. ) ;
#17655=CARTESIAN_POINT ( 'NONE',  ( -0.9500414927467377701, -0.1787899950787401604, 1.751968503883245987 ) ) ;
#17658=CARTESIAN_POINT ( 'NONE',  ( -0.9873396505805591694, -0.1113553986120547346, 0.1919291337507405548 ) ) ;
#17661=CARTESIAN_POINT ( 'NONE',  ( -0.9873396505805591694, -0.1113553986120547346, 1.412401574695621997 ) ) ;
#17662=CARTESIAN_POINT ( 'NONE',  ( 0.8759842519685039353, -0.1787899950787401882, 0.8439960629383622681 ) ) ;
#17665=ORIENTED_EDGE ( 'NONE', *, *, #5461, .F. ) ;
#17666=CARTESIAN_POINT ( 'NONE',  ( 0.7646288533564489232, 0.1113553986120547346, 0.1722440943806619884 ) ) ;
#17667=CARTESIAN_POINT ( 'NONE',  ( 0.9873396505805591694, -0.1113553986120547346, 1.304133858267716661 ) ) ;
#17668=CARTESIAN_POINT ( 'NONE',  ( 0.8151215678306394929, -0.1614990644632125771, 1.987062530839091901 ) ) ;
#17671=CARTESIAN_POINT ( 'NONE',  ( 0.6971942568897637749, 2.189545951927499583E-17, 0.5930118109698583329 ) ) ;
#17676=CARTESIAN_POINT ( 'NONE',  ( 0.8759842519685039353, -0.1787899950787401882, 0.9178149605761574126 ) ) ;
#17677=CARTESIAN_POINT ( 'NONE',  ( 0.8107537697050254399, 0.1574803149606300301, 1.478838582677165059 ) ) ;
#17678=CARTESIAN_POINT ( 'NONE',  ( 0.9873396505805591694, -0.1113553986120547346, 0.7037401573727875004 ) ) ;
#17684=CARTESIAN_POINT ( 'NONE',  ( -0.7495606340400177148, 0.1264236179284866091, 0.03690944876513417572 ) ) ;
#17686=CARTESIAN_POINT ( 'NONE',  ( 0.9500414927467378812, -0.1787899950787401604, 1.948818897584033927 ) ) ;
#17688=CARTESIAN_POINT ( 'NONE',  ( -0.7495606340400177148, 0.1264236179284866091, 1.970964566875370139 ) ) ;
#17691=CARTESIAN_POINT ( 'NONE',  ( -0.8019270111902717657, -0.1787899950787401604, 1.545275590497416696 ) ) ;
#17692=CARTESIAN_POINT ( 'NONE',  ( 0.6971942568897648851, 0.07405724077823318263, 0.8710629920722218200 ) ) ;
#17693=CARTESIAN_POINT ( 'NONE',  ( -0.6971942568897648851, 0.07405724077823318263, 0.8267716534895444003 ) ) ;
#17695=CARTESIAN_POINT ( 'NONE',  ( -0.6971942568897626646, -0.07405724077823297447, 0.3641732282926931630 ) ) ;
#17697=CARTESIAN_POINT ( 'NONE',  ( -0.9412147342319837628, -0.1574803149606297803, 0.6717519685039375910 ) ) ;
#17698=CARTESIAN_POINT ( 'NONE',  ( -0.7495606340400177148, -0.1264236179284866091, 1.941437007820252081 ) ) ;
#17699=CARTESIAN_POINT ( 'NONE',  ( -0.9873396505805591694, 0.1113553986120547346, 1.471456692913385877 ) ) ;
#17700=CARTESIAN_POINT ( 'NONE',  ( -1.033464566929134687, 0.06523048226347956391, 1.941437007874014187 ) ) ;
#17705=CARTESIAN_POINT ( 'NONE',  ( -0.7495606340400177148, -0.1264236179284866091, 0.08612204719033110523 ) ) ;
#17707=CARTESIAN_POINT ( 'NONE',  ( -1.002407869896990045, -0.1264236179284866091, 1.281988188922614125 ) ) ;
#17708=ORIENTED_EDGE ( 'NONE', *, *, #46159, .T. ) ;
#17711=( BOUNDED_CURVE ( )  B_SPLINE_CURVE ( 2, ( #35665, #10748, #39467, #43301, #38999, #3040, #39690, #32317, #13600 ),
 .UNSPECIFIED., .F., .T. ) 
 B_SPLINE_CURVE_WITH_KNOTS ( ( 3, 2, 2, 2, 3 ),
 ( 0.8699999999999999956, 0.8725000000000000533, 0.8750000000000000000, 0.8774999999999999467, 0.8800000000000000044 ),
 .UNSPECIFIED. ) 
 CURVE ( )  GEOMETRIC_REPRESENTATION_ITEM ( )  RATIONAL_B_SPLINE_CURVE ( ( 1.000000000000000000, 0.9238795325112869605, 1.000000000000000000, 0.9238795325112869605, 1.000000000000000000, 0.9238795325112869605, 1.000000000000000000, 0.9238795325112869605, 1.000000000000000000 ) ) 
 REPRESENTATION_ITEM ( '' )  ) ;
#17712=CARTESIAN_POINT ( 'NONE',  ( -0.7646288533564489232, -0.1113553986120547346, 1.363188976270427455 ) ) ;
#17716=CARTESIAN_POINT ( 'NONE',  ( -0.9873396505805591694, 0.1113553986120547346, 0.9891732282389291697 ) ) ;
#17717=CARTESIAN_POINT ( 'NONE',  ( -0.9873396505805591694, -0.1113553986120547346, 0.6742125984251968740 ) ) ;
#17718=CARTESIAN_POINT ( 'NONE',  ( 0.8759842519685039353, 0.1787899950787401882, 0.3912401574265515491 ) ) ;
#17721=VECTOR ( 'NONE', #35391, 39.37007874015748143 ) ;
#17722=CARTESIAN_POINT ( 'NONE',  ( 0.7646288533564489232, 0.1113553986120547346, 1.786417322727117840 ) ) ;
#17724=CARTESIAN_POINT ( 'NONE',  ( 0.8759842519685039353, 0.1574803149606299191, 0.8464566929133857665 ) ) ;
#17727=CARTESIAN_POINT ( 'NONE',  ( -0.9412147342319837628, 0.1574803149606300301, 1.080216535433071501 ) ) ;
#17729=CARTESIAN_POINT ( 'NONE',  ( 0.7185039370078739607, 1.928577636452523993E-17, 0.2559055117034968463 ) ) ;
#17731=DIRECTION ( 'NONE',  ( 0.000000000000000000, 0.000000000000000000, 1.000000000000000000 ) ) ;
#17735=CARTESIAN_POINT ( 'NONE',  ( 0.9873396505805591694, -0.1113553986120547346, 1.018700787294047228 ) ) ;
#17736=( BOUNDED_CURVE ( )  B_SPLINE_CURVE ( 2, ( #26071, #11226, #410, #15060, #44253, #30177, #7845, #33514, #15287 ),
 .UNSPECIFIED., .F., .T. ) 
 B_SPLINE_CURVE_WITH_KNOTS ( ( 3, 2, 2, 2, 3 ),
 ( 0.1600000000000000033, 0.1625000000000000056, 0.1650000000000000078, 0.1675000000000000100, 0.1700000000000000122 ),
 .UNSPECIFIED. ) 
 CURVE ( )  GEOMETRIC_REPRESENTATION_ITEM ( )  RATIONAL_B_SPLINE_CURVE ( ( 1.000000000000000000, 0.9238795325112869605, 1.000000000000000000, 0.9238795325112869605, 1.000000000000000000, 0.9238795325112869605, 1.000000000000000000, 0.9238795325112869605, 1.000000000000000000 ) ) 
 REPRESENTATION_ITEM ( '' )  ) ;
#17738=CARTESIAN_POINT ( 'NONE',  ( -0.9500414927467378812, 0.1787899950787401604, 0.3838582676627718127 ) ) ;
#17742=CARTESIAN_POINT ( 'NONE',  ( -1.054774247047244540, -0.07405724077823318263, 1.638779527505292988 ) ) ;
#17744=EDGE_CURVE ( 'NONE', #46310, #42055, #30107, .T. ) ;
#17745=CARTESIAN_POINT ( 'NONE',  ( 1.054774247047244540, 0.07405724077823318263, 1.604330708607653921 ) ) ;
#17747=CARTESIAN_POINT ( 'NONE',  ( -1.002407869896990045, -0.1264236179284866091, 0.6520669290800944484 ) ) ;
#17748=CARTESIAN_POINT ( 'NONE',  ( 0.8759842519685039353, -0.1787899950787401882, 0.2140748030958428971 ) ) ;
#17749=CARTESIAN_POINT ( 'NONE',  ( -1.033464566929134687, -0.06523048226347956391, 0.4699803148531029873 ) ) ;
#17750=CARTESIAN_POINT ( 'NONE',  ( 0.8759842519685039353, 0.1787899950787401882, 0.7062007873478109987 ) ) ;
#17751=CARTESIAN_POINT ( 'NONE',  ( -0.6971942568897637749, 2.189545951927499583E-17, 0.7504921259304880854 ) ) ;
#17756=CARTESIAN_POINT ( 'NONE',  ( 0.7185039370078746268, 0.06523048226347956391, 1.080216535325543958 ) ) ;
#17758=CARTESIAN_POINT ( 'NONE',  ( -0.9500414927467378812, -0.1787899950787401604, 1.437007873961985371 ) ) ;
#17759=CARTESIAN_POINT ( 'NONE',  ( -0.8759842519685039353, -0.1574803149606299191, 0.3937007874015748254 ) ) ;
#17760=CARTESIAN_POINT ( 'NONE',  ( 0.8759842519685039353, 0.1787899950787401882, 1.532972440891118060 ) ) ;
#17761=CARTESIAN_POINT ( 'NONE',  ( -0.9873396505805591694, -0.1113553986120547346, 1.579724409448818978 ) ) ;
#17762=ORIENTED_EDGE ( 'NONE', *, *, #14189, .T. ) ;
#17765=CARTESIAN_POINT ( 'NONE',  ( 1.033464566929133799, 0.000000000000000000, 0.4822834645669291653 ) ) ;
#17767=CARTESIAN_POINT ( 'NONE',  ( 0.6971942568897648851, 0.07405724077823318263, 1.456692913332062744 ) ) ;
#17772=CARTESIAN_POINT ( 'NONE',  ( -1.033464566929133799, 0.000000000000000000, 0.9842519683964094934 ) ) ;
#17774=CARTESIAN_POINT ( 'NONE',  ( 0.7495606340400177148, -0.1264236179284866091, 1.660925196796630088 ) ) ;
#17775=CARTESIAN_POINT ( 'NONE',  ( 1.002407869896990045, -0.1264236179284866091, 0.3715551180564728440 ) ) ;
#17777=DIRECTION ( 'NONE',  ( 0.000000000000000000, 0.000000000000000000, -1.000000000000000000 ) ) ;
#17778=CARTESIAN_POINT ( 'NONE',  ( 0.7185039370078739607, 1.928577636452523993E-17, 0.5708661416247566844 ) ) ;
#17779=CARTESIAN_POINT ( 'NONE',  ( 0.7495606340400177148, 0.1264236179284866091, 0.6668307086076534773 ) ) ;
#17781=CARTESIAN_POINT ( 'NONE',  ( -0.7495606340400177148, -0.1264236179284866091, 1.035925196796629866 ) ) ;
#17782=CARTESIAN_POINT ( 'NONE',  ( -0.8959059128496592583, 0.1723076359399909885, 0.03937007874015844427 ) ) ;
#17785=CARTESIAN_POINT ( 'NONE',  ( -0.8875170849661903061, -0.1744992477839313050, 1.988385192983781025 ) ) ;
#17788=CARTESIAN_POINT ( 'NONE',  ( 0.8759842519685039353, -0.1787899950787401882, 1.670767716481669440 ) ) ;
#17793=EDGE_CURVE ( 'NONE', #11128, #23920, #42162, .T. ) ;
#17794=CARTESIAN_POINT ( 'NONE',  ( 0.9873396505805591694, -0.1113553986120547346, 1.333661417215306955 ) ) ;
#17796=CARTESIAN_POINT ( 'NONE',  ( -0.9500414927467378812, -0.1787899950787401604, 0.4133858267178901480 ) ) ;
#17797=CARTESIAN_POINT ( 'NONE',  ( 0.8019270111902717657, -0.1787899950787401604, 0.5610236219934807700 ) ) ;
#17799=CARTESIAN_POINT ( 'NONE',  ( 0.7495606340400177148, -0.1264236179284866091, 0.05167322829269323931 ) ) ;
#17801=CARTESIAN_POINT ( 'NONE',  ( -1.054774247047244096, 0.000000000000000000, 1.636318897584031484 ) ) ;
#17802=ORIENTED_EDGE ( 'NONE', *, *, #42714, .F. ) ;
#17803=VECTOR ( 'NONE', #852, 39.37007874015748143 ) ;
#17806=CARTESIAN_POINT ( 'NONE',  ( 0.7495606340400177148, -0.1264236179284866091, 1.114665354276944909 ) ) ;
#17807=CARTESIAN_POINT ( 'NONE',  ( -0.7646288533564489232, 0.1113553986120547346, 0.6840551180027086842 ) ) ;
#17808=CARTESIAN_POINT ( 'NONE',  ( 0.9412147342319837628, -0.1574803149606297803, 1.498523622047243764 ) ) ;
#17809=CARTESIAN_POINT ( 'NONE',  ( 1.054774247047244540, -0.07405724077823318263, 1.870078740103715331 ) ) ;
#17810=CARTESIAN_POINT ( 'NONE',  ( -0.7185039370078746268, -0.06523048226347956391, 0.5831692913385827515 ) ) ;
#17811=CARTESIAN_POINT ( 'NONE',  ( -0.6971942568897637749, 2.189545951927499583E-17, 0.9079724408911180600 ) ) ;
#17814=CARTESIAN_POINT ( 'NONE',  ( 1.054774247047244096, 0.000000000000000000, 0.3026574802611972648 ) ) ;
#17815=CARTESIAN_POINT ( 'NONE',  ( -1.054774247047244096, 0.000000000000000000, 0.2189960629383626012 ) ) ;
#17817=CARTESIAN_POINT ( 'NONE',  ( -0.8019270111902717657, 0.1787899950787401604, 0.7431102361667091261 ) ) ;
#17818=CARTESIAN_POINT ( 'NONE',  ( 0.7646288533564489232, -0.1113553986120547346, 1.560039369971212508 ) ) ;
#17819=ORIENTED_EDGE ( 'NONE', *, *, #11248, .T. ) ;
#17822=CARTESIAN_POINT ( 'NONE',  ( 1.054774247047244096, 0.000000000000000000, 0.8538385826234016207 ) ) ;
#17823=CARTESIAN_POINT ( 'NONE',  ( -1.054774247047244096, 0.000000000000000000, 1.872539370024976391 ) ) ;
#17824=CARTESIAN_POINT ( 'NONE',  ( 0.9500414927467378812, -0.1787899950787401604, 1.943897637741510254 ) ) ;
#17832=CARTESIAN_POINT ( 'NONE',  ( 1.054774247047244540, 0.07405724077823318263, 1.048228346402928723 ) ) ;
#17835=CARTESIAN_POINT ( 'NONE',  ( -0.5314960629921260393, 0.000000000000000000, 4.498031496062992574 ) ) ;
#17837=CARTESIAN_POINT ( 'NONE',  ( 0.9412147342319837628, 0.1574803149606300301, 1.946358267716538082 ) ) ;
#17838=AXIS2_PLACEMENT_3D ( 'NONE', #4918, #19542, #34190 ) ;
#17840=CARTESIAN_POINT ( 'NONE',  ( -0.6971942568897648851, 0.07405724077823318263, 0.4773622046706456068 ) ) ;
#17842=CARTESIAN_POINT ( 'NONE',  ( 0.6971942568897637749, 2.189545951927499583E-17, 1.188484251914740275 ) ) ;
#17843=CARTESIAN_POINT ( 'NONE',  ( 1.054774247047244540, 0.07405724077823318263, 1.481299212544662902 ) ) ;
#17845=CARTESIAN_POINT ( 'NONE',  ( 0.7646288533564489232, 0.1113553986120547346, 1.717519685039369914 ) ) ;
#17846=CARTESIAN_POINT ( 'NONE',  ( -0.9412147342319837628, 0.1574803149606300301, 1.001476377952755348 ) ) ;
#17848=CARTESIAN_POINT ( 'NONE',  ( -1.033464566929134687, -0.06523048226347956391, 1.729822834538142784 ) ) ;
#17849=CARTESIAN_POINT ( 'NONE',  ( 0.6971942568897626646, -0.07405724077823297447, 0.2411417322297011168 ) ) ;
#17850=( BOUNDED_CURVE ( )  B_SPLINE_CURVE ( 2, ( #13935, #28579, #43144, #10352, #5557, #31219, #45796, #13003, #35046 ),
 .UNSPECIFIED., .F., .T. ) 
 B_SPLINE_CURVE_WITH_KNOTS ( ( 3, 2, 2, 2, 3 ),
 ( 0.3099999999999999978, 0.3125000000000000000, 0.3150000000000000022, 0.3175000000000000044, 0.3200000000000000067 ),
 .UNSPECIFIED. ) 
 CURVE ( )  GEOMETRIC_REPRESENTATION_ITEM ( )  RATIONAL_B_SPLINE_CURVE ( ( 1.000000000000000000, 0.9238795325112869605, 1.000000000000000000, 0.9238795325112869605, 1.000000000000000000, 0.9238795325112869605, 1.000000000000000000, 0.9238795325112869605, 1.000000000000000000 ) ) 
 REPRESENTATION_ITEM ( '' )  ) ;
#17851=EDGE_CURVE ( 'NONE', #36580, #29380, #16893, .T. ) ;
#17853=CARTESIAN_POINT ( 'NONE',  ( 0.6971942568897648851, 0.07405724077823318263, 1.062992125930488418 ) ) ;
#17855=DIRECTION ( 'NONE',  ( -1.000000000000000000, 0.000000000000000000, 0.000000000000000000 ) ) ;
#17856=CARTESIAN_POINT ( 'NONE',  ( 0.7185039370078746268, 0.06523048226347956391, 0.4502952754830242266 ) ) ;
#17859=EDGE_CURVE ( 'NONE', #17892, #37198, #21806, .T. ) ;
#17860=CARTESIAN_POINT ( 'NONE',  ( -0.9412147342319837628, 0.1574803149606300301, 1.897145669183811778 ) ) ;
#17862=CARTESIAN_POINT ( 'NONE',  ( -0.7646288533564489232, -0.1113553986120547346, 0.3789370077664886427 ) ) ;
#17863=CARTESIAN_POINT ( 'NONE',  ( 0.6971942568897648851, 0.07405724077823318263, 1.417322834591906222 ) ) ;
#17872=CARTESIAN_POINT ( 'NONE',  ( 0.8759842519685039353, 0.1787899950787401882, 0.5487204723871811352 ) ) ;
#17873=ORIENTED_EDGE ( 'NONE', *, *, #33087, .T. ) ;
#17875=CARTESIAN_POINT ( 'NONE',  ( -0.7495606340400177148, -0.1264236179284866091, 1.075295275536787276 ) ) ;
#17876=CARTESIAN_POINT ( 'NONE',  ( -0.9412147342319837628, 0.1574803149606300301, 0.1747047244094488694 ) ) ;
#17878=CARTESIAN_POINT ( 'NONE',  ( -0.7495606340400177148, -0.1264236179284866091, 1.149114173174582643 ) ) ;
#17879=CARTESIAN_POINT ( 'NONE',  ( -0.8019270111902717657, -0.1787899950787401604, 0.2509842519147403861 ) ) ;
#17880=FACE_OUTER_BOUND ( 'NONE', #39784, .T. ) ;
#17883=ORIENTED_EDGE ( 'NONE', *, *, #41559, .T. ) ;
#17885=VERTEX_POINT ( 'NONE', #36191 ) ;
#17886=ORIENTED_EDGE ( 'NONE', *, *, #47, .F. ) ;
#17890=CARTESIAN_POINT ( 'NONE',  ( -1.054774247047244540, -0.07405724077823318263, 0.6102362204186774219 ) ) ;
#17892=VERTEX_POINT ( 'NONE', #6693 ) ;
#17893=CARTESIAN_POINT ( 'NONE',  ( -1.054774247047244540, -0.07405724077823318263, 1.796259842465920853 ) ) ;
#17896=CARTESIAN_POINT ( 'NONE',  ( -0.6971942568897626646, -0.07405724077823297447, 0.04921259837143338728 ) ) ;
#17900=CARTESIAN_POINT ( 'NONE',  ( -0.7185039370078746268, 0.06523048226347956391, 1.434547243986962428 ) ) ;
#17901=CARTESIAN_POINT ( 'NONE',  ( 1.002407869896990045, -0.1264236179284866091, 0.8095472440407244230 ) ) ;
#17905=CARTESIAN_POINT ( 'NONE',  ( 0.8759842519685039353, -0.1574803149606299191, 1.181102362204724310 ) ) ;
#17906=CARTESIAN_POINT ( 'NONE',  ( 0.7753512748119036901, -0.1383705155101382922, 1.986206650002734886 ) ) ;
#17907=CARTESIAN_POINT ( 'NONE',  ( 0.7646288533564489232, -0.1113553986120547346, 1.845472440944881942 ) ) ;
#17909=CARTESIAN_POINT ( 'NONE',  ( 1.002407869896990045, 0.1264236179284866091, 0.6963582676627716461 ) ) ;
#17913=ORIENTED_EDGE ( 'NONE', *, *, #20556, .F. ) ;
#17916=CARTESIAN_POINT ( 'NONE',  ( 1.054774247047244096, 0.000000000000000000, 1.045767716481669440 ) ) ;
#17922=CARTESIAN_POINT ( 'NONE',  ( -0.6971942568897626646, -0.07405724077823297447, 0.1230314960092287191 ) ) ;
#17923=ORIENTED_EDGE ( 'NONE', *, *, #1026, .F. ) ;
#17924=CARTESIAN_POINT ( 'NONE',  ( 0.6971942568897648851, 0.07405724077823318263, 1.934055118056471567 ) ) ;
#17925=ORIENTED_EDGE ( 'NONE', *, *, #1132, .F. ) ;
#17926=CARTESIAN_POINT ( 'NONE',  ( -0.9500414927467377701, -0.1787899950787401604, 1.909448818843873186 ) ) ;
#17927=CARTESIAN_POINT ( 'NONE',  ( -0.9500414927467378812, -0.1787899950787401604, 1.707677165300566235 ) ) ;
#17928=CARTESIAN_POINT ( 'NONE',  ( 0.6971942568897637749, 2.189545951927499583E-17, 0.8735236219934803259 ) ) ;
#17930=CARTESIAN_POINT ( 'NONE',  ( -0.6971942568897648851, 0.07405724077823318263, 1.894685039316315489 ) ) ;
#17931=CARTESIAN_POINT ( 'NONE',  ( 0.7185039370078739607, 1.928577636452523993E-17, 0.3051181102362204856 ) ) ;
#17932=CARTESIAN_POINT ( 'NONE',  ( -0.9873396505805591694, -0.1113553986120547346, 1.894685039370078927 ) ) ;
#17936=CARTESIAN_POINT ( 'NONE',  ( -0.7185039370078739607, 1.928577636452523993E-17, 1.318897637687747926 ) ) ;
#17937=CARTESIAN_POINT ( 'NONE',  ( -0.8759842519685039353, -0.1787899950787401882, 0.1697834645131655606 ) ) ;
#17939=CARTESIAN_POINT ( 'NONE',  ( -0.8759842519685039353, 0.1787899950787401882, 1.414862204670645829 ) ) ;
#17940=ORIENTED_EDGE ( 'NONE', *, *, #26036, .T. ) ;
#17943=FACE_OUTER_BOUND ( 'NONE', #21695, .T. ) ;
#17945=CARTESIAN_POINT ( 'NONE',  ( 0.9873396505805591694, 0.1113553986120547346, 0.3297244094488189226 ) ) ;
#17946=AXIS2_PLACEMENT_3D ( 'NONE', #43625, #18697, #29319 ) ;
#17948=CARTESIAN_POINT ( 'NONE',  ( -0.7646288533564489232, 0.1113553986120547346, 0.9596456691838111119 ) ) ;
#17949=CARTESIAN_POINT ( 'NONE',  ( 0.7495606340400177148, -0.1264236179284866091, 0.4847440944344252323 ) ) ;
#17953=CARTESIAN_POINT ( 'NONE',  ( 1.033464566929134687, -0.06523048226347956391, 1.887303149498773092 ) ) ;
#17954=ORIENTED_EDGE ( 'NONE', *, *, #42714, .T. ) ;
#17955=CARTESIAN_POINT ( 'NONE',  ( -0.5314960629921260393, 0.000000000000000000, 4.842519685039370358 ) ) ;
#17956=CARTESIAN_POINT ( 'NONE',  ( 0.8107537697050253289, -0.1574803149606297803, 0.7849409448818904789 ) ) ;
#17958=CARTESIAN_POINT ( 'NONE',  ( -0.9873396505805591694, -0.1113553986120547346, 1.609251968396409493 ) ) ;
#17960=CARTESIAN_POINT ( 'NONE',  ( -0.8759842519685039353, -0.1574803149606299191, 0.4724409448818898127 ) ) ;
#17961=CARTESIAN_POINT ( 'NONE',  ( 0.7185039370078746268, 0.06523048226347956391, 0.1353346455617644717 ) ) ;
#17964=EDGE_CURVE ( 'NONE', #3817, #42967, #27700, .T. ) ;
#17965=CARTESIAN_POINT ( 'NONE',  ( 0.8759842519685039353, 0.000000000000000000, 4.498031496062992574 ) ) ;
#17966=CARTESIAN_POINT ( 'NONE',  ( 1.033464566929133799, 0.000000000000000000, 1.850393700679873854 ) ) ;
#17969=CARTESIAN_POINT ( 'NONE',  ( -0.7646288533564489232, -0.1113553986120547346, 0.1427165353255439029 ) ) ;
#17971=CARTESIAN_POINT ( 'NONE',  ( 1.033464566929133799, 0.000000000000000000, 1.023622047136567126 ) ) ;
#17975=ORIENTED_EDGE ( 'NONE', *, *, #24552, .T. ) ;
#17976=CARTESIAN_POINT ( 'NONE',  ( -1.054774247047244096, 0.000000000000000000, 1.641240157426551161 ) ) ;
#17978=CARTESIAN_POINT ( 'NONE',  ( 1.054774247047244096, 0.000000000000000000, 1.562499999946236118 ) ) ;
#17979=ORIENTED_EDGE ( 'NONE', *, *, #23177, .T. ) ;
#17980=CARTESIAN_POINT ( 'NONE',  ( -0.7495606340400177148, -0.1264236179284866091, 0.8390748030958424808 ) ) ;
#17981=CARTESIAN_POINT ( 'NONE',  ( 0.9500414927467378812, 0.1787899950787401604, 0.2312992125446618197 ) ) ;
#17982=LINE ( 'NONE', #14405, #38863 ) ;
#17983=CARTESIAN_POINT ( 'NONE',  ( 0.7495606340400177148, 0.1264236179284866091, 0.7111220471903307860 ) ) ;
#17984=CARTESIAN_POINT ( 'NONE',  ( -0.9500414927467377701, -0.1787899950787401604, 0.6446850393163160442 ) ) ;
#17985=DIRECTION ( 'NONE',  ( 0.000000000000000000, 0.000000000000000000, -1.000000000000000000 ) ) ;
#17986=CARTESIAN_POINT ( 'NONE',  ( 0.9412147342319837628, 0.1574803149606300301, 1.070374015640503496 ) ) ;
#17988=CARTESIAN_POINT ( 'NONE',  ( -0.7646288533564489232, -0.1113553986120547346, 1.914370078632629868 ) ) ;
#17991=CARTESIAN_POINT ( 'NONE',  ( -0.7646288533564489232, -0.1113553986120547346, 0.4675196850393700809 ) ) ;
#17992=CARTESIAN_POINT ( 'NONE',  ( 1.002407869896990045, -0.1264236179284866091, 1.439468503883244210 ) ) ;
#17997=( BOUNDED_CURVE ( )  B_SPLINE_CURVE ( 2, ( #42578, #13840, #17907, #20787, #32558, #14330, #46423, #35432, #43055 ),
 .UNSPECIFIED., .F., .T. ) 
 B_SPLINE_CURVE_WITH_KNOTS ( ( 3, 2, 2, 2, 3 ),
 ( 0.9300000000000000488, 0.9324999999999999956, 0.9350000000000000533, 0.9375000000000000000, 0.9399999999999999467 ),
 .UNSPECIFIED. ) 
 CURVE ( )  GEOMETRIC_REPRESENTATION_ITEM ( )  RATIONAL_B_SPLINE_CURVE ( ( 1.000000000000000000, 0.9238795325112869605, 1.000000000000000000, 0.9238795325112869605, 1.000000000000000000, 0.9238795325112869605, 1.000000000000000000, 0.9238795325112829637, 1.000000000000000000 ) ) 
 REPRESENTATION_ITEM ( '' )  ) ;
#18004=CARTESIAN_POINT ( 'NONE',  ( 1.033464566929134687, 0.06523048226347956391, 1.035925196850394192 ) ) ;
#18005=CARTESIAN_POINT ( 'NONE',  ( 0.8019270111902717657, -0.1787899950787401604, 0.3641732282926931630 ) ) ;
#18012=CARTESIAN_POINT ( 'NONE',  ( 0.7495606340400177148, -0.1264236179284866091, 0.6373031495525354195 ) ) ;
#18013=( BOUNDED_CURVE ( )  B_SPLINE_CURVE ( 2, ( #40788, #770, #11832, #15429, #26692, #30079, #26457, #8449, #23080 ),
 .UNSPECIFIED., .F., .T. ) 
 B_SPLINE_CURVE_WITH_KNOTS ( ( 3, 2, 2, 2, 3 ),
 ( 0.8000000000000000444, 0.8024999999999999911, 0.8050000000000000488, 0.8074999999999999956, 0.8100000000000000533 ),
 .UNSPECIFIED. ) 
 CURVE ( )  GEOMETRIC_REPRESENTATION_ITEM ( )  RATIONAL_B_SPLINE_CURVE ( ( 1.000000000000000000, 0.9238795325112869605, 1.000000000000000000, 0.9238795325112869605, 1.000000000000000000, 0.9238795325112869605, 1.000000000000000000, 0.9238795325112869605, 1.000000000000000000 ) ) 
 REPRESENTATION_ITEM ( '' )  ) ;
#18014=CARTESIAN_POINT ( 'NONE',  ( -0.8019270111902716547, 0.1787899950787401604, 0.9842519684501743749 ) ) ;
#18016=CARTESIAN_POINT ( 'NONE',  ( -0.9538951735880809579, 0.1509809590367724719, 0.03937007874015843040 ) ) ;
#18019=AXIS2_PLACEMENT_3D ( 'NONE', #30195, #22716, #9051 ) ;
#18021=( BOUNDED_CURVE ( )  B_SPLINE_CURVE ( 2, ( #10703, #17631, #14043, #21454, #38958, #32275, #16926, #28690, #43259 ),
 .UNSPECIFIED., .F., .F. ) 
 B_SPLINE_CURVE_WITH_KNOTS ( ( 3, 2, 2, 2, 3 ),
 ( 0.6300000000000000044, 0.6324999999999999512, 0.6350000000000000089, 0.6374999999999999556, 0.6400000000000000133 ),
 .UNSPECIFIED. ) 
 CURVE ( )  GEOMETRIC_REPRESENTATION_ITEM ( )  RATIONAL_B_SPLINE_CURVE ( ( 1.000000000000000000, 0.9238795325112899581, 1.000000000000000000, 0.9238795325112869605, 1.000000000000000000, 0.9238795325112869605, 1.000000000000000000, 0.9238795325112869605, 1.000000000000000000 ) ) 
 REPRESENTATION_ITEM ( '' )  ) ;
#18024=CARTESIAN_POINT ( 'NONE',  ( 1.002407869896990045, 0.1264236179284866091, 1.724901574749385880 ) ) ;
#18025=CARTESIAN_POINT ( 'NONE',  ( 0.7185039370078739607, 1.928577636452523993E-17, 1.289370078740157632 ) ) ;
#18026=VECTOR ( 'NONE', #45936, 39.37007874015748143 ) ;
#18030=CARTESIAN_POINT ( 'NONE',  ( 1.033464566929134687, -0.06523048226347956391, 1.336122047136566904 ) ) ;
#18032=CARTESIAN_POINT ( 'NONE',  ( -0.7495606340400177148, -0.1264236179284866091, 0.4453740156942677664 ) ) ;
#18033=CARTESIAN_POINT ( 'NONE',  ( 0.9500414927467378812, 0.1787899950787401604, 0.5413385826234012876 ) ) ;
#18035=CARTESIAN_POINT ( 'NONE',  ( 0.8759842519685039353, 0.1787899950787401882, 0.07627952750529173875 ) ) ;
#18036=CARTESIAN_POINT ( 'NONE',  ( 1.033464566929134687, 0.06523048226347956391, 1.104822834538142340 ) ) ;
#18037=CARTESIAN_POINT ( 'NONE',  ( -0.6971942568897637749, 2.189545951927499583E-17, 1.656003936954110412 ) ) ;
#18038=ORIENTED_EDGE ( 'NONE', *, *, #21423, .F. ) ;
#18039=CARTESIAN_POINT ( 'NONE',  ( -0.8019270111902717657, -0.1787899950787401604, 1.195866141678520345 ) ) ;
#18041=CARTESIAN_POINT ( 'NONE',  ( 0.9500414927467378812, 0.1787899950787401604, 1.136811023568283119 ) ) ;
#18043=CARTESIAN_POINT ( 'NONE',  ( 1.002407869896990045, -0.1264236179284866091, 1.749507873961984483 ) ) ;
#18044=CARTESIAN_POINT ( 'NONE',  ( -0.8107537697050253289, -0.1574803149606297803, 0.5880905511811019837 ) ) ;
#18045=CARTESIAN_POINT ( 'NONE',  ( -0.6971942568897637749, 2.189545951927499583E-17, 0.9473425196312755814 ) ) ;
#18047=CARTESIAN_POINT ( 'NONE',  ( 0.8759842519685039353, 0.1787899950787401882, 0.3518700786863940833 ) ) ;
#18048=CARTESIAN_POINT ( 'NONE',  ( -1.054774247047244540, -0.07405724077823318263, 0.2952755904974176948 ) ) ;
#18049=CARTESIAN_POINT ( 'NONE',  ( -0.8019270111902717657, 0.1787899950787401604, 0.7824803149068669805 ) ) ;
#18050=CARTESIAN_POINT ( 'NONE',  ( 0.7185039370078746268, 0.06523048226347956391, 1.631397637687747926 ) ) ;
#18053=CARTESIAN_POINT ( 'NONE',  ( 1.054774247047244540, 0.07405724077823318263, 0.7775590550643479704 ) ) ;
#18054=CARTESIAN_POINT ( 'NONE',  ( 0.9500414927467377701, 0.1787899950787401604, 1.097440944828127041 ) ) ;
#18055=CARTESIAN_POINT ( 'NONE',  ( -0.7495606340400177148, 0.1264236179284866091, 1.808562992072220377 ) ) ;
#18057=CARTESIAN_POINT ( 'NONE',  ( 1.002407869896990045, -0.1264236179284866091, 1.906988188922614125 ) ) ;
#18059=CARTESIAN_POINT ( 'NONE',  ( 0.8107537697050254399, -0.1574803149606297803, 1.601870078632630756 ) ) ;
#18065=CARTESIAN_POINT ( 'NONE',  ( 1.054774247047244540, 0.07405724077823318263, 1.126968503883244654 ) ) ;
#18066=EDGE_CURVE ( 'NONE', #1531, #1638, #38036, .T. ) ;
#18069=CARTESIAN_POINT ( 'NONE',  ( 0.8107537697050253289, -0.1574803149606297803, 1.966043307086614567 ) ) ;
#18073=CARTESIAN_POINT ( 'NONE',  ( -1.054774247047244540, -0.07405724077823318263, 0.5364173227808820554 ) ) ;
#18077=CARTESIAN_POINT ( 'NONE',  ( 0.9500414927467378812, 0.1787899950787401604, 1.294291338528912982 ) ) ;
#18078=CARTESIAN_POINT ( 'NONE',  ( 1.054774247047244540, 0.07405724077823318263, 1.638779527505292766 ) ) ;
#18080=CARTESIAN_POINT ( 'NONE',  ( -1.033464566929134687, 0.06523048226347956391, 1.902066929133858553 ) ) ;
#18082=DIRECTION ( 'NONE',  ( 1.000000000000000000, 0.000000000000000000, -1.822029033848725275E-16 ) ) ;
#18085=CARTESIAN_POINT ( 'NONE',  ( -0.7185039370078746268, 0.06523048226347956391, 1.749507873908222155 ) ) ;
#18086=CARTESIAN_POINT ( 'NONE',  ( 0.6971942568897626646, 0.07405724077823318263, 0.1574803149068664809 ) ) ;
#18087=CARTESIAN_POINT ( 'NONE',  ( 0.7023349083174097451, 0.03108062574093124059, 0.03937019779350070525 ) ) ;
#18088=CARTESIAN_POINT ( 'NONE',  ( 0.7495606340400177148, 0.1264236179284866091, 1.178641732229700922 ) ) ;
#18089=DIRECTION ( 'NONE',  ( 1.000000000000000000, 0.000000000000000000, -1.822029033848725275E-16 ) ) ;
#18090=CARTESIAN_POINT ( 'NONE',  ( 0.9412147342319837628, -0.1574803149606297803, 1.222933070866141669 ) ) ;
#18091=CARTESIAN_POINT ( 'NONE',  ( -1.054774247047244540, -0.07405724077823318263, 1.161417322780881278 ) ) ;
#18092=CARTESIAN_POINT ( 'NONE',  ( 0.9412147342319837628, 0.1574803149606300301, 0.5191929132782994172 ) ) ;
#18093=ORIENTED_EDGE ( 'NONE', *, *, #24893, .T. ) ;
#18095=CARTESIAN_POINT ( 'NONE',  ( 0.8663930385888580776, 0.1748445346236966735, 0.03937198857582425993 ) ) ;
#18096=CARTESIAN_POINT ( 'NONE',  ( 1.033464566929134687, -0.06523048226347956391, 0.2829724409448821643 ) ) ;
#18098=CARTESIAN_POINT ( 'NONE',  ( -0.9873396505805591694, 0.1113553986120547346, 0.3986220471365669038 ) ) ;
#18100=CARTESIAN_POINT ( 'NONE',  ( 0.9500414927467378812, -0.1787899950787401604, 1.510826771599780294 ) ) ;
#18101=CARTESIAN_POINT ( 'NONE',  ( -1.033464566929134687, -0.06523048226347956391, 1.099901574695623108 ) ) ;
#18103=CARTESIAN_POINT ( 'NONE',  ( 0.8759842519685039353, 0.1574803149606299191, 1.909448818897637956 ) ) ;
#18104=CARTESIAN_POINT ( 'NONE',  ( -0.7495606340400177148, -0.1264236179284866091, 0.04675196845017354913 ) ) ;
#18108=ORIENTED_EDGE ( 'NONE', *, *, #777, .T. ) ;
#18110=CYLINDRICAL_SURFACE ( 'NONE', #46004, 0.1574803149606299191 ) ;
#18112=CARTESIAN_POINT ( 'NONE',  ( 1.054774247047244096, 0.000000000000000000, 0.6176181101824566033 ) ) ;
#18115=CARTESIAN_POINT ( 'NONE',  ( -0.6971942568897648851, 0.07405724077823318263, 1.067913385773007651 ) ) ;
#18116=VERTEX_POINT ( 'NONE', #4746 ) ;
#18117=CARTESIAN_POINT ( 'NONE',  ( -0.6971942568897637749, 2.189545951927499583E-17, 1.065452755851747924 ) ) ;
#18118=CARTESIAN_POINT ( 'NONE',  ( -1.054774247047244540, -0.07405724077823318263, 0.8513779527021426707 ) ) ;
#18119=CARTESIAN_POINT ( 'NONE',  ( 1.033464566929134687, -0.06523048226347956391, 1.818405511811023167 ) ) ;
#18121=VERTEX_POINT ( 'NONE', #30667 ) ;
#18123=CARTESIAN_POINT ( 'NONE',  ( 0.7439266621721258854, 0.1207772627896461087, 0.03937008034557057390 ) ) ;
#18124=ORIENTED_EDGE ( 'NONE', *, *, #45815, .F. ) ;
#18125=CARTESIAN_POINT ( 'NONE',  ( -0.8759842519685039353, -0.1574803149606299191, 1.732283464566929165 ) ) ;
#18128=CARTESIAN_POINT ( 'NONE',  ( -0.8759842519685039353, 0.1787899950787401882, 0.7406496062454487328 ) ) ;
#18129=ADVANCED_FACE ( 'NONE', ( #44283 ), #26595, .T. ) ;
#18131=CARTESIAN_POINT ( 'NONE',  ( -1.054774247047244096, 0.000000000000000000, 1.838090551127338657 ) ) ;
#18133=( BOUNDED_CURVE ( )  B_SPLINE_CURVE ( 2, ( #25929, #7699, #22313, #40277, #18718, #15151, #37172, #969, #23034 ),
 .UNSPECIFIED., .F., .F. ) 
 B_SPLINE_CURVE_WITH_KNOTS ( ( 3, 2, 2, 2, 3 ),
 ( 0.5500000000000000444, 0.5524999999999999911, 0.5550000000000000488, 0.5574999999999999956, 0.5600000000000000533 ),
 .UNSPECIFIED. ) 
 CURVE ( )  GEOMETRIC_REPRESENTATION_ITEM ( )  RATIONAL_B_SPLINE_CURVE ( ( 1.000000000000000000, 0.9238795325112869605, 1.000000000000000000, 0.9238795325112869605, 1.000000000000000000, 0.9238795325112869605, 1.000000000000000000, 0.9238795325112869605, 1.000000000000000000 ) ) 
 REPRESENTATION_ITEM ( '' )  ) ;
#18135=CARTESIAN_POINT ( 'NONE',  ( 0.7185039370078746268, -0.06523048226347956391, 0.7012795275590552047 ) ) ;
#18137=CARTESIAN_POINT ( 'NONE',  ( -0.7382059478614877435, 0.08697056858538719515, 1.981492242426230899 ) ) ;
#18139=CARTESIAN_POINT ( 'NONE',  ( -0.8759842519685039353, 0.1574803149606299191, 1.348425196742866206 ) ) ;
#18140=CARTESIAN_POINT ( 'NONE',  ( 0.9500414927467378812, -0.1787899950787401604, 0.8070866141194653620 ) ) ;
#18141=CARTESIAN_POINT ( 'NONE',  ( 1.054774247047244540, 0.07405724077823318263, 1.363188976324188673 ) ) ;
#18145=CARTESIAN_POINT ( 'NONE',  ( 0.8759842519685039353, 0.1574803149606299191, 1.240157480314960647 ) ) ;
#18146=CARTESIAN_POINT ( 'NONE',  ( 0.9972096056529755614, -0.1313310934784522044, 1.990530892258217222 ) ) ;
#18147=CARTESIAN_POINT ( 'NONE',  ( 0.8759842519685039353, -0.1574803149606299191, 1.564960629813732185 ) ) ;
#18148=CARTESIAN_POINT ( 'NONE',  ( 0.8107537697050254399, -0.1574803149606297803, 1.719980314853102321 ) ) ;
#18151=AXIS2_PLACEMENT_3D ( 'NONE', #42814, #21271, #35896 ) ;
#18152=CARTESIAN_POINT ( 'NONE',  ( 0.7495606340400177148, 0.1264236179284866091, 0.6668307086076534773 ) ) ;
#18156=VERTEX_POINT ( 'NONE', #41147 ) ;
#18157=CARTESIAN_POINT ( 'NONE',  ( 0.8107537697050254399, -0.1574803149606297803, 0.6176181101286931652 ) ) ;
#18158=LINE ( 'NONE', #33276, #39710 ) ;
#18159=CARTESIAN_POINT ( 'NONE',  ( 1.054774247047244096, 0.000000000000000000, 1.006397637741511808 ) ) ;
#18164=CARTESIAN_POINT ( 'NONE',  ( -0.9500414927467378812, -0.1787899950787401604, 0.09350393695411057804 ) ) ;
#18165=EDGE_LOOP ( 'NONE', ( #18038, #43370, #37348, #38385 ) ) ;
#18166=CARTESIAN_POINT ( 'NONE',  ( 0.7185039370078746268, 0.06523048226347956391, 1.759350393700788162 ) ) ;
#18171=CARTESIAN_POINT ( 'NONE',  ( -1.002407869896990045, 0.1264236179284866091, 1.641240157426551161 ) ) ;
#18172=CARTESIAN_POINT ( 'NONE',  ( -1.002407869896990045, -0.1264236179284866091, 1.119586614119464585 ) ) ;
#18173=CARTESIAN_POINT ( 'NONE',  ( -0.8019270111902717657, 0.1787899950787401604, 0.4330708660879683536 ) ) ;
#18174=CARTESIAN_POINT ( 'NONE',  ( -0.7185039370078766252, -0.06523048226348168721, 1.793799212490897688 ) ) ;
#18183=CARTESIAN_POINT ( 'NONE',  ( -1.002407869896990045, -0.1264236179284866091, 0.3321850393163153226 ) ) ;
#18188=CARTESIAN_POINT ( 'NONE',  ( -0.8759842519685039353, -0.1787899950787401882, 1.434547244040724534 ) ) ;
#18195=CARTESIAN_POINT ( 'NONE',  ( 0.9873396505805591694, -0.1113553986120547346, 0.3986220472440945017 ) ) ;
#18198=CARTESIAN_POINT ( 'NONE',  ( -0.9873396505805591694, -0.1113553986120547346, 0.9005905510735748853 ) ) ;
#18199=CARTESIAN_POINT ( 'NONE',  ( 0.6971942568897626646, 0.07405724077823318263, 0.4773622046706456068 ) ) ;
#18201=CARTESIAN_POINT ( 'NONE',  ( 0.9412147342319837628, -0.1574803149606297803, 1.803641732175937484 ) ) ;
#18202=VERTEX_POINT ( 'NONE', #912 ) ;
#18204=CARTESIAN_POINT ( 'NONE',  ( 0.8759842519685039353, -0.1574803149606299191, 0.8267716535433071723 ) ) ;
#18208=CARTESIAN_POINT ( 'NONE',  ( 0.9873396505805591694, -0.1113553986120547346, 0.7923228346456693272 ) ) ;
#18209=ORIENTED_EDGE ( 'NONE', *, *, #10423, .T. ) ;
#18210=ORIENTED_EDGE ( 'NONE', *, *, #33520, .T. ) ;
#18211=DIRECTION ( 'NONE',  ( -1.000000000000000000, 0.000000000000000000, 0.000000000000000000 ) ) ;
#18215=CARTESIAN_POINT ( 'NONE',  ( -0.8759842519685039353, 0.1574803149606299191, 0.1673228345381423399 ) ) ;
#18218=CARTESIAN_POINT ( 'NONE',  ( 0.8107537697050253289, -0.1574803149606297803, 1.011318897530268712 ) ) ;
#18219=CARTESIAN_POINT ( 'NONE',  ( -0.8019270111902717657, -0.1787899950787401604, 0.3641732282926931630 ) ) ;
#18222=EDGE_LOOP ( 'NONE', ( #33127, #14097, #31290, #38921 ) ) ;
#18223=CARTESIAN_POINT ( 'NONE',  ( -1.002407869896990045, 0.1264236179284866091, 1.646161417269070837 ) ) ;
#18225=CARTESIAN_POINT ( 'NONE',  ( 0.9500414927467378812, -0.1787899950787401604, 1.594488188922613237 ) ) ;
#18226=ORIENTED_EDGE ( 'NONE', *, *, #11343, .T. ) ;
#18227=CARTESIAN_POINT ( 'NONE',  ( -0.8019270111902717657, 0.1787899950787401604, 0.8267716534895444003 ) ) ;
#18228=CARTESIAN_POINT ( 'NONE',  ( -1.002407869896990045, -0.1264236179284866091, 0.7258858267178898149 ) ) ;
#18231=CARTESIAN_POINT ( 'NONE',  ( -1.002407869896990045, 0.1264236179284866091, 1.528051181048598384 ) ) ;
#18232=CARTESIAN_POINT ( 'NONE',  ( -0.9412147342319837628, -0.1574803149606297803, 1.961122047136568014 ) ) ;
#18234=CARTESIAN_POINT ( 'NONE',  ( 1.033464566929133799, 0.000000000000000000, 0.9842519683964094934 ) ) ;
#18235=CARTESIAN_POINT ( 'NONE',  ( 0.6971942568897637749, 2.189545951927499583E-17, 1.503444881836000002 ) ) ;
#18241=VERTEX_POINT ( 'NONE', #2564 ) ;
#18242=VERTEX_POINT ( 'NONE', #9784 ) ;
#18250=CARTESIAN_POINT ( 'NONE',  ( 0.8019270111902717657, 0.1787899950787401604, 1.766732283410803461 ) ) ;
#18251=CARTESIAN_POINT ( 'NONE',  ( 0.7185039370078746268, 0.06523048226347956391, 0.3026574803149607029 ) ) ;
#18257=CARTESIAN_POINT ( 'NONE',  ( 1.002407869896990045, -0.1264236179284866091, 0.6077755904974173617 ) ) ;
#18258=CARTESIAN_POINT ( 'NONE',  ( -0.8206535098617165902, 0.1696709502983688167, 0.03937007874015842346 ) ) ;
#18260=CARTESIAN_POINT ( 'NONE',  ( -0.9412147342319837628, 0.1574803149606300301, 1.306594488081449290 ) ) ;
#18261=CARTESIAN_POINT ( 'NONE',  ( 0.6971942568897648851, -0.07405724077823297447, 1.742125984198204858 ) ) ;
#18263=CARTESIAN_POINT ( 'NONE',  ( 0.9873396505805591694, 0.1113553986120547346, 0.1230314959554651699 ) ) ;
#18264=CARTESIAN_POINT ( 'NONE',  ( 0.8759842519685039353, -0.1787899950787401882, 0.4847440944344252323 ) ) ;
#18265=ORIENTED_EDGE ( 'NONE', *, *, #47268, .T. ) ;
#18269=CARTESIAN_POINT ( 'NONE',  ( -0.6971942568897637749, 2.189545951927499583E-17, 0.4010826771115905687 ) ) ;
#18271=EDGE_CURVE ( 'NONE', #18481, #3331, #29825, .T. ) ;
#18273=CARTESIAN_POINT ( 'NONE',  ( 0.8759842519685039353, -0.1787899950787401882, 0.09596456687537047170 ) ) ;
#18275=VECTOR ( 'NONE', #39631, 39.37007874015748143 ) ;
#18276=CARTESIAN_POINT ( 'NONE',  ( -0.7495606340400177148, 0.1264236179284866091, 1.651082677111590513 ) ) ;
#18278=CARTESIAN_POINT ( 'NONE',  ( -0.6971942568897648851, -0.07405724077823297447, 1.112204724355684959 ) ) ;
#18279=CARTESIAN_POINT ( 'NONE',  ( 1.033464566929133799, 0.000000000000000000, 1.033464566929133799 ) ) ;
#18281=CARTESIAN_POINT ( 'NONE',  ( 0.6971942568897637749, 2.189545951927499583E-17, 1.149114173174582643 ) ) ;
#18282=CARTESIAN_POINT ( 'NONE',  ( 1.002407869896990045, -0.1264236179284866091, 1.867618110182456714 ) ) ;
#18283=CARTESIAN_POINT ( 'NONE',  ( -1.033464566929134687, -0.06523048226347956391, 0.6373031496062994128 ) ) ;
#18284=CARTESIAN_POINT ( 'NONE',  ( -0.9500414927467378812, -0.1787899950787401604, 1.117125984198206412 ) ) ;
#18287=CARTESIAN_POINT ( 'NONE',  ( 0.6971942568897637749, 2.189545951927499583E-17, 0.2829724408911185041 ) ) ;
#18288=CARTESIAN_POINT ( 'NONE',  ( -0.8759842519685039353, 0.1787899950787401882, 0.3075787401037169411 ) ) ;
#18290=CARTESIAN_POINT ( 'NONE',  ( -1.054774247047244096, 0.000000000000000000, 0.7308070865604093802 ) ) ;
#18294=CARTESIAN_POINT ( 'NONE',  ( 0.6971942568897626646, -0.07405724077823297447, 0.7185039369541108556 ) ) ;
#18295=CARTESIAN_POINT ( 'NONE',  ( 0.8019270111902716547, -0.1787899950787401604, 1.038385826717890259 ) ) ;
#18296=CARTESIAN_POINT ( 'NONE',  ( -0.7495606340400177148, 0.1264236179284866091, 1.926673228292693052 ) ) ;
#18297=CARTESIAN_POINT ( 'NONE',  ( 1.002407869896990045, 0.1264236179284866091, 1.956200787347811110 ) ) ;
#18305=ORIENTED_EDGE ( 'NONE', *, *, #40646, .F. ) ;
#18306=CARTESIAN_POINT ( 'NONE',  ( 1.054774247047244096, 0.000000000000000000, 1.163877952702141672 ) ) ;
#18310=( BOUNDED_CURVE ( )  B_SPLINE_CURVE ( 2, ( #37641, #35006, #4795, #42154, #19422, #15858, #23984, #30481, #45040 ),
 .UNSPECIFIED., .F., .F. ) 
 B_SPLINE_CURVE_WITH_KNOTS ( ( 3, 2, 2, 2, 3 ),
 ( 0.6400000000000000133, 0.6424999999999999600, 0.6450000000000000178, 0.6474999999999999645, 0.6500000000000000222 ),
 .UNSPECIFIED. ) 
 CURVE ( )  GEOMETRIC_REPRESENTATION_ITEM ( )  RATIONAL_B_SPLINE_CURVE ( ( 1.000000000000000000, 0.9238795325112869605, 1.000000000000000000, 0.9238795325112869605, 1.000000000000000000, 0.9238795325112869605, 1.000000000000000000, 0.9238795325112869605, 1.000000000000000000 ) ) 
 REPRESENTATION_ITEM ( '' )  ) ;
#18311=CARTESIAN_POINT ( 'NONE',  ( 1.002407869896990045, 0.1264236179284866091, 1.523129921206078707 ) ) ;
#18312=CARTESIAN_POINT ( 'NONE',  ( 1.054774247047244540, 0.07405724077823318263, 0.02460629915883492599 ) ) ;
#18316=CARTESIAN_POINT ( 'NONE',  ( -0.6971942568897637749, 2.189545951927499583E-17, 0.5585629920722204877 ) ) ;
#18319=CARTESIAN_POINT ( 'NONE',  ( -0.7098384388722608351, -0.01069464109018706914, 1.983455518814613017 ) ) ;
#18321=CARTESIAN_POINT ( 'NONE',  ( 0.8759842519685039353, 0.1787899950787401882, 1.218011810969858111 ) ) ;
#18322=VECTOR ( 'NONE', #27027, 39.37007874015748143 ) ;
#18323=CARTESIAN_POINT ( 'NONE',  ( 0.8019270111902716547, -0.1787899950787401604, 1.742125984198204858 ) ) ;
#18324=CARTESIAN_POINT ( 'NONE',  ( 0.8107537697050254399, 0.1574803149606300301, 1.508366141624757129 ) ) ;
#18327=DIRECTION ( 'NONE',  ( 1.822029033848725028E-16, 0.000000000000000000, 1.000000000000000000 ) ) ;
#18328=CARTESIAN_POINT ( 'NONE',  ( -0.9873396505805591694, -0.1113553986120547346, 1.934055118110236338 ) ) ;
#18330=CARTESIAN_POINT ( 'NONE',  ( 1.054774247047244540, 0.07405724077823318263, 0.1427165353793072855 ) ) ;
#18334=CARTESIAN_POINT ( 'NONE',  ( -0.9500414927467378812, 0.1787899950787401604, 1.171259842465921741 ) ) ;
#18335=CARTESIAN_POINT ( 'NONE',  ( 0.8759842519685039353, 0.1574803149606299191, 0.7185039369003465293 ) ) ;
#18336=ORIENTED_EDGE ( 'NONE', *, *, #4698, .F. ) ;
#18337=CARTESIAN_POINT ( 'NONE',  ( -0.7185039370078714072, 0.06523048226347728795, 1.129429133858268708 ) ) ;
#18338=CARTESIAN_POINT ( 'NONE',  ( -0.8107537697050253289, 0.1574803149606300301, 0.4060039369003469734 ) ) ;
#18340=CARTESIAN_POINT ( 'NONE',  ( 1.054774247047244096, 0.000000000000000000, 1.478838582623401399 ) ) ;
#18341=DIRECTION ( 'NONE',  ( 1.822029033848725028E-16, 0.000000000000000000, 1.000000000000000000 ) ) ;
#18344=ORIENTED_EDGE ( 'NONE', *, *, #2264, .F. ) ;
#18345=DIRECTION ( 'NONE',  ( -1.000000000000000000, 0.000000000000000000, 0.000000000000000000 ) ) ;
#18346=AXIS2_PLACEMENT_3D ( 'NONE', #37405, #22563, #44823 ) ;
#18347=CARTESIAN_POINT ( 'NONE',  ( 1.002407869896990045, 0.1264236179284866091, 0.6619094487651338010 ) ) ;
#18349=VERTEX_POINT ( 'NONE', #38537 ) ;
#18351=CARTESIAN_POINT ( 'NONE',  ( -0.8019270111902717657, 0.1787899950787401604, 1.102362204670646495 ) ) ;
#18353=CARTESIAN_POINT ( 'NONE',  ( 0.7185039370078714072, 0.06523048226347728795, 1.316437007766489531 ) ) ;
#18355=CARTESIAN_POINT ( 'NONE',  ( -0.8019270111902717657, 0.1787899950787401604, 0.7874015747493863238 ) ) ;
#18357=CARTESIAN_POINT ( 'NONE',  ( -0.9500414927467378812, 0.1787899950787401604, 0.2706692912848194243 ) ) ;
#18363=CARTESIAN_POINT ( 'NONE',  ( -1.033464566929134687, -0.06523048226347956391, 0.8636811022546768690 ) ) ;
#18364=ORIENTED_EDGE ( 'NONE', *, *, #40725, .F. ) ;
#18366=CARTESIAN_POINT ( 'NONE',  ( -0.6971942568897637749, 2.189545951927499583E-17, 0.7898622046706456068 ) ) ;
#18370=CARTESIAN_POINT ( 'NONE',  ( -0.7495606340400177148, -0.1264236179284866091, 1.862696850339937038 ) ) ;
#18373=CARTESIAN_POINT ( 'NONE',  ( 1.033464566929134687, -0.06523048226347956391, 0.6766732283464570452 ) ) ;
#18376=CARTESIAN_POINT ( 'NONE',  ( -0.7646288533564489232, 0.1113553986120547346, 1.510826771546015523 ) ) ;
#18377=CARTESIAN_POINT ( 'NONE',  ( 0.9500414927467378812, 0.1787899950787401604, 0.8218503936470251681 ) ) ;
#18378=CARTESIAN_POINT ( 'NONE',  ( 0.8759842519685039353, 0.1574803149606299191, 0.1673228345381423399 ) ) ;
#18379=CARTESIAN_POINT ( 'NONE',  ( 0.7185039370078739607, 1.928577636452523993E-17, 1.486220472440944906 ) ) ;
#18380=CARTESIAN_POINT ( 'NONE',  ( 0.9431103146933020875, -0.1634063081578735477, 1.989410936682964870 ) ) ;
#18383=CARTESIAN_POINT ( 'NONE',  ( 0.7646288533564489232, -0.1113553986120547346, 1.717519684931842594 ) ) ;
#18386=CARTESIAN_POINT ( 'NONE',  ( 0.8019270111902716547, -0.1787899950787401604, 0.7578740156942688211 ) ) ;
#18388=CARTESIAN_POINT ( 'NONE',  ( -0.7185039370078739607, 1.928577636452523993E-17, 0.3740157479239689664 ) ) ;
#18391=CARTESIAN_POINT ( 'NONE',  ( 0.7185039370078739607, 0.000000000000000000, 4.498031496062992574 ) ) ;
#18392=CARTESIAN_POINT ( 'NONE',  ( 1.054774247047244096, 0.000000000000000000, 0.9276574802611967652 ) ) ;
#18394=DIRECTION ( 'NONE',  ( -1.000000000000000000, 0.000000000000000000, 0.000000000000000000 ) ) ;
#18398=CARTESIAN_POINT ( 'NONE',  ( -0.8759842519685039353, -0.1787899950787401882, 0.09104330703285078152 ) ) ;
#18399=EDGE_CURVE ( 'NONE', #31524, #8209, #27072, .T. ) ;
#18401=CARTESIAN_POINT ( 'NONE',  ( -1.054774247047244540, 0.07405724077823318263, 1.678149606245448622 ) ) ;
#18403=CARTESIAN_POINT ( 'NONE',  ( -0.6971942568897626646, -0.07405724077823297447, 0.4429133857730075952 ) ) ;
#18405=CARTESIAN_POINT ( 'NONE',  ( -1.054774247047244096, 0.000000000000000000, 1.995570866087968520 ) ) ;
#18406=CARTESIAN_POINT ( 'NONE',  ( 0.7185039370078746268, 0.06523048226347956391, 0.3026574803149607029 ) ) ;
#18407=CARTESIAN_POINT ( 'NONE',  ( 0.7495606340400177148, -0.1264236179284866091, 0.04675196845017354913 ) ) ;
#18413=AXIS2_PLACEMENT_3D ( 'NONE', #13284, #27915, #27687 ) ;
#18414=CARTESIAN_POINT ( 'NONE',  ( -0.9500414927467378812, -0.1787899950787401604, 0.3690944881352128393 ) ) ;
#18415=( BOUNDED_CURVE ( )  B_SPLINE_CURVE ( 2, ( #24037, #27422, #41731, #38163, #5324, #41965, #19944, #16378, #9653 ),
 .UNSPECIFIED., .F., .F. ) 
 B_SPLINE_CURVE_WITH_KNOTS ( ( 3, 2, 2, 2, 3 ),
 ( 0.9399999999999999467, 0.9425000000000000044, 0.9449999999999999512, 0.9475000000000000089, 0.9499999999999999556 ),
 .UNSPECIFIED. ) 
 CURVE ( )  GEOMETRIC_REPRESENTATION_ITEM ( )  RATIONAL_B_SPLINE_CURVE ( ( 1.000000000000000000, 0.9238795325112899581, 1.000000000000000000, 0.9238795325112869605, 1.000000000000000000, 0.9238795325112869605, 1.000000000000000000, 0.9238795325112829637, 1.000000000000000000 ) ) 
 REPRESENTATION_ITEM ( '' )  ) ;
#18417=CARTESIAN_POINT ( 'NONE',  ( -0.8759842519685039353, -0.1787899950787401882, 1.316437007820252081 ) ) ;
#18420=CARTESIAN_POINT ( 'NONE',  ( 0.7646288533564489232, -0.1113553986120547346, 0.3887795275590551491 ) ) ;
#18423=CARTESIAN_POINT ( 'NONE',  ( -0.9412147342319837628, -0.1574803149606297803, 1.094980314853103653 ) ) ;
#18425=CARTESIAN_POINT ( 'NONE',  ( 0.9873396505805591694, 0.1113553986120547346, 1.934055118002708573 ) ) ;
#18427=CARTESIAN_POINT ( 'NONE',  ( 0.7646288533564489232, -0.1113553986120547346, 0.9793307086614173596 ) ) ;
#18431=( BOUNDED_CURVE ( )  B_SPLINE_CURVE ( 2, ( #4116, #8182, #21882, #985, #40295, #285, #32921, #18737, #33395 ),
 .UNSPECIFIED., .F., .F. ) 
 B_SPLINE_CURVE_WITH_KNOTS ( ( 3, 2, 2, 2, 3 ),
 ( 0.1600000000000000033, 0.1625000000000000056, 0.1650000000000000078, 0.1675000000000000100, 0.1700000000000000122 ),
 .UNSPECIFIED. ) 
 CURVE ( )  GEOMETRIC_REPRESENTATION_ITEM ( )  RATIONAL_B_SPLINE_CURVE ( ( 1.000000000000000000, 0.9238795325112869605, 1.000000000000000000, 0.9238795325112869605, 1.000000000000000000, 0.9238795325112869605, 1.000000000000000000, 0.9238795325112869605, 1.000000000000000000 ) ) 
 REPRESENTATION_ITEM ( '' )  ) ;
#18433=CARTESIAN_POINT ( 'NONE',  ( 1.033464566929134687, -0.06523048226347956391, 1.542814960629921073 ) ) ;
#18435=AXIS2_PLACEMENT_3D ( 'NONE', #16701, #34441, #42542 ) ;
#18439=CYLINDRICAL_SURFACE ( 'NONE', #46294, 0.1574803149606299191 ) ;
#18444=CARTESIAN_POINT ( 'NONE',  ( -0.9412147342319837628, 0.1574803149606300301, 0.08612204713656734789 ) ) ;
#18447=CARTESIAN_POINT ( 'NONE',  ( 0.9873396505805591694, 0.1113553986120547346, 0.9104330707586141269 ) ) ;
#18449=CARTESIAN_POINT ( 'NONE',  ( -0.8019270111902717657, 0.1787899950787401604, 0.3494094487651343006 ) ) ;
#18453=CARTESIAN_POINT ( 'NONE',  ( -0.8759842519685039353, 0.1787899950787401882, 1.611712598371433103 ) ) ;
#18455=CARTESIAN_POINT ( 'NONE',  ( 1.054774247047244540, 0.07405724077823318263, 1.683070866087970074 ) ) ;
#18457=CARTESIAN_POINT ( 'NONE',  ( -0.7495606340400177148, 0.1264236179284866091, 0.8686023621509606496 ) ) ;
#18458=CARTESIAN_POINT ( 'NONE',  ( 0.9500414927467378812, -0.1787899950787401604, 0.3346456692375748831 ) ) ;
#18460=CARTESIAN_POINT ( 'NONE',  ( -0.7495606340400177148, -0.1264236179284866091, 1.306594488135212728 ) ) ;
#18461=CARTESIAN_POINT ( 'NONE',  ( -1.002407869896990045, 0.1264236179284866091, 0.7357283464029290565 ) ) ;
#18464=CARTESIAN_POINT ( 'NONE',  ( -0.7495606340400177148, 0.1264236179284866091, 1.656003936954110412 ) ) ;
#18465=CARTESIAN_POINT ( 'NONE',  ( -0.7185039370078746268, -0.06523048226347956391, 1.911909448711371917 ) ) ;
#18467=CARTESIAN_POINT ( 'NONE',  ( -0.7185039370078746268, 0.06523048226347956391, 1.601870078740158077 ) ) ;
#18469=CARTESIAN_POINT ( 'NONE',  ( 1.054774247047244096, 0.000000000000000000, 1.405019684985606476 ) ) ;
#18471=ORIENTED_EDGE ( 'NONE', *, *, #30605, .T. ) ;
#18473=ORIENTED_EDGE ( 'NONE', *, *, #9702, .F. ) ;
#18474=ORIENTED_EDGE ( 'NONE', *, *, #24304, .F. ) ;
#18476=VECTOR ( 'NONE', #44092, 39.37007874015748143 ) ;
#18481=VERTEX_POINT ( 'NONE', #36376 ) ;
#18483=CARTESIAN_POINT ( 'NONE',  ( 1.002407869896990045, 0.1264236179284866091, 1.798720472387181024 ) ) ;
#18487=CARTESIAN_POINT ( 'NONE',  ( 1.002407869896990045, 0.1264236179284866091, 0.7750984251430865779 ) ) ;
#18488=CYLINDRICAL_SURFACE ( 'NONE', #6269, 0.1574803149606299191 ) ;
#18491=CARTESIAN_POINT ( 'NONE',  ( 1.033464566929133799, 0.000000000000000000, 0.9448818896562519720 ) ) ;
#18492=CARTESIAN_POINT ( 'NONE',  ( 0.7495606340400177148, 0.1264236179284866091, 1.892224409395055096 ) ) ;
#18495=CARTESIAN_POINT ( 'NONE',  ( 0.6971942568897637749, 2.189545951927499583E-17, 0.4749015747493858242 ) ) ;
#18499=CARTESIAN_POINT ( 'NONE',  ( -1.054774247047244540, -0.07405724077823318263, 0.4183070865604097133 ) ) ;
#18502=CARTESIAN_POINT ( 'NONE',  ( 1.002407869896990045, -0.1264236179284866091, 0.2189960629383626012 ) ) ;
#18503=EDGE_CURVE ( 'NONE', #24526, #24301, #10186, .T. ) ;
#18504=CARTESIAN_POINT ( 'NONE',  ( 0.9412147342319837628, 0.1574803149606300301, 0.05659448818897643008 ) ) ;
#18506=CARTESIAN_POINT ( 'NONE',  ( -1.054774247047244096, 0.000000000000000000, 1.596948818843874074 ) ) ;
#18508=CARTESIAN_POINT ( 'NONE',  ( -1.054774247047244540, -0.07405724077823318263, 1.126968503883244654 ) ) ;
#18509=CARTESIAN_POINT ( 'NONE',  ( 1.002407869896990045, -0.1264236179284866091, 1.242618110182456714 ) ) ;
#18513=CARTESIAN_POINT ( 'NONE',  ( 0.6971942568897637749, 2.189545951927499583E-17, 1.931594488135212728 ) ) ;
#18514=CARTESIAN_POINT ( 'NONE',  ( -0.8107537697050253289, 0.1574803149606300301, 0.6520669291338586637 ) ) ;
#18515=CARTESIAN_POINT ( 'NONE',  ( -0.9500414927467378812, 0.1787899950787401604, 1.092519684985605810 ) ) ;
#18519=CARTESIAN_POINT ( 'NONE',  ( 0.9500414927467377701, -0.1787899950787401604, 0.3346456692375752162 ) ) ;
#18520=CARTESIAN_POINT ( 'NONE',  ( -1.002407869896990045, 0.1264236179284866091, 0.1845472440407248116 ) ) ;
#18521=CARTESIAN_POINT ( 'NONE',  ( -1.054774247047244096, 0.000000000000000000, 0.8095472440407244230 ) ) ;
#18524=CARTESIAN_POINT ( 'NONE',  ( 1.002407869896990045, -0.1264236179284866091, 1.124507873961984261 ) ) ;
#18525=CARTESIAN_POINT ( 'NONE',  ( -1.002407869896990045, 0.1264236179284866091, 1.798720472387181024 ) ) ;
#18526=ORIENTED_EDGE ( 'NONE', *, *, #12185, .F. ) ;
#18527=CARTESIAN_POINT ( 'NONE',  ( 0.8019270111902717657, -0.1787899950787401604, 1.860236220418677089 ) ) ;
#18533=ORIENTED_EDGE ( 'NONE', *, *, #41559, .F. ) ;
#18534=CARTESIAN_POINT ( 'NONE',  ( 0.6971942568897648851, 0.07405724077823318263, 1.220472440891118504 ) ) ;
#18537=EDGE_CURVE ( 'NONE', #10815, #34169, #35661, .T. ) ;
#18538=DIRECTION ( 'NONE',  ( 1.822029033848725028E-16, 0.000000000000000000, 1.000000000000000000 ) ) ;
#18539=CARTESIAN_POINT ( 'NONE',  ( 1.054774247047244540, 0.07405724077823318263, 1.481299212544662680 ) ) ;
#18540=CARTESIAN_POINT ( 'NONE',  ( 0.8759842519685039353, -0.1787899950787401882, 0.1304133857730082613 ) ) ;
#18544=CARTESIAN_POINT ( 'NONE',  ( -0.7495606340400177148, -0.1264236179284866091, 0.4453740156942677664 ) ) ;
#18547=CARTESIAN_POINT ( 'NONE',  ( 1.002407869896990045, -0.1264236179284866091, 1.360728346402929168 ) ) ;
#18548=CARTESIAN_POINT ( 'NONE',  ( 0.8019270111902716547, 0.1787899950787401604, 1.687992125930489307 ) ) ;
#18552=FACE_OUTER_BOUND ( 'NONE', #21727, .T. ) ;
#18553=CARTESIAN_POINT ( 'NONE',  ( -0.9873396505805591694, -0.1113553986120547346, 1.028543307086614123 ) ) ;
#18554=CARTESIAN_POINT ( 'NONE',  ( 0.8107537697050254399, 0.1574803149606300301, 0.7603346455617647770 ) ) ;
#18555=CARTESIAN_POINT ( 'NONE',  ( 1.054774247047244540, -0.07405724077823318263, 0.2952755904974176393 ) ) ;
#18557=CARTESIAN_POINT ( 'NONE',  ( 0.7495606340400177148, -0.1264236179284866091, 1.267224409395055096 ) ) ;
#18561=CARTESIAN_POINT ( 'NONE',  ( -1.054774247047244540, -0.07405724077823318263, 1.240157480261197431 ) ) ;
#18562=CARTESIAN_POINT ( 'NONE',  ( 0.8107537697050253289, -0.1574803149606297803, 0.6569881888688503535 ) ) ;
#18564=CARTESIAN_POINT ( 'NONE',  ( -0.9873396505805591694, 0.1113553986120547346, 1.747047244094488194 ) ) ;
#18565=CARTESIAN_POINT ( 'NONE',  ( 0.9781702082981658108, 0.1325945652753822701, 0.03936699474371046364 ) ) ;
#18569=CARTESIAN_POINT ( 'NONE',  ( -0.7185039370078739607, 1.928577636452523993E-17, 1.122047243986960652 ) ) ;
#18570=CARTESIAN_POINT ( 'NONE',  ( 0.7495606340400177148, 0.1264236179284866091, 1.532972440891118060 ) ) ;
#18571=CARTESIAN_POINT ( 'NONE',  ( -0.9412147342319837628, 0.1574803149606300301, 1.828248031496063630 ) ) ;
#18577=CARTESIAN_POINT ( 'NONE',  ( 0.7495606340400177148, 0.1264236179284866091, 0.6323818897100157432 ) ) ;
#18580=CARTESIAN_POINT ( 'NONE',  ( -0.9500414927467378812, 0.1787899950787401604, 1.097440944828127041 ) ) ;
#18582=CARTESIAN_POINT ( 'NONE',  ( -0.8019270111902717657, 0.1787899950787401604, 0.1574803149068664809 ) ) ;
#18584=( BOUNDED_CURVE ( )  B_SPLINE_CURVE ( 2, ( #31738, #24764, #13510, #46794, #36019, #17808, #14226, #28868, #39362 ),
 .UNSPECIFIED., .F., .T. ) 
 B_SPLINE_CURVE_WITH_KNOTS ( ( 3, 2, 2, 2, 3 ),
 ( 0.7500000000000000000, 0.7524999999999999467, 0.7550000000000000044, 0.7574999999999999512, 0.7600000000000000089 ),
 .UNSPECIFIED. ) 
 CURVE ( )  GEOMETRIC_REPRESENTATION_ITEM ( )  RATIONAL_B_SPLINE_CURVE ( ( 1.000000000000000000, 0.9238795325112869605, 1.000000000000000000, 0.9238795325112869605, 1.000000000000000000, 0.9238795325112869605, 1.000000000000000000, 0.9238795325112869605, 1.000000000000000000 ) ) 
 REPRESENTATION_ITEM ( '' )  ) ;
#18585=CARTESIAN_POINT ( 'NONE',  ( 0.9873396505805591694, -0.1113553986120547346, 1.648622047136566904 ) ) ;
#18591=CARTESIAN_POINT ( 'NONE',  ( -1.002407869896990045, 0.1264236179284866091, 0.7750984251430865779 ) ) ;
#18593=CARTESIAN_POINT ( 'NONE',  ( -0.6971942568897648851, -0.07405724077823297447, 1.860236220418677089 ) ) ;
#18595=CARTESIAN_POINT ( 'NONE',  ( -0.7495606340400177148, -0.1264236179284866091, 0.05167322829269323931 ) ) ;
#18596=CARTESIAN_POINT ( 'NONE',  ( -0.9412147342319837628, 0.1574803149606300301, 0.8439960629921254842 ) ) ;
#18599=CARTESIAN_POINT ( 'NONE',  ( -0.9412147342319837628, 0.1574803149606300301, 1.503444881782235232 ) ) ;
#18601=CARTESIAN_POINT ( 'NONE',  ( 0.8019270111902717657, -0.1787899950787401604, 0.8415354330171019859 ) ) ;
#18603=CARTESIAN_POINT ( 'NONE',  ( -1.054774247047244096, 0.000000000000000000, 1.562499999946236118 ) ) ;
#18605=CARTESIAN_POINT ( 'NONE',  ( -0.9873396505805591694, 0.1113553986120547346, 0.4478346456692913202 ) ) ;
#18606=CARTESIAN_POINT ( 'NONE',  ( 0.9412147342319837628, 0.1574803149606300301, 1.355807086614173596 ) ) ;
#18607=CARTESIAN_POINT ( 'NONE',  ( 0.8499887760485748123, -0.1717780610005492925, 1.987730942720379090 ) ) ;
#18608=DIRECTION ( 'NONE',  ( 0.000000000000000000, 0.000000000000000000, -1.000000000000000000 ) ) ;
#18610=ADVANCED_FACE ( 'NONE', ( #43051 ), #24861, .T. ) ;
#18611=CARTESIAN_POINT ( 'NONE',  ( 0.6971942568897648851, -0.07405724077823297447, 0.7529527558517473684 ) ) ;
#18614=CARTESIAN_POINT ( 'NONE',  ( 1.033464566929134687, 0.06523048226347956391, 0.9178149606299221830 ) ) ;
#18615=CARTESIAN_POINT ( 'NONE',  ( 1.033464566929133799, 0.000000000000000000, 0.4035433070866141780 ) ) ;
#18616=CARTESIAN_POINT ( 'NONE',  ( 1.054774247047244540, -0.07405724077823318263, 1.043307086560409269 ) ) ;
#18621=CARTESIAN_POINT ( 'NONE',  ( -0.9500414927467378812, 0.1787899950787401604, 0.5019685038832442103 ) ) ;
#18622=VERTEX_POINT ( 'NONE', #37282 ) ;
#18624=CARTESIAN_POINT ( 'NONE',  ( -1.002407869896990045, -0.1264236179284866091, 0.2534448818360003908 ) ) ;
#18625=ORIENTED_EDGE ( 'NONE', *, *, #22560, .F. ) ;
#18627=CARTESIAN_POINT ( 'NONE',  ( -0.8759842519685039353, 0.1787899950787401882, 1.724901574749385880 ) ) ;
#18628=CARTESIAN_POINT ( 'NONE',  ( -0.6971942568897637749, 2.189545951927499583E-17, 0.8686023621509606496 ) ) ;
#18629=CARTESIAN_POINT ( 'NONE',  ( -0.7495606340400177148, 0.1264236179284866091, 0.3174212597887562382 ) ) ;
#18631=CARTESIAN_POINT ( 'NONE',  ( 0.7646288533564489232, -0.1113553986120547346, 0.9793307086614173596 ) ) ;
#18637=CARTESIAN_POINT ( 'NONE',  ( -0.8759842519685039353, 0.1574803149606299191, 1.899606299105070839 ) ) ;
#18640=CARTESIAN_POINT ( 'NONE',  ( -0.8019270111902717657, -0.1787899950787401604, 0.2460629920722207375 ) ) ;
#18643=CARTESIAN_POINT ( 'NONE',  ( -1.054774247047244096, 0.000000000000000000, 1.365649606245448844 ) ) ;
#18645=EDGE_CURVE ( 'NONE', #11192, #28460, #10483, .T. ) ;
#18648=DIRECTION ( 'NONE',  ( 1.822029033848725028E-16, 0.000000000000000000, 1.000000000000000000 ) ) ;
#18651=CARTESIAN_POINT ( 'NONE',  ( 0.7646288533564489232, 0.1113553986120547346, 0.4183070866141732624 ) ) ;
#18652=DIRECTION ( 'NONE',  ( 0.000000000000000000, 0.000000000000000000, -1.000000000000000000 ) ) ;
#18653=CARTESIAN_POINT ( 'NONE',  ( -0.9873396505805591694, -0.1113553986120547346, 1.018700787294047228 ) ) ;
#18658=CARTESIAN_POINT ( 'NONE',  ( 0.7185039370078739607, 0.000000000000000000, 4.498031496062992574 ) ) ;
#18659=VERTEX_POINT ( 'NONE', #37057 ) ;
#18661=CARTESIAN_POINT ( 'NONE',  ( 0.7185039370078739607, 1.928577636452523993E-17, 0.8956692913385826404 ) ) ;
#18663=CARTESIAN_POINT ( 'NONE',  ( 0.7646288533564489232, -0.1113553986120547346, 1.530511811023621993 ) ) ;
#18665=VECTOR ( 'NONE', #19840, 39.37007874015748143 ) ;
#18668=CARTESIAN_POINT ( 'NONE',  ( 0.9873396505805591694, 0.1113553986120547346, 1.894685039262551163 ) ) ;
#18669=CARTESIAN_POINT ( 'NONE',  ( 0.7646288533564489232, -0.1113553986120547346, 1.373031496062992352 ) ) ;
#18673=CARTESIAN_POINT ( 'NONE',  ( 0.9412147342319837628, -0.1574803149606297803, 0.9768700786326298680 ) ) ;
#18674=CARTESIAN_POINT ( 'NONE',  ( -0.7185039370078739607, 1.928577636452523993E-17, 0.4232283464566928832 ) ) ;
#18676=ORIENTED_EDGE ( 'NONE', *, *, #19255, .F. ) ;
#18678=CARTESIAN_POINT ( 'NONE',  ( -0.9500414927467378812, 0.1787899950787401604, 1.648622047190331230 ) ) ;
#18679=CARTESIAN_POINT ( 'NONE',  ( 1.002407869896990045, -0.1264236179284866091, 1.715059055064346527 ) ) ;
#18681=CARTESIAN_POINT ( 'NONE',  ( -0.8019270111902717657, -0.1787899950787401604, 0.7234251967966300878 ) ) ;
#18683=CARTESIAN_POINT ( 'NONE',  ( 1.054774247047244096, 0.000000000000000000, 0.2632874015210397434 ) ) ;
#18685=CARTESIAN_POINT ( 'NONE',  ( -0.8759842519685039353, 0.1787899950787401882, 1.291830708607653477 ) ) ;
#18687=( BOUNDED_CURVE ( )  B_SPLINE_CURVE ( 2, ( #47282, #15650, #34553, #27395, #30288, #19921, #34104, #41464, #12285 ),
 .UNSPECIFIED., .F., .T. ) 
 B_SPLINE_CURVE_WITH_KNOTS ( ( 3, 2, 2, 2, 3 ),
 ( 0.6600000000000000311, 0.6624999999999999778, 0.6650000000000000355, 0.6674999999999999822, 0.6700000000000000400 ),
 .UNSPECIFIED. ) 
 CURVE ( )  GEOMETRIC_REPRESENTATION_ITEM ( )  RATIONAL_B_SPLINE_CURVE ( ( 1.000000000000000000, 0.9238795325112869605, 1.000000000000000000, 0.9238795325112869605, 1.000000000000000000, 0.9238795325112869605, 1.000000000000000000, 0.9238795325112829637, 1.000000000000000000 ) ) 
 REPRESENTATION_ITEM ( '' )  ) ;
#18689=CARTESIAN_POINT ( 'NONE',  ( -0.8759842519685039353, -0.1787899950787401882, 1.513287401521039355 ) ) ;
#18690=CARTESIAN_POINT ( 'NONE',  ( -0.7646288533564489232, 0.1113553986120547346, 1.865157480207432883 ) ) ;
#18693=CARTESIAN_POINT ( 'NONE',  ( -0.8759842519685039353, 0.1574803149606299191, 1.594488188976378007 ) ) ;
#18695=CARTESIAN_POINT ( 'NONE',  ( 0.8019270111902716547, 0.1787899950787401604, 1.417322834591906444 ) ) ;
#18697=DIRECTION ( 'NONE',  ( 1.822029033848725028E-16, 0.000000000000000000, 1.000000000000000000 ) ) ;
#18703=( BOUNDED_CURVE ( )  B_SPLINE_CURVE ( 2, ( #22208, #19565, #11445, #26545, #4940, #34211, #44703, #41339, #37294 ),
 .UNSPECIFIED., .F., .T. ) 
 B_SPLINE_CURVE_WITH_KNOTS ( ( 3, 2, 2, 2, 3 ),
 ( 0.4199999999999999845, 0.4224999999999999867, 0.4249999999999999889, 0.4274999999999999911, 0.4299999999999999933 ),
 .UNSPECIFIED. ) 
 CURVE ( )  GEOMETRIC_REPRESENTATION_ITEM ( )  RATIONAL_B_SPLINE_CURVE ( ( 1.000000000000000000, 0.9238795325112869605, 1.000000000000000000, 0.9238795325112869605, 1.000000000000000000, 0.9238795325112869605, 1.000000000000000000, 0.9238795325112869605, 1.000000000000000000 ) ) 
 REPRESENTATION_ITEM ( '' )  ) ;
#18710=EDGE_CURVE ( 'NONE', #42764, #16359, #7389, .T. ) ;
#18713=CARTESIAN_POINT ( 'NONE',  ( 0.9412147342319837628, -0.1574803149606297803, 0.1500984250893234173 ) ) ;
#18715=CARTESIAN_POINT ( 'NONE',  ( -0.7185039370078739607, 1.928577636452523993E-17, 0.8858267715460158565 ) ) ;
#18716=CARTESIAN_POINT ( 'NONE',  ( 1.002407869896990045, 0.1264236179284866091, 0.7357283464029290565 ) ) ;
#18717=CARTESIAN_POINT ( 'NONE',  ( -0.8823337881418780171, 0.1741736834747893703, 0.03937007874015843734 ) ) ;
#18718=CARTESIAN_POINT ( 'NONE',  ( 0.8759842519685039353, -0.1574803149606299191, 1.131889763672000004 ) ) ;
#18722=CARTESIAN_POINT ( 'NONE',  ( 0.6971942568897648851, 0.07405724077823318263, 1.855314960576157635 ) ) ;
#18724=CARTESIAN_POINT ( 'NONE',  ( 0.9873396505805591694, -0.1113553986120547346, 0.08366141732283464971 ) ) ;
#18728=DIRECTION ( 'NONE',  ( 1.000000000000000000, 0.000000000000000000, -1.822029033848725275E-16 ) ) ;
#18730=CARTESIAN_POINT ( 'NONE',  ( 0.6971942568897626646, 0.07405724077823318263, 0.1624015747493861295 ) ) ;
#18732=CARTESIAN_POINT ( 'NONE',  ( 1.002407869896990045, 0.1264236179284866091, 0.5782480314422993040 ) ) ;
#18733=CARTESIAN_POINT ( 'NONE',  ( -0.8759842519685039353, 0.1787899950787401882, 1.567421259788755794 ) ) ;
#18735=VECTOR ( 'NONE', #15133, 39.37007874015748143 ) ;
#18736=CARTESIAN_POINT ( 'NONE',  ( -0.8759842519685039353, 0.1787899950787401882, 1.139271653489543290 ) ) ;
#18737=CARTESIAN_POINT ( 'NONE',  ( -0.7185039370078746268, 0.06523048226347956391, 0.3420275590551182798 ) ) ;
#18738=CARTESIAN_POINT ( 'NONE',  ( 0.7495606340400177148, -0.1264236179284866091, 1.311515747977732405 ) ) ;
#18740=CARTESIAN_POINT ( 'NONE',  ( 1.054774247047244540, -0.07405724077823318263, 0.06397637789899228433 ) ) ;
#18741=CARTESIAN_POINT ( 'NONE',  ( -0.9500414927467378812, 0.1787899950787401604, 1.131889763725763665 ) ) ;
#18742=CARTESIAN_POINT ( 'NONE',  ( -0.7185039370078739607, 1.928577636452523993E-17, 0.3740157479239689664 ) ) ;
#18744=CARTESIAN_POINT ( 'NONE',  ( 0.9500414927467377701, 0.1787899950787401604, 0.3887795275052913224 ) ) ;
#18745=CARTESIAN_POINT ( 'NONE',  ( -0.8019270111902716547, 0.1787899950787401604, 0.1525590550643468324 ) ) ;
#18746=CARTESIAN_POINT ( 'NONE',  ( -0.6971942568897626646, -0.07405724077823297447, 0.7135826771115916234 ) ) ;
#18748=CARTESIAN_POINT ( 'NONE',  ( -0.8759842519685039353, 0.1574803149606299191, 1.358267716535433323 ) ) ;
#18749=ORIENTED_EDGE ( 'NONE', *, *, #1026, .T. ) ;
#18750=CARTESIAN_POINT ( 'NONE',  ( 1.054774247047244540, 0.07405724077823318263, 0.8956692912848198684 ) ) ;
#18751=CARTESIAN_POINT ( 'NONE',  ( -0.8107537697050253289, 0.1574803149606300301, 0.1008858267716536417 ) ) ;
#18752=CARTESIAN_POINT ( 'NONE',  ( 0.8759842519685039353, 0.1787899950787401882, 1.021161417269070837 ) ) ;
#18753=CARTESIAN_POINT ( 'NONE',  ( -1.002407869896990045, -0.1264236179284866091, 1.906988188922614125 ) ) ;
#18755=CARTESIAN_POINT ( 'NONE',  ( 0.8019270111902717657, -0.1787899950787401604, 1.899606299158834943 ) ) ;
#18762=ORIENTED_EDGE ( 'NONE', *, *, #18271, .F. ) ;
#18763=CARTESIAN_POINT ( 'NONE',  ( 0.9500414927467378812, 0.1787899950787401604, 1.131889763725763665 ) ) ;
#18764=CARTESIAN_POINT ( 'NONE',  ( -1.033464566929133799, 0.000000000000000000, 0.8267716534357796299 ) ) ;
#18766=ADVANCED_FACE ( 'NONE', ( #4686 ), #14797, .T. ) ;
#18768=CARTESIAN_POINT ( 'NONE',  ( 0.7495606340400177148, -0.1264236179284866091, 0.2042322834108035723 ) ) ;
#18770=EDGE_CURVE ( 'NONE', #23920, #758, #33020, .T. ) ;
#18777=CARTESIAN_POINT ( 'NONE',  ( -0.7495606340400177148, 0.1264236179284866091, 0.5930118109698583329 ) ) ;
#18781=CARTESIAN_POINT ( 'NONE',  ( 0.6971942568897637749, 2.189545951927499583E-17, 1.424704724355685181 ) ) ;
#18782=CARTESIAN_POINT ( 'NONE',  ( 0.7495606340400177148, 0.1264236179284866091, 1.690452755851748146 ) ) ;
#18785=CARTESIAN_POINT ( 'NONE',  ( -0.7760757061066729801, 0.1264651649003885048, 1.980451458961573596 ) ) ;
#18789=CARTESIAN_POINT ( 'NONE',  ( 1.054774247047244096, 0.000000000000000000, 0.2583661416785200671 ) ) ;
#18792=CARTESIAN_POINT ( 'NONE',  ( -1.033464566929134687, 0.06523048226347956391, 0.7603346456692923194 ) ) ;
#18793=CARTESIAN_POINT ( 'NONE',  ( 1.033464566929134687, -0.06523048226347956391, 0.6274606298137325178 ) ) ;
#18795=CARTESIAN_POINT ( 'NONE',  ( 0.9873396505805591694, 0.1113553986120547346, 0.6840551181102363376 ) ) ;
#18800=CARTESIAN_POINT ( 'NONE',  ( 1.002407869896990045, 0.1264236179284866091, 1.601870078686393750 ) ) ;
#18803=CARTESIAN_POINT ( 'NONE',  ( 1.033464566929134687, 0.06523048226347956391, 1.902066929133858553 ) ) ;
#18806=ORIENTED_EDGE ( 'NONE', *, *, #5038, .F. ) ;
#18810=CARTESIAN_POINT ( 'NONE',  ( 0.6971942568897648851, -0.07405724077823297447, 0.8759842519147408302 ) ) ;
#18812=CARTESIAN_POINT ( 'NONE',  ( -0.8019270111902717657, 0.1787899950787401604, 1.299212598371432215 ) ) ;
#18815=ORIENTED_EDGE ( 'NONE', *, *, #3239, .F. ) ;
#18817=CARTESIAN_POINT ( 'NONE',  ( -0.8019270111902717657, 0.1787899950787401604, 0.3149606298674962890 ) ) ;
#18819=CARTESIAN_POINT ( 'NONE',  ( 0.7185039370078739607, 1.928577636452523993E-17, 0.8070866140657008136 ) ) ;
#18821=EDGE_LOOP ( 'NONE', ( #7577, #17979, #25806, #37741 ) ) ;
#18824=CARTESIAN_POINT ( 'NONE',  ( 0.6971942568897648851, 0.07405724077823318263, 1.023622047190330342 ) ) ;
#18831=CARTESIAN_POINT ( 'NONE',  ( -1.054774247047244540, -0.07405724077823318263, 0.1033464566391499029 ) ) ;
#18832=CARTESIAN_POINT ( 'NONE',  ( -0.9412147342319837628, 0.1574803149606300301, 0.8833661417322832277 ) ) ;
#18835=CARTESIAN_POINT ( 'NONE',  ( -0.7185039370078739607, 1.928577636452523993E-17, 0.4133858266641259882 ) ) ;
#18836=CARTESIAN_POINT ( 'NONE',  ( -0.7646288533564489232, 0.1113553986120547346, 1.550196850286173156 ) ) ;
#18837=CARTESIAN_POINT ( 'NONE',  ( 1.002407869896990045, 0.1264236179284866091, 0.9768700786863937502 ) ) ;
#18838=CARTESIAN_POINT ( 'NONE',  ( 0.8759842519685039353, 0.1787899950787401882, 1.370570866087968520 ) ) ;
#18840=CARTESIAN_POINT ( 'NONE',  ( 0.8107537697050253289, -0.1574803149606297803, 1.454232283464566677 ) ) ;
#18841=CARTESIAN_POINT ( 'NONE',  ( 0.7461016248840900422, -0.1094034688171133807, 1.985470781864962841 ) ) ;
#18842=FACE_OUTER_BOUND ( 'NONE', #43143, .T. ) ;
#18844=CARTESIAN_POINT ( 'NONE',  ( 1.002407869896990045, 0.1264236179284866091, 0.8144685038832440993 ) ) ;
#18847=EDGE_LOOP ( 'NONE', ( #38322, #22735, #32466, #26872 ) ) ;
#18850=CARTESIAN_POINT ( 'NONE',  ( 0.8759842519685039353, -0.1787899950787401882, 1.114665354276944909 ) ) ;
#18856=CARTESIAN_POINT ( 'NONE',  ( -0.6971942568897637749, 2.189545951927499583E-17, 0.1993110235682838682 ) ) ;
#18858=CARTESIAN_POINT ( 'NONE',  ( 1.033464566929133799, 0.000000000000000000, 0.3543307085538902057 ) ) ;
#18859=CARTESIAN_POINT ( 'NONE',  ( -0.8759842519685039353, -0.1787899950787401882, 1.705216535379307174 ) ) ;
#18860=CARTESIAN_POINT ( 'NONE',  ( -0.8019270111902716547, 0.1787899950787401604, 0.8612204723871810241 ) ) ;
#18861=CARTESIAN_POINT ( 'NONE',  ( -0.9500414927467378812, 0.1787899950787401604, 0.4675196849856070869 ) ) ;
#18864=CARTESIAN_POINT ( 'NONE',  ( -1.033464566929133799, 1.928577636452524610E-17, 2.869337061179095023E-17 ) ) ;
#18865=CARTESIAN_POINT ( 'NONE',  ( 0.6971942568897626646, -0.07405724077823297447, 0.04429133852891373180 ) ) ;
#18872=ADVANCED_FACE ( 'NONE', ( #45414 ), #46124, .T. ) ;
#18874=CARTESIAN_POINT ( 'NONE',  ( -0.7495606340400177148, 0.1264236179284866091, 0.3912401574265515491 ) ) ;
#18879=CARTESIAN_POINT ( 'NONE',  ( -0.9500414927467377701, -0.1787899950787401604, 1.437007873961985593 ) ) ;
#18881=EDGE_CURVE ( 'NONE', #26454, #24716, #33442, .T. ) ;
#18884=AXIS2_PLACEMENT_3D ( 'NONE', #18988, #27168, #26447 ) ;
#18885=CARTESIAN_POINT ( 'NONE',  ( 0.8759842519685039353, 0.000000000000000000, 2.007874015640504162 ) ) ;
#18887=CARTESIAN_POINT ( 'NONE',  ( 0.8759842519685039353, -0.1574803149606299191, 0.5118110236220472231 ) ) ;
#18889=CARTESIAN_POINT ( 'NONE',  ( -0.9412147342319837628, 0.1574803149606300301, 1.070374015640503496 ) ) ;
#18890=CARTESIAN_POINT ( 'NONE',  ( 1.054774247047244096, 0.000000000000000000, 0.6176181101824566033 ) ) ;
#18893=CARTESIAN_POINT ( 'NONE',  ( 0.7646288533564489232, -0.1113553986120547346, 1.993110236112944911 ) ) ;
#18894=EDGE_LOOP ( 'NONE', ( #12294, #16892, #12768, #11897 ) ) ;
#18896=CARTESIAN_POINT ( 'NONE',  ( -1.054774247047244540, -0.07405724077823318263, 1.008858267662772423 ) ) ;
#18897=CARTESIAN_POINT ( 'NONE',  ( 0.7646288533564489232, 0.1113553986120547346, 0.9694881889763780070 ) ) ;
#18901=VERTEX_POINT ( 'NONE', #1326 ) ;
#18903=CARTESIAN_POINT ( 'NONE',  ( 0.8759842519685039353, 0.1787899950787401882, 0.7012795275052913224 ) ) ;
#18906=CARTESIAN_POINT ( 'NONE',  ( -0.7185039370078739607, 1.928577636452523993E-17, 0.9744094488188976833 ) ) ;
#18910=CARTESIAN_POINT ( 'NONE',  ( 0.7185039370078746268, 0.06523048226347956391, 1.198326771546015967 ) ) ;
#18914=CARTESIAN_POINT ( 'NONE',  ( -1.002407869896990045, -0.1264236179284866091, 1.833169291284818758 ) ) ;
#18915=CARTESIAN_POINT ( 'NONE',  ( 0.8759842519685039353, -0.1787899950787401882, 1.749507873961984483 ) ) ;
#18917=DIRECTION ( 'NONE',  ( -1.000000000000000000, 0.000000000000000000, 0.000000000000000000 ) ) ;
#18918=CARTESIAN_POINT ( 'NONE',  ( 0.7495606340400177148, 0.1264236179284866091, 0.3567913385289137596 ) ) ;
#18919=CARTESIAN_POINT ( 'NONE',  ( -0.7185039370078739607, 1.928577636452523993E-17, 1.515748031388535200 ) ) ;
#18920=CARTESIAN_POINT ( 'NONE',  ( -0.8019270111902716547, -0.1787899950787401604, 1.269685039316314601 ) ) ;
#18921=CARTESIAN_POINT ( 'NONE',  ( -1.054774247047244540, 0.07405724077823318263, 0.8907480314422986378 ) ) ;
#18923=CARTESIAN_POINT ( 'NONE',  ( -0.8759842519685039353, 0.1787899950787401882, 0.1550196849856066983 ) ) ;
#18925=CARTESIAN_POINT ( 'NONE',  ( -0.9500414927467378812, 0.1787899950787401604, 1.609251968450173376 ) ) ;
#18926=CARTESIAN_POINT ( 'NONE',  ( -0.8107537697050253289, -0.1574803149606297803, 1.916830708553890705 ) ) ;
#18927=ORIENTED_EDGE ( 'NONE', *, *, #10520, .T. ) ;
#18928=CARTESIAN_POINT ( 'NONE',  ( -0.9412147342319837628, -0.1574803149606297803, 1.537893700787401841 ) ) ;
#18931=CARTESIAN_POINT ( 'NONE',  ( 0.7495606340400177148, 0.1264236179284866091, 1.537893700733637736 ) ) ;
#18933=CARTESIAN_POINT ( 'NONE',  ( 0.9873396505805591694, -0.1113553986120547346, 1.018700787294047228 ) ) ;
#18936=ORIENTED_EDGE ( 'NONE', *, *, #17593, .T. ) ;
#18946=CARTESIAN_POINT ( 'NONE',  ( -0.9412147342319837628, 0.1574803149606300301, 1.070374015640503496 ) ) ;
#18947=CARTESIAN_POINT ( 'NONE',  ( 0.7495606340400177148, -0.1264236179284866091, 0.8341535432533228045 ) ) ;
#18952=CARTESIAN_POINT ( 'NONE',  ( 0.9873396505805591694, -0.1113553986120547346, 1.264763779527559029 ) ) ;
#18953=CARTESIAN_POINT ( 'NONE',  ( 0.8759842519685039353, 0.1787899950787401882, 1.769192913332062966 ) ) ;
#18954=CARTESIAN_POINT ( 'NONE',  ( 0.8107537697050254399, -0.1574803149606297803, 1.877460629813732407 ) ) ;
#18955=CARTESIAN_POINT ( 'NONE',  ( 0.8107537697050234415, -0.1574803149606297803, 0.07627952755905517690 ) ) ;
#18956=FACE_OUTER_BOUND ( 'NONE', #23490, .T. ) ;
#18961=CARTESIAN_POINT ( 'NONE',  ( 1.054774247047244096, 0.000000000000000000, 0.2239173227808822775 ) ) ;
#18962=( BOUNDED_CURVE ( )  B_SPLINE_CURVE ( 2, ( #1158, #45236, #41628, #30913, #42110, #16742, #4999, #12699, #44995 ),
 .UNSPECIFIED., .F., .T. ) 
 B_SPLINE_CURVE_WITH_KNOTS ( ( 3, 2, 2, 2, 3 ),
 ( 0.2800000000000000266, 0.2824999999999999734, 0.2849999999999999756, 0.2874999999999999778, 0.2899999999999999800 ),
 .UNSPECIFIED. ) 
 CURVE ( )  GEOMETRIC_REPRESENTATION_ITEM ( )  RATIONAL_B_SPLINE_CURVE ( ( 1.000000000000000000, 0.9238795325112849621, 1.000000000000000000, 0.9238795325112869605, 1.000000000000000000, 0.9238795325112869605, 1.000000000000000000, 0.9238795325112869605, 1.000000000000000000 ) ) 
 REPRESENTATION_ITEM ( '' )  ) ;
#18963=CARTESIAN_POINT ( 'NONE',  ( 0.7185039370078746268, 0.06523048226347956391, 1.119586614065702035 ) ) ;
#18964=CARTESIAN_POINT ( 'NONE',  ( -0.7495606340400177148, -0.1264236179284866091, 1.818405511757259729 ) ) ;
#18966=CARTESIAN_POINT ( 'NONE',  ( -0.8759842519685039353, 0.1787899950787401882, 1.257381889710015743 ) ) ;
#18967=CARTESIAN_POINT ( 'NONE',  ( -0.9873396505805591694, 0.1113553986120547346, 0.8809055118110236116 ) ) ;
#18968=CARTESIAN_POINT ( 'NONE',  ( -1.002407869896990045, -0.1264236179284866091, 1.040846456639149764 ) ) ;
#18969=EDGE_CURVE ( 'NONE', #2757, #19233, #12859, .T. ) ;
#18971=CARTESIAN_POINT ( 'NONE',  ( 1.033464566929133799, 0.000000000000000000, 0.03937007863263043694 ) ) ;
#18972=CARTESIAN_POINT ( 'NONE',  ( 0.6971942568897648851, -0.07405724077823297447, 0.4822834645131655606 ) ) ;
#18973=CARTESIAN_POINT ( 'NONE',  ( -1.054774247047244540, 0.07405724077823318263, 0.4183070865604096578 ) ) ;
#18974=CARTESIAN_POINT ( 'NONE',  ( 1.033464566929134687, 0.06523048226347956391, 1.734744094380662904 ) ) ;
#18976=ORIENTED_EDGE ( 'NONE', *, *, #5081, .F. ) ;
#18978=CARTESIAN_POINT ( 'NONE',  ( 0.8019270111902717657, 0.1787899950787401604, 0.9055118109698585549 ) ) ;
#18979=CARTESIAN_POINT ( 'NONE',  ( -0.7646288533564489232, 0.1113553986120547346, 0.2214566929133858220 ) ) ;
#18980=ADVANCED_FACE ( 'NONE', ( #45170 ), #27953, .T. ) ;
#18981=CARTESIAN_POINT ( 'NONE',  ( 0.8759842519685039353, -0.1787899950787401882, 1.198326771599779628 ) ) ;
#18984=DIRECTION ( 'NONE',  ( 0.000000000000000000, 0.000000000000000000, 1.000000000000000000 ) ) ;
#18985=CARTESIAN_POINT ( 'NONE',  ( -0.8759842519685039353, -0.1787899950787401882, 0.8833661416785196785 ) ) ;
#18987=( BOUNDED_CURVE ( )  B_SPLINE_CURVE ( 2, ( #30640, #23194, #41357, #38511, #33771, #15542, #37808, #45201, #12425 ),
 .UNSPECIFIED., .F., .F. ) 
 B_SPLINE_CURVE_WITH_KNOTS ( ( 3, 2, 2, 2, 3 ),
 ( 0.8399999999999999689, 0.8425000000000000266, 0.8449999999999999734, 0.8475000000000000311, 0.8499999999999999778 ),
 .UNSPECIFIED. ) 
 CURVE ( )  GEOMETRIC_REPRESENTATION_ITEM ( )  RATIONAL_B_SPLINE_CURVE ( ( 1.000000000000000000, 0.9238795325112869605, 1.000000000000000000, 0.9238795325112869605, 1.000000000000000000, 0.9238795325112869605, 1.000000000000000000, 0.9238795325112869605, 1.000000000000000000 ) ) 
 REPRESENTATION_ITEM ( '' )  ) ;
#18988=CARTESIAN_POINT ( 'NONE',  ( 0.8759842519685039353, 0.000000000000000000, 4.498031496062992574 ) ) ;
#18989=CARTESIAN_POINT ( 'NONE',  ( 0.8107537697050234415, -0.1574803149606297803, 0.3125000000000000000 ) ) ;
#18995=CARTESIAN_POINT ( 'NONE',  ( 0.8019270111902717657, 0.1787899950787401604, 1.254921259788757348 ) ) ;
#18997=FACE_OUTER_BOUND ( 'NONE', #31415, .T. ) ;
#18998=CARTESIAN_POINT ( 'NONE',  ( 0.8019270111902717657, 0.1787899950787401604, 0.1525590550643468046 ) ) ;
#19001=CARTESIAN_POINT ( 'NONE',  ( 1.033464566929133799, 0.000000000000000000, 1.348425196850393748 ) ) ;
#19002=CARTESIAN_POINT ( 'NONE',  ( -1.002407869896990045, 0.1264236179284866091, 0.7012795275052913224 ) ) ;
#19006=DIRECTION ( 'NONE',  ( 0.000000000000000000, 0.000000000000000000, 1.000000000000000000 ) ) ;
#19007=CARTESIAN_POINT ( 'NONE',  ( 0.6971942568897648851, 0.07405724077823318263, 1.382874015694268044 ) ) ;
#19008=CARTESIAN_POINT ( 'NONE',  ( 1.054774247047244540, 0.07405724077823318263, 1.756889763725764553 ) ) ;
#19009=CARTESIAN_POINT ( 'NONE',  ( 1.054774247047244096, 0.000000000000000000, 0.2583661416785200671 ) ) ;
#19010=CARTESIAN_POINT ( 'NONE',  ( 0.8759842519685039353, 0.1574803149606299191, 0.1377952755905511861 ) ) ;
#19011=CARTESIAN_POINT ( 'NONE',  ( -1.033464566929134687, 0.06523048226347956391, 1.508366141732284671 ) ) ;
#19017=CARTESIAN_POINT ( 'NONE',  ( 1.054774247047244540, 0.07405724077823318263, 0.3395669290800945039 ) ) ;
#19018=CARTESIAN_POINT ( 'NONE',  ( 0.9500414927467377701, 0.1787899950787401604, 1.249999999946235896 ) ) ;
#19019=CARTESIAN_POINT ( 'NONE',  ( -0.7185039370078778465, -0.06523048226348396317, 1.715059055010583089 ) ) ;
#19020=LINE ( 'NONE', #19738, #27385 ) ;
#19022=CARTESIAN_POINT ( 'NONE',  ( -1.054774247047244540, 0.07405724077823318263, 1.363188976324188895 ) ) ;
#19023=CARTESIAN_POINT ( 'NONE',  ( 0.8759842519685039353, -0.1574803149606299191, 0.5807086613097960370 ) ) ;
#19024=ORIENTED_EDGE ( 'NONE', *, *, #42133, .F. ) ;
#19025=CARTESIAN_POINT ( 'NONE',  ( 0.8479045121278329100, 0.1739705042521020872, 0.03937007862467874209 ) ) ;
#19029=CARTESIAN_POINT ( 'NONE',  ( -0.8759842519685039353, 0.1574803149606299191, 1.112204724301921299 ) ) ;
#19030=CARTESIAN_POINT ( 'NONE',  ( 0.8019270111902717657, -0.1787899950787401604, 1.545275590497416696 ) ) ;
#19031=CARTESIAN_POINT ( 'NONE',  ( -1.033464566929133799, 0.000000000000000000, 1.269685039370078705 ) ) ;
#19035=CARTESIAN_POINT ( 'NONE',  ( -0.8107537697050234415, -0.1574803149606297803, 0.1156496062992125873 ) ) ;
#19036=CARTESIAN_POINT ( 'NONE',  ( 1.054774247047244096, 0.000000000000000000, 0.06643700782025216411 ) ) ;
#19038=ORIENTED_EDGE ( 'NONE', *, *, #42509, .T. ) ;
#19039=EDGE_CURVE ( 'NONE', #11471, #24545, #41644, .T. ) ;
#19041=EDGE_CURVE ( 'NONE', #16635, #24379, #31625, .T. ) ;
#19042=CARTESIAN_POINT ( 'NONE',  ( 0.8019270111902716547, -0.1787899950787401604, 0.9202755904974182499 ) ) ;
#19043=CARTESIAN_POINT ( 'NONE',  ( -0.8019270111902716547, 0.1787899950787401604, 1.530511810969859221 ) ) ;
#19045=CARTESIAN_POINT ( 'NONE',  ( -1.002407869896990045, -0.1264236179284866091, 1.281988188922614125 ) ) ;
#19048=CARTESIAN_POINT ( 'NONE',  ( -1.002407869896990045, -0.1264236179284866091, 0.2977362204186775885 ) ) ;
#19050=CARTESIAN_POINT ( 'NONE',  ( 0.9873396505805591694, 0.1113553986120547346, 0.8710629920184568276 ) ) ;
#19052=ORIENTED_EDGE ( 'NONE', *, *, #23872, .T. ) ;
#19053=AXIS2_PLACEMENT_3D ( 'NONE', #38663, #5592, #20199 ) ;
#19056=CARTESIAN_POINT ( 'NONE',  ( 0.6971942568897637749, 2.189545951927499583E-17, 1.026082677111590513 ) ) ;
#19061=CARTESIAN_POINT ( 'NONE',  ( -0.8759842519685039353, -0.1787899950787401882, 0.1747047243556852092 ) ) ;
#19062=CARTESIAN_POINT ( 'NONE',  ( -0.8107537697050253289, -0.1574803149606297803, 0.9424212598425207865 ) ) ;
#19063=CARTESIAN_POINT ( 'NONE',  ( -0.7185039370078739607, 1.928577636452523993E-17, 1.958661417322834719 ) ) ;
#19065=CARTESIAN_POINT ( 'NONE',  ( -0.9873396505805591694, 0.1113553986120547346, 1.934055118002708573 ) ) ;
#19066=CARTESIAN_POINT ( 'NONE',  ( -0.7646288533564489232, -0.1113553986120547346, 1.599409448711369919 ) ) ;
#19067=CARTESIAN_POINT ( 'NONE',  ( 0.6971942568897637749, 2.189545951927499583E-17, 0.9128937007336377363 ) ) ;
#19068=CARTESIAN_POINT ( 'NONE',  ( 0.9412147342319837628, 0.1574803149606300301, 1.434547244094487972 ) ) ;
#19069=CARTESIAN_POINT ( 'NONE',  ( 0.7102985908446067809, 0.006325918183498560783, 1.983153498902621159 ) ) ;
#19070=CARTESIAN_POINT ( 'NONE',  ( 1.033464566929133799, 0.000000000000000000, 1.702755905511810885 ) ) ;
#19073=CARTESIAN_POINT ( 'NONE',  ( 0.8019270111902716547, 0.1787899950787401604, 0.8612204723871810241 ) ) ;
#19074=DIRECTION ( 'NONE',  ( 1.822029033848725028E-16, 0.000000000000000000, 1.000000000000000000 ) ) ;
#19076=CARTESIAN_POINT ( 'NONE',  ( 0.8759842519685039353, 0.1787899950787401882, 1.847933070812378009 ) ) ;
#19081=CARTESIAN_POINT ( 'NONE',  ( -1.054774247047244096, 0.000000000000000000, 1.995570866087968520 ) ) ;
#19082=CARTESIAN_POINT ( 'NONE',  ( 1.002407869896990045, 0.1264236179284866091, 1.090059055064346527 ) ) ;
#19083=LINE ( 'NONE', #30400, #40202 ) ;
#19087=ADVANCED_FACE ( 'NONE', ( #9952 ), #6217, .T. ) ;
#19088=CARTESIAN_POINT ( 'NONE',  ( -1.054774247047244540, 0.07405724077823318263, 0.4970472440407249226 ) ) ;
#19091=CARTESIAN_POINT ( 'NONE',  ( -0.7495606340400177148, -0.1264236179284866091, 0.2042322834108035723 ) ) ;
#19093=CARTESIAN_POINT ( 'NONE',  ( -0.7185039370078746268, 0.06523048226347956391, 0.6176181102362199304 ) ) ;
#19097=CARTESIAN_POINT ( 'NONE',  ( 0.7185039370078739607, 1.928577636452523993E-17, 0.3346456691838114450 ) ) ;
#19098=CARTESIAN_POINT ( 'NONE',  ( -1.002407869896990045, 0.1264236179284866091, 1.798720472387181024 ) ) ;
#19099=CARTESIAN_POINT ( 'NONE',  ( -0.8759842519685039353, -0.1787899950787401882, 0.8784448818360000022 ) ) ;
#19101=CARTESIAN_POINT ( 'NONE',  ( -0.7495606340400177148, 0.1264236179284866091, 0.5536417322297008115 ) ) ;
#19103=CARTESIAN_POINT ( 'NONE',  ( -0.7185039370078739607, 1.928577636452523993E-17, 1.358267716427907779 ) ) ;
#19104=CARTESIAN_POINT ( 'NONE',  ( 0.8107537697050254399, -0.1574803149606297803, 0.9817913385826764205 ) ) ;
#19106=CARTESIAN_POINT ( 'NONE',  ( -1.033464566929133799, 0.000000000000000000, 1.702755905511810885 ) ) ;
#19109=CARTESIAN_POINT ( 'NONE',  ( -0.7185039370078692977, 0.06523048226347515077, 1.906988188868851797 ) ) ;
#19110=CARTESIAN_POINT ( 'NONE',  ( 0.9873396505805591694, 0.1113553986120547346, 1.786417322834645605 ) ) ;
#19112=CARTESIAN_POINT ( 'NONE',  ( -0.9500414927467378812, -0.1787899950787401604, 0.2509842519147403861 ) ) ;
#19113=DIRECTION ( 'NONE',  ( 1.822029033848725028E-16, 0.000000000000000000, 1.000000000000000000 ) ) ;
#19115=ORIENTED_EDGE ( 'NONE', *, *, #41927, .F. ) ;
#19118=CARTESIAN_POINT ( 'NONE',  ( -0.8019270111902716547, 0.1787899950787401604, 1.574803149552536530 ) ) ;
#19122=DIRECTION ( 'NONE',  ( 1.000000000000000000, 0.000000000000000000, -1.822029033848725275E-16 ) ) ;
#19124=CARTESIAN_POINT ( 'NONE',  ( -1.033464566929134687, 0.06523048226347956391, 1.144192913278300194 ) ) ;
#19125=CARTESIAN_POINT ( 'NONE',  ( 1.002407869896990045, -0.1264236179284866091, 0.6126968503399370380 ) ) ;
#19131=CARTESIAN_POINT ( 'NONE',  ( -0.7495606340400177148, 0.1264236179284866091, 0.9867125983714331028 ) ) ;
#19132=CARTESIAN_POINT ( 'NONE',  ( 0.8107537697050253289, -0.1574803149606297803, 1.021161417322834497 ) ) ;
#19140=CARTESIAN_POINT ( 'NONE',  ( 0.6971942568897637749, 2.189545951927499583E-17, 0.7111220471903307860 ) ) ;
#19146=CARTESIAN_POINT ( 'NONE',  ( 0.7185039370078739607, 1.928577636452523993E-17, 1.122047243986960652 ) ) ;
#19147=CARTESIAN_POINT ( 'NONE',  ( -1.033464566929134687, -0.06523048226347956391, 1.660925196850393526 ) ) ;
#19149=AXIS2_PLACEMENT_3D ( 'NONE', #9977, #47347, #2994 ) ;
#19152=CARTESIAN_POINT ( 'NONE',  ( -0.6971942568897637749, 2.189545951927499583E-17, 1.739665354276945131 ) ) ;
#19154=CARTESIAN_POINT ( 'NONE',  ( 0.6971942568897648851, 0.07405724077823318263, 1.737204724355685848 ) ) ;
#19155=CARTESIAN_POINT ( 'NONE',  ( -0.6971942568897626646, 0.07405724077823318263, 0.9104330708123776761 ) ) ;
#19156=CYLINDRICAL_SURFACE ( 'NONE', #10345, 0.1574803149606299191 ) ;
#19157=CARTESIAN_POINT ( 'NONE',  ( 0.6971942568897626646, 0.07405724077823318263, 0.2411417322297011168 ) ) ;
#19158=CIRCLE ( 'NONE', #4603, 0.1574803149606300579 ) ;
#19159=CARTESIAN_POINT ( 'NONE',  ( -0.7495606340400177148, -0.1264236179284866091, 1.424704724355685181 ) ) ;
#19161=CARTESIAN_POINT ( 'NONE',  ( -1.002407869896990045, -0.1264236179284866091, 1.316437007820252081 ) ) ;
#19163=CARTESIAN_POINT ( 'NONE',  ( -1.002407869896990045, -0.1264236179284866091, 0.8833661416785196785 ) ) ;
#19165=CARTESIAN_POINT ( 'NONE',  ( -0.7495606340400177148, -0.1264236179284866091, 0.05167322829269323931 ) ) ;
#19167=CARTESIAN_POINT ( 'NONE',  ( -0.8759842519685039353, 0.1787899950787401882, 1.532972440891118060 ) ) ;
#19168=CARTESIAN_POINT ( 'NONE',  ( -0.7495606340400177148, -0.1264236179284866091, 0.09104330703285078152 ) ) ;
#19169=CARTESIAN_POINT ( 'NONE',  ( -1.033464566929134687, 0.06523048226347956391, 1.587106299212598826 ) ) ;
#19170=CARTESIAN_POINT ( 'NONE',  ( 0.9873396505805591694, -0.1113553986120547346, 0.9793307085538898171 ) ) ;
#19171=CARTESIAN_POINT ( 'NONE',  ( 0.8019270111902716547, 0.1787899950787401604, 1.653543307032850462 ) ) ;
#19174=CARTESIAN_POINT ( 'NONE',  ( 0.7185039370078746268, 0.06523048226347956391, 0.2928149605223942520 ) ) ;
#19175=VERTEX_POINT ( 'NONE', #35598 ) ;
#19176=ORIENTED_EDGE ( 'NONE', *, *, #44093, .F. ) ;
#19177=CARTESIAN_POINT ( 'NONE',  ( -1.002407869896990045, -0.1264236179284866091, 1.163877952702141672 ) ) ;
#19179=EDGE_CURVE ( 'NONE', #41516, #43867, #41353, .T. ) ;
#19182=CARTESIAN_POINT ( 'NONE',  ( 1.054774247047244540, -0.07405724077823318263, 1.830708661363559253 ) ) ;
#19188=CARTESIAN_POINT ( 'NONE',  ( 0.8759842519685039353, 0.1787899950787401882, 0.7406496062454487328 ) ) ;
#19189=AXIS2_PLACEMENT_3D ( 'NONE', #22976, #16040, #11737 ) ;
#19190=CARTESIAN_POINT ( 'NONE',  ( -1.033464566929134687, -0.06523048226347956391, 1.572342519577513142 ) ) ;
#19192=CARTESIAN_POINT ( 'NONE',  ( 1.033464566929134687, -0.06523048226347956391, 1.267224409448818978 ) ) ;
#19193=CARTESIAN_POINT ( 'NONE',  ( 0.8019270111902717657, 0.1787899950787401604, 1.771653543253322249 ) ) ;
#19196=ADVANCED_FACE ( 'NONE', ( #11376 ), #4380, .T. ) ;
#19197=CARTESIAN_POINT ( 'NONE',  ( 0.7185039370078746268, -0.06523048226347956391, 0.1500984251968505434 ) ) ;
#19200=CYLINDRICAL_SURFACE ( 'NONE', #33150, 0.1574803149606299191 ) ;
#19202=CARTESIAN_POINT ( 'NONE',  ( 1.002407869896990045, -0.1264236179284866091, 0.2583661416785200671 ) ) ;
#19203=CARTESIAN_POINT ( 'NONE',  ( 0.7646288533564489232, 0.1113553986120547346, 0.06397637795275590289 ) ) ;
#19205=CARTESIAN_POINT ( 'NONE',  ( -1.002407869896990045, -0.1264236179284866091, 1.828248031442299082 ) ) ;
#19206=EDGE_LOOP ( 'NONE', ( #11782, #21463, #23711, #42820 ) ) ;
#19207=CARTESIAN_POINT ( 'NONE',  ( -1.054774247047244096, 0.000000000000000000, 1.286909448765133801 ) ) ;
#19210=CARTESIAN_POINT ( 'NONE',  ( -1.054774247047244096, 0.000000000000000000, 0.5388779527021417826 ) ) ;
#19211=CARTESIAN_POINT ( 'NONE',  ( 0.8759842519685039353, -0.1787899950787401882, 1.941437007820252081 ) ) ;
#19212=CARTESIAN_POINT ( 'NONE',  ( -1.054774247047244540, 0.07405724077823318263, 1.087598425143086578 ) ) ;
#19216=CARTESIAN_POINT ( 'NONE',  ( 1.002407869896990045, -0.1264236179284866091, 0.4945866141194645849 ) ) ;
#19217=CARTESIAN_POINT ( 'NONE',  ( -0.6971942568897637749, 2.189545951927499583E-17, 0.3174212597887562382 ) ) ;
#19223=CARTESIAN_POINT ( 'NONE',  ( -0.9873396505805591694, 0.1113553986120547346, 0.1328740157480315098 ) ) ;
#19224=CARTESIAN_POINT ( 'NONE',  ( 0.7495606340400177148, 0.1264236179284866091, 1.183562992072220599 ) ) ;
#19230=CARTESIAN_POINT ( 'NONE',  ( -0.7646288533564489232, -0.1113553986120547346, 0.3100393700787401619 ) ) ;
#19231=CARTESIAN_POINT ( 'NONE',  ( 0.7185039370078739607, 1.928577636452523993E-17, 1.328740157480315043 ) ) ;
#19233=VERTEX_POINT ( 'NONE', #7761 ) ;
#19235=CARTESIAN_POINT ( 'NONE',  ( 0.7185039370078739607, 1.928577636452523993E-17, 0.09842519674286673292 ) ) ;
#19238=CARTESIAN_POINT ( 'NONE',  ( 0.9412147342319837628, -0.1574803149606297803, 0.7406496061916858498 ) ) ;
#19240=CARTESIAN_POINT ( 'NONE',  ( 1.002407869896990045, -0.1264236179284866091, 0.2140748030958428971 ) ) ;
#19246=( BOUNDED_CURVE ( )  B_SPLINE_CURVE ( 2, ( #3419, #18036, #32682, #47271, #4329, #22570, #4112, #18963, #29591 ),
 .UNSPECIFIED., .F., .F. ) 
 B_SPLINE_CURVE_WITH_KNOTS ( ( 3, 2, 2, 2, 3 ),
 ( 0.5400000000000000355, 0.5424999999999999822, 0.5450000000000000400, 0.5474999999999999867, 0.5500000000000000444 ),
 .UNSPECIFIED. ) 
 CURVE ( )  GEOMETRIC_REPRESENTATION_ITEM ( )  RATIONAL_B_SPLINE_CURVE ( ( 1.000000000000000000, 0.9238795325112869605, 1.000000000000000000, 0.9238795325112869605, 1.000000000000000000, 0.9238795325112869605, 1.000000000000000000, 0.9238795325112869605, 1.000000000000000000 ) ) 
 REPRESENTATION_ITEM ( '' )  ) ;
#19247=CARTESIAN_POINT ( 'NONE',  ( -0.7495606340400177148, 0.1264236179284866091, 0.6323818897100157432 ) ) ;
#19251=DIRECTION ( 'NONE',  ( -1.000000000000000000, 0.000000000000000000, 0.000000000000000000 ) ) ;
#19253=CARTESIAN_POINT ( 'NONE',  ( 0.7495606340400177148, 0.1264236179284866091, 1.301673228292692830 ) ) ;
#19254=CARTESIAN_POINT ( 'NONE',  ( 0.8759842519685039353, 0.1787899950787401882, 1.882381889710015743 ) ) ;
#19255=EDGE_CURVE ( 'NONE', #34250, #39764, #13822, .T. ) ;
#19258=CARTESIAN_POINT ( 'NONE',  ( 1.033464566929133799, 0.000000000000000000, 0.1279527559055118058 ) ) ;
#19260=CARTESIAN_POINT ( 'NONE',  ( 0.7185039370078739607, 1.928577636452523993E-17, 1.171259842519684957 ) ) ;
#19261=CYLINDRICAL_SURFACE ( 'NONE', #15247, 0.1574803149606299191 ) ;
#19263=CARTESIAN_POINT ( 'NONE',  ( -0.9412147342319837628, 0.1574803149606300301, 1.227854330601133359 ) ) ;
#19264=CARTESIAN_POINT ( 'NONE',  ( 1.002407869896990045, -0.1264236179284866091, 0.2928149605761578567 ) ) ;
#19265=CARTESIAN_POINT ( 'NONE',  ( 0.6971942568897637749, 2.189545951927499583E-17, 1.262303149552535420 ) ) ;
#19266=CARTESIAN_POINT ( 'NONE',  ( -0.7185039370078739607, 1.928577636452523993E-17, 0.7775590551181102983 ) ) ;
#19267=CARTESIAN_POINT ( 'NONE',  ( 1.033464566929134687, 0.06523048226347956391, 0.6323818896562525271 ) ) ;
#19275=CARTESIAN_POINT ( 'NONE',  ( 0.8019270111902717657, -0.1787899950787401604, 1.584645669237574994 ) ) ;
#19276=CARTESIAN_POINT ( 'NONE',  ( -0.9412147342319837628, 0.1574803149606300301, 1.237696850393701586 ) ) ;
#19277=CARTESIAN_POINT ( 'NONE',  ( -1.033464566929133799, 0.000000000000000000, 1.141732283357039357 ) ) ;
#19280=CARTESIAN_POINT ( 'NONE',  ( -0.9873396505805591694, -0.1113553986120547346, 0.5068897636720007815 ) ) ;
#19283=( BOUNDED_CURVE ( )  B_SPLINE_CURVE ( 2, ( #29305, #3122, #3837, #36222, #7664, #3608, #22053, #17749, #43854 ),
 .UNSPECIFIED., .F., .F. ) 
 B_SPLINE_CURVE_WITH_KNOTS ( ( 3, 2, 2, 2, 3 ),
 ( 0.2099999999999999922, 0.2124999999999999944, 0.2149999999999999967, 0.2174999999999999989, 0.2200000000000000011 ),
 .UNSPECIFIED. ) 
 CURVE ( )  GEOMETRIC_REPRESENTATION_ITEM ( )  RATIONAL_B_SPLINE_CURVE ( ( 1.000000000000000000, 0.9238795325112869605, 1.000000000000000000, 0.9238795325112869605, 1.000000000000000000, 0.9238795325112869605, 1.000000000000000000, 0.9238795325112869605, 1.000000000000000000 ) ) 
 REPRESENTATION_ITEM ( '' )  ) ;
#19285=VERTEX_POINT ( 'NONE', #11850 ) ;
#19286=CARTESIAN_POINT ( 'NONE',  ( 0.8759842519685039353, 0.1787899950787401882, 0.9424212597887559051 ) ) ;
#19287=CARTESIAN_POINT ( 'NONE',  ( -0.8759842519685039353, -0.1787899950787401882, 1.547736220418677089 ) ) ;
#19289=ORIENTED_EDGE ( 'NONE', *, *, #33416, .F. ) ;
#19291=CARTESIAN_POINT ( 'NONE',  ( -0.9500414927467378812, -0.1787899950787401604, 0.3740157479777325711 ) ) ;
#19295=VERTEX_POINT ( 'NONE', #41038 ) ;
#19301=CARTESIAN_POINT ( 'NONE',  ( -1.033464566929134687, -0.06523048226347956391, 0.2731299211523157133 ) ) ;
#19303=DIRECTION ( 'NONE',  ( 1.822029033848725028E-16, 0.000000000000000000, 1.000000000000000000 ) ) ;
#19305=EDGE_CURVE ( 'NONE', #22696, #25448, #636, .T. ) ;
#19307=CARTESIAN_POINT ( 'NONE',  ( -0.7495606340400177148, -0.1264236179284866091, 0.1697834645131657827 ) ) ;
#19308=CARTESIAN_POINT ( 'NONE',  ( -0.9873396505805591694, -0.1113553986120547346, 0.8710629921259842590 ) ) ;
#19311=CARTESIAN_POINT ( 'NONE',  ( -0.8759842519685039353, 0.1574803149606299191, 1.938976377845228249 ) ) ;
#19312=CARTESIAN_POINT ( 'NONE',  ( -0.8107537697050253289, -0.1574803149606297803, 1.562499999892472458 ) ) ;
#19313=CARTESIAN_POINT ( 'NONE',  ( 0.8019270111902717657, 0.1787899950787401604, 0.8661417322297003674 ) ) ;
#19314=ADVANCED_FACE ( 'NONE', ( #11145 ), #44876, .T. ) ;
#19315=EDGE_CURVE ( 'NONE', #38268, #8361, #15371, .T. ) ;
#19316=CARTESIAN_POINT ( 'NONE',  ( -0.8759842519685039353, 0.1574803149606299191, 0.4527559055118110520 ) ) ;
#19317=CARTESIAN_POINT ( 'NONE',  ( 0.9873396505805591694, 0.1113553986120547346, 1.628937007874015963 ) ) ;
#19318=CARTESIAN_POINT ( 'NONE',  ( 0.7145608061145479750, -0.04467186410878862257, 1.984103321452833191 ) ) ;
#19324=CARTESIAN_POINT ( 'NONE',  ( 0.8759842519685039353, -0.1787899950787401882, 0.8784448818360000022 ) ) ;
#19326=CARTESIAN_POINT ( 'NONE',  ( 0.8759842519685039353, -0.1787899950787401882, 1.828248031442299082 ) ) ;
#19329=AXIS2_PLACEMENT_3D ( 'NONE', #45235, #44123, #36947 ) ;
#19331=CARTESIAN_POINT ( 'NONE',  ( -0.7185039370078746268, 0.06523048226347956391, 0.05659448808144944970 ) ) ;
#19332=CARTESIAN_POINT ( 'NONE',  ( 1.054774247047244096, 0.000000000000000000, 1.163877952702141672 ) ) ;
#19337=CARTESIAN_POINT ( 'NONE',  ( -1.054774247047244540, -0.07405724077823318263, 0.2952755904974176393 ) ) ;
#19338=VECTOR ( 'NONE', #26290, 39.37007874015748143 ) ;
#19341=CARTESIAN_POINT ( 'NONE',  ( -0.8759842519685039353, 0.1787899950787401882, 1.803641732229700700 ) ) ;
#19342=CARTESIAN_POINT ( 'NONE',  ( -1.002407869896990045, -0.1264236179284866091, 0.9227362204186770889 ) ) ;
#19343=CARTESIAN_POINT ( 'NONE',  ( -1.054774247047244096, 0.000000000000000000, 0.5388779527021417826 ) ) ;
#19349=CARTESIAN_POINT ( 'NONE',  ( -0.7185039370078739607, 0.000000000000000000, -2.869337061179095023E-17 ) ) ;
#19350=CARTESIAN_POINT ( 'NONE',  ( -1.054774247047244096, 0.000000000000000000, 0.4945866141194645849 ) ) ;
#19353=ORIENTED_EDGE ( 'NONE', *, *, #34189, .T. ) ;
#19355=CARTESIAN_POINT ( 'NONE',  ( -1.054774247047244096, 0.000000000000000000, 1.562499999946236118 ) ) ;
#19360=EDGE_CURVE ( 'NONE', #955, #43835, #29633, .T. ) ;
#19363=CARTESIAN_POINT ( 'NONE',  ( -0.7185039370078739607, 1.928577636452523993E-17, 1.801181102362204633 ) ) ;
#19364=CARTESIAN_POINT ( 'NONE',  ( -1.033464566929134687, 0.06523048226347956391, 1.026082677057828185 ) ) ;
#19365=CARTESIAN_POINT ( 'NONE',  ( 0.8019270111902717657, 0.1787899950787401604, 0.5511811023084406402 ) ) ;
#19366=CARTESIAN_POINT ( 'NONE',  ( 0.8019270111902716547, -0.1787899950787401604, 0.08858267711159095725 ) ) ;
#19368=CARTESIAN_POINT ( 'NONE',  ( 1.033464566929134687, -0.06523048226347956391, 0.3617125984251969295 ) ) ;
#19370=CARTESIAN_POINT ( 'NONE',  ( 0.8759842519685039353, 0.1574803149606299191, 1.978346456585385882 ) ) ;
#19374=CARTESIAN_POINT ( 'NONE',  ( -1.002407869896990045, 0.1264236179284866091, 1.094980314906866203 ) ) ;
#19375=CARTESIAN_POINT ( 'NONE',  ( 0.9873396505805591694, -0.1113553986120547346, 0.9498031496062993018 ) ) ;
#19376=CARTESIAN_POINT ( 'NONE',  ( -1.033464566929133799, 1.928577636452524610E-17, 2.869337061179095023E-17 ) ) ;
#19382=LINE ( 'NONE', #12213, #42091 ) ;
#19383=CARTESIAN_POINT ( 'NONE',  ( 0.8019270111902717657, -0.1787899950787401604, 0.6791338582139527791 ) ) ;
#19384=CARTESIAN_POINT ( 'NONE',  ( -1.033464566929134687, -0.06523048226347956391, 1.109744094488189115 ) ) ;
#19386=CARTESIAN_POINT ( 'NONE',  ( -1.033464566929133799, 1.928577636452524610E-17, 2.869337061179095023E-17 ) ) ;
#19392=CARTESIAN_POINT ( 'NONE',  ( 0.8759842519685039353, -0.1574803149606299191, 1.053149606191685184 ) ) ;
#19396=CARTESIAN_POINT ( 'NONE',  ( -0.8019270111902717657, -0.1787899950787401604, 1.786417322780882388 ) ) ;
#19397=CARTESIAN_POINT ( 'NONE',  ( 1.054774247047244096, 0.000000000000000000, 1.719980314906866203 ) ) ;
#19398=ORIENTED_EDGE ( 'NONE', *, *, #32638, .F. ) ;
#19401=CARTESIAN_POINT ( 'NONE',  ( 1.054774247047244540, -0.07405724077823318263, 0.3789370078202520253 ) ) ;
#19402=CARTESIAN_POINT ( 'NONE',  ( -1.054774247047244096, 0.000000000000000000, 1.439468503883244210 ) ) ;
#19403=CARTESIAN_POINT ( 'NONE',  ( -0.7185039370078739607, 0.000000000000000000, -2.869337061179095023E-17 ) ) ;
#19404=CARTESIAN_POINT ( 'NONE',  ( -1.054774247047244540, 0.07405724077823318263, 1.205708661363558365 ) ) ;
#19406=CARTESIAN_POINT ( 'NONE',  ( -0.7495606340400177148, 0.1264236179284866091, 1.695374015694267822 ) ) ;
#19407=CARTESIAN_POINT ( 'NONE',  ( -0.6971942568897626646, -0.07405724077823297447, 0.1279527558517483676 ) ) ;
#19408=DIRECTION ( 'NONE',  ( -1.000000000000000000, 0.000000000000000000, 6.938893903907228378E-15 ) ) ;
#19409=CARTESIAN_POINT ( 'NONE',  ( -0.8759842519685039353, 0.1574803149606299191, 1.633858267716535639 ) ) ;
#19411=CARTESIAN_POINT ( 'NONE',  ( 0.8759842519685039353, 0.1787899950787401882, 1.611712598371433103 ) ) ;
#19413=CARTESIAN_POINT ( 'NONE',  ( 0.8107537697050254399, -0.1574803149606297803, 1.011318897530268712 ) ) ;
#19414=CARTESIAN_POINT ( 'NONE',  ( -0.8107537697050254399, 0.1574803149606300301, 1.793799212598424342 ) ) ;
#19422=CARTESIAN_POINT ( 'NONE',  ( -0.8759842519685039353, 0.1574803149606299191, 1.279527559055118280 ) ) ;
#19427=ADVANCED_FACE ( 'NONE', ( #41268 ), #45357, .T. ) ;
#19428=CARTESIAN_POINT ( 'NONE',  ( -0.9873396505805591694, 0.1113553986120547346, 0.1328740157480315098 ) ) ;
#19429=CARTESIAN_POINT ( 'NONE',  ( 0.7495606340400177148, -0.1264236179284866091, 0.7947834645131652831 ) ) ;
#19430=FACE_OUTER_BOUND ( 'NONE', #43663, .T. ) ;
#19433=CARTESIAN_POINT ( 'NONE',  ( 1.002407869896990045, 0.1264236179284866091, 1.882381889710015743 ) ) ;
#19434=ORIENTED_EDGE ( 'NONE', *, *, #13985, .T. ) ;
#19435=CARTESIAN_POINT ( 'NONE',  ( 0.9412147342319837628, -0.1574803149606297803, 0.1599409448818898405 ) ) ;
#19440=CARTESIAN_POINT ( 'NONE',  ( 0.6971942568897637749, 2.189545951927499583E-17, 0.2829724408911185041 ) ) ;
#19441=CARTESIAN_POINT ( 'NONE',  ( -0.8759842519685039353, 0.1787899950787401882, 1.685531496009228469 ) ) ;
#19443=CARTESIAN_POINT ( 'NONE',  ( -1.002407869896990045, -0.1264236179284866091, 1.281988188922614125 ) ) ;
#19445=CARTESIAN_POINT ( 'NONE',  ( 1.054774247047244540, 0.07405724077823318263, 1.289370078686393750 ) ) ;
#19446=CARTESIAN_POINT ( 'NONE',  ( -0.8759842519685039353, 0.1787899950787401882, 1.213090551127338435 ) ) ;
#19447=CYLINDRICAL_SURFACE ( 'NONE', #3860, 0.1574803149606299191 ) ;
#19450=CARTESIAN_POINT ( 'NONE',  ( 0.8759842519685039353, 0.1787899950787401882, 0.3912401574265515491 ) ) ;
#19451=CARTESIAN_POINT ( 'NONE',  ( -0.7495606340400177148, 0.1264236179284866091, 0.3518700786863940833 ) ) ;
#19452=ORIENTED_EDGE ( 'NONE', *, *, #34771, .F. ) ;
#19453=EDGE_CURVE ( 'NONE', #40844, #10631, #34695, .T. ) ;
#19454=CARTESIAN_POINT ( 'NONE',  ( -0.8759842519685039353, 0.000000000000000000, 0.000000000000000000 ) ) ;
#19455=EDGE_LOOP ( 'NONE', ( #10206, #43679, #30583, #23957 ) ) ;
#19456=CARTESIAN_POINT ( 'NONE',  ( -0.8107537697050234415, -0.1574803149606297803, 0.2337598425196852070 ) ) ;
#19457=CARTESIAN_POINT ( 'NONE',  ( 0.8759842519685039353, 0.1787899950787401882, 1.218011810969858111 ) ) ;
#19458=CARTESIAN_POINT ( 'NONE',  ( 0.9873396505805591694, 0.1113553986120547346, 1.934055118002708573 ) ) ;
#19463=CARTESIAN_POINT ( 'NONE',  ( -0.6971942568897637749, 2.189545951927499583E-17, 0.8735236219934803259 ) ) ;
#19465=CARTESIAN_POINT ( 'NONE',  ( -0.7495606340400177148, 0.1264236179284866091, 0.03690944876513417572 ) ) ;
#19471=CARTESIAN_POINT ( 'NONE',  ( 1.033464566929133799, 0.000000000000000000, 1.309055118110236338 ) ) ;
#19474=CYLINDRICAL_SURFACE ( 'NONE', #35356, 0.1574803149606299191 ) ;
#19477=CARTESIAN_POINT ( 'NONE',  ( 0.8019270111902717657, -0.1787899950787401604, 1.584645669237574994 ) ) ;
#19484=CARTESIAN_POINT ( 'NONE',  ( -0.8019270111902716547, 0.1787899950787401604, 0.7086614172690703928 ) ) ;
#19485=CARTESIAN_POINT ( 'NONE',  ( -0.7185039370078766252, -0.06523048226348168721, 1.281988188868851353 ) ) ;
#19487=CARTESIAN_POINT ( 'NONE',  ( -1.033464566929133799, 0.000000000000000000, 1.614173228238929170 ) ) ;
#19489=CYLINDRICAL_SURFACE ( 'NONE', #16440, 0.1574803149606299191 ) ;
#19493=CARTESIAN_POINT ( 'NONE',  ( 1.002407869896990045, -0.1264236179284866091, 1.400098425143086800 ) ) ;
#19494=CARTESIAN_POINT ( 'NONE',  ( 0.8759842519685039353, -0.1787899950787401882, 1.823326771599779406 ) ) ;
#19496=ORIENTED_EDGE ( 'NONE', *, *, #17197, .F. ) ;
#19497=CARTESIAN_POINT ( 'NONE',  ( -1.033464566929133799, 1.928577636452524610E-17, 2.869337061179095023E-17 ) ) ;
#19498=ORIENTED_EDGE ( 'NONE', *, *, #45633, .T. ) ;
#19499=CARTESIAN_POINT ( 'NONE',  ( -0.7646288533564489232, -0.1113553986120547346, 1.441929133750740277 ) ) ;
#19502=CARTESIAN_POINT ( 'NONE',  ( 0.8019270111902717657, -0.1787899950787401604, 0.3248031495525355306 ) ) ;
#19503=CARTESIAN_POINT ( 'NONE',  ( -0.9412147342319837628, -0.1574803149606297803, 0.7504921259842517456 ) ) ;
#19506=CARTESIAN_POINT ( 'NONE',  ( 0.8759842519685039353, 0.1574803149606299191, 0.8759842518609765039 ) ) ;
#19508=CARTESIAN_POINT ( 'NONE',  ( 1.033464566929134687, 0.06523048226347956391, 0.6815944881889761664 ) ) ;
#19512=VERTEX_POINT ( 'NONE', #31251 ) ;
#19513=CARTESIAN_POINT ( 'NONE',  ( 0.8019270111902717657, 0.1787899950787401604, 1.609251968450173376 ) ) ;
#19514=CARTESIAN_POINT ( 'NONE',  ( -0.7185039370078746268, 0.06523048226347956391, 1.247539370078740273 ) ) ;
#19515=CARTESIAN_POINT ( 'NONE',  ( 0.9412147342319837628, 0.1574803149606300301, 0.2436023620971973780 ) ) ;
#19517=CARTESIAN_POINT ( 'NONE',  ( -0.7185039370078746268, -0.06523048226347956391, 0.4256889763779528879 ) ) ;
#19518=CARTESIAN_POINT ( 'NONE',  ( 0.9873396505805591694, 0.1113553986120547346, 0.3592519683964098820 ) ) ;
#19519=ORIENTED_EDGE ( 'NONE', *, *, #44927, .F. ) ;
#19520=ORIENTED_EDGE ( 'NONE', *, *, #14798, .F. ) ;
#19522=ORIENTED_EDGE ( 'NONE', *, *, #4131, .F. ) ;
#19523=CARTESIAN_POINT ( 'NONE',  ( -1.054774247047244540, 0.07405724077823318263, 1.560039370024976835 ) ) ;
#19525=CARTESIAN_POINT ( 'NONE',  ( -1.054774247047244540, 0.07405724077823318263, 1.249999999946235896 ) ) ;
#19528=CARTESIAN_POINT ( 'NONE',  ( -1.054774247047244540, -0.07405724077823318263, 0.3395669290800945039 ) ) ;
#19533=VERTEX_POINT ( 'NONE', #38181 ) ;
#19536=EDGE_CURVE ( 'NONE', #20455, #1520, #9438, .T. ) ;
#19540=CARTESIAN_POINT ( 'NONE',  ( 0.8759842519685039353, -0.1574803149606299191, 0.1082677164279060994 ) ) ;
#19541=( BOUNDED_CURVE ( )  B_SPLINE_CURVE ( 2, ( #13721, #35072, #17078, #24512, #28358, #39109, #10137, #13960, #6521 ),
 .UNSPECIFIED., .F., .T. ) 
 B_SPLINE_CURVE_WITH_KNOTS ( ( 3, 2, 2, 2, 3 ),
 ( 0.9100000000000000311, 0.9124999999999999778, 0.9150000000000000355, 0.9174999999999999822, 0.9200000000000000400 ),
 .UNSPECIFIED. ) 
 CURVE ( )  GEOMETRIC_REPRESENTATION_ITEM ( )  RATIONAL_B_SPLINE_CURVE ( ( 1.000000000000000000, 0.9238795325112869605, 1.000000000000000000, 0.9238795325112869605, 1.000000000000000000, 0.9238795325112869605, 1.000000000000000000, 0.9238795325112869605, 1.000000000000000000 ) ) 
 REPRESENTATION_ITEM ( '' )  ) ;
#19542=DIRECTION ( 'NONE',  ( 1.822029033848725028E-16, 0.000000000000000000, 1.000000000000000000 ) ) ;
#19544=EDGE_CURVE ( 'NONE', #11565, #13693, #9188, .T. ) ;
#19545=CARTESIAN_POINT ( 'NONE',  ( -0.8759842519685039353, -0.1787899950787401882, 0.2534448818360003908 ) ) ;
#19546=CARTESIAN_POINT ( 'NONE',  ( -1.033464566929134687, 0.06523048226347956391, 0.8784448818897642175 ) ) ;
#19549=DIRECTION ( 'NONE',  ( 0.000000000000000000, 0.000000000000000000, -1.000000000000000000 ) ) ;
#19550=CARTESIAN_POINT ( 'NONE',  ( 0.9500414927467378812, -0.1787899950787401604, 0.8464566928596233275 ) ) ;
#19551=AXIS2_PLACEMENT_3D ( 'NONE', #24130, #35384, #2529 ) ;
#19553=CARTESIAN_POINT ( 'NONE',  ( 0.8107537697050253289, -0.1574803149606297803, 1.572342519685040685 ) ) ;
#19554=CARTESIAN_POINT ( 'NONE',  ( 0.7500335542904545960, 0.1023885596843875229, 1.981118523551024468 ) ) ;
#19556=CARTESIAN_POINT ( 'NONE',  ( 1.033464566929134687, -0.06523048226347956391, 0.4699803148531029873 ) ) ;
#19558=( BOUNDED_CURVE ( )  B_SPLINE_CURVE ( 2, ( #13587, #2789, #46883, #2556, #46409, #5925, #34949, #6393, #27784 ),
 .UNSPECIFIED., .F., .F. ) 
 B_SPLINE_CURVE_WITH_KNOTS ( ( 3, 2, 2, 2, 3 ),
 ( 0.2399999999999999911, 0.2424999999999999933, 0.2449999999999999956, 0.2474999999999999978, 0.2500000000000000000 ),
 .UNSPECIFIED. ) 
 CURVE ( )  GEOMETRIC_REPRESENTATION_ITEM ( )  RATIONAL_B_SPLINE_CURVE ( ( 1.000000000000000000, 0.9238795325112869605, 1.000000000000000000, 0.9238795325112869605, 1.000000000000000000, 0.9238795325112869605, 1.000000000000000000, 0.9238795325112869605, 1.000000000000000000 ) ) 
 REPRESENTATION_ITEM ( '' )  ) ;
#19559=CARTESIAN_POINT ( 'NONE',  ( -0.9873396505805591694, 0.1113553986120547346, 1.550196850393700920 ) ) ;
#19560=CARTESIAN_POINT ( 'NONE',  ( 1.054774247047244096, 0.000000000000000000, 0.9276574802611967652 ) ) ;
#19562=CARTESIAN_POINT ( 'NONE',  ( 1.002407869896990045, -0.1264236179284866091, 1.872539370024976391 ) ) ;
#19564=VERTEX_POINT ( 'NONE', #34850 ) ;
#19565=CARTESIAN_POINT ( 'NONE',  ( -1.033464566929134687, 0.06523048226347956391, 0.8390748031496062520 ) ) ;
#19567=VECTOR ( 'NONE', #40427, 39.37007874015748143 ) ;
#19570=CARTESIAN_POINT ( 'NONE',  ( -0.8107537697050234415, -0.1574803149606297803, 0.1058070865066461225 ) ) ;
#19572=CARTESIAN_POINT ( 'NONE',  ( 1.054774247047244096, 0.000000000000000000, 1.085137795221826629 ) ) ;
#19576=CARTESIAN_POINT ( 'NONE',  ( -0.7495606340400177148, 0.1264236179284866091, 0.5093503936470236138 ) ) ;
#19577=CARTESIAN_POINT ( 'NONE',  ( 1.033464566929133799, 0.000000000000000000, 0.2460629921259842590 ) ) ;
#19578=CARTESIAN_POINT ( 'NONE',  ( -1.002407869896990045, -0.1264236179284866091, 0.1747047243556852092 ) ) ;
#19581=CARTESIAN_POINT ( 'NONE',  ( -0.8759842519685039353, 0.1787899950787401882, 1.843011810969858333 ) ) ;
#19583=CARTESIAN_POINT ( 'NONE',  ( -1.054774247047244540, 0.07405724077823318263, 0.8907480314422985268 ) ) ;
#19584=CARTESIAN_POINT ( 'NONE',  ( -0.8759842519685039353, 0.1787899950787401882, 0.5093503936470236138 ) ) ;
#19592=DIRECTION ( 'NONE',  ( 0.000000000000000000, 0.000000000000000000, -1.000000000000000000 ) ) ;
#19595=CARTESIAN_POINT ( 'NONE',  ( 0.7185039370078739607, 0.000000000000000000, 4.498031496062992574 ) ) ;
#19596=CARTESIAN_POINT ( 'NONE',  ( -0.6971942568897626646, -0.07405724077823297447, 0.3986220471903312301 ) ) ;
#19602=SURFACE_STYLE_USAGE ( .BOTH. , #41140 ) ;
#19604=CARTESIAN_POINT ( 'NONE',  ( 0.8759842519685039353, 0.1574803149606299191, 0.4527559055118110520 ) ) ;
#19605=CARTESIAN_POINT ( 'NONE',  ( 0.5314960629921260393, 0.000000000000000000, 4.498031496062992574 ) ) ;
#19606=CARTESIAN_POINT ( 'NONE',  ( -0.7185039370078746268, -0.06523048226347956391, 1.281988188868851575 ) ) ;
#19607=CARTESIAN_POINT ( 'NONE',  ( 0.9500414927467378812, -0.1787899950787401604, 0.4921259841982048577 ) ) ;
#19608=CARTESIAN_POINT ( 'NONE',  ( 1.002407869896990045, -0.1264236179284866091, 0.05659448813521283234 ) ) ;
#19611=CARTESIAN_POINT ( 'NONE',  ( 0.7185039370078739607, 1.928577636452523993E-17, 0.3346456691838114450 ) ) ;
#19614=CARTESIAN_POINT ( 'NONE',  ( 1.033464566929133799, 0.000000000000000000, 1.112204724409448842 ) ) ;
#19617=CARTESIAN_POINT ( 'NONE',  ( -0.7646288533564489232, -0.1113553986120547346, 1.254921259842519676 ) ) ;
#19621=CARTESIAN_POINT ( 'NONE',  ( 0.7185039370078739607, 1.928577636452523993E-17, 0.05905511800270921846 ) ) ;
#19622=CARTESIAN_POINT ( 'NONE',  ( 0.7646288533564489232, -0.1113553986120547346, 0.2706692913385826960 ) ) ;
#19623=CARTESIAN_POINT ( 'NONE',  ( 0.6971942568897626646, 0.07405724077823318263, 0.7480314960092282472 ) ) ;
#19625=CARTESIAN_POINT ( 'NONE',  ( 0.7646288533564489232, -0.1113553986120547346, 0.8218503937007874960 ) ) ;
#19626=LINE ( 'NONE', #4506, #21981 ) ;
#19629=CARTESIAN_POINT ( 'NONE',  ( 0.9412147342319837628, -0.1574803149606297803, 1.055610236112945799 ) ) ;
#19631=CARTESIAN_POINT ( 'NONE',  ( -0.6971942568897626646, 0.07405724077823318263, 0.4724409448281262636 ) ) ;
#19632=ORIENTED_EDGE ( 'NONE', *, *, #14732, .T. ) ;
#19634=CARTESIAN_POINT ( 'NONE',  ( -0.6971942568897648851, -0.07405724077823297447, 1.820866141678520789 ) ) ;
#19635=CARTESIAN_POINT ( 'NONE',  ( 0.6971942568897648851, -0.07405724077823297447, 1.860236220418677089 ) ) ;
#19638=CARTESIAN_POINT ( 'NONE',  ( 0.7185039370078746268, -0.06523048226347956391, 1.764271653543307616 ) ) ;
#19639=CARTESIAN_POINT ( 'NONE',  ( 0.8019270111902717657, 0.1787899950787401604, 0.4330708660879683536 ) ) ;
#19640=CARTESIAN_POINT ( 'NONE',  ( -0.8019270111902717657, 0.1787899950787401604, 1.373031496009229135 ) ) ;
#19641=CARTESIAN_POINT ( 'NONE',  ( 1.033464566929133799, 0.000000000000000000, 1.968503936900346529 ) ) ;
#19642=CARTESIAN_POINT ( 'NONE',  ( -0.8759842519685039353, -0.1787899950787401882, 1.390255905458047447 ) ) ;
#19644=CARTESIAN_POINT ( 'NONE',  ( -0.9500414927467378812, -0.1787899950787401604, 0.8809055117572599514 ) ) ;
#19645=CARTESIAN_POINT ( 'NONE',  ( -1.054774247047244096, 0.000000000000000000, 0.06643700782025216411 ) ) ;
#19647=CARTESIAN_POINT ( 'NONE',  ( -0.8019270111902717657, 0.1787899950787401604, 1.692913385773008539 ) ) ;
#19648=CARTESIAN_POINT ( 'NONE',  ( -0.9412147342319837628, 0.1574803149606300301, 1.975885826664125711 ) ) ;
#19650=CARTESIAN_POINT ( 'NONE',  ( -1.033464566929134687, 0.06523048226347956391, 1.823326771653542178 ) ) ;
#19651=CARTESIAN_POINT ( 'NONE',  ( -0.9412147342319837628, 0.1574803149606300301, 0.2928149606299214613 ) ) ;
#19652=CARTESIAN_POINT ( 'NONE',  ( 1.054774247047244096, 0.000000000000000000, 1.562499999946236118 ) ) ;
#19654=CARTESIAN_POINT ( 'NONE',  ( 0.7185039370078746268, 0.06523048226347956391, 0.2140748030420794590 ) ) ;
#19661=CARTESIAN_POINT ( 'NONE',  ( -0.7646288533564489232, -0.1113553986120547346, 0.5856299212598424786 ) ) ;
#19662=CARTESIAN_POINT ( 'NONE',  ( 0.6971942568897637749, 2.189545951927499583E-17, 1.813484251914740053 ) ) ;
#19663=CARTESIAN_POINT ( 'NONE',  ( 0.8759842519685039353, 0.1787899950787401882, 0.3863188975840318173 ) ) ;
#19668=CARTESIAN_POINT ( 'NONE',  ( -0.8107537697050254399, 0.1574803149606300301, 0.1402559055118110520 ) ) ;
#19669=CARTESIAN_POINT ( 'NONE',  ( 0.8019270111902717657, -0.1787899950787401604, 0.9940944881352130613 ) ) ;
#19670=( BOUNDED_CURVE ( )  B_SPLINE_CURVE ( 2, ( #6705, #21318, #19625, #26121, #15334, #5005, #12216, #33808, #4760 ),
 .UNSPECIFIED., .F., .T. ) 
 B_SPLINE_CURVE_WITH_KNOTS ( ( 3, 2, 2, 2, 3 ),
 ( 0.4099999999999999756, 0.4124999999999999778, 0.4149999999999999800, 0.4174999999999999822, 0.4199999999999999845 ),
 .UNSPECIFIED. ) 
 CURVE ( )  GEOMETRIC_REPRESENTATION_ITEM ( )  RATIONAL_B_SPLINE_CURVE ( ( 1.000000000000000000, 0.9238795325112879597, 1.000000000000000000, 0.9238795325112869605, 1.000000000000000000, 0.9238795325112869605, 1.000000000000000000, 0.9238795325112869605, 1.000000000000000000 ) ) 
 REPRESENTATION_ITEM ( '' )  ) ;
#19672=CARTESIAN_POINT ( 'NONE',  ( 1.002407869896990045, 0.1264236179284866091, 1.921751968450173376 ) ) ;
#19673=DIRECTION ( 'NONE',  ( 1.822029033848725028E-16, 0.000000000000000000, 1.000000000000000000 ) ) ;
#19678=CARTESIAN_POINT ( 'NONE',  ( 0.6971942568897626646, 0.07405724077823318263, 0.3198818897100162983 ) ) ;
#19679=CARTESIAN_POINT ( 'NONE',  ( -0.6971942568897648851, 0.07405724077823318263, 1.732283464513166615 ) ) ;
#19680=EDGE_LOOP ( 'NONE', ( #36907, #34860, #42248, #33722 ) ) ;
#19681=CARTESIAN_POINT ( 'NONE',  ( -1.054774247047244096, 0.000000000000000000, 1.365649606245448844 ) ) ;
#19682=CARTESIAN_POINT ( 'NONE',  ( -1.033464566929134687, 0.06523048226347956391, 1.311515748031496509 ) ) ;
#19683=CARTESIAN_POINT ( 'NONE',  ( -0.6971942568897637749, 2.189545951927499583E-17, 1.144192913332062966 ) ) ;
#19687=CARTESIAN_POINT ( 'NONE',  ( 1.054774247047244540, 0.07405724077823318263, 0.5019685038832443214 ) ) ;
#19688=CARTESIAN_POINT ( 'NONE',  ( -0.7495606340400177148, 0.1264236179284866091, 0.3124999999462365619 ) ) ;
#19695=CARTESIAN_POINT ( 'NONE',  ( -0.8107537697050234415, -0.1574803149606297803, 0.3125000000000000000 ) ) ;
#19696=CARTESIAN_POINT ( 'NONE',  ( 0.8019270111902716547, 0.1787899950787401604, 1.181102362150960428 ) ) ;
#19697=CARTESIAN_POINT ( 'NONE',  ( -0.6971942568897648851, 0.07405724077823318263, 1.968503936954110412 ) ) ;
#19701=CARTESIAN_POINT ( 'NONE',  ( -1.002407869896990045, -0.1264236179284866091, 1.006397637741511808 ) ) ;
#19702=CARTESIAN_POINT ( 'NONE',  ( -1.033464566929134687, -0.06523048226347956391, 0.3223425196850392971 ) ) ;
#19707=CARTESIAN_POINT ( 'NONE',  ( -0.7185039370078739607, 1.928577636452523993E-17, 1.397637795168062969 ) ) ;
#19712=CARTESIAN_POINT ( 'NONE',  ( 0.7646288533564489232, -0.1113553986120547346, 0.7332677164279054471 ) ) ;
#19713=AXIS2_PLACEMENT_3D ( 'NONE', #23950, #2348, #16981 ) ;
#19714=CARTESIAN_POINT ( 'NONE',  ( -1.033464566929134687, 0.06523048226347956391, 1.429625984251967852 ) ) ;
#19715=CARTESIAN_POINT ( 'NONE',  ( 0.8019270111902717657, 0.1787899950787401604, 1.648622047190331230 ) ) ;
#19720=CARTESIAN_POINT ( 'NONE',  ( -1.054774247047244540, -0.07405724077823318263, 0.5757874015210393548 ) ) ;
#19724=CYLINDRICAL_SURFACE ( 'NONE', #5718, 0.1574803149606299191 ) ;
#19725=CARTESIAN_POINT ( 'NONE',  ( -0.7185039370078739607, 0.000000000000000000, -2.869337061179095023E-17 ) ) ;
#19726=CARTESIAN_POINT ( 'NONE',  ( 0.9500414927467378812, -0.1787899950787401604, 1.476377952702141449 ) ) ;
#19727=CARTESIAN_POINT ( 'NONE',  ( 1.054774247047244540, -0.07405724077823318263, 1.830708661363559253 ) ) ;
#19728=CARTESIAN_POINT ( 'NONE',  ( 0.8019270111902716547, 0.1787899950787401604, 0.2706692912848194243 ) ) ;
#19730=DIRECTION ( 'NONE',  ( 1.822029033848725028E-16, 0.000000000000000000, 1.000000000000000000 ) ) ;
#19732=CARTESIAN_POINT ( 'NONE',  ( -0.7397356941743765679, 0.08920912498191986562, 1.981439465340073536 ) ) ;
#19735=CARTESIAN_POINT ( 'NONE',  ( 0.8019270111902717657, -0.1787899950787401604, 0.4035433070328508509 ) ) ;
#19736=CARTESIAN_POINT ( 'NONE',  ( 0.8759842519685039353, 0.1787899950787401882, 1.291830708607653477 ) ) ;
#19737=CARTESIAN_POINT ( 'NONE',  ( 0.7185039370078739607, 1.928577636452523993E-17, 1.948818897530267602 ) ) ;
#19738=CARTESIAN_POINT ( 'NONE',  ( 0.7185039370078739607, 0.000000000000000000, 4.498031496062992574 ) ) ;
#19739=CARTESIAN_POINT ( 'NONE',  ( 0.9412147342319837628, 0.1574803149606300301, 0.2140748031496061965 ) ) ;
#19740=CARTESIAN_POINT ( 'NONE',  ( 0.9412147342319837628, -0.1574803149606297803, 0.7800196849318438153 ) ) ;
#19742=CARTESIAN_POINT ( 'NONE',  ( -0.6971942568897648851, -0.07405724077823297447, 1.072834645615528659 ) ) ;
#19748=CARTESIAN_POINT ( 'NONE',  ( -0.7646288533564489232, -0.1113553986120547346, 0.4970472439869613734 ) ) ;
#19749=CARTESIAN_POINT ( 'NONE',  ( -0.8107537697050254399, 0.1574803149606300301, 0.8095472440944886383 ) ) ;
#19750=CARTESIAN_POINT ( 'NONE',  ( 0.8759842519685039353, 0.1787899950787401882, 1.685531496009228469 ) ) ;
#19751=CARTESIAN_POINT ( 'NONE',  ( -0.7646288533564489232, -0.1113553986120547346, 1.294291338582677309 ) ) ;
#19752=CARTESIAN_POINT ( 'NONE',  ( -0.9412147342319837628, -0.1574803149606297803, 1.055610236112945577 ) ) ;
#19753=CARTESIAN_POINT ( 'NONE',  ( 0.8759842519685039353, 0.000000000000000000, 4.498031496062992574 ) ) ;
#19754=CARTESIAN_POINT ( 'NONE',  ( 0.8107537697050254399, 0.1574803149606300301, 1.951279527559056870 ) ) ;
#19755=CARTESIAN_POINT ( 'NONE',  ( 1.033464566929133799, 0.000000000000000000, 0.3543307085538902057 ) ) ;
#19758=CARTESIAN_POINT ( 'NONE',  ( 1.033464566929133799, 0.000000000000000000, 1.377952755797984263 ) ) ;
#19760=VERTEX_POINT ( 'NONE', #19621 ) ;
#19763=CARTESIAN_POINT ( 'NONE',  ( -1.054774247047244540, -0.07405724077823318263, 1.515748031442299526 ) ) ;
#19765=CARTESIAN_POINT ( 'NONE',  ( -0.7495606340400177148, -0.1264236179284866091, 1.390255905458047447 ) ) ;
#19767=EDGE_LOOP ( 'NONE', ( #17913, #24417, #21784, #450 ) ) ;
#19769=CARTESIAN_POINT ( 'NONE',  ( -0.7185039370078739607, 1.928577636452523993E-17, 1.870078740049952559 ) ) ;
#19774=VERTEX_POINT ( 'NONE', #11496 ) ;
#19776=CARTESIAN_POINT ( 'NONE',  ( 0.8107537697050234415, -0.1574803149606297803, 0.1058070865066461363 ) ) ;
#19780=CARTESIAN_POINT ( 'NONE',  ( -0.8759842519685039353, 0.1574803149606299191, 1.082677165354330784 ) ) ;
#19782=CARTESIAN_POINT ( 'NONE',  ( 0.8019270111902717657, 0.1787899950787401604, 0.9055118109698585549 ) ) ;
#19783=CARTESIAN_POINT ( 'NONE',  ( 1.054774247047244096, 0.000000000000000000, 1.400098425143086800 ) ) ;
#19784=CARTESIAN_POINT ( 'NONE',  ( 0.9500414927467377701, -0.1787899950787401604, 0.1328740156942679884 ) ) ;
#19785=DIRECTION ( 'NONE',  ( 1.000000000000000000, 0.000000000000000000, -1.822029033848725275E-16 ) ) ;
#19786=CARTESIAN_POINT ( 'NONE',  ( 1.033464566929134687, 0.06523048226347956391, 1.587106299212598826 ) ) ;
#19788=DIRECTION ( 'NONE',  ( -1.000000000000000000, 0.000000000000000000, 0.000000000000000000 ) ) ;
#19792=CARTESIAN_POINT ( 'NONE',  ( 0.7495606340400177148, -0.1264236179284866091, 0.9128937007336377363 ) ) ;
#19793=CARTESIAN_POINT ( 'NONE',  ( 0.6971942568897648851, 0.07405724077823318263, 1.894685039316315489 ) ) ;
#19794=CARTESIAN_POINT ( 'NONE',  ( 0.7185039370078746268, 0.06523048226347956391, 0.2928149605223941965 ) ) ;
#19795=VERTEX_POINT ( 'NONE', #8839 ) ;
#19796=EDGE_CURVE ( 'NONE', #7898, #28992, #19382, .T. ) ;
#19798=CARTESIAN_POINT ( 'NONE',  ( 0.7185039370078766252, -0.06523048226348168721, 1.882381889763779625 ) ) ;
#19800=CARTESIAN_POINT ( 'NONE',  ( -0.8759842519685039353, -0.1574803149606299191, 0.1870078739082208508 ) ) ;
#19802=CARTESIAN_POINT ( 'NONE',  ( 0.8019270111902717657, -0.1787899950787401604, 1.151574803095843036 ) ) ;
#19806=CARTESIAN_POINT ( 'NONE',  ( -0.8759842519685039353, 0.000000000000000000, 0.000000000000000000 ) ) ;
#19808=CARTESIAN_POINT ( 'NONE',  ( -1.054774247047244096, 0.000000000000000000, 0.5733267715997795166 ) ) ;
#19809=CYLINDRICAL_SURFACE ( 'NONE', #12250, 0.1574803149606299191 ) ;
#19811=ORIENTED_EDGE ( 'NONE', *, *, #22, .F. ) ;
#19812=DIRECTION ( 'NONE',  ( 1.000000000000000000, 0.000000000000000000, -1.822029033848725275E-16 ) ) ;
#19815=CARTESIAN_POINT ( 'NONE',  ( -0.8759842519685039353, -0.1787899950787401882, 1.823326771599779406 ) ) ;
#19816=ORIENTED_EDGE ( 'NONE', *, *, #39271, .T. ) ;
#19817=AXIS2_PLACEMENT_3D ( 'NONE', #2309, #6619, #35404 ) ;
#19818=CARTESIAN_POINT ( 'NONE',  ( -1.002407869896990045, 0.1264236179284866091, 0.5831692912848189803 ) ) ;
#19827=CARTESIAN_POINT ( 'NONE',  ( -0.7495606340400177148, 0.1264236179284866091, 0.5093503936470236138 ) ) ;
#19831=CARTESIAN_POINT ( 'NONE',  ( -0.8019270111902716547, -0.1787899950787401604, 1.471456692859622217 ) ) ;
#19834=( BOUNDED_CURVE ( )  B_SPLINE_CURVE ( 2, ( #9644, #24262, #42206, #38156, #31458, #46042, #23319, #34121, #9164 ),
 .UNSPECIFIED., .F., .T. ) 
 B_SPLINE_CURVE_WITH_KNOTS ( ( 3, 2, 2, 2, 3 ),
 ( 0.5000000000000000000, 0.5024999999999999467, 0.5050000000000000044, 0.5074999999999999512, 0.5100000000000000089 ),
 .UNSPECIFIED. ) 
 CURVE ( )  GEOMETRIC_REPRESENTATION_ITEM ( )  RATIONAL_B_SPLINE_CURVE ( ( 1.000000000000000000, 0.9238795325112869605, 1.000000000000000000, 0.9238795325112869605, 1.000000000000000000, 0.9238795325112869605, 1.000000000000000000, 0.9238795325112869605, 1.000000000000000000 ) ) 
 REPRESENTATION_ITEM ( '' )  ) ;
#19836=CARTESIAN_POINT ( 'NONE',  ( 0.7185039370078746268, -0.06523048226347956391, 0.1894685039370079815 ) ) ;
#19838=CARTESIAN_POINT ( 'NONE',  ( 0.9412147342319837628, 0.1574803149606300301, 0.4896653543307081802 ) ) ;
#19840=DIRECTION ( 'NONE',  ( 0.000000000000000000, 0.000000000000000000, -1.000000000000000000 ) ) ;
#19841=CARTESIAN_POINT ( 'NONE',  ( -0.9412147342319837628, 0.1574803149606300301, 1.306594488081449290 ) ) ;
#19842=CARTESIAN_POINT ( 'NONE',  ( 0.6971942568897637749, 2.189545951927499583E-17, 0.5191929133320630774 ) ) ;
#19845=LINE ( 'NONE', #9067, #42153 ) ;
#19846=VERTEX_POINT ( 'NONE', #5232 ) ;
#19849=CARTESIAN_POINT ( 'NONE',  ( -0.7495606340400177148, -0.1264236179284866091, 1.114665354276944909 ) ) ;
#19850=CARTESIAN_POINT ( 'NONE',  ( 0.9412147342319837628, -0.1574803149606297803, 1.104822834645670104 ) ) ;
#19855=CARTESIAN_POINT ( 'NONE',  ( 0.7185039370078778465, -0.06523048226348396317, 1.675688976270425457 ) ) ;
#19864=CARTESIAN_POINT ( 'NONE',  ( 0.7185039370078739607, 1.928577636452523993E-17, 1.200787401467275695 ) ) ;
#19865=CARTESIAN_POINT ( 'NONE',  ( -0.9873396505805591694, 0.1113553986120547346, 0.4379921258767244252 ) ) ;
#19869=CARTESIAN_POINT ( 'NONE',  ( 0.9412147342319837628, 0.1574803149606300301, 1.109744094380661572 ) ) ;
#19870=CARTESIAN_POINT ( 'NONE',  ( -1.033464566929133799, 0.000000000000000000, 1.850393700679873854 ) ) ;
#19871=ORIENTED_EDGE ( 'NONE', *, *, #37918, .F. ) ;
#19873=CARTESIAN_POINT ( 'NONE',  ( -0.9500414927467378812, -0.1787899950787401604, 1.830708661363559253 ) ) ;
#19874=ORIENTED_EDGE ( 'NONE', *, *, #45431, .T. ) ;
#19876=CARTESIAN_POINT ( 'NONE',  ( -1.054774247047244096, 0.000000000000000000, 1.321358267662771757 ) ) ;
#19878=CARTESIAN_POINT ( 'NONE',  ( -0.6971942568897626646, 0.07405724077823318263, 0.9055118109698585549 ) ) ;
#19879=CARTESIAN_POINT ( 'NONE',  ( -0.7495606340400177148, 0.1264236179284866091, 0.1205708660879689087 ) ) ;
#19881=CARTESIAN_POINT ( 'NONE',  ( -1.054774247047244096, 0.000000000000000000, 1.759350393647023614 ) ) ;
#19882=CARTESIAN_POINT ( 'NONE',  ( -0.9500414927467378812, -0.1787899950787401604, 0.05905511805647267048 ) ) ;
#19884=CARTESIAN_POINT ( 'NONE',  ( -0.7646288533564489232, 0.1113553986120547346, 1.756889763779527547 ) ) ;
#19886=CARTESIAN_POINT ( 'NONE',  ( 0.9500414927467377701, -0.1787899950787401604, 1.673228346402929834 ) ) ;
#19890=ORIENTED_EDGE ( 'NONE', *, *, #46956, .F. ) ;
#19893=CARTESIAN_POINT ( 'NONE',  ( -0.8759842519685039353, -0.1574803149606299191, 0.5905511811023621549 ) ) ;
#19897=CARTESIAN_POINT ( 'NONE',  ( -1.033464566929133799, 0.000000000000000000, 0.8267716534357796299 ) ) ;
#19901=CARTESIAN_POINT ( 'NONE',  ( 0.7495606340400177148, -0.1264236179284866091, 0.9128937007336377363 ) ) ;
#19902=EDGE_CURVE ( 'NONE', #3057, #11821, #12297, .T. ) ;
#19905=CARTESIAN_POINT ( 'NONE',  ( 0.8759842519685039353, 0.1787899950787401882, 1.966043307032850462 ) ) ;
#19906=EDGE_CURVE ( 'NONE', #3623, #38634, #20251, .T. ) ;
#19908=EDGE_CURVE ( 'NONE', #14505, #32389, #14807, .T. ) ;
#19909=CYLINDRICAL_SURFACE ( 'NONE', #31356, 0.1574803149606299191 ) ;
#19913=CARTESIAN_POINT ( 'NONE',  ( -0.9500414927467378812, 0.1787899950787401604, 1.722440944828125930 ) ) ;
#19914=ORIENTED_EDGE ( 'NONE', *, *, #36817, .F. ) ;
#19915=CARTESIAN_POINT ( 'NONE',  ( -1.054774247047244540, -0.07405724077823318263, 1.284448818843874740 ) ) ;
#19916=DIRECTION ( 'NONE',  ( 1.000000000000000000, 0.000000000000000000, -1.822029033848725275E-16 ) ) ;
#19917=CARTESIAN_POINT ( 'NONE',  ( 0.8019270111902717657, 0.1787899950787401604, 1.417322834591906222 ) ) ;
#19918=CARTESIAN_POINT ( 'NONE',  ( 0.9500414927467378812, 0.1787899950787401604, 0.07381889758403178958 ) ) ;
#19919=CARTESIAN_POINT ( 'NONE',  ( -0.8019270111902717657, -0.1787899950787401604, 1.269685039316314601 ) ) ;
#19921=CARTESIAN_POINT ( 'NONE',  ( -0.8107537697050254399, 0.1574803149606300301, 1.350885826664126821 ) ) ;
#19922=CARTESIAN_POINT ( 'NONE',  ( 0.8759842519685039353, 0.1787899950787401882, 0.6274606298674959559 ) ) ;
#19923=CARTESIAN_POINT ( 'NONE',  ( -1.054774247047244540, -0.07405724077823318263, 0.3346456692375752162 ) ) ;
#19925=CARTESIAN_POINT ( 'NONE',  ( 0.7185039370078739607, 1.928577636452523993E-17, 1.673228346349165285 ) ) ;
#19927=CARTESIAN_POINT ( 'NONE',  ( -0.9412147342319837628, 0.1574803149606300301, 0.2534448818897637734 ) ) ;
#19931=CARTESIAN_POINT ( 'NONE',  ( -0.7495606340400177148, -0.1264236179284866091, 0.9571850393163149340 ) ) ;
#19933=CARTESIAN_POINT ( 'NONE',  ( -1.002407869896990045, 0.1264236179284866091, 0.1058070865604098382 ) ) ;
#19935=ORIENTED_EDGE ( 'NONE', *, *, #29161, .T. ) ;
#19936=DIRECTION ( 'NONE',  ( -1.000000000000000000, 0.000000000000000000, 0.000000000000000000 ) ) ;
#19938=CARTESIAN_POINT ( 'NONE',  ( -0.9873396505805591694, -0.1113553986120547346, 0.08366141732283464971 ) ) ;
#19939=ORIENTED_EDGE ( 'NONE', *, *, #21733, .F. ) ;
#19940=CARTESIAN_POINT ( 'NONE',  ( 0.9500414927467378812, 0.1787899950787401604, 1.289370078686393750 ) ) ;
#19943=( BOUNDED_CURVE ( )  B_SPLINE_CURVE ( 2, ( #33535, #47420, #29724, #28330, #28105, #24490, #6256, #20882, #35524 ),
 .UNSPECIFIED., .F., .T. ) 
 B_SPLINE_CURVE_WITH_KNOTS ( ( 3, 2, 2, 2, 3 ),
 ( 0.8100000000000000533, 0.8125000000000000000, 0.8149999999999999467, 0.8175000000000000044, 0.8199999999999999512 ),
 .UNSPECIFIED. ) 
 CURVE ( )  GEOMETRIC_REPRESENTATION_ITEM ( )  RATIONAL_B_SPLINE_CURVE ( ( 1.000000000000000000, 0.9238795325112869605, 1.000000000000000000, 0.9238795325112869605, 1.000000000000000000, 0.9238795325112869605, 1.000000000000000000, 0.9238795325112829637, 1.000000000000000000 ) ) 
 REPRESENTATION_ITEM ( '' )  ) ;
#19944=CARTESIAN_POINT ( 'NONE',  ( 0.7646288533564489232, 0.1113553986120547346, 1.875000000000000000 ) ) ;
#19945=CARTESIAN_POINT ( 'NONE',  ( 0.8019270111902717657, 0.1787899950787401604, 1.609251968450173376 ) ) ;
#19949=CARTESIAN_POINT ( 'NONE',  ( 0.7495606340400177148, -0.1264236179284866091, 0.4798228345919055560 ) ) ;
#19951=CARTESIAN_POINT ( 'NONE',  ( -1.002407869896990045, -0.1264236179284866091, 0.7701771653005669016 ) ) ;
#19953=CYLINDRICAL_SURFACE ( 'NONE', #40779, 0.1574803149606299191 ) ;
#19955=CARTESIAN_POINT ( 'NONE',  ( -0.8391708915589655149, -0.1694580354647786113, 1.987530892951425043 ) ) ;
#19960=CARTESIAN_POINT ( 'NONE',  ( 0.6971942568897648851, 0.07405724077823318263, 1.461614173174583753 ) ) ;
#19961=CARTESIAN_POINT ( 'NONE',  ( 0.8759842519685039353, 0.1787899950787401882, 1.843011810969858333 ) ) ;
#19962=CARTESIAN_POINT ( 'NONE',  ( 1.054774247047244540, 0.07405724077823318263, 0.4576771653005669016 ) ) ;
#19963=ORIENTED_EDGE ( 'NONE', *, *, #44983, .T. ) ;
#19966=CARTESIAN_POINT ( 'NONE',  ( -1.033464566929133799, 1.928577636452524610E-17, 2.869337061179095023E-17 ) ) ;
#19967=CYLINDRICAL_SURFACE ( 'NONE', #30586, 0.1574803149606299191 ) ;
#19969=( BOUNDED_CURVE ( )  B_SPLINE_CURVE ( 2, ( #27964, #6113, #24123 ),
 .UNSPECIFIED., .F., .F. ) 
 B_SPLINE_CURVE_WITH_KNOTS ( ( 3, 3 ),
 ( 0.9975000000000000533, 1.000000000000000000 ),
 .UNSPECIFIED. ) 
 CURVE ( )  GEOMETRIC_REPRESENTATION_ITEM ( )  RATIONAL_B_SPLINE_CURVE ( ( 1.000000000000000000, 0.9238795325112869605, 1.000000000000000000 ) ) 
 REPRESENTATION_ITEM ( '' )  ) ;
#19970=CARTESIAN_POINT ( 'NONE',  ( 0.8759842519685039353, 0.1787899950787401882, 0.4256889763241890057 ) ) ;
#19971=CARTESIAN_POINT ( 'NONE',  ( 0.7556365493957359902, -0.1147211060030528113, 0.03937312978427136290 ) ) ;
#19974=DIRECTION ( 'NONE',  ( 1.000000000000000000, 0.000000000000000000, -1.822029033848725275E-16 ) ) ;
#19975=CARTESIAN_POINT ( 'NONE',  ( -1.054774247047244096, 0.000000000000000000, 1.321358267662771757 ) ) ;
#19976=CARTESIAN_POINT ( 'NONE',  ( 0.7185039370078746268, 0.06523048226347956391, 0.8046259841444418637 ) ) ;
#19977=ORIENTED_EDGE ( 'NONE', *, *, #19544, .F. ) ;
#19978=CARTESIAN_POINT ( 'NONE',  ( 0.9500414927467378812, 0.1787899950787401604, 1.058070866087969186 ) ) ;
#19980=CARTESIAN_POINT ( 'NONE',  ( -0.7185039370078746268, 0.06523048226347956391, 0.4896653542231815259 ) ) ;
#19983=CARTESIAN_POINT ( 'NONE',  ( 0.8019270111902717657, -0.1787899950787401604, 1.742125984198204858 ) ) ;
#19984=CARTESIAN_POINT ( 'NONE',  ( -0.9873396505805591694, -0.1113553986120547346, 1.186023622047243986 ) ) ;
#19985=CARTESIAN_POINT ( 'NONE',  ( -0.9873396505805591694, 0.1113553986120547346, 0.7234251968503936370 ) ) ;
#19986=CARTESIAN_POINT ( 'NONE',  ( -0.9412147342319837628, 0.1574803149606300301, 0.7554133857192454338 ) ) ;
#19987=CARTESIAN_POINT ( 'NONE',  ( 0.6971942568897626646, 0.07405724077823318263, 0.08366141726907130871 ) ) ;
#19988=CARTESIAN_POINT ( 'NONE',  ( 1.033464566929134687, -0.06523048226347956391, 1.493602362097197211 ) ) ;
#19989=EDGE_LOOP ( 'NONE', ( #28824, #22824, #34185, #45239 ) ) ;
#19991=ORIENTED_EDGE ( 'NONE', *, *, #39545, .T. ) ;
#19993=CARTESIAN_POINT ( 'NONE',  ( 0.8019270111902716547, 0.1787899950787401604, 0.9842519684501743749 ) ) ;
#19994=CARTESIAN_POINT ( 'NONE',  ( -0.6971942568897648851, 0.07405724077823318263, 1.614173228292692386 ) ) ;
#19996=CARTESIAN_POINT ( 'NONE',  ( -0.7495606340400177148, -0.1264236179284866091, 1.468996062938362046 ) ) ;
#19997=EDGE_CURVE ( 'NONE', #43450, #31512, #40112, .T. ) ;
#19998=CARTESIAN_POINT ( 'NONE',  ( -0.9873396505805591694, 0.1113553986120547346, 0.2411417321759374011 ) ) ;
#19999=FACE_OUTER_BOUND ( 'NONE', #19989, .T. ) ;
#20004=ORIENTED_EDGE ( 'NONE', *, *, #38758, .T. ) ;
#20005=CARTESIAN_POINT ( 'NONE',  ( 0.8759842519685039353, 0.1574803149606299191, 1.742125984144440975 ) ) ;
#20006=LINE ( 'NONE', #37996, #42160 ) ;
#20007=AXIS2_PLACEMENT_3D ( 'NONE', #2912, #20903, #42923 ) ;
#20008=CARTESIAN_POINT ( 'NONE',  ( 0.8759842519685039353, 0.1574803149606299191, 1.830708661417322913 ) ) ;
#20014=CARTESIAN_POINT ( 'NONE',  ( -1.002407869896990045, 0.1264236179284866091, 0.2682086613635594752 ) ) ;
#20015=CARTESIAN_POINT ( 'NONE',  ( -0.9412147342319837628, -0.1574803149606297803, 1.065452755905511806 ) ) ;
#20018=CARTESIAN_POINT ( 'NONE',  ( 1.002407869896990045, 0.1264236179284866091, 1.016240157426551161 ) ) ;
#20019=CARTESIAN_POINT ( 'NONE',  ( 1.054774247047244540, 0.07405724077823318263, 0.1427165353793073133 ) ) ;
#20021=ADVANCED_FACE ( 'NONE', ( #3045 ), #25108, .T. ) ;
#20022=CARTESIAN_POINT ( 'NONE',  ( 0.7646288533564489232, -0.1113553986120547346, 1.569881889763779625 ) ) ;
#20023=CARTESIAN_POINT ( 'NONE',  ( 0.8024386162957400925, 0.1423545520052694469, 1.979847512675880994 ) ) ;
#20025=CARTESIAN_POINT ( 'NONE',  ( -0.7185039370078739607, 0.000000000000000000, -2.869337061179095023E-17 ) ) ;
#20028=CARTESIAN_POINT ( 'NONE',  ( 0.6971942568897648851, 0.07405724077823318263, 0.9842519684501743749 ) ) ;
#20029=CARTESIAN_POINT ( 'NONE',  ( 0.8019270111902716547, -0.1787899950787401604, 1.825787401521040243 ) ) ;
#20030=CARTESIAN_POINT ( 'NONE',  ( 1.033464566929134687, 0.06523048226347956391, 0.3174212597349925224 ) ) ;
#20033=DIRECTION ( 'NONE',  ( 1.822029033848725028E-16, 0.000000000000000000, 1.000000000000000000 ) ) ;
#20035=CARTESIAN_POINT ( 'NONE',  ( -0.7646288533564489232, -0.1113553986120547346, 0.1820866140657015630 ) ) ;
#20037=CARTESIAN_POINT ( 'NONE',  ( 0.8759842519685039353, 0.1787899950787401882, 1.291830708607653477 ) ) ;
#20040=CARTESIAN_POINT ( 'NONE',  ( 0.7185039370078714072, 0.06523048226347728795, 1.237696850286174932 ) ) ;
#20043=CARTESIAN_POINT ( 'NONE',  ( 0.7185039370078739607, 0.000000000000000000, 4.498031496062992574 ) ) ;
#20045=CARTESIAN_POINT ( 'NONE',  ( 0.8759842519685039353, 0.1574803149606299191, 0.2559055118110236116 ) ) ;
#20047=EDGE_LOOP ( 'NONE', ( #20104, #35920, #16085, #25432 ) ) ;
#20049=CARTESIAN_POINT ( 'NONE',  ( -0.7495606340400177148, 0.1264236179284866091, 0.9867125983714331028 ) ) ;
#20051=CARTESIAN_POINT ( 'NONE',  ( -1.054774247047244540, -0.07405724077823318263, 1.870078740103715331 ) ) ;
#20052=CARTESIAN_POINT ( 'NONE',  ( -0.8759842519685039353, 0.1787899950787401882, 0.6274606298674959559 ) ) ;
#20053=EDGE_CURVE ( 'NONE', #14779, #13566, #19158, .T. ) ;
#20059=CYLINDRICAL_SURFACE ( 'NONE', #31802, 0.1574803149606299191 ) ;
#20063=CARTESIAN_POINT ( 'NONE',  ( -0.8759842519685039353, -0.1787899950787401882, 0.5241141731745827537 ) ) ;
#20064=CARTESIAN_POINT ( 'NONE',  ( 0.7646288533564489232, 0.1113553986120547346, 1.195866141624756018 ) ) ;
#20065=ORIENTED_EDGE ( 'NONE', *, *, #40985, .F. ) ;
#20067=CARTESIAN_POINT ( 'NONE',  ( -0.8759842519685039353, -0.1787899950787401882, 1.473917322780881722 ) ) ;
#20076=CARTESIAN_POINT ( 'NONE',  ( -1.033464566929133799, 0.000000000000000000, 1.220472440837354400 ) ) ;
#20077=CARTESIAN_POINT ( 'NONE',  ( 0.6971942568897626646, -0.07405724077823297447, 0.6397637794737947026 ) ) ;
#20079=CARTESIAN_POINT ( 'NONE',  ( -0.8107537697050254399, 0.1574803149606300301, 1.626476377845228916 ) ) ;
#20083=EDGE_CURVE ( 'NONE', #35490, #14813, #15098, .T. ) ;
#20084=CARTESIAN_POINT ( 'NONE',  ( -0.8759842519685039353, -0.1787899950787401882, 1.119586614119464585 ) ) ;
#20085=CARTESIAN_POINT ( 'NONE',  ( 0.9412147342319837628, 0.1574803149606300301, 1.080216535433071501 ) ) ;
#20087=CARTESIAN_POINT ( 'NONE',  ( -0.7185039370078739607, 1.928577636452523993E-17, 0.2657480314960630197 ) ) ;
#20091=CARTESIAN_POINT ( 'NONE',  ( 0.8759842519685039353, 0.000000000000000000, 4.498031496062992574 ) ) ;
#20095=CARTESIAN_POINT ( 'NONE',  ( 1.033464566929134687, -0.06523048226347956391, 0.2829724409448821643 ) ) ;
#20096=CARTESIAN_POINT ( 'NONE',  ( 0.7495606340400177148, 0.1264236179284866091, 0.8636811023084409733 ) ) ;
#20097=VERTEX_POINT ( 'NONE', #26780 ) ;
#20104=ORIENTED_EDGE ( 'NONE', *, *, #31626, .F. ) ;
#20105=VERTEX_POINT ( 'NONE', #45183 ) ;
#20106=CARTESIAN_POINT ( 'NONE',  ( -0.9500414927467378812, 0.1787899950787401604, 1.963582677111591401 ) ) ;
#20107=CARTESIAN_POINT ( 'NONE',  ( 1.054774247047244096, 0.000000000000000000, 1.916830708607653477 ) ) ;
#20108=ORIENTED_EDGE ( 'NONE', *, *, #14788, .T. ) ;
#20109=CARTESIAN_POINT ( 'NONE',  ( 1.054774247047244540, -0.07405724077823318263, 0.4970472440407249226 ) ) ;
#20110=CARTESIAN_POINT ( 'NONE',  ( -0.8019270111902717657, -0.1787899950787401604, 1.387795275536786610 ) ) ;
#20112=CARTESIAN_POINT ( 'NONE',  ( -0.7495606340400177148, 0.1264236179284866091, 0.2780511810485988278 ) ) ;
#20115=CARTESIAN_POINT ( 'NONE',  ( -1.002407869896990045, -0.1264236179284866091, 1.675688976324189117 ) ) ;
#20116=CARTESIAN_POINT ( 'NONE',  ( -0.9500414927467378812, -0.1787899950787401604, 0.09842519679663024046 ) ) ;
#20118=CARTESIAN_POINT ( 'NONE',  ( -0.8107537697050253289, 0.1574803149606300301, 1.793799212598424342 ) ) ;
#20120=B_SPLINE_CURVE_WITH_KNOTS ( 'NONE', 3,
 ( #28910, #14271, #3221, #29639, #2979, #36321, #39403, #18087, #14025, #11152, #39877, #21199, #44181, #91, #32733, #24805, #10680, #14738, #39635, #6817, #7308, #25288, #21927, #29410, #47328, #17612, #14499, #29160, #28671, #43717, #7532, #33213, #43239, #10921, #40114, #25544, #40342, #10442, #36777, #14986, #36547, #35833, #21437, #3708, #43954, #22867, #34148, #45123, #25996, #37008, #4388, #33682, #15458, #41046, #8240, #4630, #27445, #19971, #8959, #5347, #20682, #34611, #46320, #35322, #9447, #12579, #9910, #1760, #16852, #42693, #24520, #35085, #17089, #2233, #2462, #38430, #9193, #17325, #45365, #31257, #13044, #38670, #13504, #27206 ),
 .UNSPECIFIED., .F., .F.,
 ( 4, 2, 2, 2, 1, 1, 2, 2, 2, 2, 1, 1, 1, 1, 2, 2, 2, 2, 2, 1, 1, 1, 2, 2, 2, 2, 2, 1, 1, 1, 1, 2, 2, 2, 2, 2, 2, 1, 2, 2, 2, 2, 1, 1, 2, 2, 2, 2, 2, 4 ),
 ( 0.000000000000000000, 0.06249999999982676357, 0.09374999999974004128, 0.1093749999996965483, 0.1171874999996747879, 0.1210937499996639910, 0.1230468749996585232, 0.1249999999996530553, 0.1874999999994784727, 0.2187499999993911814, 0.2343749999993474664, 0.2421874999993256228, 0.2460937499993147703, 0.2480468749993092747, 0.2490234374993065269, 0.2499999999993037514, 0.3124999999991173172, 0.3437499999990241140, 0.3593749999989774846, 0.3671874999989540034, 0.3710937499989422350, 0.3730468749989364619, 0.3740234374989336308, 0.3749999999989308552, 0.4374999999987470578, 0.4687499999986551869, 0.4843749999986092791, 0.4921874999985862975, 0.4960937499985745291, 0.4980468749985661470, 0.4990234374985619281, 0.4995117187485633714, 0.4999999999985648702, 0.5624999999987573274, 0.5937499999988538057, 0.6093749999989021005, 0.6171874999989263033, 0.6210937499989379607, 0.6230468749989432897, 0.6249999999989486188, 0.6874999999991322497, 0.7187499999992240651, 0.7343749999992700284, 0.7421874999992934541, 0.7460937499993046673, 0.7499999999993158806, 0.8124999999994878541, 0.8437499999995732303, 0.8749999999996586064, 1.000000000000000000 ),
 .UNSPECIFIED. ) ;
#20121=CARTESIAN_POINT ( 'NONE',  ( 1.002407869896990045, 0.1264236179284866091, 1.685531496009228469 ) ) ;
#20123=CARTESIAN_POINT ( 'NONE',  ( -0.7185039370078760701, -0.06523048226348075740, 0.7308070865066462751 ) ) ;
#20126=( BOUNDED_CURVE ( )  B_SPLINE_CURVE ( 2, ( #23727, #27590, #45501, #2601, #23969, #9822, #34512, #1907, #13416 ),
 .UNSPECIFIED., .F., .T. ) 
 B_SPLINE_CURVE_WITH_KNOTS ( ( 3, 2, 2, 2, 3 ),
 ( 0.6899999999999999467, 0.6925000000000000044, 0.6949999999999999512, 0.6975000000000000089, 0.6999999999999999556 ),
 .UNSPECIFIED. ) 
 CURVE ( )  GEOMETRIC_REPRESENTATION_ITEM ( )  RATIONAL_B_SPLINE_CURVE ( ( 1.000000000000000000, 0.9238795325112939549, 1.000000000000000000, 0.9238795325112869605, 1.000000000000000000, 0.9238795325112869605, 1.000000000000000000, 0.9238795325112829637, 1.000000000000000000 ) ) 
 REPRESENTATION_ITEM ( '' )  ) ;
#20127=EDGE_CURVE ( 'NONE', #36143, #18901, #18703, .T. ) ;
#20128=ORIENTED_EDGE ( 'NONE', *, *, #11174, .T. ) ;
#20129=( BOUNDED_CURVE ( )  B_SPLINE_CURVE ( 2, ( #29877, #806, #29420, #43965, #19029, #4402, #11163, #40350, #18569 ),
 .UNSPECIFIED., .F., .F. ) 
 B_SPLINE_CURVE_WITH_KNOTS ( ( 3, 2, 2, 2, 3 ),
 ( 0.5400000000000000355, 0.5424999999999999822, 0.5450000000000000400, 0.5474999999999999867, 0.5500000000000000444 ),
 .UNSPECIFIED. ) 
 CURVE ( )  GEOMETRIC_REPRESENTATION_ITEM ( )  RATIONAL_B_SPLINE_CURVE ( ( 1.000000000000000000, 0.9238795325112869605, 1.000000000000000000, 0.9238795325112869605, 1.000000000000000000, 0.9238795325112869605, 1.000000000000000000, 0.9238795325112869605, 1.000000000000000000 ) ) 
 REPRESENTATION_ITEM ( '' )  ) ;
#20139=CARTESIAN_POINT ( 'NONE',  ( 0.6971942568897626646, -0.07405724077823297447, 0.8710629920722218200 ) ) ;
#20142=CARTESIAN_POINT ( 'NONE',  ( 0.8759842519685039353, -0.1574803149606299191, 0.06889763768774861963 ) ) ;
#20145=CARTESIAN_POINT ( 'NONE',  ( -0.7108038343253642033, 0.06841996760810098444, 0.03937007874015843040 ) ) ;
#20149=CARTESIAN_POINT ( 'NONE',  ( -0.8759842519685039353, -0.1787899950787401882, 1.902066929080094448 ) ) ;
#20151=CARTESIAN_POINT ( 'NONE',  ( -0.6971942568897637749, 2.189545951927499583E-17, 1.503444881836000002 ) ) ;
#20153=CARTESIAN_POINT ( 'NONE',  ( 1.002407869896990045, -0.1264236179284866091, 1.439468503883244210 ) ) ;
#20155=CARTESIAN_POINT ( 'NONE',  ( -0.8019270111902717657, 0.1787899950787401604, 0.5118110235682844511 ) ) ;
#20156=CARTESIAN_POINT ( 'NONE',  ( -1.054774247047244540, 0.07405724077823318263, 1.205708661363558365 ) ) ;
#20158=CARTESIAN_POINT ( 'NONE',  ( 0.6971942568897648851, 0.07405724077823318263, 0.6742125983714336579 ) ) ;
#20159=CARTESIAN_POINT ( 'NONE',  ( -1.054774247047244540, -0.07405724077823318263, 0.4921259841982049132 ) ) ;
#20160=DIRECTION ( 'NONE',  ( 1.000000000000000000, 0.000000000000000000, -1.822029033848725275E-16 ) ) ;
#20161=ORIENTED_EDGE ( 'NONE', *, *, #30773, .T. ) ;
#20162=CARTESIAN_POINT ( 'NONE',  ( -0.8107537697050253289, 0.1574803149606300301, 0.3764763779527559029 ) ) ;
#20163=CARTESIAN_POINT ( 'NONE',  ( 0.6971942568897648851, -0.07405724077823297447, 1.348425196796630976 ) ) ;
#20165=ORIENTED_EDGE ( 'NONE', *, *, #19041, .F. ) ;
#20168=CARTESIAN_POINT ( 'NONE',  ( -0.9500414927467378812, 0.1787899950787401604, 0.9399606298674970661 ) ) ;
#20169=EDGE_CURVE ( 'NONE', #12054, #25373, #1341, .T. ) ;
#20170=CARTESIAN_POINT ( 'NONE',  ( -1.002407869896990045, 0.1264236179284866091, 0.1845472440407248116 ) ) ;
#20175=EDGE_CURVE ( 'NONE', #19533, #35669, #46280, .T. ) ;
#20178=CARTESIAN_POINT ( 'NONE',  ( 1.054774247047244096, 0.000000000000000000, 1.360728346402929168 ) ) ;
#20179=EDGE_CURVE ( 'NONE', #110, #25251, #23622, .T. ) ;
#20180=CARTESIAN_POINT ( 'NONE',  ( 1.033464566929134687, 0.06523048226347956391, 0.8784448818897643285 ) ) ;
#20183=DIRECTION ( 'NONE',  ( -1.000000000000000000, 0.000000000000000000, 0.000000000000000000 ) ) ;
#20184=CARTESIAN_POINT ( 'NONE',  ( 1.002407869896990045, -0.1264236179284866091, 1.631397637741511808 ) ) ;
#20187=CARTESIAN_POINT ( 'NONE',  ( -0.7646288533564489232, 0.1113553986120547346, 1.747047243986960652 ) ) ;
#20188=CARTESIAN_POINT ( 'NONE',  ( -0.6971942568897648851, 0.07405724077823318263, 0.8710629920722218200 ) ) ;
#20190=CARTESIAN_POINT ( 'NONE',  ( 1.033464566929133799, 0.000000000000000000, 0.07874015737278799998 ) ) ;
#20192=CARTESIAN_POINT ( 'NONE',  ( -0.7749013318191750876, -0.1380202477924483417, 1.986195989362255832 ) ) ;
#20194=CARTESIAN_POINT ( 'NONE',  ( -0.9873396505805591694, 0.1113553986120547346, 1.028543306979086802 ) ) ;
#20195=CARTESIAN_POINT ( 'NONE',  ( 0.8019270111902717657, -0.1787899950787401604, 1.550196850339937926 ) ) ;
#20196=CARTESIAN_POINT ( 'NONE',  ( 0.8759842519685039353, -0.1787899950787401882, 1.902066929080094448 ) ) ;
#20197=CARTESIAN_POINT ( 'NONE',  ( 1.054774247047244540, 0.07405724077823318263, 0.4183070865604096578 ) ) ;
#20198=CARTESIAN_POINT ( 'NONE',  ( -0.7646288533564489232, -0.1113553986120547346, 0.1427165353255439029 ) ) ;
#20199=DIRECTION ( 'NONE',  ( 1.000000000000000000, 0.000000000000000000, -1.822029033848725275E-16 ) ) ;
#20203=CARTESIAN_POINT ( 'NONE',  ( 1.002407869896990045, -0.1264236179284866091, 0.4502952755367874427 ) ) ;
#20204=CARTESIAN_POINT ( 'NONE',  ( -1.033464566929133799, 0.000000000000000000, 0.2755905510735752184 ) ) ;
#20205=CARTESIAN_POINT ( 'NONE',  ( 0.8759842519685039353, -0.1787899950787401882, 1.311515747977732405 ) ) ;
#20207=CARTESIAN_POINT ( 'NONE',  ( 0.9873396505805591694, 0.1113553986120547346, 0.2116141732283464416 ) ) ;
#20208=CARTESIAN_POINT ( 'NONE',  ( 1.033464566929134687, 0.06523048226347956391, 0.8686023620971983217 ) ) ;
#20209=ORIENTED_EDGE ( 'NONE', *, *, #11817, .F. ) ;
#20210=CARTESIAN_POINT ( 'NONE',  ( -0.6971942568897637749, 2.189545951927499583E-17, 1.070374015694267600 ) ) ;
#20211=LINE ( 'NONE', #34861, #22235 ) ;
#20212=CARTESIAN_POINT ( 'NONE',  ( 0.8759842519685039353, -0.1787899950787401882, 0.9621062991588346103 ) ) ;
#20213=ORIENTED_EDGE ( 'NONE', *, *, #20610, .F. ) ;
#20216=CARTESIAN_POINT ( 'NONE',  ( -0.7185039370078746268, -0.06523048226347956391, 0.5339566928058587791 ) ) ;
#20217=CARTESIAN_POINT ( 'NONE',  ( -0.7185039370078739607, 1.928577636452523993E-17, 1.368110236220472675 ) ) ;
#20218=CARTESIAN_POINT ( 'NONE',  ( 0.7185039370078766252, -0.06523048226348168721, 1.793799212490897688 ) ) ;
#20220=CARTESIAN_POINT ( 'NONE',  ( -0.8759842519685039353, -0.1574803149606299191, 0.4330708661417322913 ) ) ;
#20221=CARTESIAN_POINT ( 'NONE',  ( 0.8759842519685039353, 0.1787899950787401882, 0.1943897637257641919 ) ) ;
#20222=CARTESIAN_POINT ( 'NONE',  ( -0.7495606340400177148, 0.1264236179284866091, 0.1156496062454492185 ) ) ;
#20223=CARTESIAN_POINT ( 'NONE',  ( 0.8107537697050253289, -0.1574803149606297803, 1.365649606191684295 ) ) ;
#20228=VERTEX_POINT ( 'NONE', #30396 ) ;
#20229=CARTESIAN_POINT ( 'NONE',  ( 1.054774247047244096, 0.000000000000000000, 0.9719488188438739629 ) ) ;
#20230=CARTESIAN_POINT ( 'NONE',  ( -1.054774247047244540, -0.07405724077823318263, 1.712598425143087466 ) ) ;
#20232=( BOUNDED_CURVE ( )  B_SPLINE_CURVE ( 2, ( #45234, #1874, #34255, #12926, #41626, #5936, #16511, #1387, #39001 ),
 .UNSPECIFIED., .F., .F. ) 
 B_SPLINE_CURVE_WITH_KNOTS ( ( 3, 2, 2, 2, 3 ),
 ( 0.2700000000000000178, 0.2725000000000000200, 0.2750000000000000222, 0.2775000000000000244, 0.2800000000000000266 ),
 .UNSPECIFIED. ) 
 CURVE ( )  GEOMETRIC_REPRESENTATION_ITEM ( )  RATIONAL_B_SPLINE_CURVE ( ( 1.000000000000000000, 0.9238795325112869605, 1.000000000000000000, 0.9238795325112869605, 1.000000000000000000, 0.9238795325112869605, 1.000000000000000000, 0.9238795325112879597, 1.000000000000000000 ) ) 
 REPRESENTATION_ITEM ( '' )  ) ;
#20233=EDGE_CURVE ( 'NONE', #18241, #34008, #38728, .T. ) ;
#20240=ORIENTED_EDGE ( 'NONE', *, *, #30605, .F. ) ;
#20241=EDGE_CURVE ( 'NONE', #1697, #12053, #28257, .T. ) ;
#20242=ORIENTED_EDGE ( 'NONE', *, *, #44884, .F. ) ;
#20245=LINE ( 'NONE', #38706, #47029 ) ;
#20247=CARTESIAN_POINT ( 'NONE',  ( 1.033464566929133799, 0.000000000000000000, 1.899606299212598604 ) ) ;
#20251=( BOUNDED_CURVE ( )  B_SPLINE_CURVE ( 2, ( #3545, #43784, #7376, #33033, #36389, #14093, #158, #25828, #28740 ),
 .UNSPECIFIED., .F., .T. ) 
 B_SPLINE_CURVE_WITH_KNOTS ( ( 3, 2, 2, 2, 3 ),
 ( 0.5799999999999999600, 0.5825000000000000178, 0.5849999999999999645, 0.5875000000000000222, 0.5899999999999999689 ),
 .UNSPECIFIED. ) 
 CURVE ( )  GEOMETRIC_REPRESENTATION_ITEM ( )  RATIONAL_B_SPLINE_CURVE ( ( 1.000000000000000000, 0.9238795325112869605, 1.000000000000000000, 0.9238795325112869605, 1.000000000000000000, 0.9238795325112869605, 1.000000000000000000, 0.9238795325112869605, 1.000000000000000000 ) ) 
 REPRESENTATION_ITEM ( '' )  ) ;
#20252=CARTESIAN_POINT ( 'NONE',  ( -0.7495606340400177148, 0.1264236179284866091, 0.3174212597887562382 ) ) ;
#20255=CARTESIAN_POINT ( 'NONE',  ( 1.054774247047244096, 0.000000000000000000, 1.050688976324189117 ) ) ;
#20256=CARTESIAN_POINT ( 'NONE',  ( -0.8759842519685039353, 0.1574803149606299191, 0.6397637794200314865 ) ) ;
#20258=CARTESIAN_POINT ( 'NONE',  ( 1.033464566929134687, 0.06523048226347956391, 1.508366141732284449 ) ) ;
#20261=CARTESIAN_POINT ( 'NONE',  ( 1.033464566929133799, 0.000000000000000000, 0.4724409447743622148 ) ) ;
#20262=CARTESIAN_POINT ( 'NONE',  ( -0.9873396505805591694, -0.1113553986120547346, 1.648622047136566904 ) ) ;
#20264=CARTESIAN_POINT ( 'NONE',  ( 1.054774247047244540, 0.07405724077823318263, 1.008858267662772423 ) ) ;
#20265=CARTESIAN_POINT ( 'NONE',  ( 1.033464566929133799, 0.000000000000000000, 0.2755905510735752184 ) ) ;
#20268=CARTESIAN_POINT ( 'NONE',  ( 1.004041291822608928, 0.1039877302390117553, 0.03936817812369314967 ) ) ;
#20270=CARTESIAN_POINT ( 'NONE',  ( -0.7185039370078746268, -0.06523048226347956391, 0.2977362203649139283 ) ) ;
#20272=CARTESIAN_POINT ( 'NONE',  ( 1.054774247047244096, 0.000000000000000000, 1.242618110182456714 ) ) ;
#20276=CARTESIAN_POINT ( 'NONE',  ( -0.6971942568897626646, -0.07405724077823297447, 0.6348425196312760255 ) ) ;
#20279=CARTESIAN_POINT ( 'NONE',  ( 1.033464566929133799, 0.000000000000000000, 1.377952755797984263 ) ) ;
#20282=CARTESIAN_POINT ( 'NONE',  ( -0.9500414927467378812, 0.1787899950787401604, 0.9793307086076531442 ) ) ;
#20283=VECTOR ( 'NONE', #4966, 39.37007874015748143 ) ;
#20285=CARTESIAN_POINT ( 'NONE',  ( -1.033464566929133799, 0.000000000000000000, 0.04921259842519685318 ) ) ;
#20286=CARTESIAN_POINT ( 'NONE',  ( -0.7495606340400177148, -0.1264236179284866091, 0.9916338582139527791 ) ) ;
#20287=CARTESIAN_POINT ( 'NONE',  ( -1.054774247047244540, 0.07405724077823318263, 0.6988188975840318173 ) ) ;
#20288=ORIENTED_EDGE ( 'NONE', *, *, #21305, .F. ) ;
#20291=CARTESIAN_POINT ( 'NONE',  ( -0.7646288533564489232, 0.1113553986120547346, 0.09350393690034704275 ) ) ;
#20293=VERTEX_POINT ( 'NONE', #16228 ) ;
#20296=ORIENTED_EDGE ( 'NONE', *, *, #32657, .T. ) ;
#20298=EDGE_CURVE ( 'NONE', #31809, #26252, #19969, .T. ) ;
#20300=CARTESIAN_POINT ( 'NONE',  ( -0.8759842519685039353, 0.1787899950787401882, 0.5437992125446614589 ) ) ;
#20303=CARTESIAN_POINT ( 'NONE',  ( -0.9500414927467377701, 0.1787899950787401604, 1.648622047190331230 ) ) ;
#20309=CARTESIAN_POINT ( 'NONE',  ( 0.9412147342319837628, 0.1574803149606300301, 0.5684055118110235005 ) ) ;
#20312=CYLINDRICAL_SURFACE ( 'NONE', #12589, 0.1574803149606299191 ) ;
#20313=CARTESIAN_POINT ( 'NONE',  ( -0.7185039370078746268, -0.06523048226347956391, 1.203248031388535200 ) ) ;
#20314=CARTESIAN_POINT ( 'NONE',  ( 0.6971942568897626646, 0.07405724077823318263, 0.6348425196312760255 ) ) ;
#20317=AXIS2_PLACEMENT_3D ( 'NONE', #639, #23193, #37807 ) ;
#20318=CARTESIAN_POINT ( 'NONE',  ( -1.033464566929133799, 0.000000000000000000, 0.4035433070866141780 ) ) ;
#20321=CARTESIAN_POINT ( 'NONE',  ( 0.9873396505805591694, -0.1113553986120547346, 1.067913385826771755 ) ) ;
#20322=CARTESIAN_POINT ( 'NONE',  ( -1.033464566929134687, 0.06523048226347956391, 1.262303149498772425 ) ) ;
#20327=CARTESIAN_POINT ( 'NONE',  ( -1.033464566929133799, 0.000000000000000000, 1.968503936900346529 ) ) ;
#20328=LINE ( 'NONE', #5227, #30082 ) ;
#20332=CARTESIAN_POINT ( 'NONE',  ( -0.7185039370078739607, 1.928577636452523993E-17, 1.053149606299212504 ) ) ;
#20333=CARTESIAN_POINT ( 'NONE',  ( 0.9873396505805591694, 0.1113553986120547346, 1.156496062992125928 ) ) ;
#20334=CARTESIAN_POINT ( 'NONE',  ( 1.054774247047244540, -0.07405724077823318263, 0.7677165353793073965 ) ) ;
#20336=CARTESIAN_POINT ( 'NONE',  ( 0.8759842519685039353, -0.1574803149606299191, 1.456692913385826849 ) ) ;
#20341=CARTESIAN_POINT ( 'NONE',  ( 1.033464566929134687, 0.06523048226347956391, 1.222933070758614127 ) ) ;
#20342=CARTESIAN_POINT ( 'NONE',  ( 1.033464566929134687, -0.06523048226347956391, 1.178641732175937040 ) ) ;
#20345=CARTESIAN_POINT ( 'NONE',  ( -1.054774247047244540, -0.07405724077823318263, 1.953740157426552715 ) ) ;
#20346=VERTEX_POINT ( 'NONE', #5178 ) ;
#20349=CARTESIAN_POINT ( 'NONE',  ( -0.6971942568897637749, 2.189545951927499583E-17, 1.459153543253322693 ) ) ;
#20353=CARTESIAN_POINT ( 'NONE',  ( -1.054774247047244540, -0.07405724077823318263, 0.3001968503399373711 ) ) ;
#20355=CARTESIAN_POINT ( 'NONE',  ( 0.7646288533564489232, -0.1113553986120547346, 1.569881889763779625 ) ) ;
#20356=CARTESIAN_POINT ( 'NONE',  ( -0.8019270111902717657, -0.1787899950787401604, 1.668307086560410157 ) ) ;
#20357=CARTESIAN_POINT ( 'NONE',  ( -1.033464566929134687, -0.06523048226347956391, 1.818405511811023167 ) ) ;
#20359=CARTESIAN_POINT ( 'NONE',  ( 0.6971942568897648851, 0.07405724077823318263, 1.737204724355685626 ) ) ;
#20363=EDGE_CURVE ( 'NONE', #22586, #38634, #23639, .T. ) ;
#20366=CARTESIAN_POINT ( 'NONE',  ( -0.8759842519685039353, 0.1787899950787401882, 1.218011810969858111 ) ) ;
#20369=CARTESIAN_POINT ( 'NONE',  ( -1.033464566929134687, -0.06523048226347956391, 0.8243110235145187925 ) ) ;
#20370=CARTESIAN_POINT ( 'NONE',  ( -0.9873396505805591694, -0.1113553986120547346, 0.7135826771653542844 ) ) ;
#20372=CARTESIAN_POINT ( 'NONE',  ( 0.8019270111902717657, -0.1787899950787401604, 0.9547244093950547628 ) ) ;
#20375=CARTESIAN_POINT ( 'NONE',  ( 0.8759842519685039353, -0.1574803149606299191, 1.092519684931842594 ) ) ;
#20376=CARTESIAN_POINT ( 'NONE',  ( 0.7185039370078746268, 0.06523048226347956391, 0.09596456682160688090 ) ) ;
#20377=CARTESIAN_POINT ( 'NONE',  ( -0.7185039370078739607, 1.928577636452523993E-17, 1.171259842519684957 ) ) ;
#20382=CARTESIAN_POINT ( 'NONE',  ( -0.8759842519685039353, 0.1787899950787401882, 1.882381889710015743 ) ) ;
#20383=EDGE_LOOP ( 'NONE', ( #33878, #42123, #24288, #17923 ) ) ;
#20385=CARTESIAN_POINT ( 'NONE',  ( -1.002407869896990045, -0.1264236179284866091, 1.439468503883244210 ) ) ;
#20387=CARTESIAN_POINT ( 'NONE',  ( 0.8019270111902717657, 0.1787899950787401604, 1.377952755851748146 ) ) ;
#20389=CARTESIAN_POINT ( 'NONE',  ( -0.7495606340400177148, 0.1264236179284866091, 0.7111220471903307860 ) ) ;
#20390=CARTESIAN_POINT ( 'NONE',  ( 0.6971942568897637749, 2.189545951927499583E-17, 0.08612204719033110523 ) ) ;
#20391=CARTESIAN_POINT ( 'NONE',  ( -0.8759842519685039353, 0.1787899950787401882, 1.291830708607653477 ) ) ;
#20392=FACE_OUTER_BOUND ( 'NONE', #7039, .T. ) ;
#20394=CARTESIAN_POINT ( 'NONE',  ( 0.7495606340400177148, 0.1264236179284866091, 0.6717519684501732646 ) ) ;
#20395=CARTESIAN_POINT ( 'NONE',  ( -0.8759842519685039353, 0.1787899950787401882, 0.5044291338045039375 ) ) ;
#20401=CARTESIAN_POINT ( 'NONE',  ( -0.7646288533564489232, 0.1113553986120547346, 0.2608267716535432879 ) ) ;
#20402=CARTESIAN_POINT ( 'NONE',  ( 0.8019270111902716547, -0.1787899950787401604, 1.353346456639149986 ) ) ;
#20404=CARTESIAN_POINT ( 'NONE',  ( -1.033464566929134687, -0.06523048226347956391, 1.847933070758615237 ) ) ;
#20408=CARTESIAN_POINT ( 'NONE',  ( -0.8019270111902717657, 0.1787899950787401604, 1.023622047190330342 ) ) ;
#20409=EDGE_CURVE ( 'NONE', #10797, #37122, #42897, .T. ) ;
#20413=VERTEX_POINT ( 'NONE', #43481 ) ;
#20417=ORIENTED_EDGE ( 'NONE', *, *, #36217, .T. ) ;
#20418=CARTESIAN_POINT ( 'NONE',  ( 0.7495606340400177148, 0.1264236179284866091, 1.375492125930488196 ) ) ;
#20422=DIRECTION ( 'NONE',  ( -1.000000000000000000, 0.000000000000000000, 0.000000000000000000 ) ) ;
#20424=CARTESIAN_POINT ( 'NONE',  ( 1.002407869896990045, 0.1264236179284866091, 1.601870078686393750 ) ) ;
#20428=CARTESIAN_POINT ( 'NONE',  ( 0.8019270111902717657, 0.1787899950787401604, 0.5068897637257642197 ) ) ;
#20430=CARTESIAN_POINT ( 'NONE',  ( -0.6971942568897637749, 2.189545951927499583E-17, 0.7554133857730077617 ) ) ;
#20432=CARTESIAN_POINT ( 'NONE',  ( 0.8107537697050254399, 0.1574803149606300301, 0.09104330697908723236 ) ) ;
#20434=CARTESIAN_POINT ( 'NONE',  ( -0.8097075710689116690, -0.1591366973851143507, 1.986952455759391389 ) ) ;
#20436=CARTESIAN_POINT ( 'NONE',  ( 0.6971942568897637749, 2.189545951927499583E-17, 1.582185039316315045 ) ) ;
#20438=CARTESIAN_POINT ( 'NONE',  ( 0.9500414927467377701, 0.1787899950787401604, 0.3838582676627718127 ) ) ;
#20439=DIRECTION ( 'NONE',  ( -1.000000000000000000, 0.000000000000000000, 0.000000000000000000 ) ) ;
#20441=CARTESIAN_POINT ( 'NONE',  ( 0.9873396505805591694, -0.1113553986120547346, 0.8612204723334173639 ) ) ;
#20445=CARTESIAN_POINT ( 'NONE',  ( 1.054774247047244096, 0.000000000000000000, 0.4158464566391496531 ) ) ;
#20447=CARTESIAN_POINT ( 'NONE',  ( 0.8107537697050234415, -0.1574803149606297803, 0.07627952755905519078 ) ) ;
#20449=CARTESIAN_POINT ( 'NONE',  ( -0.8759842519685039353, 0.1787899950787401882, 1.449311023568283341 ) ) ;
#20450=CARTESIAN_POINT ( 'NONE',  ( 0.8759842519685039353, 0.1574803149606299191, 0.7578740156405039397 ) ) ;
#20451=ORIENTED_EDGE ( 'NONE', *, *, #38521, .T. ) ;
#20452=CYLINDRICAL_SURFACE ( 'NONE', #18413, 0.1574803149606299191 ) ;
#20454=CARTESIAN_POINT ( 'NONE',  ( 0.9500414927467378812, -0.1787899950787401604, 0.9645669290800953366 ) ) ;
#20455=VERTEX_POINT ( 'NONE', #32015 ) ;
#20457=CARTESIAN_POINT ( 'NONE',  ( -0.7185039370078746268, 0.06523048226347956391, 0.5684055117034967353 ) ) ;
#20458=FACE_OUTER_BOUND ( 'NONE', #9455, .T. ) ;
#20459=CARTESIAN_POINT ( 'NONE',  ( 1.054774247047244540, -0.07405724077823318263, 1.712598425143087688 ) ) ;
#20460=CARTESIAN_POINT ( 'NONE',  ( -0.7646288533564489232, -0.1113553986120547346, 1.451771653543306950 ) ) ;
#20462=CARTESIAN_POINT ( 'NONE',  ( -0.9412147342319837628, 0.1574803149606300301, 0.7258858267716534751 ) ) ;
#20463=CARTESIAN_POINT ( 'NONE',  ( 0.8019270111902716547, -0.1787899950787401604, 0.2116141731745827814 ) ) ;
#20464=CARTESIAN_POINT ( 'NONE',  ( -1.054774247047244540, 0.07405724077823318263, 0.1033464566391499029 ) ) ;
#20465=CARTESIAN_POINT ( 'NONE',  ( 0.9412147342319837628, 0.1574803149606300301, 1.424704724301921743 ) ) ;
#20471=CARTESIAN_POINT ( 'NONE',  ( -0.6971942568897637749, 2.189545951927499583E-17, 1.774114173174582643 ) ) ;
#20477=ORIENTED_EDGE ( 'NONE', *, *, #36334, .F. ) ;
#20479=EDGE_LOOP ( 'NONE', ( #17802, #18209, #35579, #1550 ) ) ;
#20481=CARTESIAN_POINT ( 'NONE',  ( 1.002407869896990045, -0.1264236179284866091, 1.080216535379306952 ) ) ;
#20483=CARTESIAN_POINT ( 'NONE',  ( -1.033464566929133799, 0.000000000000000000, 0.9842519683964094934 ) ) ;
#20484=CARTESIAN_POINT ( 'NONE',  ( 0.7185039370078746268, -0.06523048226347956391, 1.843011811023621327 ) ) ;
#20485=APPLICATION_CONTEXT ( 'automotive_design' ) ;
#20487=CARTESIAN_POINT ( 'NONE',  ( -1.054774247047244096, 0.000000000000000000, 0.3420275590013546751 ) ) ;
#20488=CARTESIAN_POINT ( 'NONE',  ( -0.7646288533564489232, 0.1113553986120547346, 1.008858267716535417 ) ) ;
#20492=CARTESIAN_POINT ( 'NONE',  ( 1.002407869896990045, -0.1264236179284866091, 1.124507873961984261 ) ) ;
#20493=CARTESIAN_POINT ( 'NONE',  ( 0.8759842519685039353, -0.1787899950787401882, 1.587106299158834721 ) ) ;
#20495=EDGE_CURVE ( 'NONE', #33124, #20413, #7068, .T. ) ;
#20496=CARTESIAN_POINT ( 'NONE',  ( 0.7668818483817357867, 0.1192326576165682328, 1.980675047218597218 ) ) ;
#20497=CARTESIAN_POINT ( 'NONE',  ( -0.8360297024941153454, 0.1537365954182407513, 1.979133126318196823 ) ) ;
#20499=CARTESIAN_POINT ( 'NONE',  ( 0.7185039370078739607, 1.928577636452523993E-17, 0.6889763778452283605 ) ) ;
#20502=EDGE_CURVE ( 'NONE', #42193, #8550, #13786, .T. ) ;
#20503=CARTESIAN_POINT ( 'NONE',  ( 0.8107537697050254399, -0.1574803149606297803, 1.651082677165354839 ) ) ;
#20504=CARTESIAN_POINT ( 'NONE',  ( 1.002407869896990045, -0.1264236179284866091, 1.001476377898992132 ) ) ;
#20505=CARTESIAN_POINT ( 'NONE',  ( 1.002407869896990045, -0.1264236179284866091, 1.911909448765133801 ) ) ;
#20506=CARTESIAN_POINT ( 'NONE',  ( 0.9412147342319837628, -0.1574803149606297803, 0.3075787400499532809 ) ) ;
#20507=VERTEX_POINT ( 'NONE', #21696 ) ;
#20511=CARTESIAN_POINT ( 'NONE',  ( -0.8107537697050234415, -0.1574803149606297803, 0.3026574802074335491 ) ) ;
#20512=CARTESIAN_POINT ( 'NONE',  ( 0.7495606340400177148, 0.1264236179284866091, 1.296751968450173154 ) ) ;
#20515=CARTESIAN_POINT ( 'NONE',  ( 0.8107537697050234415, -0.1574803149606297803, 0.06643700776648873985 ) ) ;
#20517=DIRECTION ( 'NONE',  ( -1.000000000000000000, 0.000000000000000000, 0.000000000000000000 ) ) ;
#20518=( BOUNDED_CURVE ( )  B_SPLINE_CURVE ( 2, ( #5839, #2001, #23579, #20447, #38189, #20915, #46078, #42475, #35554 ),
 .UNSPECIFIED., .F., .T. ) 
 B_SPLINE_CURVE_WITH_KNOTS ( ( 3, 2, 2, 2, 3 ),
 ( 0.02999999999999999889, 0.03250000000000000111, 0.03500000000000000333, 0.03749999999999999861, 0.04000000000000000083 ),
 .UNSPECIFIED. ) 
 CURVE ( )  GEOMETRIC_REPRESENTATION_ITEM ( )  RATIONAL_B_SPLINE_CURVE ( ( 1.000000000000000000, 0.9238795325112869605, 1.000000000000000000, 0.9238795325112869605, 1.000000000000000000, 0.9238795325112869605, 1.000000000000000000, 0.9238795325112869605, 1.000000000000000000 ) ) 
 REPRESENTATION_ITEM ( '' )  ) ;
#20519=CARTESIAN_POINT ( 'NONE',  ( 0.7185039370078766252, -0.06523048226348168721, 1.360728346349167284 ) ) ;
#20520=CARTESIAN_POINT ( 'NONE',  ( -0.8759842519685039353, 0.1574803149606299191, 0.2066929132782996115 ) ) ;
#20521=CARTESIAN_POINT ( 'NONE',  ( -0.8759842519685039353, 0.000000000000000000, 1.978346456692913646 ) ) ;
#20523=CARTESIAN_POINT ( 'NONE',  ( -1.002407869896990045, -0.1264236179284866091, 1.395177165300567124 ) ) ;
#20525=CARTESIAN_POINT ( 'NONE',  ( -0.8759842519685039353, -0.1787899950787401882, 0.9227362204186770889 ) ) ;
#20526=CARTESIAN_POINT ( 'NONE',  ( -0.9873396505805591694, 0.1113553986120547346, 0.01476377952755905665 ) ) ;
#20528=CARTESIAN_POINT ( 'NONE',  ( -1.054774247047244540, -0.07405724077823318263, 1.003937007820253413 ) ) ;
#20529=CARTESIAN_POINT ( 'NONE',  ( -0.8019270111902717657, 0.1787899950787401604, 0.6299212597887560161 ) ) ;
#20531=DIRECTION ( 'NONE',  ( -1.000000000000000000, 0.000000000000000000, 0.000000000000000000 ) ) ;
#20537=( BOUNDED_CURVE ( )  B_SPLINE_CURVE ( 2, ( #4779, #30239, #4528, #41177, #7669, #12237, #29542, #7911, #3842 ),
 .UNSPECIFIED., .F., .F. ) 
 B_SPLINE_CURVE_WITH_KNOTS ( ( 3, 2, 2, 2, 3 ),
 ( 0.8199999999999999512, 0.8225000000000000089, 0.8249999999999999556, 0.8275000000000000133, 0.8299999999999999600 ),
 .UNSPECIFIED. ) 
 CURVE ( )  GEOMETRIC_REPRESENTATION_ITEM ( )  RATIONAL_B_SPLINE_CURVE ( ( 1.000000000000000000, 0.9238795325112899581, 1.000000000000000000, 0.9238795325112869605, 1.000000000000000000, 0.9238795325112869605, 1.000000000000000000, 0.9238795325112799661, 1.000000000000000000 ) ) 
 REPRESENTATION_ITEM ( '' )  ) ;
#20538=CARTESIAN_POINT ( 'NONE',  ( -0.8759842519685039353, 0.1787899950787401882, 0.6619094487651338010 ) ) ;
#20539=CARTESIAN_POINT ( 'NONE',  ( -0.7185039370078739607, 1.928577636452523993E-17, 0.5708661416247566844 ) ) ;
#20541=CARTESIAN_POINT ( 'NONE',  ( -0.8759842519685039353, -0.1787899950787401882, 1.631397637741511808 ) ) ;
#20544=CARTESIAN_POINT ( 'NONE',  ( 0.9412147342319837628, -0.1574803149606297803, 0.5930118110236219930 ) ) ;
#20545=CARTESIAN_POINT ( 'NONE',  ( -1.033464566929133799, 0.000000000000000000, 0.9547244094488189781 ) ) ;
#20546=CARTESIAN_POINT ( 'NONE',  ( -0.7646288533564489232, 0.1113553986120547346, 1.274606299105070839 ) ) ;
#20550=EDGE_LOOP ( 'NONE', ( #28819, #44776, #38319, #19520, #296 ) ) ;
#20552=CARTESIAN_POINT ( 'NONE',  ( 0.9412147342319837628, -0.1574803149606297803, 1.144192913385827737 ) ) ;
#20553=CARTESIAN_POINT ( 'NONE',  ( -0.8759842519685039353, 0.1574803149606299191, 1.269685039262551163 ) ) ;
#20555=CARTESIAN_POINT ( 'NONE',  ( 0.7185039370078746268, -0.06523048226347956391, 1.961122047244095778 ) ) ;
#20556=EDGE_CURVE ( 'NONE', #47261, #31760, #35612, .T. ) ;
#20558=VECTOR ( 'NONE', #4440, 39.37007874015748143 ) ;
#20563=CARTESIAN_POINT ( 'NONE',  ( -0.8759842519685039353, -0.1574803149606299191, 1.062992125984252079 ) ) ;
#20565=CARTESIAN_POINT ( 'NONE',  ( 0.8759842519685039353, 0.1787899950787401882, 0.8587598424659212970 ) ) ;
#20575=CARTESIAN_POINT ( 'NONE',  ( -0.8019270111902717657, -0.1787899950787401604, 1.865157480261195877 ) ) ;
#20576=CARTESIAN_POINT ( 'NONE',  ( 1.054774247047244096, 0.000000000000000000, 1.877460629867496067 ) ) ;
#20578=CYLINDRICAL_SURFACE ( 'NONE', #35588, 0.1574803149606299191 ) ;
#20579=CARTESIAN_POINT ( 'NONE',  ( -0.7495606340400177148, -0.1264236179284866091, 1.503444881836000002 ) ) ;
#20581=CARTESIAN_POINT ( 'NONE',  ( -0.9500414927467378812, 0.1787899950787401604, 1.013779527505291878 ) ) ;
#20582=CARTESIAN_POINT ( 'NONE',  ( -0.6971942568897637749, 2.189545951927499583E-17, 0.1648622046706460786 ) ) ;
#20584=CARTESIAN_POINT ( 'NONE',  ( -1.054774247047244540, -0.07405724077823318263, 1.914370078686394860 ) ) ;
#20586=CARTESIAN_POINT ( 'NONE',  ( -1.033464566929133799, 0.000000000000000000, 1.820866141732283561 ) ) ;
#20587=CARTESIAN_POINT ( 'NONE',  ( -0.8759842519685039353, 0.000000000000000000, 1.995570866087968520 ) ) ;
#20590=DIRECTION ( 'NONE',  ( 0.000000000000000000, 0.000000000000000000, -1.000000000000000000 ) ) ;
#20591=DIRECTION ( 'NONE',  ( 0.000000000000000000, 0.000000000000000000, -1.000000000000000000 ) ) ;
#20594=ORIENTED_EDGE ( 'NONE', *, *, #32334, .T. ) ;
#20595=CARTESIAN_POINT ( 'NONE',  ( -1.054774247047244540, 0.07405724077823318263, 1.249999999946235896 ) ) ;
#20598=AXIS2_PLACEMENT_3D ( 'NONE', #37265, #26280, #8033 ) ;
#20601=CARTESIAN_POINT ( 'NONE',  ( 0.6971942568897626646, -0.07405724077823297447, 0.3986220471903312301 ) ) ;
#20604=CARTESIAN_POINT ( 'NONE',  ( -0.9873396505805591694, -0.1113553986120547346, 0.7824803148531023211 ) ) ;
#20605=CARTESIAN_POINT ( 'NONE',  ( -0.8107537697050253289, 0.1574803149606300301, 0.7308070866141725963 ) ) ;
#20608=CARTESIAN_POINT ( 'NONE',  ( 0.8019270111902717657, -0.1787899950787401604, 0.8759842519147408302 ) ) ;
#20610=EDGE_CURVE ( 'NONE', #32499, #43205, #10770, .T. ) ;
#20611=DIRECTION ( 'NONE',  ( 0.000000000000000000, 0.000000000000000000, -1.000000000000000000 ) ) ;
#20612=CARTESIAN_POINT ( 'NONE',  ( 0.7495606340400177148, -0.1264236179284866091, 1.980807086560409491 ) ) ;
#20614=ORIENTED_EDGE ( 'NONE', *, *, #38037, .T. ) ;
#20615=CARTESIAN_POINT ( 'NONE',  ( 0.7185039370078741827, 0.06523048226347841205, 0.7258858266641272650 ) ) ;
#20618=CARTESIAN_POINT ( 'NONE',  ( 1.054774247047244096, 0.000000000000000000, 0.3420275590013546751 ) ) ;
#20620=CARTESIAN_POINT ( 'NONE',  ( -0.6971942568897648851, 0.07405724077823318263, 1.968503936954110189 ) ) ;
#20622=CARTESIAN_POINT ( 'NONE',  ( -1.054774247047244540, 0.07405724077823318263, 1.407480314906865981 ) ) ;
#20623=CARTESIAN_POINT ( 'NONE',  ( 0.8019270111902717657, -0.1787899950787401604, 1.353346456639149986 ) ) ;
#20626=CARTESIAN_POINT ( 'NONE',  ( -0.6971942568897637749, 2.189545951927499583E-17, 0.7160433070328504623 ) ) ;
#20628=CARTESIAN_POINT ( 'NONE',  ( -1.033464566929134687, 0.06523048226347956391, 1.616633858160190229 ) ) ;
#20629=CARTESIAN_POINT ( 'NONE',  ( 0.8759842519685039353, -0.1787899950787401882, 0.6471456692375747721 ) ) ;
#20630=CARTESIAN_POINT ( 'NONE',  ( -1.054774247047244540, 0.07405724077823318263, 0.4970472440407249226 ) ) ;
#20633=CARTESIAN_POINT ( 'NONE',  ( 0.9873396505805591694, 0.1113553986120547346, 1.658464566821606256 ) ) ;
#20636=CARTESIAN_POINT ( 'NONE',  ( -0.7646288533564489232, -0.1113553986120547346, 0.5068897637795275468 ) ) ;
#20638=CARTESIAN_POINT ( 'NONE',  ( 1.002407869896990045, -0.1264236179284866091, 1.242618110182456714 ) ) ;
#20642=CARTESIAN_POINT ( 'NONE',  ( -0.9500414927467378812, -0.1787899950787401604, 1.003937007820251193 ) ) ;
#20647=CARTESIAN_POINT ( 'NONE',  ( 0.7185039370078746268, 0.06523048226347956391, 0.4995078740157475883 ) ) ;
#20653=CARTESIAN_POINT ( 'NONE',  ( -0.8107537697050254399, -0.1574803149606297803, 0.9719488187901104137 ) ) ;
#20656=FACE_OUTER_BOUND ( 'NONE', #25409, .T. ) ;
#20657=CARTESIAN_POINT ( 'NONE',  ( 1.002407869896990045, -0.1264236179284866091, 0.4502952755367874427 ) ) ;
#20659=AXIS2_PLACEMENT_3D ( 'NONE', #12723, #38329, #31638 ) ;
#20660=CARTESIAN_POINT ( 'NONE',  ( -1.002407869896990045, -0.1264236179284866091, 0.8489173227808819444 ) ) ;
#20661=EDGE_CURVE ( 'NONE', #18242, #40994, #17182, .T. ) ;
#20662=CARTESIAN_POINT ( 'NONE',  ( -1.033464566929133799, 0.000000000000000000, 1.299212598317669221 ) ) ;
#20668=CARTESIAN_POINT ( 'NONE',  ( -0.7646288533564489232, -0.1113553986120547346, 1.245078740049952559 ) ) ;
#20669=CARTESIAN_POINT ( 'NONE',  ( 1.054774247047244096, 0.000000000000000000, 1.444389763725763665 ) ) ;
#20670=CARTESIAN_POINT ( 'NONE',  ( 0.9500414927467377701, 0.1787899950787401604, 1.958661417269071947 ) ) ;
#20672=CARTESIAN_POINT ( 'NONE',  ( 0.8759842519685039353, -0.1787899950787401882, 0.3272637794737956463 ) ) ;
#20677=DIRECTION ( 'NONE',  ( 1.000000000000000000, 0.000000000000000000, 0.000000000000000000 ) ) ;
#20680=CARTESIAN_POINT ( 'NONE',  ( 0.9500414927467378812, -0.1787899950787401604, 0.5659448818360001132 ) ) ;
#20682=CARTESIAN_POINT ( 'NONE',  ( 0.7593162293221857873, -0.1180121082641624880, 0.03937054915593885679 ) ) ;
#20683=CARTESIAN_POINT ( 'NONE',  ( -0.9873396505805591694, -0.1113553986120547346, 0.9399606298137322957 ) ) ;
#20685=CARTESIAN_POINT ( 'NONE',  ( -0.6971942568897648851, 0.07405724077823318263, 1.417322834591906222 ) ) ;
#20686=ORIENTED_EDGE ( 'NONE', *, *, #37025, .F. ) ;
#20687=DIRECTION ( 'NONE',  ( 1.822029033848725028E-16, 0.000000000000000000, 1.000000000000000000 ) ) ;
#20688=CARTESIAN_POINT ( 'NONE',  ( 0.8759842519685039353, -0.1787899950787401882, 1.001476377898992132 ) ) ;
#20689=CARTESIAN_POINT ( 'NONE',  ( -1.033464566929134687, 0.06523048226347956391, 0.5536417321759372623 ) ) ;
#20691=CARTESIAN_POINT ( 'NONE',  ( -1.054774247047244096, 0.000000000000000000, 0.8882874015210394658 ) ) ;
#20692=CARTESIAN_POINT ( 'NONE',  ( -1.033464566929133799, 0.000000000000000000, 0.5118110235145196807 ) ) ;
#20693=CARTESIAN_POINT ( 'NONE',  ( 1.054774247047244096, 0.000000000000000000, 0.1451771653005673179 ) ) ;
#20694=CARTESIAN_POINT ( 'NONE',  ( -0.7495606340400177148, -0.1264236179284866091, 0.08612204719033110523 ) ) ;
#20695=CARTESIAN_POINT ( 'NONE',  ( 0.9412147342319837628, 0.1574803149606300301, 1.345964566821607589 ) ) ;
#20699=CARTESIAN_POINT ( 'NONE',  ( -0.6971942568897648851, 0.07405724077823318263, 1.732283464513166615 ) ) ;
#20703=CARTESIAN_POINT ( 'NONE',  ( -0.8759842519685039353, -0.1574803149606299191, 0.7874015748031496509 ) ) ;
#20709=ORIENTED_EDGE ( 'NONE', *, *, #17582, .T. ) ;
#20710=EDGE_CURVE ( 'NONE', #36693, #37979, #14994, .T. ) ;
#20711=CARTESIAN_POINT ( 'NONE',  ( 0.9412147342319837628, 0.1574803149606300301, 1.739665354223181470 ) ) ;
#20712=CARTESIAN_POINT ( 'NONE',  ( -1.033464566929133799, 1.928577636452524610E-17, 2.869337061179095023E-17 ) ) ;
#20713=CARTESIAN_POINT ( 'NONE',  ( 0.8107537697050253289, 0.1574803149606300301, 1.793799212598424342 ) ) ;
#20716=CARTESIAN_POINT ( 'NONE',  ( -0.7185039370078739607, 1.928577636452523993E-17, 1.053149606299212504 ) ) ;
#20720=CARTESIAN_POINT ( 'NONE',  ( 1.054774247047244096, 0.000000000000000000, 1.011318897584031484 ) ) ;
#20721=CARTESIAN_POINT ( 'NONE',  ( 0.7495606340400177148, -0.1264236179284866091, 1.582185039316315045 ) ) ;
#20723=CARTESIAN_POINT ( 'NONE',  ( 0.9873396505805591694, 0.1113553986120547346, 1.668307086614173373 ) ) ;
#20724=CARTESIAN_POINT ( 'NONE',  ( 0.8314579112631774738, 0.1526854885466115419, 1.979225999458145813 ) ) ;
#20728=CARTESIAN_POINT ( 'NONE',  ( 0.7646288533564489232, 0.1113553986120547346, 0.6840551180027086842 ) ) ;
#20730=CARTESIAN_POINT ( 'NONE',  ( -1.033464566929133799, 0.000000000000000000, 1.653543306979086580 ) ) ;
#20732=DIRECTION ( 'NONE',  ( 1.000000000000000000, 0.000000000000000000, -1.822029033848725275E-16 ) ) ;
#20733=CARTESIAN_POINT ( 'NONE',  ( 0.6971942568897648851, -0.07405724077823297447, 1.067913385773007651 ) ) ;
#20735=CARTESIAN_POINT ( 'NONE',  ( 0.8759842519685039353, -0.1574803149606299191, 0.5413385825696385156 ) ) ;
#20736=ORIENTED_EDGE ( 'NONE', *, *, #37998, .T. ) ;
#20738=CARTESIAN_POINT ( 'NONE',  ( 0.9873396505805591694, 0.1113553986120547346, 0.2509842519685039353 ) ) ;
#20739=CARTESIAN_POINT ( 'NONE',  ( -0.9412147342319837628, 0.1574803149606300301, 0.2829724408373550104 ) ) ;
#20740=ORIENTED_EDGE ( 'NONE', *, *, #1082, .T. ) ;
#20741=CARTESIAN_POINT ( 'NONE',  ( 0.8759842519685039353, -0.1787899950787401882, 1.232775590497417362 ) ) ;
#20743=DIRECTION ( 'NONE',  ( -1.000000000000000000, 0.000000000000000000, 0.000000000000000000 ) ) ;
#20745=CARTESIAN_POINT ( 'NONE',  ( 0.8759842519685039353, 0.1574803149606299191, 0.4429133857192448787 ) ) ;
#20748=LINE ( 'NONE', #12882, #17721 ) ;
#20749=ORIENTED_EDGE ( 'NONE', *, *, #35980, .F. ) ;
#20750=CARTESIAN_POINT ( 'NONE',  ( -1.054774247047244540, -0.07405724077823318263, 1.358267716481669662 ) ) ;
#20752=CARTESIAN_POINT ( 'NONE',  ( -0.8759842519685039353, 0.1787899950787401882, 0.9817913385289134265 ) ) ;
#20753=CARTESIAN_POINT ( 'NONE',  ( -1.054774247047244540, 0.07405724077823318263, 1.914370078686394860 ) ) ;
#20755=CARTESIAN_POINT ( 'NONE',  ( -0.7495606340400177148, -0.1264236179284866091, 0.6422244093950550958 ) ) ;
#20758=CARTESIAN_POINT ( 'NONE',  ( -0.9412147342319837628, 0.1574803149606300301, 0.08612204713656733401 ) ) ;
#20760=CARTESIAN_POINT ( 'NONE',  ( -1.033464566929133799, 0.000000000000000000, 1.456692913278299084 ) ) ;
#20762=ORIENTED_EDGE ( 'NONE', *, *, #9766, .F. ) ;
#20766=EDGE_CURVE ( 'NONE', #22060, #23610, #45009, .T. ) ;
#20768=CARTESIAN_POINT ( 'NONE',  ( -0.8019270111902717657, -0.1787899950787401604, 0.6397637794737947026 ) ) ;
#20769=CARTESIAN_POINT ( 'NONE',  ( 0.7185039370078739607, 1.928577636452523993E-17, 1.358267716427907779 ) ) ;
#20771=ORIENTED_EDGE ( 'NONE', *, *, #37662, .F. ) ;
#20775=CARTESIAN_POINT ( 'NONE',  ( -0.9412147342319837628, -0.1574803149606297803, 0.1894685038294807999 ) ) ;
#20777=CARTESIAN_POINT ( 'NONE',  ( 0.8759842519685039353, 0.1574803149606299191, 0.6102362204724409711 ) ) ;
#20778=CARTESIAN_POINT ( 'NONE',  ( 0.8107537697050254399, 0.1574803149606300301, 0.6422244093412927679 ) ) ;
#20779=CARTESIAN_POINT ( 'NONE',  ( 1.054774247047244096, 0.000000000000000000, 0.6569881889226141247 ) ) ;
#20783=ORIENTED_EDGE ( 'NONE', *, *, #251, .F. ) ;
#20785=CARTESIAN_POINT ( 'NONE',  ( 0.8107537697050253289, 0.1574803149606300301, 1.203248031496062520 ) ) ;
#20787=CARTESIAN_POINT ( 'NONE',  ( 0.8107537697050254399, -0.1574803149606297803, 1.847933070866142780 ) ) ;
#20788=( BOUNDED_CURVE ( )  B_SPLINE_CURVE ( 2, ( #11440, #38480, #9008, #1813, #12863, #5651, #41809, #19556, #20261 ),
 .UNSPECIFIED., .F., .T. ) 
 B_SPLINE_CURVE_WITH_KNOTS ( ( 3, 2, 2, 2, 3 ),
 ( 0.2099999999999999922, 0.2124999999999999944, 0.2149999999999999967, 0.2174999999999999989, 0.2200000000000000011 ),
 .UNSPECIFIED. ) 
 CURVE ( )  GEOMETRIC_REPRESENTATION_ITEM ( )  RATIONAL_B_SPLINE_CURVE ( ( 1.000000000000000000, 0.9238795325112869605, 1.000000000000000000, 0.9238795325112869605, 1.000000000000000000, 0.9238795325112869605, 1.000000000000000000, 0.9238795325112869605, 1.000000000000000000 ) ) 
 REPRESENTATION_ITEM ( '' )  ) ;
#20790=CARTESIAN_POINT ( 'NONE',  ( 0.6971942568897648851, 0.07405724077823318263, 0.7480314960092282472 ) ) ;
#20799=CARTESIAN_POINT ( 'NONE',  ( 1.054774247047244540, 0.07405724077823318263, 0.8907480314422986378 ) ) ;
#20800=FACE_OUTER_BOUND ( 'NONE', #202, .T. ) ;
#20801=CARTESIAN_POINT ( 'NONE',  ( -0.7646288533564489232, 0.1113553986120547346, 0.5364173228346457156 ) ) ;
#20805=CARTESIAN_POINT ( 'NONE',  ( 0.9873396505805591694, 0.1113553986120547346, 1.225393700679874076 ) ) ;
#20807=ADVANCED_FACE ( 'NONE', ( #45664 ), #33012, .T. ) ;
#20808=CARTESIAN_POINT ( 'NONE',  ( -1.054774247047244096, 0.000000000000000000, 1.838090551127338657 ) ) ;
#20809=CARTESIAN_POINT ( 'NONE',  ( -0.9412147342319837628, -0.1574803149606297803, 0.8193897636719996713 ) ) ;
#20812=CARTESIAN_POINT ( 'NONE',  ( -0.6971942568897648851, -0.07405724077823297447, 1.899606299158834943 ) ) ;
#20813=CARTESIAN_POINT ( 'NONE',  ( -0.8759842519685039353, -0.1787899950787401882, 1.508366141678519678 ) ) ;
#20815=CARTESIAN_POINT ( 'NONE',  ( -1.054774247047244540, 0.07405724077823318263, 1.008858267662772423 ) ) ;
#20816=CARTESIAN_POINT ( 'NONE',  ( -0.8019270111902717657, 0.1787899950787401604, 0.1968503936470238913 ) ) ;
#20817=( BOUNDED_CURVE ( )  B_SPLINE_CURVE ( 2, ( #25747, #39848, #47051, #21898, #7037, #10417, #25017, #21663, #36521 ),
 .UNSPECIFIED., .F., .T. ) 
 B_SPLINE_CURVE_WITH_KNOTS ( ( 3, 2, 2, 2, 3 ),
 ( 0.6600000000000000311, 0.6624999999999999778, 0.6650000000000000355, 0.6674999999999999822, 0.6700000000000000400 ),
 .UNSPECIFIED. ) 
 CURVE ( )  GEOMETRIC_REPRESENTATION_ITEM ( )  RATIONAL_B_SPLINE_CURVE ( ( 1.000000000000000000, 0.9238795325112869605, 1.000000000000000000, 0.9238795325112869605, 1.000000000000000000, 0.9238795325112869605, 1.000000000000000000, 0.9238795325112869605, 1.000000000000000000 ) ) 
 REPRESENTATION_ITEM ( '' )  ) ;
#20819=CARTESIAN_POINT ( 'NONE',  ( -0.7495606340400177148, 0.1264236179284866091, 1.970964566875370139 ) ) ;
#20820=CARTESIAN_POINT ( 'NONE',  ( -0.8759842519685039353, 0.1574803149606299191, 1.830708661417322913 ) ) ;
#20821=DIRECTION ( 'NONE',  ( -1.000000000000000000, 0.000000000000000000, 0.000000000000000000 ) ) ;
#20831=AXIS2_PLACEMENT_3D ( 'NONE', #1761, #2234, #34373 ) ;
#20839=CARTESIAN_POINT ( 'NONE',  ( -1.033464566929134687, 0.06523048226347956391, 0.7504921258767240921 ) ) ;
#20840=CARTESIAN_POINT ( 'NONE',  ( -0.7646288533564489232, 0.1113553986120547346, 0.7726377952755906220 ) ) ;
#20842=CARTESIAN_POINT ( 'NONE',  ( 1.033464566929134687, -0.06523048226347956391, 0.7554133858267707557 ) ) ;
#20844=CARTESIAN_POINT ( 'NONE',  ( -0.8107537697050254399, 0.1574803149606300301, 1.085137795275590955 ) ) ;
#20847=CARTESIAN_POINT ( 'NONE',  ( 0.9412147342319837628, -0.1574803149606297803, 0.1107283463491660208 ) ) ;
#20848=EDGE_LOOP ( 'NONE', ( #38883, #9157, #25480, #14705 ) ) ;
#20854=VERTEX_POINT ( 'NONE', #16927 ) ;
#20855=CARTESIAN_POINT ( 'NONE',  ( -0.6971942568897648851, 0.07405724077823318263, 1.422244094434426120 ) ) ;
#20856=CARTESIAN_POINT ( 'NONE',  ( 0.8759842519685039353, -0.1787899950787401882, 1.513287401521039355 ) ) ;
#20857=ORIENTED_EDGE ( 'NONE', *, *, #23701, .T. ) ;
#20858=CARTESIAN_POINT ( 'NONE',  ( 0.7185039370078746268, -0.06523048226347956391, 0.9276574802074332160 ) ) ;
#20859=CARTESIAN_POINT ( 'NONE',  ( -1.002407869896990045, -0.1264236179284866091, 0.5733267715997795166 ) ) ;
#20860=AXIS2_PLACEMENT_3D ( 'NONE', #25692, #32652, #10835 ) ;
#20862=CARTESIAN_POINT ( 'NONE',  ( 0.8759842519685039353, -0.1787899950787401882, 0.1353346456155279653 ) ) ;
#20863=CARTESIAN_POINT ( 'NONE',  ( 1.054774247047244540, 0.07405724077823318263, 0.6594488188438737408 ) ) ;
#20864=CARTESIAN_POINT ( 'NONE',  ( -1.054774247047244540, 0.07405724077823318263, 0.5364173227808820554 ) ) ;
#20866=PLANE ( 'NONE',  #41257 ) ;
#20869=CARTESIAN_POINT ( 'NONE',  ( -0.8759842519685039353, -0.1787899950787401882, 1.395177165300567124 ) ) ;
#20870=CARTESIAN_POINT ( 'NONE',  ( -1.033464566929134687, -0.06523048226347956391, 1.464074803149607140 ) ) ;
#20872=CARTESIAN_POINT ( 'NONE',  ( -0.7185039370078746268, 0.06523048226347956391, 0.4995078740157484765 ) ) ;
#20873=CARTESIAN_POINT ( 'NONE',  ( 0.8019270111902716547, 0.1787899950787401604, 1.377952755851748368 ) ) ;
#20877=EDGE_CURVE ( 'NONE', #11036, #21900, #20748, .T. ) ;
#20880=LINE ( 'NONE', #36174, #33470 ) ;
#20882=CARTESIAN_POINT ( 'NONE',  ( 1.033464566929136907, -0.06523048226347749612, 1.621555118110237670 ) ) ;
#20884=ORIENTED_EDGE ( 'NONE', *, *, #27375, .F. ) ;
#20885=CARTESIAN_POINT ( 'NONE',  ( 0.6971942568897648851, 0.07405724077823318263, 1.417322834591906222 ) ) ;
#20886=EDGE_CURVE ( 'NONE', #6712, #9090, #2072, .T. ) ;
#20892=CARTESIAN_POINT ( 'NONE',  ( 0.9500414927467378812, -0.1787899950787401604, 0.3297244093950552069 ) ) ;
#20893=CARTESIAN_POINT ( 'NONE',  ( 1.033464566929133799, 0.000000000000000000, 1.062992125876724314 ) ) ;
#20898=AXIS2_PLACEMENT_3D ( 'NONE', #44193, #25780, #3943 ) ;
#20899=CARTESIAN_POINT ( 'NONE',  ( -1.054774247047244096, 0.000000000000000000, 0.7750984251430865779 ) ) ;
#20903=DIRECTION ( 'NONE',  ( 0.000000000000000000, 0.000000000000000000, -1.000000000000000000 ) ) ;
#20904=CARTESIAN_POINT ( 'NONE',  ( 1.054774247047244540, 0.07405724077823318263, 1.722440944828125930 ) ) ;
#20905=CARTESIAN_POINT ( 'NONE',  ( 0.8759842519685039353, 0.1787899950787401882, 1.961122047190330786 ) ) ;
#20907=CARTESIAN_POINT ( 'NONE',  ( 0.8019270111902716547, -0.1787899950787401604, 0.4035433070328507954 ) ) ;
#20908=EDGE_LOOP ( 'NONE', ( #38815, #7383, #9685, #32051 ) ) ;
#20910=CARTESIAN_POINT ( 'NONE',  ( 0.8759842519685039353, 0.000000000000000000, 4.498031496062992574 ) ) ;
#20912=CARTESIAN_POINT ( 'NONE',  ( 0.6971942568897626646, -0.07405724077823297447, 0.5561023621509617598 ) ) ;
#20915=CARTESIAN_POINT ( 'NONE',  ( 0.9412147342319837628, -0.1574803149606297803, 0.08120078740157483932 ) ) ;
#20916=CARTESIAN_POINT ( 'NONE',  ( -0.7185039370078766252, -0.06523048226348168721, 1.518208661309796481 ) ) ;
#20917=CARTESIAN_POINT ( 'NONE',  ( -1.054774247047244540, 0.07405724077823318263, 1.441929133804504604 ) ) ;
#20920=CARTESIAN_POINT ( 'NONE',  ( 0.8019270111902717657, -0.1787899950787401604, 1.156496062938362046 ) ) ;
#20921=CARTESIAN_POINT ( 'NONE',  ( -0.8107537697050253289, -0.1574803149606297803, 0.6569881888688503535 ) ) ;
#20922=CARTESIAN_POINT ( 'NONE',  ( 1.054774247047244096, 0.000000000000000000, 1.872539370024976391 ) ) ;
#20923=CARTESIAN_POINT ( 'NONE',  ( -0.7185039370078746268, 0.06523048226347956391, 1.444389763779527991 ) ) ;
#20924=CARTESIAN_POINT ( 'NONE',  ( -0.8759842519685039353, 0.1787899950787401882, 0.8981299212060788184 ) ) ;
#20926=CARTESIAN_POINT ( 'NONE',  ( -0.8212486197303469071, -0.1522654806920532289, 0.03937007874015844427 ) ) ;
#20927=CARTESIAN_POINT ( 'NONE',  ( 1.002407869896990045, 0.1264236179284866091, 0.07135826766277185429 ) ) ;
#20928=CARTESIAN_POINT ( 'NONE',  ( 0.7185039370078739607, 1.928577636452523993E-17, 1.555118110128692832 ) ) ;
#20929=VERTEX_POINT ( 'NONE', #30872 ) ;
#20931=DIRECTION ( 'NONE',  ( -0.8660254037844389297, -1.060575238724907285E-16, -0.4999999999999994449 ) ) ;
#20934=CARTESIAN_POINT ( 'NONE',  ( -0.7495606340400177148, -0.1264236179284866091, 1.621555118056472455 ) ) ;
#20942=CARTESIAN_POINT ( 'NONE',  ( 1.054774247047244096, 0.000000000000000000, 1.085137795221826629 ) ) ;
#20946=CARTESIAN_POINT ( 'NONE',  ( 0.8759842519685039353, 0.1574803149606299191, 1.870078740157480324 ) ) ;
#20947=CARTESIAN_POINT ( 'NONE',  ( -0.6971942568897648851, -0.07405724077823297447, 0.3641732282926931630 ) ) ;
#20951=CARTESIAN_POINT ( 'NONE',  ( 0.6971942568897648851, -0.07405724077823297447, 1.112204724355684959 ) ) ;
#20952=CARTESIAN_POINT ( 'NONE',  ( 1.054774247047244096, 0.000000000000000000, 1.596948818843874074 ) ) ;
#20954=CARTESIAN_POINT ( 'NONE',  ( 0.8107537697050254399, 0.1574803149606300301, 1.715059055118110631 ) ) ;
#20955=CARTESIAN_POINT ( 'NONE',  ( 1.033464566929133799, 0.000000000000000000, 0.7874015746956221085 ) ) ;
#20956=CARTESIAN_POINT ( 'NONE',  ( -0.7646288533564489232, -0.1113553986120547346, 1.796259842412157415 ) ) ;
#20958=CARTESIAN_POINT ( 'NONE',  ( 1.002407869896990045, 0.1264236179284866091, 0.1845472440407248116 ) ) ;
#20960=CARTESIAN_POINT ( 'NONE',  ( 0.6971942568897648851, -0.07405724077823297447, 1.146653543253323582 ) ) ;
#20961=CARTESIAN_POINT ( 'NONE',  ( -0.7185039370078739607, 1.928577636452523993E-17, 1.958661417322834719 ) ) ;
#20962=CARTESIAN_POINT ( 'NONE',  ( 1.054774247047244540, -0.07405724077823318263, 1.953740157426552715 ) ) ;
#20963=CARTESIAN_POINT ( 'NONE',  ( 0.8107537697050253289, -0.1574803149606297803, 0.4995078739082208230 ) ) ;
#20965=AXIS2_PLACEMENT_3D ( 'NONE', #1203, #30713, #12964 ) ;
#20966=CARTESIAN_POINT ( 'NONE',  ( -0.8759842519685039353, 0.1574803149606299191, 1.122047244094488194 ) ) ;
#20967=CARTESIAN_POINT ( 'NONE',  ( -0.7185039370078739607, 1.928577636452523993E-17, 0.3346456691838114450 ) ) ;
#20968=CARTESIAN_POINT ( 'NONE',  ( -0.7185039370078739607, 1.928577636452523993E-17, 1.525590551181102317 ) ) ;
#20969=CARTESIAN_POINT ( 'NONE',  ( 1.002407869896990045, 0.1264236179284866091, 1.286909448765133801 ) ) ;
#20970=CARTESIAN_POINT ( 'NONE',  ( 1.033464566929133799, 0.000000000000000000, 0.9842519683964094934 ) ) ;
#20971=CARTESIAN_POINT ( 'NONE',  ( -0.9412147342319837628, 0.1574803149606300301, 0.2829724408373550104 ) ) ;
#20977=ORIENTED_EDGE ( 'NONE', *, *, #36302, .T. ) ;
#20978=CARTESIAN_POINT ( 'NONE',  ( 0.8019270111902717657, -0.1787899950787401604, 0.4084645668753704717 ) ) ;
#20980=ORIENTED_EDGE ( 'NONE', *, *, #36215, .T. ) ;
#20983=CARTESIAN_POINT ( 'NONE',  ( -1.002407869896990045, 0.1264236179284866091, 1.956200787347811110 ) ) ;
#20984=CARTESIAN_POINT ( 'NONE',  ( -0.9500414927467377701, -0.1787899950787401604, 1.077755905458048113 ) ) ;
#20985=CARTESIAN_POINT ( 'NONE',  ( -1.054774247047244540, -0.07405724077823318263, 0.7332677164816707727 ) ) ;
#20992=AXIS2_PLACEMENT_3D ( 'NONE', #16898, #44868, #12080 ) ;
#20994=CARTESIAN_POINT ( 'NONE',  ( 0.7185039370078739607, 1.928577636452523993E-17, 0.7775590551181102983 ) ) ;
#20995=ADVANCED_FACE ( 'NONE', ( #25559 ), #18110, .T. ) ;
#20996=CARTESIAN_POINT ( 'NONE',  ( -0.8759842519685039353, 0.000000000000000000, 0.000000000000000000 ) ) ;
#20997=CARTESIAN_POINT ( 'NONE',  ( -0.9500414927467378812, -0.1787899950787401604, 0.6446850393163160442 ) ) ;
#21002=CARTESIAN_POINT ( 'NONE',  ( -0.6971942568897637749, 2.189545951927499583E-17, 1.621555118056472455 ) ) ;
#21004=CARTESIAN_POINT ( 'NONE',  ( 0.8107537697050254399, 0.1574803149606300301, 1.035925196742866650 ) ) ;
#21008=CARTESIAN_POINT ( 'NONE',  ( -0.8107537697050253289, 0.1574803149606300301, 1.429625984144440531 ) ) ;
#21009=CARTESIAN_POINT ( 'NONE',  ( 0.6971942568897626646, -0.07405724077823297447, 0.6791338582139527791 ) ) ;
#21014=CARTESIAN_POINT ( 'NONE',  ( 0.7185039370078739607, 1.928577636452523993E-17, 1.289370078740157632 ) ) ;
#21015=DIRECTION ( 'NONE',  ( 0.000000000000000000, 0.000000000000000000, -1.000000000000000000 ) ) ;
#21018=CARTESIAN_POINT ( 'NONE',  ( 0.8019270111902716547, -0.1787899950787401604, 0.6003937007336380693 ) ) ;
#21020=CARTESIAN_POINT ( 'NONE',  ( -0.7185039370078739607, 1.928577636452523993E-17, 0.6988188976377952555 ) ) ;
#21028=CARTESIAN_POINT ( 'NONE',  ( 0.9500414927467378812, -0.1787899950787401604, 0.8415354330171019859 ) ) ;
#21030=CARTESIAN_POINT ( 'NONE',  ( -1.033464566929133799, 0.000000000000000000, 0.7185039370078739607 ) ) ;
#21031=CYLINDRICAL_SURFACE ( 'NONE', #28929, 0.1574803149606299191 ) ;
#21035=CARTESIAN_POINT ( 'NONE',  ( 0.7185039370078739607, 1.928577636452523993E-17, 1.279527558947590515 ) ) ;
#21038=CARTESIAN_POINT ( 'NONE',  ( -0.8019270111902717657, -0.1787899950787401604, 1.943897637741510254 ) ) ;
#21041=EDGE_CURVE ( 'NONE', #8391, #15306, #2765, .T. ) ;
#21042=CARTESIAN_POINT ( 'NONE',  ( 0.8759842519685039353, 0.1787899950787401882, 1.926673228292693052 ) ) ;
#21043=ORIENTED_EDGE ( 'NONE', *, *, #43437, .T. ) ;
#21044=CARTESIAN_POINT ( 'NONE',  ( -0.8759842519685039353, 0.1787899950787401882, 1.926673228292693052 ) ) ;
#21045=CARTESIAN_POINT ( 'NONE',  ( -1.054774247047244096, 0.000000000000000000, 1.557578740103716441 ) ) ;
#21046=CARTESIAN_POINT ( 'NONE',  ( -0.8759842519685039353, -0.1787899950787401882, 1.035925196796629866 ) ) ;
#21047=CARTESIAN_POINT ( 'NONE',  ( -0.9500414927467378812, 0.1787899950787401604, 0.1919291338045042428 ) ) ;
#21049=CARTESIAN_POINT ( 'NONE',  ( -0.8019270111902717657, -0.1787899950787401604, 1.904527559001354398 ) ) ;
#21051=CARTESIAN_POINT ( 'NONE',  ( -0.7185039370078746268, -0.06523048226347956391, 1.961122047244095778 ) ) ;
#21056=CARTESIAN_POINT ( 'NONE',  ( -0.8759842519685039353, 0.1787899950787401882, 0.1107283464029295283 ) ) ;
#21058=VECTOR ( 'NONE', #22772, 39.37007874015748143 ) ;
#21059=CARTESIAN_POINT ( 'NONE',  ( -0.6971942568897648851, -0.07405724077823297447, 1.269685039316314601 ) ) ;
#21060=VERTEX_POINT ( 'NONE', #17632 ) ;
#21065=( BOUNDED_CURVE ( )  B_SPLINE_CURVE ( 2, ( #11905, #34196, #15981, #8285, #30602, #34656, #45638, #37525, #45166 ),
 .UNSPECIFIED., .F., .T. ) 
 B_SPLINE_CURVE_WITH_KNOTS ( ( 3, 2, 2, 2, 3 ),
 ( 0.5500000000000000444, 0.5524999999999999911, 0.5550000000000000488, 0.5574999999999999956, 0.5600000000000000533 ),
 .UNSPECIFIED. ) 
 CURVE ( )  GEOMETRIC_REPRESENTATION_ITEM ( )  RATIONAL_B_SPLINE_CURVE ( ( 1.000000000000000000, 0.9238795325112869605, 1.000000000000000000, 0.9238795325112869605, 1.000000000000000000, 0.9238795325112869605, 1.000000000000000000, 0.9238795325112869605, 1.000000000000000000 ) ) 
 REPRESENTATION_ITEM ( '' )  ) ;
#21066=CARTESIAN_POINT ( 'NONE',  ( -0.7185039370078766252, -0.06523048226348168721, 1.360728346349167284 ) ) ;
#21069=CARTESIAN_POINT ( 'NONE',  ( -0.8107537697050253289, -0.1574803149606297803, 0.8932086613097963701 ) ) ;
#21070=CARTESIAN_POINT ( 'NONE',  ( -0.7646288533564489232, 0.1113553986120547346, 0.7332677165354331006 ) ) ;
#21072=CARTESIAN_POINT ( 'NONE',  ( 1.033464566929134687, 0.06523048226347956391, 1.813484251860976393 ) ) ;
#21074=CARTESIAN_POINT ( 'NONE',  ( 0.7185039370078739607, 1.928577636452523993E-17, 0.8562992125984251190 ) ) ;
#21079=CARTESIAN_POINT ( 'NONE',  ( 1.033464566929134687, 0.06523048226347956391, 0.1993110235145201248 ) ) ;
#21086=( BOUNDED_CURVE ( )  B_SPLINE_CURVE ( 2, ( #19769, #8270, #26512, #23138, #44673, #31059, #45623, #16193, #12126 ),
 .UNSPECIFIED., .F., .F. ) 
 B_SPLINE_CURVE_WITH_KNOTS ( ( 3, 2, 2, 2, 3 ),
 ( 0.9300000000000000488, 0.9324999999999999956, 0.9350000000000000533, 0.9375000000000000000, 0.9399999999999999467 ),
 .UNSPECIFIED. ) 
 CURVE ( )  GEOMETRIC_REPRESENTATION_ITEM ( )  RATIONAL_B_SPLINE_CURVE ( ( 1.000000000000000000, 0.9238795325112899581, 1.000000000000000000, 0.9238795325112869605, 1.000000000000000000, 0.9238795325112869605, 1.000000000000000000, 0.9238795325112829637, 1.000000000000000000 ) ) 
 REPRESENTATION_ITEM ( '' )  ) ;
#21089=CARTESIAN_POINT ( 'NONE',  ( -0.6971942568897648851, 0.07405724077823318263, 1.889763779473794258 ) ) ;
#21091=EDGE_LOOP ( 'NONE', ( #18526, #35846, #25306, #17762 ) ) ;
#21092=CARTESIAN_POINT ( 'NONE',  ( -0.6971942568897648851, -0.07405724077823297447, 1.387795275536786610 ) ) ;
#21096=CARTESIAN_POINT ( 'NONE',  ( -0.9500414927467378812, -0.1787899950787401604, 0.6102362204186774219 ) ) ;
#21098=CARTESIAN_POINT ( 'NONE',  ( -0.8759842519685039353, 0.000000000000000000, 0.000000000000000000 ) ) ;
#21099=CARTESIAN_POINT ( 'NONE',  ( 1.002407869896990045, 0.1264236179284866091, 0.7800196849856062542 ) ) ;
#21100=CARTESIAN_POINT ( 'NONE',  ( -0.9500414927467377701, -0.1787899950787401604, 0.4872047243556847929 ) ) ;
#21102=CARTESIAN_POINT ( 'NONE',  ( 0.8107537697050254399, -0.1574803149606297803, 1.139271653543306506 ) ) ;
#21104=CARTESIAN_POINT ( 'NONE',  ( -0.6971942568897648851, 0.07405724077823318263, 1.500984251914741607 ) ) ;
#21105=CARTESIAN_POINT ( 'NONE',  ( -0.9873396505805591694, -0.1113553986120547346, 1.461614173228346525 ) ) ;
#21106=CARTESIAN_POINT ( 'NONE',  ( -1.033464566929133799, 0.000000000000000000, 0.4822834645669291653 ) ) ;
#21107=CARTESIAN_POINT ( 'NONE',  ( 0.6971942568897637749, 2.189545951927499583E-17, 1.306594488135212728 ) ) ;
#21113=ORIENTED_EDGE ( 'NONE', *, *, #21177, .F. ) ;
#21115=CARTESIAN_POINT ( 'NONE',  ( 0.7185039370078739607, 0.000000000000000000, 4.498031496062992574 ) ) ;
#21117=CARTESIAN_POINT ( 'NONE',  ( 0.8019270111902717657, -0.1787899950787401604, 1.387795275536786610 ) ) ;
#21120=DIRECTION ( 'NONE',  ( 0.000000000000000000, 0.000000000000000000, -1.000000000000000000 ) ) ;
#21125=CARTESIAN_POINT ( 'NONE',  ( 0.6971942568897626646, -0.07405724077823297447, 0.2805118109698587214 ) ) ;
#21128=CARTESIAN_POINT ( 'NONE',  ( -0.7185039370078739607, 1.928577636452523993E-17, 0.1870078740157480324 ) ) ;
#21129=CARTESIAN_POINT ( 'NONE',  ( -0.8759842519685039353, -0.1574803149606299191, 1.486220472333417142 ) ) ;
#21131=CARTESIAN_POINT ( 'NONE',  ( 0.6971942568897626646, 0.07405724077823318263, 0.6299212597887560161 ) ) ;
#21132=CARTESIAN_POINT ( 'NONE',  ( -0.9500414927467377701, -0.1787899950787401604, 1.043307086560409269 ) ) ;
#21136=CARTESIAN_POINT ( 'NONE',  ( 1.002407869896990045, -0.1264236179284866091, 1.675688976324189117 ) ) ;
#21144=CARTESIAN_POINT ( 'NONE',  ( 1.054774247047244096, 0.000000000000000000, 0.6520669290800944484 ) ) ;
#21146=CARTESIAN_POINT ( 'NONE',  ( 0.7495606340400177148, -0.1264236179284866091, 0.1304133857730082613 ) ) ;
#21150=CARTESIAN_POINT ( 'NONE',  ( -0.9500414927467378812, 0.1787899950787401604, 1.486220472387181690 ) ) ;
#21153=CARTESIAN_POINT ( 'NONE',  ( -0.7185039370078739607, 1.928577636452523993E-17, 0.6496062991050708391 ) ) ;
#21154=CARTESIAN_POINT ( 'NONE',  ( 1.054774247047244096, 0.000000000000000000, 1.793799212544661348 ) ) ;
#21155=CARTESIAN_POINT ( 'NONE',  ( -0.7185039370078746268, -0.06523048226347956391, 1.331200787401575436 ) ) ;
#21156=CARTESIAN_POINT ( 'NONE',  ( -1.054774247047244096, 0.000000000000000000, 0.9670275590013542866 ) ) ;
#21158=CARTESIAN_POINT ( 'NONE',  ( -0.7646288533564489232, 0.1113553986120547346, 0.5265748030420794867 ) ) ;
#21160=CARTESIAN_POINT ( 'NONE',  ( 1.002407869896990045, -0.1264236179284866091, 0.3371062991588349989 ) ) ;
#21161=CARTESIAN_POINT ( 'NONE',  ( -0.9500414927467377701, -0.1787899950787401604, 0.09350393695411057804 ) ) ;
#21162=CARTESIAN_POINT ( 'NONE',  ( -0.9500414927467378812, -0.1787899950787401604, 0.5659448818360001132 ) ) ;
#21163=CARTESIAN_POINT ( 'NONE',  ( 0.7185039370078739607, 1.928577636452523993E-17, 1.515748031388535200 ) ) ;
#21166=CARTESIAN_POINT ( 'NONE',  ( 1.002407869896990045, -0.1264236179284866091, 0.7308070865604093802 ) ) ;
#21167=CARTESIAN_POINT ( 'NONE',  ( -1.002407869896990045, -0.1264236179284866091, 1.710137795221826851 ) ) ;
#21170=CARTESIAN_POINT ( 'NONE',  ( -0.8759842519685039353, 0.1574803149606299191, 0.6496062992125984925 ) ) ;
#21173=ORIENTED_EDGE ( 'NONE', *, *, #29973, .T. ) ;
#21177=EDGE_CURVE ( 'NONE', #47236, #27709, #28543, .T. ) ;
#21178=CARTESIAN_POINT ( 'NONE',  ( -0.9412147342319837628, 0.1574803149606300301, 0.9128937006798734100 ) ) ;
#21179=AXIS2_PLACEMENT_3D ( 'NONE', #23552, #12304, #19936 ) ;
#21180=CARTESIAN_POINT ( 'NONE',  ( 0.7185039370078746268, -0.06523048226347956391, 1.961122047244095778 ) ) ;
#21184=CARTESIAN_POINT ( 'NONE',  ( -1.054774247047244540, -0.07405724077823318263, 0.3395669290800949480 ) ) ;
#21187=CARTESIAN_POINT ( 'NONE',  ( 0.8019270111902716547, 0.1787899950787401604, 1.530511810969859221 ) ) ;
#21188=CARTESIAN_POINT ( 'NONE',  ( 0.6971942568897637749, 2.189545951927499583E-17, 0.1599409448281264023 ) ) ;
#21189=CARTESIAN_POINT ( 'NONE',  ( -0.8759842519685039353, 0.1574803149606299191, 1.909448818897637956 ) ) ;
#21190=CARTESIAN_POINT ( 'NONE',  ( 0.8107537697050253289, 0.1574803149606300301, 1.675688976377952777 ) ) ;
#21192=CARTESIAN_POINT ( 'NONE',  ( -0.9873396505805591694, 0.1113553986120547346, 0.9990157480314961758 ) ) ;
#21193=CARTESIAN_POINT ( 'NONE',  ( 0.7185039370078746268, 0.06523048226347956391, 1.719980314960630086 ) ) ;
#21194=CARTESIAN_POINT ( 'NONE',  ( 0.8107537697050254399, -0.1574803149606297803, 1.444389763672000671 ) ) ;
#21195=CYLINDRICAL_SURFACE ( 'NONE', #2184, 0.1574803149606299191 ) ;
#21196=CARTESIAN_POINT ( 'NONE',  ( -0.7185039370078739607, 1.928577636452523993E-17, 1.673228346349165285 ) ) ;
#21197=CARTESIAN_POINT ( 'NONE',  ( 1.002407869896990045, 0.1264236179284866091, 0.1451771653005673179 ) ) ;
#21198=( BOUNDED_CURVE ( )  B_SPLINE_CURVE ( 2, ( #29352, #21564, #14151, #28073, #36202, #39291, #17030, #39527, #17966 ),
 .UNSPECIFIED., .F., .T. ) 
 B_SPLINE_CURVE_WITH_KNOTS ( ( 3, 2, 2, 2, 3 ),
 ( 0.9100000000000000311, 0.9124999999999999778, 0.9150000000000000355, 0.9174999999999999822, 0.9200000000000000400 ),
 .UNSPECIFIED. ) 
 CURVE ( )  GEOMETRIC_REPRESENTATION_ITEM ( )  RATIONAL_B_SPLINE_CURVE ( ( 1.000000000000000000, 0.9238795325112899581, 1.000000000000000000, 0.9238795325112869605, 1.000000000000000000, 0.9238795325112869605, 1.000000000000000000, 0.9238795325112869605, 1.000000000000000000 ) ) 
 REPRESENTATION_ITEM ( '' )  ) ;
#21199=CARTESIAN_POINT ( 'NONE',  ( 0.7020444741911990860, 0.02838807324270386373, 0.03937007977071780435 ) ) ;
#21200=ADVANCED_FACE ( 'NONE', ( #35739 ), #9863, .T. ) ;
#21201=CARTESIAN_POINT ( 'NONE',  ( 1.054774247047244540, -0.07405724077823318263, 1.200787401521039355 ) ) ;
#21202=CARTESIAN_POINT ( 'NONE',  ( 0.8759842519685039353, -0.1787899950787401882, 1.906988188922614125 ) ) ;
#21203=CARTESIAN_POINT ( 'NONE',  ( 0.7646288533564489232, 0.1113553986120547346, 0.4872047243019220208 ) ) ;
#21206=CARTESIAN_POINT ( 'NONE',  ( 0.8905045487882523592, 0.1730449873529631977, 0.03937009343063418987 ) ) ;
#21207=CARTESIAN_POINT ( 'NONE',  ( -0.7185039370078746268, 0.06523048226347956391, 0.4109251967428667052 ) ) ;
#21209=CARTESIAN_POINT ( 'NONE',  ( 0.7495606340400177148, -0.1264236179284866091, 1.503444881836000002 ) ) ;
#21212=DIRECTION ( 'NONE',  ( 0.000000000000000000, 0.000000000000000000, -1.000000000000000000 ) ) ;
#21216=CYLINDRICAL_SURFACE ( 'NONE', #19149, 0.1574803149606299191 ) ;
#21217=VERTEX_POINT ( 'NONE', #27636 ) ;
#21218=CARTESIAN_POINT ( 'NONE',  ( -0.8759842519685039353, 0.000000000000000000, 0.000000000000000000 ) ) ;
#21221=CARTESIAN_POINT ( 'NONE',  ( 1.054774247047244096, 0.000000000000000000, 0.5782480314422993040 ) ) ;
#21222=CARTESIAN_POINT ( 'NONE',  ( -1.002407869896990045, 0.1264236179284866091, 1.326279527505291433 ) ) ;
#21225=CARTESIAN_POINT ( 'NONE',  ( -1.054774247047244540, -0.07405724077823318263, 1.205708661363558365 ) ) ;
#21226=CARTESIAN_POINT ( 'NONE',  ( -0.9412147342319837628, 0.1574803149606300301, 0.01722440944881892255 ) ) ;
#21228=CARTESIAN_POINT ( 'NONE',  ( -0.6971942568897637749, 2.189545951927499583E-17, 1.026082677111590513 ) ) ;
#21229=CARTESIAN_POINT ( 'NONE',  ( -1.002407869896990045, -0.1264236179284866091, 0.8095472440407244230 ) ) ;
#21230=CARTESIAN_POINT ( 'NONE',  ( -1.002407869896990045, -0.1264236179284866091, 0.1796259841982051075 ) ) ;
#21231=CARTESIAN_POINT ( 'NONE',  ( -0.7185039370078739607, 1.928577636452523993E-17, 0.3444881889763780070 ) ) ;
#21239=CARTESIAN_POINT ( 'NONE',  ( -1.054774247047244540, -0.07405724077823318263, 0.6496062991588353874 ) ) ;
#21243=CARTESIAN_POINT ( 'NONE',  ( -1.054774247047244540, 0.07405724077823318263, 1.643700787347811998 ) ) ;
#21249=CARTESIAN_POINT ( 'NONE',  ( 0.7185039370078746268, 0.06523048226347956391, 0.6176181102362200415 ) ) ;
#21251=DIRECTION ( 'NONE',  ( -1.000000000000000000, 0.000000000000000000, 0.000000000000000000 ) ) ;
#21252=CARTESIAN_POINT ( 'NONE',  ( -0.7646288533564489232, -0.1113553986120547346, 1.323818897530267602 ) ) ;
#21254=CARTESIAN_POINT ( 'NONE',  ( 0.9500414927467378812, 0.1787899950787401604, 0.7824803149068669805 ) ) ;
#21258=CARTESIAN_POINT ( 'NONE',  ( 0.7185039370078746268, -0.06523048226347956391, 1.331200787401575436 ) ) ;
#21259=CARTESIAN_POINT ( 'NONE',  ( 0.9335544921821857800, -0.1666633839053672239, 1.989226213591378301 ) ) ;
#21263=CARTESIAN_POINT ( 'NONE',  ( 0.9500414927467377701, -0.1787899950787401604, 0.6053149605761580787 ) ) ;
#21264=CARTESIAN_POINT ( 'NONE',  ( 0.7185039370078739607, 1.928577636452523993E-17, 0.2559055117034968463 ) ) ;
#21265=CARTESIAN_POINT ( 'NONE',  ( 0.7185039370078746268, 0.06523048226347956391, 1.562500000000000000 ) ) ;
#21267=CARTESIAN_POINT ( 'NONE',  ( 0.7185039370078760701, -0.06523048226348075740, 0.7012795275590564259 ) ) ;
#21268=CARTESIAN_POINT ( 'NONE',  ( 1.054774247047244096, 0.000000000000000000, 0.9670275590013542866 ) ) ;
#21270=CARTESIAN_POINT ( 'NONE',  ( 0.9873396505805591694, 0.1113553986120547346, 1.471456692913385877 ) ) ;
#21271=DIRECTION ( 'NONE',  ( 0.000000000000000000, 0.000000000000000000, -1.000000000000000000 ) ) ;
#21279=CARTESIAN_POINT ( 'NONE',  ( -0.8019270111902717657, -0.1787899950787401604, 0.04921259837143338034 ) ) ;
#21280=EDGE_LOOP ( 'NONE', ( #24020, #13642, #7805, #4754 ) ) ;
#21281=CARTESIAN_POINT ( 'NONE',  ( -0.6971942568897648851, -0.07405724077823297447, 1.938976377898990799 ) ) ;
#21282=CARTESIAN_POINT ( 'NONE',  ( -1.054774247047244096, 0.000000000000000000, 1.518208661363559031 ) ) ;
#21283=CARTESIAN_POINT ( 'NONE',  ( -0.8759842519685039353, 0.1787899950787401882, 1.094980314906866203 ) ) ;
#21284=VECTOR ( 'NONE', #34054, 39.37007874015748143 ) ;
#21286=CARTESIAN_POINT ( 'NONE',  ( -1.054774247047244540, 0.07405724077823318263, 1.879921259788756016 ) ) ;
#21287=CARTESIAN_POINT ( 'NONE',  ( -1.033464566929133799, 0.000000000000000000, 1.466535433070866201 ) ) ;
#21288=CARTESIAN_POINT ( 'NONE',  ( -1.033464566929133799, 0.000000000000000000, 1.860236220472440971 ) ) ;
#21291=DIRECTION ( 'NONE',  ( 0.000000000000000000, 0.000000000000000000, -1.000000000000000000 ) ) ;
#21293=CARTESIAN_POINT ( 'NONE',  ( -0.6971942568897626646, 0.07405724077823318263, 0.2362204723871814960 ) ) ;
#21294=EDGE_LOOP ( 'NONE', ( #26952, #39246, #37640, #26910 ) ) ;
#21295=CARTESIAN_POINT ( 'NONE',  ( -0.7495606340400177148, -0.1264236179284866091, 1.272145669237574772 ) ) ;
#21296=ORIENTED_EDGE ( 'NONE', *, *, #30947, .T. ) ;
#21300=VECTOR ( 'NONE', #32254, 39.37007874015748143 ) ;
#21303=CARTESIAN_POINT ( 'NONE',  ( -0.7646288533564489232, -0.1113553986120547346, 0.9301181101286929431 ) ) ;
#21304=CARTESIAN_POINT ( 'NONE',  ( -0.7185039370078746268, -0.06523048226347956391, 0.7012795275590552047 ) ) ;
#21305=EDGE_CURVE ( 'NONE', #23548, #22068, #36224, .T. ) ;
#21307=CARTESIAN_POINT ( 'NONE',  ( 1.033464566929134687, -0.06523048226347956391, 1.847933070758615015 ) ) ;
#21310=CARTESIAN_POINT ( 'NONE',  ( 0.7646288533564489232, -0.1113553986120547346, 0.7824803149606299746 ) ) ;
#21314=CARTESIAN_POINT ( 'NONE',  ( -0.7185039370078739607, 1.928577636452523993E-17, 1.446850393700787274 ) ) ;
#21315=CARTESIAN_POINT ( 'NONE',  ( 0.7646288533564489232, 0.1113553986120547346, 0.2509842518609771700 ) ) ;
#21317=ORIENTED_EDGE ( 'NONE', *, *, #20886, .F. ) ;
#21318=CARTESIAN_POINT ( 'NONE',  ( 0.7185039370078760701, -0.06523048226348075740, 0.8193897637795283240 ) ) ;
#21319=LINE ( 'NONE', #35950, #17180 ) ;
#21323=CARTESIAN_POINT ( 'NONE',  ( 0.7646288533564489232, -0.1113553986120547346, 0.9694881888688504645 ) ) ;
#21324=CARTESIAN_POINT ( 'NONE',  ( 0.8759842519685039353, 0.1574803149606299191, 0.5314960629921260393 ) ) ;
#21325=CARTESIAN_POINT ( 'NONE',  ( -0.7495606340400177148, -0.1264236179284866091, 0.3617125983714334359 ) ) ;
#21327=CARTESIAN_POINT ( 'NONE',  ( -0.9500414927467378812, -0.1787899950787401604, 1.594488188922613237 ) ) ;
#21329=CARTESIAN_POINT ( 'NONE',  ( 1.002407869896990045, -0.1264236179284866091, 1.557578740103716441 ) ) ;
#21331=CARTESIAN_POINT ( 'NONE',  ( -1.054774247047244540, -0.07405724077823318263, 0.5757874015210394658 ) ) ;
#21332=CARTESIAN_POINT ( 'NONE',  ( 0.9500414927467378812, 0.1787899950787401604, 0.1919291338045042428 ) ) ;
#21333=DIRECTION ( 'NONE',  ( -1.000000000000000000, 0.000000000000000000, 0.000000000000000000 ) ) ;
#21334=CARTESIAN_POINT ( 'NONE',  ( 0.8759842519685039353, -0.1787899950787401882, 0.7652559054580472253 ) ) ;
#21335=CARTESIAN_POINT ( 'NONE',  ( -0.7495606340400177148, 0.1264236179284866091, 0.7455708660879684091 ) ) ;
#21338=DIRECTION ( 'NONE',  ( 1.822029033848725028E-16, 0.000000000000000000, 1.000000000000000000 ) ) ;
#21340=CARTESIAN_POINT ( 'NONE',  ( -0.9500414927467378812, 0.1787899950787401604, 1.373031496009229135 ) ) ;
#21342=CARTESIAN_POINT ( 'NONE',  ( -1.033464566929134687, 0.06523048226347956391, 1.468996062992126150 ) ) ;
#21343=CARTESIAN_POINT ( 'NONE',  ( -0.7185039370078746268, 0.06523048226347956391, 0.3813976377952755237 ) ) ;
#21345=CARTESIAN_POINT ( 'NONE',  ( 0.9500414927467377701, -0.1787899950787401604, 1.515748031442299526 ) ) ;
#21347=ORIENTED_EDGE ( 'NONE', *, *, #30488, .T. ) ;
#21350=ORIENTED_EDGE ( 'NONE', *, *, #5250, .T. ) ;
#21352=ORIENTED_EDGE ( 'NONE', *, *, #16140, .T. ) ;
#21353=CARTESIAN_POINT ( 'NONE',  ( 0.8019270111902717657, 0.1787899950787401604, 1.412401574749386990 ) ) ;
#21357=ADVANCED_FACE ( 'NONE', ( #39772 ), #29058, .T. ) ;
#21361=CARTESIAN_POINT ( 'NONE',  ( 0.9500414927467378812, -0.1787899950787401604, 0.2903543306548980185 ) ) ;
#21369=CARTESIAN_POINT ( 'NONE',  ( 0.9500414927467378812, -0.1787899950787401604, 0.6446850393163160442 ) ) ;
#21370=( BOUNDED_CURVE ( )  B_SPLINE_CURVE ( 2, ( #27578, #19638, #9342, #42129, #31399, #42380, #5733, #23491, #45970 ),
 .UNSPECIFIED., .F., .T. ) 
 B_SPLINE_CURVE_WITH_KNOTS ( ( 3, 2, 2, 2, 3 ),
 ( 0.8900000000000000133, 0.8924999999999999600, 0.8950000000000000178, 0.8974999999999999645, 0.9000000000000000222 ),
 .UNSPECIFIED. ) 
 CURVE ( )  GEOMETRIC_REPRESENTATION_ITEM ( )  RATIONAL_B_SPLINE_CURVE ( ( 1.000000000000000000, 0.9238795325112869605, 1.000000000000000000, 0.9238795325112869605, 1.000000000000000000, 0.9238795325112869605, 1.000000000000000000, 0.9238795325112869605, 1.000000000000000000 ) ) 
 REPRESENTATION_ITEM ( '' )  ) ;
#21371=CARTESIAN_POINT ( 'NONE',  ( -1.002407869896990045, 0.1264236179284866091, 1.016240157426551161 ) ) ;
#21373=DIRECTION ( 'NONE',  ( 0.000000000000000000, 0.000000000000000000, -1.000000000000000000 ) ) ;
#21376=CARTESIAN_POINT ( 'NONE',  ( -0.8898633633897504724, -0.1743928684788044192, 1.988427853007691981 ) ) ;
#21378=CARTESIAN_POINT ( 'NONE',  ( 1.054774247047244096, 0.000000000000000000, 1.641240157426551161 ) ) ;
#21379=CARTESIAN_POINT ( 'NONE',  ( 0.8019270111902716547, 0.1787899950787401604, 1.963582677111591401 ) ) ;
#21381=ORIENTED_EDGE ( 'NONE', *, *, #5406, .T. ) ;
#21384=VECTOR ( 'NONE', #11355, 39.37007874015748143 ) ;
#21385=CARTESIAN_POINT ( 'NONE',  ( 0.7495606340400177148, 0.1264236179284866091, 0.6668307086076534773 ) ) ;
#21387=CARTESIAN_POINT ( 'NONE',  ( 1.054774247047244096, 0.000000000000000000, 0.1451771653005673179 ) ) ;
#21389=CARTESIAN_POINT ( 'NONE',  ( -1.054774247047244540, -0.07405724077823318263, 1.594488188922613237 ) ) ;
#21391=CARTESIAN_POINT ( 'NONE',  ( 1.033464566929133799, 0.000000000000000000, 0.1673228346456692994 ) ) ;
#21392=CARTESIAN_POINT ( 'NONE',  ( 0.9500414927467378812, -0.1787899950787401604, 1.161417322780881278 ) ) ;
#21395=CARTESIAN_POINT ( 'NONE',  ( 0.6971942568897648851, 0.07405724077823318263, 1.850393700733638624 ) ) ;
#21396=CARTESIAN_POINT ( 'NONE',  ( -0.7646288533564489232, 0.1113553986120547346, 0.5757874015748032370 ) ) ;
#21397=CARTESIAN_POINT ( 'NONE',  ( -0.6971942568897637749, 2.189545951927499583E-17, 0.8686023621509606496 ) ) ;
#21398=CARTESIAN_POINT ( 'NONE',  ( -0.7646288533564489232, -0.1113553986120547346, 1.609251968503937036 ) ) ;
#21400=CARTESIAN_POINT ( 'NONE',  ( 0.7495606340400177148, 0.1264236179284866091, 0.2386811023084413619 ) ) ;
#21401=CARTESIAN_POINT ( 'NONE',  ( -0.6971942568897626646, 0.07405724077823318263, 0.1968503936470238636 ) ) ;
#21402=CARTESIAN_POINT ( 'NONE',  ( -1.002407869896990045, 0.1264236179284866091, 0.6569881889226141247 ) ) ;
#21403=CARTESIAN_POINT ( 'NONE',  ( 0.7185039370078746268, 0.06523048226347956391, 1.592027558947591848 ) ) ;
#21406=CARTESIAN_POINT ( 'NONE',  ( 0.8019270111902717657, 0.1787899950787401604, 0.7480314960092282472 ) ) ;
#21407=CARTESIAN_POINT ( 'NONE',  ( -1.002407869896990045, -0.1264236179284866091, 1.788877952702141672 ) ) ;
#21416=CARTESIAN_POINT ( 'NONE',  ( 0.8759842519685039353, -0.1787899950787401882, 1.114665354276944909 ) ) ;
#21421=CARTESIAN_POINT ( 'NONE',  ( 1.033464566929134687, 0.06523048226347956391, 1.941437007874014187 ) ) ;
#21423=EDGE_CURVE ( 'NONE', #3237, #36143, #40250, .T. ) ;
#21424=CARTESIAN_POINT ( 'NONE',  ( -0.6971942568897648851, -0.07405724077823297447, 0.5216535432533228045 ) ) ;
#21426=CARTESIAN_POINT ( 'NONE',  ( -0.7124453589342143456, -0.03434907305620428508, 1.983904522674447390 ) ) ;
#21428=CARTESIAN_POINT ( 'NONE',  ( 1.002407869896990045, -0.1264236179284866091, 1.163877952702141672 ) ) ;
#21429=CARTESIAN_POINT ( 'NONE',  ( 0.8019270111902716547, 0.1787899950787401604, 1.569881889710015299 ) ) ;
#21430=CARTESIAN_POINT ( 'NONE',  ( 0.8107537697050253289, 0.1574803149606300301, 1.715059055118110631 ) ) ;
#21431=CARTESIAN_POINT ( 'NONE',  ( 1.033464566929133799, 0.000000000000000000, 0.009842519685039369942 ) ) ;
#21433=CARTESIAN_POINT ( 'NONE',  ( 0.9873396505805591694, -0.1113553986120547346, 0.7824803148531023211 ) ) ;
#21434=CARTESIAN_POINT ( 'NONE',  ( -1.033464566929134687, -0.06523048226347956391, 1.808562992018457383 ) ) ;
#21436=CARTESIAN_POINT ( 'NONE',  ( 0.7495606340400177148, 0.1264236179284866091, 0.2337598424659216578 ) ) ;
#21437=CARTESIAN_POINT ( 'NONE',  ( 0.7318012926787728079, -0.08735924986328225117, 0.03937095280083596077 ) ) ;
#21438=CARTESIAN_POINT ( 'NONE',  ( 1.054774247047244540, 0.07405724077823318263, 1.205708661363558365 ) ) ;
#21439=CARTESIAN_POINT ( 'NONE',  ( -0.7646288533564489232, 0.1113553986120547346, 1.825787401467275473 ) ) ;
#21440=CARTESIAN_POINT ( 'NONE',  ( 0.7185039370078739607, 1.928577636452523993E-17, 1.053149606299212504 ) ) ;
#21441=CARTESIAN_POINT ( 'NONE',  ( 0.7646288533564489232, 0.1113553986120547346, 0.4478346455617645550 ) ) ;
#21443=CARTESIAN_POINT ( 'NONE',  ( 0.9617971027165344022, 0.1454179922531197988, 0.03936767230047344412 ) ) ;
#21445=CARTESIAN_POINT ( 'NONE',  ( -1.033464566929133799, 0.000000000000000000, 0.4724409447743622148 ) ) ;
#21446=CARTESIAN_POINT ( 'NONE',  ( -1.033464566929134687, -0.06523048226347956391, 1.542814960629921073 ) ) ;
#21447=CARTESIAN_POINT ( 'NONE',  ( 0.7495606340400177148, 0.1264236179284866091, 1.375492125930488196 ) ) ;
#21448=CARTESIAN_POINT ( 'NONE',  ( -0.7646288533564489232, 0.1113553986120547346, 0.1033464566929133965 ) ) ;
#21449=CARTESIAN_POINT ( 'NONE',  ( -1.033464566929133799, 0.000000000000000000, 0.2755905510735752184 ) ) ;
#21454=CARTESIAN_POINT ( 'NONE',  ( 0.8107537697050254399, -0.1574803149606297803, 1.286909448711370585 ) ) ;
#21457=CARTESIAN_POINT ( 'NONE',  ( 0.6971942568897637749, 2.189545951927499583E-17, 0.5585629920722204877 ) ) ;
#21458=ORIENTED_EDGE ( 'NONE', *, *, #19041, .T. ) ;
#21459=CARTESIAN_POINT ( 'NONE',  ( -1.054774247047244540, 0.07405724077823318263, 1.481299212544662902 ) ) ;
#21461=CARTESIAN_POINT ( 'NONE',  ( -0.9500414927467378812, -0.1787899950787401604, 1.122047244040725644 ) ) ;
#21462=CARTESIAN_POINT ( 'NONE',  ( -0.8759842519685039353, -0.1574803149606299191, 0.1181102362204724532 ) ) ;
#21463=ORIENTED_EDGE ( 'NONE', *, *, #6648, .F. ) ;
#21464=CARTESIAN_POINT ( 'NONE',  ( -1.054774247047244540, -0.07405724077823318263, 1.082677165300567346 ) ) ;
#21466=CARTESIAN_POINT ( 'NONE',  ( 1.033464566929133799, 0.000000000000000000, 0.7874015746956221085 ) ) ;
#21470=CARTESIAN_POINT ( 'NONE',  ( 0.8075642843603819676, 0.1651804176431314886, 0.03937007863263043694 ) ) ;
#21471=ORIENTED_EDGE ( 'NONE', *, *, #19039, .F. ) ;
#21472=CARTESIAN_POINT ( 'NONE',  ( 0.7646288533564489232, 0.1113553986120547346, 0.7726377952755906220 ) ) ;
#21473=CARTESIAN_POINT ( 'NONE',  ( -0.8759842519685039353, 0.1574803149606299191, 0.5610236219397165547 ) ) ;
#21474=CARTESIAN_POINT ( 'NONE',  ( -1.054774247047244540, 0.07405724077823318263, 0.6545275590013545086 ) ) ;
#21475=ADVANCED_FACE ( 'NONE', ( #25674 ), #10588, .T. ) ;
#21478=CARTESIAN_POINT ( 'NONE',  ( -0.8759842519685039353, 0.1787899950787401882, 1.808562992072220377 ) ) ;
#21479=VECTOR ( 'NONE', #16918, 39.37007874015748143 ) ;
#21480=EDGE_CURVE ( 'NONE', #22163, #33650, #46564, .T. ) ;
#21481=VECTOR ( 'NONE', #37189, 39.37007874015748143 ) ;
#21483=( BOUNDED_CURVE ( )  B_SPLINE_CURVE ( 2, ( #16152, #35540, #32667, #13954, #13490, #46299, #21620, #29089, #39337 ),
 .UNSPECIFIED., .F., .F. ) 
 B_SPLINE_CURVE_WITH_KNOTS ( ( 3, 2, 2, 2, 3 ),
 ( 0.4799999999999999822, 0.4824999999999999845, 0.4849999999999999867, 0.4874999999999999889, 0.4899999999999999911 ),
 .UNSPECIFIED. ) 
 CURVE ( )  GEOMETRIC_REPRESENTATION_ITEM ( )  RATIONAL_B_SPLINE_CURVE ( ( 1.000000000000000000, 0.9238795325112869605, 1.000000000000000000, 0.9238795325112869605, 1.000000000000000000, 0.9238795325112869605, 1.000000000000000000, 0.9238795325112869605, 1.000000000000000000 ) ) 
 REPRESENTATION_ITEM ( '' )  ) ;
#21484=CARTESIAN_POINT ( 'NONE',  ( -0.7747078546254108078, 0.1515708385138800074, 0.04064907247438850901 ) ) ;
#21486=CARTESIAN_POINT ( 'NONE',  ( 0.9412147342319837628, 0.1574803149606300301, 0.6865157480314957317 ) ) ;
#21488=CARTESIAN_POINT ( 'NONE',  ( 0.8759842519685039353, 0.000000000000000000, 4.498031496062992574 ) ) ;
#21489=CARTESIAN_POINT ( 'NONE',  ( -0.9873396505805591694, 0.1113553986120547346, 1.382874015640503940 ) ) ;
#21490=CARTESIAN_POINT ( 'NONE',  ( 0.6971942568897637749, 2.189545951927499583E-17, 0.7160433070328504623 ) ) ;
#21492=CARTESIAN_POINT ( 'NONE',  ( 0.7185039370078739607, 1.928577636452523993E-17, 1.879921259842519676 ) ) ;
#21494=CARTESIAN_POINT ( 'NONE',  ( 0.8107537697050253289, -0.1574803149606297803, 1.336122047244094446 ) ) ;
#21495=CARTESIAN_POINT ( 'NONE',  ( 0.8107812902180758785, -0.1596208643658766357, 1.986974409371305095 ) ) ;
#21498=CARTESIAN_POINT ( 'NONE',  ( 0.7495606340400177148, -0.1264236179284866091, 0.6766732282926929409 ) ) ;
#21499=CARTESIAN_POINT ( 'NONE',  ( 0.7646288533564489232, -0.1113553986120547346, 0.2608267715460165226 ) ) ;
#21505=CARTESIAN_POINT ( 'NONE',  ( 1.002407869896990045, -0.1264236179284866091, 1.001476377898992132 ) ) ;
#21510=ADVANCED_FACE ( 'NONE', ( #8617 ), #34980, .F. ) ;
#21511=CARTESIAN_POINT ( 'NONE',  ( 0.7185039370078739607, 0.000000000000000000, 4.498031496062992574 ) ) ;
#21513=CARTESIAN_POINT ( 'NONE',  ( -1.054774247047244540, 0.07405724077823318263, 0.06397637789899228433 ) ) ;
#21514=CARTESIAN_POINT ( 'NONE',  ( 0.8019270111902717657, -0.1787899950787401604, 1.943897637741510254 ) ) ;
#21517=CARTESIAN_POINT ( 'NONE',  ( -0.7185039370078746268, -0.06523048226347956391, 1.843011811023621327 ) ) ;
#21520=CARTESIAN_POINT ( 'NONE',  ( -0.7495606340400177148, -0.1264236179284866091, 1.700295275536787498 ) ) ;
#21521=CARTESIAN_POINT ( 'NONE',  ( 0.8759842519685039353, 0.1787899950787401882, 0.9030511810485984947 ) ) ;
#21523=CARTESIAN_POINT ( 'NONE',  ( -0.7495606340400177148, 0.1264236179284866091, 0.3567913385289137596 ) ) ;
#21524=CARTESIAN_POINT ( 'NONE',  ( 1.033464566929133799, 0.000000000000000000, 0.5511811022546778682 ) ) ;
#21525=CARTESIAN_POINT ( 'NONE',  ( -1.054774247047244096, 0.000000000000000000, 1.877460629867496067 ) ) ;
#21526=CARTESIAN_POINT ( 'NONE',  ( -0.8759842519685039353, 0.1574803149606299191, 1.476377952755905554 ) ) ;
#21527=CARTESIAN_POINT ( 'NONE',  ( -0.7185039370078739607, 1.928577636452523993E-17, 1.840551181102362266 ) ) ;
#21535=CARTESIAN_POINT ( 'NONE',  ( -1.054774247047244540, 0.07405724077823318263, 0.1427165353793072855 ) ) ;
#21539=CARTESIAN_POINT ( 'NONE',  ( -1.054774247047244540, -0.07405724077823318263, 1.363188976324188673 ) ) ;
#21544=VECTOR ( 'NONE', #439, 39.37007874015748143 ) ;
#21546=CARTESIAN_POINT ( 'NONE',  ( 0.7185039370078739607, 1.928577636452523993E-17, 0.3444881889763780070 ) ) ;
#21547=CARTESIAN_POINT ( 'NONE',  ( -1.033464566929134687, -0.06523048226347956391, 0.2436023622047245041 ) ) ;
#21548=CARTESIAN_POINT ( 'NONE',  ( -0.9412147342319837628, -0.1574803149606297803, 0.9768700786326298680 ) ) ;
#21549=CARTESIAN_POINT ( 'NONE',  ( -0.8107537697050253289, 0.1574803149606300301, 0.9276574803149607584 ) ) ;
#21550=CARTESIAN_POINT ( 'NONE',  ( 1.054774247047244096, 0.000000000000000000, 0.4601377952218267953 ) ) ;
#21552=CARTESIAN_POINT ( 'NONE',  ( 0.7185039370078739607, 1.928577636452523993E-17, 1.751968503829480106 ) ) ;
#21555=CARTESIAN_POINT ( 'NONE',  ( 0.7185039370078739607, 1.928577636452523993E-17, 0.7381889763779527769 ) ) ;
#21561=CARTESIAN_POINT ( 'NONE',  ( 0.9873396505805591694, 0.1113553986120547346, 0.1624015746956226358 ) ) ;
#21562=ORIENTED_EDGE ( 'NONE', *, *, #11600, .F. ) ;
#21563=CARTESIAN_POINT ( 'NONE',  ( 0.8759842519685039353, -0.1574803149606299191, 0.2362204724409449064 ) ) ;
#21564=CARTESIAN_POINT ( 'NONE',  ( 0.7185039370078766252, -0.06523048226348168721, 1.833169291231055542 ) ) ;
#21567=CARTESIAN_POINT ( 'NONE',  ( -0.8759842519685039353, -0.1574803149606299191, 0.1476377951680635792 ) ) ;
#21569=CARTESIAN_POINT ( 'NONE',  ( 0.9412147342319837628, 0.1574803149606300301, 0.9522637794200313754 ) ) ;
#21571=CARTESIAN_POINT ( 'NONE',  ( -1.054774247047244540, 0.07405724077823318263, 0.4183070865604097133 ) ) ;
#21574=CARTESIAN_POINT ( 'NONE',  ( -0.8759842519685039353, 0.1787899950787401882, 1.651082677111590513 ) ) ;
#21575=ORIENTED_EDGE ( 'NONE', *, *, #429, .F. ) ;
#21576=CARTESIAN_POINT ( 'NONE',  ( 1.054774247047244540, 0.07405724077823318263, 1.486220472387181690 ) ) ;
#21577=CARTESIAN_POINT ( 'NONE',  ( -0.6971942568897626646, -0.07405724077823297447, 0.7972440944344250102 ) ) ;
#21578=CARTESIAN_POINT ( 'NONE',  ( 1.002407869896990045, 0.1264236179284866091, 0.1500984251430867999 ) ) ;
#21579=CARTESIAN_POINT ( 'NONE',  ( -0.9412147342319837628, -0.1574803149606297803, 1.685531495955465697 ) ) ;
#21580=CARTESIAN_POINT ( 'NONE',  ( 0.6971942568897637749, 2.189545951927499583E-17, 0.7947834645131652831 ) ) ;
#21581=CARTESIAN_POINT ( 'NONE',  ( -0.8759842519685039353, -0.1787899950787401882, 0.6815944881352126172 ) ) ;
#21583=DIRECTION ( 'NONE',  ( 1.000000000000000000, 0.000000000000000000, -1.822029033848725275E-16 ) ) ;
#21584=AXIS2_PLACEMENT_3D ( 'NONE', #8168, #27136, #12030 ) ;
#21588=CARTESIAN_POINT ( 'NONE',  ( -0.7185039370078746268, 0.06523048226347956391, 1.828248031388536310 ) ) ;
#21590=LINE ( 'NONE', #14176, #27198 ) ;
#21591=CARTESIAN_POINT ( 'NONE',  ( -1.033464566929133799, 0.000000000000000000, 1.505905511811023612 ) ) ;
#21592=CARTESIAN_POINT ( 'NONE',  ( -0.7185039370078739607, 1.928577636452523993E-17, 0.4625984251968504046 ) ) ;
#21594=CARTESIAN_POINT ( 'NONE',  ( 0.7495606340400177148, -0.1264236179284866091, 1.508366141678519678 ) ) ;
#21607=EDGE_CURVE ( 'NONE', #21900, #5382, #24884, .T. ) ;
#21610=CARTESIAN_POINT ( 'NONE',  ( 1.054774247047244540, 0.07405724077823318263, 0.3395669290800945039 ) ) ;
#21615=CARTESIAN_POINT ( 'NONE',  ( 0.7185039370078739607, 1.928577636452523993E-17, 0.4527559054042842868 ) ) ;
#21616=CARTESIAN_POINT ( 'NONE',  ( 0.9500414927467378812, -0.1787899950787401604, 0.6840551180564720113 ) ) ;
#21618=CARTESIAN_POINT ( 'NONE',  ( -0.8019270111902716547, -0.1787899950787401604, 0.9596456692375763264 ) ) ;
#21620=CARTESIAN_POINT ( 'NONE',  ( 0.7646288533564489232, 0.1113553986120547346, 0.9990157479239685223 ) ) ;
#21622=CARTESIAN_POINT ( 'NONE',  ( 0.9412147342319837628, -0.1574803149606297803, 1.695374015748031926 ) ) ;
#21623=CARTESIAN_POINT ( 'NONE',  ( 1.002407869896990045, -0.1264236179284866091, 1.715059055064346527 ) ) ;
#21631=CARTESIAN_POINT ( 'NONE',  ( -0.7495606340400177148, 0.1264236179284866091, 0.3961614172690708924 ) ) ;
#21632=CARTESIAN_POINT ( 'NONE',  ( 0.8019270111902717657, 0.1787899950787401604, 0.5856299212060785964 ) ) ;
#21634=CARTESIAN_POINT ( 'NONE',  ( 0.9500414927467378812, 0.1787899950787401604, 0.03444881884387430981 ) ) ;
#21635=CARTESIAN_POINT ( 'NONE',  ( -0.7185039370078739607, 1.928577636452523993E-17, 1.161417322727118284 ) ) ;
#21636=CARTESIAN_POINT ( 'NONE',  ( -0.6971942568897648851, 0.07405724077823318263, 1.653543307032850462 ) ) ;
#21639=CARTESIAN_POINT ( 'NONE',  ( -1.054774247047244540, -0.07405724077823318263, 1.166338582623402509 ) ) ;
#21644=CARTESIAN_POINT ( 'NONE',  ( 0.6971942568897648851, -0.07405724077823297447, 1.894685039316315489 ) ) ;
#21645=CARTESIAN_POINT ( 'NONE',  ( -0.9412147342319837628, 0.1574803149606300301, 0.6077755905511815770 ) ) ;
#21646=CARTESIAN_POINT ( 'NONE',  ( -0.7495606340400177148, 0.1264236179284866091, 0.9030511810485984947 ) ) ;
#21649=CARTESIAN_POINT ( 'NONE',  ( 1.054774247047244540, -0.07405724077823318263, 0.3001968503399373711 ) ) ;
#21650=CARTESIAN_POINT ( 'NONE',  ( -1.054774247047244540, 0.07405724077823318263, 0.1820866141194649179 ) ) ;
#21651=CARTESIAN_POINT ( 'NONE',  ( -0.9500414927467378812, -0.1787899950787401604, 0.6840551180564720113 ) ) ;
#21652=CARTESIAN_POINT ( 'NONE',  ( 1.033464566929134687, 0.06523048226347956391, 1.498523621939716444 ) ) ;
#21656=CARTESIAN_POINT ( 'NONE',  ( 1.002407869896990045, 0.1264236179284866091, 0.8587598424659212970 ) ) ;
#21658=CARTESIAN_POINT ( 'NONE',  ( 0.8759842519685039353, -0.1787899950787401882, 1.080216535379306952 ) ) ;
#21659=CARTESIAN_POINT ( 'NONE',  ( -0.8759842519685039353, -0.1787899950787401882, 1.862696850339937038 ) ) ;
#21663=CARTESIAN_POINT ( 'NONE',  ( 0.7185039370078746268, 0.06523048226347956391, 1.326279527559055982 ) ) ;
#21668=CARTESIAN_POINT ( 'NONE',  ( 0.6971942568897648851, 0.07405724077823318263, 1.141732283410804349 ) ) ;
#21669=CARTESIAN_POINT ( 'NONE',  ( -1.033464566929133799, 1.928577636452524610E-17, 2.869337061179095023E-17 ) ) ;
#21671=DIRECTION ( 'NONE',  ( 0.000000000000000000, 1.000000000000000000, 0.000000000000000000 ) ) ;
#21673=( BOUNDED_CURVE ( )  B_SPLINE_CURVE ( 2, ( #7444, #44103, #36689, #47233, #3850, #14889, #17761, #14417, #24958 ),
 .UNSPECIFIED., .F., .T. ) 
 B_SPLINE_CURVE_WITH_KNOTS ( ( 3, 2, 2, 2, 3 ),
 ( 0.7900000000000000355, 0.7924999999999999822, 0.7950000000000000400, 0.7974999999999999867, 0.8000000000000000444 ),
 .UNSPECIFIED. ) 
 CURVE ( )  GEOMETRIC_REPRESENTATION_ITEM ( )  RATIONAL_B_SPLINE_CURVE ( ( 1.000000000000000000, 0.9238795325112869605, 1.000000000000000000, 0.9238795325112869605, 1.000000000000000000, 0.9238795325112869605, 1.000000000000000000, 0.9238795325112869605, 1.000000000000000000 ) ) 
 REPRESENTATION_ITEM ( '' )  ) ;
#21674=CARTESIAN_POINT ( 'NONE',  ( 1.054774247047244540, -0.07405724077823318263, 0.09842519679663024046 ) ) ;
#21676=CARTESIAN_POINT ( 'NONE',  ( -0.9500414927467377701, 0.1787899950787401604, 0.5068897637257642197 ) ) ;
#21677=CARTESIAN_POINT ( 'NONE',  ( -0.7185039370078746268, 0.06523048226347956391, 0.6865157479239700766 ) ) ;
#21679=CARTESIAN_POINT ( 'NONE',  ( -0.7236033548003161231, -0.07168286384238391207, 1.984649071003595999 ) ) ;
#21681=CARTESIAN_POINT ( 'NONE',  ( 1.002407869896990045, -0.1264236179284866091, 1.281988188922614125 ) ) ;
#21682=CARTESIAN_POINT ( 'NONE',  ( 1.002407869896990045, -0.1264236179284866091, 1.670767716481669440 ) ) ;
#21685=CARTESIAN_POINT ( 'NONE',  ( -0.7640189571129942792, 0.1165819918074077199, 1.980746850915923174 ) ) ;
#21688=CARTESIAN_POINT ( 'NONE',  ( -0.8107537697050253289, -0.1574803149606297803, 1.680610236112946687 ) ) ;
#21689=CARTESIAN_POINT ( 'NONE',  ( 0.9500414927467378812, 0.1787899950787401604, 0.1870078739619845387 ) ) ;
#21690=CARTESIAN_POINT ( 'NONE',  ( 0.7495606340400177148, -0.1264236179284866091, 1.188484251914740275 ) ) ;
#21691=DIRECTION ( 'NONE',  ( 1.822029033848725028E-16, 0.000000000000000000, 1.000000000000000000 ) ) ;
#21693=CARTESIAN_POINT ( 'NONE',  ( -0.7495606340400177148, 0.1264236179284866091, 1.218011810969858111 ) ) ;
#21694=CARTESIAN_POINT ( 'NONE',  ( 0.8759842519685039353, -0.1574803149606299191, 0.5019685038294811052 ) ) ;
#21695=EDGE_LOOP ( 'NONE', ( #27945, #46410, #15331, #30442 ) ) ;
#21696=CARTESIAN_POINT ( 'NONE',  ( -0.7185039370078739607, 1.928577636452523993E-17, 1.397637795168062969 ) ) ;
#21698=CARTESIAN_POINT ( 'NONE',  ( -0.8107537697050253289, -0.1574803149606297803, 0.3813976376877488139 ) ) ;
#21699=ORIENTED_EDGE ( 'NONE', *, *, #35276, .T. ) ;
#21700=CARTESIAN_POINT ( 'NONE',  ( 0.8759842519685039353, 0.1787899950787401882, 1.409940944828126153 ) ) ;
#21701=CARTESIAN_POINT ( 'NONE',  ( -1.033464566929133799, 0.000000000000000000, 0.08858267716535432601 ) ) ;
#21702=CYLINDRICAL_SURFACE ( 'NONE', #46057, 0.1787899950787401049 ) ;
#21707=ORIENTED_EDGE ( 'NONE', *, *, #35926, .T. ) ;
#21711=CARTESIAN_POINT ( 'NONE',  ( 1.002407869896990045, -0.1264236179284866091, 0.5733267715997795166 ) ) ;
#21713=ADVANCED_FACE ( 'NONE', ( #21752 ), #36384, .T. ) ;
#21715=CARTESIAN_POINT ( 'NONE',  ( -1.002407869896990045, 0.1264236179284866091, 1.173720472387181246 ) ) ;
#21716=CARTESIAN_POINT ( 'NONE',  ( -0.9873396505805591694, 0.1113553986120547346, 0.09350393700787401619 ) ) ;
#21718=CARTESIAN_POINT ( 'NONE',  ( -0.7495606340400177148, 0.1264236179284866091, 1.021161417269070837 ) ) ;
#21720=CARTESIAN_POINT ( 'NONE',  ( -1.054774247047244540, 0.07405724077823318263, 0.8169291338045038264 ) ) ;
#21721=CARTESIAN_POINT ( 'NONE',  ( -0.6971942568897626646, 0.07405724077823318263, 0.2411417322297011168 ) ) ;
#21722=CARTESIAN_POINT ( 'NONE',  ( -1.033464566929134687, -0.06523048226347956391, 0.3617125984251969295 ) ) ;
#21723=CARTESIAN_POINT ( 'NONE',  ( 0.5314960629921259283, 0.000000000000000000, 4.685039370078739829 ) ) ;
#21727=EDGE_LOOP ( 'NONE', ( #17082, #17293, #15613, #18265 ) ) ;
#21729=CARTESIAN_POINT ( 'NONE',  ( -0.7185039370078739607, 0.000000000000000000, -2.869337061179095023E-17 ) ) ;
#21730=CARTESIAN_POINT ( 'NONE',  ( -0.6971942568897626646, 0.07405724077823318263, 0.7480314960092282472 ) ) ;
#21731=CARTESIAN_POINT ( 'NONE',  ( 0.7185039370078739607, 1.928577636452523993E-17, 0.8562992125984251190 ) ) ;
#21733=EDGE_CURVE ( 'NONE', #40966, #5319, #22071, .T. ) ;
#21734=CARTESIAN_POINT ( 'NONE',  ( 0.7185039370078746268, -0.06523048226347956391, 1.331200787401575436 ) ) ;
#21735=CARTESIAN_POINT ( 'NONE',  ( -0.6971942568897626646, 0.07405724077823318263, 0.08366141726907130871 ) ) ;
#21736=CARTESIAN_POINT ( 'NONE',  ( 0.7185039370078739607, 1.928577636452523993E-17, 0.6988188976377952555 ) ) ;
#21739=CARTESIAN_POINT ( 'NONE',  ( -0.7646288533564489232, -0.1113553986120547346, 1.363188976270427455 ) ) ;
#21741=CARTESIAN_POINT ( 'NONE',  ( 1.054774247047244540, -0.07405724077823318263, 0.7726377952218265177 ) ) ;
#21744=ORIENTED_EDGE ( 'NONE', *, *, #22778, .T. ) ;
#21746=CARTESIAN_POINT ( 'NONE',  ( 0.9412147342319837628, 0.1574803149606300301, 1.198326771653543510 ) ) ;
#21747=CARTESIAN_POINT ( 'NONE',  ( 0.8638812610618022969, -0.1737634973235707980, 1.987989868856034681 ) ) ;
#21749=CARTESIAN_POINT ( 'NONE',  ( 0.7185039370078739607, 1.928577636452523993E-17, 0.3346456691838114450 ) ) ;
#21751=CARTESIAN_POINT ( 'NONE',  ( 0.6971942568897648851, -0.07405724077823297447, 0.5954724408911187261 ) ) ;
#21752=FACE_OUTER_BOUND ( 'NONE', #46751, .T. ) ;
#21757=CARTESIAN_POINT ( 'NONE',  ( 1.002407869896990045, -0.1264236179284866091, 1.040846456639149764 ) ) ;
#21763=CARTESIAN_POINT ( 'NONE',  ( -1.054774247047244540, -0.07405724077823318263, 0.1377952755367876370 ) ) ;
#21768=AXIS2_PLACEMENT_3D ( 'NONE', #28965, #40622, #11431 ) ;
#21769=CARTESIAN_POINT ( 'NONE',  ( -0.8759842519685039353, 0.1787899950787401882, 1.887303149552535420 ) ) ;
#21770=CARTESIAN_POINT ( 'NONE',  ( -0.6971942568897637749, 2.189545951927499583E-17, 1.734744094434425232 ) ) ;
#21771=EDGE_CURVE ( 'NONE', #21060, #14891, #22443, .T. ) ;
#21772=CARTESIAN_POINT ( 'NONE',  ( -0.6971942568897637749, 2.189545951927499583E-17, 0.4010826771115905687 ) ) ;
#21773=CARTESIAN_POINT ( 'NONE',  ( 0.8759842519685039353, 0.000000000000000000, 4.498031496062992574 ) ) ;
#21774=CARTESIAN_POINT ( 'NONE',  ( -1.002407869896990045, -0.1264236179284866091, 1.990649606245448844 ) ) ;
#21776=CARTESIAN_POINT ( 'NONE',  ( -0.8107537697050253289, 0.1574803149606300301, 1.872539370078740495 ) ) ;
#21780=DIRECTION ( 'NONE',  ( 0.000000000000000000, 0.000000000000000000, 1.000000000000000000 ) ) ;
#21782=CARTESIAN_POINT ( 'NONE',  ( -0.8759842519685039353, -0.1787899950787401882, 0.2485236219934806867 ) ) ;
#21783=( BOUNDED_CURVE ( )  B_SPLINE_CURVE ( 2, ( #37895, #44345, #33612, #23281, #8643, #26175, #33379, #22796, #15388 ),
 .UNSPECIFIED., .F., .T. ) 
 B_SPLINE_CURVE_WITH_KNOTS ( ( 3, 2, 2, 2, 3 ),
 ( 0.2200000000000000011, 0.2225000000000000033, 0.2250000000000000056, 0.2275000000000000078, 0.2300000000000000100 ),
 .UNSPECIFIED. ) 
 CURVE ( )  GEOMETRIC_REPRESENTATION_ITEM ( )  RATIONAL_B_SPLINE_CURVE ( ( 1.000000000000000000, 0.9238795325112869605, 1.000000000000000000, 0.9238795325112869605, 1.000000000000000000, 0.9238795325112869605, 1.000000000000000000, 0.9238795325112869605, 1.000000000000000000 ) ) 
 REPRESENTATION_ITEM ( '' )  ) ;
#21784=ORIENTED_EDGE ( 'NONE', *, *, #18399, .T. ) ;
#21787=CARTESIAN_POINT ( 'NONE',  ( -0.8019270111902716547, -0.1787899950787401604, 1.432086614119464141 ) ) ;
#21795=CARTESIAN_POINT ( 'NONE',  ( 1.033464566929133799, 0.000000000000000000, 0.3248031496062992463 ) ) ;
#21797=CARTESIAN_POINT ( 'NONE',  ( -0.9412147342319837628, 0.1574803149606300301, 0.9522637794200313754 ) ) ;
#21798=CARTESIAN_POINT ( 'NONE',  ( 1.002407869896990045, 0.1264236179284866091, 0.3863188975840318173 ) ) ;
#21800=AXIS2_PLACEMENT_3D ( 'NONE', #13094, #2507, #35129 ) ;
#21801=CARTESIAN_POINT ( 'NONE',  ( 0.9873396505805591694, 0.1113553986120547346, 1.776574803042078488 ) ) ;
#21802=ORIENTED_EDGE ( 'NONE', *, *, #11974, .T. ) ;
#21804=CARTESIAN_POINT ( 'NONE',  ( 0.8107537697050253289, 0.1574803149606300301, 0.8095472440944886383 ) ) ;
#21806=( BOUNDED_CURVE ( )  B_SPLINE_CURVE ( 2, ( #10798, #29026, #11027, #17484, #39517, #29281, #36428, #46705, #39281 ),
 .UNSPECIFIED., .F., .F. ) 
 B_SPLINE_CURVE_WITH_KNOTS ( ( 3, 2, 2, 2, 3 ),
 ( 0.08999999999999999667, 0.09249999999999999889, 0.09500000000000000111, 0.09750000000000000333, 0.1000000000000000056 ),
 .UNSPECIFIED. ) 
 CURVE ( )  GEOMETRIC_REPRESENTATION_ITEM ( )  RATIONAL_B_SPLINE_CURVE ( ( 1.000000000000000000, 0.9238795325112869605, 1.000000000000000000, 0.9238795325112869605, 1.000000000000000000, 0.9238795325112869605, 1.000000000000000000, 0.9238795325112869605, 1.000000000000000000 ) ) 
 REPRESENTATION_ITEM ( '' )  ) ;
#21808=CARTESIAN_POINT ( 'NONE',  ( 0.8759842519685039353, -0.1574803149606299191, 0.1476377951680635792 ) ) ;
#21810=ADVANCED_FACE ( 'NONE', ( #35835 ), #9963, .T. ) ;
#21811=CARTESIAN_POINT ( 'NONE',  ( 0.7185039370078739607, 1.928577636452523993E-17, 1.909448818790110192 ) ) ;
#21815=CARTESIAN_POINT ( 'NONE',  ( -0.9873396505805591694, 0.1113553986120547346, 0.1624015746956226358 ) ) ;
#21817=CARTESIAN_POINT ( 'NONE',  ( 1.033464566929134687, -0.06523048226347956391, 0.9817913384751510986 ) ) ;
#21820=ORIENTED_EDGE ( 'NONE', *, *, #45284, .F. ) ;
#21821=CARTESIAN_POINT ( 'NONE',  ( -0.6971942568897637749, 2.189545951927499583E-17, 1.542814960576157413 ) ) ;
#21822=CARTESIAN_POINT ( 'NONE',  ( 1.054774247047244096, 0.000000000000000000, 1.523129921206078707 ) ) ;
#21824=CARTESIAN_POINT ( 'NONE',  ( -0.7495606340400177148, 0.1264236179284866091, 0.7898622046706456068 ) ) ;
#21825=CARTESIAN_POINT ( 'NONE',  ( 1.002407869896990045, -0.1264236179284866091, 0.1402559054580474474 ) ) ;
#21827=CARTESIAN_POINT ( 'NONE',  ( 0.6971942568897648851, 0.07405724077823318263, 0.7135826771115916234 ) ) ;
#21828=CARTESIAN_POINT ( 'NONE',  ( -0.6971942568897648851, -0.07405724077823297447, 0.7529527558517473684 ) ) ;
#21829=ADVANCED_FACE ( 'NONE', ( #46603 ), #13781, .T. ) ;
#21833=CARTESIAN_POINT ( 'NONE',  ( -0.8759842519685039353, -0.1574803149606299191, 1.919291338475149544 ) ) ;
#21836=CARTESIAN_POINT ( 'NONE',  ( -0.7185039370078746268, 0.06523048226347956391, 1.523129921259841923 ) ) ;
#21838=CARTESIAN_POINT ( 'NONE',  ( 0.7495606340400177148, 0.1264236179284866091, 1.419783464513165505 ) ) ;
#21843=ORIENTED_EDGE ( 'NONE', *, *, #3852, .F. ) ;
#21846=EDGE_CURVE ( 'NONE', #40728, #23847, #35255, .T. ) ;
#21850=CARTESIAN_POINT ( 'NONE',  ( 0.9500414927467378812, 0.1787899950787401604, 0.3051181101824569919 ) ) ;
#21856=CARTESIAN_POINT ( 'NONE',  ( 0.8019270111902717657, -0.1787899950787401604, 0.5610236219934807700 ) ) ;
#21857=CARTESIAN_POINT ( 'NONE',  ( -0.8340766383913040816, 0.1725986337945408233, 0.03937007874015843040 ) ) ;
#21858=CARTESIAN_POINT ( 'NONE',  ( 0.9412147342319837628, 0.1574803149606300301, 1.119586614173229577 ) ) ;
#21860=VECTOR ( 'NONE', #19113, 39.37007874015748143 ) ;
#21862=CARTESIAN_POINT ( 'NONE',  ( -0.9873396505805591694, 0.1113553986120547346, 1.304133858160188897 ) ) ;
#21863=CARTESIAN_POINT ( 'NONE',  ( 0.6971942568897648851, -0.07405724077823297447, 1.663385826717890925 ) ) ;
#21865=CARTESIAN_POINT ( 'NONE',  ( 1.054774247047244096, 0.000000000000000000, 0.4945866141194645849 ) ) ;
#21873=CARTESIAN_POINT ( 'NONE',  ( -1.054774247047244540, 0.07405724077823318263, 0.4625984251430869665 ) ) ;
#21874=CARTESIAN_POINT ( 'NONE',  ( 0.7646288533564489232, 0.1113553986120547346, 0.4872047243019220208 ) ) ;
#21876=CARTESIAN_POINT ( 'NONE',  ( 0.8759842519685039353, 0.1787899950787401882, 0.03690944876513417572 ) ) ;
#21878=EDGE_CURVE ( 'NONE', #37983, #41227, #39838, .T. ) ;
#21879=CARTESIAN_POINT ( 'NONE',  ( -1.002407869896990045, -0.1264236179284866091, 1.552657480261196765 ) ) ;
#21881=CARTESIAN_POINT ( 'NONE',  ( -0.6971942568897637749, 2.189545951927499583E-17, 1.109744094434425232 ) ) ;
#21882=CARTESIAN_POINT ( 'NONE',  ( -0.9873396505805591694, 0.1113553986120547346, 0.3297244094488189226 ) ) ;
#21883=CARTESIAN_POINT ( 'NONE',  ( 0.8759842519685039353, 0.1787899950787401882, 1.139271653489543290 ) ) ;
#21884=CARTESIAN_POINT ( 'NONE',  ( 0.6971942568897648851, 0.07405724077823318263, 1.771653543253322249 ) ) ;
#21885=CARTESIAN_POINT ( 'NONE',  ( -0.8759842519685039353, -0.1787899950787401882, 1.114665354276944909 ) ) ;
#21888=CARTESIAN_POINT ( 'NONE',  ( 0.8019270111902716547, -0.1787899950787401604, 0.2509842519147403861 ) ) ;
#21889=CARTESIAN_POINT ( 'NONE',  ( -0.8759842519685039353, -0.1787899950787401882, 0.2878937007336381804 ) ) ;
#21890=CARTESIAN_POINT ( 'NONE',  ( -1.054774247047244096, 0.000000000000000000, 0.6914370078202519698 ) ) ;
#21891=CARTESIAN_POINT ( 'NONE',  ( 0.8107537697050253289, -0.1574803149606297803, 1.641240157372788611 ) ) ;
#21894=CARTESIAN_POINT ( 'NONE',  ( 1.002407869896990045, -0.1264236179284866091, 0.7701771653005669016 ) ) ;
#21895=CARTESIAN_POINT ( 'NONE',  ( 0.8759842519685039353, -0.1787899950787401882, 1.001476377898992132 ) ) ;
#21896=CARTESIAN_POINT ( 'NONE',  ( -0.8759842519685039353, -0.1787899950787401882, 1.902066929080094448 ) ) ;
#21897=CARTESIAN_POINT ( 'NONE',  ( 0.8019270111902717657, -0.1787899950787401604, 1.978346456639149320 ) ) ;
#21898=CARTESIAN_POINT ( 'NONE',  ( 0.9412147342319837628, 0.1574803149606300301, 1.316437007874015519 ) ) ;
#21900=VERTEX_POINT ( 'NONE', #28673 ) ;
#21903=AXIS2_PLACEMENT_3D ( 'NONE', #1260, #12792, #9175 ) ;
#21904=ORIENTED_EDGE ( 'NONE', *, *, #837, .T. ) ;
#21905=CARTESIAN_POINT ( 'NONE',  ( 0.6971942568897648851, -0.07405724077823297447, 1.264763779473795813 ) ) ;
#21908=CARTESIAN_POINT ( 'NONE',  ( 0.9500414927467378812, 0.1787899950787401604, 1.525590551127340433 ) ) ;
#21909=CARTESIAN_POINT ( 'NONE',  ( 0.6971942568897626646, 0.07405724077823318263, 0.07874015742655145200 ) ) ;
#21913=CARTESIAN_POINT ( 'NONE',  ( -1.054774247047244096, 0.000000000000000000, 0.4207677164816693294 ) ) ;
#21916=CARTESIAN_POINT ( 'NONE',  ( -0.7204869834275922091, -0.06397302528968762392, 1.984489880467943390 ) ) ;
#21918=CARTESIAN_POINT ( 'NONE',  ( 0.9500414927467378812, -0.1787899950787401604, 1.240157480261197431 ) ) ;
#21919=CARTESIAN_POINT ( 'NONE',  ( 0.6971942568897648851, -0.07405724077823297447, 1.697834645615527771 ) ) ;
#21920=EDGE_CURVE ( 'NONE', #23661, #5728, #2195, .T. ) ;
#21923=DIRECTION ( 'NONE',  ( 0.000000000000000000, 0.000000000000000000, -1.000000000000000000 ) ) ;
#21926=CARTESIAN_POINT ( 'NONE',  ( 1.054774247047244096, 0.000000000000000000, 0.1402559054580474474 ) ) ;
#21927=CARTESIAN_POINT ( 'NONE',  ( 0.7026940052797937541, -0.01276303134770263512, 0.03936938617317344707 ) ) ;
#21928=CARTESIAN_POINT ( 'NONE',  ( -1.033464566929133799, 0.000000000000000000, 0.5511811022546772021 ) ) ;
#21929=FACE_OUTER_BOUND ( 'NONE', #1592, .T. ) ;
#21930=CARTESIAN_POINT ( 'NONE',  ( -1.054774247047244096, 0.000000000000000000, 1.163877952702141672 ) ) ;
#21931=CARTESIAN_POINT ( 'NONE',  ( 1.033464566929133799, 0.000000000000000000, 0.6299212597349921339 ) ) ;
#21933=CARTESIAN_POINT ( 'NONE',  ( -0.7495606340400177148, 0.1264236179284866091, 1.065452755851747924 ) ) ;
#21934=CARTESIAN_POINT ( 'NONE',  ( -1.033464566929134687, 0.06523048226347956391, 1.114665354330708125 ) ) ;
#21935=CARTESIAN_POINT ( 'NONE',  ( 0.9040863184708680667, 0.1705322868731493358, 0.03937075118789555572 ) ) ;
#21936=CARTESIAN_POINT ( 'NONE',  ( 0.7185039370078741827, 0.06523048226347841205, 0.8439960628845994961 ) ) ;
#21937=CARTESIAN_POINT ( 'NONE',  ( -0.7646288533564489232, 0.1113553986120547346, 0.4478346455617645550 ) ) ;
#21938=CARTESIAN_POINT ( 'NONE',  ( -1.033464566929133799, 0.000000000000000000, 0.04921259842519685318 ) ) ;
#21939=CARTESIAN_POINT ( 'NONE',  ( 0.9500414927467378812, 0.1787899950787401604, 1.446850393647023614 ) ) ;
#21940=CARTESIAN_POINT ( 'NONE',  ( -0.7185039370078739607, 1.928577636452523993E-17, 0.3346456691838114450 ) ) ;
#21941=CARTESIAN_POINT ( 'NONE',  ( -1.002407869896990045, 0.1264236179284866091, 0.06643700782025216411 ) ) ;
#21944=LINE ( 'NONE', #14756, #9216 ) ;
#21945=CYLINDRICAL_SURFACE ( 'NONE', #8393, 0.1574803149606299191 ) ;
#21947=CARTESIAN_POINT ( 'NONE',  ( 1.002407869896990045, -0.1264236179284866091, 0.6520669290800944484 ) ) ;
#21948=EDGE_LOOP ( 'NONE', ( #1472, #21381, #31263, #36447, #4810 ) ) ;
#21950=CARTESIAN_POINT ( 'NONE',  ( -0.9500414927467378812, 0.1787899950787401604, 1.176181102308441417 ) ) ;
#21951=CARTESIAN_POINT ( 'NONE',  ( -0.7495606340400177148, -0.1264236179284866091, 1.070374015694267600 ) ) ;
#21952=CARTESIAN_POINT ( 'NONE',  ( -1.002407869896990045, 0.1264236179284866091, 0.7800196849856062542 ) ) ;
#21954=CARTESIAN_POINT ( 'NONE',  ( -0.7495606340400177148, 0.1264236179284866091, 0.1993110235682838682 ) ) ;
#21959=CARTESIAN_POINT ( 'NONE',  ( -0.8759842519685039353, 0.1574803149606299191, 1.466535432963338437 ) ) ;
#21961=ORIENTED_EDGE ( 'NONE', *, *, #32611, .T. ) ;
#21963=CARTESIAN_POINT ( 'NONE',  ( -0.6971942568897626646, -0.07405724077823297447, 0.7135826771115916234 ) ) ;
#21965=CARTESIAN_POINT ( 'NONE',  ( -0.8019270111902716547, -0.1787899950787401604, 1.825787401521040243 ) ) ;
#21968=CARTESIAN_POINT ( 'NONE',  ( -0.7495606340400177148, -0.1264236179284866091, 0.09104330703285078152 ) ) ;
#21970=CARTESIAN_POINT ( 'NONE',  ( -0.8759842519685039353, 0.000000000000000000, 2.007874015640504162 ) ) ;
#21971=CARTESIAN_POINT ( 'NONE',  ( -0.7185039370078746268, -0.06523048226347956391, 1.478838582569637294 ) ) ;
#21972=CARTESIAN_POINT ( 'NONE',  ( 1.054774247047244096, 0.000000000000000000, 0.7750984251430865779 ) ) ;
#21976=CARTESIAN_POINT ( 'NONE',  ( 0.8759842519685039353, 0.1574803149606299191, 1.358267716535433323 ) ) ;
#21977=CARTESIAN_POINT ( 'NONE',  ( 0.7754090590921228765, -0.1384152968776324877, 1.986207984632974766 ) ) ;
#21979=CARTESIAN_POINT ( 'NONE',  ( 1.033464566929134687, -0.06523048226347956391, 1.493602362097197211 ) ) ;
#21981=VECTOR ( 'NONE', #45004, 39.37007874015748143 ) ;
#21982=CARTESIAN_POINT ( 'NONE',  ( 1.002407869896990045, 0.1264236179284866091, 0.7750984251430865779 ) ) ;
#21985=CARTESIAN_POINT ( 'NONE',  ( -0.8759842519685039353, 0.000000000000000000, 0.000000000000000000 ) ) ;
#21986=VERTEX_POINT ( 'NONE', #1043 ) ;
#21989=CARTESIAN_POINT ( 'NONE',  ( 1.054774247047244540, 0.07405724077823318263, 1.008858267662772423 ) ) ;
#21993=CARTESIAN_POINT ( 'NONE',  ( -0.6971942568897637749, 2.189545951927499583E-17, 0.04183070860765386589 ) ) ;
#21994=CARTESIAN_POINT ( 'NONE',  ( -1.033464566929133799, 0.000000000000000000, 0.7185039370078739607 ) ) ;
#21997=CARTESIAN_POINT ( 'NONE',  ( -0.6971942568897648851, 0.07405724077823318263, 1.614173228292692386 ) ) ;
#21998=CARTESIAN_POINT ( 'NONE',  ( -0.7495606340400177148, 0.1264236179284866091, 1.099901574749385880 ) ) ;
#21999=CARTESIAN_POINT ( 'NONE',  ( -0.6971942568897626646, 0.07405724077823318263, 0.3198818897100162983 ) ) ;
#22002=CARTESIAN_POINT ( 'NONE',  ( 0.8019270111902717657, 0.1787899950787401604, 0.07381889758403178958 ) ) ;
#22009=CARTESIAN_POINT ( 'NONE',  ( -0.6971942568897626646, -0.07405724077823297447, 0.3592519684501735977 ) ) ;
#22010=ORIENTED_EDGE ( 'NONE', *, *, #14666, .F. ) ;
#22012=CARTESIAN_POINT ( 'NONE',  ( -0.7495606340400177148, -0.1264236179284866091, 1.429625984198204858 ) ) ;
#22016=EDGE_CURVE ( 'NONE', #42193, #46242, #7105, .T. ) ;
#22020=CARTESIAN_POINT ( 'NONE',  ( -0.8759842519685039353, -0.1574803149606299191, 0.9350393699712126194 ) ) ;
#22021=CARTESIAN_POINT ( 'NONE',  ( 0.8019270111902717657, -0.1787899950787401604, 0.4478346456155276045 ) ) ;
#22023=CARTESIAN_POINT ( 'NONE',  ( 0.9412147342319837628, 0.1574803149606300301, 1.779035432963339991 ) ) ;
#22027=CARTESIAN_POINT ( 'NONE',  ( 0.7185039370078739607, 1.928577636452523993E-17, 0.9350393700787401619 ) ) ;
#22035=ORIENTED_EDGE ( 'NONE', *, *, #23605, .F. ) ;
#22043=CARTESIAN_POINT ( 'NONE',  ( 0.8759842519685039353, 0.1574803149606299191, 0.9940944880814488460 ) ) ;
#22045=CARTESIAN_POINT ( 'NONE',  ( -1.054774247047244540, -0.07405724077823318263, 0.3740157479777325711 ) ) ;
#22047=ORIENTED_EDGE ( 'NONE', *, *, #28773, .F. ) ;
#22048=CARTESIAN_POINT ( 'NONE',  ( -1.054774247047244540, 0.07405724077823318263, 1.683070866087970074 ) ) ;
#22049=CARTESIAN_POINT ( 'NONE',  ( 1.002407869896990045, 0.1264236179284866091, 1.646161417269070837 ) ) ;
#22051=CARTESIAN_POINT ( 'NONE',  ( -0.8019270111902717657, 0.1787899950787401604, 0.7480314960092282472 ) ) ;
#22052=CARTESIAN_POINT ( 'NONE',  ( 0.6971942568897637749, 2.189545951927499583E-17, 0.3223425196312759144 ) ) ;
#22053=CARTESIAN_POINT ( 'NONE',  ( -0.9873396505805591694, -0.1113553986120547346, 0.4675196849318432601 ) ) ;
#22054=CARTESIAN_POINT ( 'NONE',  ( 0.8019270111902716547, 0.1787899950787401604, 0.7086614172690703928 ) ) ;
#22055=CARTESIAN_POINT ( 'NONE',  ( -0.6971942568897648851, -0.07405724077823297447, 0.6742125983714336579 ) ) ;
#22057=( BOUNDED_CURVE ( )  B_SPLINE_CURVE ( 2, ( #2068, #27274, #42539, #38956, #9025, #9743, #45661, #5668, #38496 ),
 .UNSPECIFIED., .F., .F. ) 
 B_SPLINE_CURVE_WITH_KNOTS ( ( 3, 2, 2, 2, 3 ),
 ( 0.9399999999999999467, 0.9425000000000000044, 0.9449999999999999512, 0.9475000000000000089, 0.9499999999999999556 ),
 .UNSPECIFIED. ) 
 CURVE ( )  GEOMETRIC_REPRESENTATION_ITEM ( )  RATIONAL_B_SPLINE_CURVE ( ( 1.000000000000000000, 0.9238795325112899581, 1.000000000000000000, 0.9238795325112869605, 1.000000000000000000, 0.9238795325112869605, 1.000000000000000000, 0.9238795325112829637, 1.000000000000000000 ) ) 
 REPRESENTATION_ITEM ( '' )  ) ;
#22058=CARTESIAN_POINT ( 'NONE',  ( -0.8759842519685039353, -0.1787899950787401882, 1.592027559001354398 ) ) ;
#22059=CARTESIAN_POINT ( 'NONE',  ( -0.8107537697050253289, 0.1574803149606300301, 1.862696850286174710 ) ) ;
#22060=VERTEX_POINT ( 'NONE', #40808 ) ;
#22061=CARTESIAN_POINT ( 'NONE',  ( -0.7185039370078739607, 1.928577636452523993E-17, 1.643700787401574992 ) ) ;
#22062=DIRECTION ( 'NONE',  ( -1.000000000000000000, 0.000000000000000000, 0.000000000000000000 ) ) ;
#22063=CARTESIAN_POINT ( 'NONE',  ( 0.8019270111902716547, -0.1787899950787401604, 1.392716535379308285 ) ) ;
#22066=AXIS2_PLACEMENT_3D ( 'NONE', #17204, #13386, #28731 ) ;
#22068=VERTEX_POINT ( 'NONE', #22868 ) ;
#22071=( BOUNDED_CURVE ( )  B_SPLINE_CURVE ( 2, ( #40403, #22686, #33271, #12152, #33974, #7590, #1100, #26775, #41335 ),
 .UNSPECIFIED., .F., .T. ) 
 B_SPLINE_CURVE_WITH_KNOTS ( ( 3, 2, 2, 2, 3 ),
 ( 0.7099999999999999645, 0.7125000000000000222, 0.7149999999999999689, 0.7175000000000000266, 0.7199999999999999734 ),
 .UNSPECIFIED. ) 
 CURVE ( )  GEOMETRIC_REPRESENTATION_ITEM ( )  RATIONAL_B_SPLINE_CURVE ( ( 1.000000000000000000, 0.9238795325112869605, 1.000000000000000000, 0.9238795325112869605, 1.000000000000000000, 0.9238795325112869605, 1.000000000000000000, 0.9238795325112869605, 1.000000000000000000 ) ) 
 REPRESENTATION_ITEM ( '' )  ) ;
#22073=VERTEX_POINT ( 'NONE', #8242 ) ;
#22074=ADVANCED_FACE ( 'NONE', ( #4165 ), #37481, .T. ) ;
#22076=CARTESIAN_POINT ( 'NONE',  ( 0.6971942568897637749, 2.189545951927502049E-17, 4.498031496062992574 ) ) ;
#22077=CARTESIAN_POINT ( 'NONE',  ( 1.054774247047244540, -0.07405724077823318263, 1.791338582623401177 ) ) ;
#22081=CARTESIAN_POINT ( 'NONE',  ( 0.7185039370078746268, -0.06523048226347956391, 0.1402559054042841202 ) ) ;
#22083=CARTESIAN_POINT ( 'NONE',  ( 0.9500414927467378812, 0.1787899950787401604, 0.6594488188438737408 ) ) ;
#22085=CARTESIAN_POINT ( 'NONE',  ( 0.7185039370078739607, 1.928577636452523993E-17, 0.6889763778452283605 ) ) ;
#22086=CARTESIAN_POINT ( 'NONE',  ( 0.8107537697050254399, 0.1574803149606300301, 0.9571850392625507187 ) ) ;
#22087=CARTESIAN_POINT ( 'NONE',  ( 0.6971942568897637749, 2.189545951927499583E-17, 1.897145669237574772 ) ) ;
#22089=CARTESIAN_POINT ( 'NONE',  ( 0.8759842519685039353, 0.1574803149606299191, 0.1279527557979848462 ) ) ;
#22094=CARTESIAN_POINT ( 'NONE',  ( 0.7495606340400177148, 0.1264236179284866091, 0.08120078734781142893 ) ) ;
#22097=CARTESIAN_POINT ( 'NONE',  ( -1.054774247047244540, -0.07405724077823318263, 1.673228346402929834 ) ) ;
#22099=CARTESIAN_POINT ( 'NONE',  ( -1.002407869896990045, 0.1264236179284866091, 1.173720472387181246 ) ) ;
#22100=CARTESIAN_POINT ( 'NONE',  ( 0.7185039370078739607, 1.928577636452523993E-17, 0.2952755904436539236 ) ) ;
#22101=CARTESIAN_POINT ( 'NONE',  ( 0.8019270111902717657, -0.1787899950787401604, 0.05413385821395302888 ) ) ;
#22102=CARTESIAN_POINT ( 'NONE',  ( -0.7646288533564489232, -0.1113553986120547346, 0.6250000000000000000 ) ) ;
#22103=CARTESIAN_POINT ( 'NONE',  ( -1.054774247047244540, 0.07405724077823318263, 1.126968503883244654 ) ) ;
#22106=CARTESIAN_POINT ( 'NONE',  ( 0.8019270111902716547, 0.1787899950787401604, 0.3149606298674962890 ) ) ;
#22107=CARTESIAN_POINT ( 'NONE',  ( -1.054774247047244540, 0.07405724077823318263, 0.3001968503399373711 ) ) ;
#22109=CARTESIAN_POINT ( 'NONE',  ( -1.002407869896990045, -0.1264236179284866091, 0.7652559054580472253 ) ) ;
#22110=CARTESIAN_POINT ( 'NONE',  ( 0.8107537697050253289, -0.1574803149606297803, 1.719980314853102321 ) ) ;
#22115=CARTESIAN_POINT ( 'NONE',  ( 1.002407869896990045, 0.1264236179284866091, 0.7800196849856062542 ) ) ;
#22117=CARTESIAN_POINT ( 'NONE',  ( -0.7495606340400177148, 0.1264236179284866091, 1.887303149552535420 ) ) ;
#22118=ORIENTED_EDGE ( 'NONE', *, *, #27522, .F. ) ;
#22119=CARTESIAN_POINT ( 'NONE',  ( 0.9500414927467378812, 0.1787899950787401604, 1.879921259788756016 ) ) ;
#22127=CARTESIAN_POINT ( 'NONE',  ( 1.002407869896990045, 0.1264236179284866091, 1.168799212544661348 ) ) ;
#22132=CARTESIAN_POINT ( 'NONE',  ( 0.6971942568897626646, -0.07405724077823297447, 0.08366141726907129483 ) ) ;
#22136=CARTESIAN_POINT ( 'NONE',  ( -0.8019270111902716547, 0.1787899950787401604, 0.4724409448281262636 ) ) ;
#22137=CARTESIAN_POINT ( 'NONE',  ( 0.9412147342319837628, -0.1574803149606297803, 0.3075787400499532809 ) ) ;
#22139=CARTESIAN_POINT ( 'NONE',  ( -0.7103339159022584726, 0.006824654076337659594, 1.983144407867949655 ) ) ;
#22140=CARTESIAN_POINT ( 'NONE',  ( 0.8759842519685039353, 0.1574803149606299191, 1.437007874015747921 ) ) ;
#22141=CARTESIAN_POINT ( 'NONE',  ( 0.7495606340400177148, -0.1264236179284866091, 1.193405511757259951 ) ) ;
#22142=CARTESIAN_POINT ( 'NONE',  ( 0.7495606340400177148, 0.1264236179284866091, 1.611712598371433103 ) ) ;
#22144=CARTESIAN_POINT ( 'NONE',  ( 0.9412147342319837628, -0.1574803149606297803, 0.8981299211523156023 ) ) ;
#22145=CARTESIAN_POINT ( 'NONE',  ( -1.033464566929133799, 0.000000000000000000, 1.938976377952756014 ) ) ;
#22146=CARTESIAN_POINT ( 'NONE',  ( 0.9412147342319837628, -0.1574803149606297803, 0.5437992124908980207 ) ) ;
#22147=CARTESIAN_POINT ( 'NONE',  ( -1.033464566929134687, -0.06523048226347956391, 1.729822834538142784 ) ) ;
#22149=CARTESIAN_POINT ( 'NONE',  ( -0.8019270111902717657, 0.1787899950787401604, 1.254921259788757348 ) ) ;
#22150=CARTESIAN_POINT ( 'NONE',  ( 0.7185039370078739607, 1.928577636452523993E-17, 0.7283464565853858819 ) ) ;
#22151=EDGE_LOOP ( 'NONE', ( #20417, #11069, #17181, #30915 ) ) ;
#22153=CARTESIAN_POINT ( 'NONE',  ( 0.8857703219174262177, 0.1737007691241557183, 0.03937007805475359334 ) ) ;
#22154=CARTESIAN_POINT ( 'NONE',  ( -1.033464566929134687, 0.06523048226347956391, 1.587106299212598604 ) ) ;
#22155=CARTESIAN_POINT ( 'NONE',  ( 1.054774247047244540, 0.07405724077823318263, 1.638779527505292988 ) ) ;
#22156=CARTESIAN_POINT ( 'NONE',  ( -0.7185039370078739607, 1.928577636452523993E-17, 1.171259842519684957 ) ) ;
#22157=CARTESIAN_POINT ( 'NONE',  ( 0.7185039370078746268, 0.06523048226347956391, 1.916830708661418026 ) ) ;
#22159=CARTESIAN_POINT ( 'NONE',  ( 1.033464566929134687, -0.06523048226347956391, 1.336122047136566904 ) ) ;
#22160=ORIENTED_EDGE ( 'NONE', *, *, #19536, .F. ) ;
#22162=CARTESIAN_POINT ( 'NONE',  ( 0.9500414927467378812, 0.1787899950787401604, 0.5856299212060785964 ) ) ;
#22163=VERTEX_POINT ( 'NONE', #41276 ) ;
#22164=CARTESIAN_POINT ( 'NONE',  ( -1.054774247047244540, 0.07405724077823318263, 1.441929133804504604 ) ) ;
#22166=CARTESIAN_POINT ( 'NONE',  ( -0.8759842519685039353, -0.1787899950787401882, 1.198326771599779628 ) ) ;
#22171=CARTESIAN_POINT ( 'NONE',  ( -0.6971942568897626646, -0.07405724077823297447, 0.8366141731745828647 ) ) ;
#22173=CARTESIAN_POINT ( 'NONE',  ( -0.7495606340400177148, 0.1264236179284866091, 0.2386811023084413619 ) ) ;
#22174=DIRECTION ( 'NONE',  ( 0.000000000000000000, 0.000000000000000000, -1.000000000000000000 ) ) ;
#22175=CARTESIAN_POINT ( 'NONE',  ( 1.033464566929136907, -0.06523048226347749612, 1.651082677057827519 ) ) ;
#22180=VERTEX_POINT ( 'NONE', #14740 ) ;
#22181=EDGE_CURVE ( 'NONE', #18659, #23819, #40577, .T. ) ;
#22183=CARTESIAN_POINT ( 'NONE',  ( 0.8759842519685039353, -0.1574803149606299191, 1.210629921152315047 ) ) ;
#22184=CARTESIAN_POINT ( 'NONE',  ( -1.054774247047244540, -0.07405724077823318263, 0.7677165353793073965 ) ) ;
#22185=( BOUNDED_CURVE ( )  B_SPLINE_CURVE ( 2, ( #13422, #32353, #10537, #28520, #39033, #35917, #13638, #35695, #35464 ),
 .UNSPECIFIED., .F., .T. ) 
 B_SPLINE_CURVE_WITH_KNOTS ( ( 3, 2, 2, 2, 3 ),
 ( 0.5100000000000000089, 0.5124999999999999556, 0.5150000000000000133, 0.5174999999999999600, 0.5200000000000000178 ),
 .UNSPECIFIED. ) 
 CURVE ( )  GEOMETRIC_REPRESENTATION_ITEM ( )  RATIONAL_B_SPLINE_CURVE ( ( 1.000000000000000000, 0.9238795325112869605, 1.000000000000000000, 0.9238795325112869605, 1.000000000000000000, 0.9238795325112869605, 1.000000000000000000, 0.9238795325112869605, 1.000000000000000000 ) ) 
 REPRESENTATION_ITEM ( '' )  ) ;
#22187=CARTESIAN_POINT ( 'NONE',  ( -1.054774247047244540, -0.07405724077823318263, 1.835629921206078485 ) ) ;
#22188=EDGE_CURVE ( 'NONE', #13130, #8550, #13133, .T. ) ;
#22191=CARTESIAN_POINT ( 'NONE',  ( -0.9500414927467377701, 0.1787899950787401604, 0.07381889758403178958 ) ) ;
#22194=CARTESIAN_POINT ( 'NONE',  ( -0.7646288533564489232, -0.1113553986120547346, 1.481299212490897466 ) ) ;
#22195=CARTESIAN_POINT ( 'NONE',  ( 1.054774247047244540, 0.07405724077823318263, 0.8169291338045038264 ) ) ;
#22196=CARTESIAN_POINT ( 'NONE',  ( 0.8759842519685039353, -0.1787899950787401882, 1.350885826717889815 ) ) ;
#22198=CARTESIAN_POINT ( 'NONE',  ( 0.7646288533564489232, 0.1113553986120547346, 1.441929133858267598 ) ) ;
#22199=CARTESIAN_POINT ( 'NONE',  ( 0.7836433926840684627, -0.1444537073663495208, 1.986395014210853738 ) ) ;
#22202=CARTESIAN_POINT ( 'NONE',  ( -1.033464566929133799, 0.000000000000000000, 0.9055118109160944506 ) ) ;
#22204=CARTESIAN_POINT ( 'NONE',  ( 0.7495606340400177148, 0.1264236179284866091, 0.9030511810485984947 ) ) ;
#22205=DIRECTION ( 'NONE',  ( 0.000000000000000000, 0.000000000000000000, -1.000000000000000000 ) ) ;
#22208=CARTESIAN_POINT ( 'NONE',  ( -1.033464566929133799, 0.000000000000000000, 0.8366141732283465249 ) ) ;
#22209=DIRECTION ( 'NONE',  ( 1.822029033848725028E-16, 0.000000000000000000, 1.000000000000000000 ) ) ;
#22210=CARTESIAN_POINT ( 'NONE',  ( 0.6971942568897648851, -0.07405724077823297447, 1.028543307032851795 ) ) ;
#22216=CARTESIAN_POINT ( 'NONE',  ( -0.9500414927467378812, 0.1787899950787401604, 0.06889763774151215492 ) ) ;
#22217=EDGE_LOOP ( 'NONE', ( #34827, #27613, #8011 ) ) ;
#22218=CARTESIAN_POINT ( 'NONE',  ( -0.8107537697050254399, -0.1574803149606297803, 0.7062007874015745479 ) ) ;
#22219=CARTESIAN_POINT ( 'NONE',  ( 1.033464566929134687, -0.06523048226347956391, 0.3518700786326304231 ) ) ;
#22220=CARTESIAN_POINT ( 'NONE',  ( -1.054774247047244540, -0.07405724077823318263, 1.751968503883245765 ) ) ;
#22222=CARTESIAN_POINT ( 'NONE',  ( -1.002407869896990045, 0.1264236179284866091, 1.050688976324189117 ) ) ;
#22225=CARTESIAN_POINT ( 'NONE',  ( 0.8759842519685039353, -0.1574803149606299191, 0.9842519685039370358 ) ) ;
#22232=EDGE_CURVE ( 'NONE', #12067, #10459, #16202, .T. ) ;
#22235=VECTOR ( 'NONE', #16633, 39.37007874015748143 ) ;
#22236=CARTESIAN_POINT ( 'NONE',  ( -0.8019270111902717657, -0.1787899950787401604, 0.2854330708123783422 ) ) ;
#22238=CARTESIAN_POINT ( 'NONE',  ( 0.7646288533564489232, 0.1113553986120547346, 0.8120078740157481434 ) ) ;
#22240=CARTESIAN_POINT ( 'NONE',  ( -0.9500414927467377701, -0.1787899950787401604, 1.397637795221827517 ) ) ;
#22241=ORIENTED_EDGE ( 'NONE', *, *, #34217, .F. ) ;
#22245=CARTESIAN_POINT ( 'NONE',  ( 0.8107537697050253289, -0.1574803149606297803, 0.3518700787401576324 ) ) ;
#22248=CARTESIAN_POINT ( 'NONE',  ( -0.7185039370078746268, -0.06523048226347956391, 1.085137795168063413 ) ) ;
#22249=CARTESIAN_POINT ( 'NONE',  ( 0.7495606340400177148, -0.1264236179284866091, 0.4060039369541102450 ) ) ;
#22250=CARTESIAN_POINT ( 'NONE',  ( -0.9873396505805591694, -0.1113553986120547346, 1.491141732175936818 ) ) ;
#22252=CARTESIAN_POINT ( 'NONE',  ( 0.7185039370078746268, -0.06523048226347956391, 1.951279527451529772 ) ) ;
#22255=CARTESIAN_POINT ( 'NONE',  ( 0.7646288533564489232, 0.1113553986120547346, 1.008858267716535417 ) ) ;
#22256=CARTESIAN_POINT ( 'NONE',  ( -1.033464566929133799, 0.000000000000000000, 1.850393700679873854 ) ) ;
#22262=DIRECTION ( 'NONE',  ( 0.000000000000000000, 0.000000000000000000, -1.000000000000000000 ) ) ;
#22263=CARTESIAN_POINT ( 'NONE',  ( -1.033464566929134687, -0.06523048226347956391, 0.9916338582677169944 ) ) ;
#22268=CARTESIAN_POINT ( 'NONE',  ( 0.9412147342319837628, 0.1574803149606300301, 1.031003936900347639 ) ) ;
#22269=CARTESIAN_POINT ( 'NONE',  ( 1.033464566929134687, 0.06523048226347956391, 1.823326771653542178 ) ) ;
#22270=CARTESIAN_POINT ( 'NONE',  ( -0.8019270111902717657, 0.1787899950787401604, 0.3887795275052913224 ) ) ;
#22272=ORIENTED_EDGE ( 'NONE', *, *, #14131, .F. ) ;
#22273=VERTEX_POINT ( 'NONE', #26959 ) ;
#22274=CARTESIAN_POINT ( 'NONE',  ( -1.054774247047244540, 0.07405724077823318263, 1.643700787347811998 ) ) ;
#22276=CARTESIAN_POINT ( 'NONE',  ( 1.054774247047244540, -0.07405724077823318263, 1.717519684985606476 ) ) ;
#22277=CARTESIAN_POINT ( 'NONE',  ( -0.6971942568897626646, -0.07405724077823297447, 0.7578740156942689321 ) ) ;
#22279=CARTESIAN_POINT ( 'NONE',  ( 0.8759842519685039353, -0.1787899950787401882, 0.2534448818360003908 ) ) ;
#22281=CARTESIAN_POINT ( 'NONE',  ( -1.054774247047244096, 0.000000000000000000, 1.203248031442299304 ) ) ;
#22282=CARTESIAN_POINT ( 'NONE',  ( -1.054774247047244540, -0.07405724077823318263, 0.8070866141194653620 ) ) ;
#22283=CARTESIAN_POINT ( 'NONE',  ( 0.9412147342319837628, 0.1574803149606300301, 0.9128937006798734100 ) ) ;
#22285=LINE ( 'NONE', #45022, #16833 ) ;
#22286=CARTESIAN_POINT ( 'NONE',  ( -1.002407869896990045, 0.1264236179284866091, 1.567421259788755794 ) ) ;
#22287=CARTESIAN_POINT ( 'NONE',  ( -0.7185039370078746268, -0.06523048226347956391, 1.951279527451529772 ) ) ;
#22288=EDGE_LOOP ( 'NONE', ( #31628, #23686, #28885, #15925 ) ) ;
#22290=CARTESIAN_POINT ( 'NONE',  ( -0.9412147342319837628, 0.1574803149606300301, 1.552657480314961536 ) ) ;
#22291=CARTESIAN_POINT ( 'NONE',  ( 0.8759842519685039353, 0.000000000000000000, 4.498031496062992574 ) ) ;
#22292=CARTESIAN_POINT ( 'NONE',  ( 0.6971942568897648851, 0.07405724077823318263, 1.422244094434425898 ) ) ;
#22301=AXIS2_PLACEMENT_3D ( 'NONE', #26302, #37775, #4928 ) ;
#22310=CARTESIAN_POINT ( 'NONE',  ( 0.8759842519685039353, -0.1574803149606299191, 0.1476377951680635792 ) ) ;
#22311=CARTESIAN_POINT ( 'NONE',  ( 1.054774247047244096, 0.000000000000000000, 0.7308070865604093802 ) ) ;
#22312=CARTESIAN_POINT ( 'NONE',  ( -1.011560127499680828, 0.09259506503980204084, 0.03937007874015843734 ) ) ;
#22313=CARTESIAN_POINT ( 'NONE',  ( 0.7646288533564489232, -0.1113553986120547346, 1.126968503829480328 ) ) ;
#22316=CARTESIAN_POINT ( 'NONE',  ( 0.8107537697050254399, -0.1574803149606297803, 1.690452755905512916 ) ) ;
#22317=CARTESIAN_POINT ( 'NONE',  ( 0.6971942568897637749, 2.189545951927499583E-17, 1.779035433017102319 ) ) ;
#22320=VECTOR ( 'NONE', #35308, 39.37007874015748143 ) ;
#22321=CARTESIAN_POINT ( 'NONE',  ( 0.7185039370078739607, 1.928577636452523993E-17, 1.318897637687747926 ) ) ;
#22324=CARTESIAN_POINT ( 'NONE',  ( 0.7185039370078739607, 1.928577636452523993E-17, 0.06889763779527559306 ) ) ;
#22326=CARTESIAN_POINT ( 'NONE',  ( 0.7495606340400177148, -0.1264236179284866091, 0.1697834645131657827 ) ) ;
#22327=( BOUNDED_CURVE ( )  B_SPLINE_CURVE ( 2, ( #7297, #29150, #14491, #15206, #44397, #36054, #10912, #40103, #3697 ),
 .UNSPECIFIED., .F., .F. ) 
 B_SPLINE_CURVE_WITH_KNOTS ( ( 3, 2, 2, 2, 3 ),
 ( 0.5999999999999999778, 0.6025000000000000355, 0.6049999999999999822, 0.6075000000000000400, 0.6099999999999999867 ),
 .UNSPECIFIED. ) 
 CURVE ( )  GEOMETRIC_REPRESENTATION_ITEM ( )  RATIONAL_B_SPLINE_CURVE ( ( 1.000000000000000000, 0.9238795325112869605, 1.000000000000000000, 0.9238795325112869605, 1.000000000000000000, 0.9238795325112869605, 1.000000000000000000, 0.9238795325112869605, 1.000000000000000000 ) ) 
 REPRESENTATION_ITEM ( '' )  ) ;
#22329=CARTESIAN_POINT ( 'NONE',  ( -0.6971942568897648851, -0.07405724077823297447, 1.619094488135213838 ) ) ;
#22331=CARTESIAN_POINT ( 'NONE',  ( -1.002407869896990045, -0.1264236179284866091, 1.124507873961984261 ) ) ;
#22332=CARTESIAN_POINT ( 'NONE',  ( 0.9500414927467378812, 0.1787899950787401604, 1.294291338528912982 ) ) ;
#22334=AXIS2_PLACEMENT_3D ( 'NONE', #3542, #19074, #41100 ) ;
#22335=CARTESIAN_POINT ( 'NONE',  ( 0.9500414927467378812, -0.1787899950787401604, 0.05905511805647267048 ) ) ;
#22336=CARTESIAN_POINT ( 'NONE',  ( -0.6971942568897637749, 2.189545951927499583E-17, 1.065452755851747924 ) ) ;
#22337=CARTESIAN_POINT ( 'NONE',  ( -0.6971942568897637749, -2.189545951927502049E-17, 1.990649606245448844 ) ) ;
#22339=CARTESIAN_POINT ( 'NONE',  ( 0.8019270111902716547, 0.1787899950787401604, 0.3937007873478114983 ) ) ;
#22340=CARTESIAN_POINT ( 'NONE',  ( -0.9500414927467377701, -0.1787899950787401604, 0.2509842519147403861 ) ) ;
#22341=CARTESIAN_POINT ( 'NONE',  ( -0.6971942568897637749, 2.189545951927499583E-17, 0.7898622046706456068 ) ) ;
#22342=CARTESIAN_POINT ( 'NONE',  ( 0.9412147342319837628, -0.1574803149606297803, 1.724901574695621553 ) ) ;
#22343=ORIENTED_EDGE ( 'NONE', *, *, #19902, .F. ) ;
#22344=ADVANCED_FACE ( 'NONE', ( #27681 ), #35086, .T. ) ;
#22346=CARTESIAN_POINT ( 'NONE',  ( 0.7495606340400177148, -0.1264236179284866091, 0.8784448818360000022 ) ) ;
#22347=CARTESIAN_POINT ( 'NONE',  ( 0.6971942568897637749, 2.189545951927499583E-17, 0.9916338582139527791 ) ) ;
#22348=CARTESIAN_POINT ( 'NONE',  ( -0.6971942568897648851, 0.07405724077823318263, 1.850393700733638624 ) ) ;
#22349=VERTEX_POINT ( 'NONE', #31495 ) ;
#22351=( BOUNDED_CURVE ( )  B_SPLINE_CURVE ( 2, ( #34389, #26737, #8493, #11874, #15237, #26262, #23126, #40824, #41527, #4407, #1529, #45383, #19036, #15475, #20927, #35568, #31275, #9461, #35335, #19987, #5856, #42708, #34627, #9926, #38908, #28385, #45853, #28148, #2245, #6304, #31745, #6069, #24533, #42006, #13744, #31043, #24079, #5368, #42953, #31975, #1776, #12829, #2476, #9210, #20693, #17102, #34870, #46331, #27923, #13515, #2713, #2017, #42486, #17340, #45611, #39133, #38687, #46559, #16416, #27460, #38445, #23831, #5614, #9693, #20221, #16865, #16645, #10161, #38206, #13061, #27698, #20463, #42262, #35098, #31508, #46090, #13294, #24307, #40304, #17572, #32461, #39832, #21400, #10640, #14939, #43192, #36025, #21888, #7270, #28635, #11113, #43432, #29601, #10882, #14697, #10404, #36509, #25733, #3664, #47040, #18287, #29371, #39604, #6781, #32929, #3186, #25006, #21649, #17814, #24770, #39367, #43911, #25245, #22106, #7487, #14232, #6548, #29120, #28874, #7024, #36282, #18519, #21160, #3433, #32212, #25502, #50, #35793, #18047, #32692, #36734, #46800, #47283, #14460, #3892, #33171, #293, #2935, #13984, #43671, #40070, #33402, #7722, #18744, #19450, #22339, #12286, #15409, #748, #37195, #16121, #36967, #41001, #25954, #4581, #519, #45071, #4827, #40533, #30510, #41465, #30743, #11341, #30056, #26438, #22813, #4120, #15886, #15177, #26905, #12051, #1461, #4339, #1232, #37427, #8663, #11573, #8189, #5071, #29820, #44366, #18972, #23299, #26200, #33634, #37916, #19216, #30289, #994, #19687, #40766, #7962, #34331, #8427, #22581, #44598, #11814, #33875, #15651, #44841, #26673, #41223, #23055, #37675, #34105, #9392, #12534, #9861, #1706, #16803, #42649, #24473, #35033, #17042, #27634, #1952, #5548, #35506, #17279, #45316, #16583, #27154, #12992, #2411, #41709, #13458, #34554, #41940, #8909, #31211, #45784, #23540, #9147, #2181, #28088, #38141, #6009, #42187, #39068, #5305, #19922, #6238, #16353, #30976, #31443, #45542, #24010, #12765, #20629, #38842, #27396, #31683, #38611, #20863, #23765, #5789, #38374, #2646, #20394, #20158, #34808, #46024, #13236, #27864, #42421, #9629, #24246, #46263, #29056, #14406, #35737, #32869, #17750, #22054, #17983, #21827, #17509, #43612, #23997, #40010, #6719, #32398, #36454, #13919, #28566, #7205, #43134, #32143, #28812, #2874, #31915, #42881, #14637, #46975, #29306, #11057, #21334, #10091, #3374, #35965, #43374, #24703, #21099, #10586, #39769, #40247, #6960, #7435, #21580, #39304, #32636, #47223, #7790, #15012, #37033, #22655, #43323, #33236, #10284, #4183, #363, #40833, #46676, #32341, #44432, #10525, #37260, #35908, #3063, #26022, #24892, #39491, #29888, #39715, #43079, #35687, #24659, #39253, #8026, #17692, #17928, #18810, #46922, #22407, #11648, #13867, #28755, #6427, #29666, #25123, #33467, #15242, #21521, #14111, #36158, #3312, #11404, #40597, #4412, #19042, #26270, #818, #15480, #12118, #23375, #5621, #8264, #26740, #19286, #41778, #8979, #16653, #41532, #5137, #23600, #41299, #34395, #8499, #38212, #31051, #20229, #22888, #11881, #1304, #15960, #19993, #37502, #39842, #22347, #28882, #33410, #36517, #21895, #10890, #37203, #10648, #14703, #47048, #25740, #7031, #18752, #29378, #3672, #40080, #22590, #4346, #32469, #18295, #57, #43918, #43443, #36973, #14241, #4128, #33179, #25253, #25510, #15184, #11123, #29830, #44373, #11581, #36290, #7969, #21658, #300, #3442, #7277, #26208, #40313, #40773, #18054, #14946, #32701, #47291, #14471, #29127, #32936, #43681, #7496, #36741, #3899, #18524, #44150, #11350, #30753, #45324, #15657, #12540, #8672, #41715, #30983, #37682, #26914, #4588, #8917, #41468, #5312, #45550, #34563, #38381, #4835, #12770, #12057, #26681, #19696, #19224, #33881, #1715, #34111, #22822, #26443, #18981, #33644, #41948, #37439, #12291, #37922, #9154, #41008, #19457, #8199, #23064, #15894, #23305, #45080, #5076, #34337, #24254, #45793, #20638, #38851, #9402, #6016, #35746, #32154, #24017, #35283, #39314, #17517, #35515, #46742, #34816, #38619, #12999, #6248, #2656, #43141, #2420, #17050, #17287, #27642, #13466, #2189, #31922, #24714, #21107, #13687, #46506, #28095, #28323, #42196, #1958, #5796, #42892, #16591, #6489, #9636, #42429, #31449, #10347, #31216, #31692, #20163, #46272, #20402, #2881, #10102, #35042, #13931, #28576, #24956, #5554, #9871, #39076, #20873, #16811, #46033, #27870, #11295, #43383, #22063, #3848, #36231, #36688, #29317, #18469, #36927, #10830, #4808, #25192, #18695, #21838, #22292, #32409, #47231, #25907, #25445, #4079, #3384, #17992, #40256, #39778, #6970, #44101, #7214, #10594, #3132, #44325, #11528, #33356, #33120, #477, #245, #14416, #14888, #15131, #46984, #43623, #39554, #43864, #36461, #29550, #29776, #3618, #14178, #18235, #32879, #21594, #14645, #6727, #21345, #11066, #32646, #29065, #25684, #7443, #35973, #17760, #28821, #18931, #26866, #37877, #30943, #12009, #41182, #5030, #33590, #1190, #22770, #19652, #16080, #34296, #37150, #26148, #948, #8146, #703, #22532, #15361, #1421, #4298, #27117, #30245, #15607, #4534, #45504, #30011, #8385, #40718, #19411, #15849, #45271, #23014, #44796, #26630, #44557, #11775, #26393, #37627, #4785, #30472, #40956, #30705, #37379, #12491, #41427, #19171, #45028, #41664, #12243, #8624, #23502, #38104, #5268, #19886, #1667, #27830, #12728, #38334, #20121, #31173, #31410, #23730, #34998, #42390, #23973, #45986, #27594, #45746, #16546, #24209, #42144, #9352, #2143, #27358, #38576, #13194, #41901, #9110, #5745, #20359, #5507, #16769, #34768, #1910, #4694, #12400, #23636, #857, #16225, #15516, #26777, #22687, #12869, #1817, #37291, #11918, #27021, #41101, #34208, #4442, #30857, #1573, #22922, #27261, #37784, #38247, #37535, #41336, #44700, #4936, #5408, #26541, #15758, #41813, #8535, #20029, #19326, #33975, #8775, #8295, #1101, #12637, #23167, #30392, #19076, #27502, #33748, #34670, #44941, #9014, #34427, #12153, #5175, #16454, #19562, #1336, #15992, #45179, #30615, #38014, #45420, #41570, #23410, #19793, #31087, #45651, #13332, #24808, #21202, #46371, #20505, #16915, #9499, #38944, #35836, #38485, #13107, #34912, #42747, #39175, #32260, #27961, #9730, #6348, #2055, #2518, #38725, #20962, #13783, #35608, #5655, #42053, #31554, #24120, #16688, #27738, #5893, #2749, #35142, #42994, #46132, #42528, #24347 ),
 .UNSPECIFIED., .F., .T. ) 
 B_SPLINE_CURVE_WITH_KNOTS ( ( 3, 2, 2, 2, 2, 2, 2, 2, 2, 2, 2, 2, 2, 2, 2, 2, 2, 2, 2, 2, 2, 2, 2, 2, 2, 2, 2, 2, 2, 2, 2, 2, 2, 2, 2, 2, 2, 2, 2, 2, 2, 2, 2, 2, 2, 2, 2, 2, 2, 2, 2, 2, 2, 2, 2, 2, 2, 2, 2, 2, 2, 2, 2, 2, 2, 2, 2, 2, 2, 2, 2, 2, 2, 2, 2, 2, 2, 2, 2, 2, 2, 2, 2, 2, 2, 2, 2, 2, 2, 2, 2, 2, 2, 2, 2, 2, 2, 2, 2, 2, 2, 2, 2, 2, 2, 2, 2, 2, 2, 2, 2, 2, 2, 2, 2, 2, 2, 2, 2, 2, 2, 2, 2, 2, 2, 2, 2, 2, 2, 2, 2, 2, 2, 2, 2, 2, 2, 2, 2, 2, 2, 2, 2, 2, 2, 2, 2, 2, 2, 2, 2, 2, 2, 2, 2, 2, 2, 2, 2, 2, 2, 2, 2, 2, 2, 2, 2, 2, 2, 2, 2, 2, 2, 2, 2, 2, 2, 2, 2, 2, 2, 2, 2, 2, 2, 2, 2, 2, 2, 2, 2, 2, 2, 2, 2, 2, 2, 2, 2, 2, 2, 2, 2, 2, 2, 2, 2, 2, 2, 2, 2, 2, 2, 2, 2, 2, 2, 2, 2, 2, 2, 2, 2, 2, 2, 2, 2, 2, 2, 2, 2, 2, 2, 2, 2, 2, 2, 2, 2, 2, 2, 2, 2, 2, 2, 2, 2, 2, 2, 2, 2, 2, 2, 2, 2, 2, 2, 2, 2, 2, 2, 2, 2, 2, 2, 2, 2, 2, 2, 2, 2, 2, 2, 2, 2, 2, 2, 2, 2, 2, 2, 2, 2, 2, 2, 2, 2, 2, 2, 2, 2, 2, 2, 2, 2, 2, 2, 2, 2, 2, 2, 2, 2, 2, 2, 2, 2, 2, 2, 2, 2, 2, 2, 2, 2, 2, 2, 2, 2, 2, 2, 2, 2, 2, 2, 2, 2, 2, 2, 2, 2, 2, 2, 2, 2, 2, 2, 2, 2, 2, 2, 2, 2, 2, 2, 2, 2, 2, 2, 2, 2, 2, 2, 2, 2, 2, 2, 2, 2, 2, 2, 2, 2, 2, 2, 2, 2, 2, 2, 2, 2, 2, 2, 2, 2, 2, 2, 2, 2, 2, 2, 2, 2, 2, 2, 2, 2, 2, 2, 2, 2, 2, 2, 2, 2, 2, 2, 3 ),
 ( 0.006249999973727609834, 0.007499999999999999722, 0.01000000000000000021, 0.01250000000000000069, 0.01499999999999999944, 0.01750000000000000167, 0.02000000000000000042, 0.02249999999999999917, 0.02500000000000000139, 0.02750000000000000361, 0.02999999999999999889, 0.03249999999999999417, 0.03500000000000000333, 0.03749999999999999861, 0.04000000000000000083, 0.04250000000000000305, 0.04499999999999999833, 0.04750000000000000056, 0.05000000000000000278, 0.05249999999999999806, 0.05500000000000000028, 0.05750000000000000250, 0.05999999999999999778, 0.06250000000000000000, 0.06500000000000000222, 0.06750000000000000444, 0.07000000000000000666, 0.07249999999999999500, 0.07500000000000001110, 0.07749999999999999944, 0.08000000000000000167, 0.08250000000000000389, 0.08500000000000000611, 0.08749999999999999445, 0.08999999999999999667, 0.09249999999999999889, 0.09500000000000000111, 0.09750000000000000333, 0.1000000000000000056, 0.1024999999999999939, 0.1049999999999999961, 0.1074999999999999983, 0.1100000000000000006, 0.1125000000000000028, 0.1150000000000000050, 0.1174999999999999933, 0.1199999999999999956, 0.1224999999999999978, 0.1250000000000000000, 0.1275000000000000022, 0.1300000000000000044, 0.1325000000000000067, 0.1350000000000000089, 0.1374999999999999833, 0.1400000000000000133, 0.1424999999999999878, 0.1449999999999999900, 0.1474999999999999922, 0.1499999999999999944, 0.1524999999999999967, 0.1549999999999999989, 0.1575000000000000011, 0.1600000000000000033, 0.1625000000000000056, 0.1650000000000000078, 0.1675000000000000100, 0.1700000000000000122, 0.1724999999999999867, 0.1749999999999999889, 0.1774999999999999911, 0.1799999999999999933, 0.1824999999999999956, 0.1849999999999999978, 0.1875000000000000000, 0.1900000000000000022, 0.1925000000000000044, 0.1950000000000000067, 0.1975000000000000089, 0.2000000000000000111, 0.2025000000000000133, 0.2049999999999999878, 0.2074999999999999900, 0.2099999999999999922, 0.2124999999999999944, 0.2149999999999999967, 0.2174999999999999989, 0.2200000000000000011, 0.2225000000000000033, 0.2250000000000000056, 0.2275000000000000078, 0.2300000000000000100, 0.2325000000000000122, 0.2349999999999999867, 0.2374999999999999889, 0.2399999999999999911, 0.2424999999999999933, 0.2449999999999999956, 0.2474999999999999978, 0.2500000000000000000, 0.2525000000000000022, 0.2550000000000000044, 0.2575000000000000067, 0.2600000000000000089, 0.2625000000000000111, 0.2650000000000000133, 0.2675000000000000155, 0.2700000000000000178, 0.2725000000000000200, 0.2750000000000000222, 0.2775000000000000244, 0.2800000000000000266, 0.2824999999999999734, 0.2849999999999999756, 0.2874999999999999778, 0.2899999999999999800, 0.2924999999999999822, 0.2949999999999999845, 0.2974999999999999867, 0.2999999999999999889, 0.3024999999999999911, 0.3049999999999999933, 0.3074999999999999956, 0.3099999999999999978, 0.3125000000000000000, 0.3150000000000000022, 0.3175000000000000044, 0.3200000000000000067, 0.3225000000000000089, 0.3250000000000000111, 0.3275000000000000133, 0.3300000000000000155, 0.3325000000000000178, 0.3350000000000000200, 0.3375000000000000222, 0.3400000000000000244, 0.3425000000000000266, 0.3449999999999999734, 0.3474999999999999756, 0.3499999999999999778, 0.3524999999999999800, 0.3549999999999999822, 0.3574999999999999845, 0.3599999999999999867, 0.3624999999999999889, 0.3649999999999999911, 0.3674999999999999933, 0.3699999999999999956, 0.3724999999999999978, 0.3750000000000000000, 0.3775000000000000022, 0.3800000000000000044, 0.3825000000000000067, 0.3850000000000000089, 0.3875000000000000111, 0.3900000000000000133, 0.3925000000000000155, 0.3950000000000000178, 0.3975000000000000200, 0.4000000000000000222, 0.4025000000000000244, 0.4050000000000000266, 0.4074999999999999734, 0.4099999999999999756, 0.4124999999999999778, 0.4149999999999999800, 0.4174999999999999822, 0.4199999999999999845, 0.4224999999999999867, 0.4249999999999999889, 0.4274999999999999911, 0.4299999999999999933, 0.4324999999999999956, 0.4349999999999999978, 0.4375000000000000000, 0.4400000000000000022, 0.4425000000000000044, 0.4450000000000000067, 0.4475000000000000089, 0.4500000000000000111, 0.4525000000000000133, 0.4550000000000000155, 0.4575000000000000178, 0.4600000000000000200, 0.4625000000000000222, 0.4650000000000000244, 0.4675000000000000266, 0.4699999999999999734, 0.4724999999999999756, 0.4749999999999999778, 0.4774999999999999800, 0.4799999999999999822, 0.4824999999999999845, 0.4849999999999999867, 0.4874999999999999889, 0.4899999999999999911, 0.4924999999999999933, 0.4949999999999999956, 0.4974999999999999978, 0.5000000000000000000, 0.5024999999999999467, 0.5050000000000000044, 0.5074999999999999512, 0.5100000000000000089, 0.5124999999999999556, 0.5150000000000000133, 0.5174999999999999600, 0.5200000000000000178, 0.5224999999999999645, 0.5250000000000000222, 0.5274999999999999689, 0.5300000000000000266, 0.5324999999999999734, 0.5350000000000000311, 0.5374999999999999778, 0.5400000000000000355, 0.5424999999999999822, 0.5450000000000000400, 0.5474999999999999867, 0.5500000000000000444, 0.5524999999999999911, 0.5550000000000000488, 0.5574999999999999956, 0.5600000000000000533, 0.5625000000000000000, 0.5649999999999999467, 0.5675000000000000044, 0.5699999999999999512, 0.5725000000000000089, 0.5749999999999999556, 0.5775000000000000133, 0.5799999999999999600, 0.5825000000000000178, 0.5849999999999999645, 0.5875000000000000222, 0.5899999999999999689, 0.5925000000000000266, 0.5949999999999999734, 0.5975000000000000311, 0.5999999999999999778, 0.6025000000000000355, 0.6049999999999999822, 0.6075000000000000400, 0.6099999999999999867, 0.6125000000000000444, 0.6149999999999999911, 0.6175000000000000488, 0.6199999999999999956, 0.6225000000000000533, 0.6250000000000000000, 0.6274999999999999467, 0.6300000000000000044, 0.6324999999999999512, 0.6350000000000000089, 0.6374999999999999556, 0.6400000000000000133, 0.6424999999999999600, 0.6450000000000000178, 0.6474999999999999645, 0.6500000000000000222, 0.6524999999999999689, 0.6550000000000000266, 0.6574999999999999734, 0.6600000000000000311, 0.6624999999999999778, 0.6650000000000000355, 0.6674999999999999822, 0.6700000000000000400, 0.6724999999999999867, 0.6750000000000000444, 0.6774999999999999911, 0.6800000000000000488, 0.6824999999999999956, 0.6850000000000000533, 0.6875000000000000000, 0.6899999999999999467, 0.6925000000000000044, 0.6949999999999999512, 0.6975000000000000089, 0.6999999999999999556, 0.7025000000000000133, 0.7049999999999999600, 0.7075000000000000178, 0.7099999999999999645, 0.7125000000000000222, 0.7149999999999999689, 0.7175000000000000266, 0.7199999999999999734, 0.7225000000000000311, 0.7249999999999999778, 0.7275000000000000355, 0.7299999999999999822, 0.7325000000000000400, 0.7349999999999999867, 0.7375000000000000444, 0.7399999999999999911, 0.7425000000000000488, 0.7449999999999999956, 0.7475000000000000533, 0.7500000000000000000, 0.7524999999999999467, 0.7550000000000000044, 0.7574999999999999512, 0.7600000000000000089, 0.7624999999999999556, 0.7650000000000000133, 0.7674999999999999600, 0.7700000000000000178, 0.7724999999999999645, 0.7750000000000000222, 0.7774999999999999689, 0.7799999999999999156, 0.7824999999999999734, 0.7850000000000000311, 0.7874999999999999778, 0.7900000000000000355, 0.7924999999999999822, 0.7950000000000000400, 0.7975000000000000977, 0.8000000000000000444, 0.8024999999999999911, 0.8050000000000000488, 0.8074999999999999956, 0.8100000000000000533, 0.8125000000000000000, 0.8150000000000000577, 0.8175000000000000044, 0.8199999999999999512, 0.8225000000000000089, 0.8249999999999999556, 0.8275000000000000133, 0.8299999999999999600, 0.8325000000000000178, 0.8349999999999999645, 0.8375000000000000222, 0.8399999999999999689, 0.8425000000000000266, 0.8449999999999999734, 0.8475000000000000311, 0.8499999999999999778, 0.8525000000000000355, 0.8549999999999999822, 0.8575000000000000400, 0.8599999999999999867, 0.8625000000000000444, 0.8649999999999999911, 0.8675000000000000488, 0.8699999999999999956, 0.8725000000000000533, 0.8750000000000000000, 0.8774999999999999467, 0.8800000000000000044, 0.8824999999999999512, 0.8850000000000000089, 0.8874999999999999556, 0.8900000000000000133, 0.8924999999999999600, 0.8950000000000000178, 0.8974999999999999645, 0.9000000000000000222, 0.9024999999999999689, 0.9050000000000000266, 0.9074999999999999734, 0.9100000000000000311, 0.9124999999999999778, 0.9150000000000000355, 0.9174999999999999822, 0.9200000000000000400, 0.9224999999999999867, 0.9250000000000000444, 0.9274999999999999911, 0.9300000000000000488, 0.9324999999999999956, 0.9350000000000000533, 0.9375000000000000000, 0.9399999999999999467, 0.9425000000000000044, 0.9449999999999999512, 0.9475000000000000089, 0.9499999999999999556, 0.9525000000000000133, 0.9549999999999999600, 0.9575000000000000178, 0.9599999999999999645, 0.9625000000000000222, 0.9649999999999999689, 0.9675000000000000266, 0.9699999999999999734, 0.9725000000000000311, 0.9749999999999999778, 0.9775000000000000355, 0.9799999999999999822, 0.9825000000000000400, 0.9849999999999999867, 0.9875000000000000444, 0.9899999999999999911, 0.9925000000000000488, 0.9949999999999999956, 0.9975000000000000533 ),
 .UNSPECIFIED. ) 
 CURVE ( )  GEOMETRIC_REPRESENTATION_ITEM ( )  RATIONAL_B_SPLINE_CURVE ( ( 0.9619397662556429252, 0.9619397654556960386, 1.000000000000000000, 0.9238795325112869605, 1.000000000000000000, 0.9238795325112869605, 1.000000000000000000, 0.9238795325112869605, 1.000000000000000000, 0.9238795325112869605, 1.000000000000000000, 0.9238795325112869605, 1.000000000000000000, 0.9238795325112869605, 1.000000000000000000, 0.9238795325112869605, 1.000000000000000000, 0.9238795325112869605, 1.000000000000000000, 0.9238795325112869605, 1.000000000000000000, 0.9238795325112869605, 1.000000000000000000, 0.9238795325112869605, 1.000000000000000000, 0.9238795325112869605, 1.000000000000000000, 0.9238795325112869605, 1.000000000000000000, 0.9238795325112869605, 1.000000000000000000, 0.9238795325112869605, 1.000000000000000000, 0.9238795325112869605, 1.000000000000000000, 0.9238795325112869605, 1.000000000000000000, 0.9238795325112869605, 1.000000000000000000, 0.9238795325112869605, 1.000000000000000000, 0.9238795325112869605, 1.000000000000000000, 0.9238795325112869605, 1.000000000000000000, 0.9238795325112869605, 1.000000000000000000, 0.9238795325112869605, 1.000000000000000000, 0.9238795325112869605, 1.000000000000000000, 0.9238795325112869605, 1.000000000000000000, 0.9238795325112869605, 1.000000000000000000, 0.9238795325112869605, 1.000000000000000000, 0.9238795325112869605, 1.000000000000000000, 0.9238795325112869605, 1.000000000000000000, 0.9238795325112869605, 1.000000000000000000, 0.9238795325112869605, 1.000000000000000000, 0.9238795325112869605, 1.000000000000000000, 0.9238795325112869605, 1.000000000000000000, 0.9238795325112869605, 1.000000000000000000, 0.9238795325112869605, 1.000000000000000000, 0.9238795325112869605, 1.000000000000000000, 0.9238795325112869605, 1.000000000000000000, 0.9238795325112869605, 1.000000000000000000, 0.9238795325112869605, 1.000000000000000000, 0.9238795325112869605, 1.000000000000000000, 0.9238795325112869605, 1.000000000000000000, 0.9238795325112869605, 1.000000000000000000, 0.9238795325112869605, 1.000000000000000000, 0.9238795325112869605, 1.000000000000000000, 0.9238795325112869605, 1.000000000000000000, 0.9238795325112869605, 1.000000000000000000, 0.9238795325112869605, 1.000000000000000000, 0.9238795325112869605, 1.000000000000000000, 0.9238795325112869605, 1.000000000000000000, 0.9238795325112869605, 1.000000000000000000, 0.9238795325112869605, 1.000000000000000000, 0.9238795325112869605, 1.000000000000000000, 0.9238795325112869605, 1.000000000000000000, 0.9238795325112869605, 1.000000000000000000, 0.9238795325112869605, 1.000000000000000000, 0.9238795325112869605, 1.000000000000000000, 0.9238795325112869605, 1.000000000000000000, 0.9238795325112869605, 1.000000000000000000, 0.9238795325112869605, 1.000000000000000000, 0.9238795325112869605, 1.000000000000000000, 0.9238795325112869605, 1.000000000000000000, 0.9238795325112869605, 1.000000000000000000, 0.9238795325112869605, 1.000000000000000000, 0.9238795325112869605, 1.000000000000000000, 0.9238795325112869605, 1.000000000000000000, 0.9238795325112869605, 1.000000000000000000, 0.9238795325112869605, 1.000000000000000000, 0.9238795325112869605, 1.000000000000000000, 0.9238795325112869605, 1.000000000000000000, 0.9238795325112869605, 1.000000000000000000, 0.9238795325112869605, 1.000000000000000000, 0.9238795325112869605, 1.000000000000000000, 0.9238795325112869605, 1.000000000000000000, 0.9238795325112869605, 1.000000000000000000, 0.9238795325112869605, 1.000000000000000000, 0.9238795325112869605, 1.000000000000000000, 0.9238795325112869605, 1.000000000000000000, 0.9238795325112869605, 1.000000000000000000, 0.9238795325112869605, 1.000000000000000000, 0.9238795325112869605, 1.000000000000000000, 0.9238795325112869605, 1.000000000000000000, 0.9238795325112869605, 1.000000000000000000, 0.9238795325112869605, 1.000000000000000000, 0.9238795325112869605, 1.000000000000000000, 0.9238795325112869605, 1.000000000000000000, 0.9238795325112869605, 1.000000000000000000, 0.9238795325112869605, 1.000000000000000000, 0.9238795325112869605, 1.000000000000000000, 0.9238795325112869605, 1.000000000000000000, 0.9238795325112869605, 1.000000000000000000, 0.9238795325112869605, 1.000000000000000000, 0.9238795325112869605, 1.000000000000000000, 0.9238795325112869605, 1.000000000000000000, 0.9238795325112869605, 1.000000000000000000, 0.9238795325112869605, 1.000000000000000000, 0.9238795325112869605, 1.000000000000000000, 0.9238795325112869605, 1.000000000000000000, 0.9238795325112869605, 1.000000000000000000, 0.9238795325112869605, 1.000000000000000000, 0.9238795325112869605, 1.000000000000000000, 0.9238795325112869605, 1.000000000000000000, 0.9238795325112869605, 1.000000000000000000, 0.9238795325112869605, 1.000000000000000000, 0.9238795325112869605, 1.000000000000000000, 0.9238795325112869605, 1.000000000000000000, 0.9238795325112869605, 1.000000000000000000, 0.9238795325112869605, 1.000000000000000000, 0.9238795325112869605, 1.000000000000000000, 0.9238795325112869605, 1.000000000000000000, 0.9238795325112869605, 1.000000000000000000, 0.9238795325112869605, 1.000000000000000000, 0.9238795325112869605, 1.000000000000000000, 0.9238795325112869605, 1.000000000000000000, 0.9238795325112869605, 1.000000000000000000, 0.9238795325112869605, 1.000000000000000000, 0.9238795325112869605, 1.000000000000000000, 0.9238795325112869605, 1.000000000000000000, 0.9238795325112869605, 1.000000000000000000, 0.9238795325112869605, 1.000000000000000000, 0.9238795325112869605, 1.000000000000000000, 0.9238795325112869605, 1.000000000000000000, 0.9238795325112869605, 1.000000000000000000, 0.9238795325112869605, 1.000000000000000000, 0.9238795325112869605, 1.000000000000000000, 0.9238795325112869605, 1.000000000000000000, 0.9238795325112869605, 1.000000000000000000, 0.9238795325112869605, 1.000000000000000000, 0.9238795325112869605, 1.000000000000000000, 0.9238795325112869605, 1.000000000000000000, 0.9238795325112869605, 1.000000000000000000, 0.9238795325112869605, 1.000000000000000000, 0.9238795325112869605, 1.000000000000000000, 0.9238795325112869605, 1.000000000000000000, 0.9238795325112869605, 1.000000000000000000, 0.9238795325112869605, 1.000000000000000000, 0.9238795325112869605, 1.000000000000000000, 0.9238795325112869605, 1.000000000000000000, 0.9238795325112869605, 1.000000000000000000, 0.9238795325112869605, 1.000000000000000000, 0.9238795325112869605, 1.000000000000000000, 0.9238795325112869605, 1.000000000000000000, 0.9238795325112869605, 1.000000000000000000, 0.9238795325112869605, 1.000000000000000000, 0.9238795325112869605, 1.000000000000000000, 0.9238795325112869605, 1.000000000000000000, 0.9238795325112869605, 1.000000000000000000, 0.9238795325112869605, 1.000000000000000000, 0.9238795325112869605, 1.000000000000000000, 0.9238795325112869605, 1.000000000000000000, 0.9238795325112869605, 1.000000000000000000, 0.9238795325112869605, 1.000000000000000000, 0.9238795325112869605, 1.000000000000000000, 0.9238795325112869605, 1.000000000000000000, 0.9238795325112869605, 1.000000000000000000, 0.9238795325112869605, 1.000000000000000000, 0.9238795325112869605, 1.000000000000000000, 0.9238795325112869605, 1.000000000000000000, 0.9238795325112869605, 1.000000000000000000, 0.9238795325112869605, 1.000000000000000000, 0.9238795325112869605, 1.000000000000000000, 0.9238795325112869605, 1.000000000000000000, 0.9238795325112869605, 1.000000000000000000, 0.9238795325112869605, 1.000000000000000000, 0.9238795325112869605, 1.000000000000000000, 0.9238795325112869605, 1.000000000000000000, 0.9238795325112869605, 1.000000000000000000, 0.9238795325112869605, 1.000000000000000000, 0.9238795325112869605, 1.000000000000000000, 0.9238795325112869605, 1.000000000000000000, 0.9238795325112869605, 1.000000000000000000, 0.9238795325112869605, 1.000000000000000000, 0.9238795325112869605, 1.000000000000000000, 0.9238795325112869605, 1.000000000000000000, 0.9238795325112869605, 1.000000000000000000, 0.9238795325112869605, 1.000000000000000000, 0.9238795325112869605, 1.000000000000000000, 0.9238795325112869605, 1.000000000000000000, 0.9238795325112869605, 1.000000000000000000, 0.9238795325112869605, 1.000000000000000000, 0.9238795325112869605, 1.000000000000000000, 0.9238795325112869605, 1.000000000000000000, 0.9238795325112869605, 1.000000000000000000, 0.9238795325112869605, 1.000000000000000000, 0.9238795325112869605, 1.000000000000000000, 0.9238795325112869605, 1.000000000000000000, 0.9238795325112869605, 1.000000000000000000, 0.9238795325112869605, 1.000000000000000000, 0.9238795325112869605, 1.000000000000000000, 0.9238795325112869605, 1.000000000000000000, 0.9238795325112869605, 1.000000000000000000, 0.9238795325112869605, 1.000000000000000000, 0.9238795325112869605, 1.000000000000000000, 0.9238795325112869605, 1.000000000000000000, 0.9238795325112869605, 1.000000000000000000, 0.9238795325112869605, 1.000000000000000000, 0.9238795325112869605, 1.000000000000000000, 0.9238795325112869605, 1.000000000000000000, 0.9238795325112869605, 1.000000000000000000, 0.9238795325112869605, 1.000000000000000000, 0.9238795325112869605, 1.000000000000000000, 0.9238795325112869605, 1.000000000000000000, 0.9238795325112869605, 1.000000000000000000, 0.9238795325112869605, 1.000000000000000000, 0.9238795325112869605, 1.000000000000000000, 0.9238795325112869605, 1.000000000000000000, 0.9238795325112869605, 1.000000000000000000, 0.9238795325112869605, 1.000000000000000000, 0.9238795325112869605, 1.000000000000000000, 0.9238795325112869605, 1.000000000000000000, 0.9238795325112869605, 1.000000000000000000, 0.9238795325112869605, 1.000000000000000000, 0.9238795325112869605, 1.000000000000000000, 0.9238795325112869605, 1.000000000000000000, 0.9238795325112869605, 1.000000000000000000, 0.9238795325112869605, 1.000000000000000000, 0.9238795325112869605, 1.000000000000000000, 0.9238795325112869605, 1.000000000000000000, 0.9238795325112869605, 1.000000000000000000, 0.9238795325112869605, 1.000000000000000000, 0.9238795325112869605, 1.000000000000000000, 0.9238795325112869605, 1.000000000000000000, 0.9238795325112869605, 1.000000000000000000, 0.9238795325112869605, 1.000000000000000000, 0.9238795325112869605, 1.000000000000000000, 0.9238795325112869605, 1.000000000000000000, 0.9238795325112869605, 1.000000000000000000, 0.9238795325112869605, 1.000000000000000000, 0.9238795325112869605, 1.000000000000000000, 0.9238795325112869605, 1.000000000000000000, 0.9238795325112869605, 1.000000000000000000, 0.9238795325112869605, 1.000000000000000000, 0.9238795325112869605, 1.000000000000000000, 0.9238795325112869605, 1.000000000000000000, 0.9238795325112869605, 1.000000000000000000, 0.9238795325112869605, 1.000000000000000000, 0.9238795325112869605, 1.000000000000000000, 0.9238795325112869605, 1.000000000000000000, 0.9238795325112869605, 1.000000000000000000, 0.9238795325112869605, 1.000000000000000000, 0.9238795325112869605, 1.000000000000000000, 0.9238795325112869605, 1.000000000000000000, 0.9238795325112869605, 1.000000000000000000, 0.9238795325112869605, 1.000000000000000000, 0.9238795325112869605, 1.000000000000000000, 0.9238795325112869605, 1.000000000000000000, 0.9238795325112869605, 1.000000000000000000, 0.9238795325112869605, 1.000000000000000000, 0.9238795325112869605, 1.000000000000000000, 0.9238795325112869605, 1.000000000000000000, 0.9238795325112869605, 1.000000000000000000, 0.9238795325112869605, 1.000000000000000000, 0.9238795325112869605, 1.000000000000000000, 0.9238795325112869605, 1.000000000000000000, 0.9238795325112869605, 1.000000000000000000, 0.9238795325112869605, 1.000000000000000000, 0.9238795325112869605, 1.000000000000000000, 0.9238795325112869605, 1.000000000000000000, 0.9238795325112869605, 1.000000000000000000, 0.9238795325112869605, 1.000000000000000000, 0.9238795325112869605, 1.000000000000000000, 0.9238795325112869605, 1.000000000000000000, 0.9238795325112869605, 1.000000000000000000, 0.9238795325112869605, 1.000000000000000000, 0.9238795325112869605, 1.000000000000000000, 0.9238795325112869605, 1.000000000000000000, 0.9238795325112869605, 1.000000000000000000, 0.9238795325112869605, 1.000000000000000000, 0.9238795325112869605, 1.000000000000000000, 0.9238795325112869605, 1.000000000000000000, 0.9238795325112869605, 1.000000000000000000, 0.9238795325112869605, 1.000000000000000000, 0.9238795325112869605, 1.000000000000000000, 0.9238795325112869605, 1.000000000000000000, 0.9238795325112869605, 1.000000000000000000, 0.9238795325112869605, 1.000000000000000000, 0.9238795325112869605, 1.000000000000000000, 0.9238795325112869605, 1.000000000000000000, 0.9238795325112869605, 1.000000000000000000, 0.9238795325112869605, 1.000000000000000000, 0.9238795325112869605, 1.000000000000000000, 0.9238795325112869605, 1.000000000000000000, 0.9238795325112869605, 1.000000000000000000, 0.9238795325112869605, 1.000000000000000000, 0.9238795325112869605, 1.000000000000000000, 0.9238795325112869605, 1.000000000000000000, 0.9238795325112869605, 1.000000000000000000, 0.9238795325112869605, 1.000000000000000000, 0.9238795325112869605, 1.000000000000000000, 0.9238795325112869605, 1.000000000000000000, 0.9238795325112869605, 1.000000000000000000, 0.9238795325112869605, 1.000000000000000000, 0.9238795325112869605, 1.000000000000000000, 0.9238795325112869605, 1.000000000000000000, 0.9238795325112869605, 1.000000000000000000, 0.9238795325112869605, 1.000000000000000000, 0.9238795325112869605, 1.000000000000000000, 0.9238795325112869605, 1.000000000000000000, 0.9238795325112869605, 1.000000000000000000, 0.9238795325112869605, 1.000000000000000000, 0.9238795325112869605, 1.000000000000000000, 0.9238795325112869605, 1.000000000000000000, 0.9238795325112869605, 1.000000000000000000, 0.9238795325112869605, 1.000000000000000000, 0.9238795325112869605, 1.000000000000000000, 0.9238795325112869605, 1.000000000000000000, 0.9238795325112869605, 1.000000000000000000, 0.9238795325112869605, 1.000000000000000000, 0.9238795325112869605, 1.000000000000000000, 0.9238795325112869605, 1.000000000000000000, 0.9238795325112869605, 1.000000000000000000, 0.9238795325112869605, 1.000000000000000000, 0.9238795325112869605, 1.000000000000000000, 0.9238795325112869605, 1.000000000000000000, 0.9238795325112869605, 1.000000000000000000, 0.9238795325112869605, 1.000000000000000000, 0.9238795325112869605, 1.000000000000000000, 0.9238795325112869605, 1.000000000000000000, 0.9238795325112869605, 1.000000000000000000, 0.9238795325112869605, 1.000000000000000000, 0.9238795325112869605, 1.000000000000000000, 0.9238795325112869605, 1.000000000000000000, 0.9238795325112869605, 1.000000000000000000, 0.9238795325112869605, 1.000000000000000000, 0.9238795325112869605, 1.000000000000000000, 0.9238795325112869605, 1.000000000000000000, 0.9238795325112869605, 1.000000000000000000, 0.9238795325112869605, 1.000000000000000000, 0.9238795325112869605, 1.000000000000000000, 0.9238795325112869605, 1.000000000000000000, 0.9238795325112869605, 1.000000000000000000, 0.9238795325112869605, 1.000000000000000000, 0.9238795325112869605, 1.000000000000000000, 0.9238795325112869605, 1.000000000000000000, 0.9238795325112869605, 1.000000000000000000, 0.9238795325112869605, 1.000000000000000000, 0.9238795325112869605, 1.000000000000000000, 0.9238795325112869605, 1.000000000000000000, 0.9238795325112869605, 1.000000000000000000, 0.9238795325112869605, 1.000000000000000000, 0.9238795325112869605, 1.000000000000000000, 0.9238795325112869605, 1.000000000000000000, 0.9238795325112869605, 1.000000000000000000, 0.9238795325112869605, 1.000000000000000000, 0.9238795325112869605, 1.000000000000000000, 0.9238795325112869605, 1.000000000000000000, 0.9238795325112869605, 1.000000000000000000, 0.9238795325112869605, 1.000000000000000000, 0.9238795325112869605, 1.000000000000000000, 0.9238795325112869605, 1.000000000000000000, 0.9238795325112869605, 1.000000000000000000, 0.9238795325112869605, 1.000000000000000000, 0.9238795325112869605, 1.000000000000000000, 0.9238795325112869605, 1.000000000000000000, 0.9238795325112869605, 1.000000000000000000, 0.9238795325112869605, 1.000000000000000000, 0.9238795325112869605, 1.000000000000000000, 0.9238795325112869605, 1.000000000000000000, 0.9238795325112869605, 1.000000000000000000, 0.9238795325112869605, 1.000000000000000000, 0.9238795325112869605, 1.000000000000000000, 0.9238795325112869605, 1.000000000000000000, 0.9238795325112869605, 1.000000000000000000, 0.9238795325112869605, 1.000000000000000000, 0.9238795325112869605, 1.000000000000000000, 0.9238795325112869605, 1.000000000000000000, 0.9238795325112869605, 1.000000000000000000, 0.9238795325112869605, 1.000000000000000000, 0.9238795325112869605, 1.000000000000000000, 0.9238795325112869605, 1.000000000000000000, 0.9238795325112869605, 1.000000000000000000, 0.9238795325112869605, 1.000000000000000000, 0.9238795325112869605, 1.000000000000000000, 0.9238795325112869605, 1.000000000000000000, 0.9238795325112869605, 1.000000000000000000, 0.9238795325112869605, 1.000000000000000000, 0.9238795325112869605, 1.000000000000000000, 0.9238795325112869605, 1.000000000000000000, 0.9238795325112869605, 1.000000000000000000, 0.9238795325112869605, 1.000000000000000000, 0.9238795325112869605, 1.000000000000000000, 0.9238795325112869605, 1.000000000000000000, 0.9238795325112869605, 1.000000000000000000, 0.9238795325112869605, 1.000000000000000000, 0.9238795325112869605, 1.000000000000000000, 0.9238795325112869605, 1.000000000000000000, 0.9238795325112869605, 1.000000000000000000, 0.9238795325112869605, 1.000000000000000000, 0.9238795325112869605, 1.000000000000000000, 0.9238795325112869605, 1.000000000000000000, 0.9238795325112869605, 1.000000000000000000, 0.9238795325112869605, 1.000000000000000000, 0.9238795325112869605, 1.000000000000000000, 0.9238795325112869605, 1.000000000000000000, 0.9238795325112869605, 1.000000000000000000, 0.9238795325112869605, 1.000000000000000000, 0.9238795325112869605, 1.000000000000000000 ) ) 
 REPRESENTATION_ITEM ( '' )  ) ;
#22354=ORIENTED_EDGE ( 'NONE', *, *, #34217, .T. ) ;
#22355=DIRECTION ( 'NONE',  ( 1.822029033848725028E-16, 0.000000000000000000, 1.000000000000000000 ) ) ;
#22357=CARTESIAN_POINT ( 'NONE',  ( 0.7185039370078739607, 1.928577636452523993E-17, 0.5019685039370078705 ) ) ;
#22359=CARTESIAN_POINT ( 'NONE',  ( 0.6971942568897637749, 2.189545951927499583E-17, 1.183562992072220599 ) ) ;
#22363=CARTESIAN_POINT ( 'NONE',  ( 0.8019270111902717657, -0.1787899950787401604, 1.505905511757261284 ) ) ;
#22364=CARTESIAN_POINT ( 'NONE',  ( 1.054774247047244540, 0.07405724077823318263, 0.1820866141194649179 ) ) ;
#22371=CARTESIAN_POINT ( 'NONE',  ( -1.054774247047244540, -0.07405724077823318263, 0.4576771653005669016 ) ) ;
#22372=CARTESIAN_POINT ( 'NONE',  ( 0.8759842519685039353, 0.1574803149606299191, 0.3740157480314960647 ) ) ;
#22374=CARTESIAN_POINT ( 'NONE',  ( -0.7123958336783836609, -0.03406646599270943959, 1.983899093309475781 ) ) ;
#22376=CARTESIAN_POINT ( 'NONE',  ( 0.6971942568897637749, 2.189545951927499583E-17, 1.345964566875370139 ) ) ;
#22377=CARTESIAN_POINT ( 'NONE',  ( 0.6971942568897648851, 0.07405724077823318263, 1.614173228292692386 ) ) ;
#22380=CARTESIAN_POINT ( 'NONE',  ( 1.033464566929133799, 0.000000000000000000, 0.8267716534357796299 ) ) ;
#22383=CARTESIAN_POINT ( 'NONE',  ( 0.9500414927467378812, -0.1787899950787401604, 0.2903543306548980185 ) ) ;
#22384=CARTESIAN_POINT ( 'NONE',  ( -0.9412147342319837628, -0.1574803149606297803, 1.724901574695621775 ) ) ;
#22387=CARTESIAN_POINT ( 'NONE',  ( -0.6971942568897648851, 0.07405724077823318263, 1.181102362150960428 ) ) ;
#22388=CARTESIAN_POINT ( 'NONE',  ( 0.8107537697050253289, -0.1574803149606297803, 0.5782480313885360879 ) ) ;
#22389=ORIENTED_EDGE ( 'NONE', *, *, #6070, .F. ) ;
#22392=ORIENTED_EDGE ( 'NONE', *, *, #30909, .F. ) ;
#22393=CARTESIAN_POINT ( 'NONE',  ( 0.7185039370078746268, 0.06523048226347956391, 0.2632874015748031260 ) ) ;
#22395=CARTESIAN_POINT ( 'NONE',  ( -0.7185039370078746268, 0.06523048226347956391, 1.601870078740158077 ) ) ;
#22396=CARTESIAN_POINT ( 'NONE',  ( 0.8759842519685039353, 0.1787899950787401882, 1.567421259788755794 ) ) ;
#22397=CARTESIAN_POINT ( 'NONE',  ( -0.8107537697050254399, 0.1574803149606300301, 1.833169291338582640 ) ) ;
#22398=CARTESIAN_POINT ( 'NONE',  ( 0.8759842519685039353, 0.1574803149606299191, 1.673228346456693050 ) ) ;
#22403=EDGE_CURVE ( 'NONE', #27881, #28992, #35509, .T. ) ;
#22404=EDGE_CURVE ( 'NONE', #43583, #12067, #1199, .T. ) ;
#22407=CARTESIAN_POINT ( 'NONE',  ( 0.8019270111902716547, -0.1787899950787401604, 0.8809055117572600624 ) ) ;
#22408=CARTESIAN_POINT ( 'NONE',  ( -0.6971942568897648851, -0.07405724077823297447, 1.461614173174583753 ) ) ;
#22410=CARTESIAN_POINT ( 'NONE',  ( -1.054774247047244096, 0.000000000000000000, 1.326279527505291433 ) ) ;
#22413=ORIENTED_EDGE ( 'NONE', *, *, #45284, .T. ) ;
#22415=CARTESIAN_POINT ( 'NONE',  ( -0.9500414927467378812, -0.1787899950787401604, 0.3346456692375748831 ) ) ;
#22421=CARTESIAN_POINT ( 'NONE',  ( 0.7670496988260933069, 0.1418927192561055817, 0.03937512220365226023 ) ) ;
#22422=ORIENTED_EDGE ( 'NONE', *, *, #8615, .T. ) ;
#22426=VERTEX_POINT ( 'NONE', #17326 ) ;
#22428=CARTESIAN_POINT ( 'NONE',  ( -0.6971942568897626646, -0.07405724077823297447, 0.08858267711159095725 ) ) ;
#22429=CARTESIAN_POINT ( 'NONE',  ( -1.033464566929133799, 0.000000000000000000, 0.9547244094488189781 ) ) ;
#22433=CARTESIAN_POINT ( 'NONE',  ( -1.033464566929134687, -0.06523048226347956391, 1.532972440837355066 ) ) ;
#22434=CARTESIAN_POINT ( 'NONE',  ( 0.8019270111902717657, 0.1787899950787401604, 0.9842519684501742638 ) ) ;
#22438=CARTESIAN_POINT ( 'NONE',  ( 0.9873396505805591694, 0.1113553986120547346, 1.432086614173228245 ) ) ;
#22439=CARTESIAN_POINT ( 'NONE',  ( 0.7125671091357160813, -0.03503208222838762737, 1.983917631934041026 ) ) ;
#22442=CARTESIAN_POINT ( 'NONE',  ( 0.8759842519685039353, -0.1787899950787401882, 0.7603346456155274380 ) ) ;
#22443=LINE ( 'NONE', #37783, #1677 ) ;
#22447=CARTESIAN_POINT ( 'NONE',  ( 0.7185039370078746268, 0.06523048226347956391, 1.090059055118109965 ) ) ;
#22448=CARTESIAN_POINT ( 'NONE',  ( 1.054774247047244540, 0.07405724077823318263, 1.087598425143086578 ) ) ;
#22453=CARTESIAN_POINT ( 'NONE',  ( 0.8759842519685039353, -0.1574803149606300579, 0.03937007874015747977 ) ) ;
#22454=CARTESIAN_POINT ( 'NONE',  ( -1.054774247047244096, 0.000000000000000000, 0.2189960629383626012 ) ) ;
#22456=CARTESIAN_POINT ( 'NONE',  ( -1.033464566929134687, -0.06523048226347956391, 0.7160433070866151217 ) ) ;
#22458=CARTESIAN_POINT ( 'NONE',  ( 0.7185039370078746268, -0.06523048226347956391, 0.3371062991050715607 ) ) ;
#22459=CARTESIAN_POINT ( 'NONE',  ( -0.6971942568897648851, -0.07405724077823297447, 1.619094488135213838 ) ) ;
#22460=CARTESIAN_POINT ( 'NONE',  ( -0.9500414927467377701, -0.1787899950787401604, 0.9202755904974182499 ) ) ;
#22463=CARTESIAN_POINT ( 'NONE',  ( -0.9500414927467378812, -0.1787899950787401604, 0.5708661416785201226 ) ) ;
#22464=( BOUNDED_CURVE ( )  B_SPLINE_CURVE ( 2, ( #27531, #42083, #26572, #27048, #11951, #41127, #8324, #34002, #1131 ),
 .UNSPECIFIED., .F., .T. ) 
 B_SPLINE_CURVE_WITH_KNOTS ( ( 3, 2, 2, 2, 3 ),
 ( 0.9699999999999999734, 0.9725000000000000311, 0.9749999999999999778, 0.9775000000000000355, 0.9799999999999999822 ),
 .UNSPECIFIED. ) 
 CURVE ( )  GEOMETRIC_REPRESENTATION_ITEM ( )  RATIONAL_B_SPLINE_CURVE ( ( 1.000000000000000000, 0.9238795325112869605, 1.000000000000000000, 0.9238795325112869605, 1.000000000000000000, 0.9238795325112869605, 1.000000000000000000, 0.9238795325112869605, 1.000000000000000000 ) ) 
 REPRESENTATION_ITEM ( '' )  ) ;
#22467=CARTESIAN_POINT ( 'NONE',  ( 1.033464566929133799, 0.000000000000000000, 0.9940944881889764995 ) ) ;
#22468=CYLINDRICAL_SURFACE ( 'NONE', #20317, 0.1574803149606299191 ) ;
#22469=CARTESIAN_POINT ( 'NONE',  ( 0.7495606340400177148, -0.1264236179284866091, 0.08612204719033110523 ) ) ;
#22477=CARTESIAN_POINT ( 'NONE',  ( -0.6971942568897637749, 2.189545951927499583E-17, 0.3174212597887562382 ) ) ;
#22480=CARTESIAN_POINT ( 'NONE',  ( -0.6971942568897637749, 2.189545951927499583E-17, 1.424704724355685181 ) ) ;
#22485=CARTESIAN_POINT ( 'NONE',  ( 0.7185039370078746268, -0.06523048226347956391, 0.3469488188976379561 ) ) ;
#22487=CARTESIAN_POINT ( 'NONE',  ( -0.9873396505805591694, -0.1113553986120547346, 1.097440944774362270 ) ) ;
#22488=CARTESIAN_POINT ( 'NONE',  ( 0.6971942568897626646, 0.07405724077823318263, 0.5167322834108034613 ) ) ;
#22489=CARTESIAN_POINT ( 'NONE',  ( 1.033464566929133799, 0.000000000000000000, 0.5511811022546778682 ) ) ;
#22495=CARTESIAN_POINT ( 'NONE',  ( -1.054774247047244096, 0.000000000000000000, 0.9325787401037164415 ) ) ;
#22496=CARTESIAN_POINT ( 'NONE',  ( 0.9873396505805591694, 0.1113553986120547346, 0.9990157480314961758 ) ) ;
#22499=LINE ( 'NONE', #4498, #14851 ) ;
#22500=CARTESIAN_POINT ( 'NONE',  ( 0.8759842519685039353, -0.1574803149606299191, 1.535433070866141669 ) ) ;
#22511=CARTESIAN_POINT ( 'NONE',  ( 0.9873396505805591694, -0.1113553986120547346, 1.097440944774362270 ) ) ;
#22516=ORIENTED_EDGE ( 'NONE', *, *, #43595, .T. ) ;
#22517=CARTESIAN_POINT ( 'NONE',  ( -0.7495606340400177148, 0.1264236179284866091, 1.813484251914740053 ) ) ;
#22518=CARTESIAN_POINT ( 'NONE',  ( 0.9500414927467378812, 0.1787899950787401604, 1.648622047190331230 ) ) ;
#22519=CARTESIAN_POINT ( 'NONE',  ( -0.8759842519685039353, 0.1787899950787401882, 0.8636811023084409733 ) ) ;
#22521=CARTESIAN_POINT ( 'NONE',  ( 0.9500414927467378812, -0.1787899950787401604, 0.2559055117572600624 ) ) ;
#22522=CARTESIAN_POINT ( 'NONE',  ( -1.033464566929134687, 0.06523048226347956391, 1.498523621939716444 ) ) ;
#22523=CARTESIAN_POINT ( 'NONE',  ( -0.8019270111902716547, -0.1787899950787401604, 1.309055118056473122 ) ) ;
#22524=CARTESIAN_POINT ( 'NONE',  ( -0.6971942568897637749, 2.189545951927499583E-17, 0.7898622046706456068 ) ) ;
#22525=CARTESIAN_POINT ( 'NONE',  ( -0.9500414927467378812, 0.1787899950787401604, 0.9350393700249758355 ) ) ;
#22527=CARTESIAN_POINT ( 'NONE',  ( -0.8019270111902717657, 0.1787899950787401604, 1.653543307032850462 ) ) ;
#22528=CARTESIAN_POINT ( 'NONE',  ( -0.8759842519685039353, -0.1574803149606299191, 1.879921259734992134 ) ) ;
#22530=CARTESIAN_POINT ( 'NONE',  ( -1.033464566929133799, 0.000000000000000000, 1.624015748031496287 ) ) ;
#22532=CARTESIAN_POINT ( 'NONE',  ( 0.6971942568897637749, 2.189545951927499583E-17, 1.582185039316315045 ) ) ;
#22534=CARTESIAN_POINT ( 'NONE',  ( 0.7646288533564489232, -0.1113553986120547346, 1.008858267609007875 ) ) ;
#22535=ORIENTED_EDGE ( 'NONE', *, *, #33520, .F. ) ;
#22547=CARTESIAN_POINT ( 'NONE',  ( 0.8759842519685039353, -0.1787899950787401882, 1.783956692859621995 ) ) ;
#22551=CARTESIAN_POINT ( 'NONE',  ( 0.6971942568897637749, 2.189545951927499583E-17, 0.8292322834108031282 ) ) ;
#22553=DIRECTION ( 'NONE',  ( 0.000000000000000000, 0.000000000000000000, -1.000000000000000000 ) ) ;
#22554=CARTESIAN_POINT ( 'NONE',  ( 0.7646288533564489232, 0.1113553986120547346, 1.126968503937007871 ) ) ;
#22555=FACE_OUTER_BOUND ( 'NONE', #31589, .T. ) ;
#22557=CARTESIAN_POINT ( 'NONE',  ( 0.8759842519685039353, -0.1574803149606299191, 1.259842519685039353 ) ) ;
#22558=CARTESIAN_POINT ( 'NONE',  ( 1.054774247047244540, -0.07405724077823318263, 1.835629921206078485 ) ) ;
#22560=EDGE_CURVE ( 'NONE', #41698, #41647, #32720, .T. ) ;
#22561=EDGE_CURVE ( 'NONE', #33076, #36696, #24177, .T. ) ;
#22562=CARTESIAN_POINT ( 'NONE',  ( 1.033464566929134687, 0.06523048226347956391, 0.1304133858267717272 ) ) ;
#22563=DIRECTION ( 'NONE',  ( 0.000000000000000000, 0.000000000000000000, -1.000000000000000000 ) ) ;
#22566=CARTESIAN_POINT ( 'NONE',  ( -0.8759842519685039353, -0.1787899950787401882, 0.4109251967966299213 ) ) ;
#22569=CARTESIAN_POINT ( 'NONE',  ( 0.7495606340400177148, 0.1264236179284866091, 0.2780511810485988278 ) ) ;
#22570=CARTESIAN_POINT ( 'NONE',  ( 0.8107537697050254399, 0.1574803149606300301, 1.114665354223180804 ) ) ;
#22571=CARTESIAN_POINT ( 'NONE',  ( -0.9500414927467378812, -0.1787899950787401604, 1.786417322780882388 ) ) ;
#22572=ORIENTED_EDGE ( 'NONE', *, *, #42184, .T. ) ;
#22573=CARTESIAN_POINT ( 'NONE',  ( 0.8019270111902717657, -0.1787899950787401604, 1.313976377898992132 ) ) ;
#22577=CARTESIAN_POINT ( 'NONE',  ( 1.054774247047244096, 0.000000000000000000, 0.02706692908009476414 ) ) ;
#22578=CARTESIAN_POINT ( 'NONE',  ( -0.8759842519685039353, 0.1787899950787401882, 1.016240157426551161 ) ) ;
#22581=CARTESIAN_POINT ( 'NONE',  ( 0.7495606340400177148, 0.1264236179284866091, 0.5142716534895434011 ) ) ;
#22582=CARTESIAN_POINT ( 'NONE',  ( -0.6971942568897626646, 0.07405724077823318263, 0.3149606298674962890 ) ) ;
#22583=CARTESIAN_POINT ( 'NONE',  ( -0.9500414927467378812, 0.1787899950787401604, 0.6988188975840318173 ) ) ;
#22584=CARTESIAN_POINT ( 'NONE',  ( 0.9873396505805591694, 0.1113553986120547346, 1.697834645561763889 ) ) ;
#22585=ORIENTED_EDGE ( 'NONE', *, *, #23019, .T. ) ;
#22586=VERTEX_POINT ( 'NONE', #21635 ) ;
#22587=CYLINDRICAL_SURFACE ( 'NONE', #47426, 0.1574803149606299191 ) ;
#22589=CARTESIAN_POINT ( 'NONE',  ( -1.033464566929133799, 0.000000000000000000, 0.1673228346456692994 ) ) ;
#22590=CARTESIAN_POINT ( 'NONE',  ( 0.6971942568897637749, 2.189545951927499583E-17, 1.031003936954110189 ) ) ;
#22592=ORIENTED_EDGE ( 'NONE', *, *, #3528, .T. ) ;
#22593=CARTESIAN_POINT ( 'NONE',  ( 0.8759842519685039353, -0.1787899950787401882, 1.862696850339937038 ) ) ;
#22594=CARTESIAN_POINT ( 'NONE',  ( -0.6971942568897626646, -0.07405724077823297447, 0.8759842519147408302 ) ) ;
#22596=CARTESIAN_POINT ( 'NONE',  ( -0.6971942568897626646, 0.07405724077823318263, 0.07874015742655145200 ) ) ;
#22598=ORIENTED_EDGE ( 'NONE', *, *, #44107, .F. ) ;
#22602=CARTESIAN_POINT ( 'NONE',  ( 0.8019270111902717657, -0.1787899950787401604, 1.230314960576156746 ) ) ;
#22603=CARTESIAN_POINT ( 'NONE',  ( 1.033464566929133799, 0.000000000000000000, 1.978346456692913646 ) ) ;
#22604=CARTESIAN_POINT ( 'NONE',  ( 0.7185039370078739607, 1.928577636452523993E-17, 0.7283464565853858819 ) ) ;
#22605=CARTESIAN_POINT ( 'NONE',  ( -0.9412147342319837628, 0.1574803149606300301, 1.434547244094487972 ) ) ;
#22606=CARTESIAN_POINT ( 'NONE',  ( 1.054774247047244540, -0.07405724077823318263, 1.515748031442299526 ) ) ;
#22607=AXIS2_PLACEMENT_3D ( 'NONE', #885, #44734, #11950 ) ;
#22612=CARTESIAN_POINT ( 'NONE',  ( 0.7646288533564489232, -0.1113553986120547346, 1.333661417322834719 ) ) ;
#22613=( BOUNDED_CURVE ( )  B_SPLINE_CURVE ( 2, ( #32791, #30157, #18383, #18148, #7587, #44696, #47386, #14559, #14803 ),
 .UNSPECIFIED., .F., .T. ) 
 B_SPLINE_CURVE_WITH_KNOTS ( ( 3, 2, 2, 2, 3 ),
 ( 0.8499999999999999778, 0.8525000000000000355, 0.8549999999999999822, 0.8575000000000000400, 0.8599999999999999867 ),
 .UNSPECIFIED. ) 
 CURVE ( )  GEOMETRIC_REPRESENTATION_ITEM ( )  RATIONAL_B_SPLINE_CURVE ( ( 1.000000000000000000, 0.9238795325112939549, 1.000000000000000000, 0.9238795325112869605, 1.000000000000000000, 0.9238795325112869605, 1.000000000000000000, 0.9238795325112869605, 1.000000000000000000 ) ) 
 REPRESENTATION_ITEM ( '' )  ) ;
#22614=EDGE_CURVE ( 'NONE', #14891, #5868, #19246, .T. ) ;
#22615=CARTESIAN_POINT ( 'NONE',  ( -0.6971942568897648851, 0.07405724077823318263, 0.6742125983714336579 ) ) ;
#22617=CARTESIAN_POINT ( 'NONE',  ( 0.7646288533564489232, 0.1113553986120547346, 0.3789370078740157410 ) ) ;
#22621=CARTESIAN_POINT ( 'NONE',  ( 0.8759842519685039353, -0.1787899950787401882, 1.316437007820252081 ) ) ;
#22622=CARTESIAN_POINT ( 'NONE',  ( 0.7495606340400177148, 0.1264236179284866091, 1.729822834591905556 ) ) ;
#22623=CARTESIAN_POINT ( 'NONE',  ( 0.8759842519685039353, 0.1787899950787401882, 0.2682086613635594752 ) ) ;
#22627=CARTESIAN_POINT ( 'NONE',  ( 0.9412147342319837628, -0.1574803149606297803, 0.8193897636719996713 ) ) ;
#22629=CARTESIAN_POINT ( 'NONE',  ( 0.9873396505805591694, -0.1113553986120547346, 0.5462598424121581919 ) ) ;
#22630=CARTESIAN_POINT ( 'NONE',  ( 1.054774247047244096, 0.000000000000000000, 0.3371062991588349989 ) ) ;
#22631=CARTESIAN_POINT ( 'NONE',  ( 0.9500414927467377701, 0.1787899950787401604, 1.289370078686393750 ) ) ;
#22632=CARTESIAN_POINT ( 'NONE',  ( -0.8759842519685039353, 0.1574803149606299191, 1.712598425196850238 ) ) ;
#22633=CARTESIAN_POINT ( 'NONE',  ( -1.033464566929134687, -0.06523048226347956391, 1.336122047136566904 ) ) ;
#22634=CARTESIAN_POINT ( 'NONE',  ( -0.7646288533564489232, 0.1113553986120547346, 0.9596456691838111119 ) ) ;
#22635=CARTESIAN_POINT ( 'NONE',  ( -0.8019270111902717657, -0.1787899950787401604, 1.348425196796630976 ) ) ;
#22636=CARTESIAN_POINT ( 'NONE',  ( 0.8759842519685039353, -0.1574803149606299191, 0.6988188975302678241 ) ) ;
#22638=CARTESIAN_POINT ( 'NONE',  ( 0.7185039370078739607, 1.928577636452523993E-17, 1.407480314960629864 ) ) ;
#22640=ORIENTED_EDGE ( 'NONE', *, *, #44884, .T. ) ;
#22646=CARTESIAN_POINT ( 'NONE',  ( 0.9500414927467378812, -0.1787899950787401604, 1.589566929080094448 ) ) ;
#22647=CARTESIAN_POINT ( 'NONE',  ( -1.033464566929134687, -0.06523048226347956391, 1.227854330708661124 ) ) ;
#22648=AXIS2_PLACEMENT_3D ( 'NONE', #14098, #17443, #7137 ) ;
#22653=( BOUNDED_CURVE ( )  B_SPLINE_CURVE ( 2, ( #42424, #38614, #20633, #12995, #46029, #23768, #5308, #27638, #19925 ),
 .UNSPECIFIED., .F., .F. ) 
 B_SPLINE_CURVE_WITH_KNOTS ( ( 3, 2, 2, 2, 3 ),
 ( 0.8199999999999999512, 0.8225000000000000089, 0.8249999999999999556, 0.8275000000000000133, 0.8299999999999999600 ),
 .UNSPECIFIED. ) 
 CURVE ( )  GEOMETRIC_REPRESENTATION_ITEM ( )  RATIONAL_B_SPLINE_CURVE ( ( 1.000000000000000000, 0.9238795325112899581, 1.000000000000000000, 0.9238795325112869605, 1.000000000000000000, 0.9238795325112869605, 1.000000000000000000, 0.9238795325112799661, 1.000000000000000000 ) ) 
 REPRESENTATION_ITEM ( '' )  ) ;
#22655=CARTESIAN_POINT ( 'NONE',  ( 1.054774247047244540, -0.07405724077823318263, 0.8120078739619844832 ) ) ;
#22657=CARTESIAN_POINT ( 'NONE',  ( -0.8019270111902717657, -0.1787899950787401604, 1.353346456639149986 ) ) ;
#22658=AXIS2_PLACEMENT_3D ( 'NONE', #2674, #2903, #16831 ) ;
#22659=EDGE_LOOP ( 'NONE', ( #2631, #7989, #36081, #19498 ) ) ;
#22661=CARTESIAN_POINT ( 'NONE',  ( -0.9500414927467378812, -0.1787899950787401604, 0.2952755904974176393 ) ) ;
#22667=CARTESIAN_POINT ( 'NONE',  ( 0.7185039370078739607, 1.928577636452523993E-17, 1.131889763779527547 ) ) ;
#22669=CARTESIAN_POINT ( 'NONE',  ( 1.033464566929131356, 0.06523048226348168721, 1.419783464459401845 ) ) ;
#22673=ADVANCED_FACE ( 'NONE', ( #33862 ), #11563, .T. ) ;
#22674=CARTESIAN_POINT ( 'NONE',  ( -0.6971942568897637749, 2.189545951927499583E-17, 0.1648622046706460786 ) ) ;
#22675=CARTESIAN_POINT ( 'NONE',  ( -0.8107537697050253289, -0.1574803149606297803, 0.8636811023622045225 ) ) ;
#22678=CARTESIAN_POINT ( 'NONE',  ( -0.8759842519685039353, 0.1574803149606299191, 1.505905511703495847 ) ) ;
#22679=CARTESIAN_POINT ( 'NONE',  ( 0.6971942568897626646, -0.07405724077823297447, 0.8759842519147408302 ) ) ;
#22680=CARTESIAN_POINT ( 'NONE',  ( 0.6971942568897648851, 0.07405724077823318263, 1.338582677111590069 ) ) ;
#22681=CARTESIAN_POINT ( 'NONE',  ( 0.8759842519685039353, 0.1574803149606299191, 1.476377952755905554 ) ) ;
#22682=CARTESIAN_POINT ( 'NONE',  ( 0.7140868796910422311, 0.03190629090790177841, 1.982670689315033652 ) ) ;
#22684=CARTESIAN_POINT ( 'NONE',  ( 0.9412147342319837628, 0.1574803149606300301, 0.3223425195775121432 ) ) ;
#22685=CARTESIAN_POINT ( 'NONE',  ( 1.002407869896990045, 0.1264236179284866091, 0.8538385826234016207 ) ) ;
#22686=CARTESIAN_POINT ( 'NONE',  ( -0.7185039370078746268, -0.06523048226347956391, 1.409940944881891367 ) ) ;
#22687=CARTESIAN_POINT ( 'NONE',  ( 0.9500414927467377701, 0.1787899950787401604, 1.766732283410803239 ) ) ;
#22689=ORIENTED_EDGE ( 'NONE', *, *, #10414, .F. ) ;
#22690=CARTESIAN_POINT ( 'NONE',  ( 0.9412147342319837628, -0.1574803149606297803, 0.4256889762704256230 ) ) ;
#22692=CARTESIAN_POINT ( 'NONE',  ( 1.002407869896990045, -0.1264236179284866091, 1.080216535379306952 ) ) ;
#22696=VERTEX_POINT ( 'NONE', #30043 ) ;
#22698=CARTESIAN_POINT ( 'NONE',  ( -0.8019270111902717657, 0.1787899950787401604, 0.2312992125446618197 ) ) ;
#22699=CARTESIAN_POINT ( 'NONE',  ( -1.033464566929133799, 0.000000000000000000, 0.6003937007874016185 ) ) ;
#22700=EDGE_LOOP ( 'NONE', ( #20240, #38225, #4759, #12717 ) ) ;
#22702=CARTESIAN_POINT ( 'NONE',  ( -0.8759842519685039353, 0.1787899950787401882, 1.882381889710015743 ) ) ;
#22703=CARTESIAN_POINT ( 'NONE',  ( -0.9500414927467377701, 0.1787899950787401604, 0.9350393700249758355 ) ) ;
#22704=CARTESIAN_POINT ( 'NONE',  ( -1.054774247047244540, 0.07405724077823318263, 1.126968503883244654 ) ) ;
#22705=CARTESIAN_POINT ( 'NONE',  ( -0.8019270111902717657, -0.1787899950787401604, 0.4478346456155276045 ) ) ;
#22706=CARTESIAN_POINT ( 'NONE',  ( -0.7646288533564489232, -0.1113553986120547346, 0.1525590551181102428 ) ) ;
#22709=CARTESIAN_POINT ( 'NONE',  ( 0.8019270111902717657, -0.1787899950787401604, 0.04921259837143338034 ) ) ;
#22713=FACE_OUTER_BOUND ( 'NONE', #32271, .T. ) ;
#22714=CARTESIAN_POINT ( 'NONE',  ( -1.033464566929133799, 0.000000000000000000, 1.968503936900346529 ) ) ;
#22715=CARTESIAN_POINT ( 'NONE',  ( -0.8759842519685039353, 0.1787899950787401882, 0.3075787401037169411 ) ) ;
#22716=DIRECTION ( 'NONE',  ( 1.822029033848725028E-16, 0.000000000000000000, 1.000000000000000000 ) ) ;
#22718=ORIENTED_EDGE ( 'NONE', *, *, #8665, .T. ) ;
#22720=CARTESIAN_POINT ( 'NONE',  ( -1.054774247047244540, -0.07405724077823318263, 1.560039370024976835 ) ) ;
#22721=VERTEX_POINT ( 'NONE', #44588 ) ;
#22726=CARTESIAN_POINT ( 'NONE',  ( 0.7185039370078739607, 0.000000000000000000, 4.498031496062992574 ) ) ;
#22727=FACE_OUTER_BOUND ( 'NONE', #35732, .T. ) ;
#22728=CARTESIAN_POINT ( 'NONE',  ( 0.8107537697050253289, 0.1574803149606300301, 0.4945866141732282451 ) ) ;
#22729=FACE_OUTER_BOUND ( 'NONE', #7274, .T. ) ;
#22730=CARTESIAN_POINT ( 'NONE',  ( -0.8107537697050253289, -0.1574803149606297803, 1.090059055010582423 ) ) ;
#22731=CARTESIAN_POINT ( 'NONE',  ( 0.6971942568897626646, 0.07405724077823318263, 0.5561023621509617598 ) ) ;
#22734=CARTESIAN_POINT ( 'NONE',  ( 0.9873396505805591694, -0.1113553986120547346, 1.963582677057826853 ) ) ;
#22735=ORIENTED_EDGE ( 'NONE', *, *, #43445, .F. ) ;
#22737=CARTESIAN_POINT ( 'NONE',  ( -1.054774247047244540, -0.07405724077823318263, 0.8907480314422985268 ) ) ;
#22738=CARTESIAN_POINT ( 'NONE',  ( 0.7185039370078746268, 0.06523048226347956391, 0.8932086614173218031 ) ) ;
#22741=CARTESIAN_POINT ( 'NONE',  ( 1.033464566929133799, 0.000000000000000000, 1.545275590551181244 ) ) ;
#22745=ORIENTED_EDGE ( 'NONE', *, *, #20363, .F. ) ;
#22747=CARTESIAN_POINT ( 'NONE',  ( 0.7185039370078714072, 0.06523048226347728795, 1.158956692805858779 ) ) ;
#22751=CARTESIAN_POINT ( 'NONE',  ( 0.8107537697050253289, -0.1574803149606297803, 1.090059055010582423 ) ) ;
#22752=( BOUNDED_CURVE ( )  B_SPLINE_CURVE ( 2, ( #42672, #16826, #17062, #31467, #31703, #23789, #12785, #35531, #30776 ),
 .UNSPECIFIED., .F., .T. ) 
 B_SPLINE_CURVE_WITH_KNOTS ( ( 3, 2, 2, 2, 3 ),
 ( 0.07000000000000000666, 0.07249999999999999500, 0.07499999999999999722, 0.07749999999999999944, 0.08000000000000000167 ),
 .UNSPECIFIED. ) 
 CURVE ( )  GEOMETRIC_REPRESENTATION_ITEM ( )  RATIONAL_B_SPLINE_CURVE ( ( 1.000000000000000000, 0.9238795325112869605, 1.000000000000000000, 0.9238795325112869605, 1.000000000000000000, 0.9238795325112869605, 1.000000000000000000, 0.9238795325112869605, 1.000000000000000000 ) ) 
 REPRESENTATION_ITEM ( '' )  ) ;
#22753=CARTESIAN_POINT ( 'NONE',  ( -0.9873396505805591694, -0.1113553986120547346, 1.658464566929134021 ) ) ;
#22754=CARTESIAN_POINT ( 'NONE',  ( -1.054774247047244540, -0.07405724077823318263, 0.4921259841982048577 ) ) ;
#22757=CARTESIAN_POINT ( 'NONE',  ( -0.6971942568897648851, 0.07405724077823318263, 1.737204724355685848 ) ) ;
#22758=CARTESIAN_POINT ( 'NONE',  ( 0.6971942568897637749, 2.189545951927499583E-17, 1.660925196796630088 ) ) ;
#22760=CARTESIAN_POINT ( 'NONE',  ( 0.9500414927467378812, 0.1787899950787401604, 0.2706692912848194243 ) ) ;
#22761=FACE_OUTER_BOUND ( 'NONE', #17169, .T. ) ;
#22762=CARTESIAN_POINT ( 'NONE',  ( -1.002407869896990045, -0.1264236179284866091, 1.277066929080094448 ) ) ;
#22763=VECTOR ( 'NONE', #37255, 39.37007874015748143 ) ;
#22764=CARTESIAN_POINT ( 'NONE',  ( -0.8019270111902717657, 0.1787899950787401604, 0.1181102361667090567 ) ) ;
#22766=CARTESIAN_POINT ( 'NONE',  ( -1.054774247047244096, 0.000000000000000000, 1.523129921206078707 ) ) ;
#22768=CARTESIAN_POINT ( 'NONE',  ( -0.8759842519685039353, -0.1574803149606299191, 1.535433070866141669 ) ) ;
#22769=CARTESIAN_POINT ( 'NONE',  ( 0.7185039370078739607, 1.928577636452523993E-17, 0.8858267715460158565 ) ) ;
#22770=CARTESIAN_POINT ( 'NONE',  ( 1.054774247047244540, -0.07405724077823318263, 1.560039370024976835 ) ) ;
#22772=DIRECTION ( 'NONE',  ( 0.000000000000000000, 0.000000000000000000, -1.000000000000000000 ) ) ;
#22774=ORIENTED_EDGE ( 'NONE', *, *, #38591, .F. ) ;
#22777=EDGE_LOOP ( 'NONE', ( #25350, #21113, #9747, #34688 ) ) ;
#22778=EDGE_CURVE ( 'NONE', #1638, #23930, #8195, .T. ) ;
#22779=CARTESIAN_POINT ( 'NONE',  ( -0.9500414927467377701, -0.1787899950787401604, 1.161417322780881278 ) ) ;
#22784=LINE ( 'NONE', #10845, #10252 ) ;
#22786=CARTESIAN_POINT ( 'NONE',  ( 0.6971942568897648851, -0.07405724077823297447, 1.815944881835999558 ) ) ;
#22791=CARTESIAN_POINT ( 'NONE',  ( 0.8019270111902717657, -0.1787899950787401604, 0.7185039369541108556 ) ) ;
#22793=CARTESIAN_POINT ( 'NONE',  ( -0.8759842519685039353, -0.1574803149606299191, 1.564960629813732185 ) ) ;
#22796=CARTESIAN_POINT ( 'NONE',  ( 0.7185039370078746268, 0.06523048226347956391, 0.4601377952755902889 ) ) ;
#22797=CARTESIAN_POINT ( 'NONE',  ( 0.9500414927467378812, 0.1787899950787401604, 1.766732283410803461 ) ) ;
#22798=DIRECTION ( 'NONE',  ( 1.822029033848725028E-16, 0.000000000000000000, 1.000000000000000000 ) ) ;
#22800=CARTESIAN_POINT ( 'NONE',  ( 1.033464566929134687, 0.06523048226347956391, 0.4749015746956221085 ) ) ;
#22802=CARTESIAN_POINT ( 'NONE',  ( 0.8019270111902717657, 0.1787899950787401604, 0.2362204723871814960 ) ) ;
#22803=CARTESIAN_POINT ( 'NONE',  ( 0.9873396505805591694, 0.1113553986120547346, 0.05413385826771653642 ) ) ;
#22804=CARTESIAN_POINT ( 'NONE',  ( -0.8019270111902717657, -0.1787899950787401604, 1.820866141678520789 ) ) ;
#22806=CARTESIAN_POINT ( 'NONE',  ( -0.6971942568897648851, 0.07405724077823318263, 1.264763779473795813 ) ) ;
#22808=CARTESIAN_POINT ( 'NONE',  ( 0.9500414927467378812, 0.1787899950787401604, 0.03444881884387430981 ) ) ;
#22809=CARTESIAN_POINT ( 'NONE',  ( -0.7495606340400177148, 0.1264236179284866091, 1.060531496009228247 ) ) ;
#22813=CARTESIAN_POINT ( 'NONE',  ( 0.6971942568897648851, -0.07405724077823297447, 0.4429133857730084833 ) ) ;
#22814=CARTESIAN_POINT ( 'NONE',  ( -0.8759842519685039353, 0.1787899950787401882, 0.4650590550643464716 ) ) ;
#22815=CARTESIAN_POINT ( 'NONE',  ( 0.8759842519685039353, 0.1574803149606299191, 1.702755905404283565 ) ) ;
#22819=ORIENTED_EDGE ( 'NONE', *, *, #7149, .F. ) ;
#22820=CARTESIAN_POINT ( 'NONE',  ( 0.7495606340400177148, -0.1264236179284866091, 0.9178149605761574126 ) ) ;
#22821=CARTESIAN_POINT ( 'NONE',  ( -1.033464566929133799, 0.000000000000000000, 0.08858267716535432601 ) ) ;
#22822=CARTESIAN_POINT ( 'NONE',  ( 0.7495606340400177148, -0.1264236179284866091, 1.193405511757259951 ) ) ;
#22824=ORIENTED_EDGE ( 'NONE', *, *, #39682, .T. ) ;
#22827=CARTESIAN_POINT ( 'NONE',  ( -1.054774247047244096, 0.000000000000000000, 0.8932086613635591421 ) ) ;
#22830=CARTESIAN_POINT ( 'NONE',  ( 1.033464566929133799, 0.000000000000000000, 0.7972440944881890035 ) ) ;
#22838=CARTESIAN_POINT ( 'NONE',  ( 1.054774247047244540, 0.07405724077823318263, 1.284448818843874740 ) ) ;
#22839=ADVANCED_FACE ( 'NONE', ( #45060 ), #1935, .T. ) ;
#22844=CARTESIAN_POINT ( 'NONE',  ( 0.7495606340400177148, -0.1264236179284866091, 0.1648622046706460786 ) ) ;
#22849=CARTESIAN_POINT ( 'NONE',  ( -0.8759842519685039353, 0.1787899950787401882, 0.5880905511273386566 ) ) ;
#22853=CARTESIAN_POINT ( 'NONE',  ( 0.8759842519685039353, 0.000000000000000000, 4.498031496062992574 ) ) ;
#22854=LINE ( 'NONE', #19725, #37589 ) ;
#22855=CARTESIAN_POINT ( 'NONE',  ( 1.054774247047244540, 0.07405724077823318263, 1.407480314906865981 ) ) ;
#22856=CARTESIAN_POINT ( 'NONE',  ( 0.8759842519685039353, -0.1787899950787401882, 1.862696850339937038 ) ) ;
#22857=CARTESIAN_POINT ( 'NONE',  ( 0.6971942568897626646, 0.07405724077823318263, 0.2755905511273391006 ) ) ;
#22862=CARTESIAN_POINT ( 'NONE',  ( 1.033464566929133799, 1.928577636452524610E-17, 2.007874015640504162 ) ) ;
#22863=CARTESIAN_POINT ( 'NONE',  ( -0.8759842519685039353, -0.1574803149606299191, 1.023622047244094446 ) ) ;
#22866=CARTESIAN_POINT ( 'NONE',  ( 0.6971942568897626646, 0.07405724077823318263, 0.3543307086076538659 ) ) ;
#22867=CARTESIAN_POINT ( 'NONE',  ( 0.7328829063313654357, -0.08888254389784847054, 0.03937018366421114746 ) ) ;
#22868=CARTESIAN_POINT ( 'NONE',  ( 1.033464566929133799, 0.000000000000000000, 0.8661417321759370402 ) ) ;
#22869=CARTESIAN_POINT ( 'NONE',  ( 1.033464566929133799, 0.000000000000000000, 0.03937007863263043694 ) ) ;
#22870=CARTESIAN_POINT ( 'NONE',  ( -0.7185039370078739607, 1.928577636452523993E-17, 1.289370078740157632 ) ) ;
#22871=CARTESIAN_POINT ( 'NONE',  ( -1.054774247047244540, -0.07405724077823318263, 1.279527559001355286 ) ) ;
#22872=CARTESIAN_POINT ( 'NONE',  ( 0.9873396505805591694, 0.1113553986120547346, 0.5954724408373543998 ) ) ;
#22874=CARTESIAN_POINT ( 'NONE',  ( 0.8107537697050254399, 0.1574803149606300301, 1.400098425196850904 ) ) ;
#22875=CARTESIAN_POINT ( 'NONE',  ( 0.7185039370078739607, 1.928577636452523993E-17, 0.6988188976377952555 ) ) ;
#22880=CARTESIAN_POINT ( 'NONE',  ( -0.9873396505805591694, 0.1113553986120547346, 1.195866141732283561 ) ) ;
#22883=CARTESIAN_POINT ( 'NONE',  ( -0.8759842519685039353, 0.1574803149606299191, 0.7578740156405039397 ) ) ;
#22884=CARTESIAN_POINT ( 'NONE',  ( 0.7185039370078739607, 1.928577636452523993E-17, 1.318897637687747926 ) ) ;
#22885=EDGE_LOOP ( 'NONE', ( #16962, #19816, #2114, #42175 ) ) ;
#22887=CARTESIAN_POINT ( 'NONE',  ( 0.6971942568897626646, 0.07405724077823318263, 0.6742125983714335469 ) ) ;
#22888=CARTESIAN_POINT ( 'NONE',  ( 1.054774247047244540, 0.07405724077823318263, 0.9744094487651340231 ) ) ;
#22889=CARTESIAN_POINT ( 'NONE',  ( -0.8759842519685039353, -0.1787899950787401882, 1.508366141678519678 ) ) ;
#22891=CARTESIAN_POINT ( 'NONE',  ( -0.9500414927467378812, 0.1787899950787401604, 1.215551181048599272 ) ) ;
#22894=VECTOR ( 'NONE', #40517, 39.37007874015748143 ) ;
#22895=CARTESIAN_POINT ( 'NONE',  ( -0.7495606340400177148, 0.1264236179284866091, 0.3567913385289137596 ) ) ;
#22900=VERTEX_POINT ( 'NONE', #24002 ) ;
#22901=ADVANCED_FACE ( 'NONE', ( #41696 ), #5775, .T. ) ;
#22905=( BOUNDED_CURVE ( )  B_SPLINE_CURVE ( 2, ( #30106, #12095, #37006, #44640, #7529, #22146, #22629, #14984, #29637 ),
 .UNSPECIFIED., .F., .T. ) 
 B_SPLINE_CURVE_WITH_KNOTS ( ( 3, 2, 2, 2, 3 ),
 ( 0.2500000000000000000, 0.2525000000000000022, 0.2550000000000000044, 0.2575000000000000067, 0.2600000000000000089 ),
 .UNSPECIFIED. ) 
 CURVE ( )  GEOMETRIC_REPRESENTATION_ITEM ( )  RATIONAL_B_SPLINE_CURVE ( ( 1.000000000000000000, 0.9238795325112859613, 1.000000000000000000, 0.9238795325112869605, 1.000000000000000000, 0.9238795325112869605, 1.000000000000000000, 0.9238795325112869605, 1.000000000000000000 ) ) 
 REPRESENTATION_ITEM ( '' )  ) ;
#22908=CARTESIAN_POINT ( 'NONE',  ( -1.002407869896990045, -0.1264236179284866091, 0.2583661416785200671 ) ) ;
#22909=CARTESIAN_POINT ( 'NONE',  ( -0.8107537697050253289, 0.1574803149606300301, 0.8095472440944886383 ) ) ;
#22912=CARTESIAN_POINT ( 'NONE',  ( -0.7185039370078739607, 1.928577636452523993E-17, 1.555118110128692832 ) ) ;
#22913=CARTESIAN_POINT ( 'NONE',  ( 0.6971942568897637749, 2.189545951927499583E-17, 0.9522637794737952577 ) ) ;
#22914=CARTESIAN_POINT ( 'NONE',  ( 1.054774247047244540, -0.07405724077823318263, 1.358267716481669662 ) ) ;
#22916=CARTESIAN_POINT ( 'NONE',  ( 1.033464566929134687, -0.06523048226347956391, 1.424704724409449064 ) ) ;
#22917=CARTESIAN_POINT ( 'NONE',  ( 0.7395153858165040006, 0.08906846876865334717, 1.981445972419700885 ) ) ;
#22919=( BOUNDED_CURVE ( )  B_SPLINE_CURVE ( 2, ( #12782, #12313, #41482, #34352, #1484, #16141, #15596, #44782, #29764 ),
 .UNSPECIFIED., .F., .T. ) 
 B_SPLINE_CURVE_WITH_KNOTS ( ( 3, 2, 2, 2, 3 ),
 ( 0.7199999999999999734, 0.7225000000000000311, 0.7249999999999999778, 0.7275000000000000355, 0.7299999999999999822 ),
 .UNSPECIFIED. ) 
 CURVE ( )  GEOMETRIC_REPRESENTATION_ITEM ( )  RATIONAL_B_SPLINE_CURVE ( ( 1.000000000000000000, 0.9238795325112869605, 1.000000000000000000, 0.9238795325112869605, 1.000000000000000000, 0.9238795325112869605, 1.000000000000000000, 0.9238795325112799661, 1.000000000000000000 ) ) 
 REPRESENTATION_ITEM ( '' )  ) ;
#22921=CARTESIAN_POINT ( 'NONE',  ( 1.002407869896990045, -0.1264236179284866091, 0.8833661416785196785 ) ) ;
#22922=CARTESIAN_POINT ( 'NONE',  ( 1.002407869896990045, -0.1264236179284866091, 1.793799212544661348 ) ) ;
#22925=( BOUNDED_CURVE ( )  B_SPLINE_CURVE ( 2, ( #46097, #31749, #17579, #46806, #42491, #13519, #35798, #32221, #31978 ),
 .UNSPECIFIED., .F., .T. ) 
 B_SPLINE_CURVE_WITH_KNOTS ( ( 3, 2, 2, 2, 3 ),
 ( 0.8800000000000000044, 0.8824999999999999512, 0.8850000000000000089, 0.8874999999999999556, 0.8900000000000000133 ),
 .UNSPECIFIED. ) 
 CURVE ( )  GEOMETRIC_REPRESENTATION_ITEM ( )  RATIONAL_B_SPLINE_CURVE ( ( 1.000000000000000000, 0.9238795325112869605, 1.000000000000000000, 0.9238795325112869605, 1.000000000000000000, 0.9238795325112869605, 1.000000000000000000, 0.9238795325112829637, 1.000000000000000000 ) ) 
 REPRESENTATION_ITEM ( '' )  ) ;
#22927=CARTESIAN_POINT ( 'NONE',  ( 1.033464566929133799, 0.000000000000000000, 0.4330708660342047489 ) ) ;
#22930=CARTESIAN_POINT ( 'NONE',  ( -1.033464566929133799, 0.000000000000000000, 0.1181102361129454797 ) ) ;
#22931=CARTESIAN_POINT ( 'NONE',  ( 0.8019270111902717657, 0.1787899950787401604, 1.215551181048599272 ) ) ;
#22938=CARTESIAN_POINT ( 'NONE',  ( -1.002407869896990045, 0.1264236179284866091, 0.2239173227808822775 ) ) ;
#22944=CARTESIAN_POINT ( 'NONE',  ( -0.8019270111902717657, 0.1787899950787401604, 1.766732283410803461 ) ) ;
#22945=CARTESIAN_POINT ( 'NONE',  ( -1.002407869896990045, -0.1264236179284866091, 0.9621062991588346103 ) ) ;
#22946=CARTESIAN_POINT ( 'NONE',  ( -0.7495606340400177148, -0.1264236179284866091, 0.5634842519147401640 ) ) ;
#22955=LINE ( 'NONE', #19349, #38652 ) ;
#22958=CARTESIAN_POINT ( 'NONE',  ( -0.9500414927467378812, 0.1787899950787401604, 0.4625984251430869665 ) ) ;
#22960=AXIS2_PLACEMENT_3D ( 'NONE', #13120, #9510, #20517 ) ;
#22962=CARTESIAN_POINT ( 'NONE',  ( -0.7495606340400177148, 0.1264236179284866091, 1.537893700733637736 ) ) ;
#22963=ORIENTED_EDGE ( 'NONE', *, *, #24304, .T. ) ;
#22966=CARTESIAN_POINT ( 'NONE',  ( 1.033464566929134687, -0.06523048226347956391, 0.2042322834645668717 ) ) ;
#22969=CARTESIAN_POINT ( 'NONE',  ( -1.033464566929134687, -0.06523048226347956391, 1.021161417215306955 ) ) ;
#22970=CARTESIAN_POINT ( 'NONE',  ( 0.9500414927467378812, 0.1787899950787401604, 0.5068897637257642197 ) ) ;
#22971=CARTESIAN_POINT ( 'NONE',  ( 0.6971942568897637749, 2.189545951927499583E-17, 0.04183070860765386589 ) ) ;
#22974=CARTESIAN_POINT ( 'NONE',  ( 0.9412147342319837628, -0.1574803149606297803, 1.921751968396409493 ) ) ;
#22976=CARTESIAN_POINT ( 'NONE',  ( 0.8759842519685039353, 0.000000000000000000, 4.498031496062992574 ) ) ;
#22977=CARTESIAN_POINT ( 'NONE',  ( 0.8759842519685039353, -0.1574803149606299191, 0.9055118110236221041 ) ) ;
#22986=CARTESIAN_POINT ( 'NONE',  ( 0.8759842519685039353, -0.1787899950787401882, 0.7209645668753701386 ) ) ;
#22993=CARTESIAN_POINT ( 'NONE',  ( 0.7185039370078746268, -0.06523048226347956391, 1.163877952648379344 ) ) ;
#22994=CARTESIAN_POINT ( 'NONE',  ( -0.7646288533564489232, -0.1113553986120547346, 1.648622047244094668 ) ) ;
#22997=ORIENTED_EDGE ( 'NONE', *, *, #22016, .T. ) ;
#22999=CARTESIAN_POINT ( 'NONE',  ( 1.054774247047244540, -0.07405724077823318263, 1.756889763725764553 ) ) ;
#23000=CARTESIAN_POINT ( 'NONE',  ( -0.9500414927467378812, 0.1787899950787401604, 0.9005905511273389896 ) ) ;
#23002=CARTESIAN_POINT ( 'NONE',  ( 0.8019270111902717657, -0.1787899950787401604, 0.4478346456155276045 ) ) ;
#23003=CARTESIAN_POINT ( 'NONE',  ( -0.6971942568897648851, 0.07405724077823318263, 1.338582677111590069 ) ) ;
#23004=CARTESIAN_POINT ( 'NONE',  ( -0.9873396505805591694, 0.1113553986120547346, 1.500984251860976171 ) ) ;
#23005=CARTESIAN_POINT ( 'NONE',  ( -0.8019270111902716547, 0.1787899950787401604, 1.254921259788757348 ) ) ;
#23006=CARTESIAN_POINT ( 'NONE',  ( -0.9500414927467378812, -0.1787899950787401604, 0.9202755904974182499 ) ) ;
#23007=CARTESIAN_POINT ( 'NONE',  ( -1.002407869896990045, 0.1264236179284866091, 0.1500984251430867999 ) ) ;
#23010=CARTESIAN_POINT ( 'NONE',  ( -1.054774247047244096, 0.000000000000000000, 1.798720472387181024 ) ) ;
#23011=CARTESIAN_POINT ( 'NONE',  ( -0.6971942568897626646, 0.07405724077823318263, 0.1230314960092287191 ) ) ;
#23012=CARTESIAN_POINT ( 'NONE',  ( -1.033464566929134687, -0.06523048226347956391, 1.542814960629920851 ) ) ;
#23014=CARTESIAN_POINT ( 'NONE',  ( 0.6971942568897648851, 0.07405724077823318263, 1.619094488135213838 ) ) ;
#23017=CARTESIAN_POINT ( 'NONE',  ( 0.9412147342319837628, 0.1574803149606300301, 0.2829724408373550104 ) ) ;
#23019=EDGE_CURVE ( 'NONE', #4424, #18622, #46307, .T. ) ;
#23022=ORIENTED_EDGE ( 'NONE', *, *, #12457, .F. ) ;
#23031=CARTESIAN_POINT ( 'NONE',  ( 0.8019270111902717657, -0.1787899950787401604, 0.7972440944344250102 ) ) ;
#23033=( BOUNDED_CURVE ( )  B_SPLINE_CURVE ( 2, ( #42115, #23949, #38555, #23703, #20336, #16748, #5945, #17217, #39239 ),
 .UNSPECIFIED., .F., .T. ) 
 B_SPLINE_CURVE_WITH_KNOTS ( ( 3, 2, 2, 2, 3 ),
 ( 0.7299999999999999822, 0.7325000000000000400, 0.7349999999999999867, 0.7375000000000000444, 0.7399999999999999911 ),
 .UNSPECIFIED. ) 
 CURVE ( )  GEOMETRIC_REPRESENTATION_ITEM ( )  RATIONAL_B_SPLINE_CURVE ( ( 1.000000000000000000, 0.9238795325112869605, 1.000000000000000000, 0.9238795325112869605, 1.000000000000000000, 0.9238795325112869605, 1.000000000000000000, 0.9238795325112869605, 1.000000000000000000 ) ) 
 REPRESENTATION_ITEM ( '' )  ) ;
#23034=CARTESIAN_POINT ( 'NONE',  ( 1.033464566929133799, 0.000000000000000000, 1.141732283357039357 ) ) ;
#23036=CARTESIAN_POINT ( 'NONE',  ( -0.9412147342319837628, -0.1574803149606297803, 0.07135826760900840227 ) ) ;
#23037=CARTESIAN_POINT ( 'NONE',  ( 0.8759842519685039353, 0.1787899950787401882, 1.808562992072220377 ) ) ;
#23038=CARTESIAN_POINT ( 'NONE',  ( 1.033464566929133799, 0.000000000000000000, 0.04921259842519685318 ) ) ;
#23039=LINE ( 'NONE', #5289, #43568 ) ;
#23041=CARTESIAN_POINT ( 'NONE',  ( 0.7185039370078732945, -0.06523048226347920309, 0.1107283464566930498 ) ) ;
#23043=CARTESIAN_POINT ( 'NONE',  ( 0.6971942568897637749, 2.189545951927499583E-17, 0.1648622046706460786 ) ) ;
#23044=CARTESIAN_POINT ( 'NONE',  ( -1.054774247047244540, 0.07405724077823318263, 1.796259842465923073 ) ) ;
#23046=CARTESIAN_POINT ( 'NONE',  ( -1.054774247047244540, 0.07405724077823318263, 1.289370078686393750 ) ) ;
#23048=EDGE_CURVE ( 'NONE', #43073, #37122, #9900, .T. ) ;
#23050=CARTESIAN_POINT ( 'NONE',  ( 0.8019270111902717657, 0.1787899950787401604, 0.03937007868639399305 ) ) ;
#23051=CARTESIAN_POINT ( 'NONE',  ( -1.054774247047244540, 0.07405724077823318263, 1.166338582623402509 ) ) ;
#23052=DIRECTION ( 'NONE',  ( 1.822029033848725028E-16, 0.000000000000000000, 1.000000000000000000 ) ) ;
#23054=CARTESIAN_POINT ( 'NONE',  ( 0.7646288533564489232, 0.1113553986120547346, 0.05413385816018952829 ) ) ;
#23055=CARTESIAN_POINT ( 'NONE',  ( 1.002407869896990045, -0.1264236179284866091, 0.5339566928596221063 ) ) ;
#23056=CARTESIAN_POINT ( 'NONE',  ( -0.6971942568897648851, -0.07405724077823297447, 0.4379921259304883074 ) ) ;
#23057=CARTESIAN_POINT ( 'NONE',  ( -0.9500414927467378812, 0.1787899950787401604, 0.8169291338045038264 ) ) ;
#23062=CARTESIAN_POINT ( 'NONE',  ( 1.054774247047244096, 0.000000000000000000, 0.8932086613635591421 ) ) ;
#23063=CARTESIAN_POINT ( 'NONE',  ( -0.8107537697050234415, -0.1574803149606297803, 0.1550196850393702197 ) ) ;
#23064=CARTESIAN_POINT ( 'NONE',  ( 0.7495606340400177148, 0.1264236179284866091, 1.222933070812378009 ) ) ;
#23065=CARTESIAN_POINT ( 'NONE',  ( -1.054774247047244540, -0.07405724077823318263, 1.988188976324191781 ) ) ;
#23069=VECTOR ( 'NONE', #31103, 39.37007874015748143 ) ;
#23074=CARTESIAN_POINT ( 'NONE',  ( -0.9500414927467378812, 0.1787899950787401604, 0.02952755900135462311 ) ) ;
#23080=CARTESIAN_POINT ( 'NONE',  ( 0.7185039370078739607, 1.928577636452523993E-17, 1.604330708661417360 ) ) ;
#23082=CARTESIAN_POINT ( 'NONE',  ( 0.8019270111902717657, -0.1787899950787401604, 0.1279527558517483676 ) ) ;
#23086=CYLINDRICAL_SURFACE ( 'NONE', #5033, 0.1574803149606299191 ) ;
#23088=CARTESIAN_POINT ( 'NONE',  ( -0.9500414927467377701, 0.1787899950787401604, 0.6643700786863929730 ) ) ;
#23091=CARTESIAN_POINT ( 'NONE',  ( -0.7185039370078739607, 1.928577636452523993E-17, 1.594488188868850242 ) ) ;
#23094=CARTESIAN_POINT ( 'NONE',  ( 0.6971942568897637749, 2.189545951927499583E-17, 1.385334645615527549 ) ) ;
#23095=CARTESIAN_POINT ( 'NONE',  ( 0.8759842519685039353, 0.1787899950787401882, 1.921751968450173376 ) ) ;
#23096=CARTESIAN_POINT ( 'NONE',  ( 0.6971942568897626646, -0.07405724077823297447, 0.2805118109698587214 ) ) ;
#23100=CARTESIAN_POINT ( 'NONE',  ( -0.7185039370078739607, 1.928577636452523993E-17, 0.1377952754830242266 ) ) ;
#23102=EDGE_LOOP ( 'NONE', ( #2453, #18976, #28802, #24320 ) ) ;
#23108=CARTESIAN_POINT ( 'NONE',  ( 0.8019270111902717657, 0.1787899950787401604, 0.3494094487651343006 ) ) ;
#23109=EDGE_CURVE ( 'NONE', #25373, #38468, #19541, .T. ) ;
#23110=CARTESIAN_POINT ( 'NONE',  ( -0.7185039370078746268, -0.06523048226347956391, 0.7406496062992133922 ) ) ;
#23111=CARTESIAN_POINT ( 'NONE',  ( -0.9412147342319837628, -0.1574803149606297803, 1.331200787294047672 ) ) ;
#23112=CARTESIAN_POINT ( 'NONE',  ( 0.9873396505805591694, 0.1113553986120547346, 0.8415354330708662012 ) ) ;
#23113=CARTESIAN_POINT ( 'NONE',  ( -0.8759842519685039353, 0.1574803149606299191, 0.7677165354330708347 ) ) ;
#23114=CARTESIAN_POINT ( 'NONE',  ( 0.9412147342319837628, -0.1574803149606297803, 0.8587598424121576368 ) ) ;
#23122=CARTESIAN_POINT ( 'NONE',  ( 0.6971942568897648851, -0.07405724077823297447, 1.619094488135213838 ) ) ;
#23123=CARTESIAN_POINT ( 'NONE',  ( -0.8759842519685039353, -0.1574803149606299191, 1.259842519685039353 ) ) ;
#23125=CARTESIAN_POINT ( 'NONE',  ( -1.033464566929134687, 0.06523048226347956391, 0.7504921258767240921 ) ) ;
#23126=CARTESIAN_POINT ( 'NONE',  ( 0.7495606340400177148, -0.1264236179284866091, 0.05167322829269323931 ) ) ;
#23127=CARTESIAN_POINT ( 'NONE',  ( 0.9873396505805591694, -0.1113553986120547346, 1.333661417215306955 ) ) ;
#23130=CARTESIAN_POINT ( 'NONE',  ( -0.8759842519685039353, 0.1787899950787401882, 1.567421259788755794 ) ) ;
#23132=CARTESIAN_POINT ( 'NONE',  ( -0.8019270111902717657, 0.1787899950787401604, 1.259842519631276359 ) ) ;
#23136=CARTESIAN_POINT ( 'NONE',  ( -0.9500414927467378812, 0.1787899950787401604, 0.3887795275052913224 ) ) ;
#23138=CARTESIAN_POINT ( 'NONE',  ( -0.8107537697050254399, -0.1574803149606297803, 1.877460629813732407 ) ) ;
#23140=ORIENTED_EDGE ( 'NONE', *, *, #14732, .F. ) ;
#23144=CIRCLE ( 'NONE', #5544, 0.1787899950787401049 ) ;
#23145=CARTESIAN_POINT ( 'NONE',  ( -0.7185039370078746268, -0.06523048226347956391, 0.2583661416247562959 ) ) ;
#23147=FACE_OUTER_BOUND ( 'NONE', #30987, .T. ) ;
#23149=CARTESIAN_POINT ( 'NONE',  ( -0.9500414927467377701, 0.1787899950787401604, 0.1919291338045042705 ) ) ;
#23150=CARTESIAN_POINT ( 'NONE',  ( -0.7185039370078746268, 0.06523048226347956391, 0.8932086614173218031 ) ) ;
#23154=CYLINDRICAL_SURFACE ( 'NONE', #40148, 0.1574803149606299191 ) ;
#23155=CARTESIAN_POINT ( 'NONE',  ( 0.8019270111902717657, -0.1787899950787401604, 0.9596456692375764375 ) ) ;
#23157=CARTESIAN_POINT ( 'NONE',  ( 1.033464566929134687, -0.06523048226347956391, 1.582185039370078927 ) ) ;
#23158=CARTESIAN_POINT ( 'NONE',  ( 0.7102849092615979298, 0.006128682583928486173, 1.983157089510096949 ) ) ;
#23162=EDGE_CURVE ( 'NONE', #27640, #32335, #47399, .T. ) ;
#23165=CARTESIAN_POINT ( 'NONE',  ( 1.002407869896990045, 0.1264236179284866091, 1.011318897584031484 ) ) ;
#23167=CARTESIAN_POINT ( 'NONE',  ( 1.002407869896990045, 0.1264236179284866091, 1.843011810969858333 ) ) ;
#23174=CARTESIAN_POINT ( 'NONE',  ( -0.7646288533564489232, -0.1113553986120547346, 0.1033464565853864231 ) ) ;
#23176=CARTESIAN_POINT ( 'NONE',  ( 0.8019270111902717657, 0.1787899950787401604, 1.176181102308441417 ) ) ;
#23177=EDGE_CURVE ( 'NONE', #26106, #31809, #23144, .T. ) ;
#23182=CARTESIAN_POINT ( 'NONE',  ( -1.054774247047244540, 0.07405724077823318263, 0.1820866141194649179 ) ) ;
#23188=CARTESIAN_POINT ( 'NONE',  ( -1.054774247047244540, 0.07405724077823318263, 1.874999999946236784 ) ) ;
#23189=CARTESIAN_POINT ( 'NONE',  ( -1.054774247047244540, -0.07405724077823318263, 0.9645669290800954476 ) ) ;
#23190=CARTESIAN_POINT ( 'NONE',  ( -0.9500414927467378812, -0.1787899950787401604, 0.4921259841982048577 ) ) ;
#23191=CARTESIAN_POINT ( 'NONE',  ( 0.7185039370078739607, 1.928577636452523993E-17, 0.5314960628845992741 ) ) ;
#23193=DIRECTION ( 'NONE',  ( 0.000000000000000000, 0.000000000000000000, -1.000000000000000000 ) ) ;
#23194=CARTESIAN_POINT ( 'NONE',  ( -1.033464566929134687, 0.06523048226347956391, 1.665846456692914312 ) ) ;
#23197=CARTESIAN_POINT ( 'NONE',  ( 0.7646288533564489232, -0.1113553986120547346, 0.4675196850393700809 ) ) ;
#23198=CARTESIAN_POINT ( 'NONE',  ( -0.7185039370078739607, 1.928577636452523993E-17, 1.161417322727118284 ) ) ;
#23199=CARTESIAN_POINT ( 'NONE',  ( -0.8019270111902717657, -0.1787899950787401604, 0.4429133857730075952 ) ) ;
#23200=CARTESIAN_POINT ( 'NONE',  ( 1.033464566929134687, 0.06523048226347956391, 1.183562992018456272 ) ) ;
#23204=CARTESIAN_POINT ( 'NONE',  ( -0.8759842519685039353, 0.1787899950787401882, 1.572342519631275692 ) ) ;
#23205=CARTESIAN_POINT ( 'NONE',  ( -0.8759842519685039353, 0.1787899950787401882, 0.7406496062454487328 ) ) ;
#23209=( BOUNDED_CURVE ( )  B_SPLINE_CURVE ( 2, ( #42987, #28667, #10436, #39168, #32252, #2281, #35600, #42740, #17367 ),
 .UNSPECIFIED., .F., .F. ) 
 B_SPLINE_CURVE_WITH_KNOTS ( ( 3, 2, 2, 2, 3 ),
 ( 0.5500000000000000444, 0.5524999999999999911, 0.5550000000000000488, 0.5574999999999999956, 0.5600000000000000533 ),
 .UNSPECIFIED. ) 
 CURVE ( )  GEOMETRIC_REPRESENTATION_ITEM ( )  RATIONAL_B_SPLINE_CURVE ( ( 1.000000000000000000, 0.9238795325112869605, 1.000000000000000000, 0.9238795325112869605, 1.000000000000000000, 0.9238795325112869605, 1.000000000000000000, 0.9238795325112869605, 1.000000000000000000 ) ) 
 REPRESENTATION_ITEM ( '' )  ) ;
#23211=CARTESIAN_POINT ( 'NONE',  ( 0.9412147342319837628, -0.1574803149606297803, 0.1993110236220472509 ) ) ;
#23212=CARTESIAN_POINT ( 'NONE',  ( 0.7646288533564489232, 0.1113553986120547346, 0.9694881889763780070 ) ) ;
#23213=CARTESIAN_POINT ( 'NONE',  ( 0.8107537697050253289, -0.1574803149606297803, 0.4306102362204725642 ) ) ;
#23215=CARTESIAN_POINT ( 'NONE',  ( -0.8759842519685039353, -0.1574803149606299191, 1.053149606191685184 ) ) ;
#23216=CARTESIAN_POINT ( 'NONE',  ( 0.9500414927467378812, 0.1787899950787401604, 0.6249999999462356737 ) ) ;
#23219=CARTESIAN_POINT ( 'NONE',  ( 0.9412147342319837628, -0.1574803149606297803, 0.3567913385826773087 ) ) ;
#23220=CARTESIAN_POINT ( 'NONE',  ( 0.9412147342319837628, -0.1574803149606297803, 2.000492125876725424 ) ) ;
#23221=ORIENTED_EDGE ( 'NONE', *, *, #16944, .T. ) ;
#23223=CARTESIAN_POINT ( 'NONE',  ( -0.6971942568897648851, -0.07405724077823297447, 1.151574803095843036 ) ) ;
#23224=CARTESIAN_POINT ( 'NONE',  ( 0.8107537697050253289, 0.1574803149606300301, 1.163877952755904666 ) ) ;
#23225=CARTESIAN_POINT ( 'NONE',  ( -0.8759842519685039353, 0.1574803149606299191, 0.7185039369003465293 ) ) ;
#23228=FACE_OUTER_BOUND ( 'NONE', #42265, .T. ) ;
#23229=DIRECTION ( 'NONE',  ( 1.822029033848725028E-16, 0.000000000000000000, 1.000000000000000000 ) ) ;
#23232=EDGE_LOOP ( 'NONE', ( #8335, #15556, #30298, #8201 ) ) ;
#23234=CARTESIAN_POINT ( 'NONE',  ( 1.002407869896990045, -0.1264236179284866091, 0.6865157479777322935 ) ) ;
#23235=CARTESIAN_POINT ( 'NONE',  ( -1.033464566929133799, 0.000000000000000000, 1.112204724409448842 ) ) ;
#23236=EDGE_CURVE ( 'NONE', #40379, #19512, #27275, .T. ) ;
#23242=CARTESIAN_POINT ( 'NONE',  ( 0.7646288533564489232, 0.1113553986120547346, 1.195866141624756018 ) ) ;
#23246=CARTESIAN_POINT ( 'NONE',  ( -0.6971942568897637749, 2.189545951927499583E-17, 1.779035433017102319 ) ) ;
#23247=CARTESIAN_POINT ( 'NONE',  ( 1.002407869896990045, -0.1264236179284866091, 1.793799212544661348 ) ) ;
#23250=CARTESIAN_POINT ( 'NONE',  ( 0.8759842519685039353, 0.1787899950787401882, 0.4306102361667086820 ) ) ;
#23251=CARTESIAN_POINT ( 'NONE',  ( -0.8019270111902717657, -0.1787899950787401604, 1.309055118056472899 ) ) ;
#23252=CARTESIAN_POINT ( 'NONE',  ( -0.7185039370078739607, 1.928577636452523993E-17, 0.7283464565853858819 ) ) ;
#23253=CARTESIAN_POINT ( 'NONE',  ( -0.6971942568897637749, 2.189545951927499583E-17, 1.301673228292692830 ) ) ;
#23254=CARTESIAN_POINT ( 'NONE',  ( -1.054774247047244540, -0.07405724077823318263, 0.8858267715997791836 ) ) ;
#23255=CARTESIAN_POINT ( 'NONE',  ( -0.6971942568897626646, 0.07405724077823318263, 0.04429133852891373180 ) ) ;
#23257=CARTESIAN_POINT ( 'NONE',  ( -1.054774247047244540, 0.07405724077823318263, 1.801181102308441861 ) ) ;
#23258=CARTESIAN_POINT ( 'NONE',  ( -0.8019270111902717657, 0.1787899950787401604, 0.07874015742655145200 ) ) ;
#23259=CARTESIAN_POINT ( 'NONE',  ( -0.7185039370078739607, 1.928577636452523993E-17, 1.830708661309795149 ) ) ;
#23260=CARTESIAN_POINT ( 'NONE',  ( -0.9873396505805591694, -0.1113553986120547346, 1.776574803149606252 ) ) ;
#23261=CARTESIAN_POINT ( 'NONE',  ( -1.033464566929134687, 0.06523048226347956391, 0.2878937007874017850 ) ) ;
#23263=CARTESIAN_POINT ( 'NONE',  ( 0.9873396505805591694, 0.1113553986120547346, 0.2017716534357799352 ) ) ;
#23276=CARTESIAN_POINT ( 'NONE',  ( 0.9500414927467378812, 0.1787899950787401604, 0.6988188975840318173 ) ) ;
#23281=CARTESIAN_POINT ( 'NONE',  ( 0.9412147342319837628, 0.1574803149606300301, 0.4502952755905510474 ) ) ;
#23282=CARTESIAN_POINT ( 'NONE',  ( 0.7495606340400177148, 0.1264236179284866091, 1.931594488135212728 ) ) ;
#23283=ADVANCED_FACE ( 'NONE', ( #33147 ), #43892, .T. ) ;
#23284=CARTESIAN_POINT ( 'NONE',  ( 0.8107537697050234415, -0.1574803149606297803, 0.1156496062992125873 ) ) ;
#23287=CARTESIAN_POINT ( 'NONE',  ( 0.7646288533564489232, -0.1113553986120547346, 0.1131889763779527630 ) ) ;
#23289=CARTESIAN_POINT ( 'NONE',  ( 0.9500414927467378812, 0.1787899950787401604, 0.1919291338045042428 ) ) ;
#23290=CARTESIAN_POINT ( 'NONE',  ( -0.7495606340400177148, -0.1264236179284866091, 1.700295275536787498 ) ) ;
#23292=CARTESIAN_POINT ( 'NONE',  ( -1.002407869896990045, 0.1264236179284866091, 1.370570866087968520 ) ) ;
#23293=CARTESIAN_POINT ( 'NONE',  ( 0.8759842519685039353, 0.1787899950787401882, 1.454232283410803017 ) ) ;
#23294=CARTESIAN_POINT ( 'NONE',  ( 0.9500414927467378812, 0.1787899950787401604, 0.1131889763241892138 ) ) ;
#23295=CARTESIAN_POINT ( 'NONE',  ( -1.054774247047244540, -0.07405724077823318263, 1.161417322780881278 ) ) ;
#23298=CARTESIAN_POINT ( 'NONE',  ( 0.7185039370078739607, 1.928577636452523993E-17, 1.210629921259842590 ) ) ;
#23299=CARTESIAN_POINT ( 'NONE',  ( 0.7495606340400177148, -0.1264236179284866091, 0.4847440944344252323 ) ) ;
#23300=CARTESIAN_POINT ( 'NONE',  ( -1.002407869896990045, 0.1264236179284866091, 0.4207677164816693294 ) ) ;
#23301=CARTESIAN_POINT ( 'NONE',  ( -0.7646288533564489232, 0.1113553986120547346, 0.8809055117034961802 ) ) ;
#23302=ORIENTED_EDGE ( 'NONE', *, *, #34435, .F. ) ;
#23304=CARTESIAN_POINT ( 'NONE',  ( -0.8107537697050253289, 0.1574803149606300301, 0.2977362204724410821 ) ) ;
#23305=CARTESIAN_POINT ( 'NONE',  ( 0.6971942568897637749, 2.189545951927499583E-17, 1.227854330654897685 ) ) ;
#23306=CARTESIAN_POINT ( 'NONE',  ( -1.002407869896990045, 0.1264236179284866091, 1.956200787347811110 ) ) ;
#23309=VECTOR ( 'NONE', #14382, 39.37007874015748143 ) ;
#23312=CARTESIAN_POINT ( 'NONE',  ( -0.6971942568897626646, 0.07405724077823318263, 0.9891732282926934960 ) ) ;
#23314=CARTESIAN_POINT ( 'NONE',  ( -0.7646288533564489232, 0.1113553986120547346, 1.471456692805858113 ) ) ;
#23319=CARTESIAN_POINT ( 'NONE',  ( 0.7646288533564489232, 0.1113553986120547346, 1.008858267716535417 ) ) ;
#23322=CARTESIAN_POINT ( 'NONE',  ( 0.9873396505805591694, 0.1113553986120547346, 0.8809055118110236116 ) ) ;
#23323=CARTESIAN_POINT ( 'NONE',  ( 1.033464566929133799, 0.000000000000000000, 0.7480314959554645871 ) ) ;
#23325=( BOUNDED_SURFACE ( )  B_SPLINE_SURFACE ( 1, 2, ( 
 ( #21431, #25282, #36314, #24750, #43412, #17553, #39345, #10621, #39812, #25481, #46778, #26180, #15866, #30037, #37897, #4323, #23038, #499, #15158, #15632, #29802, #33384, #44580, #4105, #5054, #33153, #37656, #18955, #30494, #4812, #18724, #274, #37404, #40748, #11799, #12034, #14918, #44349, #29583, #7945, #40516, #33856, #30270, #23284, #731, #15393, #44822, #7705, #40986, #22562, #44125, #37179, #8647, #26417, #8170, #4562, #26657, #19197, #975, #41204, #8410, #19435, #34085, #1215, #45053, #12265, #26888, #41445, #30729, #24233, #45298, #17029, #2166, #24454, #12751, #41923, #16563, #27139, #45766, #27614, #31667, #12516, #41690, #45527, #8893, #5288, #23524, #34538, #1690, #42168, #10078, #35947, #21563, #23879, #38489, #45896, #13337, #27745, #20738, #35379, #43483, #14508, #14278, #22393, #32976, #11392, #36073, #14747, #7070, #348, #43247, #18096, #29170, #14997, #28919, #26005, #25049, #15143, #36476, #18251, #29333, #11, #962, #12020, #17477, #33308, #47430, #7869, #21795, #40444, #17945, #32604, #194, #47191, #14373, #14601, #21546, #22485, #46943, #22245, #36419, #434, #36877, #36184, #14133, #36644, #10790, #25636, #29506, #28778, #6922, #10547, #25400, #25145, #18420, #14841, #40672, #3577, #18195, #44053, #7170, #11251, #32835, #25862, #4031, #26100, #18651, #15086, #29733, #44274, #11478, #23213, #15564, #26348, #34017, #40907, #38056, #27063, #1141, #41855, #19604, #30428, #9059, #34466, #1616, #26818, #8816, #41375, #41612, #37575, #44512, #4736, #44980, #8106, #8575, #19838, #16266, #22728, #37827, #4982, #30659, #23453, #4483, #5210, #18887, #45219, #30203, #15311, #11729, #11966, #26587, #12441, #42567, #13374, #42790, #34950, #39218, #12912, #35418, #42345, #9775, #46177, #34719, #45692, #1858, #9299, #13589, #20309, #35652, #9541, #13150, #17419, #10005, #31360, #45940, #38289, #16956, #20544, #13831, #31596, #24386, #43042, #38985, #6154, #20777, #17191, #7356, #21249, #39926, #137, #3027, #40389, #46885, #6865, #14073, #3523, #36827, #33015, #36593, #28721, #14790, #36118, #43290, #47374, #29451, #10490, #3750, #28963, #7113, #43764, #10734, #18373, #25088, #40157, #7578, #21486, #3273, #14546, #32545, #47133, #21736, #18135, #36368, #32780, #29216, #10966, #25584, #29027, #29282, #39518, #35712, #24925, #43827, #10067, #2848, #36192, #21555, #42856, #25411, #39987, #14380, #6694, #28294, #20842, #17485, #39047, #36429, #46706, #3348, #43586, #46474, #43108, #6216, #28786, #21310, #17956, #10799, #35939, #11028, #24685, #32119, #32613, #47200, #39282, #7179, #21804, #3585, #3098, #6457, #35483, #13896, #2622, #18204, #28540, #32845, #47440, #13657, #10314, #17255, #43352, #17724, #14608, #31893, #32373, #21074, #46951, #14146, #10556, #25155, #39745, #6932, #44063, #40686, #40920, #11739, #26597, #29516, #41149, #37586, #22738, #18661, #4748, #30438, #33320, #22977, #37116, #44524, #15323, #30214, #36889, #8351, #14853, #37343, #44285, #29976, #668, #22027, #204, #36652, #33081, #33796, #3811, #19375, #29742, #15096, #34028, #914, #11261, #443, #40220, #18897, #25871, #1154, #7879, #18427, #44991, #15575, #15809, #11490, #26111, #4494, #40455, #22496, #44759, #25645, #7640, #22255, #4043, #4264, #33552, #26359, #19132, #23933, #4996, #34960, #38066, #41385, #1869, #2105, #12203, #5705, #30906, #41867, #45704, #45467, #9310, #16041, #42104, #38540, #8831, #20321, #16507, #16735, #9552, #12693, #20085, #45230, #31371, #34731, #45948, #24173, #13160, #2338, #27318, #23464, #19850, #27795, #42356, #19614, #16278, #26829, #31136, #9070, #38774, #5934, #23689, #34252, #38300, #5468, #30670, #12922, #20552, #35193, #12454, #27552, #16964, #31605, #8587, #27074, #23224, #37838, #1385, #5221, #41622, #34477, #1629, #17905, #10499, #38994, #6639, #42798, #28014, #24395, #21746, #10013, #20785, #3534, #39687, #32315, #46893, #24628, #35428, #28480, #2565, #47143, #36127, #10258, #36377, #28729, #43052, #18145, #43529, #10744, #35883, #32555, #3036, #3283, #39228, #6401, #46186, #13383, #17428, #13837, #24862, #42576, #14327, #9785, #28972, #14084, #6165, #21014, #35662, #2797, #17200, #32065, #39464, #17667, #25353, #31836, #46653, #43299, #46420, #39935, #25097, #7123, #13597, #28236, #21258, #6874, #21494, #8055, #40860, #144, #4437, #15040, #850, #14799, #18606, #21976, #11911, #29690, #15510, #25592, #44231, #29459, #15267, #4687, #44004, #11207, #33495, #33021, #25819, #37283, #11437, #36599, #30154, #33265, #40398, #26054, #4211, #7584, #44693, #40625, #29918, #7821, #22916, #26533, #41093, #22438, #19068, #37058, #33739, #22198, #36834, #32788, #47383, #3985, #18840, #611, #29225, #37529, #14555, #43773, #44464, #10976, #11677, #22681, #40164, #7364, #3756, #18379, #23630, #34905, #9492, #45171, #5398, #37776, #23865, #38240, #20258, #5647, #26769, #4929, #45415, #15750, #42044, #12860, #34200, #38477, #1565, #2046, #1327, #5167, #8527, #45886, #16218, #16681, #12146, #30848, #15984, #1810, #38718, #30606, #12393, #20022, #19553, #27014, #31308, #34419, #23157, #13098, #19786, #41560, #12629, #34662, #8767, #27731, #27254, #24112, #38006, #9247, #23403, #41806, #16448, #9005, #31079, #45643, #27493, #19317, #33966, #42295, #1093, #30385, #44931, #41327, #35136, #39394, #46362, #42985, #32249, #2279, #24338, #16907, #6100, #20723, #6579, #17603, #21190, #31546, #25035, #46829, #35367, #35824, #28178, #42738, #9954, #5888, #24565, #39166, #2972, #14017, #28664, #43230, #21430, #17845, #47073, #14266, #31849, #28247, #10509, #24639, #46903, #6884, #35672, #2809, #28492, #43062, #31295, #30839, #35586, #38925, #46349, #9236, #34895, #13313, #45406, #45876, #6087, #16205, #31764, #5389, #12850, #12617, #9483, #42729, #20713, #27941, #8996, #35354, #42033, #27241, #5878, #2500, #41796, #9715, #2036, #13088, #2267, #16666, #42510, #20008, #46115, #24327, #27482, #17124, #20484, #13533, #28168, #27718, #24098, #1801, #9943, #38708, #24549, #39157, #6327, #20946, #42284, #23853, #35120, #23619, #34650, #38466, #38230, #16437, #31068, #45631, #5637, #20247, #16890, #31533, #31993, #43216, #2729, #73, #10426, #47309, #7288, #10182, #6801, #17358, #39857, #3207, #32717, #25530, #21421, #42972, #17837, #36049, #6570, #32481, #32952, #29392, #21180, #47060, #18069, #36304, #36531, #35812, #3688, #14719 ),
 ( #39385, #18312, #40095, #14255, #40326, #14483, #24788, #10661, #14006, #46584, #28404, #25756, #25027, #2959, #7510, #43696, #3455, #29143, #39623, #17596, #28897, #32238, #43938, #21909, #43456, #22132, #10906, #25268, #13764, #11134, #7047, #21674, #8453, #41024, #41251, #29846, #33428, #8693, #36760, #7984, #4367, #773, #33195, #23082, #18540, #37699, #37458, #26935, #44388, #11603, #26223, #44164, #37220, #18998, #8217, #4853, #3916, #15197, #22844, #7749, #1256, #4608, #15911, #30536, #11365, #22364, #15432, #316, #12072, #30312, #4145, #45098, #33659, #14965, #18768, #44622, #25973, #29625, #19240, #40558, #36990, #33899, #541, #1019, #40790, #15677, #44863, #26696, #12787, #27423, #27888, #13259, #13705, #40034, #43156, #17536, #24971, #28838, #35758, #7230, #6743, #14660, #28593, #47246, #6507, #21125, #39793, #2898, #10120, #21361, #28341, #29332, #9886, #14428, #10366, #21850, #29080, #42912, #24500, #43395, #32170, #35989, #3394, #39093, #46760, #20892, #13946, #2671, #10607, #21610, #25206, #17302, #43637, #3150, #10, #36475, #3629, #6986, #10847, #18005, #32893, #39566, #17775, #31936, #46525, #32660, #12739, #23739, #19663, #16782, #12503, #45999, #9363, #20601, #23516, #34525, #27369, #27126, #1920, #23986, #5762, #9601, #5981, #23794, #31472, #16384, #2441, #2213, #46295, #31710, #5329, #31004, #24045, #8942, #20657, #38872, #27429, #13487, #42223, #28116, #38408, #31239, #1740, #24504, #38646, #9891, #19949, #5820, #5581, #27893, #17307, #34837, #1982, #46056, #45816, #13024, #39098, #20428, #35062, #6271, #13264, #42456, #9660, #24276, #6036, #35536, #35305, #2677, #45347, #12559, #27185, #46766, #14433, #13950, #32178, #28842, #2906, #36706, #3869, #21856, #3155, #29341, #3637, #17541, #46529, #36250, #24977, #10612, #10855, #13711, #35764, #28347, #28602, #24736, #32665, #43645, #47252, #10127, #18257, #25467, #39333, #39800, #43164, #42917, #6511, #7460, #39572, #21131, #31943, #40039, #18012, #29086, #6748, #21369, #14198, #35996, #32899, #36482, #43401, #22083, #7236, #3401, #17779, #14667, #25209, #32428, #47006, #17, #6991, #21616, #43884, #11084, #25704, #40275, #36941, #23276, #37892, #8404, #37170, #15862, #37647, #4093, #33137, #22791, #44340, #44573, #44815, #265, #22311, #14909, #18716, #11312, #19188, #30264, #33846, #44117, #4800, #12025, #25926, #26410, #15148, #29571, #40508, #8639, #29793, #7697, #18487, #26650, #4553, #967, #11548, #33373, #722, #492, #19429, #23031, #30031, #26170, #15625, #15383, #40739, #30486, #45046, #8164, #34081, #37398, #1209, #7935, #22551, #4314, #18947, #11793, #40976, #41198, #12260, #26883, #34309, #24229, #5767, #42631, #45522, #27376, #41916, #12508, #23742, #20139, #9369, #20608, #9838, #30956, #38592, #23520, #9608, #23993, #5987, #38824, #27133, #38123, #31188, #1439, #27846, #46005, #19901, #35253, #34785, #2389, #34531, #38351, #41681, #31660, #1926, #17023, #45292, #16558, #1686, #35012, #24448, #16333, #12745, #20372, #5283, #9127, #46235, #45761, #8888, #13438, #5525, #12972, #27608, #28068, #42163, #5050, #2160, #16788, #31426, #19669, #13211, #16099, #42407, #30722, #374, #15255, #47368, #44217, #26035, #33480, #40611, #18824, #19056, #598, #44445, #30138, #44678, #41078, #37515, #40150, #7350, #17832, #31989, #10656, #39151, #43212, #46346, #13529, #35810, #28165, #42724, #46579, #6322, #25264, #20481, #25022, #20942, #32477, #6798, #35582, #2263, #2954, #28401, #42968, #32235, #16887, #17592, #31528, #21416, #13310, #47056, #4142, #40553, #18065, #11596, #18763, #32712, #312, #36527, #21668, #47304, #15428, #3683, #29138, #44615, #33423, #25969, #7745, #18306, #43693, #22127, #10899, #40785, #29841, #3912, #30078, #22359, #36754, #11831, #37214, #4361, #29621, #26219, #44161, #44384, #32948, #68, #39853, #7043, #11131, #7507, #18534, #36300, #7980, #3452, #22602, #537, #25523, #14713, #29387, #43934, #40090, #25753, #33188, #11361, #18995, #7285, #40322, #15193, #21905, #33653, #768, #14959, #12781, #33893, #12068, #5088, #22838, #1729, #19940, #41244, #30772, #45561, #27175, #30998, #12310, #37694, #45804, #26455, #26930, #41481, #37936, #37452, #27417, #8210, #41960, #41727, #31227, #8687, #34351, #23555, #44858, #5322, #34575, #16373, #9168, #41020, #38397, #20178, #34828, #1971, #4602, #13941, #46752, #20418, #27882, #39086, #9412, #35753, #21117, #2432, #32161, #42667, #43148, #46285, #13474, #2202, #6736, #24493, #21353, #35053, #20885, #28107, #24723, #32415, #35527, #2666, #13699, #17297, #31930, #17530, #46519, #16820, #35983, #28333, #2889, #3139, #17767, #13011, #27654, #42209, #24030, #38635, #32596, #36759, #3915, #44387, #18539, #14718, #11364, #72, #29142, #43695, #33658, #40557, #11835, #30085, #22363, #10905, #11602, #7983, #22606, #37219, #40094, #18311, #21908, #44621, #3687, #26462, #41023, #8216, #37457, #4607, #12786, #41250, #23561, #45097, #30311, #8452, #24039, #12317, #37698, #5815, #41966, #34582, #1735, #26934, #4852, #45342, #19477, #1976, #38402, #27179, #38642, #9171, #5325, #20424, #45811, #13019, #19945, #16607, #30535, #34354, #41486, #42217, #23790, #31233, #8692, #20184, #23327, #34832, #1018, #37941, #5092, #9420, #19715, #16145, #15676, #44862, #46290, #17774, #17301, #42674, #46524, #6506, #24499, #14192, #13704, #46051, #28340, #28837, #42911, #10119, #17535, #32169, #10365, #27887, #42448, #40969, #32659, #11540, #40270, #33604, #40734, #40033, #47245, #25921, #9, #257, #487, #14427, #25461, #29079, #7229, #43636, #33368, #15142, #29790, #10846, #7928, #44336, #36474, #29566, #18250, #32892, #29331, #11788, #43877, #25698, #7456, #22547, #7690, #37163, #22077, #36702, #3863, #18483, #4310, #717, #33131, #14904, #15377, #19662, #22786, #37394, #4549, #45287, #9123, #23515, #19182, #1204, #45041, #15620, #30260, #41439, #34305, #1432, #8635, #16093, #30714, #38119, #18527, #22593, #10892, #40082, #7279, #25256, #36519, #32940, #22119, #33415, #37207, #43684, #3904, #3444, #36976, #36745, #18755, #4132, #39845, #18057, #43924, #14243, #40543, #11353, #32703, #530, #29833, #29612, #10650, #44376, #25513, #28884, #7499, #11586, #17824, #25962, #3674, #14706, #304, #18297, #14950, #47294, #44153, #26211, #14474, #43446, #7034, #29129, #21897, #25744, #12296, #4591, #16130, #26920 ) ),
 .UNSPECIFIED., .F., .F., .T. ) 
 B_SPLINE_SURFACE_WITH_KNOTS ( ( 2, 2 ),
 ( 3, 2, 2, 2, 2, 2, 2, 2, 2, 2, 2, 2, 2, 2, 2, 2, 2, 2, 2, 2, 2, 2, 2, 2, 2, 2, 2, 2, 2, 2, 2, 2, 2, 2, 2, 2, 2, 2, 2, 2, 2, 2, 2, 2, 2, 2, 2, 2, 2, 2, 2, 2, 2, 2, 2, 2, 2, 2, 2, 2, 2, 2, 2, 2, 2, 2, 2, 2, 2, 2, 2, 2, 2, 2, 2, 2, 2, 2, 2, 2, 2, 2, 2, 2, 2, 2, 2, 2, 2, 2, 2, 2, 2, 2, 2, 2, 2, 2, 2, 2, 2, 2, 2, 2, 2, 2, 2, 2, 2, 2, 2, 2, 2, 2, 2, 2, 2, 2, 2, 2, 2, 2, 2, 2, 2, 2, 2, 2, 2, 2, 2, 2, 2, 2, 2, 2, 2, 2, 2, 2, 2, 2, 2, 2, 2, 2, 2, 2, 2, 2, 2, 2, 2, 2, 2, 2, 2, 2, 2, 2, 2, 2, 2, 2, 2, 2, 2, 2, 2, 2, 2, 2, 2, 2, 2, 2, 2, 2, 2, 2, 2, 2, 2, 2, 2, 2, 2, 2, 2, 2, 2, 2, 2, 2, 2, 2, 2, 2, 2, 2, 2, 2, 2, 2, 2, 2, 2, 2, 2, 2, 2, 2, 2, 2, 2, 2, 2, 2, 2, 2, 2, 2, 2, 2, 2, 2, 2, 2, 2, 2, 2, 2, 2, 2, 2, 2, 2, 2, 2, 2, 2, 2, 2, 2, 2, 2, 2, 2, 2, 2, 2, 2, 2, 2, 2, 2, 2, 2, 2, 2, 2, 2, 2, 2, 2, 2, 2, 2, 2, 2, 2, 2, 2, 2, 2, 2, 2, 2, 2, 2, 2, 2, 2, 2, 2, 2, 2, 2, 2, 2, 2, 2, 2, 2, 2, 2, 2, 2, 2, 2, 2, 2, 2, 2, 2, 2, 2, 2, 2, 2, 2, 2, 2, 2, 2, 2, 2, 2, 2, 2, 2, 2, 2, 2, 2, 2, 2, 2, 2, 2, 2, 2, 2, 2, 2, 2, 2, 2, 2, 2, 2, 2, 2, 2, 2, 2, 2, 2, 2, 2, 2, 2, 2, 2, 2, 2, 2, 2, 2, 2, 2, 2, 2, 2, 2, 2, 2, 2, 2, 2, 2, 2, 2, 2, 2, 2, 2, 2, 2, 2, 2, 2, 2, 2, 2, 2, 2, 2, 2, 2, 2, 2, 2, 2, 2, 2, 2, 2, 2, 2, 3 ),
 ( 0.000000000000000000, 1.000000000000000000 ),
 ( 0.000000000000000000, 0.002500000000000000052, 0.005000000000000000104, 0.007499999999999999722, 0.01000000000000000021, 0.01250000000000000069, 0.01499999999999999944, 0.01750000000000000167, 0.02000000000000000042, 0.02249999999999999917, 0.02500000000000000139, 0.02750000000000000014, 0.02999999999999999889, 0.03250000000000000111, 0.03500000000000000333, 0.03749999999999999861, 0.04000000000000000083, 0.04250000000000000305, 0.04499999999999999833, 0.04750000000000000056, 0.05000000000000000278, 0.05249999999999999806, 0.05500000000000000028, 0.05750000000000000250, 0.05999999999999999778, 0.06250000000000000000, 0.06500000000000000222, 0.06750000000000000444, 0.07000000000000000666, 0.07249999999999999500, 0.07499999999999999722, 0.07749999999999999944, 0.08000000000000000167, 0.08250000000000000389, 0.08500000000000000611, 0.08749999999999999445, 0.08999999999999999667, 0.09249999999999999889, 0.09500000000000000111, 0.09750000000000000333, 0.1000000000000000056, 0.1024999999999999939, 0.1049999999999999961, 0.1074999999999999983, 0.1100000000000000006, 0.1125000000000000028, 0.1150000000000000050, 0.1174999999999999933, 0.1199999999999999956, 0.1224999999999999978, 0.1250000000000000000, 0.1275000000000000022, 0.1300000000000000044, 0.1325000000000000067, 0.1350000000000000089, 0.1375000000000000111, 0.1400000000000000133, 0.1424999999999999878, 0.1449999999999999900, 0.1474999999999999922, 0.1499999999999999944, 0.1524999999999999967, 0.1549999999999999989, 0.1575000000000000011, 0.1600000000000000033, 0.1625000000000000056, 0.1650000000000000078, 0.1675000000000000100, 0.1700000000000000122, 0.1724999999999999867, 0.1749999999999999889, 0.1774999999999999911, 0.1799999999999999933, 0.1824999999999999956, 0.1849999999999999978, 0.1875000000000000000, 0.1900000000000000022, 0.1925000000000000044, 0.1950000000000000067, 0.1975000000000000089, 0.2000000000000000111, 0.2025000000000000133, 0.2049999999999999878, 0.2074999999999999900, 0.2099999999999999922, 0.2124999999999999944, 0.2149999999999999967, 0.2174999999999999989, 0.2200000000000000011, 0.2225000000000000033, 0.2250000000000000056, 0.2275000000000000078, 0.2300000000000000100, 0.2325000000000000122, 0.2349999999999999867, 0.2374999999999999889, 0.2399999999999999911, 0.2424999999999999933, 0.2449999999999999956, 0.2474999999999999978, 0.2500000000000000000, 0.2525000000000000022, 0.2550000000000000044, 0.2575000000000000067, 0.2600000000000000089, 0.2625000000000000111, 0.2650000000000000133, 0.2675000000000000155, 0.2700000000000000178, 0.2725000000000000200, 0.2750000000000000222, 0.2775000000000000244, 0.2800000000000000266, 0.2824999999999999734, 0.2849999999999999756, 0.2874999999999999778, 0.2899999999999999800, 0.2924999999999999822, 0.2949999999999999845, 0.2974999999999999867, 0.2999999999999999889, 0.3024999999999999911, 0.3049999999999999933, 0.3074999999999999956, 0.3099999999999999978, 0.3125000000000000000, 0.3150000000000000022, 0.3175000000000000044, 0.3200000000000000067, 0.3225000000000000089, 0.3250000000000000111, 0.3275000000000000133, 0.3300000000000000155, 0.3325000000000000178, 0.3350000000000000200, 0.3375000000000000222, 0.3400000000000000244, 0.3425000000000000266, 0.3449999999999999734, 0.3474999999999999756, 0.3499999999999999778, 0.3524999999999999800, 0.3549999999999999822, 0.3574999999999999845, 0.3599999999999999867, 0.3624999999999999889, 0.3649999999999999911, 0.3674999999999999933, 0.3699999999999999956, 0.3724999999999999978, 0.3750000000000000000, 0.3775000000000000022, 0.3800000000000000044, 0.3825000000000000067, 0.3850000000000000089, 0.3875000000000000111, 0.3900000000000000133, 0.3925000000000000155, 0.3950000000000000178, 0.3975000000000000200, 0.4000000000000000222, 0.4025000000000000244, 0.4050000000000000266, 0.4074999999999999734, 0.4099999999999999756, 0.4124999999999999778, 0.4149999999999999800, 0.4174999999999999822, 0.4199999999999999845, 0.4224999999999999867, 0.4249999999999999889, 0.4274999999999999911, 0.4299999999999999933, 0.4324999999999999956, 0.4349999999999999978, 0.4375000000000000000, 0.4400000000000000022, 0.4425000000000000044, 0.4450000000000000067, 0.4475000000000000089, 0.4500000000000000111, 0.4525000000000000133, 0.4550000000000000155, 0.4575000000000000178, 0.4600000000000000200, 0.4625000000000000222, 0.4650000000000000244, 0.4675000000000000266, 0.4699999999999999734, 0.4724999999999999756, 0.4749999999999999778, 0.4774999999999999800, 0.4799999999999999822, 0.4824999999999999845, 0.4849999999999999867, 0.4874999999999999889, 0.4899999999999999911, 0.4924999999999999933, 0.4949999999999999956, 0.4974999999999999978, 0.5000000000000000000, 0.5024999999999999467, 0.5050000000000000044, 0.5074999999999999512, 0.5100000000000000089, 0.5124999999999999556, 0.5150000000000000133, 0.5174999999999999600, 0.5200000000000000178, 0.5224999999999999645, 0.5250000000000000222, 0.5274999999999999689, 0.5300000000000000266, 0.5324999999999999734, 0.5350000000000000311, 0.5374999999999999778, 0.5400000000000000355, 0.5424999999999999822, 0.5450000000000000400, 0.5474999999999999867, 0.5500000000000000444, 0.5524999999999999911, 0.5550000000000000488, 0.5574999999999999956, 0.5600000000000000533, 0.5625000000000000000, 0.5649999999999999467, 0.5675000000000000044, 0.5699999999999999512, 0.5725000000000000089, 0.5749999999999999556, 0.5775000000000000133, 0.5799999999999999600, 0.5825000000000000178, 0.5849999999999999645, 0.5875000000000000222, 0.5899999999999999689, 0.5925000000000000266, 0.5949999999999999734, 0.5975000000000000311, 0.5999999999999999778, 0.6025000000000000355, 0.6049999999999999822, 0.6075000000000000400, 0.6099999999999999867, 0.6125000000000000444, 0.6149999999999999911, 0.6175000000000000488, 0.6199999999999999956, 0.6225000000000000533, 0.6250000000000000000, 0.6274999999999999467, 0.6300000000000000044, 0.6324999999999999512, 0.6350000000000000089, 0.6374999999999999556, 0.6400000000000000133, 0.6424999999999999600, 0.6450000000000000178, 0.6474999999999999645, 0.6500000000000000222, 0.6524999999999999689, 0.6550000000000000266, 0.6574999999999999734, 0.6600000000000000311, 0.6624999999999999778, 0.6650000000000000355, 0.6674999999999999822, 0.6700000000000000400, 0.6724999999999999867, 0.6750000000000000444, 0.6774999999999999911, 0.6800000000000000488, 0.6824999999999999956, 0.6850000000000000533, 0.6875000000000000000, 0.6899999999999999467, 0.6925000000000000044, 0.6949999999999999512, 0.6975000000000000089, 0.6999999999999999556, 0.7025000000000000133, 0.7049999999999999600, 0.7075000000000000178, 0.7099999999999999645, 0.7125000000000000222, 0.7149999999999999689, 0.7175000000000000266, 0.7199999999999999734, 0.7225000000000000311, 0.7249999999999999778, 0.7275000000000000355, 0.7299999999999999822, 0.7325000000000000400, 0.7349999999999999867, 0.7375000000000000444, 0.7399999999999999911, 0.7425000000000000488, 0.7449999999999999956, 0.7475000000000000533, 0.7500000000000000000, 0.7524999999999999467, 0.7550000000000000044, 0.7574999999999999512, 0.7600000000000000089, 0.7624999999999999556, 0.7650000000000000133, 0.7674999999999999600, 0.7700000000000000178, 0.7724999999999999645, 0.7750000000000000222, 0.7774999999999999689, 0.7800000000000000266, 0.7824999999999999734, 0.7850000000000000311, 0.7874999999999999778, 0.7900000000000000355, 0.7924999999999999822, 0.7950000000000000400, 0.7974999999999999867, 0.8000000000000000444, 0.8024999999999999911, 0.8050000000000000488, 0.8074999999999999956, 0.8100000000000000533, 0.8125000000000000000, 0.8149999999999999467, 0.8175000000000000044, 0.8199999999999999512, 0.8225000000000000089, 0.8249999999999999556, 0.8275000000000000133, 0.8299999999999999600, 0.8325000000000000178, 0.8349999999999999645, 0.8375000000000000222, 0.8399999999999999689, 0.8425000000000000266, 0.8449999999999999734, 0.8475000000000000311, 0.8499999999999999778, 0.8525000000000000355, 0.8549999999999999822, 0.8575000000000000400, 0.8599999999999999867, 0.8625000000000000444, 0.8649999999999999911, 0.8675000000000000488, 0.8699999999999999956, 0.8725000000000000533, 0.8750000000000000000, 0.8774999999999999467, 0.8800000000000000044, 0.8824999999999999512, 0.8850000000000000089, 0.8874999999999999556, 0.8900000000000000133, 0.8924999999999999600, 0.8950000000000000178, 0.8974999999999999645, 0.9000000000000000222, 0.9024999999999999689, 0.9050000000000000266, 0.9074999999999999734, 0.9100000000000000311, 0.9124999999999999778, 0.9150000000000000355, 0.9174999999999999822, 0.9200000000000000400, 0.9224999999999999867, 0.9250000000000000444, 0.9274999999999999911, 0.9300000000000000488, 0.9324999999999999956, 0.9350000000000000533, 0.9375000000000000000, 0.9399999999999999467, 0.9425000000000000044, 0.9449999999999999512, 0.9475000000000000089, 0.9499999999999999556, 0.9525000000000000133, 0.9549999999999999600, 0.9575000000000000178, 0.9599999999999999645, 0.9625000000000000222, 0.9649999999999999689, 0.9675000000000000266, 0.9699999999999999734, 0.9725000000000000311, 0.9749999999999999778, 0.9775000000000000355, 0.9799999999999999822, 0.9825000000000000400, 0.9849999999999999867, 0.9875000000000000444, 0.9899999999999999911, 0.9925000000000000488, 0.9949999999999999956, 0.9975000000000000533, 1.000000000000000000 ),
 .UNSPECIFIED. ) 
 GEOMETRIC_REPRESENTATION_ITEM ( )  RATIONAL_B_SPLINE_SURFACE ( (
 ( 1.000000000000000000, 0.9238795325112869605, 1.000000000000000000, 0.9238795325112869605, 1.000000000000000000, 0.9238795325112869605, 1.000000000000000000, 0.9238795325112869605, 1.000000000000000000, 0.9238795325112869605, 1.000000000000000000, 0.9238795325112869605, 1.000000000000000000, 0.9238795325112869605, 1.000000000000000000, 0.9238795325112869605, 1.000000000000000000, 0.9238795325112869605, 1.000000000000000000, 0.9238795325112869605, 1.000000000000000000, 0.9238795325112869605, 1.000000000000000000, 0.9238795325112869605, 1.000000000000000000, 0.9238795325112869605, 1.000000000000000000, 0.9238795325112869605, 1.000000000000000000, 0.9238795325112869605, 1.000000000000000000, 0.9238795325112869605, 1.000000000000000000, 0.9238795325112869605, 1.000000000000000000, 0.9238795325112869605, 1.000000000000000000, 0.9238795325112869605, 1.000000000000000000, 0.9238795325112869605, 1.000000000000000000, 0.9238795325112869605, 1.000000000000000000, 0.9238795325112869605, 1.000000000000000000, 0.9238795325112869605, 1.000000000000000000, 0.9238795325112869605, 1.000000000000000000, 0.9238795325112869605, 1.000000000000000000, 0.9238795325112869605, 1.000000000000000000, 0.9238795325112869605, 1.000000000000000000, 0.9238795325112869605, 1.000000000000000000, 0.9238795325112869605, 1.000000000000000000, 0.9238795325112869605, 1.000000000000000000, 0.9238795325112869605, 1.000000000000000000, 0.9238795325112869605, 1.000000000000000000, 0.9238795325112869605, 1.000000000000000000, 0.9238795325112869605, 1.000000000000000000, 0.9238795325112869605, 1.000000000000000000, 0.9238795325112869605, 1.000000000000000000, 0.9238795325112869605, 1.000000000000000000, 0.9238795325112869605, 1.000000000000000000, 0.9238795325112869605, 1.000000000000000000, 0.9238795325112869605, 1.000000000000000000, 0.9238795325112869605, 1.000000000000000000, 0.9238795325112869605, 1.000000000000000000, 0.9238795325112869605, 1.000000000000000000, 0.9238795325112869605, 1.000000000000000000, 0.9238795325112869605, 1.000000000000000000, 0.9238795325112869605, 1.000000000000000000, 0.9238795325112869605, 1.000000000000000000, 0.9238795325112869605, 1.000000000000000000, 0.9238795325112869605, 1.000000000000000000, 0.9238795325112869605, 1.000000000000000000, 0.9238795325112869605, 1.000000000000000000, 0.9238795325112869605, 1.000000000000000000, 0.9238795325112869605, 1.000000000000000000, 0.9238795325112869605, 1.000000000000000000, 0.9238795325112869605, 1.000000000000000000, 0.9238795325112869605, 1.000000000000000000, 0.9238795325112869605, 1.000000000000000000, 0.9238795325112869605, 1.000000000000000000, 0.9238795325112869605, 1.000000000000000000, 0.9238795325112869605, 1.000000000000000000, 0.9238795325112869605, 1.000000000000000000, 0.9238795325112869605, 1.000000000000000000, 0.9238795325112869605, 1.000000000000000000, 0.9238795325112869605, 1.000000000000000000, 0.9238795325112869605, 1.000000000000000000, 0.9238795325112869605, 1.000000000000000000, 0.9238795325112869605, 1.000000000000000000, 0.9238795325112869605, 1.000000000000000000, 0.9238795325112869605, 1.000000000000000000, 0.9238795325112869605, 1.000000000000000000, 0.9238795325112869605, 1.000000000000000000, 0.9238795325112869605, 1.000000000000000000, 0.9238795325112869605, 1.000000000000000000, 0.9238795325112869605, 1.000000000000000000, 0.9238795325112869605, 1.000000000000000000, 0.9238795325112869605, 1.000000000000000000, 0.9238795325112869605, 1.000000000000000000, 0.9238795325112869605, 1.000000000000000000, 0.9238795325112869605, 1.000000000000000000, 0.9238795325112869605, 1.000000000000000000, 0.9238795325112869605, 1.000000000000000000, 0.9238795325112869605, 1.000000000000000000, 0.9238795325112869605, 1.000000000000000000, 0.9238795325112869605, 1.000000000000000000, 0.9238795325112869605, 1.000000000000000000, 0.9238795325112869605, 1.000000000000000000, 0.9238795325112869605, 1.000000000000000000, 0.9238795325112869605, 1.000000000000000000, 0.9238795325112869605, 1.000000000000000000, 0.9238795325112869605, 1.000000000000000000, 0.9238795325112869605, 1.000000000000000000, 0.9238795325112869605, 1.000000000000000000, 0.9238795325112869605, 1.000000000000000000, 0.9238795325112869605, 1.000000000000000000, 0.9238795325112869605, 1.000000000000000000, 0.9238795325112869605, 1.000000000000000000, 0.9238795325112869605, 1.000000000000000000, 0.9238795325112869605, 1.000000000000000000, 0.9238795325112869605, 1.000000000000000000, 0.9238795325112869605, 1.000000000000000000, 0.9238795325112869605, 1.000000000000000000, 0.9238795325112869605, 1.000000000000000000, 0.9238795325112869605, 1.000000000000000000, 0.9238795325112869605, 1.000000000000000000, 0.9238795325112869605, 1.000000000000000000, 0.9238795325112869605, 1.000000000000000000, 0.9238795325112869605, 1.000000000000000000, 0.9238795325112869605, 1.000000000000000000, 0.9238795325112869605, 1.000000000000000000, 0.9238795325112869605, 1.000000000000000000, 0.9238795325112869605, 1.000000000000000000, 0.9238795325112869605, 1.000000000000000000, 0.9238795325112869605, 1.000000000000000000, 0.9238795325112869605, 1.000000000000000000, 0.9238795325112869605, 1.000000000000000000, 0.9238795325112869605, 1.000000000000000000, 0.9238795325112869605, 1.000000000000000000, 0.9238795325112869605, 1.000000000000000000, 0.9238795325112869605, 1.000000000000000000, 0.9238795325112869605, 1.000000000000000000, 0.9238795325112869605, 1.000000000000000000, 0.9238795325112869605, 1.000000000000000000, 0.9238795325112869605, 1.000000000000000000, 0.9238795325112869605, 1.000000000000000000, 0.9238795325112869605, 1.000000000000000000, 0.9238795325112869605, 1.000000000000000000, 0.9238795325112869605, 1.000000000000000000, 0.9238795325112869605, 1.000000000000000000, 0.9238795325112869605, 1.000000000000000000, 0.9238795325112869605, 1.000000000000000000, 0.9238795325112869605, 1.000000000000000000, 0.9238795325112869605, 1.000000000000000000, 0.9238795325112869605, 1.000000000000000000, 0.9238795325112869605, 1.000000000000000000, 0.9238795325112869605, 1.000000000000000000, 0.9238795325112869605, 1.000000000000000000, 0.9238795325112869605, 1.000000000000000000, 0.9238795325112869605, 1.000000000000000000, 0.9238795325112869605, 1.000000000000000000, 0.9238795325112869605, 1.000000000000000000, 0.9238795325112869605, 1.000000000000000000, 0.9238795325112869605, 1.000000000000000000, 0.9238795325112869605, 1.000000000000000000, 0.9238795325112869605, 1.000000000000000000, 0.9238795325112869605, 1.000000000000000000, 0.9238795325112869605, 1.000000000000000000, 0.9238795325112869605, 1.000000000000000000, 0.9238795325112869605, 1.000000000000000000, 0.9238795325112869605, 1.000000000000000000, 0.9238795325112869605, 1.000000000000000000, 0.9238795325112869605, 1.000000000000000000, 0.9238795325112869605, 1.000000000000000000, 0.9238795325112869605, 1.000000000000000000, 0.9238795325112869605, 1.000000000000000000, 0.9238795325112869605, 1.000000000000000000, 0.9238795325112869605, 1.000000000000000000, 0.9238795325112869605, 1.000000000000000000, 0.9238795325112869605, 1.000000000000000000, 0.9238795325112869605, 1.000000000000000000, 0.9238795325112869605, 1.000000000000000000, 0.9238795325112869605, 1.000000000000000000, 0.9238795325112869605, 1.000000000000000000, 0.9238795325112869605, 1.000000000000000000, 0.9238795325112869605, 1.000000000000000000, 0.9238795325112869605, 1.000000000000000000, 0.9238795325112869605, 1.000000000000000000, 0.9238795325112869605, 1.000000000000000000, 0.9238795325112869605, 1.000000000000000000, 0.9238795325112869605, 1.000000000000000000, 0.9238795325112869605, 1.000000000000000000, 0.9238795325112869605, 1.000000000000000000, 0.9238795325112869605, 1.000000000000000000, 0.9238795325112869605, 1.000000000000000000, 0.9238795325112869605, 1.000000000000000000, 0.9238795325112869605, 1.000000000000000000, 0.9238795325112869605, 1.000000000000000000, 0.9238795325112869605, 1.000000000000000000, 0.9238795325112869605, 1.000000000000000000, 0.9238795325112869605, 1.000000000000000000, 0.9238795325112869605, 1.000000000000000000, 0.9238795325112869605, 1.000000000000000000, 0.9238795325112869605, 1.000000000000000000, 0.9238795325112869605, 1.000000000000000000, 0.9238795325112869605, 1.000000000000000000, 0.9238795325112869605, 1.000000000000000000, 0.9238795325112869605, 1.000000000000000000, 0.9238795325112869605, 1.000000000000000000, 0.9238795325112869605, 1.000000000000000000, 0.9238795325112869605, 1.000000000000000000, 0.9238795325112869605, 1.000000000000000000, 0.9238795325112869605, 1.000000000000000000, 0.9238795325112869605, 1.000000000000000000, 0.9238795325112869605, 1.000000000000000000, 0.9238795325112869605, 1.000000000000000000, 0.9238795325112869605, 1.000000000000000000, 0.9238795325112869605, 1.000000000000000000, 0.9238795325112869605, 1.000000000000000000, 0.9238795325112869605, 1.000000000000000000, 0.9238795325112869605, 1.000000000000000000, 0.9238795325112869605, 1.000000000000000000, 0.9238795325112869605, 1.000000000000000000, 0.9238795325112869605, 1.000000000000000000, 0.9238795325112869605, 1.000000000000000000, 0.9238795325112869605, 1.000000000000000000, 0.9238795325112869605, 1.000000000000000000, 0.9238795325112869605, 1.000000000000000000, 0.9238795325112869605, 1.000000000000000000, 0.9238795325112869605, 1.000000000000000000, 0.9238795325112869605, 1.000000000000000000, 0.9238795325112869605, 1.000000000000000000, 0.9238795325112869605, 1.000000000000000000, 0.9238795325112869605, 1.000000000000000000, 0.9238795325112869605, 1.000000000000000000, 0.9238795325112869605, 1.000000000000000000, 0.9238795325112869605, 1.000000000000000000, 0.9238795325112869605, 1.000000000000000000, 0.9238795325112869605, 1.000000000000000000, 0.9238795325112869605, 1.000000000000000000, 0.9238795325112869605, 1.000000000000000000, 0.9238795325112869605, 1.000000000000000000, 0.9238795325112869605, 1.000000000000000000, 0.9238795325112869605, 1.000000000000000000, 0.9238795325112869605, 1.000000000000000000, 0.9238795325112869605, 1.000000000000000000, 0.9238795325112869605, 1.000000000000000000, 0.9238795325112869605, 1.000000000000000000, 0.9238795325112869605, 1.000000000000000000, 0.9238795325112869605, 1.000000000000000000, 0.9238795325112869605, 1.000000000000000000, 0.9238795325112869605, 1.000000000000000000, 0.9238795325112869605, 1.000000000000000000, 0.9238795325112869605, 1.000000000000000000, 0.9238795325112869605, 1.000000000000000000, 0.9238795325112869605, 1.000000000000000000, 0.9238795325112869605, 1.000000000000000000, 0.9238795325112869605, 1.000000000000000000, 0.9238795325112869605, 1.000000000000000000, 0.9238795325112869605, 1.000000000000000000, 0.9238795325112869605, 1.000000000000000000, 0.9238795325112869605, 1.000000000000000000, 0.9238795325112869605, 1.000000000000000000, 0.9238795325112869605, 1.000000000000000000, 0.9238795325112869605, 1.000000000000000000, 0.9238795325112869605, 1.000000000000000000, 0.9238795325112869605, 1.000000000000000000, 0.9238795325112869605, 1.000000000000000000, 0.9238795325112869605, 1.000000000000000000, 0.9238795325112869605, 1.000000000000000000, 0.9238795325112869605, 1.000000000000000000, 0.9238795325112869605, 1.000000000000000000, 0.9238795325112869605, 1.000000000000000000, 0.9238795325112869605, 1.000000000000000000, 0.9238795325112869605, 1.000000000000000000, 0.9238795325112869605, 1.000000000000000000, 0.9238795325112869605, 1.000000000000000000, 0.9238795325112869605, 1.000000000000000000, 0.9238795325112869605, 1.000000000000000000, 0.9238795325112869605, 1.000000000000000000, 0.9238795325112869605, 1.000000000000000000, 0.9238795325112869605, 1.000000000000000000, 0.9238795325112869605, 1.000000000000000000, 0.9238795325112869605, 1.000000000000000000, 0.9238795325112869605, 1.000000000000000000, 0.9238795325112869605, 1.000000000000000000, 0.9238795325112869605, 1.000000000000000000, 0.9238795325112869605, 1.000000000000000000, 0.9238795325112869605, 1.000000000000000000, 0.9238795325112869605, 1.000000000000000000, 0.9238795325112869605, 1.000000000000000000, 0.9238795325112869605, 1.000000000000000000, 0.9238795325112869605, 1.000000000000000000, 0.9238795325112869605, 1.000000000000000000, 0.9238795325112869605, 1.000000000000000000, 0.9238795325112869605, 1.000000000000000000, 0.9238795325112869605, 1.000000000000000000, 0.9238795325112869605, 1.000000000000000000, 0.9238795325112869605, 1.000000000000000000, 0.9238795325112869605, 1.000000000000000000, 0.9238795325112869605, 1.000000000000000000, 0.9238795325112869605, 1.000000000000000000, 0.9238795325112869605, 1.000000000000000000, 0.9238795325112869605, 1.000000000000000000, 0.9238795325112869605, 1.000000000000000000, 0.9238795325112869605, 1.000000000000000000, 0.9238795325112869605, 1.000000000000000000, 0.9238795325112869605, 1.000000000000000000, 0.9238795325112869605, 1.000000000000000000, 0.9238795325112869605, 1.000000000000000000, 0.9238795325112869605, 1.000000000000000000, 0.9238795325112869605, 1.000000000000000000, 0.9238795325112869605, 1.000000000000000000, 0.9238795325112869605, 1.000000000000000000, 0.9238795325112869605, 1.000000000000000000, 0.9238795325112869605, 1.000000000000000000, 0.9238795325112869605, 1.000000000000000000, 0.9238795325112869605, 1.000000000000000000, 0.9238795325112869605, 1.000000000000000000, 0.9238795325112869605, 1.000000000000000000, 0.9238795325112869605, 1.000000000000000000, 0.9238795325112869605, 1.000000000000000000, 0.9238795325112869605, 1.000000000000000000, 0.9238795325112869605, 1.000000000000000000, 0.9238795325112869605, 1.000000000000000000, 0.9238795325112869605, 1.000000000000000000, 0.9238795325112869605, 1.000000000000000000, 0.9238795325112869605, 1.000000000000000000, 0.9238795325112869605, 1.000000000000000000, 0.9238795325112869605, 1.000000000000000000, 0.9238795325112869605, 1.000000000000000000, 0.9238795325112869605, 1.000000000000000000, 0.9238795325112869605, 1.000000000000000000, 0.9238795325112869605, 1.000000000000000000, 0.9238795325112869605, 1.000000000000000000, 0.9238795325112869605, 1.000000000000000000, 0.9238795325112869605, 1.000000000000000000, 0.9238795325112869605, 1.000000000000000000, 0.9238795325112869605, 1.000000000000000000, 0.9238795325112869605, 1.000000000000000000, 0.9238795325112869605, 1.000000000000000000, 0.9238795325112869605, 1.000000000000000000, 0.9238795325112869605, 1.000000000000000000, 0.9238795325112869605, 1.000000000000000000, 0.9238795325112869605, 1.000000000000000000, 0.9238795325112869605, 1.000000000000000000, 0.9238795325112869605, 1.000000000000000000, 0.9238795325112869605, 1.000000000000000000, 0.9238795325112869605, 1.000000000000000000, 0.9238795325112869605, 1.000000000000000000, 0.9238795325112869605, 1.000000000000000000, 0.9238795325112869605, 1.000000000000000000, 0.9238795325112869605, 1.000000000000000000, 0.9238795325112869605, 1.000000000000000000, 0.9238795325112869605, 1.000000000000000000, 0.9238795325112869605, 1.000000000000000000, 0.9238795325112869605, 1.000000000000000000, 0.9238795325112869605, 1.000000000000000000, 0.9238795325112869605, 1.000000000000000000, 0.9238795325112869605, 1.000000000000000000, 0.9238795325112869605, 1.000000000000000000, 0.9238795325112869605, 1.000000000000000000, 0.9238795325112869605, 1.000000000000000000, 0.9238795325112869605, 1.000000000000000000, 0.9238795325112869605, 1.000000000000000000, 0.9238795325112869605, 1.000000000000000000, 0.9238795325112869605, 1.000000000000000000, 0.9238795325112869605, 1.000000000000000000, 0.9238795325112869605, 1.000000000000000000, 0.9238795325112869605, 1.000000000000000000, 0.9238795325112869605, 1.000000000000000000, 0.9238795325112869605, 1.000000000000000000, 0.9238795325112869605, 1.000000000000000000, 0.9238795325112869605, 1.000000000000000000, 0.9238795325112869605, 1.000000000000000000, 0.9238795325112869605, 1.000000000000000000, 0.9238795325112869605, 1.000000000000000000, 0.9238795325112869605, 1.000000000000000000, 0.9238795325112869605, 1.000000000000000000, 0.9238795325112869605, 1.000000000000000000, 0.9238795325112869605, 1.000000000000000000, 0.9238795325112869605, 1.000000000000000000, 0.9238795325112869605, 1.000000000000000000, 0.9238795325112869605, 1.000000000000000000, 0.9238795325112869605, 1.000000000000000000, 0.9238795325112869605, 1.000000000000000000, 0.9238795325112869605, 1.000000000000000000, 0.9238795325112869605, 1.000000000000000000, 0.9238795325112869605, 1.000000000000000000, 0.9238795325112869605, 1.000000000000000000, 0.9238795325112869605, 1.000000000000000000, 0.9238795325112869605, 1.000000000000000000, 0.9238795325112869605, 1.000000000000000000, 0.9238795325112869605, 1.000000000000000000, 0.9238795325112869605, 1.000000000000000000, 0.9238795325112869605, 1.000000000000000000, 0.9238795325112869605, 1.000000000000000000, 0.9238795325112869605, 1.000000000000000000, 0.9238795325112869605, 1.000000000000000000, 0.9238795325112869605, 1.000000000000000000, 0.9238795325112869605, 1.000000000000000000, 0.9238795325112869605, 1.000000000000000000, 0.9238795325112869605, 1.000000000000000000, 0.9238795325112869605, 1.000000000000000000, 0.9238795325112869605, 1.000000000000000000, 0.9238795325112869605, 1.000000000000000000, 0.9238795325112869605, 1.000000000000000000, 0.9238795325112869605, 1.000000000000000000, 0.9238795325112869605, 1.000000000000000000, 0.9238795325112869605, 1.000000000000000000, 0.9238795325112869605, 1.000000000000000000, 0.9238795325112869605, 1.000000000000000000, 0.9238795325112869605, 1.000000000000000000, 0.9238795325112869605, 1.000000000000000000, 0.9238795325112869605, 1.000000000000000000, 0.9238795325112869605, 1.000000000000000000, 0.9238795325112869605, 1.000000000000000000, 0.9238795325112869605, 1.000000000000000000, 0.9238795325112869605, 1.000000000000000000, 0.9238795325112869605, 1.000000000000000000, 0.9238795325112869605, 1.000000000000000000, 0.9238795325112869605, 1.000000000000000000),
 ( 1.000000000000000000, 0.9238795325112869605, 1.000000000000000000, 0.9238795325112869605, 1.000000000000000000, 0.9238795325112869605, 1.000000000000000000, 0.9238795325112869605, 1.000000000000000000, 0.9238795325112869605, 1.000000000000000000, 0.9238795325112869605, 1.000000000000000000, 0.9238795325112869605, 1.000000000000000000, 0.9238795325112869605, 1.000000000000000000, 0.9238795325112869605, 1.000000000000000000, 0.9238795325112869605, 1.000000000000000000, 0.9238795325112869605, 1.000000000000000000, 0.9238795325112869605, 1.000000000000000000, 0.9238795325112869605, 1.000000000000000000, 0.9238795325112869605, 1.000000000000000000, 0.9238795325112869605, 1.000000000000000000, 0.9238795325112869605, 1.000000000000000000, 0.9238795325112869605, 1.000000000000000000, 0.9238795325112869605, 1.000000000000000000, 0.9238795325112869605, 1.000000000000000000, 0.9238795325112869605, 1.000000000000000000, 0.9238795325112869605, 1.000000000000000000, 0.9238795325112869605, 1.000000000000000000, 0.9238795325112869605, 1.000000000000000000, 0.9238795325112869605, 1.000000000000000000, 0.9238795325112869605, 1.000000000000000000, 0.9238795325112869605, 1.000000000000000000, 0.9238795325112869605, 1.000000000000000000, 0.9238795325112869605, 1.000000000000000000, 0.9238795325112869605, 1.000000000000000000, 0.9238795325112869605, 1.000000000000000000, 0.9238795325112869605, 1.000000000000000000, 0.9238795325112869605, 1.000000000000000000, 0.9238795325112869605, 1.000000000000000000, 0.9238795325112869605, 1.000000000000000000, 0.9238795325112869605, 1.000000000000000000, 0.9238795325112869605, 1.000000000000000000, 0.9238795325112869605, 1.000000000000000000, 0.9238795325112869605, 1.000000000000000000, 0.9238795325112869605, 1.000000000000000000, 0.9238795325112869605, 1.000000000000000000, 0.9238795325112869605, 1.000000000000000000, 0.9238795325112869605, 1.000000000000000000, 0.9238795325112869605, 1.000000000000000000, 0.9238795325112869605, 1.000000000000000000, 0.9238795325112869605, 1.000000000000000000, 0.9238795325112869605, 1.000000000000000000, 0.9238795325112869605, 1.000000000000000000, 0.9238795325112869605, 1.000000000000000000, 0.9238795325112869605, 1.000000000000000000, 0.9238795325112869605, 1.000000000000000000, 0.9238795325112869605, 1.000000000000000000, 0.9238795325112869605, 1.000000000000000000, 0.9238795325112869605, 1.000000000000000000, 0.9238795325112869605, 1.000000000000000000, 0.9238795325112869605, 1.000000000000000000, 0.9238795325112869605, 1.000000000000000000, 0.9238795325112869605, 1.000000000000000000, 0.9238795325112869605, 1.000000000000000000, 0.9238795325112869605, 1.000000000000000000, 0.9238795325112869605, 1.000000000000000000, 0.9238795325112869605, 1.000000000000000000, 0.9238795325112869605, 1.000000000000000000, 0.9238795325112869605, 1.000000000000000000, 0.9238795325112869605, 1.000000000000000000, 0.9238795325112869605, 1.000000000000000000, 0.9238795325112869605, 1.000000000000000000, 0.9238795325112869605, 1.000000000000000000, 0.9238795325112869605, 1.000000000000000000, 0.9238795325112869605, 1.000000000000000000, 0.9238795325112869605, 1.000000000000000000, 0.9238795325112869605, 1.000000000000000000, 0.9238795325112869605, 1.000000000000000000, 0.9238795325112869605, 1.000000000000000000, 0.9238795325112869605, 1.000000000000000000, 0.9238795325112869605, 1.000000000000000000, 0.9238795325112869605, 1.000000000000000000, 0.9238795325112869605, 1.000000000000000000, 0.9238795325112869605, 1.000000000000000000, 0.9238795325112869605, 1.000000000000000000, 0.9238795325112869605, 1.000000000000000000, 0.9238795325112869605, 1.000000000000000000, 0.9238795325112869605, 1.000000000000000000, 0.9238795325112869605, 1.000000000000000000, 0.9238795325112869605, 1.000000000000000000, 0.9238795325112869605, 1.000000000000000000, 0.9238795325112869605, 1.000000000000000000, 0.9238795325112869605, 1.000000000000000000, 0.9238795325112869605, 1.000000000000000000, 0.9238795325112869605, 1.000000000000000000, 0.9238795325112869605, 1.000000000000000000, 0.9238795325112869605, 1.000000000000000000, 0.9238795325112869605, 1.000000000000000000, 0.9238795325112869605, 1.000000000000000000, 0.9238795325112869605, 1.000000000000000000, 0.9238795325112869605, 1.000000000000000000, 0.9238795325112869605, 1.000000000000000000, 0.9238795325112869605, 1.000000000000000000, 0.9238795325112869605, 1.000000000000000000, 0.9238795325112869605, 1.000000000000000000, 0.9238795325112869605, 1.000000000000000000, 0.9238795325112869605, 1.000000000000000000, 0.9238795325112869605, 1.000000000000000000, 0.9238795325112869605, 1.000000000000000000, 0.9238795325112869605, 1.000000000000000000, 0.9238795325112869605, 1.000000000000000000, 0.9238795325112869605, 1.000000000000000000, 0.9238795325112869605, 1.000000000000000000, 0.9238795325112869605, 1.000000000000000000, 0.9238795325112869605, 1.000000000000000000, 0.9238795325112869605, 1.000000000000000000, 0.9238795325112869605, 1.000000000000000000, 0.9238795325112869605, 1.000000000000000000, 0.9238795325112869605, 1.000000000000000000, 0.9238795325112869605, 1.000000000000000000, 0.9238795325112869605, 1.000000000000000000, 0.9238795325112869605, 1.000000000000000000, 0.9238795325112869605, 1.000000000000000000, 0.9238795325112869605, 1.000000000000000000, 0.9238795325112869605, 1.000000000000000000, 0.9238795325112869605, 1.000000000000000000, 0.9238795325112869605, 1.000000000000000000, 0.9238795325112869605, 1.000000000000000000, 0.9238795325112869605, 1.000000000000000000, 0.9238795325112869605, 1.000000000000000000, 0.9238795325112869605, 1.000000000000000000, 0.9238795325112869605, 1.000000000000000000, 0.9238795325112869605, 1.000000000000000000, 0.9238795325112869605, 1.000000000000000000, 0.9238795325112869605, 1.000000000000000000, 0.9238795325112869605, 1.000000000000000000, 0.9238795325112869605, 1.000000000000000000, 0.9238795325112869605, 1.000000000000000000, 0.9238795325112869605, 1.000000000000000000, 0.9238795325112869605, 1.000000000000000000, 0.9238795325112869605, 1.000000000000000000, 0.9238795325112869605, 1.000000000000000000, 0.9238795325112869605, 1.000000000000000000, 0.9238795325112869605, 1.000000000000000000, 0.9238795325112869605, 1.000000000000000000, 0.9238795325112869605, 1.000000000000000000, 0.9238795325112869605, 1.000000000000000000, 0.9238795325112869605, 1.000000000000000000, 0.9238795325112869605, 1.000000000000000000, 0.9238795325112869605, 1.000000000000000000, 0.9238795325112869605, 1.000000000000000000, 0.9238795325112869605, 1.000000000000000000, 0.9238795325112869605, 1.000000000000000000, 0.9238795325112869605, 1.000000000000000000, 0.9238795325112869605, 1.000000000000000000, 0.9238795325112869605, 1.000000000000000000, 0.9238795325112869605, 1.000000000000000000, 0.9238795325112869605, 1.000000000000000000, 0.9238795325112869605, 1.000000000000000000, 0.9238795325112869605, 1.000000000000000000, 0.9238795325112869605, 1.000000000000000000, 0.9238795325112869605, 1.000000000000000000, 0.9238795325112869605, 1.000000000000000000, 0.9238795325112869605, 1.000000000000000000, 0.9238795325112869605, 1.000000000000000000, 0.9238795325112869605, 1.000000000000000000, 0.9238795325112869605, 1.000000000000000000, 0.9238795325112869605, 1.000000000000000000, 0.9238795325112869605, 1.000000000000000000, 0.9238795325112869605, 1.000000000000000000, 0.9238795325112869605, 1.000000000000000000, 0.9238795325112869605, 1.000000000000000000, 0.9238795325112869605, 1.000000000000000000, 0.9238795325112869605, 1.000000000000000000, 0.9238795325112869605, 1.000000000000000000, 0.9238795325112869605, 1.000000000000000000, 0.9238795325112869605, 1.000000000000000000, 0.9238795325112869605, 1.000000000000000000, 0.9238795325112869605, 1.000000000000000000, 0.9238795325112869605, 1.000000000000000000, 0.9238795325112869605, 1.000000000000000000, 0.9238795325112869605, 1.000000000000000000, 0.9238795325112869605, 1.000000000000000000, 0.9238795325112869605, 1.000000000000000000, 0.9238795325112869605, 1.000000000000000000, 0.9238795325112869605, 1.000000000000000000, 0.9238795325112869605, 1.000000000000000000, 0.9238795325112869605, 1.000000000000000000, 0.9238795325112869605, 1.000000000000000000, 0.9238795325112869605, 1.000000000000000000, 0.9238795325112869605, 1.000000000000000000, 0.9238795325112869605, 1.000000000000000000, 0.9238795325112869605, 1.000000000000000000, 0.9238795325112869605, 1.000000000000000000, 0.9238795325112869605, 1.000000000000000000, 0.9238795325112869605, 1.000000000000000000, 0.9238795325112869605, 1.000000000000000000, 0.9238795325112869605, 1.000000000000000000, 0.9238795325112869605, 1.000000000000000000, 0.9238795325112869605, 1.000000000000000000, 0.9238795325112869605, 1.000000000000000000, 0.9238795325112869605, 1.000000000000000000, 0.9238795325112869605, 1.000000000000000000, 0.9238795325112869605, 1.000000000000000000, 0.9238795325112869605, 1.000000000000000000, 0.9238795325112869605, 1.000000000000000000, 0.9238795325112869605, 1.000000000000000000, 0.9238795325112869605, 1.000000000000000000, 0.9238795325112869605, 1.000000000000000000, 0.9238795325112869605, 1.000000000000000000, 0.9238795325112869605, 1.000000000000000000, 0.9238795325112869605, 1.000000000000000000, 0.9238795325112869605, 1.000000000000000000, 0.9238795325112869605, 1.000000000000000000, 0.9238795325112869605, 1.000000000000000000, 0.9238795325112869605, 1.000000000000000000, 0.9238795325112869605, 1.000000000000000000, 0.9238795325112869605, 1.000000000000000000, 0.9238795325112869605, 1.000000000000000000, 0.9238795325112869605, 1.000000000000000000, 0.9238795325112869605, 1.000000000000000000, 0.9238795325112869605, 1.000000000000000000, 0.9238795325112869605, 1.000000000000000000, 0.9238795325112869605, 1.000000000000000000, 0.9238795325112869605, 1.000000000000000000, 0.9238795325112869605, 1.000000000000000000, 0.9238795325112869605, 1.000000000000000000, 0.9238795325112869605, 1.000000000000000000, 0.9238795325112869605, 1.000000000000000000, 0.9238795325112869605, 1.000000000000000000, 0.9238795325112869605, 1.000000000000000000, 0.9238795325112869605, 1.000000000000000000, 0.9238795325112869605, 1.000000000000000000, 0.9238795325112869605, 1.000000000000000000, 0.9238795325112869605, 1.000000000000000000, 0.9238795325112869605, 1.000000000000000000, 0.9238795325112869605, 1.000000000000000000, 0.9238795325112869605, 1.000000000000000000, 0.9238795325112869605, 1.000000000000000000, 0.9238795325112869605, 1.000000000000000000, 0.9238795325112869605, 1.000000000000000000, 0.9238795325112869605, 1.000000000000000000, 0.9238795325112869605, 1.000000000000000000, 0.9238795325112869605, 1.000000000000000000, 0.9238795325112869605, 1.000000000000000000, 0.9238795325112869605, 1.000000000000000000, 0.9238795325112869605, 1.000000000000000000, 0.9238795325112869605, 1.000000000000000000, 0.9238795325112869605, 1.000000000000000000, 0.9238795325112869605, 1.000000000000000000, 0.9238795325112869605, 1.000000000000000000, 0.9238795325112869605, 1.000000000000000000, 0.9238795325112869605, 1.000000000000000000, 0.9238795325112869605, 1.000000000000000000, 0.9238795325112869605, 1.000000000000000000, 0.9238795325112869605, 1.000000000000000000, 0.9238795325112869605, 1.000000000000000000, 0.9238795325112869605, 1.000000000000000000, 0.9238795325112869605, 1.000000000000000000, 0.9238795325112869605, 1.000000000000000000, 0.9238795325112869605, 1.000000000000000000, 0.9238795325112869605, 1.000000000000000000, 0.9238795325112869605, 1.000000000000000000, 0.9238795325112869605, 1.000000000000000000, 0.9238795325112869605, 1.000000000000000000, 0.9238795325112869605, 1.000000000000000000, 0.9238795325112869605, 1.000000000000000000, 0.9238795325112869605, 1.000000000000000000, 0.9238795325112869605, 1.000000000000000000, 0.9238795325112869605, 1.000000000000000000, 0.9238795325112869605, 1.000000000000000000, 0.9238795325112869605, 1.000000000000000000, 0.9238795325112869605, 1.000000000000000000, 0.9238795325112869605, 1.000000000000000000, 0.9238795325112869605, 1.000000000000000000, 0.9238795325112869605, 1.000000000000000000, 0.9238795325112869605, 1.000000000000000000, 0.9238795325112869605, 1.000000000000000000, 0.9238795325112869605, 1.000000000000000000, 0.9238795325112869605, 1.000000000000000000, 0.9238795325112869605, 1.000000000000000000, 0.9238795325112869605, 1.000000000000000000, 0.9238795325112869605, 1.000000000000000000, 0.9238795325112869605, 1.000000000000000000, 0.9238795325112869605, 1.000000000000000000, 0.9238795325112869605, 1.000000000000000000, 0.9238795325112869605, 1.000000000000000000, 0.9238795325112869605, 1.000000000000000000, 0.9238795325112869605, 1.000000000000000000, 0.9238795325112869605, 1.000000000000000000, 0.9238795325112869605, 1.000000000000000000, 0.9238795325112869605, 1.000000000000000000, 0.9238795325112869605, 1.000000000000000000, 0.9238795325112869605, 1.000000000000000000, 0.9238795325112869605, 1.000000000000000000, 0.9238795325112869605, 1.000000000000000000, 0.9238795325112869605, 1.000000000000000000, 0.9238795325112869605, 1.000000000000000000, 0.9238795325112869605, 1.000000000000000000, 0.9238795325112869605, 1.000000000000000000, 0.9238795325112869605, 1.000000000000000000, 0.9238795325112869605, 1.000000000000000000, 0.9238795325112869605, 1.000000000000000000, 0.9238795325112869605, 1.000000000000000000, 0.9238795325112869605, 1.000000000000000000, 0.9238795325112869605, 1.000000000000000000, 0.9238795325112869605, 1.000000000000000000, 0.9238795325112869605, 1.000000000000000000, 0.9238795325112869605, 1.000000000000000000, 0.9238795325112869605, 1.000000000000000000, 0.9238795325112869605, 1.000000000000000000, 0.9238795325112869605, 1.000000000000000000, 0.9238795325112869605, 1.000000000000000000, 0.9238795325112869605, 1.000000000000000000, 0.9238795325112869605, 1.000000000000000000, 0.9238795325112869605, 1.000000000000000000, 0.9238795325112869605, 1.000000000000000000, 0.9238795325112869605, 1.000000000000000000, 0.9238795325112869605, 1.000000000000000000, 0.9238795325112869605, 1.000000000000000000, 0.9238795325112869605, 1.000000000000000000, 0.9238795325112869605, 1.000000000000000000, 0.9238795325112869605, 1.000000000000000000, 0.9238795325112869605, 1.000000000000000000, 0.9238795325112869605, 1.000000000000000000, 0.9238795325112869605, 1.000000000000000000, 0.9238795325112869605, 1.000000000000000000, 0.9238795325112869605, 1.000000000000000000, 0.9238795325112869605, 1.000000000000000000, 0.9238795325112869605, 1.000000000000000000, 0.9238795325112869605, 1.000000000000000000, 0.9238795325112869605, 1.000000000000000000, 0.9238795325112869605, 1.000000000000000000, 0.9238795325112869605, 1.000000000000000000, 0.9238795325112869605, 1.000000000000000000, 0.9238795325112869605, 1.000000000000000000, 0.9238795325112869605, 1.000000000000000000, 0.9238795325112869605, 1.000000000000000000, 0.9238795325112869605, 1.000000000000000000, 0.9238795325112869605, 1.000000000000000000, 0.9238795325112869605, 1.000000000000000000, 0.9238795325112869605, 1.000000000000000000, 0.9238795325112869605, 1.000000000000000000, 0.9238795325112869605, 1.000000000000000000, 0.9238795325112869605, 1.000000000000000000, 0.9238795325112869605, 1.000000000000000000, 0.9238795325112869605, 1.000000000000000000, 0.9238795325112869605, 1.000000000000000000, 0.9238795325112869605, 1.000000000000000000, 0.9238795325112869605, 1.000000000000000000, 0.9238795325112869605, 1.000000000000000000, 0.9238795325112869605, 1.000000000000000000, 0.9238795325112869605, 1.000000000000000000, 0.9238795325112869605, 1.000000000000000000, 0.9238795325112869605, 1.000000000000000000, 0.9238795325112869605, 1.000000000000000000, 0.9238795325112869605, 1.000000000000000000, 0.9238795325112869605, 1.000000000000000000, 0.9238795325112869605, 1.000000000000000000, 0.9238795325112869605, 1.000000000000000000, 0.9238795325112869605, 1.000000000000000000, 0.9238795325112869605, 1.000000000000000000, 0.9238795325112869605, 1.000000000000000000, 0.9238795325112869605, 1.000000000000000000, 0.9238795325112869605, 1.000000000000000000, 0.9238795325112869605, 1.000000000000000000, 0.9238795325112869605, 1.000000000000000000, 0.9238795325112869605, 1.000000000000000000, 0.9238795325112869605, 1.000000000000000000, 0.9238795325112869605, 1.000000000000000000, 0.9238795325112869605, 1.000000000000000000, 0.9238795325112869605, 1.000000000000000000, 0.9238795325112869605, 1.000000000000000000, 0.9238795325112869605, 1.000000000000000000, 0.9238795325112869605, 1.000000000000000000, 0.9238795325112869605, 1.000000000000000000, 0.9238795325112869605, 1.000000000000000000, 0.9238795325112869605, 1.000000000000000000, 0.9238795325112869605, 1.000000000000000000, 0.9238795325112869605, 1.000000000000000000, 0.9238795325112869605, 1.000000000000000000, 0.9238795325112869605, 1.000000000000000000, 0.9238795325112869605, 1.000000000000000000, 0.9238795325112869605, 1.000000000000000000, 0.9238795325112869605, 1.000000000000000000, 0.9238795325112869605, 1.000000000000000000, 0.9238795325112869605, 1.000000000000000000, 0.9238795325112869605, 1.000000000000000000, 0.9238795325112869605, 1.000000000000000000, 0.9238795325112869605, 1.000000000000000000, 0.9238795325112869605, 1.000000000000000000, 0.9238795325112869605, 1.000000000000000000, 0.9238795325112869605, 1.000000000000000000, 0.9238795325112869605, 1.000000000000000000, 0.9238795325112869605, 1.000000000000000000, 0.9238795325112869605, 1.000000000000000000, 0.9238795325112869605, 1.000000000000000000, 0.9238795325112869605, 1.000000000000000000, 0.9238795325112869605, 1.000000000000000000, 0.9238795325112869605, 1.000000000000000000, 0.9238795325112869605, 1.000000000000000000, 0.9238795325112869605, 1.000000000000000000, 0.9238795325112869605, 1.000000000000000000, 0.9238795325112869605, 1.000000000000000000, 0.9238795325112869605, 1.000000000000000000, 0.9238795325112869605, 1.000000000000000000) ) ) 
 REPRESENTATION_ITEM ( '' )  SURFACE ( )  ) ;
#23327=CARTESIAN_POINT ( 'NONE',  ( 1.054774247047244540, -0.07405724077823318263, 1.633858267662771313 ) ) ;
#23332=DIRECTION ( 'NONE',  ( 0.000000000000000000, 0.000000000000000000, -1.000000000000000000 ) ) ;
#23333=CARTESIAN_POINT ( 'NONE',  ( -0.9500414927467377701, -0.1787899950787401604, 0.6496062991588353874 ) ) ;
#23335=CARTESIAN_POINT ( 'NONE',  ( -0.8759842519685039353, -0.1574803149606299191, 1.289370078632629868 ) ) ;
#23342=CARTESIAN_POINT ( 'NONE',  ( 0.6971942568897648851, -0.07405724077823297447, 1.466535433017102763 ) ) ;
#23343=CARTESIAN_POINT ( 'NONE',  ( 0.6971942568897648851, -0.07405724077823297447, 1.776574803095843702 ) ) ;
#23350=( BOUNDED_CURVE ( )  B_SPLINE_CURVE ( 2, ( #37908, #19682, #8902, #26898, #37666, #34096, #31204, #23534, #1224 ),
 .UNSPECIFIED., .F., .F. ) 
 B_SPLINE_CURVE_WITH_KNOTS ( ( 3, 2, 2, 2, 3 ),
 ( 0.6600000000000000311, 0.6624999999999999778, 0.6650000000000000355, 0.6674999999999999822, 0.6700000000000000400 ),
 .UNSPECIFIED. ) 
 CURVE ( )  GEOMETRIC_REPRESENTATION_ITEM ( )  RATIONAL_B_SPLINE_CURVE ( ( 1.000000000000000000, 0.9238795325112869605, 1.000000000000000000, 0.9238795325112869605, 1.000000000000000000, 0.9238795325112869605, 1.000000000000000000, 0.9238795325112869605, 1.000000000000000000 ) ) 
 REPRESENTATION_ITEM ( '' )  ) ;
#23351=CARTESIAN_POINT ( 'NONE',  ( 0.6971942568897626646, -0.07405724077823297447, 0.5167322834108034613 ) ) ;
#23352=CARTESIAN_POINT ( 'NONE',  ( -1.033464566929133799, 0.000000000000000000, 0.7578740157480314821 ) ) ;
#23354=CARTESIAN_POINT ( 'NONE',  ( 0.7185039370078739607, 1.928577636452523993E-17, 0.8562992125984251190 ) ) ;
#23356=CARTESIAN_POINT ( 'NONE',  ( 1.033464566929134687, 0.06523048226347956391, 0.7504921258767240921 ) ) ;
#23359=ORIENTED_EDGE ( 'NONE', *, *, #12733, .F. ) ;
#23362=CARTESIAN_POINT ( 'NONE',  ( -0.9873396505805591694, -0.1113553986120547346, 0.6249999998924724576 ) ) ;
#23364=CARTESIAN_POINT ( 'NONE',  ( 1.054774247047244096, 0.000000000000000000, 1.675688976324189117 ) ) ;
#23365=CARTESIAN_POINT ( 'NONE',  ( -1.033464566929134687, 0.06523048226347956391, 1.193405511811024278 ) ) ;
#23366=CARTESIAN_POINT ( 'NONE',  ( -0.8107537697050254399, -0.1574803149606297803, 1.050688976270426567 ) ) ;
#23370=CARTESIAN_POINT ( 'NONE',  ( 0.7646288533564489232, -0.1113553986120547346, 1.402559055010582645 ) ) ;
#23374=ORIENTED_EDGE ( 'NONE', *, *, #40028, .T. ) ;
#23375=CARTESIAN_POINT ( 'NONE',  ( 1.054774247047244096, 0.000000000000000000, 0.9325787401037164415 ) ) ;
#23376=CARTESIAN_POINT ( 'NONE',  ( -0.9500414927467377701, -0.1787899950787401604, 1.510826771599780294 ) ) ;
#23378=CARTESIAN_POINT ( 'NONE',  ( -0.6971942568897637749, 2.189545951927499583E-17, 1.227854330654897685 ) ) ;
#23382=CARTESIAN_POINT ( 'NONE',  ( -0.8759842519685039353, -0.1787899950787401882, 0.2928149605761578567 ) ) ;
#23388=AXIS2_PLACEMENT_3D ( 'NONE', #14822, #4720, #33523 ) ;
#23390=EDGE_CURVE ( 'NONE', #37016, #47083, #31609, .T. ) ;
#23391=LINE ( 'NONE', #26519, #13891 ) ;
#23394=CARTESIAN_POINT ( 'NONE',  ( -0.9500414927467377701, 0.1787899950787401604, 0.2706692912848194243 ) ) ;
#23395=CARTESIAN_POINT ( 'NONE',  ( -0.9412147342319837628, 0.1574803149606300301, 1.001476377952755348 ) ) ;
#23398=CARTESIAN_POINT ( 'NONE',  ( 0.7185039370078746268, 0.06523048226347956391, 0.4207677165354331561 ) ) ;
#23399=CARTESIAN_POINT ( 'NONE',  ( 0.8759842519685039353, 0.1787899950787401882, 0.9424212597887559051 ) ) ;
#23400=CARTESIAN_POINT ( 'NONE',  ( 0.8759842519685039353, -0.1787899950787401882, 0.1304133857730082613 ) ) ;
#23403=CARTESIAN_POINT ( 'NONE',  ( 0.8107537697050253289, -0.1574803149606297803, 1.611712598425196319 ) ) ;
#23404=CARTESIAN_POINT ( 'NONE',  ( 0.7127101691150015128, -0.03581842120577477528, 1.983932702903218770 ) ) ;
#23408=CARTESIAN_POINT ( 'NONE',  ( 0.7185039370078739607, 1.928577636452523993E-17, 0.7775590551181102983 ) ) ;
#23409=CARTESIAN_POINT ( 'NONE',  ( 1.002407869896990045, 0.1264236179284866091, 0.9325787401037164415 ) ) ;
#23410=CARTESIAN_POINT ( 'NONE',  ( 0.7495606340400177148, 0.1264236179284866091, 1.892224409395055096 ) ) ;
#23411=CARTESIAN_POINT ( 'NONE',  ( 0.9873396505805591694, 0.1113553986120547346, 0.3198818896562523606 ) ) ;
#23416=CARTESIAN_POINT ( 'NONE',  ( -0.5314960629921260393, 0.000000000000000000, 4.685039370078739829 ) ) ;
#23418=CARTESIAN_POINT ( 'NONE',  ( -0.9412147342319837628, 0.1574803149606300301, 0.2042322833570398011 ) ) ;
#23419=CARTESIAN_POINT ( 'NONE',  ( 0.7495606340400177148, -0.1264236179284866091, 1.149114173174582643 ) ) ;
#23420=EDGE_LOOP ( 'NONE', ( #36238, #3363, #37693, #25665 ) ) ;
#23423=CARTESIAN_POINT ( 'NONE',  ( -0.7185039370078739607, 1.928577636452523993E-17, 1.043307086506645831 ) ) ;
#23425=CARTESIAN_POINT ( 'NONE',  ( -1.002407869896990045, -0.1264236179284866091, 0.2140748030958428971 ) ) ;
#23428=CARTESIAN_POINT ( 'NONE',  ( -0.6971942568897648851, -0.07405724077823297447, 1.815944881835999558 ) ) ;
#23429=CARTESIAN_POINT ( 'NONE',  ( -0.8019270111902717657, 0.1787899950787401604, 0.5118110235682844511 ) ) ;
#23434=CARTESIAN_POINT ( 'NONE',  ( -1.033464566929133799, 0.000000000000000000, 1.889763779420031486 ) ) ;
#23439=CARTESIAN_POINT ( 'NONE',  ( -1.054774247047244540, 0.07405724077823318263, 0.4970472440407249226 ) ) ;
#23441=EDGE_CURVE ( 'NONE', #33816, #47229, #39119, .T. ) ;
#23445=CARTESIAN_POINT ( 'NONE',  ( -1.002407869896990045, 0.1264236179284866091, 1.567421259788755794 ) ) ;
#23453=CARTESIAN_POINT ( 'NONE',  ( 0.7185039370078746268, -0.06523048226347956391, 0.5044291338582675976 ) ) ;
#23455=CARTESIAN_POINT ( 'NONE',  ( -0.9873396505805591694, 0.1113553986120547346, 1.225393700679874076 ) ) ;
#23456=CARTESIAN_POINT ( 'NONE',  ( 1.054774247047244540, 0.07405724077823318263, 0.5019685038832442103 ) ) ;
#23457=CARTESIAN_POINT ( 'NONE',  ( 1.054774247047244096, 0.000000000000000000, 0.1008858267178899676 ) ) ;
#23459=CARTESIAN_POINT ( 'NONE',  ( 0.7185039370078739607, 1.928577636452523993E-17, 0.3444881889763780070 ) ) ;
#23461=EDGE_LOOP ( 'NONE', ( #14185, #30068, #46458, #9397 ) ) ;
#23462=CARTESIAN_POINT ( 'NONE',  ( 0.8759842519685039353, 0.1574803149606299191, 1.584645669183810890 ) ) ;
#23463=CARTESIAN_POINT ( 'NONE',  ( -1.054774247047244096, 0.000000000000000000, 1.090059055064346527 ) ) ;
#23464=CARTESIAN_POINT ( 'NONE',  ( 0.8759842519685039353, -0.1574803149606299191, 1.102362204724409489 ) ) ;
#23470=CARTESIAN_POINT ( 'NONE',  ( -0.9412147342319837628, -0.1574803149606297803, 1.262303149606299746 ) ) ;
#23476=CARTESIAN_POINT ( 'NONE',  ( 0.8759842519685039353, -0.1787899950787401882, 0.6815944881352126172 ) ) ;
#23477=CARTESIAN_POINT ( 'NONE',  ( -0.8107537697050253289, 0.1574803149606300301, 1.124507874015748810 ) ) ;
#23480=CARTESIAN_POINT ( 'NONE',  ( 0.8107537697050254399, -0.1574803149606297803, 0.9030511811023625990 ) ) ;
#23484=CARTESIAN_POINT ( 'NONE',  ( 0.7646288533564489232, -0.1113553986120547346, 1.166338582569637961 ) ) ;
#23486=ORIENTED_EDGE ( 'NONE', *, *, #30541, .T. ) ;
#23488=CARTESIAN_POINT ( 'NONE',  ( -1.054774247047244096, 0.000000000000000000, 1.798720472387181024 ) ) ;
#23489=CARTESIAN_POINT ( 'NONE',  ( 1.054774247047244096, 0.000000000000000000, 1.798720472387181024 ) ) ;
#23490=EDGE_LOOP ( 'NONE', ( #6473, #11497, #25083, #31730 ) ) ;
#23491=CARTESIAN_POINT ( 'NONE',  ( 1.033464566929134687, -0.06523048226347956391, 1.779035433070867311 ) ) ;
#23492=CARTESIAN_POINT ( 'NONE',  ( 1.054774247047244540, -0.07405724077823318263, 0.4183070865604097133 ) ) ;
#23493=CARTESIAN_POINT ( 'NONE',  ( -0.8019270111902717657, 0.1787899950787401604, 1.333661417269071059 ) ) ;
#23495=CARTESIAN_POINT ( 'NONE',  ( -0.6971942568897626646, 0.07405724077823318263, 0.1230314960092287191 ) ) ;
#23496=CARTESIAN_POINT ( 'NONE',  ( -1.033464566929133799, 1.928577636452524610E-17, 2.869337061179095023E-17 ) ) ;
#23497=CARTESIAN_POINT ( 'NONE',  ( -1.054774247047244540, -0.07405724077823318263, 1.717519684985606476 ) ) ;
#23498=CARTESIAN_POINT ( 'NONE',  ( -0.9500414927467378812, 0.1787899950787401604, 0.03444881884387430981 ) ) ;
#23499=CARTESIAN_POINT ( 'NONE',  ( -0.7185039370078746268, 0.06523048226347956391, 1.680610236220472231 ) ) ;
#23501=LINE ( 'NONE', #30471, #12135 ) ;
#23502=CARTESIAN_POINT ( 'NONE',  ( 0.7495606340400177148, -0.1264236179284866091, 1.665846456639149764 ) ) ;
#23504=CARTESIAN_POINT ( 'NONE',  ( 1.033464566929133799, 1.928577636452524610E-17, 4.498031496062992574 ) ) ;
#23505=CARTESIAN_POINT ( 'NONE',  ( 0.8759842519685039353, 0.1574803149606299191, 0.2854330707586145710 ) ) ;
#23509=( BOUNDED_CURVE ( )  B_SPLINE_CURVE ( 2, ( #26007, #571, #44417, #15228, #26254, #36787, #40817, #101, #29650 ),
 .UNSPECIFIED., .F., .T. ) 
 B_SPLINE_CURVE_WITH_KNOTS ( ( 3, 2, 2, 2, 3 ),
 ( 0.1300000000000000044, 0.1325000000000000067, 0.1350000000000000089, 0.1375000000000000111, 0.1400000000000000133 ),
 .UNSPECIFIED. ) 
 CURVE ( )  GEOMETRIC_REPRESENTATION_ITEM ( )  RATIONAL_B_SPLINE_CURVE ( ( 1.000000000000000000, 0.9238795325112869605, 1.000000000000000000, 0.9238795325112869605, 1.000000000000000000, 0.9238795325112869605, 1.000000000000000000, 0.9238795325112869605, 1.000000000000000000 ) ) 
 REPRESENTATION_ITEM ( '' )  ) ;
#23511=EDGE_CURVE ( 'NONE', #47093, #27914, #24439, .T. ) ;
#23515=CARTESIAN_POINT ( 'NONE',  ( 1.002407869896990045, -0.1264236179284866091, 1.828248031442299082 ) ) ;
#23516=CARTESIAN_POINT ( 'NONE',  ( 0.7495606340400177148, -0.1264236179284866091, 0.4010826771115905687 ) ) ;
#23518=CARTESIAN_POINT ( 'NONE',  ( -0.7646288533564489232, 0.1113553986120547346, 0.8021653542231811373 ) ) ;
#23520=CARTESIAN_POINT ( 'NONE',  ( 1.054774247047244540, -0.07405724077823318263, 0.8858267715997791836 ) ) ;
#23523=CARTESIAN_POINT ( 'NONE',  ( 1.054774247047244540, -0.07405724077823318263, 1.953740157426552715 ) ) ;
#23524=CARTESIAN_POINT ( 'NONE',  ( 0.7646288533564489232, 0.1113553986120547346, 0.2214566929133858220 ) ) ;
#23525=FACE_OUTER_BOUND ( 'NONE', #45422, .T. ) ;
#23527=CARTESIAN_POINT ( 'NONE',  ( 0.9873396505805591694, -0.1113553986120547346, 0.1230314960629921295 ) ) ;
#23531=CARTESIAN_POINT ( 'NONE',  ( -0.8759842519685039353, 0.1787899950787401882, 1.764271653489543290 ) ) ;
#23533=CARTESIAN_POINT ( 'NONE',  ( -0.6971942568897637749, 2.189545951927499583E-17, 1.306594488135212728 ) ) ;
#23534=CARTESIAN_POINT ( 'NONE',  ( -0.7185039370078746268, 0.06523048226347956391, 1.326279527559055982 ) ) ;
#23535=CARTESIAN_POINT ( 'NONE',  ( 0.9500414927467378812, 0.1787899950787401604, 1.451771653489543290 ) ) ;
#23536=CARTESIAN_POINT ( 'NONE',  ( -0.8759842519685039353, 0.1787899950787401882, 1.173720472387181246 ) ) ;
#23537=CARTESIAN_POINT ( 'NONE',  ( 0.8107537697050254399, 0.1574803149606300301, 1.547736220364914983 ) ) ;
#23539=CARTESIAN_POINT ( 'NONE',  ( -1.033464566929133799, 1.928577636452524610E-17, 2.869337061179095023E-17 ) ) ;
#23540=CARTESIAN_POINT ( 'NONE',  ( 0.8019270111902716547, -0.1787899950787401604, 0.6053149605761580787 ) ) ;
#23541=CARTESIAN_POINT ( 'NONE',  ( -1.054774247047244540, -0.07405724077823318263, 0.4527559054580477249 ) ) ;
#23545=CARTESIAN_POINT ( 'NONE',  ( -1.033464566929133799, 0.000000000000000000, 0.2460629921259842590 ) ) ;
#23548=VERTEX_POINT ( 'NONE', #33441 ) ;
#23550=CARTESIAN_POINT ( 'NONE',  ( -0.7185039370078692977, 0.06523048226347515077, 1.473917322727118506 ) ) ;
#23552=CARTESIAN_POINT ( 'NONE',  ( 0.8759842519685039353, 0.000000000000000000, 4.498031496062992574 ) ) ;
#23555=CARTESIAN_POINT ( 'NONE',  ( 0.6971942568897637749, 2.189545951927499583E-17, 1.341043307032850462 ) ) ;
#23561=CARTESIAN_POINT ( 'NONE',  ( 0.9500414927467378812, -0.1787899950787401604, 1.550196850339937926 ) ) ;
#23564=CARTESIAN_POINT ( 'NONE',  ( -1.054774247047244096, 0.000000000000000000, 0.6963582676627716461 ) ) ;
#23566=DIRECTION ( 'NONE',  ( -1.000000000000000000, 0.000000000000000000, 6.938893903907228378E-15 ) ) ;
#23571=CARTESIAN_POINT ( 'NONE',  ( 0.8019270111902717657, -0.1787899950787401604, 1.589566929080094448 ) ) ;
#23572=CARTESIAN_POINT ( 'NONE',  ( 0.9500414927467377701, -0.1787899950787401604, 1.825787401521040243 ) ) ;
#23573=ORIENTED_EDGE ( 'NONE', *, *, #40182, .F. ) ;
#23578=CARTESIAN_POINT ( 'NONE',  ( 0.8019270111902717657, -0.1787899950787401604, 0.5216535432533228045 ) ) ;
#23579=CARTESIAN_POINT ( 'NONE',  ( 0.7646288533564489232, -0.1113553986120547346, 0.07381889763779526936 ) ) ;
#23581=CARTESIAN_POINT ( 'NONE',  ( 1.033464566929133799, 0.000000000000000000, 0.8366141732283465249 ) ) ;
#23582=CARTESIAN_POINT ( 'NONE',  ( -1.002407869896990045, 0.1264236179284866091, 1.365649606245448844 ) ) ;
#23583=CARTESIAN_POINT ( 'NONE',  ( 1.033464566929134687, -0.06523048226347956391, 0.7455708660342049710 ) ) ;
#23585=CARTESIAN_POINT ( 'NONE',  ( 1.054774247047244540, -0.07405724077823318263, 0.9694881889226144578 ) ) ;
#23587=CARTESIAN_POINT ( 'NONE',  ( -0.8107537697050253289, 0.1574803149606300301, 0.6028543306011346914 ) ) ;
#23589=CARTESIAN_POINT ( 'NONE',  ( 0.6971942568897648851, 0.07405724077823318263, 1.732283464513166615 ) ) ;
#23590=CARTESIAN_POINT ( 'NONE',  ( -0.8107537697050253289, -0.1574803149606297803, 1.257381889763780736 ) ) ;
#23591=CARTESIAN_POINT ( 'NONE',  ( 0.7185039370078746268, 0.06523048226347956391, 0.2534448817822371192 ) ) ;
#23592=CARTESIAN_POINT ( 'NONE',  ( 0.7185039370078746268, 0.06523048226347956391, 1.956200787401576102 ) ) ;
#23593=CARTESIAN_POINT ( 'NONE',  ( 0.8759842491179902213, 0.1574803149606299191, 1.978346456692913646 ) ) ;
#23594=CARTESIAN_POINT ( 'NONE',  ( 0.7185039370078746268, 0.06523048226347956391, 1.473917322727117840 ) ) ;
#23595=ORIENTED_EDGE ( 'NONE', *, *, #2499, .F. ) ;
#23596=ORIENTED_EDGE ( 'NONE', *, *, #9928, .F. ) ;
#23600=CARTESIAN_POINT ( 'NONE',  ( 0.7495606340400177148, -0.1264236179284866091, 0.9571850393163149340 ) ) ;
#23601=CARTESIAN_POINT ( 'NONE',  ( -0.8759842519685039353, 0.1787899950787401882, 1.606791338528913426 ) ) ;
#23603=CARTESIAN_POINT ( 'NONE',  ( -0.9500414927467378812, 0.1787899950787401604, 1.412401574749386990 ) ) ;
#23604=( BOUNDED_CURVE ( )  B_SPLINE_CURVE ( 2, ( #41098, #8292, #19559, #10200, #9497, #5891, #2283, #34668, #42745 ),
 .UNSPECIFIED., .F., .T. ) 
 B_SPLINE_CURVE_WITH_KNOTS ( ( 3, 2, 2, 2, 3 ),
 ( 0.7800000000000000266, 0.7824999999999999734, 0.7850000000000000311, 0.7874999999999999778, 0.7900000000000000355 ),
 .UNSPECIFIED. ) 
 CURVE ( )  GEOMETRIC_REPRESENTATION_ITEM ( )  RATIONAL_B_SPLINE_CURVE ( ( 1.000000000000000000, 0.9238795325112869605, 1.000000000000000000, 0.9238795325112869605, 1.000000000000000000, 0.9238795325112869605, 1.000000000000000000, 0.9238795325112869605, 1.000000000000000000 ) ) 
 REPRESENTATION_ITEM ( '' )  ) ;
#23605=EDGE_CURVE ( 'NONE', #26131, #31988, #40637, .T. ) ;
#23607=CYLINDRICAL_SURFACE ( 'NONE', #12689, 0.1574803149606299191 ) ;
#23610=VERTEX_POINT ( 'NONE', #26480 ) ;
#23612=ORIENTED_EDGE ( 'NONE', *, *, #36465, .F. ) ;
#23613=ORIENTED_EDGE ( 'NONE', *, *, #10180, .T. ) ;
#23616=CARTESIAN_POINT ( 'NONE',  ( 1.033464566929134687, -0.06523048226347956391, 0.1156496061916856694 ) ) ;
#23617=EDGE_CURVE ( 'NONE', #16359, #16139, #22905, .T. ) ;
#23618=VECTOR ( 'NONE', #16221, 39.37007874015748143 ) ;
#23619=CARTESIAN_POINT ( 'NONE',  ( 0.7185039370078739607, 1.928577636452523993E-17, 1.879921259842519676 ) ) ;
#23621=AXIS2_PLACEMENT_3D ( 'NONE', #5266, #8623, #34514 ) ;
#23622=( BOUNDED_CURVE ( )  B_SPLINE_CURVE ( 2, ( #33505, #30619, #617, #44472, #8298, #22690, #30163, #11924, #22927 ),
 .UNSPECIFIED., .F., .T. ) 
 B_SPLINE_CURVE_WITH_KNOTS ( ( 3, 2, 2, 2, 3 ),
 ( 0.1900000000000000022, 0.1925000000000000044, 0.1950000000000000067, 0.1975000000000000089, 0.2000000000000000111 ),
 .UNSPECIFIED. ) 
 CURVE ( )  GEOMETRIC_REPRESENTATION_ITEM ( )  RATIONAL_B_SPLINE_CURVE ( ( 1.000000000000000000, 0.9238795325112869605, 1.000000000000000000, 0.9238795325112869605, 1.000000000000000000, 0.9238795325112869605, 1.000000000000000000, 0.9238795325112879597, 1.000000000000000000 ) ) 
 REPRESENTATION_ITEM ( '' )  ) ;
#23623=CARTESIAN_POINT ( 'NONE',  ( -0.6971942568897637749, 2.189545951927499583E-17, 0.2042322834108035723 ) ) ;
#23624=CARTESIAN_POINT ( 'NONE',  ( -0.9412147342319837628, -0.1574803149606297803, 1.104822834645670104 ) ) ;
#23626=CARTESIAN_POINT ( 'NONE',  ( 1.054774247047244540, -0.07405724077823318263, 1.048228346402930944 ) ) ;
#23627=CARTESIAN_POINT ( 'NONE',  ( 0.9500414927467377701, 0.1787899950787401604, 1.446850393647023836 ) ) ;
#23628=CARTESIAN_POINT ( 'NONE',  ( 0.6971942568897626646, -0.07405724077823297447, 0.1230314960092287191 ) ) ;
#23630=CARTESIAN_POINT ( 'NONE',  ( 0.7185039370078746268, -0.06523048226347956391, 1.488681102362205300 ) ) ;
#23631=CARTESIAN_POINT ( 'NONE',  ( 0.7830934527162080050, 0.1313591056386028688, 1.980287732290521019 ) ) ;
#23635=CARTESIAN_POINT ( 'NONE',  ( 0.8019270111902716547, 0.1787899950787401604, 0.9793307086076531442 ) ) ;
#23636=CARTESIAN_POINT ( 'NONE',  ( 1.002407869896990045, -0.1264236179284866091, 1.754429133804503715 ) ) ;
#23637=CARTESIAN_POINT ( 'NONE',  ( 0.8107537697050253289, 0.1574803149606300301, 0.3666338581601894520 ) ) ;
#23639=LINE ( 'NONE', #27743, #21479 ) ;
#23641=CARTESIAN_POINT ( 'NONE',  ( -0.9412147342319837628, 0.1574803149606300301, 0.2436023620971974057 ) ) ;
#23642=CARTESIAN_POINT ( 'NONE',  ( 0.8759842519685039353, 0.000000000000000000, 4.498031496062992574 ) ) ;
#23643=CARTESIAN_POINT ( 'NONE',  ( 0.6971942568897637749, 2.189545951927499583E-17, 1.222933070812378009 ) ) ;
#23648=LINE ( 'NONE', #20043, #26810 ) ;
#23650=CARTESIAN_POINT ( 'NONE',  ( -0.6971942568897637749, 2.189545951927499583E-17, 0.5536417322297008115 ) ) ;
#23651=CARTESIAN_POINT ( 'NONE',  ( -0.9412147342319837628, -0.1574803149606297803, 0.2780511811023620439 ) ) ;
#23656=CARTESIAN_POINT ( 'NONE',  ( -1.054774247047244096, 0.000000000000000000, 1.050688976324189117 ) ) ;
#23657=CARTESIAN_POINT ( 'NONE',  ( -1.054774247047244096, 0.000000000000000000, 1.793799212544661348 ) ) ;
#23658=CARTESIAN_POINT ( 'NONE',  ( -0.7495606340400177148, 0.1264236179284866091, 0.9817913385289134265 ) ) ;
#23660=CARTESIAN_POINT ( 'NONE',  ( -0.7495606340400177148, -0.1264236179284866091, 0.7209645668753701386 ) ) ;
#23661=VERTEX_POINT ( 'NONE', #7305 ) ;
#23668=CARTESIAN_POINT ( 'NONE',  ( 0.7185039370078739607, 1.928577636452523993E-17, 1.801181102362204633 ) ) ;
#23671=CARTESIAN_POINT ( 'NONE',  ( -0.9500414927467378812, -0.1787899950787401604, 0.4478346456155276045 ) ) ;
#23672=LINE ( 'NONE', #11956, #21860 ) ;
#23673=ORIENTED_EDGE ( 'NONE', *, *, #35571, .F. ) ;
#23675=CARTESIAN_POINT ( 'NONE',  ( -0.8759842519685039353, 0.1787899950787401882, 1.532972440891118060 ) ) ;
#23680=CARTESIAN_POINT ( 'NONE',  ( 1.033464566929134687, -0.06523048226347956391, 0.9522637795275589179 ) ) ;
#23681=CARTESIAN_POINT ( 'NONE',  ( -0.8107537697050253289, -0.1574803149606297803, 1.168799212490898354 ) ) ;
#23682=CARTESIAN_POINT ( 'NONE',  ( 0.6971942568897626646, 0.07405724077823318263, 0.07874015742655143812 ) ) ;
#23684=CARTESIAN_POINT ( 'NONE',  ( -0.8759842519685039353, 0.1574803149606299191, 1.624015747923968522 ) ) ;
#23686=ORIENTED_EDGE ( 'NONE', *, *, #2215, .F. ) ;
#23688=CARTESIAN_POINT ( 'NONE',  ( -0.6971942568897637749, 2.189545951927499583E-17, 1.149114173174582643 ) ) ;
#23689=CARTESIAN_POINT ( 'NONE',  ( 0.7185039370078746268, 0.06523048226347956391, 1.129429133858268042 ) ) ;
#23691=AXIS2_PLACEMENT_3D ( 'NONE', #33718, #1070, #12609 ) ;
#23692=DIRECTION ( 'NONE',  ( 1.822029033848725028E-16, 0.000000000000000000, 1.000000000000000000 ) ) ;
#23699=CARTESIAN_POINT ( 'NONE',  ( 0.8759842519685039353, -0.1574803149606299191, 0.2755905511811023723 ) ) ;
#23700=CARTESIAN_POINT ( 'NONE',  ( 0.6971942568897626646, -0.07405724077823297447, 0.8316929133320636325 ) ) ;
#23701=EDGE_CURVE ( 'NONE', #41516, #16491, #14737, .T. ) ;
#23703=CARTESIAN_POINT ( 'NONE',  ( 0.8107537697050254399, -0.1574803149606297803, 1.454232283464566677 ) ) ;
#23704=CARTESIAN_POINT ( 'NONE',  ( 0.7185039370078739607, 1.928577636452523993E-17, 0.8956692913385826404 ) ) ;
#23708=CARTESIAN_POINT ( 'NONE',  ( 0.8759842519685039353, 0.1574803149606299191, 1.269685039262551163 ) ) ;
#23711=ORIENTED_EDGE ( 'NONE', *, *, #44860, .T. ) ;
#23712=VERTEX_POINT ( 'NONE', #11623 ) ;
#23713=CARTESIAN_POINT ( 'NONE',  ( -1.054774247047244096, 0.000000000000000000, 1.877460629867496067 ) ) ;
#23715=CARTESIAN_POINT ( 'NONE',  ( 1.054774247047244096, 0.000000000000000000, 1.838090551127338657 ) ) ;
#23718=CARTESIAN_POINT ( 'NONE',  ( 0.9500414927467378812, 0.1787899950787401604, 0.4281496062454490659 ) ) ;
#23719=CARTESIAN_POINT ( 'NONE',  ( -1.002407869896990045, 0.1264236179284866091, 1.326279527505291433 ) ) ;
#23720=EDGE_CURVE ( 'NONE', #42434, #3668, #4830, .T. ) ;
#23721=DIRECTION ( 'NONE',  ( 0.000000000000000000, 0.000000000000000000, -1.000000000000000000 ) ) ;
#23722=CARTESIAN_POINT ( 'NONE',  ( -0.7495606340400177148, 0.1264236179284866091, 0.9817913385289134265 ) ) ;
#23723=CARTESIAN_POINT ( 'NONE',  ( -1.054774247047244096, 0.000000000000000000, 0.02706692908009476414 ) ) ;
#23725=CARTESIAN_POINT ( 'NONE',  ( -0.6971942568897648851, 0.07405724077823318263, 1.815944881835999558 ) ) ;
#23726=CARTESIAN_POINT ( 'NONE',  ( -0.7185039370078739607, 1.928577636452523993E-17, 1.988188976270425234 ) ) ;
#23727=CARTESIAN_POINT ( 'NONE',  ( 0.7185039370078739607, 1.928577636452523993E-17, 1.397637795168062969 ) ) ;
#23728=CARTESIAN_POINT ( 'NONE',  ( -1.033464566929134687, -0.06523048226347956391, 1.779035433070867089 ) ) ;
#23730=CARTESIAN_POINT ( 'NONE',  ( 0.8019270111902716547, 0.1787899950787401604, 1.692913385773008539 ) ) ;
#23732=CARTESIAN_POINT ( 'NONE',  ( 0.8759842519685039353, 0.000000000000000000, 4.498031496062992574 ) ) ;
#23733=CARTESIAN_POINT ( 'NONE',  ( -0.7646288533564489232, 0.1113553986120547346, 1.796259842519684957 ) ) ;
#23734=ORIENTED_EDGE ( 'NONE', *, *, #8504, .T. ) ;
#23739=CARTESIAN_POINT ( 'NONE',  ( 0.9500414927467378812, 0.1787899950787401604, 0.3838582676627718127 ) ) ;
#23742=CARTESIAN_POINT ( 'NONE',  ( 0.6971942568897637749, 2.189545951927499583E-17, 0.8686023621509606496 ) ) ;
#23744=CARTESIAN_POINT ( 'NONE',  ( 1.033464566929133799, 0.000000000000000000, 0.6003937007874016185 ) ) ;
#23745=CARTESIAN_POINT ( 'NONE',  ( 0.8107537697050253289, 0.1574803149606300301, 0.05167322823892971095 ) ) ;
#23747=ORIENTED_EDGE ( 'NONE', *, *, #11703, .F. ) ;
#23752=CARTESIAN_POINT ( 'NONE',  ( 0.8019270111902717657, 0.1787899950787401604, 0.3543307086076538659 ) ) ;
#23754=CARTESIAN_POINT ( 'NONE',  ( -1.054774247047244096, 0.000000000000000000, 1.872539370024976391 ) ) ;
#23756=CARTESIAN_POINT ( 'NONE',  ( -0.6971942568897648851, -0.07405724077823297447, 1.505905511757261284 ) ) ;
#23758=CARTESIAN_POINT ( 'NONE',  ( 0.7495606340400177148, 0.1264236179284866091, 1.459153543253322693 ) ) ;
#23760=CARTESIAN_POINT ( 'NONE',  ( 0.7495606340400177148, -0.1264236179284866091, 0.09104330703285078152 ) ) ;
#23761=CARTESIAN_POINT ( 'NONE',  ( -0.6971942568897648851, 0.07405724077823318263, 1.181102362150960428 ) ) ;
#23762=EDGE_CURVE ( 'NONE', #16198, #42764, #45545, .T. ) ;
#23765=CARTESIAN_POINT ( 'NONE',  ( 1.002407869896990045, 0.1264236179284866091, 0.6619094487651338010 ) ) ;
#23766=CARTESIAN_POINT ( 'NONE',  ( -0.8019270111902716547, 0.1787899950787401604, 0.5856299212060785964 ) ) ;
#23768=CARTESIAN_POINT ( 'NONE',  ( 0.8107537697050254399, 0.1574803149606300301, 1.665846456585386548 ) ) ;
#23769=ORIENTED_EDGE ( 'NONE', *, *, #14189, .F. ) ;
#23771=CARTESIAN_POINT ( 'NONE',  ( -0.9873396505805591694, 0.1113553986120547346, 0.3690944881889763884 ) ) ;
#23774=CARTESIAN_POINT ( 'NONE',  ( -0.6971942568897626646, 0.07405724077823318263, 0.9498031495525356416 ) ) ;
#23775=AXIS2_PLACEMENT_3D ( 'NONE', #7243, #25934, #36712 ) ;
#23776=CARTESIAN_POINT ( 'NONE',  ( -0.8019270111902717657, -0.1787899950787401604, 0.1279527558517483676 ) ) ;
#23779=CARTESIAN_POINT ( 'NONE',  ( -0.9412147342319837628, 0.1574803149606300301, 1.385334645561763445 ) ) ;
#23782=ORIENTED_EDGE ( 'NONE', *, *, #36965, .T. ) ;
#23784=EDGE_CURVE ( 'NONE', #16808, #43835, #30910, .T. ) ;
#23789=CARTESIAN_POINT ( 'NONE',  ( 0.9412147342319837628, -0.1574803149606297803, 0.1894685038294807999 ) ) ;
#23790=CARTESIAN_POINT ( 'NONE',  ( 0.8019270111902717657, -0.1787899950787401604, 1.624015747977732849 ) ) ;
#23794=CARTESIAN_POINT ( 'NONE',  ( 0.9500414927467378812, 0.1787899950787401604, 0.4232283464029293896 ) ) ;
#23795=CARTESIAN_POINT ( 'NONE',  ( -0.6971942568897648851, 0.07405724077823318263, 0.8316929133320636325 ) ) ;
#23798=CARTESIAN_POINT ( 'NONE',  ( -0.8186592603503980436, -0.1631638552240416984, 1.987135399130128155 ) ) ;
#23801=CARTESIAN_POINT ( 'NONE',  ( -0.9873396505805591694, -0.1113553986120547346, 1.254921259734991912 ) ) ;
#23802=CARTESIAN_POINT ( 'NONE',  ( 1.002407869896990045, 0.1264236179284866091, 1.528051181048598384 ) ) ;
#23803=CARTESIAN_POINT ( 'NONE',  ( 0.9500414927467377701, -0.1787899950787401604, 1.865157480261198097 ) ) ;
#23804=CARTESIAN_POINT ( 'NONE',  ( 0.8759842519685039353, 0.1787899950787401882, 0.3469488188438744070 ) ) ;
#23805=ORIENTED_EDGE ( 'NONE', *, *, #24792, .F. ) ;
#23807=FACE_OUTER_BOUND ( 'NONE', #15137, .T. ) ;
#23810=CARTESIAN_POINT ( 'NONE',  ( 0.7495606340400177148, 0.1264236179284866091, 0.3912401574265515491 ) ) ;
#23812=CARTESIAN_POINT ( 'NONE',  ( 0.7646288533564489232, -0.1113553986120547346, 1.953740157372787500 ) ) ;
#23813=CARTESIAN_POINT ( 'NONE',  ( -0.9873396505805591694, 0.1113553986120547346, 1.579724409341291214 ) ) ;
#23814=CARTESIAN_POINT ( 'NONE',  ( -1.002407869896990045, 0.1264236179284866091, 1.405019684985606476 ) ) ;
#23815=CARTESIAN_POINT ( 'NONE',  ( 0.7646288533564489232, -0.1113553986120547346, 0.7726377951680629685 ) ) ;
#23817=CARTESIAN_POINT ( 'NONE',  ( -0.7185039370078739607, 0.000000000000000000, -2.869337061179095023E-17 ) ) ;
#23818=CARTESIAN_POINT ( 'NONE',  ( 0.9500414927467378812, -0.1787899950787401604, 1.082677165300567346 ) ) ;
#23819=VERTEX_POINT ( 'NONE', #11560 ) ;
#23822=ORIENTED_EDGE ( 'NONE', *, *, #13868, .T. ) ;
#23823=CARTESIAN_POINT ( 'NONE',  ( -1.033464566929134687, 0.06523048226347956391, 0.6323818896562525271 ) ) ;
#23825=CARTESIAN_POINT ( 'NONE',  ( 0.9412147342319837628, 0.1574803149606300301, 0.09596456692913379882 ) ) ;
#23826=CARTESIAN_POINT ( 'NONE',  ( -0.7185039370078746268, -0.06523048226347956391, 1.409940944881891367 ) ) ;
#23831=CARTESIAN_POINT ( 'NONE',  ( 1.054774247047244540, 0.07405724077823318263, 0.1870078739619845110 ) ) ;
#23833=CARTESIAN_POINT ( 'NONE',  ( 0.8107537697050253289, -0.1574803149606297803, 1.405019684931842816 ) ) ;
#23838=CARTESIAN_POINT ( 'NONE',  ( 0.7495606340400177148, 0.1264236179284866091, 0.7111220471903307860 ) ) ;
#23839=CARTESIAN_POINT ( 'NONE',  ( -0.9500414927467377701, 0.1787899950787401604, 1.761811023568284229 ) ) ;
#23847=VERTEX_POINT ( 'NONE', #26421 ) ;
#23851=CARTESIAN_POINT ( 'NONE',  ( -0.7646288533564489232, -0.1113553986120547346, 0.4183070865066456645 ) ) ;
#23853=CARTESIAN_POINT ( 'NONE',  ( 0.7646288533564489232, 0.1113553986120547346, 1.875000000000000000 ) ) ;
#23854=AXIS2_PLACEMENT_3D ( 'NONE', #2667, #38862, #16602 ) ;
#23857=AXIS2_PLACEMENT_3D ( 'NONE', #25351, #35881, #7363 ) ;
#23858=CARTESIAN_POINT ( 'NONE',  ( -0.7495606340400177148, -0.1264236179284866091, 0.3272637794737956463 ) ) ;
#23859=CARTESIAN_POINT ( 'NONE',  ( -0.9873396505805591694, 0.1113553986120547346, 1.038385826771653475 ) ) ;
#23861=CARTESIAN_POINT ( 'NONE',  ( -0.7162142114693390571, 0.04048521711225155223, 1.982498882657834915 ) ) ;
#23863=CARTESIAN_POINT ( 'NONE',  ( 0.8759842519685039353, -0.1787899950787401882, 1.040846456639149764 ) ) ;
#23864=CARTESIAN_POINT ( 'NONE',  ( -0.8759842519685039353, 0.000000000000000000, 0.000000000000000000 ) ) ;
#23865=CARTESIAN_POINT ( 'NONE',  ( 1.033464566929134687, -0.06523048226347956391, 1.503444881889762774 ) ) ;
#23866=CARTESIAN_POINT ( 'NONE',  ( 0.7945469227473396234, 0.1381752303017431960, 1.980025006398726806 ) ) ;
#23870=CARTESIAN_POINT ( 'NONE',  ( -0.8107537697050253289, -0.1574803149606297803, 1.641240157372788611 ) ) ;
#23872=EDGE_CURVE ( 'NONE', #5354, #16198, #40371, .T. ) ;
#23873=CARTESIAN_POINT ( 'NONE',  ( 0.9500414927467377701, 0.1787899950787401604, 0.9350393700249758355 ) ) ;
#23875=CARTESIAN_POINT ( 'NONE',  ( 0.8759842519685039353, -0.1574803149606299191, 0.3838582676090082635 ) ) ;
#23876=ORIENTED_EDGE ( 'NONE', *, *, #21480, .F. ) ;
#23877=CARTESIAN_POINT ( 'NONE',  ( 0.8107537697050254399, -0.1574803149606297803, 1.247539369971212508 ) ) ;
#23878=CARTESIAN_POINT ( 'NONE',  ( 1.030962330798375515, 0.04070495257795413852, 0.03937007855506236692 ) ) ;
#23879=CARTESIAN_POINT ( 'NONE',  ( 0.9412147342319837628, -0.1574803149606297803, 0.2386811023622048278 ) ) ;
#23881=CARTESIAN_POINT ( 'NONE',  ( -0.9412147342319837628, -0.1574803149606297803, 0.1894685038294807722 ) ) ;
#23882=CARTESIAN_POINT ( 'NONE',  ( 1.002407869896990045, -0.1264236179284866091, 1.316437007820252081 ) ) ;
#23883=AXIS2_PLACEMENT_3D ( 'NONE', #24231, #1441, #9372 ) ;
#23884=ADVANCED_FACE ( 'NONE', ( #37408 ), #19200, .T. ) ;
#23887=CARTESIAN_POINT ( 'NONE',  ( -0.7646288533564489232, -0.1113553986120547346, 1.008858267609007875 ) ) ;
#23888=( BOUNDED_CURVE ( )  B_SPLINE_CURVE ( 2, ( #21449, #2292, #24355, #20971, #38734, #17624, #35842, #38954, #36078 ),
 .UNSPECIFIED., .F., .T. ) 
 B_SPLINE_CURVE_WITH_KNOTS ( ( 3, 2, 2, 2, 3 ),
 ( 0.1199999999999999956, 0.1224999999999999978, 0.1250000000000000000, 0.1275000000000000022, 0.1300000000000000044 ),
 .UNSPECIFIED. ) 
 CURVE ( )  GEOMETRIC_REPRESENTATION_ITEM ( )  RATIONAL_B_SPLINE_CURVE ( ( 1.000000000000000000, 0.9238795325112869605, 1.000000000000000000, 0.9238795325112869605, 1.000000000000000000, 0.9238795325112869605, 1.000000000000000000, 0.9238795325112869605, 1.000000000000000000 ) ) 
 REPRESENTATION_ITEM ( '' )  ) ;
#23890=CARTESIAN_POINT ( 'NONE',  ( -1.054774247047244096, 0.000000000000000000, 0.5339566928596221063 ) ) ;
#23891=CARTESIAN_POINT ( 'NONE',  ( 0.7185039370078746268, 0.06523048226347956391, 0.2632874015748031260 ) ) ;
#23896=CARTESIAN_POINT ( 'NONE',  ( -0.7495606340400177148, 0.1264236179284866091, 0.9473425196312755814 ) ) ;
#23899=CARTESIAN_POINT ( 'NONE',  ( -0.7495606340400177148, 0.1264236179284866091, 1.926673228292693052 ) ) ;
#23900=CARTESIAN_POINT ( 'NONE',  ( -0.8019270111902717657, 0.1787899950787401604, 0.7480314960092282472 ) ) ;
#23908=CARTESIAN_POINT ( 'NONE',  ( 0.7185039370078746268, -0.06523048226347956391, 0.4650590551181104093 ) ) ;
#23909=ORIENTED_EDGE ( 'NONE', *, *, #11434, .F. ) ;
#23911=DIRECTION ( 'NONE',  ( 1.822029033848725028E-16, 0.000000000000000000, 1.000000000000000000 ) ) ;
#23912=( BOUNDED_CURVE ( )  B_SPLINE_CURVE ( 2, ( #37124, #15335, #18669, #43837, #29987, #8124, #11038, #680, #14862 ),
 .UNSPECIFIED., .F., .T. ) 
 B_SPLINE_CURVE_WITH_KNOTS ( ( 3, 2, 2, 2, 3 ),
 ( 0.6899999999999999467, 0.6925000000000000044, 0.6949999999999999512, 0.6975000000000000089, 0.6999999999999999556 ),
 .UNSPECIFIED. ) 
 CURVE ( )  GEOMETRIC_REPRESENTATION_ITEM ( )  RATIONAL_B_SPLINE_CURVE ( ( 1.000000000000000000, 0.9238795325112899581, 1.000000000000000000, 0.9238795325112869605, 1.000000000000000000, 0.9238795325112869605, 1.000000000000000000, 0.9238795325112829637, 1.000000000000000000 ) ) 
 REPRESENTATION_ITEM ( '' )  ) ;
#23913=CARTESIAN_POINT ( 'NONE',  ( -0.9500414927467378812, -0.1787899950787401604, 0.5265748030958428139 ) ) ;
#23915=ORIENTED_EDGE ( 'NONE', *, *, #16095, .F. ) ;
#23916=CARTESIAN_POINT ( 'NONE',  ( -0.6971942568897637749, 2.189545951927499583E-17, 1.700295275536787498 ) ) ;
#23920=VERTEX_POINT ( 'NONE', #14682 ) ;
#23922=CARTESIAN_POINT ( 'NONE',  ( 0.9412147342319837628, -0.1574803149606297803, 0.9473425196850396857 ) ) ;
#23923=CARTESIAN_POINT ( 'NONE',  ( -0.8107537697050253289, 0.1574803149606300301, 1.272145669183810668 ) ) ;
#23924=ADVANCED_FACE ( 'NONE', ( #11327 ), #25939, .T. ) ;
#23925=CARTESIAN_POINT ( 'NONE',  ( 0.8019270111902717657, 0.1787899950787401604, 0.6299212597887560161 ) ) ;
#23930=VERTEX_POINT ( 'NONE', #22324 ) ;
#23932=CARTESIAN_POINT ( 'NONE',  ( -0.9500414927467377701, -0.1787899950787401604, 1.122047244040725422 ) ) ;
#23933=CARTESIAN_POINT ( 'NONE',  ( 0.8759842519685039353, -0.1574803149606299191, 1.023622047244094446 ) ) ;
#23943=EDGE_LOOP ( 'NONE', ( #5482, #6552, #37032, #43318 ) ) ;
#23946=CARTESIAN_POINT ( 'NONE',  ( 1.054774247047244540, 0.07405724077823318263, 0.8120078739619844832 ) ) ;
#23949=CARTESIAN_POINT ( 'NONE',  ( 0.7185039370078746268, -0.06523048226347956391, 1.449311023622047445 ) ) ;
#23950=CARTESIAN_POINT ( 'NONE',  ( -0.8759842519685039353, 0.000000000000000000, 0.000000000000000000 ) ) ;
#23954=CARTESIAN_POINT ( 'NONE',  ( 0.9873396505805591694, -0.1113553986120547346, 1.176181102254677313 ) ) ;
#23957=ORIENTED_EDGE ( 'NONE', *, *, #5473, .T. ) ;
#23958=CARTESIAN_POINT ( 'NONE',  ( -1.054774247047244096, 0.000000000000000000, 1.916830708607653477 ) ) ;
#23959=CARTESIAN_POINT ( 'NONE',  ( 1.054774247047244540, -0.07405724077823318263, 1.835629921206078485 ) ) ;
#23962=CARTESIAN_POINT ( 'NONE',  ( -1.002407869896990045, -0.1264236179284866091, 1.513287401521039355 ) ) ;
#23964=CARTESIAN_POINT ( 'NONE',  ( -1.002407869896990045, -0.1264236179284866091, 1.001476377898992132 ) ) ;
#23965=CARTESIAN_POINT ( 'NONE',  ( -0.9500414927467378812, 0.1787899950787401604, 0.2312992125446618197 ) ) ;
#23968=CARTESIAN_POINT ( 'NONE',  ( -0.6971942568897648851, 0.07405724077823318263, 1.776574803095843924 ) ) ;
#23969=CARTESIAN_POINT ( 'NONE',  ( 0.8759842519685039353, -0.1574803149606299191, 1.407480314853102321 ) ) ;
#23970=CARTESIAN_POINT ( 'NONE',  ( -0.7646288533564489232, -0.1113553986120547346, 1.806102362204724532 ) ) ;
#23973=CARTESIAN_POINT ( 'NONE',  ( 0.6971942568897637749, 2.189545951927499583E-17, 1.700295275536787498 ) ) ;
#23975=CARTESIAN_POINT ( 'NONE',  ( -0.7185039370078739607, 1.928577636452523993E-17, 1.486220472440944906 ) ) ;
#23979=CARTESIAN_POINT ( 'NONE',  ( -1.054774247047244540, 0.07405724077823318263, 1.289370078686393750 ) ) ;
#23984=CARTESIAN_POINT ( 'NONE',  ( -0.7646288533564489232, 0.1113553986120547346, 1.284448818897637956 ) ) ;
#23986=CARTESIAN_POINT ( 'NONE',  ( 1.054774247047244540, -0.07405724077823318263, 0.4133858267178901480 ) ) ;
#23989=CARTESIAN_POINT ( 'NONE',  ( -0.9873396505805591694, 0.1113553986120547346, 0.7923228345381417848 ) ) ;
#23993=CARTESIAN_POINT ( 'NONE',  ( 1.054774247047244540, 0.07405724077823318263, 0.8907480314422986378 ) ) ;
#23996=CARTESIAN_POINT ( 'NONE',  ( 0.8107537697050253289, 0.1574803149606300301, 0.09104330697908720460 ) ) ;
#23997=CARTESIAN_POINT ( 'NONE',  ( 0.7495606340400177148, -0.1264236179284866091, 0.7209645668753701386 ) ) ;
#24002=CARTESIAN_POINT ( 'NONE',  ( 0.7185039370078739607, 1.928577636452523993E-17, 0.4232283464566928832 ) ) ;
#24003=CARTESIAN_POINT ( 'NONE',  ( -1.054774247047244096, 0.000000000000000000, 1.833169291284818758 ) ) ;
#24005=CARTESIAN_POINT ( 'NONE',  ( -1.054774247047244096, 0.000000000000000000, 1.405019684985606476 ) ) ;
#24007=CARTESIAN_POINT ( 'NONE',  ( -0.8019270111902717657, 0.1787899950787401604, 0.7086614172690703928 ) ) ;
#24008=CARTESIAN_POINT ( 'NONE',  ( -1.002407869896990045, -0.1264236179284866091, 1.277066929080094448 ) ) ;
#24009=LINE ( 'NONE', #31913, #17456 ) ;
#24010=CARTESIAN_POINT ( 'NONE',  ( 0.7495606340400177148, -0.1264236179284866091, 0.6422244093950550958 ) ) ;
#24011=CARTESIAN_POINT ( 'NONE',  ( -0.8019270111902716547, 0.1787899950787401604, 0.4675196849856070314 ) ) ;
#24014=ORIENTED_EDGE ( 'NONE', *, *, #17469, .F. ) ;
#24016=CARTESIAN_POINT ( 'NONE',  ( -0.8759842519685039353, -0.1574803149606299191, 0.2362204724409449064 ) ) ;
#24017=CARTESIAN_POINT ( 'NONE',  ( 0.8759842519685039353, 0.1787899950787401882, 1.257381889710015743 ) ) ;
#24019=CARTESIAN_POINT ( 'NONE',  ( -0.8107537697050254399, -0.1574803149606297803, 1.838090551073574774 ) ) ;
#24020=ORIENTED_EDGE ( 'NONE', *, *, #33595, .F. ) ;
#24022=CARTESIAN_POINT ( 'NONE',  ( -1.054774247047244540, 0.07405724077823318263, 1.013779527505291878 ) ) ;
#24023=( BOUNDED_CURVE ( )  B_SPLINE_CURVE ( 2, ( #45211, #1851, #31120, #45683, #44970, #16025, #27052, #12183, #26808 ),
 .UNSPECIFIED., .F., .T. ) 
 B_SPLINE_CURVE_WITH_KNOTS ( ( 3, 2, 2, 2, 3 ),
 ( 0.1900000000000000022, 0.1925000000000000044, 0.1950000000000000067, 0.1975000000000000089, 0.2000000000000000111 ),
 .UNSPECIFIED. ) 
 CURVE ( )  GEOMETRIC_REPRESENTATION_ITEM ( )  RATIONAL_B_SPLINE_CURVE ( ( 1.000000000000000000, 0.9238795325112869605, 1.000000000000000000, 0.9238795325112869605, 1.000000000000000000, 0.9238795325112869605, 1.000000000000000000, 0.9238795325112869605, 1.000000000000000000 ) ) 
 REPRESENTATION_ITEM ( '' )  ) ;
#24029=EDGE_LOOP ( 'NONE', ( #15906, #46045, #44645, #12588 ) ) ;
#24030=CARTESIAN_POINT ( 'NONE',  ( 0.8019270111902717657, -0.1787899950787401604, 1.466535433017102763 ) ) ;
#24037=CARTESIAN_POINT ( 'NONE',  ( 1.033464566929133799, 0.000000000000000000, 1.860236220472440971 ) ) ;
#24039=CARTESIAN_POINT ( 'NONE',  ( 1.054774247047244540, 0.07405724077823318263, 1.560039370024977057 ) ) ;
#24040=EDGE_CURVE ( 'NONE', #740, #3655, #34088, .T. ) ;
#24043=CARTESIAN_POINT ( 'NONE',  ( -0.6971942568897643300, 0.000000000000000000, 1.995570866087968520 ) ) ;
#24045=CARTESIAN_POINT ( 'NONE',  ( 0.8759842519685039353, -0.1787899950787401882, 0.4453740156942677664 ) ) ;
#24047=CARTESIAN_POINT ( 'NONE',  ( -0.6971942568897637749, 2.189545951927499583E-17, 0.8341535432533228045 ) ) ;
#24049=LINE ( 'NONE', #46060, #44606 ) ;
#24052=CARTESIAN_POINT ( 'NONE',  ( -0.8107537697050254399, 0.1574803149606300301, 1.035925196742866650 ) ) ;
#24053=CARTESIAN_POINT ( 'NONE',  ( 1.054774247047244540, 0.07405724077823318263, 1.486220472387181690 ) ) ;
#24055=CARTESIAN_POINT ( 'NONE',  ( 0.6971942568897626646, -0.07405724077823297447, 0.3198818897100159098 ) ) ;
#24061=CARTESIAN_POINT ( 'NONE',  ( 0.6971942568897637749, 2.189545951927499583E-17, 0.4355314960092284138 ) ) ;
#24063=CARTESIAN_POINT ( 'NONE',  ( 0.8759842491179902213, 0.1574803149606299191, 1.978346456692913646 ) ) ;
#24064=CARTESIAN_POINT ( 'NONE',  ( -0.6971942568897648851, 0.07405724077823318263, 1.377952755851748146 ) ) ;
#24065=CARTESIAN_POINT ( 'NONE',  ( 0.7646288533564489232, 0.1113553986120547346, 0.7627952754830236159 ) ) ;
#24068=CARTESIAN_POINT ( 'NONE',  ( 0.8019270111902717657, -0.1787899950787401604, 0.9990157479777320715 ) ) ;
#24072=CARTESIAN_POINT ( 'NONE',  ( -1.033464566929134687, -0.06523048226347956391, 0.5093503935932609528 ) ) ;
#24074=CARTESIAN_POINT ( 'NONE',  ( 0.9500414927467378812, 0.1787899950787401604, 1.683070866087970074 ) ) ;
#24075=CARTESIAN_POINT ( 'NONE',  ( -0.8759842519685039353, 0.1574803149606299191, 1.437007874015747921 ) ) ;
#24076=CARTESIAN_POINT ( 'NONE',  ( 0.8759842519685039353, -0.1574803149606299191, 1.801181102254677091 ) ) ;
#24077=CARTESIAN_POINT ( 'NONE',  ( -0.8759842519685039353, 0.1574803149606299191, 0.7283464566929134243 ) ) ;
#24079=CARTESIAN_POINT ( 'NONE',  ( 0.6971942568897637749, 2.189545951927499583E-17, 0.1254921259304885850 ) ) ;
#24080=CARTESIAN_POINT ( 'NONE',  ( -0.6971942568897637749, 2.189545951927499583E-17, 0.1205708660879689087 ) ) ;
#24081=CARTESIAN_POINT ( 'NONE',  ( 1.033464566929133799, 0.000000000000000000, 1.417322834538141674 ) ) ;
#24083=EDGE_LOOP ( 'NONE', ( #30172, #2254, #29704, #35641 ) ) ;
#24086=CARTESIAN_POINT ( 'NONE',  ( -0.6971942568897637749, 2.189545951927499583E-17, 1.734744094434425232 ) ) ;
#24091=VERTEX_POINT ( 'NONE', #8413 ) ;
#24096=CARTESIAN_POINT ( 'NONE',  ( -1.033464566929133799, 0.000000000000000000, 0.4330708660342047489 ) ) ;
#24098=CARTESIAN_POINT ( 'NONE',  ( 0.9412147342319837628, -0.1574803149606297803, 1.852854330708662012 ) ) ;
#24104=CARTESIAN_POINT ( 'NONE',  ( -1.002407869896990045, 0.1264236179284866091, 0.3863188975840318173 ) ) ;
#24105=CARTESIAN_POINT ( 'NONE',  ( -0.8107537697050253289, -0.1574803149606297803, 0.9817913385826764205 ) ) ;
#24108=CARTESIAN_POINT ( 'NONE',  ( 0.8759842519685039353, -0.1787899950787401882, 1.119586614119464585 ) ) ;
#24109=CARTESIAN_POINT ( 'NONE',  ( 0.6971942568897637749, 2.189545951927499583E-17, 1.419783464513165505 ) ) ;
#24110=CARTESIAN_POINT ( 'NONE',  ( 0.6971942568897626646, -0.07405724077823297447, 0.1624015747493861017 ) ) ;
#24112=CARTESIAN_POINT ( 'NONE',  ( 0.7185039370078739607, 1.928577636452523993E-17, 1.604330708661417360 ) ) ;
#24113=CARTESIAN_POINT ( 'NONE',  ( 0.7185039370078746268, -0.06523048226347956391, 1.409940944881891367 ) ) ;
#24116=CARTESIAN_POINT ( 'NONE',  ( -1.033464566929133799, 1.928577636452524610E-17, 2.869337061179095023E-17 ) ) ;
#24119=CARTESIAN_POINT ( 'NONE',  ( 1.002407869896990045, -0.1264236179284866091, 0.9227362204186770889 ) ) ;
#24120=CARTESIAN_POINT ( 'NONE',  ( 0.8019270111902716547, 0.1787899950787401604, 1.968503936954110412 ) ) ;
#24121=CARTESIAN_POINT ( 'NONE',  ( 0.9412147342319837628, -0.1574803149606297803, 0.3863188975302684902 ) ) ;
#24122=ORIENTED_EDGE ( 'NONE', *, *, #37129, .F. ) ;
#24123=CARTESIAN_POINT ( 'NONE',  ( 1.054774247047244096, 0.000000000000000000, 1.995570866087968520 ) ) ;
#24126=CARTESIAN_POINT ( 'NONE',  ( -0.8759842519685039353, 0.1574803149606299191, 0.3248031494987720369 ) ) ;
#24128=CARTESIAN_POINT ( 'NONE',  ( 0.8759842519685039353, -0.1787899950787401882, 1.350885826717889815 ) ) ;
#24129=CIRCLE ( 'NONE', #9592, 0.1787899950787401049 ) ;
#24130=CARTESIAN_POINT ( 'NONE',  ( -0.5314960629921260393, 0.000000000000000000, 4.842519685039370358 ) ) ;
#24131=CARTESIAN_POINT ( 'NONE',  ( 1.033464566929134687, -0.06523048226347956391, 0.07627952745152805081 ) ) ;
#24135=CARTESIAN_POINT ( 'NONE',  ( -0.9500414927467378812, 0.1787899950787401604, 0.5413385826234012876 ) ) ;
#24140=CARTESIAN_POINT ( 'NONE',  ( -1.054774247047244540, 0.07405724077823318263, 1.402559055064346749 ) ) ;
#24142=CARTESIAN_POINT ( 'NONE',  ( -0.7495606340400177148, -0.1264236179284866091, 0.9965551180564724554 ) ) ;
#24144=CARTESIAN_POINT ( 'NONE',  ( -0.7495606340400177148, 0.1264236179284866091, 1.966043307032850462 ) ) ;
#24145=ORIENTED_EDGE ( 'NONE', *, *, #23236, .F. ) ;
#24146=CARTESIAN_POINT ( 'NONE',  ( -0.7495606340400177148, 0.1264236179284866091, 0.6717519684501732646 ) ) ;
#24153=EDGE_LOOP ( 'NONE', ( #44097, #43619, #30292, #45556 ) ) ;
#24154=FACE_OUTER_BOUND ( 'NONE', #4331, .T. ) ;
#24155=CARTESIAN_POINT ( 'NONE',  ( -0.8019270111902717657, 0.1787899950787401604, 0.6249999999462366729 ) ) ;
#24157=EDGE_CURVE ( 'NONE', #39441, #34250, #45274, .T. ) ;
#24159=CARTESIAN_POINT ( 'NONE',  ( -1.054774247047244540, 0.07405724077823318263, 1.722440944828126153 ) ) ;
#24160=EDGE_CURVE ( 'NONE', #20228, #35982, #8896, .T. ) ;
#24161=CARTESIAN_POINT ( 'NONE',  ( -0.8759842519685039353, -0.1574803149606299191, 0.1870078739082208508 ) ) ;
#24163=VECTOR ( 'NONE', #10955, 39.37007874015748143 ) ;
#24165=CARTESIAN_POINT ( 'NONE',  ( -0.8759842519685039353, 0.1574803149606299191, 0.9645669291338583307 ) ) ;
#24166=CARTESIAN_POINT ( 'NONE',  ( -1.033464566929134687, -0.06523048226347956391, 1.257381889656253193 ) ) ;
#24169=AXIS2_PLACEMENT_3D ( 'NONE', #24497, #34581, #16144 ) ;
#24173=CARTESIAN_POINT ( 'NONE',  ( 0.7185039370078739607, 1.928577636452523993E-17, 1.092519685039370136 ) ) ;
#24176=DIRECTION ( 'NONE',  ( 0.000000000000000000, 0.000000000000000000, -1.000000000000000000 ) ) ;
#24177=( BOUNDED_CURVE ( )  B_SPLINE_CURVE ( 2, ( #46321, #20916, #31962, #35555, #46547, #13730, #25231, #39819, #7008 ),
 .UNSPECIFIED., .F., .T. ) 
 B_SPLINE_CURVE_WITH_KNOTS ( ( 3, 2, 2, 2, 3 ),
 ( 0.7500000000000000000, 0.7524999999999999467, 0.7550000000000000044, 0.7574999999999999512, 0.7600000000000000089 ),
 .UNSPECIFIED. ) 
 CURVE ( )  GEOMETRIC_REPRESENTATION_ITEM ( )  RATIONAL_B_SPLINE_CURVE ( ( 1.000000000000000000, 0.9238795325112899581, 1.000000000000000000, 0.9238795325112869605, 1.000000000000000000, 0.9238795325112869605, 1.000000000000000000, 0.9238795325112869605, 1.000000000000000000 ) ) 
 REPRESENTATION_ITEM ( '' )  ) ;
#24182=ORIENTED_EDGE ( 'NONE', *, *, #34682, .F. ) ;
#24183=CARTESIAN_POINT ( 'NONE',  ( -0.7185039370078746268, -0.06523048226347956391, 1.055610236220473341 ) ) ;
#24185=CARTESIAN_POINT ( 'NONE',  ( 1.002407869896990045, 0.1264236179284866091, 0.8538385826234016207 ) ) ;
#24187=CARTESIAN_POINT ( 'NONE',  ( -0.8759842519685039353, 0.1574803149606299191, 0.5314960629921260393 ) ) ;
#24191=CARTESIAN_POINT ( 'NONE',  ( -0.8107537697050254399, 0.1574803149606300301, 1.400098425196850904 ) ) ;
#24193=CARTESIAN_POINT ( 'NONE',  ( -0.6971942568897637749, 2.189545951927499583E-17, 1.975885826717889815 ) ) ;
#24194=CARTESIAN_POINT ( 'NONE',  ( 1.002407869896990045, 0.1264236179284866091, 1.882381889710015743 ) ) ;
#24197=CARTESIAN_POINT ( 'NONE',  ( -0.8019270111902717657, -0.1787899950787401604, 1.505905511757261284 ) ) ;
#24199=FACE_OUTER_BOUND ( 'NONE', #41603, .T. ) ;
#24200=CARTESIAN_POINT ( 'NONE',  ( -0.6971942568897626646, -0.07405724077823297447, 0.2460629920722207375 ) ) ;
#24201=( BOUNDED_CURVE ( )  B_SPLINE_CURVE ( 2, ( #24646, #28029, #32329, #10026, #24187, #28500, #20801, #42370, #2120 ),
 .UNSPECIFIED., .F., .F. ) 
 B_SPLINE_CURVE_WITH_KNOTS ( ( 3, 2, 2, 2, 3 ),
 ( 0.2600000000000000089, 0.2625000000000000111, 0.2650000000000000133, 0.2675000000000000155, 0.2700000000000000178 ),
 .UNSPECIFIED. ) 
 CURVE ( )  GEOMETRIC_REPRESENTATION_ITEM ( )  RATIONAL_B_SPLINE_CURVE ( ( 1.000000000000000000, 0.9238795325112869605, 1.000000000000000000, 0.9238795325112869605, 1.000000000000000000, 0.9238795325112869605, 1.000000000000000000, 0.9238795325112869605, 1.000000000000000000 ) ) 
 REPRESENTATION_ITEM ( '' )  ) ;
#24202=CARTESIAN_POINT ( 'NONE',  ( -0.9873396505805591694, 0.1113553986120547346, 0.5659448818897637734 ) ) ;
#24203=CARTESIAN_POINT ( 'NONE',  ( -0.8759842519685039353, 0.1787899950787401882, 1.926673228292693052 ) ) ;
#24205=CARTESIAN_POINT ( 'NONE',  ( -0.8107537697050253289, -0.1574803149606297803, 1.808562992125984703 ) ) ;
#24209=CARTESIAN_POINT ( 'NONE',  ( 0.9500414927467377701, -0.1787899950787401604, 1.712598425143087466 ) ) ;
#24220=ADVANCED_FACE ( 'NONE', ( #44705 ), #6086, .F. ) ;
#24221=CARTESIAN_POINT ( 'NONE',  ( -0.8107537697050254399, -0.1574803149606297803, 1.365649606191686294 ) ) ;
#24225=CARTESIAN_POINT ( 'NONE',  ( -1.033464566929134687, 0.06523048226347956391, 0.7898622046168821687 ) ) ;
#24226=CARTESIAN_POINT ( 'NONE',  ( -0.9412147342319837628, 0.1574803149606300301, 0.7258858267716535861 ) ) ;
#24229=CARTESIAN_POINT ( 'NONE',  ( 1.054774247047244540, 0.07405724077823318263, 0.8513779527021426707 ) ) ;
#24231=CARTESIAN_POINT ( 'NONE',  ( 0.8759842519685039353, 0.000000000000000000, 2.007874015640504162 ) ) ;
#24232=CARTESIAN_POINT ( 'NONE',  ( 0.7185039370078746268, 0.06523048226347956391, 0.05659448808144944970 ) ) ;
#24233=CARTESIAN_POINT ( 'NONE',  ( 0.8107537697050253289, 0.1574803149606300301, 0.1796259842519684069 ) ) ;
#24234=CARTESIAN_POINT ( 'NONE',  ( 1.033464566929134687, 0.06523048226347956391, 0.7111220471365682361 ) ) ;
#24237=CARTESIAN_POINT ( 'NONE',  ( -0.8759842519685039353, 0.1787899950787401882, 1.961122047190330786 ) ) ;
#24239=CARTESIAN_POINT ( 'NONE',  ( -0.7495606340400177148, 0.1264236179284866091, 1.459153543253322693 ) ) ;
#24240=CARTESIAN_POINT ( 'NONE',  ( 0.7495606340400177148, -0.1264236179284866091, 1.429625984198204858 ) ) ;
#24243=CARTESIAN_POINT ( 'NONE',  ( -0.8759842519685039353, 0.1787899950787401882, 0.6274606298674959559 ) ) ;
#24246=CARTESIAN_POINT ( 'NONE',  ( 1.002407869896990045, -0.1264236179284866091, 0.6914370078202519698 ) ) ;
#24247=CARTESIAN_POINT ( 'NONE',  ( -0.8759842519685039353, -0.1787899950787401882, 0.6028543306548976854 ) ) ;
#24252=CARTESIAN_POINT ( 'NONE',  ( -0.8107537697050253289, 0.1574803149606300301, 0.2583661417322835052 ) ) ;
#24254=CARTESIAN_POINT ( 'NONE',  ( 0.8759842519685039353, -0.1787899950787401882, 1.237696850339937038 ) ) ;
#24259=CARTESIAN_POINT ( 'NONE',  ( -0.8019270111902717657, 0.1787899950787401604, 0.9055118109698585549 ) ) ;
#24262=CARTESIAN_POINT ( 'NONE',  ( 1.033464566929134687, 0.06523048226347956391, 0.9965551181102363376 ) ) ;
#24264=DIRECTION ( 'NONE',  ( -1.000000000000000000, 0.000000000000000000, 0.000000000000000000 ) ) ;
#24269=EDGE_CURVE ( 'NONE', #3655, #110, #1464, .T. ) ;
#24275=DIRECTION ( 'NONE',  ( 1.822029033848725028E-16, 0.000000000000000000, 1.000000000000000000 ) ) ;
#24276=CARTESIAN_POINT ( 'NONE',  ( 0.8019270111902717657, -0.1787899950787401604, 0.5216535432533228045 ) ) ;
#24278=CARTESIAN_POINT ( 'NONE',  ( -0.9500414927467377701, -0.1787899950787401604, 0.8858267715997791836 ) ) ;
#24280=CARTESIAN_POINT ( 'NONE',  ( 0.8759842519685039353, 0.000000000000000000, 4.498031496062992574 ) ) ;
#24282=CARTESIAN_POINT ( 'NONE',  ( -0.8493115269941948764, -0.1716529789732494093, 1.987718322235668911 ) ) ;
#24284=CARTESIAN_POINT ( 'NONE',  ( 1.054774247047244096, 0.000000000000000000, 1.483759842465921075 ) ) ;
#24285=CARTESIAN_POINT ( 'NONE',  ( 1.054774247047244096, 0.000000000000000000, 1.951279527505291433 ) ) ;
#24287=CARTESIAN_POINT ( 'NONE',  ( 0.6971942568897637749, 2.189545951927499583E-17, 0.4355314960092284138 ) ) ;
#24288=ORIENTED_EDGE ( 'NONE', *, *, #162, .T. ) ;
#24290=CARTESIAN_POINT ( 'NONE',  ( 1.033464566929133799, 1.928577636452524610E-17, 4.498031496062992574 ) ) ;
#24293=CARTESIAN_POINT ( 'NONE',  ( 0.8019270111902717657, 0.1787899950787401604, 0.4281496062454490659 ) ) ;
#24295=CARTESIAN_POINT ( 'NONE',  ( 0.8759842519685039353, 0.000000000000000000, 4.498031496062992574 ) ) ;
#24297=CARTESIAN_POINT ( 'NONE',  ( -1.054774247047244096, 0.000000000000000000, 1.439468503883244210 ) ) ;
#24300=CARTESIAN_POINT ( 'NONE',  ( -0.9412147342319837628, -0.1574803149606297803, 0.5831692912310553201 ) ) ;
#24301=VERTEX_POINT ( 'NONE', #40426 ) ;
#24302=CARTESIAN_POINT ( 'NONE',  ( -0.7185039370078746268, 0.06523048226347956391, 1.326279527559055982 ) ) ;
#24303=CARTESIAN_POINT ( 'NONE',  ( -1.002407869896990045, 0.1264236179284866091, 0.8538385826234016207 ) ) ;
#24304=EDGE_CURVE ( 'NONE', #18202, #32512, #37588, .T. ) ;
#24307=CARTESIAN_POINT ( 'NONE',  ( 1.054774247047244540, 0.07405724077823318263, 0.2263779527021417270 ) ) ;
#24308=CARTESIAN_POINT ( 'NONE',  ( 0.8759842519685039353, 0.1574803149606299191, 1.466535432963338437 ) ) ;
#24313=CARTESIAN_POINT ( 'NONE',  ( -0.6971942568897637749, 2.189545951927499583E-17, 1.695374015694267822 ) ) ;
#24320=ORIENTED_EDGE ( 'NONE', *, *, #42657, .T. ) ;
#24322=ORIENTED_EDGE ( 'NONE', *, *, #13752, .F. ) ;
#24323=ORIENTED_EDGE ( 'NONE', *, *, #46629, .F. ) ;
#24325=CARTESIAN_POINT ( 'NONE',  ( -0.7646288533564489232, 0.1113553986120547346, 0.9202755904436535905 ) ) ;
#24327=CARTESIAN_POINT ( 'NONE',  ( 0.7646288533564489232, 0.1113553986120547346, 1.835629921259842590 ) ) ;
#24330=CARTESIAN_POINT ( 'NONE',  ( -0.7495606340400177148, 0.1264236179284866091, 0.3961614172690708924 ) ) ;
#24331=CARTESIAN_POINT ( 'NONE',  ( -0.8759842519685039353, 0.1574803149606299191, 1.043307086614173151 ) ) ;
#24335=CARTESIAN_POINT ( 'NONE',  ( 0.7495606340400177148, -0.1264236179284866091, 1.154035433017102319 ) ) ;
#24336=CARTESIAN_POINT ( 'NONE',  ( 0.8759842519685039353, 0.1787899950787401882, 1.528051181048598384 ) ) ;
#24338=CARTESIAN_POINT ( 'NONE',  ( 1.033464566929134687, -0.06523048226347956391, 1.660925196850393526 ) ) ;
#24340=CARTESIAN_POINT ( 'NONE',  ( 1.033464566929134687, 0.06523048226347956391, 1.705216535433070613 ) ) ;
#24341=CARTESIAN_POINT ( 'NONE',  ( 0.7185039370078739607, 1.928577636452523993E-17, 1.437007873908220601 ) ) ;
#24342=DIRECTION ( 'NONE',  ( 0.000000000000000000, 0.000000000000000000, -1.000000000000000000 ) ) ;
#24343=AXIS2_PLACEMENT_3D ( 'NONE', #35791, #13292, #27921 ) ;
#24346=CARTESIAN_POINT ( 'NONE',  ( 0.6971942568897648851, 0.07405724077823318263, 1.181102362150960428 ) ) ;
#24347=CARTESIAN_POINT ( 'NONE',  ( 1.002407869896990045, -0.1264236179284866091, 1.990649606245448844 ) ) ;
#24348=CARTESIAN_POINT ( 'NONE',  ( 0.9873396505805591694, -0.1113553986120547346, 0.2706692912310554866 ) ) ;
#24351=CARTESIAN_POINT ( 'NONE',  ( -0.8107537697050253289, 0.1574803149606300301, 0.2091535431995598104 ) ) ;
#24353=CARTESIAN_POINT ( 'NONE',  ( 0.8759842519685039353, 0.1787899950787401882, 1.370570866087968520 ) ) ;
#24355=CARTESIAN_POINT ( 'NONE',  ( -0.9873396505805591694, 0.1113553986120547346, 0.2805118109160948947 ) ) ;
#24358=CARTESIAN_POINT ( 'NONE',  ( -1.033464566929134687, -0.06523048226347956391, 1.021161417215306955 ) ) ;
#24361=CARTESIAN_POINT ( 'NONE',  ( -0.9873396505805591694, 0.1113553986120547346, 0.2017716534357799352 ) ) ;
#24365=CARTESIAN_POINT ( 'NONE',  ( -0.6971942568897637749, 2.189545951927499583E-17, 0.9522637794737952577 ) ) ;
#24366=CARTESIAN_POINT ( 'NONE',  ( -1.033464566929134687, 0.06523048226347956391, 0.01230314960629920289 ) ) ;
#24368=CARTESIAN_POINT ( 'NONE',  ( -0.9500414927467378812, 0.1787899950787401604, 0.6249999999462356737 ) ) ;
#24371=CARTESIAN_POINT ( 'NONE',  ( 0.8759842519685039353, 0.000000000000000000, 4.498031496062992574 ) ) ;
#24378=CARTESIAN_POINT ( 'NONE',  ( -1.054774247047244540, 0.07405724077823318263, 0.6938976377415123631 ) ) ;
#24379=VERTEX_POINT ( 'NONE', #44962 ) ;
#24380=CARTESIAN_POINT ( 'NONE',  ( -0.8759842519685039353, 0.1787899950787401882, 1.729822834591905556 ) ) ;
#24383=CARTESIAN_POINT ( 'NONE',  ( 0.7185039370078739607, 1.928577636452523993E-17, 0.3444881889763780070 ) ) ;
#24386=CARTESIAN_POINT ( 'NONE',  ( 1.033464566929133799, 0.000000000000000000, 0.6003937007874016185 ) ) ;
#24389=CARTESIAN_POINT ( 'NONE',  ( -0.8759842519685039353, 0.1574803149606299191, 1.387795275483023616 ) ) ;
#24395=CARTESIAN_POINT ( 'NONE',  ( 0.9873396505805591694, 0.1113553986120547346, 1.195866141732283561 ) ) ;
#24397=DIRECTION ( 'NONE',  ( 0.000000000000000000, 0.000000000000000000, -1.000000000000000000 ) ) ;
#24398=CARTESIAN_POINT ( 'NONE',  ( 0.7185039370078739607, 1.928577636452523993E-17, 1.958661417322834719 ) ) ;
#24402=CARTESIAN_POINT ( 'NONE',  ( -1.033464566929133799, 1.928577636452524610E-17, 2.869337061179095023E-17 ) ) ;
#24407=CARTESIAN_POINT ( 'NONE',  ( 0.9500414927467378812, 0.1787899950787401604, 0.8169291338045038264 ) ) ;
#24408=FACE_OUTER_BOUND ( 'NONE', #36340, .T. ) ;
#24416=CARTESIAN_POINT ( 'NONE',  ( -0.8019270111902717657, -0.1787899950787401604, 1.904527559001354398 ) ) ;
#24417=ORIENTED_EDGE ( 'NONE', *, *, #38250, .F. ) ;
#24418=CARTESIAN_POINT ( 'NONE',  ( -0.8107537697050254399, -0.1574803149606297803, 0.8144685038294804391 ) ) ;
#24420=CARTESIAN_POINT ( 'NONE',  ( 0.7185039370078746268, -0.06523048226347956391, 0.5437992125984247860 ) ) ;
#24421=CARTESIAN_POINT ( 'NONE',  ( -1.002407869896990045, 0.1264236179284866091, 1.562499999946236118 ) ) ;
#24422=DIRECTION ( 'NONE',  ( 1.822029033848725028E-16, 0.000000000000000000, 1.000000000000000000 ) ) ;
#24424=CARTESIAN_POINT ( 'NONE',  ( -1.002407869896990045, -0.1264236179284866091, 0.2977362204186775885 ) ) ;
#24426=CARTESIAN_POINT ( 'NONE',  ( -1.054774247047244540, 0.07405724077823318263, 1.958661417269071947 ) ) ;
#24428=CARTESIAN_POINT ( 'NONE',  ( -0.7646288533564489232, -0.1113553986120547346, 1.924212598425196985 ) ) ;
#24433=CARTESIAN_POINT ( 'NONE',  ( -1.033464566929135131, 1.928577636452536319E-17, 0.03937007874015843040 ) ) ;
#24435=CARTESIAN_POINT ( 'NONE',  ( -0.9500414927467377701, -0.1787899950787401604, 1.200787401521039355 ) ) ;
#24439=( BOUNDED_CURVE ( )  B_SPLINE_CURVE ( 2, ( #45471, #16281, #34736, #1875, #45710, #12927, #42109, #9318, #20327 ),
 .UNSPECIFIED., .F., .T. ) 
 B_SPLINE_CURVE_WITH_KNOTS ( ( 3, 2, 2, 2, 3 ),
 ( 0.9699999999999999734, 0.9725000000000000311, 0.9749999999999999778, 0.9775000000000000355, 0.9799999999999999822 ),
 .UNSPECIFIED. ) 
 CURVE ( )  GEOMETRIC_REPRESENTATION_ITEM ( )  RATIONAL_B_SPLINE_CURVE ( ( 1.000000000000000000, 0.9238795325112939549, 1.000000000000000000, 0.9238795325112869605, 1.000000000000000000, 0.9238795325112869605, 1.000000000000000000, 0.9238795325112869605, 1.000000000000000000 ) ) 
 REPRESENTATION_ITEM ( '' )  ) ;
#24444=CARTESIAN_POINT ( 'NONE',  ( -0.7646288533564489232, -0.1113553986120547346, 0.8513779526483780113 ) ) ;
#24445=CARTESIAN_POINT ( 'NONE',  ( -0.9412147342319837628, -0.1574803149606297803, 0.6717519685039377020 ) ) ;
#24446=AXIS2_PLACEMENT_3D ( 'NONE', #23642, #34919, #15999 ) ;
#24448=CARTESIAN_POINT ( 'NONE',  ( 0.6971942568897637749, 2.189545951927499583E-17, 0.9473425196312755814 ) ) ;
#24449=CARTESIAN_POINT ( 'NONE',  ( -1.033464566929133799, 0.000000000000000000, 1.072834645669291431 ) ) ;
#24452=CARTESIAN_POINT ( 'NONE',  ( 0.7185039370078739607, 1.928577636452523993E-17, 1.082677165246803241 ) ) ;
#24453=CARTESIAN_POINT ( 'NONE',  ( 0.9412147342319837628, -0.1574803149606297803, 0.1894685038294807722 ) ) ;
#24454=CARTESIAN_POINT ( 'NONE',  ( 0.7185039370078746268, -0.06523048226347956391, 0.1894685039370080093 ) ) ;
#24456=CARTESIAN_POINT ( 'NONE',  ( 0.7185039370078739607, 1.928577636452523993E-17, 0.3740157479239689664 ) ) ;
#24459=( BOUNDED_CURVE ( )  B_SPLINE_CURVE ( 2, ( #23198, #37814, #45209, #12431, #15299, #29952, #26337, #9292, #9531 ),
 .UNSPECIFIED., .F., .F. ) 
 B_SPLINE_CURVE_WITH_KNOTS ( ( 3, 2, 2, 2, 3 ),
 ( 0.5699999999999999512, 0.5725000000000000089, 0.5749999999999999556, 0.5775000000000000133, 0.5799999999999999600 ),
 .UNSPECIFIED. ) 
 CURVE ( )  GEOMETRIC_REPRESENTATION_ITEM ( )  RATIONAL_B_SPLINE_CURVE ( ( 1.000000000000000000, 0.9238795325112899581, 1.000000000000000000, 0.9238795325112869605, 1.000000000000000000, 0.9238795325112869605, 1.000000000000000000, 0.9238795325112869605, 1.000000000000000000 ) ) 
 REPRESENTATION_ITEM ( '' )  ) ;
#24462=CARTESIAN_POINT ( 'NONE',  ( -1.054774247047244540, 0.07405724077823318263, 1.874999999946236784 ) ) ;
#24464=CARTESIAN_POINT ( 'NONE',  ( -0.7495606340400177148, 0.1264236179284866091, 1.419783464513165505 ) ) ;
#24465=CARTESIAN_POINT ( 'NONE',  ( 1.054774247047244540, -0.07405724077823318263, 1.481299212544662680 ) ) ;
#24469=CARTESIAN_POINT ( 'NONE',  ( -1.054774247047244540, -0.07405724077823318263, 0.6938976377415123631 ) ) ;
#24470=CARTESIAN_POINT ( 'NONE',  ( 1.002407869896990045, 0.1264236179284866091, 0.1894685038832444879 ) ) ;
#24473=CARTESIAN_POINT ( 'NONE',  ( 0.6971942568897648851, 0.07405724077823318263, 0.5561023621509617598 ) ) ;
#24474=CARTESIAN_POINT ( 'NONE',  ( -1.054774247047244540, -0.07405724077823318263, 0.6102362204186774219 ) ) ;
#24477=ADVANCED_FACE ( 'NONE', ( #29407 ), #44881, .T. ) ;
#24481=CARTESIAN_POINT ( 'NONE',  ( -0.6971942568897648851, -0.07405724077823297447, 1.387795275536786610 ) ) ;
#24482=CARTESIAN_POINT ( 'NONE',  ( -1.033464566929133799, 0.000000000000000000, 0.4035433070866141780 ) ) ;
#24490=CARTESIAN_POINT ( 'NONE',  ( 0.9412147342319837628, -0.1574803149606297803, 1.616633858267715773 ) ) ;
#24491=CARTESIAN_POINT ( 'NONE',  ( 0.8759842519685039353, -0.1574803149606299191, 0.3937007874015748254 ) ) ;
#24493=CARTESIAN_POINT ( 'NONE',  ( 0.8759842519685039353, 0.1787899950787401882, 1.409940944828126153 ) ) ;
#24497=CARTESIAN_POINT ( 'NONE',  ( -0.8759842519685039353, 0.000000000000000000, 0.000000000000000000 ) ) ;
#24499=CARTESIAN_POINT ( 'NONE',  ( 1.054774247047244540, -0.07405724077823318263, 1.673228346402929834 ) ) ;
#24500=CARTESIAN_POINT ( 'NONE',  ( 0.7495606340400177148, 0.1264236179284866091, 0.3124999999462365619 ) ) ;
#24503=CARTESIAN_POINT ( 'NONE',  ( 0.8759842519685039353, 0.000000000000000000, 4.498031496062992574 ) ) ;
#24504=CARTESIAN_POINT ( 'NONE',  ( 0.6971942568897626646, 0.07405724077823318263, 0.4724409448281262636 ) ) ;
#24505=CARTESIAN_POINT ( 'NONE',  ( -0.8759842519685039353, -0.1787899950787401882, 0.7652559054580472253 ) ) ;
#24509=CARTESIAN_POINT ( 'NONE',  ( -0.8262250934091986965, -0.1657888017163012262, 1.987284192870486521 ) ) ;
#24510=CARTESIAN_POINT ( 'NONE',  ( 0.8019270111902717657, 0.1787899950787401604, 1.692913385773008539 ) ) ;
#24512=CARTESIAN_POINT ( 'NONE',  ( -0.8107537697050254399, -0.1574803149606297803, 1.808562992125984481 ) ) ;
#24513=CARTESIAN_POINT ( 'NONE',  ( 1.002407869896990045, 0.1264236179284866091, 0.4207677164816693294 ) ) ;
#24515=ORIENTED_EDGE ( 'NONE', *, *, #33323, .T. ) ;
#24518=CARTESIAN_POINT ( 'NONE',  ( 1.002407869896990045, -0.1264236179284866091, 0.6077755904974173617 ) ) ;
#24520=CARTESIAN_POINT ( 'NONE',  ( 0.7895178597430446699, -0.1388632226133483527, 0.03936991021426686221 ) ) ;
#24521=CARTESIAN_POINT ( 'NONE',  ( -0.7185039370078746268, -0.06523048226347956391, 0.9276574802074332160 ) ) ;
#24522=CARTESIAN_POINT ( 'NONE',  ( -1.002407869896990045, -0.1264236179284866091, 1.513287401521039355 ) ) ;
#24525=CARTESIAN_POINT ( 'NONE',  ( 1.054774247047244096, 0.000000000000000000, 1.011318897584031484 ) ) ;
#24526=VERTEX_POINT ( 'NONE', #14736 ) ;
#24528=CARTESIAN_POINT ( 'NONE',  ( 0.7495606340400177148, -0.1264236179284866091, 1.857775590497417362 ) ) ;
#24529=CARTESIAN_POINT ( 'NONE',  ( -0.9873396505805591694, -0.1113553986120547346, 1.343503937007874072 ) ) ;
#24530=CARTESIAN_POINT ( 'NONE',  ( -0.9500414927467378812, -0.1787899950787401604, 0.9202755904974182499 ) ) ;
#24533=CARTESIAN_POINT ( 'NONE',  ( 0.8759842519685039353, 0.1787899950787401882, 0.1156496062454492185 ) ) ;
#24534=EDGE_CURVE ( 'NONE', #24379, #37983, #14372, .T. ) ;
#24536=CARTESIAN_POINT ( 'NONE',  ( 0.9873396505805591694, 0.1113553986120547346, 1.619094488081448846 ) ) ;
#24537=ORIENTED_EDGE ( 'NONE', *, *, #15774, .F. ) ;
#24539=CARTESIAN_POINT ( 'NONE',  ( -0.7495606340400177148, 0.1264236179284866091, 1.651082677111590513 ) ) ;
#24543=CARTESIAN_POINT ( 'NONE',  ( -0.7185039370078739607, 1.928577636452523993E-17, 0.7775590551181102983 ) ) ;
#24545=VERTEX_POINT ( 'NONE', #11148 ) ;
#24549=CARTESIAN_POINT ( 'NONE',  ( 1.033464566929134687, 0.06523048226347956391, 1.862696850393700254 ) ) ;
#24552=EDGE_CURVE ( 'NONE', #19233, #25854, #29396, .T. ) ;
#24555=CARTESIAN_POINT ( 'NONE',  ( -1.054774247047244540, -0.07405724077823318263, 0.3001968503399373711 ) ) ;
#24559=CARTESIAN_POINT ( 'NONE',  ( 0.6971942568897637749, 2.189545951927499583E-17, 1.109744094434425232 ) ) ;
#24560=CARTESIAN_POINT ( 'NONE',  ( 1.002407869896990045, 0.1264236179284866091, 1.523129921206078707 ) ) ;
#24561=CARTESIAN_POINT ( 'NONE',  ( 0.9500414927467377701, -0.1787899950787401604, 0.1722440944344254543 ) ) ;
#24563=VECTOR ( 'NONE', #2986, 39.37007874015748143 ) ;
#24564=CARTESIAN_POINT ( 'NONE',  ( -0.7185039370078739607, 1.928577636452523993E-17, 1.919291338582677309 ) ) ;
#24565=CARTESIAN_POINT ( 'NONE',  ( 1.033464566929134687, -0.06523048226347956391, 1.700295275590550936 ) ) ;
#24567=CARTESIAN_POINT ( 'NONE',  ( 1.033464566929133799, 0.000000000000000000, 0.3937007872940480047 ) ) ;
#24569=FACE_OUTER_BOUND ( 'NONE', #25299, .T. ) ;
#24570=CARTESIAN_POINT ( 'NONE',  ( -0.8107537697050253289, 0.1574803149606300301, 1.783956692805858779 ) ) ;
#24571=CARTESIAN_POINT ( 'NONE',  ( 0.6971942568897637749, 2.189545951927499583E-17, 0.1599409448281264023 ) ) ;
#24572=( BOUNDED_CURVE ( )  B_SPLINE_CURVE ( 2, ( #23581, #8477, #23112, #8718, #1762, #9195, #27447, #37725, #23354 ),
 .UNSPECIFIED., .F., .T. ) 
 B_SPLINE_CURVE_WITH_KNOTS ( ( 3, 2, 2, 2, 3 ),
 ( 0.4199999999999999845, 0.4224999999999999867, 0.4249999999999999889, 0.4274999999999999911, 0.4299999999999999933 ),
 .UNSPECIFIED. ) 
 CURVE ( )  GEOMETRIC_REPRESENTATION_ITEM ( )  RATIONAL_B_SPLINE_CURVE ( ( 1.000000000000000000, 0.9238795325112869605, 1.000000000000000000, 0.9238795325112869605, 1.000000000000000000, 0.9238795325112869605, 1.000000000000000000, 0.9238795325112869605, 1.000000000000000000 ) ) 
 REPRESENTATION_ITEM ( '' )  ) ;
#24574=CARTESIAN_POINT ( 'NONE',  ( 0.9500414927467377701, -0.1787899950787401604, 1.117125984198203970 ) ) ;
#24575=CARTESIAN_POINT ( 'NONE',  ( -1.033464566929134687, 0.06523048226347956391, 1.813484251860976171 ) ) ;
#24576=CARTESIAN_POINT ( 'NONE',  ( 1.033464566929133799, 0.000000000000000000, 0.6692913384751496553 ) ) ;
#24577=CARTESIAN_POINT ( 'NONE',  ( 0.9873396505805591694, 0.1113553986120547346, 0.4379921258767252024 ) ) ;
#24581=CARTESIAN_POINT ( 'NONE',  ( 1.027827790200348312, 0.05458466606556203887, 0.03937234633583642368 ) ) ;
#24582=CARTESIAN_POINT ( 'NONE',  ( -0.7185039370078746268, -0.06523048226347956391, 0.4552165353255435698 ) ) ;
#24584=CARTESIAN_POINT ( 'NONE',  ( 0.7495606340400177148, 0.1264236179284866091, 1.336122047190330786 ) ) ;
#24585=CARTESIAN_POINT ( 'NONE',  ( -0.7185039370078739607, 1.928577636452523993E-17, 0.1082677165354330728 ) ) ;
#24588=CARTESIAN_POINT ( 'NONE',  ( 0.9873396505805591694, 0.1113553986120547346, 0.4379921258767252024 ) ) ;
#24590=CARTESIAN_POINT ( 'NONE',  ( 0.7646288533564489232, -0.1113553986120547346, 0.5068897637795275468 ) ) ;
#24591=CARTESIAN_POINT ( 'NONE',  ( 0.9500414927467378812, 0.1787899950787401604, 0.4675196849856070869 ) ) ;
#24594=CARTESIAN_POINT ( 'NONE',  ( -1.002407869896990045, -0.1264236179284866091, 0.9276574802611967652 ) ) ;
#24595=CARTESIAN_POINT ( 'NONE',  ( -1.033464566929134687, -0.06523048226347956391, 0.04675196850393704279 ) ) ;
#24597=CARTESIAN_POINT ( 'NONE',  ( -0.8019270111902716547, 0.1787899950787401604, 1.136811023568283119 ) ) ;
#24598=CARTESIAN_POINT ( 'NONE',  ( -0.6971942568897637749, 2.189545951927499583E-17, 0.6766732282926929409 ) ) ;
#24599=AXIS2_PLACEMENT_3D ( 'NONE', #33144, #14438, #3160 ) ;
#24605=ORIENTED_EDGE ( 'NONE', *, *, #20502, .F. ) ;
#24606=CARTESIAN_POINT ( 'NONE',  ( -0.7646288533564489232, -0.1113553986120547346, 1.727362204724409489 ) ) ;
#24608=AXIS2_PLACEMENT_3D ( 'NONE', #7438, #40482, #235 ) ;
#24609=AXIS2_PLACEMENT_3D ( 'NONE', #32727, #47072, #10673 ) ;
#24610=DIRECTION ( 'NONE',  ( 1.822029033848725028E-16, 0.000000000000000000, 1.000000000000000000 ) ) ;
#24611=CARTESIAN_POINT ( 'NONE',  ( -0.8759842519685039353, -0.1787899950787401882, 0.6028543306548976854 ) ) ;
#24614=CARTESIAN_POINT ( 'NONE',  ( -0.8759842519685039353, 0.1787899950787401882, 1.690452755851748146 ) ) ;
#24621=CARTESIAN_POINT ( 'NONE',  ( -1.033464566929133799, 0.000000000000000000, 1.377952755797984263 ) ) ;
#24624=FACE_OUTER_BOUND ( 'NONE', #39883, .T. ) ;
#24628=CARTESIAN_POINT ( 'NONE',  ( 0.7646288533564489232, -0.1113553986120547346, 1.215551181102362266 ) ) ;
#24629=CARTESIAN_POINT ( 'NONE',  ( -0.9412147342319837628, 0.1574803149606300301, 1.267224409341291436 ) ) ;
#24633=CARTESIAN_POINT ( 'NONE',  ( 0.8759842519685039353, 0.1787899950787401882, 0.6619094487651338010 ) ) ;
#24634=CARTESIAN_POINT ( 'NONE',  ( 1.033464566929134687, -0.06523048226347956391, 0.2731299211523157133 ) ) ;
#24638=CARTESIAN_POINT ( 'NONE',  ( -0.7646288533564489232, -0.1113553986120547346, 1.058070866141732402 ) ) ;
#24639=CARTESIAN_POINT ( 'NONE',  ( 0.8759842519685039353, -0.1574803149606299191, 1.732283464566929165 ) ) ;
#24643=CARTESIAN_POINT ( 'NONE',  ( 0.6971942568897626646, -0.07405724077823297447, 0.7923228345919055560 ) ) ;
#24645=CYLINDRICAL_SURFACE ( 'NONE', #11166, 0.1574803149606299191 ) ;
#24646=CARTESIAN_POINT ( 'NONE',  ( -1.033464566929133799, 0.000000000000000000, 0.5216535433070865757 ) ) ;
#24651=CARTESIAN_POINT ( 'NONE',  ( 0.9412147342319837628, 0.1574803149606300301, 1.267224409341291436 ) ) ;
#24653=CARTESIAN_POINT ( 'NONE',  ( -1.002407869896990045, -0.1264236179284866091, 1.911909448765133801 ) ) ;
#24655=LINE ( 'NONE', #16989, #34407 ) ;
#24657=CARTESIAN_POINT ( 'NONE',  ( -1.054774247047244540, 0.07405724077823318263, 1.958661417269071947 ) ) ;
#24658=CARTESIAN_POINT ( 'NONE',  ( -1.054774247047244540, -0.07405724077823318263, 1.555118110182455382 ) ) ;
#24659=CARTESIAN_POINT ( 'NONE',  ( 0.8759842519685039353, 0.1787899950787401882, 0.8636811023084409733 ) ) ;
#24660=CARTESIAN_POINT ( 'NONE',  ( -0.7495606340400177148, -0.1264236179284866091, 1.031003936954110189 ) ) ;
#24661=CARTESIAN_POINT ( 'NONE',  ( -0.9500414927467378812, -0.1787899950787401604, 0.1771653542769452139 ) ) ;
#24662=CARTESIAN_POINT ( 'NONE',  ( -0.7646288533564489232, -0.1113553986120547346, 1.796259842412157415 ) ) ;
#24663=CARTESIAN_POINT ( 'NONE',  ( -0.6971942568897648851, 0.07405724077823318263, 1.855314960576157635 ) ) ;
#24664=CARTESIAN_POINT ( 'NONE',  ( -0.9412147342319837628, 0.1574803149606300301, 1.828248031496063630 ) ) ;
#24669=CARTESIAN_POINT ( 'NONE',  ( -1.054774247047244540, 0.07405724077823318263, 0.1033464566391498751 ) ) ;
#24671=CARTESIAN_POINT ( 'NONE',  ( -1.054774247047244096, 0.000000000000000000, 1.247539370024976391 ) ) ;
#24678=CARTESIAN_POINT ( 'NONE',  ( -0.9873396505805591694, 0.1113553986120547346, 1.540354330601133803 ) ) ;
#24680=CARTESIAN_POINT ( 'NONE',  ( -0.8759842519685039353, -0.1574803149606299191, 0.2362204724409449064 ) ) ;
#24681=CARTESIAN_POINT ( 'NONE',  ( -0.9873396505805591694, 0.1113553986120547346, 0.8021653543307086798 ) ) ;
#24683=CARTESIAN_POINT ( 'NONE',  ( 0.7185039370078746268, -0.06523048226347956391, 1.872539369971213841 ) ) ;
#24685=CARTESIAN_POINT ( 'NONE',  ( 1.033464566929134687, -0.06523048226347956391, 0.7947834645669291653 ) ) ;
#24689=CARTESIAN_POINT ( 'NONE',  ( 0.9412147342319837628, -0.1574803149606297803, 0.1500984250893234451 ) ) ;
#24690=CARTESIAN_POINT ( 'NONE',  ( -0.8759842519685039353, 0.1574803149606299191, 1.584645669183810890 ) ) ;
#24691=CARTESIAN_POINT ( 'NONE',  ( -0.8759842519685039353, -0.1574803149606299191, 1.181102362204724310 ) ) ;
#24695=CARTESIAN_POINT ( 'NONE',  ( -0.6971942568897637749, 2.189545951927499583E-17, 1.931594488135212728 ) ) ;
#24697=CARTESIAN_POINT ( 'NONE',  ( -0.6971942568897648851, -0.07405724077823297447, 1.466535433017102763 ) ) ;
#24698=CARTESIAN_POINT ( 'NONE',  ( 0.8019270111902717657, 0.1787899950787401604, 1.535433070812378675 ) ) ;
#24700=CARTESIAN_POINT ( 'NONE',  ( -0.8759842519685039353, 0.1787899950787401882, 0.5880905511273386566 ) ) ;
#24702=CARTESIAN_POINT ( 'NONE',  ( 1.033464566929133799, 0.000000000000000000, 0.9153543307086614567 ) ) ;
#24703=CARTESIAN_POINT ( 'NONE',  ( 1.054774247047244540, 0.07405724077823318263, 0.7775590550643457499 ) ) ;
#24704=CARTESIAN_POINT ( 'NONE',  ( -0.9500414927467377701, 0.1787899950787401604, 0.6200787401037166635 ) ) ;
#24709=CARTESIAN_POINT ( 'NONE',  ( -0.6971942568897648851, 0.07405724077823318263, 1.461614173174583753 ) ) ;
#24711=CARTESIAN_POINT ( 'NONE',  ( -0.8759842519685039353, -0.1574803149606299191, 1.496062992125984259 ) ) ;
#24713=CARTESIAN_POINT ( 'NONE',  ( -0.7185039370078746268, -0.06523048226347956391, 0.4256889763779528324 ) ) ;
#24714=CARTESIAN_POINT ( 'NONE',  ( 0.6971942568897648851, 0.07405724077823318263, 1.304133858213953667 ) ) ;
#24716=VERTEX_POINT ( 'NONE', #28288 ) ;
#24719=ORIENTED_EDGE ( 'NONE', *, *, #12733, .T. ) ;
#24723=CARTESIAN_POINT ( 'NONE',  ( 0.6971942568897648851, -0.07405724077823297447, 1.422244094434426120 ) ) ;
#24725=CARTESIAN_POINT ( 'NONE',  ( -1.033464566929134687, -0.06523048226347956391, 1.149114173228346969 ) ) ;
#24730=DIRECTION ( 'NONE',  ( 0.000000000000000000, 0.000000000000000000, -1.000000000000000000 ) ) ;
#24735=CARTESIAN_POINT ( 'NONE',  ( -0.7646288533564489232, -0.1113553986120547346, 1.481299212490897466 ) ) ;
#24736=CARTESIAN_POINT ( 'NONE',  ( 0.6971942568897626646, -0.07405724077823297447, 0.5954724408911187261 ) ) ;
#24737=( BOUNDED_CURVE ( )  B_SPLINE_CURVE ( 2, ( #13249, #37932, #45557, #23779, #9408, #4843, #5320, #27878, #19707 ),
 .UNSPECIFIED., .F., .T. ) 
 B_SPLINE_CURVE_WITH_KNOTS ( ( 3, 2, 2, 2, 3 ),
 ( 0.6800000000000000488, 0.6824999999999999956, 0.6850000000000000533, 0.6875000000000000000, 0.6899999999999999467 ),
 .UNSPECIFIED. ) 
 CURVE ( )  GEOMETRIC_REPRESENTATION_ITEM ( )  RATIONAL_B_SPLINE_CURVE ( ( 1.000000000000000000, 0.9238795325112869605, 1.000000000000000000, 0.9238795325112869605, 1.000000000000000000, 0.9238795325112869605, 1.000000000000000000, 0.9238795325112799661, 1.000000000000000000 ) ) 
 REPRESENTATION_ITEM ( '' )  ) ;
#24738=CARTESIAN_POINT ( 'NONE',  ( -0.8759842519685039353, 0.1787899950787401882, 0.9424212597887559051 ) ) ;
#24743=CARTESIAN_POINT ( 'NONE',  ( -0.7185039370078766252, -0.06523048226348168721, 1.242618110128693276 ) ) ;
#24744=CARTESIAN_POINT ( 'NONE',  ( 0.8019270111902717657, -0.1787899950787401604, 1.628937007820252303 ) ) ;
#24745=CARTESIAN_POINT ( 'NONE',  ( 0.8759842519685039353, -0.1787899950787401882, 1.980807086560409491 ) ) ;
#24747=CARTESIAN_POINT ( 'NONE',  ( 0.8019270111902716547, -0.1787899950787401604, 0.5216535432533228045 ) ) ;
#24750=CARTESIAN_POINT ( 'NONE',  ( 0.9412147342319837628, 0.1574803149606300301, 0.01722440944881892255 ) ) ;
#24753=CARTESIAN_POINT ( 'NONE',  ( 0.7495606340400177148, 0.1264236179284866091, 0.5880905511273386566 ) ) ;
#24755=CARTESIAN_POINT ( 'NONE',  ( 1.002407869896990045, -0.1264236179284866091, 0.1402559054580474474 ) ) ;
#24757=CARTESIAN_POINT ( 'NONE',  ( 0.8019270111902716547, 0.1787899950787401604, 0.5462598424659214080 ) ) ;
#24758=CARTESIAN_POINT ( 'NONE',  ( 0.8759842519685039353, 0.1574803149606299191, 1.151574803042078710 ) ) ;
#24759=ORIENTED_EDGE ( 'NONE', *, *, #12746, .F. ) ;
#24760=CARTESIAN_POINT ( 'NONE',  ( 0.9873396505805591694, -0.1113553986120547346, 0.4379921259842519676 ) ) ;
#24761=CARTESIAN_POINT ( 'NONE',  ( 0.8759842519685039353, -0.1787899950787401882, 1.119586614119464585 ) ) ;
#24763=CARTESIAN_POINT ( 'NONE',  ( -1.033464566929133799, 0.000000000000000000, 0.6692913384751496553 ) ) ;
#24764=CARTESIAN_POINT ( 'NONE',  ( 0.7185039370078746268, -0.06523048226347956391, 1.488681102362205300 ) ) ;
#24765=CARTESIAN_POINT ( 'NONE',  ( 0.8759842519685039353, 0.1787899950787401882, 1.764271653489543290 ) ) ;
#24766=CARTESIAN_POINT ( 'NONE',  ( -0.8107537697050253289, 0.1574803149606300301, 1.400098425196850904 ) ) ;
#24767=CARTESIAN_POINT ( 'NONE',  ( -0.7495606340400177148, -0.1264236179284866091, 0.8735236219934803259 ) ) ;
#24769=CARTESIAN_POINT ( 'NONE',  ( -0.8759842519685039353, -0.1574803149606299191, 0.03937007874015843040 ) ) ;
#24770=CARTESIAN_POINT ( 'NONE',  ( 1.054774247047244540, 0.07405724077823318263, 0.3051181101824569919 ) ) ;
#24771=CARTESIAN_POINT ( 'NONE',  ( 0.8107537697050253289, 0.1574803149606300301, 1.508366141624757129 ) ) ;
#24775=CARTESIAN_POINT ( 'NONE',  ( 0.6971942568897626646, -0.07405724077823297447, 0.8366141731745828647 ) ) ;
#24776=CARTESIAN_POINT ( 'NONE',  ( -0.7495606340400177148, -0.1264236179284866091, 1.700295275536787498 ) ) ;
#24777=ORIENTED_EDGE ( 'NONE', *, *, #4362, .T. ) ;
#24786=CARTESIAN_POINT ( 'NONE',  ( -0.8107537697050254399, -0.1574803149606297803, 1.454232283464566677 ) ) ;
#24788=CARTESIAN_POINT ( 'NONE',  ( 0.7495606340400177148, 0.1264236179284866091, 0.03690944876513417572 ) ) ;
#24792=EDGE_CURVE ( 'NONE', #41784, #46518, #37748, .T. ) ;
#24793=CARTESIAN_POINT ( 'NONE',  ( -0.8759842519685039353, -0.1787899950787401882, 0.3715551180564728440 ) ) ;
#24796=CARTESIAN_POINT ( 'NONE',  ( -0.7226907848552633906, 0.05979789147634147206, 1.982109394411383230 ) ) ;
#24798=CARTESIAN_POINT ( 'NONE',  ( 0.7495606340400177148, 0.1264236179284866091, 1.183562992072220599 ) ) ;
#24799=CARTESIAN_POINT ( 'NONE',  ( 0.6971942568897648851, -0.07405724077823297447, 1.540354330654897685 ) ) ;
#24801=CARTESIAN_POINT ( 'NONE',  ( 0.9873396505805591694, -0.1113553986120547346, 1.530511810916094451 ) ) ;
#24803=CARTESIAN_POINT ( 'NONE',  ( -0.8107537697050253289, 0.1574803149606300301, 1.665846456585386548 ) ) ;
#24804=CARTESIAN_POINT ( 'NONE',  ( 0.8759842519685039353, 0.1787899950787401882, 0.2288385826234019815 ) ) ;
#24805=CARTESIAN_POINT ( 'NONE',  ( 0.7012303660228902391, 0.004218421126415324365, 0.03936661617635339033 ) ) ;
#24806=CARTESIAN_POINT ( 'NONE',  ( 0.6971942568897648851, -0.07405724077823297447, 1.107283464513165727 ) ) ;
#24807=CARTESIAN_POINT ( 'NONE',  ( -0.9412147342319837628, 0.1574803149606300301, 1.946358267716537638 ) ) ;
#24808=CARTESIAN_POINT ( 'NONE',  ( 0.8019270111902716547, -0.1787899950787401604, 1.904527559001354398 ) ) ;
#24809=CARTESIAN_POINT ( 'NONE',  ( 0.7185039370078739607, 1.928577636452523993E-17, 0.5708661416247566844 ) ) ;
#24812=CARTESIAN_POINT ( 'NONE',  ( 0.9403060794343187645, 0.1577454412895565594, 0.03936873803210047540 ) ) ;
#24813=CARTESIAN_POINT ( 'NONE',  ( -0.7185039370078746268, 0.06523048226347956391, 0.3321850392625518844 ) ) ;
#24815=CARTESIAN_POINT ( 'NONE',  ( 0.7495606340400177148, 0.1264236179284866091, 1.414862204670645829 ) ) ;
#24816=CARTESIAN_POINT ( 'NONE',  ( -0.8107537697050254399, 0.1574803149606300301, 1.636318897637794922 ) ) ;
#24817=CARTESIAN_POINT ( 'NONE',  ( -0.9412147342319837628, -0.1574803149606297803, 0.2288385825696384601 ) ) ;
#24820=CARTESIAN_POINT ( 'NONE',  ( 0.9412147342319837628, 0.1574803149606300301, 0.4404527557979849850 ) ) ;
#24822=CYLINDRICAL_SURFACE ( 'NONE', #41266, 0.1574803149606299191 ) ;
#24825=CARTESIAN_POINT ( 'NONE',  ( 1.002407869896990045, 0.1264236179284866091, 0.6225393700249762796 ) ) ;
#24827=CARTESIAN_POINT ( 'NONE',  ( -1.054774247047244096, 0.000000000000000000, 1.321358267662771757 ) ) ;
#24830=CARTESIAN_POINT ( 'NONE',  ( -1.002407869896990045, -0.1264236179284866091, 1.203248031442299304 ) ) ;
#24831=CARTESIAN_POINT ( 'NONE',  ( -0.8759842519685039353, 0.1787899950787401882, 1.961122047190330786 ) ) ;
#24832=ORIENTED_EDGE ( 'NONE', *, *, #19906, .F. ) ;
#24833=EDGE_CURVE ( 'NONE', #14468, #30794, #42626, .T. ) ;
#24834=CARTESIAN_POINT ( 'NONE',  ( -1.054774247047244540, 0.07405724077823318263, 1.048228346402928723 ) ) ;
#24835=CARTESIAN_POINT ( 'NONE',  ( -0.8759842519685039353, -0.1787899950787401882, 0.8439960629383622681 ) ) ;
#24840=VERTEX_POINT ( 'NONE', #43345 ) ;
#24845=ORIENTED_EDGE ( 'NONE', *, *, #27252, .F. ) ;
#24847=CARTESIAN_POINT ( 'NONE',  ( -0.7495606340400177148, 0.1264236179284866091, 0.7062007873478109987 ) ) ;
#24848=CARTESIAN_POINT ( 'NONE',  ( 0.9412147342319837628, 0.1574803149606300301, 1.345964566821607589 ) ) ;
#24850=CARTESIAN_POINT ( 'NONE',  ( -0.6971942568897637749, 2.189545951927499583E-17, 1.660925196796630088 ) ) ;
#24851=CARTESIAN_POINT ( 'NONE',  ( -0.9412147342319837628, -0.1574803149606297803, 1.134350393593259732 ) ) ;
#24852=( BOUNDED_CURVE ( )  B_SPLINE_CURVE ( 2, ( #4538, #706, #16083, #23017, #23505, #38108, #15364, #19174, #30014 ),
 .UNSPECIFIED., .F., .T. ) 
 B_SPLINE_CURVE_WITH_KNOTS ( ( 3, 2, 2, 2, 3 ),
 ( 0.1199999999999999956, 0.1224999999999999978, 0.1250000000000000000, 0.1275000000000000022, 0.1300000000000000044 ),
 .UNSPECIFIED. ) 
 CURVE ( )  GEOMETRIC_REPRESENTATION_ITEM ( )  RATIONAL_B_SPLINE_CURVE ( ( 1.000000000000000000, 0.9238795325112869605, 1.000000000000000000, 0.9238795325112869605, 1.000000000000000000, 0.9238795325112869605, 1.000000000000000000, 0.9238795325112869605, 1.000000000000000000 ) ) 
 REPRESENTATION_ITEM ( '' )  ) ;
#24853=CARTESIAN_POINT ( 'NONE',  ( -1.033464566929133799, 0.000000000000000000, 0.1181102361129454797 ) ) ;
#24858=CARTESIAN_POINT ( 'NONE',  ( 0.9500414927467378812, -0.1787899950787401604, 0.6889763778989935750 ) ) ;
#24861=CYLINDRICAL_SURFACE ( 'NONE', #23857, 0.1574803149606299191 ) ;
#24862=CARTESIAN_POINT ( 'NONE',  ( 1.033464566929134687, 0.06523048226347956391, 1.272145669291338432 ) ) ;
#24863=CARTESIAN_POINT ( 'NONE',  ( 0.7516165683754897353, -0.1160273600567148788, 1.985629433047727543 ) ) ;
#24864=CARTESIAN_POINT ( 'NONE',  ( -0.7185039370078739607, 1.928577636452523993E-17, 0.2559055117034968463 ) ) ;
#24867=CARTESIAN_POINT ( 'NONE',  ( 1.054774247047244096, 0.000000000000000000, 0.6520669290800944484 ) ) ;
#24868=DIRECTION ( 'NONE',  ( 0.000000000000000000, 0.000000000000000000, -1.000000000000000000 ) ) ;
#24873=CARTESIAN_POINT ( 'NONE',  ( 0.5314960629921260393, 0.000000000000000000, 4.842519685039370358 ) ) ;
#24875=VECTOR ( 'NONE', #25329, 39.37007874015748143 ) ;
#24878=CARTESIAN_POINT ( 'NONE',  ( 0.8759842519685039353, 0.1787899950787401882, 0.9768700786863937502 ) ) ;
#24880=CARTESIAN_POINT ( 'NONE',  ( 0.7646288533564489232, -0.1113553986120547346, 0.6938976376877481478 ) ) ;
#24884=( BOUNDED_CURVE ( )  B_SPLINE_CURVE ( 2, ( #21264, #46660, #21499, #13843, #43780, #32793, #36134, #24634, #39232 ),
 .UNSPECIFIED., .F., .T. ) 
 B_SPLINE_CURVE_WITH_KNOTS ( ( 3, 2, 2, 2, 3 ),
 ( 0.1100000000000000006, 0.1125000000000000028, 0.1150000000000000050, 0.1174999999999999933, 0.1199999999999999956 ),
 .UNSPECIFIED. ) 
 CURVE ( )  GEOMETRIC_REPRESENTATION_ITEM ( )  RATIONAL_B_SPLINE_CURVE ( ( 1.000000000000000000, 0.9238795325112869605, 1.000000000000000000, 0.9238795325112869605, 1.000000000000000000, 0.9238795325112869605, 1.000000000000000000, 0.9238795325112869605, 1.000000000000000000 ) ) 
 REPRESENTATION_ITEM ( '' )  ) ;
#24886=CARTESIAN_POINT ( 'NONE',  ( -0.6971942568897637749, 2.189545951927499583E-17, 0.1205708660879689087 ) ) ;
#24888=ORIENTED_EDGE ( 'NONE', *, *, #31189, .F. ) ;
#24889=CARTESIAN_POINT ( 'NONE',  ( 0.6971942568897648851, -0.07405724077823297447, 1.978346456639149320 ) ) ;
#24891=CARTESIAN_POINT ( 'NONE',  ( -0.6971942568897648851, 0.07405724077823318263, 1.894685039316315489 ) ) ;
#24892=CARTESIAN_POINT ( 'NONE',  ( 1.002407869896990045, -0.1264236179284866091, 0.8489173227808819444 ) ) ;
#24893=EDGE_CURVE ( 'NONE', #12346, #13468, #33985, .T. ) ;
#24894=CARTESIAN_POINT ( 'NONE',  ( -1.054774247047244540, 0.07405724077823318263, 1.087598425143086578 ) ) ;
#24895=CARTESIAN_POINT ( 'NONE',  ( -1.002407869896990045, 0.1264236179284866091, 0.2288385826234019815 ) ) ;
#24898=CARTESIAN_POINT ( 'NONE',  ( -0.8019270111902717657, 0.1787899950787401604, 1.889763779473794258 ) ) ;
#24899=CARTESIAN_POINT ( 'NONE',  ( -1.002407869896990045, -0.1264236179284866091, 0.1402559054580474474 ) ) ;
#24900=CARTESIAN_POINT ( 'NONE',  ( 0.7646288533564489232, 0.1113553986120547346, 0.3001968503937008093 ) ) ;
#24901=CARTESIAN_POINT ( 'NONE',  ( -0.9412147342319837628, 0.1574803149606300301, 1.906988188976377563 ) ) ;
#24902=CARTESIAN_POINT ( 'NONE',  ( -0.8759842519685039353, -0.1574803149606299191, 1.889763779527559251 ) ) ;
#24904=CARTESIAN_POINT ( 'NONE',  ( 0.7185039370078739607, 1.928577636452523993E-17, 1.751968503829480106 ) ) ;
#24905=CARTESIAN_POINT ( 'NONE',  ( -0.9873396505805591694, 0.1113553986120547346, 0.04429133847515007855 ) ) ;
#24909=CARTESIAN_POINT ( 'NONE',  ( -1.054774247047244540, -0.07405724077823318263, 0.1771653542769450751 ) ) ;
#24911=ORIENTED_EDGE ( 'NONE', *, *, #40650, .F. ) ;
#24912=AXIS2_PLACEMENT_3D ( 'NONE', #23732, #20590, #9354 ) ;
#24913=CARTESIAN_POINT ( 'NONE',  ( -0.9500414927467377701, -0.1787899950787401604, 1.240157480261197875 ) ) ;
#24914=ORIENTED_EDGE ( 'NONE', *, *, #5639, .T. ) ;
#24918=CARTESIAN_POINT ( 'NONE',  ( -1.033464566929133799, 0.000000000000000000, 1.535433070758614127 ) ) ;
#24920=CARTESIAN_POINT ( 'NONE',  ( -0.8107537697050253289, -0.1574803149606297803, 0.9325787400499522262 ) ) ;
#24921=CARTESIAN_POINT ( 'NONE',  ( -1.033464566929133799, 0.000000000000000000, 0.7578740157480314821 ) ) ;
#24923=CARTESIAN_POINT ( 'NONE',  ( 0.9412147342319837628, 0.1574803149606300301, 1.818405511703498068 ) ) ;
#24925=CARTESIAN_POINT ( 'NONE',  ( 0.9412147342319837628, 0.1574803149606300301, 0.7258858267716535861 ) ) ;
#24927=CARTESIAN_POINT ( 'NONE',  ( -0.7185039370078739607, 1.928577636452523993E-17, 1.092519685039370136 ) ) ;
#24930=CARTESIAN_POINT ( 'NONE',  ( 1.033464566929134687, 0.06523048226347956391, 0.2386811022546777294 ) ) ;
#24934=CARTESIAN_POINT ( 'NONE',  ( -1.033464566929133799, 0.000000000000000000, 0.6299212597349921339 ) ) ;
#24938=CARTESIAN_POINT ( 'NONE',  ( 0.7185039370078739607, 1.928577636452523993E-17, 0.9645669290263307882 ) ) ;
#24940=CARTESIAN_POINT ( 'NONE',  ( -0.8019270111902717657, -0.1787899950787401604, 0.4429133857730075952 ) ) ;
#24942=CARTESIAN_POINT ( 'NONE',  ( -0.7495606340400177148, -0.1264236179284866091, 1.587106299158834721 ) ) ;
#24943=CARTESIAN_POINT ( 'NONE',  ( 0.7495606340400177148, -0.1264236179284866091, 1.508366141678519678 ) ) ;
#24946=CARTESIAN_POINT ( 'NONE',  ( -1.033464566929133799, 0.000000000000000000, 0.4822834645669291653 ) ) ;
#24947=CARTESIAN_POINT ( 'NONE',  ( -0.9500414927467378812, 0.1787899950787401604, 0.6643700786863929730 ) ) ;
#24948=FACE_OUTER_BOUND ( 'NONE', #12013, .T. ) ;
#24949=CARTESIAN_POINT ( 'NONE',  ( -0.8019270111902716547, -0.1787899950787401604, 0.7185039369541108556 ) ) ;
#24953=CARTESIAN_POINT ( 'NONE',  ( -0.6971942568897648851, 0.07405724077823318263, 1.382874015694268044 ) ) ;
#24954=ORIENTED_EDGE ( 'NONE', *, *, #28058, .T. ) ;
#24955=CARTESIAN_POINT ( 'NONE',  ( -0.9412147342319837628, 0.1574803149606300301, 0.4502952755905510474 ) ) ;
#24956=CARTESIAN_POINT ( 'NONE',  ( 1.054774247047244540, 0.07405724077823318263, 1.368110236166710125 ) ) ;
#24958=CARTESIAN_POINT ( 'NONE',  ( -1.033464566929133799, 0.000000000000000000, 1.584645669291338654 ) ) ;
#24959=ORIENTED_EDGE ( 'NONE', *, *, #37372, .T. ) ;
#24962=ORIENTED_EDGE ( 'NONE', *, *, #15700, .F. ) ;
#24963=CARTESIAN_POINT ( 'NONE',  ( -0.8759842519685039353, 0.000000000000000000, 0.000000000000000000 ) ) ;
#24971=CARTESIAN_POINT ( 'NONE',  ( 1.054774247047244096, 0.000000000000000000, 0.2583661416785200671 ) ) ;
#24977=CARTESIAN_POINT ( 'NONE',  ( 1.002407869896990045, 0.1264236179284866091, 0.5782480314422993040 ) ) ;
#24978=CARTESIAN_POINT ( 'NONE',  ( -0.8759842519685039353, 0.1787899950787401882, 0.9030511810485984947 ) ) ;
#24979=CARTESIAN_POINT ( 'NONE',  ( -0.9999090329106934405, 0.1097224490248799866, 0.03937007874015842346 ) ) ;
#24983=CARTESIAN_POINT ( 'NONE',  ( 1.002407869896990045, -0.1264236179284866091, 1.596948818843874074 ) ) ;
#24984=CARTESIAN_POINT ( 'NONE',  ( -1.033464566929133799, 0.000000000000000000, 1.190944881889763884 ) ) ;
#24989=CARTESIAN_POINT ( 'NONE',  ( 1.033464566929133799, 0.000000000000000000, 0.7874015746956221085 ) ) ;
#24992=CARTESIAN_POINT ( 'NONE',  ( 0.6971942568897637749, 2.189545951927499583E-17, 0.6323818897100157432 ) ) ;
#24994=CARTESIAN_POINT ( 'NONE',  ( 0.6971942568897626646, 0.07405724077823318263, 0.08366141726907129483 ) ) ;
#24995=CARTESIAN_POINT ( 'NONE',  ( -0.8759842519685039353, -0.1574803149606299191, 0.9350393699712126194 ) ) ;
#24996=CARTESIAN_POINT ( 'NONE',  ( -0.6971942568897637749, 2.189545951927499583E-17, 1.537893700733637736 ) ) ;
#24998=CARTESIAN_POINT ( 'NONE',  ( 0.9412147342319837628, -0.1574803149606297803, 0.1599409448818898405 ) ) ;
#24999=CARTESIAN_POINT ( 'NONE',  ( 0.7495606340400177148, -0.1264236179284866091, 1.154035433017102319 ) ) ;
#25001=CARTESIAN_POINT ( 'NONE',  ( -0.9873396505805591694, -0.1113553986120547346, 0.7037401573727875004 ) ) ;
#25002=CARTESIAN_POINT ( 'NONE',  ( 0.7185039370078739607, 1.928577636452523993E-17, 1.397637795168062969 ) ) ;
#25003=CARTESIAN_POINT ( 'NONE',  ( -0.8759842519685039353, 0.1787899950787401882, 0.9768700786863937502 ) ) ;
#25005=CARTESIAN_POINT ( 'NONE',  ( -0.7831748123774774362, -0.1359591512319747730, 0.03937007874015843734 ) ) ;
#25006=CARTESIAN_POINT ( 'NONE',  ( 1.002407869896990045, -0.1264236179284866091, 0.2977362204186775885 ) ) ;
#25007=CARTESIAN_POINT ( 'NONE',  ( -0.8019270111902716547, -0.1787899950787401604, 0.1673228345919057503 ) ) ;
#25008=CARTESIAN_POINT ( 'NONE',  ( -0.8019270111902717657, -0.1787899950787401604, 0.6397637794737947026 ) ) ;
#25009=CARTESIAN_POINT ( 'NONE',  ( 0.7185039370078739607, 1.928577636452523993E-17, 1.633858267609007875 ) ) ;
#25010=ORIENTED_EDGE ( 'NONE', *, *, #36320, .F. ) ;
#25013=CARTESIAN_POINT ( 'NONE',  ( 0.7495606340400177148, 0.1264236179284866091, 0.7504921259304880854 ) ) ;
#25014=CARTESIAN_POINT ( 'NONE',  ( -0.7495606340400177148, -0.1264236179284866091, 1.779035433017102319 ) ) ;
#25017=CARTESIAN_POINT ( 'NONE',  ( 0.7646288533564489232, 0.1113553986120547346, 1.323818897637795367 ) ) ;
#25019=ORIENTED_EDGE ( 'NONE', *, *, #3669, .T. ) ;
#25022=CARTESIAN_POINT ( 'NONE',  ( 1.054774247047244540, -0.07405724077823318263, 1.082677165300567346 ) ) ;
#25026=( BOUNDED_CURVE ( )  B_SPLINE_CURVE ( 2, ( #34339, #1471, #40369, #27407, #12293, #14769, #5078, #43979, #26916 ),
 .UNSPECIFIED., .F., .F. ) 
 B_SPLINE_CURVE_WITH_KNOTS ( ( 3, 2, 2, 2, 3 ),
 ( 0.9899999999999999911, 0.9925000000000000488, 0.9949999999999999956, 0.9975000000000000533, 1.000000000000000000 ),
 .UNSPECIFIED. ) 
 CURVE ( )  GEOMETRIC_REPRESENTATION_ITEM ( )  RATIONAL_B_SPLINE_CURVE ( ( 1.000000000000000000, 0.9238795325112869605, 1.000000000000000000, 0.9238795325112869605, 1.000000000000000000, 0.9238795325112869605, 1.000000000000000000, 0.9238795325112869605, 1.000000000000000000 ) ) 
 REPRESENTATION_ITEM ( '' )  ) ;
#25027=CARTESIAN_POINT ( 'NONE',  ( 0.8759842519685039353, -0.1787899950787401882, 0.05167322829269314910 ) ) ;
#25030=CARTESIAN_POINT ( 'NONE',  ( -1.054774247047244540, -0.07405724077823318263, 0.4970472440407249226 ) ) ;
#25032=CARTESIAN_POINT ( 'NONE',  ( 1.002407869896990045, -0.1264236179284866091, 1.242618110182456714 ) ) ;
#25033=CARTESIAN_POINT ( 'NONE',  ( 0.8019270111902716547, -0.1787899950787401604, 1.466535433017102763 ) ) ;
#25034=CARTESIAN_POINT ( 'NONE',  ( -0.9412147342319837628, 0.1574803149606300301, 0.5979330707586145710 ) ) ;
#25035=CARTESIAN_POINT ( 'NONE',  ( 0.7185039370078746268, 0.06523048226347956391, 1.680610236220472231 ) ) ;
#25037=CARTESIAN_POINT ( 'NONE',  ( 1.033464566929134687, 0.06523048226347956391, 0.6717519683964101596 ) ) ;
#25038=CARTESIAN_POINT ( 'NONE',  ( -0.8107537697050253289, -0.1574803149606297803, 1.798720472333418918 ) ) ;
#25039=CARTESIAN_POINT ( 'NONE',  ( 0.8759842519685039353, 0.1787899950787401882, 0.1500984251430870220 ) ) ;
#25040=CARTESIAN_POINT ( 'NONE',  ( 1.054774247047244540, 0.07405724077823318263, 1.126968503883244654 ) ) ;
#25042=CARTESIAN_POINT ( 'NONE',  ( -1.033464566929134687, -0.06523048226347956391, 1.926673228238929170 ) ) ;
#25043=CARTESIAN_POINT ( 'NONE',  ( -0.6971942568897648851, 0.07405724077823318263, 1.141732283410804349 ) ) ;
#25044=CARTESIAN_POINT ( 'NONE',  ( 0.9412147342319837628, -0.1574803149606297803, 0.4256889762704256230 ) ) ;
#25047=CARTESIAN_POINT ( 'NONE',  ( -1.033464566929133799, 0.000000000000000000, 1.112204724409448842 ) ) ;
#25048=CARTESIAN_POINT ( 'NONE',  ( 0.8692927555521646754, 0.1747984728378554065, 0.03936921762936072822 ) ) ;
#25049=CARTESIAN_POINT ( 'NONE',  ( 0.8759842519685039353, 0.1574803149606299191, 0.2952755905511810774 ) ) ;
#25050=CARTESIAN_POINT ( 'NONE',  ( -0.7185039370078739607, 1.928577636452523993E-17, 0.4133858266641267654 ) ) ;
#25051=EDGE_LOOP ( 'NONE', ( #3782, #7877, #2847, #13464 ) ) ;
#25052=CARTESIAN_POINT ( 'NONE',  ( 0.8759842519685039353, 0.1787899950787401882, 1.528051181048598384 ) ) ;
#25053=CARTESIAN_POINT ( 'NONE',  ( -0.9873396505805591694, -0.1113553986120547346, 1.776574803149606252 ) ) ;
#25058=CARTESIAN_POINT ( 'NONE',  ( 0.8107537697050254399, 0.1574803149606300301, 0.4453740156405042727 ) ) ;
#25059=ADVANCED_FACE ( 'NONE', ( #22729 ), #25402, .T. ) ;
#25060=ORIENTED_EDGE ( 'NONE', *, *, #27158, .F. ) ;
#25061=CARTESIAN_POINT ( 'NONE',  ( 1.033464566929133799, 1.928577636452524610E-17, 4.498031496062992574 ) ) ;
#25062=CARTESIAN_POINT ( 'NONE',  ( 0.6971942568897626646, -0.07405724077823297447, 0.5216535432533228045 ) ) ;
#25065=CARTESIAN_POINT ( 'NONE',  ( -0.6971942568897648851, -0.07405724077823297447, 1.112204724355684959 ) ) ;
#25066=CARTESIAN_POINT ( 'NONE',  ( -1.033464566929134687, 0.06523048226347956391, 0.09104330708661413640 ) ) ;
#25068=CARTESIAN_POINT ( 'NONE',  ( -0.8759842519685039353, -0.1787899950787401882, 1.154035433017102319 ) ) ;
#25070=CARTESIAN_POINT ( 'NONE',  ( -0.8759842519685039353, 0.1787899950787401882, 0.8243110235682834519 ) ) ;
#25071=CARTESIAN_POINT ( 'NONE',  ( -0.9500414927467378812, 0.1787899950787401604, 0.1525590550643468046 ) ) ;
#25078=ORIENTED_EDGE ( 'NONE', *, *, #18066, .F. ) ;
#25081=CARTESIAN_POINT ( 'NONE',  ( -0.6971942568897637749, 2.189545951927499583E-17, 0.5930118109698583329 ) ) ;
#25083=ORIENTED_EDGE ( 'NONE', *, *, #36431, .T. ) ;
#25084=CARTESIAN_POINT ( 'NONE',  ( -1.054774247047244540, 0.07405724077823318263, 1.801181102308441861 ) ) ;
#25086=CARTESIAN_POINT ( 'NONE',  ( -0.7185039370078746268, -0.06523048226347956391, 1.124507873908221267 ) ) ;
#25087=CARTESIAN_POINT ( 'NONE',  ( -0.9500414927467377701, -0.1787899950787401604, 0.05905511805647267048 ) ) ;
#25088=CARTESIAN_POINT ( 'NONE',  ( 1.033464566929133799, 0.000000000000000000, 0.6791338582677166613 ) ) ;
#25091=CARTESIAN_POINT ( 'NONE',  ( -0.8759842519685039353, -0.1574803149606299191, 1.446850393593259732 ) ) ;
#25092=CARTESIAN_POINT ( 'NONE',  ( 1.054774247047244540, -0.07405724077823318263, 0.7332677164816707727 ) ) ;
#25097=CARTESIAN_POINT ( 'NONE',  ( 0.8107537697050253289, 0.1574803149606300301, 1.321358267716534751 ) ) ;
#25098=CARTESIAN_POINT ( 'NONE',  ( 0.8230356807856350487, -0.1645567810599724290, 1.987220178087543143 ) ) ;
#25102=CARTESIAN_POINT ( 'NONE',  ( 0.9500414927467377701, 0.1787899950787401604, 0.6200787401037166635 ) ) ;
#25108=CYLINDRICAL_SURFACE ( 'NONE', #45934, 0.1574803149606299191 ) ;
#25110=CARTESIAN_POINT ( 'NONE',  ( 0.6971942568897637749, 2.189545951927499583E-17, 0.9473425196312755814 ) ) ;
#25117=CARTESIAN_POINT ( 'NONE',  ( -1.002407869896990045, 0.1264236179284866091, 0.06643700782025216411 ) ) ;
#25118=EDGE_LOOP ( 'NONE', ( #221, #36743, #10702, #35329 ) ) ;
#25119=CARTESIAN_POINT ( 'NONE',  ( 0.9500414927467378812, -0.1787899950787401604, 1.988188976324187562 ) ) ;
#25121=CARTESIAN_POINT ( 'NONE',  ( -0.8759842519685039353, -0.1787899950787401882, 1.906988188922614125 ) ) ;
#25122=CARTESIAN_POINT ( 'NONE',  ( -0.6971942568897637749, 2.189545951927499583E-17, 1.616633858213952779 ) ) ;
#25123=CARTESIAN_POINT ( 'NONE',  ( 1.054774247047244540, 0.07405724077823318263, 0.8956692912848198684 ) ) ;
#25125=CARTESIAN_POINT ( 'NONE',  ( -1.002407869896990045, -0.1264236179284866091, 0.4158464566391496531 ) ) ;
#25126=CARTESIAN_POINT ( 'NONE',  ( -0.9873396505805591694, -0.1113553986120547346, 1.806102362097196767 ) ) ;
#25127=CARTESIAN_POINT ( 'NONE',  ( -0.9500414927467378812, 0.1787899950787401604, 1.884842519631275026 ) ) ;
#25128=CARTESIAN_POINT ( 'NONE',  ( 1.033464566929133799, 0.000000000000000000, 0.2854330708661417804 ) ) ;
#25129=CARTESIAN_POINT ( 'NONE',  ( -0.8107537697050253289, 0.1574803149606300301, 1.911909448818899238 ) ) ;
#25130=CARTESIAN_POINT ( 'NONE',  ( -0.9412147342319837628, -0.1574803149606297803, 1.892224409448819866 ) ) ;
#25134=CARTESIAN_POINT ( 'NONE',  ( -1.054774247047244540, -0.07405724077823318263, 0.09842519679663024046 ) ) ;
#25135=( BOUNDED_CURVE ( )  B_SPLINE_CURVE ( 2, ( #29345, #7702, #10617, #22316, #39807, #21622, #36255, #40043, #3407 ),
 .UNSPECIFIED., .F., .F. ) 
 B_SPLINE_CURVE_WITH_KNOTS ( ( 3, 2, 2, 2, 3 ),
 ( 0.8499999999999999778, 0.8525000000000000355, 0.8549999999999999822, 0.8575000000000000400, 0.8599999999999999867 ),
 .UNSPECIFIED. ) 
 CURVE ( )  GEOMETRIC_REPRESENTATION_ITEM ( )  RATIONAL_B_SPLINE_CURVE ( ( 1.000000000000000000, 0.9238795325112869605, 1.000000000000000000, 0.9238795325112869605, 1.000000000000000000, 0.9238795325112869605, 1.000000000000000000, 0.9238795325112869605, 1.000000000000000000 ) ) 
 REPRESENTATION_ITEM ( '' )  ) ;
#25137=ORIENTED_EDGE ( 'NONE', *, *, #5759, .F. ) ;
#25138=CARTESIAN_POINT ( 'NONE',  ( -0.8019270111902716547, -0.1787899950787401604, 1.392716535379308285 ) ) ;
#25139=ORIENTED_EDGE ( 'NONE', *, *, #16149, .T. ) ;
#25143=CARTESIAN_POINT ( 'NONE',  ( -0.7185039370078739607, 1.928577636452523993E-17, 1.555118110128692832 ) ) ;
#25144=LENGTH_MEASURE_WITH_UNIT ( LENGTH_MEASURE( 0.02539999999999999897 ), #6207 ) ;
#25145=CARTESIAN_POINT ( 'NONE',  ( 0.7185039370078746268, -0.06523048226347956391, 0.3863188976377951445 ) ) ;
#25147=CARTESIAN_POINT ( 'NONE',  ( -0.7646288533564489232, 0.1113553986120547346, 0.8809055117034961802 ) ) ;
#25148=CARTESIAN_POINT ( 'NONE',  ( -0.9412147342319837628, -0.1574803149606297803, 0.8292322834645677876 ) ) ;
#25150=CARTESIAN_POINT ( 'NONE',  ( 0.6971942568897626646, -0.07405724077823297447, 0.4035433070328508509 ) ) ;
#25152=CARTESIAN_POINT ( 'NONE',  ( 0.8107537697050253289, 0.1574803149606300301, 1.862696850286174710 ) ) ;
#25155=CARTESIAN_POINT ( 'NONE',  ( 0.8759842519685039353, -0.1574803149606299191, 0.8661417322834645827 ) ) ;
#25157=CARTESIAN_POINT ( 'NONE',  ( -0.5314960629921259283, 1.928577636452524610E-17, 5.000000000000000000 ) ) ;
#25158=( BOUNDED_CURVE ( )  B_SPLINE_CURVE ( 2, ( #721, #15861, #15381, #18946, #15624, #30030, #44339, #11547, #8403 ),
 .UNSPECIFIED., .F., .F. ) 
 B_SPLINE_CURVE_WITH_KNOTS ( ( 3, 2, 2, 2, 3 ),
 ( 0.5200000000000000178, 0.5224999999999999645, 0.5250000000000000222, 0.5274999999999999689, 0.5300000000000000266 ),
 .UNSPECIFIED. ) 
 CURVE ( )  GEOMETRIC_REPRESENTATION_ITEM ( )  RATIONAL_B_SPLINE_CURVE ( ( 1.000000000000000000, 0.9238795325112869605, 1.000000000000000000, 0.9238795325112869605, 1.000000000000000000, 0.9238795325112869605, 1.000000000000000000, 0.9238795325112869605, 1.000000000000000000 ) ) 
 REPRESENTATION_ITEM ( '' )  ) ;
#25161=CARTESIAN_POINT ( 'NONE',  ( 0.9412147342319837628, 0.1574803149606300301, 1.513287401574803681 ) ) ;
#25162=CARTESIAN_POINT ( 'NONE',  ( 0.9873396505805591694, -0.1113553986120547346, 0.1919291337507405548 ) ) ;
#25163=ADVANCED_FACE ( 'NONE', ( #37104 ), #7405, .T. ) ;
#25168=CARTESIAN_POINT ( 'NONE',  ( 0.8759842519685039353, 0.1574803149606299191, 1.899606299105070839 ) ) ;
#25172=CARTESIAN_POINT ( 'NONE',  ( 0.7646288533564489232, 0.1113553986120547346, 0.9202755904436535905 ) ) ;
#25174=CARTESIAN_POINT ( 'NONE',  ( -1.002407869896990045, -0.1264236179284866091, 0.4502952755367874427 ) ) ;
#25175=ORIENTED_EDGE ( 'NONE', *, *, #1287, .T. ) ;
#25176=ORIENTED_EDGE ( 'NONE', *, *, #6307, .F. ) ;
#25177=CARTESIAN_POINT ( 'NONE',  ( -0.8019270111902717657, 0.1787899950787401604, 1.614173228292692386 ) ) ;
#25179=CARTESIAN_POINT ( 'NONE',  ( 0.8019270111902717657, 0.1787899950787401604, 1.614173228292692386 ) ) ;
#25181=CARTESIAN_POINT ( 'NONE',  ( -0.9500414927467378812, 0.1787899950787401604, 0.7824803149068669805 ) ) ;
#25182=CARTESIAN_POINT ( 'NONE',  ( -0.8019270111902717657, 0.1787899950787401604, 1.294291338528912982 ) ) ;
#25183=CARTESIAN_POINT ( 'NONE',  ( -0.8759842519685039353, 0.1787899950787401882, 0.6225393700249762796 ) ) ;
#25186=DIRECTION ( 'NONE',  ( 1.000000000000000000, 0.000000000000000000, -1.822029033848725275E-16 ) ) ;
#25188=CARTESIAN_POINT ( 'NONE',  ( -1.002407869896990045, 0.1264236179284866091, 1.449311023568283341 ) ) ;
#25190=CARTESIAN_POINT ( 'NONE',  ( -0.7185039370078739607, 1.928577636452523993E-17, 1.840551181102362266 ) ) ;
#25191=CARTESIAN_POINT ( 'NONE',  ( -0.8107537697050253289, 0.1574803149606300301, 0.4158464566929134243 ) ) ;
#25192=CARTESIAN_POINT ( 'NONE',  ( 0.8759842519685039353, 0.1787899950787401882, 1.414862204670645829 ) ) ;
#25200=CARTESIAN_POINT ( 'NONE',  ( 0.7646288533564489232, 0.1113553986120547346, 0.4970472440944882497 ) ) ;
#25201=ORIENTED_EDGE ( 'NONE', *, *, #2376, .T. ) ;
#25204=DIRECTION ( 'NONE',  ( 1.000000000000000000, 0.000000000000000000, -1.822029033848725275E-16 ) ) ;
#25206=CARTESIAN_POINT ( 'NONE',  ( 1.002407869896990045, 0.1264236179284866091, 0.3420275590013546751 ) ) ;
#25209=CARTESIAN_POINT ( 'NONE',  ( 0.6971942568897637749, 2.189545951927499583E-17, 0.6717519684501732646 ) ) ;
#25211=CARTESIAN_POINT ( 'NONE',  ( -0.7495606340400177148, 0.1264236179284866091, 0.9473425196312755814 ) ) ;
#25214=CARTESIAN_POINT ( 'NONE',  ( -0.7185039370078739607, 0.000000000000000000, -2.869337061179095023E-17 ) ) ;
#25216=CARTESIAN_POINT ( 'NONE',  ( 0.7185039370078739607, 1.928577636452523993E-17, 0.9645669290263307882 ) ) ;
#25217=CARTESIAN_POINT ( 'NONE',  ( 0.9500414927467378812, -0.1787899950787401604, 1.712598425143087688 ) ) ;
#25220=CARTESIAN_POINT ( 'NONE',  ( 1.054774247047244540, -0.07405724077823318263, 0.4921259841982049132 ) ) ;
#25223=ADVANCED_FACE ( 'NONE', ( #4033 ), #33543, .T. ) ;
#25227=AXIS2_PLACEMENT_3D ( 'NONE', #13622, #39249, #43074 ) ;
#25228=CARTESIAN_POINT ( 'NONE',  ( 0.6971942568897626646, 0.07405724077823318263, 0.5511811023084406402 ) ) ;
#25230=CARTESIAN_POINT ( 'NONE',  ( 0.8759842519685039353, 0.1787899950787401882, 0.1550196849856066983 ) ) ;
#25231=CARTESIAN_POINT ( 'NONE',  ( -0.9873396505805591694, -0.1113553986120547346, 1.530511810916094451 ) ) ;
#25232=CARTESIAN_POINT ( 'NONE',  ( -0.7495606340400177148, 0.1264236179284866091, 1.611712598371433103 ) ) ;
#25233=ORIENTED_EDGE ( 'NONE', *, *, #35611, .T. ) ;
#25234=CARTESIAN_POINT ( 'NONE',  ( -1.054774247047244096, 0.000000000000000000, 1.129429133804503937 ) ) ;
#25237=CARTESIAN_POINT ( 'NONE',  ( 0.6971942568897637749, 2.189545951927499583E-17, 1.227854330654897685 ) ) ;
#25239=CARTESIAN_POINT ( 'NONE',  ( -0.8759842519685039353, 0.1574803149606299191, 0.7185039369003465293 ) ) ;
#25240=CARTESIAN_POINT ( 'NONE',  ( 0.7185039370078746268, 0.06523048226347977208, 0.1058070866141732902 ) ) ;
#25241=CARTESIAN_POINT ( 'NONE',  ( 0.8759842519685039353, 0.1787899950787401882, 1.843011810969858333 ) ) ;
#25242=CARTESIAN_POINT ( 'NONE',  ( -0.7646288533564489232, 0.1113553986120547346, 0.6151574803149606474 ) ) ;
#25243=CARTESIAN_POINT ( 'NONE',  ( -0.9500414927467378812, -0.1787899950787401604, 0.8809055117572599514 ) ) ;
#25245=CARTESIAN_POINT ( 'NONE',  ( 0.8759842519685039353, 0.1787899950787401882, 0.3124999999462365619 ) ) ;
#25246=CARTESIAN_POINT ( 'NONE',  ( -0.8759842519685039353, 0.1787899950787401882, 0.1894685038832444879 ) ) ;
#25247=CARTESIAN_POINT ( 'NONE',  ( -1.054774247047244096, 0.000000000000000000, 0.7701771653005669016 ) ) ;
#25248=CARTESIAN_POINT ( 'NONE',  ( 1.033464566929134687, -0.06523048226347956391, 1.532972440837355066 ) ) ;
#25251=VERTEX_POINT ( 'NONE', #658 ) ;
#25252=CARTESIAN_POINT ( 'NONE',  ( 1.002407869896990045, -0.1264236179284866091, 0.8489173227808819444 ) ) ;
#25253=CARTESIAN_POINT ( 'NONE',  ( 0.9500414927467377701, 0.1787899950787401604, 1.058070866087969186 ) ) ;
#25254=CARTESIAN_POINT ( 'NONE',  ( -0.6971942568897648851, 0.07405724077823318263, 1.929133858213952557 ) ) ;
#25256=CARTESIAN_POINT ( 'NONE',  ( 1.054774247047244096, 0.000000000000000000, 1.872539370024976391 ) ) ;
#25257=ORIENTED_EDGE ( 'NONE', *, *, #20179, .F. ) ;
#25259=CARTESIAN_POINT ( 'NONE',  ( -1.033464566929133799, 1.928577636452524610E-17, 2.869337061179095023E-17 ) ) ;
#25263=ORIENTED_EDGE ( 'NONE', *, *, #17211, .T. ) ;
#25264=CARTESIAN_POINT ( 'NONE',  ( 0.9500414927467378812, -0.1787899950787401604, 1.077755905458048113 ) ) ;
#25268=CARTESIAN_POINT ( 'NONE',  ( 0.8019270111902717657, -0.1787899950787401604, 0.08858267711159097113 ) ) ;
#25273=CARTESIAN_POINT ( 'NONE',  ( -1.054774247047244096, 0.000000000000000000, 0.4601377952218267953 ) ) ;
#25276=CARTESIAN_POINT ( 'NONE',  ( -0.7196516388670834985, -0.06167255061999755983, 1.984442901297172490 ) ) ;
#25278=CARTESIAN_POINT ( 'NONE',  ( 0.8019270111902717657, 0.1787899950787401604, 1.259842519631276359 ) ) ;
#25279=CARTESIAN_POINT ( 'NONE',  ( 0.8019270111902716547, -0.1787899950787401604, 1.624015747977732849 ) ) ;
#25282=CARTESIAN_POINT ( 'NONE',  ( 1.033464566929134687, 0.06523048226347956391, 0.01230314960629920289 ) ) ;
#25284=CARTESIAN_POINT ( 'NONE',  ( 0.7185039370078739607, 1.928577636452523993E-17, 0.8070866140657008136 ) ) ;
#25285=CARTESIAN_POINT ( 'NONE',  ( -1.033464566929134687, 0.06523048226347956391, 1.656003936900346085 ) ) ;
#25287=CARTESIAN_POINT ( 'NONE',  ( 0.8019270111902717657, -0.1787899950787401604, 0.1673228345919057225 ) ) ;
#25288=CARTESIAN_POINT ( 'NONE',  ( 0.7026501795067128242, -0.01243134911390358054, 0.03936888280061108525 ) ) ;
#25289=CARTESIAN_POINT ( 'NONE',  ( 1.002407869896990045, -0.1264236179284866091, 1.158956692859621995 ) ) ;
#25292=CARTESIAN_POINT ( 'NONE',  ( 0.7646288533564489232, -0.1113553986120547346, 1.215551181102362266 ) ) ;
#25293=CARTESIAN_POINT ( 'NONE',  ( 0.9412147342319837628, -0.1574803149606297803, 0.5044291337507409434 ) ) ;
#25295=CARTESIAN_POINT ( 'NONE',  ( -0.7646288533564489232, 0.1113553986120547346, 1.126968503937007871 ) ) ;
#25296=CARTESIAN_POINT ( 'NONE',  ( 0.9427463997941362139, 0.1565286221232543296, 0.03936821677798599262 ) ) ;
#25297=CARTESIAN_POINT ( 'NONE',  ( -0.8759842519685039353, 0.1574803149606299191, 0.3641732282389295583 ) ) ;
#25299=EDGE_LOOP ( 'NONE', ( #42641, #16600, #46081, #27082 ) ) ;
#25300=CARTESIAN_POINT ( 'NONE',  ( 1.002407869896990045, 0.1264236179284866091, 1.444389763725763665 ) ) ;
#25301=CARTESIAN_POINT ( 'NONE',  ( -0.7646288533564489232, 0.1113553986120547346, 1.638779527559055316 ) ) ;
#25303=CARTESIAN_POINT ( 'NONE',  ( -1.054774247047244540, 0.07405724077823318263, 0.06397637789899228433 ) ) ;
#25305=AXIS2_PLACEMENT_3D ( 'NONE', #12344, #20687, #38898 ) ;
#25306=ORIENTED_EDGE ( 'NONE', *, *, #30192, .T. ) ;
#25307=CARTESIAN_POINT ( 'NONE',  ( 1.033464566929134909, 0.06523048226347841205, 0.4355314959554649201 ) ) ;
#25308=ORIENTED_EDGE ( 'NONE', *, *, #22403, .T. ) ;
#25311=CARTESIAN_POINT ( 'NONE',  ( 0.7495606340400177148, 0.1264236179284866091, 0.5536417322297008115 ) ) ;
#25312=ORIENTED_EDGE ( 'NONE', *, *, #23109, .F. ) ;
#25313=CARTESIAN_POINT ( 'NONE',  ( -1.002407869896990045, 0.1264236179284866091, 1.483759842465921075 ) ) ;
#25315=CARTESIAN_POINT ( 'NONE',  ( -0.7495606340400177148, 0.1264236179284866091, 1.183562992072220599 ) ) ;
#25316=CARTESIAN_POINT ( 'NONE',  ( -0.9873396505805591694, -0.1113553986120547346, 0.08366141732283464971 ) ) ;
#25318=CARTESIAN_POINT ( 'NONE',  ( -0.6971942568897648851, 0.07405724077823318263, 1.141732283410804349 ) ) ;
#25319=ADVANCED_FACE ( 'NONE', ( #12442 ), #27103, .T. ) ;
#25320=CARTESIAN_POINT ( 'NONE',  ( -0.7495606340400177148, -0.1264236179284866091, 0.1697834645131657827 ) ) ;
#25322=CARTESIAN_POINT ( 'NONE',  ( 0.8759842519685039353, -0.1574803149606299191, 1.643700787294047228 ) ) ;
#25326=CARTESIAN_POINT ( 'NONE',  ( -0.9412147342319837628, -0.1574803149606297803, 0.8587598424121577478 ) ) ;
#25329=DIRECTION ( 'NONE',  ( 0.000000000000000000, 0.000000000000000000, -1.000000000000000000 ) ) ;
#25331=CARTESIAN_POINT ( 'NONE',  ( -0.8019270111902717657, -0.1787899950787401604, 0.7185039369541108556 ) ) ;
#25334=ORIENTED_EDGE ( 'NONE', *, *, #43038, .T. ) ;
#25335=CARTESIAN_POINT ( 'NONE',  ( -1.002407869896990045, 0.1264236179284866091, 1.764271653489543290 ) ) ;
#25337=EDGE_CURVE ( 'NONE', #14813, #33650, #45694, .T. ) ;
#25342=CARTESIAN_POINT ( 'NONE',  ( -0.6971942568897626646, -0.07405724077823297447, 0.1279527558517483676 ) ) ;
#25345=CARTESIAN_POINT ( 'NONE',  ( -0.9412147342319837628, 0.1574803149606300301, 1.345964566821607589 ) ) ;
#25347=CARTESIAN_POINT ( 'NONE',  ( 0.7495606340400177148, 0.1264236179284866091, 0.7111220471903307860 ) ) ;
#25350=ORIENTED_EDGE ( 'NONE', *, *, #6158, .F. ) ;
#25351=CARTESIAN_POINT ( 'NONE',  ( -0.8759842519685039353, 0.000000000000000000, 0.000000000000000000 ) ) ;
#25353=CARTESIAN_POINT ( 'NONE',  ( 1.033464566929134687, -0.06523048226347956391, 1.306594488188977055 ) ) ;
#25354=CARTESIAN_POINT ( 'NONE',  ( 0.7801632783431100560, -0.1419831758506162611, 1.986316665493995215 ) ) ;
#25358=CARTESIAN_POINT ( 'NONE',  ( 0.6971942568897637749, 2.189545951927499583E-17, 0.6323818897100157432 ) ) ;
#25360=CARTESIAN_POINT ( 'NONE',  ( -1.033464566929134687, -0.06523048226347956391, 0.3912401573727880555 ) ) ;
#25364=CARTESIAN_POINT ( 'NONE',  ( 0.9500414927467378812, 0.1787899950787401604, 1.013779527505291878 ) ) ;
#25370=CARTESIAN_POINT ( 'NONE',  ( -0.6971942568897626646, -0.07405724077823297447, 0.1624015747493861295 ) ) ;
#25373=VERTEX_POINT ( 'NONE', #19363 ) ;
#25375=CARTESIAN_POINT ( 'NONE',  ( -0.8019270111902716547, 0.1787899950787401604, 1.929133858213952557 ) ) ;
#25378=CARTESIAN_POINT ( 'NONE',  ( -1.054774247047244096, 0.000000000000000000, 1.715059055064346527 ) ) ;
#25379=CARTESIAN_POINT ( 'NONE',  ( -0.7495606340400177148, 0.1264236179284866091, 1.060531496009228247 ) ) ;
#25381=CARTESIAN_POINT ( 'NONE',  ( -1.054774247047244096, 0.000000000000000000, 0.4207677164816693294 ) ) ;
#25384=CARTESIAN_POINT ( 'NONE',  ( 0.8759842519685039353, 0.1574803149606299191, 0.4035433069790866356 ) ) ;
#25388=CARTESIAN_POINT ( 'NONE',  ( -0.8759842519685039353, 0.000000000000000000, 0.000000000000000000 ) ) ;
#25389=CARTESIAN_POINT ( 'NONE',  ( -0.7495606340400177148, -0.1264236179284866091, 0.1648622046706460786 ) ) ;
#25392=EDGE_CURVE ( 'NONE', #3114, #42764, #37828, .T. ) ;
#25393=CARTESIAN_POINT ( 'NONE',  ( -0.9500414927467377701, -0.1787899950787401604, 1.318897637741511364 ) ) ;
#25394=ORIENTED_EDGE ( 'NONE', *, *, #42957, .F. ) ;
#25400=CARTESIAN_POINT ( 'NONE',  ( 0.7185039370078739607, 1.928577636452523993E-17, 0.3838582677165354173 ) ) ;
#25402=CYLINDRICAL_SURFACE ( 'NONE', #4847, 0.1574803149606299191 ) ;
#25403=CARTESIAN_POINT ( 'NONE',  ( -0.7185039370078746268, 0.06523048226347956391, 1.001476377845228027 ) ) ;
#25408=CARTESIAN_POINT ( 'NONE',  ( 0.7185039370078746268, -0.06523048226347956391, 1.754429133750741387 ) ) ;
#25409=EDGE_LOOP ( 'NONE', ( #44296, #47132, #2702, #21317 ) ) ;
#25411=CARTESIAN_POINT ( 'NONE',  ( 0.7646288533564489232, -0.1113553986120547346, 0.7431102362204724532 ) ) ;
#25413=B_SPLINE_CURVE_WITH_KNOTS ( 'NONE', 3,
 ( #21470, #10721, #43754, #22421, #36102, #47115, #15024, #18123, #3261, #40378, #36579, #29898 ),
 .UNSPECIFIED., .F., .F.,
 ( 4, 2, 2, 2, 2, 4 ),
 ( 0.000000000000000000, 0.2500000000000016098, 0.3750000000000012212, 0.5000000000000008882, 0.7500000000000004441, 1.000000000000000000 ),
 .UNSPECIFIED. ) ;
#25416=CARTESIAN_POINT ( 'NONE',  ( 0.7185039370078739607, 1.928577636452523993E-17, 1.525590551181102317 ) ) ;
#25417=CARTESIAN_POINT ( 'NONE',  ( 0.7646288533564489232, -0.1113553986120547346, 0.2214566928058590567 ) ) ;
#25419=CARTESIAN_POINT ( 'NONE',  ( 0.9412147342319837628, 0.1574803149606300301, 1.897145669183811778 ) ) ;
#25420=CARTESIAN_POINT ( 'NONE',  ( -0.7646288533564489232, -0.1113553986120547346, 0.7726377951680629685 ) ) ;
#25423=CARTESIAN_POINT ( 'NONE',  ( -0.7185039370078739607, 1.928577636452523993E-17, 0.09842519674286673292 ) ) ;
#25425=CARTESIAN_POINT ( 'NONE',  ( 1.033464566929134687, -0.06523048226347956391, 0.9030511809948348345 ) ) ;
#25427=CARTESIAN_POINT ( 'NONE',  ( -0.7495606340400177148, -0.1264236179284866091, 0.4404527558517480901 ) ) ;
#25430=CARTESIAN_POINT ( 'NONE',  ( -0.6971942568897648851, 0.07405724077823318263, 1.540354330654897685 ) ) ;
#25431=CARTESIAN_POINT ( 'NONE',  ( 0.8019270111902717657, -0.1787899950787401604, 1.510826771599780294 ) ) ;
#25432=ORIENTED_EDGE ( 'NONE', *, *, #42032, .F. ) ;
#25433=CARTESIAN_POINT ( 'NONE',  ( -1.002407869896990045, -0.1264236179284866091, 0.7308070865604093802 ) ) ;
#25434=CARTESIAN_POINT ( 'NONE',  ( 0.7495606340400177148, -0.1264236179284866091, 0.1697834645131657827 ) ) ;
#25435=CARTESIAN_POINT ( 'NONE',  ( -0.8019270111902716547, -0.1787899950787401604, 0.6397637794737947026 ) ) ;
#25438=( BOUNDED_CURVE ( )  B_SPLINE_CURVE ( 2, ( #28346, #10126, #24735, #662, #21129, #44057, #22250, #4256, #39332 ),
 .UNSPECIFIED., .F., .T. ) 
 B_SPLINE_CURVE_WITH_KNOTS ( ( 3, 2, 2, 2, 3 ),
 ( 0.7299999999999999822, 0.7325000000000000400, 0.7349999999999999867, 0.7375000000000000444, 0.7399999999999999911 ),
 .UNSPECIFIED. ) 
 CURVE ( )  GEOMETRIC_REPRESENTATION_ITEM ( )  RATIONAL_B_SPLINE_CURVE ( ( 1.000000000000000000, 0.9238795325112939549, 1.000000000000000000, 0.9238795325112869605, 1.000000000000000000, 0.9238795325112869605, 1.000000000000000000, 0.9238795325112869605, 1.000000000000000000 ) ) 
 REPRESENTATION_ITEM ( '' )  ) ;
#25440=CARTESIAN_POINT ( 'NONE',  ( 0.7185039370078739607, 1.928577636452523993E-17, 0.6496062991050708391 ) ) ;
#25442=CARTESIAN_POINT ( 'NONE',  ( -0.7646288533564489232, 0.1113553986120547346, 1.825787401467275473 ) ) ;
#25444=CARTESIAN_POINT ( 'NONE',  ( 0.7185039370078739607, 1.928577636452523993E-17, 1.643700787401574992 ) ) ;
#25445=CARTESIAN_POINT ( 'NONE',  ( 0.8019270111902716547, -0.1787899950787401604, 1.432086614119464141 ) ) ;
#25448=VERTEX_POINT ( 'NONE', #16268 ) ;
#25450=EDGE_CURVE ( 'NONE', #14813, #3281, #11016, .T. ) ;
#25453=ADVANCED_FACE ( 'NONE', ( #38290 ), #20312, .T. ) ;
#25459=CARTESIAN_POINT ( 'NONE',  ( 0.7185039370078739607, 1.928577636452523993E-17, 1.840551181102362266 ) ) ;
#25461=CARTESIAN_POINT ( 'NONE',  ( 0.6971942568897648851, -0.07405724077823297447, 1.737204724355685848 ) ) ;
#25466=CARTESIAN_POINT ( 'NONE',  ( 1.033464566929133799, 1.928577636452524610E-17, 4.498031496062992574 ) ) ;
#25467=CARTESIAN_POINT ( 'NONE',  ( 1.054774247047244540, -0.07405724077823318263, 0.6102362204186774219 ) ) ;
#25469=CARTESIAN_POINT ( 'NONE',  ( -0.9160508336777043459, 0.1674337118376148514, 0.03937007874015843040 ) ) ;
#25473=CARTESIAN_POINT ( 'NONE',  ( -1.033464566929133799, 0.000000000000000000, 1.299212598317669221 ) ) ;
#25474=CARTESIAN_POINT ( 'NONE',  ( 1.054774247047244096, 0.000000000000000000, 1.601870078686393750 ) ) ;
#25476=CARTESIAN_POINT ( 'NONE',  ( 0.7185039370078766252, -0.06523048226348168721, 1.872539369971213619 ) ) ;
#25477=CARTESIAN_POINT ( 'NONE',  ( 1.002407869896990045, -0.1264236179284866091, 0.4896653542769449086 ) ) ;
#25480=ORIENTED_EDGE ( 'NONE', *, *, #17197, .T. ) ;
#25481=CARTESIAN_POINT ( 'NONE',  ( 0.7185039370078746268, -0.06523048226347956391, 0.03198818897637801389 ) ) ;
#25485=CARTESIAN_POINT ( 'NONE',  ( -0.9500414927467378812, 0.1787899950787401604, 0.4281496062454490659 ) ) ;
#25486=DIRECTION ( 'NONE',  ( -1.000000000000000000, 0.000000000000000000, 0.000000000000000000 ) ) ;
#25488=CARTESIAN_POINT ( 'NONE',  ( 0.7495606340400177148, 0.1264236179284866091, 0.04183070860765386589 ) ) ;
#25490=CARTESIAN_POINT ( 'NONE',  ( -0.8759842519685039353, 0.1787899950787401882, 1.606791338528913426 ) ) ;
#25491=ORIENTED_EDGE ( 'NONE', *, *, #28993, .T. ) ;
#25493=CARTESIAN_POINT ( 'NONE',  ( -0.8759842519685039353, 0.1787899950787401882, 1.099901574749385880 ) ) ;
#25495=CARTESIAN_POINT ( 'NONE',  ( 1.054774247047244540, 0.07405724077823318263, 1.131889763725763665 ) ) ;
#25497=CARTESIAN_POINT ( 'NONE',  ( 0.6971942568897648851, -0.07405724077823297447, 1.776574803095843924 ) ) ;
#25498=CARTESIAN_POINT ( 'NONE',  ( -0.8759842519685039353, -0.1574803149606299191, 0.6299212598425196763 ) ) ;
#25499=CARTESIAN_POINT ( 'NONE',  ( -0.6971942568897637749, 2.189545951927499583E-17, 1.104822834591905556 ) ) ;
#25502=CARTESIAN_POINT ( 'NONE',  ( 1.054774247047244540, 0.07405724077823318263, 0.3444881889226146243 ) ) ;
#25503=CARTESIAN_POINT ( 'NONE',  ( -1.002407869896990045, -0.1264236179284866091, 0.2534448818360003908 ) ) ;
#25504=CARTESIAN_POINT ( 'NONE',  ( -0.6971942568897637749, 2.189545951927499583E-17, 0.7504921259304880854 ) ) ;
#25505=CARTESIAN_POINT ( 'NONE',  ( 1.033464566929134687, -0.06523048226347956391, 1.651082677057826853 ) ) ;
#25506=EDGE_LOOP ( 'NONE', ( #15181, #34824, #46871, #32390 ) ) ;
#25508=ORIENTED_EDGE ( 'NONE', *, *, #45760, .F. ) ;
#25509=CARTESIAN_POINT ( 'NONE',  ( 0.7495606340400177148, 0.1264236179284866091, 0.8686023621509606496 ) ) ;
#25510=CARTESIAN_POINT ( 'NONE',  ( 0.8759842519685039353, 0.1787899950787401882, 1.060531496009228247 ) ) ;
#25511=CARTESIAN_POINT ( 'NONE',  ( -1.054774247047244540, 0.07405724077823318263, 1.835629921206078485 ) ) ;
#25513=CARTESIAN_POINT ( 'NONE',  ( 0.6971942568897648851, -0.07405724077823297447, 1.934055118056471567 ) ) ;
#25523=CARTESIAN_POINT ( 'NONE',  ( 0.9500414927467378812, -0.1787899950787401604, 1.235236220418678199 ) ) ;
#25530=CARTESIAN_POINT ( 'NONE',  ( 1.033464566929133799, 0.000000000000000000, 1.938976377952756014 ) ) ;
#25533=CARTESIAN_POINT ( 'NONE',  ( -0.8759842519685039353, 0.1787899950787401882, 0.5487204723871811352 ) ) ;
#25536=CARTESIAN_POINT ( 'NONE',  ( 0.8019270111902717657, -0.1787899950787401604, 1.195866141678520345 ) ) ;
#25537=CARTESIAN_POINT ( 'NONE',  ( 1.054774247047244540, -0.07405724077823318263, 1.673228346402929834 ) ) ;
#25538=CARTESIAN_POINT ( 'NONE',  ( -0.9412147342319837628, 0.1574803149606300301, 1.906988188976377563 ) ) ;
#25541=CARTESIAN_POINT ( 'NONE',  ( -0.7185039370078746268, -0.06523048226347956391, 1.016240157480315487 ) ) ;
#25542=CARTESIAN_POINT ( 'NONE',  ( -0.7646288533564489232, -0.1113553986120547346, 1.678149606191684962 ) ) ;
#25543=CARTESIAN_POINT ( 'NONE',  ( 0.6971942568897626646, -0.07405724077823297447, 0.1230314960092287191 ) ) ;
#25544=CARTESIAN_POINT ( 'NONE',  ( 0.7130838980242285574, -0.05254116306688896842, 0.03937007909647829984 ) ) ;
#25545=CARTESIAN_POINT ( 'NONE',  ( -0.7185039370078714072, 0.06523048226347728795, 1.828248031388537198 ) ) ;
#25546=CARTESIAN_POINT ( 'NONE',  ( 1.033464566929133799, 0.000000000000000000, 1.230314960629921295 ) ) ;
#25547=CARTESIAN_POINT ( 'NONE',  ( 0.8107537697050253289, 0.1574803149606300301, 0.5634842518609766149 ) ) ;
#25549=CARTESIAN_POINT ( 'NONE',  ( 0.8565624266329610048, 0.1746252292145809570, 0.03937093662838074548 ) ) ;
#25550=CARTESIAN_POINT ( 'NONE',  ( -0.8759842519685039353, -0.1574803149606299191, 0.3838582676090082635 ) ) ;
#25552=CARTESIAN_POINT ( 'NONE',  ( 0.7495606340400177148, -0.1264236179284866091, 1.424704724355685181 ) ) ;
#25553=CARTESIAN_POINT ( 'NONE',  ( -0.9412147342319837628, 0.1574803149606300301, 1.158956692913385655 ) ) ;
#25554=CARTESIAN_POINT ( 'NONE',  ( 0.9412147342319837628, 0.1574803149606300301, 1.670767716535433545 ) ) ;
#25557=CARTESIAN_POINT ( 'NONE',  ( 1.033464566929134687, 0.06523048226347956391, 0.7209645669291341319 ) ) ;
#25558=CARTESIAN_POINT ( 'NONE',  ( -1.033464566929133799, 1.928577636452524610E-17, 2.869337061179095023E-17 ) ) ;
#25559=FACE_OUTER_BOUND ( 'NONE', #7638, .T. ) ;
#25561=CARTESIAN_POINT ( 'NONE',  ( 0.8759842519685039353, -0.1787899950787401882, 0.6471456692375747721 ) ) ;
#25563=CARTESIAN_POINT ( 'NONE',  ( -0.7495606340400177148, 0.1264236179284866091, 1.454232283410803017 ) ) ;
#25565=CARTESIAN_POINT ( 'NONE',  ( -0.9500414927467378812, -0.1787899950787401604, 1.161417322780881278 ) ) ;
#25566=CARTESIAN_POINT ( 'NONE',  ( -1.054774247047244096, 0.000000000000000000, 1.124507873961984261 ) ) ;
#25567=ADVANCED_FACE ( 'NONE', ( #5928 ), #2557, .T. ) ;
#25569=CARTESIAN_POINT ( 'NONE',  ( -1.002407869896990045, -0.1264236179284866091, 0.2189960629383626012 ) ) ;
#25570=CARTESIAN_POINT ( 'NONE',  ( 0.9873396505805591694, 0.1113553986120547346, 0.7923228345381417848 ) ) ;
#25573=CARTESIAN_POINT ( 'NONE',  ( -1.033464566929134687, 0.06523048226347956391, 0.05167322834645669133 ) ) ;
#25575=ORIENTED_EDGE ( 'NONE', *, *, #141, .F. ) ;
#25576=ORIENTED_EDGE ( 'NONE', *, *, #39112, .F. ) ;
#25577=EDGE_CURVE ( 'NONE', #35449, #815, #38845, .T. ) ;
#25579=CARTESIAN_POINT ( 'NONE',  ( -0.6971942568897626646, 0.07405724077823318263, 0.7874015747493863238 ) ) ;
#25580=( BOUNDED_CURVE ( )  B_SPLINE_CURVE ( 2, ( #5922, #35868, #6142, #24848, #2089, #17653, #27779, #9294, #20769 ),
 .UNSPECIFIED., .F., .T. ) 
 B_SPLINE_CURVE_WITH_KNOTS ( ( 3, 2, 2, 2, 3 ),
 ( 0.6600000000000000311, 0.6624999999999999778, 0.6650000000000000355, 0.6674999999999999822, 0.6700000000000000400 ),
 .UNSPECIFIED. ) 
 CURVE ( )  GEOMETRIC_REPRESENTATION_ITEM ( )  RATIONAL_B_SPLINE_CURVE ( ( 1.000000000000000000, 0.9238795325112869605, 1.000000000000000000, 0.9238795325112869605, 1.000000000000000000, 0.9238795325112869605, 1.000000000000000000, 0.9238795325112829637, 1.000000000000000000 ) ) 
 REPRESENTATION_ITEM ( '' )  ) ;
#25583=CARTESIAN_POINT ( 'NONE',  ( -0.7495606340400177148, 0.1264236179284866091, 1.774114173174582643 ) ) ;
#25584=CARTESIAN_POINT ( 'NONE',  ( 0.9873396505805591694, -0.1113553986120547346, 0.7135826771653542844 ) ) ;
#25586=DIRECTION ( 'NONE',  ( 0.000000000000000000, 0.000000000000000000, -1.000000000000000000 ) ) ;
#25587=CARTESIAN_POINT ( 'NONE',  ( -1.033464566929133799, 0.000000000000000000, 1.574803149498771537 ) ) ;
#25588=VECTOR ( 'NONE', #3340, 39.37007874015748143 ) ;
#25589=CARTESIAN_POINT ( 'NONE',  ( 1.054774247047244096, 0.000000000000000000, 0.7357283464029290565 ) ) ;
#25592=CARTESIAN_POINT ( 'NONE',  ( 0.7185039370078739607, 1.928577636452523993E-17, 1.368110236220472675 ) ) ;
#25593=CARTESIAN_POINT ( 'NONE',  ( 0.8559655446573316562, -0.1727717671435132496, 1.987845004397921445 ) ) ;
#25595=CARTESIAN_POINT ( 'NONE',  ( 0.9873396505805591694, -0.1113553986120547346, 1.491141732175936818 ) ) ;
#25598=CARTESIAN_POINT ( 'NONE',  ( 0.7495606340400177148, 0.1264236179284866091, 0.7455708660879684091 ) ) ;
#25601=CARTESIAN_POINT ( 'NONE',  ( -1.033464566929133799, 0.000000000000000000, 0.3937007872940476716 ) ) ;
#25604=CARTESIAN_POINT ( 'NONE',  ( 0.7495606340400177148, -0.1264236179284866091, 0.9916338582139527791 ) ) ;
#25609=CARTESIAN_POINT ( 'NONE',  ( -1.054774247047244540, 0.07405724077823318263, 0.02460629915883492599 ) ) ;
#25611=CARTESIAN_POINT ( 'NONE',  ( -0.8107537697050254399, 0.1574803149606300301, 0.6126968503937006982 ) ) ;
#25612=ORIENTED_EDGE ( 'NONE', *, *, #34278, .F. ) ;
#25614=CARTESIAN_POINT ( 'NONE',  ( -0.7185039370078739607, 1.928577636452523993E-17, 1.840551181102362266 ) ) ;
#25615=CARTESIAN_POINT ( 'NONE',  ( -0.6971942568897648851, 0.07405724077823318263, 1.653543307032850462 ) ) ;
#25616=CARTESIAN_POINT ( 'NONE',  ( -0.6971942568897648851, -0.07405724077823297447, 1.107283464513165949 ) ) ;
#25618=CARTESIAN_POINT ( 'NONE',  ( -1.033464566929134687, -0.06523048226347956391, 0.1648622047244094890 ) ) ;
#25619=CARTESIAN_POINT ( 'NONE',  ( 0.9500414927467378812, 0.1787899950787401604, 0.06889763774151215492 ) ) ;
#25624=DIRECTION ( 'NONE',  ( 0.000000000000000000, 0.000000000000000000, -1.000000000000000000 ) ) ;
#25627=CARTESIAN_POINT ( 'NONE',  ( -0.7495606340400177148, -0.1264236179284866091, 0.3223425196312759144 ) ) ;
#25631=CARTESIAN_POINT ( 'NONE',  ( -0.9500414927467377701, 0.1787899950787401604, 1.412401574749386990 ) ) ;
#25632=ORIENTED_EDGE ( 'NONE', *, *, #1730, .F. ) ;
#25636=CARTESIAN_POINT ( 'NONE',  ( 0.9412147342319837628, 0.1574803149606300301, 0.3715551181102361711 ) ) ;
#25638=CARTESIAN_POINT ( 'NONE',  ( -0.7646288533564489232, 0.1113553986120547346, 0.9202755904436535905 ) ) ;
#25639=CARTESIAN_POINT ( 'NONE',  ( 0.9500414927467378812, -0.1787899950787401604, 0.4133858267178901480 ) ) ;
#25641=STYLED_ITEM ( 'NONE', ( #8813 ), #5043 ) ;
#25642=CARTESIAN_POINT ( 'NONE',  ( 0.7185039370078739607, 1.928577636452523993E-17, 1.830708661309795149 ) ) ;
#25645=CARTESIAN_POINT ( 'NONE',  ( 0.8759842519685039353, 0.1574803149606299191, 1.003937007874015741 ) ) ;
#25647=CARTESIAN_POINT ( 'NONE',  ( 0.7185039370078739607, 1.928577636452523993E-17, 1.013779527559055094 ) ) ;
#25652=CARTESIAN_POINT ( 'NONE',  ( 0.8759842519685039353, 0.000000000000000000, 4.498031496062992574 ) ) ;
#25660=CARTESIAN_POINT ( 'NONE',  ( 0.8759842519685039353, -0.1574803149606299191, 0.9744094487113701408 ) ) ;
#25664=CARTESIAN_POINT ( 'NONE',  ( -0.8759842519685039353, 0.1787899950787401882, 1.572342519631275692 ) ) ;
#25665=ORIENTED_EDGE ( 'NONE', *, *, #41740, .T. ) ;
#25666=EDGE_CURVE ( 'NONE', #31512, #15464, #25722, .T. ) ;
#25667=CARTESIAN_POINT ( 'NONE',  ( 0.6971942568897637749, 2.189545951927499583E-17, 1.739665354276945131 ) ) ;
#25670=CARTESIAN_POINT ( 'NONE',  ( -0.8759842519685039353, -0.1787899950787401882, 0.8046259841982047467 ) ) ;
#25671=CARTESIAN_POINT ( 'NONE',  ( 1.054774247047244540, -0.07405724077823318263, 0.2608267715997796832 ) ) ;
#25672=DIRECTION ( 'NONE',  ( 1.822029033848725028E-16, 0.000000000000000000, 1.000000000000000000 ) ) ;
#25673=CARTESIAN_POINT ( 'NONE',  ( -0.8759842519685039353, -0.1787899950787401882, 0.7603346456155274380 ) ) ;
#25674=FACE_OUTER_BOUND ( 'NONE', #8022, .T. ) ;
#25676=CARTESIAN_POINT ( 'NONE',  ( -0.7185039370078746268, -0.06523048226347956391, 0.8587598425196851792 ) ) ;
#25677=CARTESIAN_POINT ( 'NONE',  ( -1.002407869896990045, -0.1264236179284866091, 1.557578740103716441 ) ) ;
#25678=CARTESIAN_POINT ( 'NONE',  ( -0.9412147342319837628, 0.1574803149606300301, 1.818405511703498068 ) ) ;
#25682=CARTESIAN_POINT ( 'NONE',  ( -0.7646288533564489232, 0.1113553986120547346, 1.638779527559055316 ) ) ;
#25683=DIRECTION ( 'NONE',  ( 0.000000000000000000, 0.000000000000000000, -1.000000000000000000 ) ) ;
#25684=CARTESIAN_POINT ( 'NONE',  ( 1.054774247047244540, 0.07405724077823318263, 1.525590551127339989 ) ) ;
#25686=CARTESIAN_POINT ( 'NONE',  ( -1.033464566929133799, 0.000000000000000000, 0.3543307085538902057 ) ) ;
#25688=VECTOR ( 'NONE', #16589, 39.37007874015748143 ) ;
#25690=ADVANCED_FACE ( 'NONE', ( #139 ), #44000, .T. ) ;
#25692=CARTESIAN_POINT ( 'NONE',  ( 0.000000000000000000, 0.000000000000000000, 0.000000000000000000 ) ) ;
#25696=CARTESIAN_POINT ( 'NONE',  ( 0.8759842519685039353, 0.1574803149606299191, 1.043307086614173151 ) ) ;
#25698=CARTESIAN_POINT ( 'NONE',  ( 0.7495606340400177148, -0.1264236179284866091, 1.779035433017102319 ) ) ;
#25703=AXIS2_PLACEMENT_3D ( 'NONE', #16921, #17155, #31563 ) ;
#25704=CARTESIAN_POINT ( 'NONE',  ( 1.054774247047244096, 0.000000000000000000, 0.6914370078202519698 ) ) ;
#25705=CARTESIAN_POINT ( 'NONE',  ( -1.023926211165723021, 0.06782980145170247610, 0.03937007874015843040 ) ) ;
#25708=CARTESIAN_POINT ( 'NONE',  ( 0.9412147342319837628, 0.1574803149606300301, 0.9522637794200313754 ) ) ;
#25709=CARTESIAN_POINT ( 'NONE',  ( 1.002407869896990045, 0.1264236179284866091, 1.843011810969858333 ) ) ;
#25711=CARTESIAN_POINT ( 'NONE',  ( 1.033464566929133799, 0.000000000000000000, 1.889763779420031486 ) ) ;
#25718=CARTESIAN_POINT ( 'NONE',  ( -0.6971942568897626646, 0.07405724077823318263, 0.4773622046706456068 ) ) ;
#25721=CARTESIAN_POINT ( 'NONE',  ( 0.9500414927467378812, 0.1787899950787401604, 0.1131889763241892138 ) ) ;
#25722=( BOUNDED_CURVE ( )  B_SPLINE_CURVE ( 2, ( #16957, #39680, #31597, #6867, #35654, #20778, #2792, #46178, #13375 ),
 .UNSPECIFIED., .F., .T. ) 
 B_SPLINE_CURVE_WITH_KNOTS ( ( 3, 2, 2, 2, 3 ),
 ( 0.2999999999999999889, 0.3024999999999999911, 0.3049999999999999933, 0.3074999999999999956, 0.3099999999999999978 ),
 .UNSPECIFIED. ) 
 CURVE ( )  GEOMETRIC_REPRESENTATION_ITEM ( )  RATIONAL_B_SPLINE_CURVE ( ( 1.000000000000000000, 0.9238795325112869605, 1.000000000000000000, 0.9238795325112869605, 1.000000000000000000, 0.9238795325112869605, 1.000000000000000000, 0.9238795325112869605, 1.000000000000000000 ) ) 
 REPRESENTATION_ITEM ( '' )  ) ;
#25725=CARTESIAN_POINT ( 'NONE',  ( -1.054774247047244540, -0.07405724077823318263, 1.205708661363558365 ) ) ;
#25726=CARTESIAN_POINT ( 'NONE',  ( 0.7185039370078746268, -0.06523048226347956391, 1.016240157480315487 ) ) ;
#25727=ADVANCED_FACE ( 'NONE', ( #14792 ), #28662, .T. ) ;
#25728=CARTESIAN_POINT ( 'NONE',  ( 0.7495606340400177148, -0.1264236179284866091, 1.193405511757259951 ) ) ;
#25729=CARTESIAN_POINT ( 'NONE',  ( -0.8759842519685039353, -0.1574803149606299191, 0.5511811023622047445 ) ) ;
#25730=CARTESIAN_POINT ( 'NONE',  ( -0.7495606340400177148, -0.1264236179284866091, 1.109744094434425232 ) ) ;
#25733=CARTESIAN_POINT ( 'NONE',  ( 0.8019270111902716547, 0.1787899950787401604, 0.2755905511273391006 ) ) ;
#25734=CARTESIAN_POINT ( 'NONE',  ( -1.054774247047244540, 0.07405724077823318263, 0.2214566928596221063 ) ) ;
#25735=CARTESIAN_POINT ( 'NONE',  ( -1.002407869896990045, 0.1264236179284866091, 0.7750984251430865779 ) ) ;
#25736=CARTESIAN_POINT ( 'NONE',  ( 1.033464566929134687, 0.06523048226347956391, 1.695374015640504828 ) ) ;
#25737=ORIENTED_EDGE ( 'NONE', *, *, #575, .T. ) ;
#25739=CARTESIAN_POINT ( 'NONE',  ( 1.002407869896990045, -0.1264236179284866091, 0.8095472440407244230 ) ) ;
#25740=CARTESIAN_POINT ( 'NONE',  ( 1.002407869896990045, 0.1264236179284866091, 1.016240157426551161 ) ) ;
#25741=CARTESIAN_POINT ( 'NONE',  ( -0.8759842519685039353, 0.1787899950787401882, 1.882381889710015743 ) ) ;
#25744=CARTESIAN_POINT ( 'NONE',  ( 0.8759842519685039353, -0.1787899950787401882, 1.980807086560409491 ) ) ;
#25746=EDGE_CURVE ( 'NONE', #1914, #43027, #3007, .T. ) ;
#25747=CARTESIAN_POINT ( 'NONE',  ( 1.033464566929133799, 0.000000000000000000, 1.309055118110236338 ) ) ;
#25751=AXIS2_PLACEMENT_3D ( 'NONE', #25388, #180, #33060 ) ;
#25752=ORIENTED_EDGE ( 'NONE', *, *, #38696, .T. ) ;
#25753=CARTESIAN_POINT ( 'NONE',  ( 1.002407869896990045, 0.1264236179284866091, 1.247539370024976391 ) ) ;
#25754=CARTESIAN_POINT ( 'NONE',  ( -0.9873396505805591694, 0.1113553986120547346, 0.8316929132782993062 ) ) ;
#25756=CARTESIAN_POINT ( 'NONE',  ( 0.8019270111902717657, -0.1787899950787401604, 0.04921259837143338034 ) ) ;
#25759=CARTESIAN_POINT ( 'NONE',  ( -1.054774247047244096, 0.000000000000000000, 0.4995078739619842612 ) ) ;
#25760=CARTESIAN_POINT ( 'NONE',  ( 0.8759842519685039353, -0.1574803149606299191, 0.3051181101286932762 ) ) ;
#25762=CARTESIAN_POINT ( 'NONE',  ( 0.7495606340400177148, 0.1264236179284866091, 1.262303149552535420 ) ) ;
#25763=CARTESIAN_POINT ( 'NONE',  ( 0.9500414927467377701, -0.1787899950787401604, 1.628937007820252303 ) ) ;
#25764=CARTESIAN_POINT ( 'NONE',  ( 0.9412147342319837628, 0.1574803149606300301, 0.1353346456692914035 ) ) ;
#25767=CARTESIAN_POINT ( 'NONE',  ( -0.8107537697050254399, 0.1574803149606300301, 1.006397637795276800 ) ) ;
#25771=CARTESIAN_POINT ( 'NONE',  ( 0.6971942568897637749, 2.189545951927499583E-17, 0.3174212597887562382 ) ) ;
#25775=CARTESIAN_POINT ( 'NONE',  ( 0.9873396505805591694, 0.1113553986120547346, 0.6348425195775118102 ) ) ;
#25776=ORIENTED_EDGE ( 'NONE', *, *, #29559, .T. ) ;
#25779=CARTESIAN_POINT ( 'NONE',  ( 0.9141235117445012381, 0.1680089951793457825, 0.03937079690018885358 ) ) ;
#25780=DIRECTION ( 'NONE',  ( 0.000000000000000000, 0.000000000000000000, -1.000000000000000000 ) ) ;
#25781=CARTESIAN_POINT ( 'NONE',  ( 0.8019270111902717657, 0.1787899950787401604, 1.373031496009229135 ) ) ;
#25782=CARTESIAN_POINT ( 'NONE',  ( -0.7646288533564489232, 0.1113553986120547346, 1.166338582677165281 ) ) ;
#25783=EDGE_CURVE ( 'NONE', #28038, #1697, #44227, .T. ) ;
#25784=CARTESIAN_POINT ( 'NONE',  ( -0.8759842519685039353, 0.1574803149606299191, 1.830708661417322913 ) ) ;
#25785=CARTESIAN_POINT ( 'NONE',  ( 1.033464566929133799, 0.000000000000000000, 1.899606299212598604 ) ) ;
#25789=CARTESIAN_POINT ( 'NONE',  ( 0.7185039370078714072, 0.06523048226347728795, 1.552657480207434659 ) ) ;
#25792=CARTESIAN_POINT ( 'NONE',  ( 0.8759842519685039353, -0.1787899950787401882, 0.5290354330171024300 ) ) ;
#25795=CARTESIAN_POINT ( 'NONE',  ( -0.7495606340400177148, -0.1264236179284866091, 1.193405511757259951 ) ) ;
#25796=ORIENTED_EDGE ( 'NONE', *, *, #11840, .T. ) ;
#25798=CARTESIAN_POINT ( 'NONE',  ( -0.8019270111902717657, -0.1787899950787401604, 0.8021653542769460188 ) ) ;
#25799=CARTESIAN_POINT ( 'NONE',  ( -0.9500414927467378812, 0.1787899950787401604, 0.1919291338045042428 ) ) ;
#25800=CARTESIAN_POINT ( 'NONE',  ( 1.033464566929134687, -0.06523048226347956391, 0.6766732283464570452 ) ) ;
#25806=ORIENTED_EDGE ( 'NONE', *, *, #20298, .T. ) ;
#25808=CARTESIAN_POINT ( 'NONE',  ( -0.8019270111902717657, 0.1787899950787401604, 0.7824803149068669805 ) ) ;
#25810=VERTEX_POINT ( 'NONE', #11673 ) ;
#25811=CARTESIAN_POINT ( 'NONE',  ( -0.7495606340400177148, -0.1264236179284866091, 1.783956692859621995 ) ) ;
#25813=ORIENTED_EDGE ( 'NONE', *, *, #41040, .F. ) ;
#25815=CARTESIAN_POINT ( 'NONE',  ( -0.7646288533564489232, 0.1113553986120547346, 0.4084645668216063119 ) ) ;
#25816=CARTESIAN_POINT ( 'NONE',  ( -0.7646288533564489232, 0.1113553986120547346, 1.589566929026330566 ) ) ;
#25817=CARTESIAN_POINT ( 'NONE',  ( 0.9500414927467378812, 0.1787899950787401604, 0.7037401574265510495 ) ) ;
#25819=CARTESIAN_POINT ( 'NONE',  ( 1.033464566929134687, 0.06523048226347956391, 1.390255905511810441 ) ) ;
#25821=CARTESIAN_POINT ( 'NONE',  ( 0.8505431175464920335, -0.1718778923049482099, 1.987741662751643767 ) ) ;
#25822=CARTESIAN_POINT ( 'NONE',  ( 0.7185039370078739607, 0.000000000000000000, 4.498031496062992574 ) ) ;
#25826=CARTESIAN_POINT ( 'NONE',  ( 1.054774247047244540, -0.07405724077823318263, 0.8858267715997791836 ) ) ;
#25828=CARTESIAN_POINT ( 'NONE',  ( -0.7185039370078746268, 0.06523048226347956391, 1.168799212598425896 ) ) ;
#25830=CARTESIAN_POINT ( 'NONE',  ( 1.002407869896990045, 0.1264236179284866091, 1.011318897584031484 ) ) ;
#25832=LINE ( 'NONE', #10269, #4239 ) ;
#25834=CARTESIAN_POINT ( 'NONE',  ( -0.7185039370078739607, 1.928577636452523993E-17, 0.5019685039370078705 ) ) ;
#25837=CARTESIAN_POINT ( 'NONE',  ( -0.6971942568897637749, 2.189545951927499583E-17, 0.1599409448281264023 ) ) ;
#25838=CARTESIAN_POINT ( 'NONE',  ( 0.9412147342319837628, 0.1574803149606300301, 1.749507874015747699 ) ) ;
#25840=CARTESIAN_POINT ( 'NONE',  ( -0.8759842519685039353, 0.1787899950787401882, 1.685531496009228469 ) ) ;
#25841=CARTESIAN_POINT ( 'NONE',  ( -1.054774247047244540, -0.07405724077823318263, 0.8464566928596233275 ) ) ;
#25842=CARTESIAN_POINT ( 'NONE',  ( -0.6971942568897626646, -0.07405724077823297447, 0.3248031495525359746 ) ) ;
#25846=CARTESIAN_POINT ( 'NONE',  ( -1.033464566929134687, -0.06523048226347956391, 1.975885826771653475 ) ) ;
#25853=CARTESIAN_POINT ( 'NONE',  ( -0.7495606340400177148, -0.1264236179284866091, 0.2829724408911185041 ) ) ;
#25854=VERTEX_POINT ( 'NONE', #16214 ) ;
#25856=CARTESIAN_POINT ( 'NONE',  ( -1.002407869896990045, -0.1264236179284866091, 1.321358267662771757 ) ) ;
#25862=CARTESIAN_POINT ( 'NONE',  ( 0.9412147342319837628, 0.1574803149606300301, 0.4109251968503938590 ) ) ;
#25863=CARTESIAN_POINT ( 'NONE',  ( -0.8759842519685039353, 0.000000000000000000, 0.000000000000000000 ) ) ;
#25864=CARTESIAN_POINT ( 'NONE',  ( -0.9873396505805591694, -0.1113553986120547346, 1.136811023514519681 ) ) ;
#25865=CARTESIAN_POINT ( 'NONE',  ( 0.6971942568897626646, 0.07405724077823318263, 0.3986220471903312301 ) ) ;
#25866=CARTESIAN_POINT ( 'NONE',  ( -0.9873396505805591694, -0.1113553986120547346, 1.697834645669291209 ) ) ;
#25869=ORIENTED_EDGE ( 'NONE', *, *, #10584, .T. ) ;
#25871=CARTESIAN_POINT ( 'NONE',  ( 0.7185039370078746268, 0.06523048226347956391, 0.9719488188976380671 ) ) ;
#25874=ADVANCED_FACE ( 'NONE', ( #12388 ), #23154, .T. ) ;
#25876=CARTESIAN_POINT ( 'NONE',  ( -0.7646288533564489232, -0.1113553986120547346, 0.4675196850393700809 ) ) ;
#25880=CARTESIAN_POINT ( 'NONE',  ( -0.7185039370078739607, 1.928577636452523993E-17, 0.6102362203649134287 ) ) ;
#25881=CARTESIAN_POINT ( 'NONE',  ( -0.9412147342319837628, -0.1574803149606297803, 0.9867125984251977622 ) ) ;
#25887=CARTESIAN_POINT ( 'NONE',  ( 0.9873396505805591694, -0.1113553986120547346, 0.9399606298137322957 ) ) ;
#25889=EDGE_LOOP ( 'NONE', ( #525, #12371, #14319, #5231 ) ) ;
#25892=CARTESIAN_POINT ( 'NONE',  ( -1.002407869896990045, 0.1264236179284866091, 1.567421259788755794 ) ) ;
#25893=CARTESIAN_POINT ( 'NONE',  ( 1.054774247047244540, 0.07405724077823318263, 1.761811023568284007 ) ) ;
#25894=CARTESIAN_POINT ( 'NONE',  ( -1.054774247047244540, -0.07405724077823318263, 0.8120078739619844832 ) ) ;
#25895=FACE_OUTER_BOUND ( 'NONE', #9306, .T. ) ;
#25896=CARTESIAN_POINT ( 'NONE',  ( 1.002407869896990045, 0.1264236179284866091, 0.3469488188438744070 ) ) ;
#25898=CARTESIAN_POINT ( 'NONE',  ( -1.054774247047244096, 0.000000000000000000, 1.281988188922614125 ) ) ;
#25899=CARTESIAN_POINT ( 'NONE',  ( -1.054774247047244096, 0.000000000000000000, 0.6520669290800944484 ) ) ;
#25902=CARTESIAN_POINT ( 'NONE',  ( -0.8019270111902717657, 0.1787899950787401604, 1.614173228292692386 ) ) ;
#25903=CARTESIAN_POINT ( 'NONE',  ( -0.9412147342319837628, -0.1574803149606297803, 1.921751968396409493 ) ) ;
#25905=CARTESIAN_POINT ( 'NONE',  ( -0.7185039370078746268, 0.06523048226347956391, 1.641240157480315931 ) ) ;
#25907=CARTESIAN_POINT ( 'NONE',  ( 0.7495606340400177148, -0.1264236179284866091, 1.429625984198204858 ) ) ;
#25908=CARTESIAN_POINT ( 'NONE',  ( -1.033464566929134687, 0.06523048226347956391, 0.3567913384751500994 ) ) ;
#25911=EDGE_CURVE ( 'NONE', #35669, #21060, #21065, .T. ) ;
#25918=ORIENTED_EDGE ( 'NONE', *, *, #36161, .T. ) ;
#25921=CARTESIAN_POINT ( 'NONE',  ( 0.8759842519685039353, 0.1787899950787401882, 1.724901574749385880 ) ) ;
#25926=CARTESIAN_POINT ( 'NONE',  ( 0.7495606340400177148, -0.1264236179284866091, 0.7554133857730077617 ) ) ;
#25928=CYLINDRICAL_SURFACE ( 'NONE', #15509, 0.1574803149606299191 ) ;
#25929=CARTESIAN_POINT ( 'NONE',  ( 0.7185039370078739607, 1.928577636452523993E-17, 1.122047243986960652 ) ) ;
#25931=CARTESIAN_POINT ( 'NONE',  ( -0.9193554356332743760, -0.1704440316159954449, 1.988959660599587398 ) ) ;
#25933=CARTESIAN_POINT ( 'NONE',  ( 0.8019270111902717657, -0.1787899950787401604, 1.904527559001354398 ) ) ;
#25934=DIRECTION ( 'NONE',  ( 1.822029033848725028E-16, 0.000000000000000000, 1.000000000000000000 ) ) ;
#25936=EDGE_CURVE ( 'NONE', #740, #22900, #9756, .T. ) ;
#25939=CYLINDRICAL_SURFACE ( 'NONE', #40747, 0.1574803149606299191 ) ;
#25941=CARTESIAN_POINT ( 'NONE',  ( 0.8759842519685039353, 0.1787899950787401882, 0.2731299212060791515 ) ) ;
#25943=CARTESIAN_POINT ( 'NONE',  ( 1.054774247047244540, 0.07405724077823318263, 0.5757874015210393548 ) ) ;
#25944=CARTESIAN_POINT ( 'NONE',  ( -0.8019270111902717657, 0.1787899950787401604, 1.609251968450173376 ) ) ;
#25946=CARTESIAN_POINT ( 'NONE',  ( -0.8019270111902717657, 0.1787899950787401604, 1.141732283410804349 ) ) ;
#25947=CARTESIAN_POINT ( 'NONE',  ( 1.033464566929133799, 1.928577636452524610E-17, 4.498031496062992574 ) ) ;
#25950=CARTESIAN_POINT ( 'NONE',  ( 0.9500414927467378812, -0.1787899950787401604, 1.904527559001354398 ) ) ;
#25951=CARTESIAN_POINT ( 'NONE',  ( -1.054774247047244540, 0.07405724077823318263, 1.048228346402928723 ) ) ;
#25954=CARTESIAN_POINT ( 'NONE',  ( 0.9500414927467377701, -0.1787899950787401604, 0.4133858267178901480 ) ) ;
#25955=CARTESIAN_POINT ( 'NONE',  ( -1.054774247047244540, -0.07405724077823318263, 0.2559055117572600624 ) ) ;
#25956=CARTESIAN_POINT ( 'NONE',  ( 0.8107537697050253289, -0.1574803149606297803, 1.680610236112946687 ) ) ;
#25958=CARTESIAN_POINT ( 'NONE',  ( -0.8759842519685039353, 0.1574803149606299191, 0.8759842518609765039 ) ) ;
#25960=CARTESIAN_POINT ( 'NONE',  ( -0.9500414927467377701, -0.1787899950787401604, 1.865157480261198097 ) ) ;
#25962=CARTESIAN_POINT ( 'NONE',  ( 1.002407869896990045, -0.1264236179284866091, 1.946358267662771757 ) ) ;
#25967=CARTESIAN_POINT ( 'NONE',  ( -1.033464566929133799, 0.000000000000000000, 0.2854330708661417804 ) ) ;
#25968=VERTEX_POINT ( 'NONE', #12141 ) ;
#25969=CARTESIAN_POINT ( 'NONE',  ( 1.002407869896990045, -0.1264236179284866091, 1.158956692859621995 ) ) ;
#25970=CARTESIAN_POINT ( 'NONE',  ( -0.7185039370078739607, 1.928577636452523993E-17, 0.8464566928058583350 ) ) ;
#25971=CARTESIAN_POINT ( 'NONE',  ( 0.9412147342319837628, 0.1574803149606300301, 1.385334645561763445 ) ) ;
#25973=CARTESIAN_POINT ( 'NONE',  ( 0.8759842519685039353, -0.1787899950787401882, 0.2091535432533232486 ) ) ;
#25974=EDGE_CURVE ( 'NONE', #9411, #47093, #6374, .T. ) ;
#25978=EDGE_LOOP ( 'NONE', ( #40775, #40638, #13940, #31900 ) ) ;
#25979=( BOUNDED_CURVE ( )  B_SPLINE_CURVE ( 2, ( #17361, #46121, #35595, #42981, #45882, #42517, #38473, #28173, #38932 ),
 .UNSPECIFIED., .F., .T. ) 
 B_SPLINE_CURVE_WITH_KNOTS ( ( 3, 2, 2, 2, 3 ),
 ( 0.1000000000000000056, 0.1024999999999999939, 0.1049999999999999961, 0.1074999999999999983, 0.1100000000000000006 ),
 .UNSPECIFIED. ) 
 CURVE ( )  GEOMETRIC_REPRESENTATION_ITEM ( )  RATIONAL_B_SPLINE_CURVE ( ( 1.000000000000000000, 0.9238795325112869605, 1.000000000000000000, 0.9238795325112869605, 1.000000000000000000, 0.9238795325112869605, 1.000000000000000000, 0.9238795325112869605, 1.000000000000000000 ) ) 
 REPRESENTATION_ITEM ( '' )  ) ;
#25980=CARTESIAN_POINT ( 'NONE',  ( -0.6971942568897648851, 0.07405724077823318263, 0.5561023621509617598 ) ) ;
#25981=CARTESIAN_POINT ( 'NONE',  ( 0.8107537697050254399, 0.1574803149606300301, 0.3764763779527559029 ) ) ;
#25983=CARTESIAN_POINT ( 'NONE',  ( -0.7121474872820316993, -0.03261578266289449912, 1.983871201520547300 ) ) ;
#25985=CARTESIAN_POINT ( 'NONE',  ( 0.7495606340400177148, 0.1264236179284866091, 1.419783464513165505 ) ) ;
#25986=CARTESIAN_POINT ( 'NONE',  ( 1.054774247047244540, 0.07405724077823318263, 1.678149606245448622 ) ) ;
#25987=DIRECTION ( 'NONE',  ( 1.822029033848725028E-16, 0.000000000000000000, 1.000000000000000000 ) ) ;
#25989=CARTESIAN_POINT ( 'NONE',  ( 0.8759842519685039353, -0.1574803149606299191, 0.8956692912310552090 ) ) ;
#25990=CARTESIAN_POINT ( 'NONE',  ( -0.7904050636569344146, 0.1360127284603924458, 1.980115632570861983 ) ) ;
#25991=CARTESIAN_POINT ( 'NONE',  ( 0.9873396505805591694, -0.1113553986120547346, 0.8218503935932598425 ) ) ;
#25995=CARTESIAN_POINT ( 'NONE',  ( 1.002407869896990045, -0.1264236179284866091, 0.3321850393163153226 ) ) ;
#25996=CARTESIAN_POINT ( 'NONE',  ( 0.7331143493074542272, -0.08920476175640286443, 0.03937008031052523227 ) ) ;
#25997=CARTESIAN_POINT ( 'NONE',  ( -1.033464566929134687, 0.06523048226347956391, 1.705216535433070613 ) ) ;
#26000=CARTESIAN_POINT ( 'NONE',  ( 0.7646288533564489232, -0.1113553986120547346, 0.5757874014672763607 ) ) ;
#26004=ORIENTED_EDGE ( 'NONE', *, *, #11594, .T. ) ;
#26005=CARTESIAN_POINT ( 'NONE',  ( 0.9412147342319837628, 0.1574803149606300301, 0.2928149606299214613 ) ) ;
#26007=CARTESIAN_POINT ( 'NONE',  ( -0.7185039370078739607, 1.928577636452523993E-17, 0.2952755904436539236 ) ) ;
#26008=CARTESIAN_POINT ( 'NONE',  ( -0.9412147342319837628, 0.1574803149606300301, 0.4798228345381422844 ) ) ;
#26009=CARTESIAN_POINT ( 'NONE',  ( -0.8107537697050254399, 0.1574803149606300301, 1.596948818897636624 ) ) ;
#26010=CARTESIAN_POINT ( 'NONE',  ( 0.9500414927467378812, -0.1787899950787401604, 1.628937007820252303 ) ) ;
#26013=CARTESIAN_POINT ( 'NONE',  ( 1.033464566929134687, 0.06523048226347956391, 1.665846456692914312 ) ) ;
#26014=CARTESIAN_POINT ( 'NONE',  ( 1.033464566929133799, 1.928577636452524610E-17, 4.498031496062992574 ) ) ;
#26015=CARTESIAN_POINT ( 'NONE',  ( -0.8019270111902716547, -0.1787899950787401604, 0.04921259837143338728 ) ) ;
#26017=CARTESIAN_POINT ( 'NONE',  ( 0.8759842519685039353, -0.1574803149606299191, 1.328740157372787278 ) ) ;
#26018=EDGE_LOOP ( 'NONE', ( #10782, #7108, #31485, #4141 ) ) ;
#26019=( BOUNDED_CURVE ( )  B_SPLINE_CURVE ( 2, ( #24543, #17115, #39145, #10173, #20703, #35344, #13079, #28396, #46338 ),
 .UNSPECIFIED., .F., .F. ) 
 B_SPLINE_CURVE_WITH_KNOTS ( ( 3, 2, 2, 2, 3 ),
 ( 0.3900000000000000133, 0.3925000000000000155, 0.3950000000000000178, 0.3975000000000000200, 0.4000000000000000222 ),
 .UNSPECIFIED. ) 
 CURVE ( )  GEOMETRIC_REPRESENTATION_ITEM ( )  RATIONAL_B_SPLINE_CURVE ( ( 1.000000000000000000, 0.9238795325112869605, 1.000000000000000000, 0.9238795325112869605, 1.000000000000000000, 0.9238795325112869605, 1.000000000000000000, 0.9238795325112869605, 1.000000000000000000 ) ) 
 REPRESENTATION_ITEM ( '' )  ) ;
#26022=CARTESIAN_POINT ( 'NONE',  ( 0.9500414927467377701, -0.1787899950787401604, 0.8464566928596233275 ) ) ;
#26024=CARTESIAN_POINT ( 'NONE',  ( -0.9500414927467378812, -0.1787899950787401604, 1.279527559001355286 ) ) ;
#26028=CARTESIAN_POINT ( 'NONE',  ( -0.8759842519685039353, -0.1787899950787401882, 0.1747047243556852092 ) ) ;
#26035=CARTESIAN_POINT ( 'NONE',  ( 0.8759842519685039353, 0.1787899950787401882, 1.016240157426551161 ) ) ;
#26036=EDGE_CURVE ( 'NONE', #40552, #12346, #25979, .T. ) ;
#26038=CARTESIAN_POINT ( 'NONE',  ( -0.6971942568897626646, -0.07405724077823297447, 0.7529527558517473684 ) ) ;
#26041=CARTESIAN_POINT ( 'NONE',  ( -0.9500414927467377701, 0.1787899950787401604, 1.845472440891119392 ) ) ;
#26045=CARTESIAN_POINT ( 'NONE',  ( -0.6971942568897637749, 2.189545951927499583E-17, 0.04675196845017354913 ) ) ;
#26046=CARTESIAN_POINT ( 'NONE',  ( -0.9412147342319837628, -0.1574803149606297803, 0.9079724409448818312 ) ) ;
#26049=CARTESIAN_POINT ( 'NONE',  ( 0.7185039370078739607, 0.000000000000000000, 4.498031496062992574 ) ) ;
#26050=CARTESIAN_POINT ( 'NONE',  ( -1.033464566929133799, 0.000000000000000000, 1.456692913278299084 ) ) ;
#26051=CARTESIAN_POINT ( 'NONE',  ( 1.054774247047244096, 0.000000000000000000, 0.8932086613635591421 ) ) ;
#26054=CARTESIAN_POINT ( 'NONE',  ( 0.7185039370078739607, 1.928577636452523993E-17, 1.407480314960629864 ) ) ;
#26055=CARTESIAN_POINT ( 'NONE',  ( 0.7128155616400300154, -0.03638212410272396308, 1.983943496710521837 ) ) ;
#26058=CARTESIAN_POINT ( 'NONE',  ( 1.054774247047244540, -0.07405724077823318263, 0.8464566928596233275 ) ) ;
#26064=CARTESIAN_POINT ( 'NONE',  ( 1.002407869896990045, 0.1264236179284866091, 1.168799212544661348 ) ) ;
#26069=CARTESIAN_POINT ( 'NONE',  ( -0.8019270111902717657, 0.1787899950787401604, 0.3100393700249766682 ) ) ;
#26070=ORIENTED_EDGE ( 'NONE', *, *, #33363, .T. ) ;
#26071=CARTESIAN_POINT ( 'NONE',  ( 1.033464566929133799, 0.000000000000000000, 0.3248031496062992463 ) ) ;
#26073=CARTESIAN_POINT ( 'NONE',  ( -1.054774247047244096, 0.000000000000000000, 1.675688976324189117 ) ) ;
#26074=CARTESIAN_POINT ( 'NONE',  ( -0.9500414927467377701, -0.1787899950787401604, 0.8415354330171020969 ) ) ;
#26075=CARTESIAN_POINT ( 'NONE',  ( -0.9500414927467378812, 0.1787899950787401604, 0.5462598424659214080 ) ) ;
#26077=CARTESIAN_POINT ( 'NONE',  ( -0.7185039370078739607, 1.928577636452523993E-17, 0.09842519674286673292 ) ) ;
#26078=CARTESIAN_POINT ( 'NONE',  ( 1.033464566929134687, -0.06523048226347956391, 0.9916338582677169944 ) ) ;
#26083=CARTESIAN_POINT ( 'NONE',  ( -1.033464566929133355, 0.06523048226348168721, 1.892224409341292546 ) ) ;
#26086=ADVANCED_FACE ( 'NONE', ( #6333 ), #6575, .T. ) ;
#26089=CARTESIAN_POINT ( 'NONE',  ( -1.054774247047244540, -0.07405724077823318263, 0.2559055117572600624 ) ) ;
#26092=ORIENTED_EDGE ( 'NONE', *, *, #28058, .F. ) ;
#26094=CARTESIAN_POINT ( 'NONE',  ( -0.6971942568897648851, -0.07405724077823297447, 1.309055118056473122 ) ) ;
#26095=ORIENTED_EDGE ( 'NONE', *, *, #11174, .F. ) ;
#26100=CARTESIAN_POINT ( 'NONE',  ( 0.8107537697050253289, 0.1574803149606300301, 0.4158464566929134243 ) ) ;
#26102=CARTESIAN_POINT ( 'NONE',  ( -1.033464566929134687, 0.06523048226347956391, 1.104822834538142340 ) ) ;
#26103=CARTESIAN_POINT ( 'NONE',  ( 1.054774247047244540, 0.07405724077823318263, 0.4625984251430869665 ) ) ;
#26106=VERTEX_POINT ( 'NONE', #47316 ) ;
#26107=CARTESIAN_POINT ( 'NONE',  ( 1.033464566929134687, -0.06523048226347956391, 2.005413385719245323 ) ) ;
#26110=CARTESIAN_POINT ( 'NONE',  ( -1.054774247047244096, 0.000000000000000000, 0.8932086613635591421 ) ) ;
#26111=CARTESIAN_POINT ( 'NONE',  ( 1.033464566929134687, -0.06523048226347956391, 0.9916338582677171054 ) ) ;
#26119=CARTESIAN_POINT ( 'NONE',  ( 1.054774247047244540, 0.07405724077823318263, 0.5364173227808821665 ) ) ;
#26120=ORIENTED_EDGE ( 'NONE', *, *, #11974, .F. ) ;
#26121=CARTESIAN_POINT ( 'NONE',  ( 0.8107537697050254399, -0.1574803149606297803, 0.8243110236220465570 ) ) ;
#26122=CARTESIAN_POINT ( 'NONE',  ( 0.7185039370078739607, 1.928577636452523993E-17, 0.5708661416247566844 ) ) ;
#26127=CARTESIAN_POINT ( 'NONE',  ( 0.9873396505805591694, -0.1113553986120547346, 1.136811023514519681 ) ) ;
#26128=( BOUNDED_CURVE ( )  B_SPLINE_CURVE ( 2, ( #39647, #107, #28684, #32745, #10213, #24816, #25301, #39416, #43003 ),
 .UNSPECIFIED., .F., .T. ) 
 B_SPLINE_CURVE_WITH_KNOTS ( ( 3, 2, 2, 2, 3 ),
 ( 0.8199999999999999512, 0.8225000000000000089, 0.8249999999999999556, 0.8275000000000000133, 0.8299999999999999600 ),
 .UNSPECIFIED. ) 
 CURVE ( )  GEOMETRIC_REPRESENTATION_ITEM ( )  RATIONAL_B_SPLINE_CURVE ( ( 1.000000000000000000, 0.9238795325112899581, 1.000000000000000000, 0.9238795325112869605, 1.000000000000000000, 0.9238795325112869605, 1.000000000000000000, 0.9238795325112829637, 1.000000000000000000 ) ) 
 REPRESENTATION_ITEM ( '' )  ) ;
#26130=ORIENTED_EDGE ( 'NONE', *, *, #29391, .F. ) ;
#26131=VERTEX_POINT ( 'NONE', #44170 ) ;
#26133=CARTESIAN_POINT ( 'NONE',  ( -0.8759842519685039353, -0.1787899950787401882, 1.749507873961984483 ) ) ;
#26134=CARTESIAN_POINT ( 'NONE',  ( 0.8759842519685039353, 0.1787899950787401882, 1.690452755851748146 ) ) ;
#26136=CARTESIAN_POINT ( 'NONE',  ( -0.9500414927467378812, 0.1787899950787401604, 0.8218503936470251681 ) ) ;
#26138=CARTESIAN_POINT ( 'NONE',  ( 0.8019270111902717657, -0.1787899950787401604, 0.2903543306548980185 ) ) ;
#26139=CARTESIAN_POINT ( 'NONE',  ( -0.9500414927467377701, -0.1787899950787401604, 1.274606299158834277 ) ) ;
#26141=DIRECTION ( 'NONE',  ( 1.822029033848725028E-16, 0.000000000000000000, 1.000000000000000000 ) ) ;
#26142=CARTESIAN_POINT ( 'NONE',  ( -0.6971942568897648851, 0.07405724077823318263, 1.619094488135213838 ) ) ;
#26143=CARTESIAN_POINT ( 'NONE',  ( -0.8107537697050253289, 0.1574803149606300301, 1.823326771546016856 ) ) ;
#26146=CARTESIAN_POINT ( 'NONE',  ( -0.9873396505805591694, 0.1113553986120547346, 1.550196850393700920 ) ) ;
#26147=CARTESIAN_POINT ( 'NONE',  ( 0.7185039370078739607, 1.928577636452523993E-17, 0.9645669290263307882 ) ) ;
#26148=CARTESIAN_POINT ( 'NONE',  ( 0.8759842519685039353, 0.1787899950787401882, 1.572342519631275692 ) ) ;
#26150=DIRECTION ( 'NONE',  ( 1.822029033848725028E-16, 0.000000000000000000, 1.000000000000000000 ) ) ;
#26153=AXIS2_PLACEMENT_3D ( 'NONE', #24295, #38893, #46783 ) ;
#26158=EDGE_CURVE ( 'NONE', #31350, #13767, #22327, .T. ) ;
#26169=DIRECTION ( 'NONE',  ( 0.000000000000000000, 0.000000000000000000, -1.000000000000000000 ) ) ;
#26170=CARTESIAN_POINT ( 'NONE',  ( 0.9500414927467378812, -0.1787899950787401604, 0.8021653542769460188 ) ) ;
#26175=CARTESIAN_POINT ( 'NONE',  ( 0.8107537697050254399, 0.1574803149606300301, 0.4552165354330711677 ) ) ;
#26176=CARTESIAN_POINT ( 'NONE',  ( 0.7495606340400177148, -0.1264236179284866091, 1.783956692859621995 ) ) ;
#26177=CARTESIAN_POINT ( 'NONE',  ( 0.8759842519685039353, 0.000000000000000000, 1.990649606245448844 ) ) ;
#26180=CARTESIAN_POINT ( 'NONE',  ( 0.8107537697050234415, -0.1574803149606297803, 0.03690944881889771101 ) ) ;
#26184=CARTESIAN_POINT ( 'NONE',  ( -0.7185039370078739607, 1.928577636452523993E-17, 0.1870078740157480324 ) ) ;
#26186=CARTESIAN_POINT ( 'NONE',  ( 0.9500414927467378812, -0.1787899950787401604, 0.1771653542769452139 ) ) ;
#26189=CARTESIAN_POINT ( 'NONE',  ( -0.7495606340400177148, 0.1264236179284866091, 1.808562992072220377 ) ) ;
#26191=CARTESIAN_POINT ( 'NONE',  ( -0.9500414927467378812, 0.1787899950787401604, 1.215551181048599272 ) ) ;
#26192=CARTESIAN_POINT ( 'NONE',  ( -0.7185039370078739607, 0.000000000000000000, -2.869337061179095023E-17 ) ) ;
#26193=CARTESIAN_POINT ( 'NONE',  ( 0.6971942568897637749, 2.189545951927499583E-17, 1.306594488135212728 ) ) ;
#26196=CARTESIAN_POINT ( 'NONE',  ( 0.7495606340400177148, 0.1264236179284866091, 1.966043307032850462 ) ) ;
#26197=CARTESIAN_POINT ( 'NONE',  ( -0.7495606340400177148, -0.1264236179284866091, 0.9916338582139527791 ) ) ;
#26200=CARTESIAN_POINT ( 'NONE',  ( 0.8019270111902716547, -0.1787899950787401604, 0.4872047243556847929 ) ) ;
#26201=CARTESIAN_POINT ( 'NONE',  ( -0.6971942568897648851, 0.07405724077823318263, 0.3937007873478114983 ) ) ;
#26202=CARTESIAN_POINT ( 'NONE',  ( -0.8759842519685039353, -0.1787899950787401882, 0.7997047243556849594 ) ) ;
#26204=ORIENTED_EDGE ( 'NONE', *, *, #45808, .F. ) ;
#26205=CARTESIAN_POINT ( 'NONE',  ( -0.8107537697050254399, 0.1574803149606300301, 1.360728346456693050 ) ) ;
#26207=CARTESIAN_POINT ( 'NONE',  ( -0.8759842519685039353, 0.1574803149606299191, 0.2165354330708661457 ) ) ;
#26208=CARTESIAN_POINT ( 'NONE',  ( 1.054774247047244096, 0.000000000000000000, 1.090059055064346527 ) ) ;
#26210=ORIENTED_EDGE ( 'NONE', *, *, #37653, .T. ) ;
#26211=CARTESIAN_POINT ( 'NONE',  ( 0.7495606340400177148, 0.1264236179284866091, 1.966043307032850462 ) ) ;
#26213=CARTESIAN_POINT ( 'NONE',  ( -0.8759842519685039353, 0.1787899950787401882, 0.07135826766277185429 ) ) ;
#26215=EDGE_LOOP ( 'NONE', ( #12670, #33126, #40916, #29870 ) ) ;
#26218=ORIENTED_EDGE ( 'NONE', *, *, #30192, .F. ) ;
#26219=CARTESIAN_POINT ( 'NONE',  ( 1.002407869896990045, -0.1264236179284866091, 1.198326771599779628 ) ) ;
#26223=CARTESIAN_POINT ( 'NONE',  ( 1.002407869896990045, 0.1264236179284866091, 0.1451771653005673179 ) ) ;
#26229=CARTESIAN_POINT ( 'NONE',  ( -0.8759842519685039353, -0.1574803149606299191, 1.131889763672000004 ) ) ;
#26231=CARTESIAN_POINT ( 'NONE',  ( -0.6971942568897648851, 0.07405724077823318263, 0.5954724408911187261 ) ) ;
#26235=CARTESIAN_POINT ( 'NONE',  ( 0.8759842519685039353, -0.1787899950787401882, 1.434547244040724534 ) ) ;
#26236=CARTESIAN_POINT ( 'NONE',  ( 0.8759842519685039353, 0.1787899950787401882, 1.724901574749385880 ) ) ;
#26237=CARTESIAN_POINT ( 'NONE',  ( -0.9412147342319837628, -0.1574803149606297803, 1.646161417215307843 ) ) ;
#26239=CARTESIAN_POINT ( 'NONE',  ( -0.7444854923987453965, 0.09565579475716033675, 1.981284257674885918 ) ) ;
#26241=DIRECTION ( 'NONE',  ( -1.000000000000000000, 0.000000000000000000, 0.000000000000000000 ) ) ;
#26243=CARTESIAN_POINT ( 'NONE',  ( 0.6971942568897626646, -0.07405724077823297447, 0.3198818897100162983 ) ) ;
#26244=CARTESIAN_POINT ( 'NONE',  ( -0.7646288533564489232, -0.1113553986120547346, 1.717519684931842594 ) ) ;
#26247=CARTESIAN_POINT ( 'NONE',  ( -0.6971942568897637749, 2.189545951927499583E-17, 1.262303149552535420 ) ) ;
#26248=CARTESIAN_POINT ( 'NONE',  ( 0.9412147342319837628, 0.1574803149606300301, 0.6373031494987718704 ) ) ;
#26250=CARTESIAN_POINT ( 'NONE',  ( -1.033464566929133799, 0.000000000000000000, 0.1968503935932602311 ) ) ;
#26252=VERTEX_POINT ( 'NONE', #33203 ) ;
#26254=CARTESIAN_POINT ( 'NONE',  ( -0.8759842519685039353, -0.1574803149606299191, 0.3051181101286932762 ) ) ;
#26257=CARTESIAN_POINT ( 'NONE',  ( 0.6971942568897648851, -0.07405724077823297447, 1.658464566875369472 ) ) ;
#26258=CARTESIAN_POINT ( 'NONE',  ( -0.7185039370078746268, 0.06523048226347956391, 1.129429133858268042 ) ) ;
#26259=DIRECTION ( 'NONE',  ( 1.822029033848725028E-16, 0.000000000000000000, 1.000000000000000000 ) ) ;
#26261=CARTESIAN_POINT ( 'NONE',  ( 0.7185039370078746268, 0.06523048226347956391, 1.680610236220472009 ) ) ;
#26262=CARTESIAN_POINT ( 'NONE',  ( 0.6971942568897626646, -0.07405724077823297447, 0.04921259837143338728 ) ) ;
#26263=CARTESIAN_POINT ( 'NONE',  ( -0.9500414927467377701, -0.1787899950787401604, 0.05413385821395302888 ) ) ;
#26270=CARTESIAN_POINT ( 'NONE',  ( 0.8759842519685039353, -0.1787899950787401882, 0.9227362204186770889 ) ) ;
#26271=CARTESIAN_POINT ( 'NONE',  ( -1.054774247047244540, 0.07405724077823318263, 1.520669291284818758 ) ) ;
#26273=CARTESIAN_POINT ( 'NONE',  ( -0.8759842519685039353, 0.1787899950787401882, 1.257381889710015743 ) ) ;
#26275=VECTOR ( 'NONE', #43952, 39.37007874015748143 ) ;
#26276=ORIENTED_EDGE ( 'NONE', *, *, #42281, .F. ) ;
#26278=CARTESIAN_POINT ( 'NONE',  ( -1.054774247047244096, 0.000000000000000000, 0.3026574802611972648 ) ) ;
#26280=DIRECTION ( 'NONE',  ( 0.000000000000000000, 0.000000000000000000, -1.000000000000000000 ) ) ;
#26283=ORIENTED_EDGE ( 'NONE', *, *, #22561, .F. ) ;
#26289=EDGE_CURVE ( 'NONE', #31847, #12102, #14649, .T. ) ;
#26290=DIRECTION ( 'NONE',  ( 0.000000000000000000, 0.000000000000000000, -1.000000000000000000 ) ) ;
#26293=CARTESIAN_POINT ( 'NONE',  ( -1.054774247047244540, 0.07405724077823318263, 0.2263779527021417270 ) ) ;
#26294=CARTESIAN_POINT ( 'NONE',  ( -1.033464566929134687, -0.06523048226347956391, 0.8341535433070870198 ) ) ;
#26298=CARTESIAN_POINT ( 'NONE',  ( -0.9412147342319837628, -0.1574803149606297803, 1.567421259734991690 ) ) ;
#26299=CARTESIAN_POINT ( 'NONE',  ( 0.7495606340400177148, -0.1264236179284866091, 0.8784448818360000022 ) ) ;
#26302=CARTESIAN_POINT ( 'NONE',  ( 0.8759842519685039353, 0.000000000000000000, 4.498031496062992574 ) ) ;
#26303=CARTESIAN_POINT ( 'NONE',  ( 0.7100943080231756355, -0.01414046681897546467, 1.983520156233079756 ) ) ;
#26304=CARTESIAN_POINT ( 'NONE',  ( 0.7185039370078766252, -0.06523048226348168721, 1.557578740049954558 ) ) ;
#26307=( BOUNDED_CURVE ( )  B_SPLINE_CURVE ( 2, ( #30754, #12058, #19458, #37683, #34338, #11582, #33645, #16127, #8673 ),
 .UNSPECIFIED., .F., .F. ) 
 B_SPLINE_CURVE_WITH_KNOTS ( ( 3, 2, 2, 2, 3 ),
 ( 0.9599999999999999645, 0.9625000000000000222, 0.9649999999999999689, 0.9675000000000000266, 0.9699999999999999734 ),
 .UNSPECIFIED. ) 
 CURVE ( )  GEOMETRIC_REPRESENTATION_ITEM ( )  RATIONAL_B_SPLINE_CURVE ( ( 1.000000000000000000, 0.9238795325112869605, 1.000000000000000000, 0.9238795325112869605, 1.000000000000000000, 0.9238795325112869605, 1.000000000000000000, 0.9238795325112799661, 1.000000000000000000 ) ) 
 REPRESENTATION_ITEM ( '' )  ) ;
#26308=CARTESIAN_POINT ( 'NONE',  ( 0.7495606340400177148, -0.1264236179284866091, 0.8735236219934803259 ) ) ;
#26314=CARTESIAN_POINT ( 'NONE',  ( 0.8759842519685039353, 0.1787899950787401882, 1.213090551127338435 ) ) ;
#26320=CYLINDRICAL_SURFACE ( 'NONE', #36727, 0.1574803149606299191 ) ;
#26321=CARTESIAN_POINT ( 'NONE',  ( -0.8019270111902717657, -0.1787899950787401604, 0.2460629920722207375 ) ) ;
#26327=CARTESIAN_POINT ( 'NONE',  ( -1.054774247047244096, 0.000000000000000000, 1.872539370024976391 ) ) ;
#26328=CARTESIAN_POINT ( 'NONE',  ( -0.6971942568897626646, -0.07405724077823297447, 0.4822834645131655606 ) ) ;
#26329=CARTESIAN_POINT ( 'NONE',  ( -1.033464566929134687, -0.06523048226347956391, 0.6766732283464570452 ) ) ;
#26330=CARTESIAN_POINT ( 'NONE',  ( 0.7185039370078746268, 0.06523048226347956391, 0.4109251967428667052 ) ) ;
#26332=CARTESIAN_POINT ( 'NONE',  ( -1.033464566929133799, 0.000000000000000000, 1.978346456692913646 ) ) ;
#26336=CYLINDRICAL_SURFACE ( 'NONE', #22607, 0.1574803149606299191 ) ;
#26337=CARTESIAN_POINT ( 'NONE',  ( -0.9873396505805591694, -0.1113553986120547346, 1.176181102254677313 ) ) ;
#26338=CARTESIAN_POINT ( 'NONE',  ( -0.9500414927467378812, 0.1787899950787401604, 0.2657480314422993595 ) ) ;
#26342=CARTESIAN_POINT ( 'NONE',  ( -0.7495606340400177148, -0.1264236179284866091, 1.547736220418677089 ) ) ;
#26348=CARTESIAN_POINT ( 'NONE',  ( 0.9412147342319837628, -0.1574803149606297803, 0.4355314960629916299 ) ) ;
#26350=CARTESIAN_POINT ( 'NONE',  ( -0.7646288533564489232, -0.1113553986120547346, 1.126968503829480328 ) ) ;
#26351=CARTESIAN_POINT ( 'NONE',  ( 1.054774247047244540, -0.07405724077823318263, 0.4970472440407249226 ) ) ;
#26354=CARTESIAN_POINT ( 'NONE',  ( 0.9873396505805591694, 0.1113553986120547346, 1.973425196742866206 ) ) ;
#26356=AXIS2_PLACEMENT_3D ( 'NONE', #3101, #2852, #10802 ) ;
#26358=CARTESIAN_POINT ( 'NONE',  ( -0.8759842519685039353, 0.1787899950787401882, 1.021161417269070837 ) ) ;
#26359=CARTESIAN_POINT ( 'NONE',  ( 0.7646288533564489232, -0.1113553986120547346, 1.018700787401574770 ) ) ;
#26361=CARTESIAN_POINT ( 'NONE',  ( -0.7646288533564489232, -0.1113553986120547346, 0.8218503937007874960 ) ) ;
#26368=DIRECTION ( 'NONE',  ( 1.822029033848725028E-16, 0.000000000000000000, 1.000000000000000000 ) ) ;
#26369=CARTESIAN_POINT ( 'NONE',  ( 0.9412147342319837628, 0.1574803149606300301, 1.149114173120819427 ) ) ;
#26373=CARTESIAN_POINT ( 'NONE',  ( 0.9412147342319837628, -0.1574803149606297803, 1.173720472333417586 ) ) ;
#26374=EDGE_CURVE ( 'NONE', #14529, #28682, #38172, .T. ) ;
#26375=CARTESIAN_POINT ( 'NONE',  ( 0.9873396505805591694, 0.1113553986120547346, 1.825787401574803237 ) ) ;
#26378=CARTESIAN_POINT ( 'NONE',  ( -0.6971942568897637749, 2.189545951927499583E-17, 1.700295275536787498 ) ) ;
#26379=EDGE_CURVE ( 'NONE', #13566, #2118, #39360, .T. ) ;
#26380=CARTESIAN_POINT ( 'NONE',  ( 1.054774247047244540, 0.07405724077823318263, 1.643700787347811998 ) ) ;
#26381=CARTESIAN_POINT ( 'NONE',  ( 1.033464566929133799, 0.000000000000000000, 0.1673228346456692994 ) ) ;
#26382=CARTESIAN_POINT ( 'NONE',  ( 0.8019270111902717657, -0.1787899950787401604, 0.2509842519147403861 ) ) ;
#26384=CARTESIAN_POINT ( 'NONE',  ( -0.6971942568897648851, -0.07405724077823297447, 1.186023621993481658 ) ) ;
#26385=CARTESIAN_POINT ( 'NONE',  ( -0.6971942568897626646, 0.07405724077823318263, 0.9448818897100165204 ) ) ;
#26386=CARTESIAN_POINT ( 'NONE',  ( -0.7495606340400177148, 0.1264236179284866091, 0.08120078734781142893 ) ) ;
#26387=DIRECTION ( 'NONE',  ( 1.000000000000000000, 0.000000000000000000, -1.822029033848725275E-16 ) ) ;
#26388=CARTESIAN_POINT ( 'NONE',  ( -0.8019270111902717657, -0.1787899950787401604, 1.550196850339937926 ) ) ;
#26389=CARTESIAN_POINT ( 'NONE',  ( -1.033464566929134687, 0.06523048226347956391, 1.813484251860976393 ) ) ;
#26390=ORIENTED_EDGE ( 'NONE', *, *, #2264, .T. ) ;
#26391=CARTESIAN_POINT ( 'NONE',  ( -0.9873396505805591694, 0.1113553986120547346, 1.668307086614173373 ) ) ;
#26393=CARTESIAN_POINT ( 'NONE',  ( 0.8759842519685039353, -0.1787899950787401882, 1.631397637741511808 ) ) ;
#26404=ORIENTED_EDGE ( 'NONE', *, *, #10481, .T. ) ;
#26405=CARTESIAN_POINT ( 'NONE',  ( -1.033464566929133799, 0.000000000000000000, 0.07874015737278799998 ) ) ;
#26409=LINE ( 'NONE', #4552, #40617 ) ;
#26410=CARTESIAN_POINT ( 'NONE',  ( 0.8019270111902717657, -0.1787899950787401604, 0.7578740156942689321 ) ) ;
#26415=CARTESIAN_POINT ( 'NONE',  ( 1.054774247047244096, 0.000000000000000000, 1.877460629867496067 ) ) ;
#26417=CARTESIAN_POINT ( 'NONE',  ( 0.8107537697050253289, 0.1574803149606300301, 0.1402559055118110520 ) ) ;
#26421=CARTESIAN_POINT ( 'NONE',  ( -1.033464566929133799, 0.000000000000000000, 0.5511811022546772021 ) ) ;
#26423=CARTESIAN_POINT ( 'NONE',  ( 1.002407869896990045, 0.1264236179284866091, 0.2682086613635594752 ) ) ;
#26424=ADVANCED_FACE ( 'NONE', ( #27190 ), #19489, .T. ) ;
#26426=CARTESIAN_POINT ( 'NONE',  ( -1.002407869896990045, 0.1264236179284866091, 1.680610236166708793 ) ) ;
#26429=CARTESIAN_POINT ( 'NONE',  ( -1.002407869896990045, 0.1264236179284866091, 1.291830708607653477 ) ) ;
#26430=CARTESIAN_POINT ( 'NONE',  ( 0.7185039370078739607, 1.928577636452523993E-17, 1.013779527559055094 ) ) ;
#26432=CARTESIAN_POINT ( 'NONE',  ( -0.9500414927467378812, -0.1787899950787401604, 0.4921259841982048577 ) ) ;
#26433=CARTESIAN_POINT ( 'NONE',  ( 1.002407869896990045, -0.1264236179284866091, 1.906988188922614125 ) ) ;
#26434=CARTESIAN_POINT ( 'NONE',  ( -0.8019270111902717657, 0.1787899950787401604, 1.058070866087969186 ) ) ;
#26437=DIRECTION ( 'NONE',  ( 1.000000000000000000, 0.000000000000000000, -1.822029033848725275E-16 ) ) ;
#26438=CARTESIAN_POINT ( 'NONE',  ( 0.6971942568897637749, 2.189545951927499583E-17, 0.4404527558517480901 ) ) ;
#26439=CARTESIAN_POINT ( 'NONE',  ( -0.7495606340400177148, -0.1264236179284866091, 0.4404527558517480901 ) ) ;
#26440=VERTEX_POINT ( 'NONE', #33669 ) ;
#26442=CARTESIAN_POINT ( 'NONE',  ( -0.8107537697050253289, 0.1574803149606300301, 0.1796259842519684069 ) ) ;
#26443=CARTESIAN_POINT ( 'NONE',  ( 0.8019270111902716547, -0.1787899950787401604, 1.195866141678520345 ) ) ;
#26446=CARTESIAN_POINT ( 'NONE',  ( -0.8107537697050254399, -0.1574803149606297803, 1.296751968503936592 ) ) ;
#26447=DIRECTION ( 'NONE',  ( -1.000000000000000000, 0.000000000000000000, 0.000000000000000000 ) ) ;
#26448=CARTESIAN_POINT ( 'NONE',  ( -0.9412147342319837628, -0.1574803149606297803, 0.1993110236220472509 ) ) ;
#26450=ORIENTED_EDGE ( 'NONE', *, *, #6617, .F. ) ;
#26453=CARTESIAN_POINT ( 'NONE',  ( -1.033464566929134687, 0.06523048226347956391, 1.695374015640504828 ) ) ;
#26454=VERTEX_POINT ( 'NONE', #5100 ) ;
#26455=CARTESIAN_POINT ( 'NONE',  ( 0.8759842519685039353, -0.1787899950787401882, 1.311515747977732405 ) ) ;
#26457=CARTESIAN_POINT ( 'NONE',  ( 0.7646288533564489232, 0.1113553986120547346, 1.599409448818897683 ) ) ;
#26462=CARTESIAN_POINT ( 'NONE',  ( 0.7495606340400177148, 0.1264236179284866091, 1.532972440891118060 ) ) ;
#26468=CARTESIAN_POINT ( 'NONE',  ( -1.054774247047244540, -0.07405724077823318263, 0.6938976377415124741 ) ) ;
#26470=CARTESIAN_POINT ( 'NONE',  ( 1.033464566929134687, -0.06523048226347956391, 0.3124999998924728462 ) ) ;
#26474=CARTESIAN_POINT ( 'NONE',  ( 1.054774247047244540, 0.07405724077823318263, 1.874999999946236784 ) ) ;
#26475=CARTESIAN_POINT ( 'NONE',  ( 0.7185039370078739607, 1.928577636452523993E-17, 0.1476377952755905387 ) ) ;
#26477=FACE_OUTER_BOUND ( 'NONE', #20848, .T. ) ;
#26479=CARTESIAN_POINT ( 'NONE',  ( -0.9412147342319837628, -0.1574803149606297803, 1.026082677165353729 ) ) ;
#26480=CARTESIAN_POINT ( 'NONE',  ( -0.7185039370078739607, 1.928577636452523993E-17, 0.2165354329633393804 ) ) ;
#26481=CARTESIAN_POINT ( 'NONE',  ( 0.6971942568897626646, 0.07405724077823318263, 0.3149606298674962890 ) ) ;
#26482=ADVANCED_FACE ( 'NONE', ( #1267 ), #19724, .T. ) ;
#26484=DIRECTION ( 'NONE',  ( -1.000000000000000000, 0.000000000000000000, 0.000000000000000000 ) ) ;
#26485=CARTESIAN_POINT ( 'NONE',  ( 1.033464566929134687, 0.06523048226347956391, 0.5930118109160945616 ) ) ;
#26487=CARTESIAN_POINT ( 'NONE',  ( -0.7495606340400177148, -0.1264236179284866091, 1.075295275536787276 ) ) ;
#26488=CARTESIAN_POINT ( 'NONE',  ( 1.033464566929133799, 0.000000000000000000, 1.387795275590551158 ) ) ;
#26489=CARTESIAN_POINT ( 'NONE',  ( 0.7646288533564489232, 0.1113553986120547346, 0.6938976377952755792 ) ) ;
#26494=CARTESIAN_POINT ( 'NONE',  ( 1.002407869896990045, -0.1264236179284866091, 1.592027559001354398 ) ) ;
#26495=CARTESIAN_POINT ( 'NONE',  ( -0.7646288533564489232, 0.1113553986120547346, 1.205708661417322913 ) ) ;
#26500=CARTESIAN_POINT ( 'NONE',  ( 1.033464566929133799, 1.928577636452524610E-17, 4.498031496062991685 ) ) ;
#26501=CARTESIAN_POINT ( 'NONE',  ( -1.033464566929133799, 0.000000000000000000, 0.5118110235145196807 ) ) ;
#26505=DIRECTION ( 'NONE',  ( 1.000000000000000000, 0.000000000000000000, -1.822029033848725275E-16 ) ) ;
#26506=CARTESIAN_POINT ( 'NONE',  ( -1.002407869896990045, 0.1264236179284866091, 1.562499999946236118 ) ) ;
#26510=CARTESIAN_POINT ( 'NONE',  ( -0.7495606340400177148, 0.1264236179284866091, 0.2780511810485988278 ) ) ;
#26512=CARTESIAN_POINT ( 'NONE',  ( -0.7646288533564489232, -0.1113553986120547346, 1.874999999892472458 ) ) ;
#26519=CARTESIAN_POINT ( 'NONE',  ( 1.033464566929133799, 1.928577636452524610E-17, 4.498031496062992574 ) ) ;
#26521=CARTESIAN_POINT ( 'NONE',  ( 0.7185039370078739607, 1.928577636452523993E-17, 1.437007873908220601 ) ) ;
#26523=CARTESIAN_POINT ( 'NONE',  ( -0.8019270111902716547, -0.1787899950787401604, 0.1722440944344256208 ) ) ;
#26524=CARTESIAN_POINT ( 'NONE',  ( -0.8759842519685039353, 0.1574803149606299191, 0.9645669291338583307 ) ) ;
#26525=CARTESIAN_POINT ( 'NONE',  ( -0.7185039370078739607, 0.000000000000000000, -2.869337061179095023E-17 ) ) ;
#26526=DIRECTION ( 'NONE',  ( 0.000000000000000000, 1.000000000000000000, 0.000000000000000000 ) ) ;
#26529=CARTESIAN_POINT ( 'NONE',  ( -0.9412147342319837628, 0.1574803149606300301, 1.464074803042079598 ) ) ;
#26530=ADVANCED_FACE ( 'NONE', ( #41034 ), #8228, .T. ) ;
#26531=CARTESIAN_POINT ( 'NONE',  ( 1.002407869896990045, -0.1264236179284866091, 0.9670275590013542866 ) ) ;
#26532=CARTESIAN_POINT ( 'NONE',  ( 0.7185039370078739607, 1.928577636452523993E-17, 0.5314960628845992741 ) ) ;
#26533=CARTESIAN_POINT ( 'NONE',  ( 1.033464566929133799, 0.000000000000000000, 1.427165354330708569 ) ) ;
#26534=CARTESIAN_POINT ( 'NONE',  ( 0.7101297187648138998, 0.003597347259315822592, 1.983202747004803257 ) ) ;
#26537=CARTESIAN_POINT ( 'NONE',  ( 1.033464566929134687, -0.06523048226347956391, 0.7947834645669290543 ) ) ;
#26538=EDGE_CURVE ( 'NONE', #14442, #36086, #11298, .T. ) ;
#26539=CARTESIAN_POINT ( 'NONE',  ( 1.054774247047244096, 0.000000000000000000, 0.7701771653005669016 ) ) ;
#26541=CARTESIAN_POINT ( 'NONE',  ( 0.6971942568897648851, 0.07405724077823318263, 1.815944881835999780 ) ) ;
#26545=CARTESIAN_POINT ( 'NONE',  ( -0.9412147342319837628, 0.1574803149606300301, 0.8439960629921254842 ) ) ;
#26547=CARTESIAN_POINT ( 'NONE',  ( -0.7185039370078746268, 0.06523048226347956391, 0.1353346455617644717 ) ) ;
#26548=CARTESIAN_POINT ( 'NONE',  ( 1.002407869896990045, -0.1264236179284866091, 1.158956692859621995 ) ) ;
#26550=CARTESIAN_POINT ( 'NONE',  ( -0.8759842519685039353, 0.1574803149606299191, 1.043307086614173151 ) ) ;
#26552=CARTESIAN_POINT ( 'NONE',  ( 1.033464566929134687, 0.06523048226347956391, 1.301673228238930502 ) ) ;
#26555=CARTESIAN_POINT ( 'NONE',  ( -0.6971942568897637749, 2.189545951927499583E-17, 0.5142716534895434011 ) ) ;
#26558=CARTESIAN_POINT ( 'NONE',  ( -1.002407869896990045, 0.1264236179284866091, 0.3026574802611972648 ) ) ;
#26562=CARTESIAN_POINT ( 'NONE',  ( -0.6971942568897637749, 2.189545951927499583E-17, 1.774114173174582643 ) ) ;
#26563=CARTESIAN_POINT ( 'NONE',  ( -0.6971942568897648851, -0.07405724077823297447, 0.8316929133320636325 ) ) ;
#26564=CARTESIAN_POINT ( 'NONE',  ( -0.7495606340400177148, 0.1264236179284866091, 0.5142716534895434011 ) ) ;
#26567=CARTESIAN_POINT ( 'NONE',  ( -0.9873396505805591694, 0.1113553986120547346, 0.3198818896562523606 ) ) ;
#26571=FACE_OUTER_BOUND ( 'NONE', #30446, .T. ) ;
#26572=CARTESIAN_POINT ( 'NONE',  ( 0.7646288533564489232, -0.1113553986120547346, 1.924212598425196985 ) ) ;
#26574=CARTESIAN_POINT ( 'NONE',  ( -0.6971942568897637749, 2.189545951927499583E-17, 0.2780511810485988278 ) ) ;
#26579=CARTESIAN_POINT ( 'NONE',  ( -0.8019270111902716547, 0.1787899950787401604, 1.496062992072220599 ) ) ;
#26584=( BOUNDED_CURVE ( )  B_SPLINE_CURVE ( 2, ( #599, #33482, #29900, #1315, #22183, #40846, #11196, #37270, #33248 ),
 .UNSPECIFIED., .F., .F. ) 
 B_SPLINE_CURVE_WITH_KNOTS ( ( 3, 2, 2, 2, 3 ),
 ( 0.5899999999999999689, 0.5925000000000000266, 0.5949999999999999734, 0.5975000000000000311, 0.5999999999999999778 ),
 .UNSPECIFIED. ) 
 CURVE ( )  GEOMETRIC_REPRESENTATION_ITEM ( )  RATIONAL_B_SPLINE_CURVE ( ( 1.000000000000000000, 0.9238795325112869605, 1.000000000000000000, 0.9238795325112869605, 1.000000000000000000, 0.9238795325112869605, 1.000000000000000000, 0.9238795325112869605, 1.000000000000000000 ) ) 
 REPRESENTATION_ITEM ( '' )  ) ;
#26587=CARTESIAN_POINT ( 'NONE',  ( 0.9873396505805591694, 0.1113553986120547346, 0.5265748031496062520 ) ) ;
#26589=CARTESIAN_POINT ( 'NONE',  ( -0.8759842519685039353, -0.1574803149606299191, 1.013779527451527551 ) ) ;
#26592=VERTEX_POINT ( 'NONE', #6934 ) ;
#26593=CARTESIAN_POINT ( 'NONE',  ( 0.9412147342319837628, -0.1574803149606297803, 1.961122047136568014 ) ) ;
#26595=CYLINDRICAL_SURFACE ( 'NONE', #19189, 0.1574803149606299191 ) ;
#26596=CARTESIAN_POINT ( 'NONE',  ( -0.8019270111902716547, 0.1787899950787401604, 1.062992125930488418 ) ) ;
#26597=CARTESIAN_POINT ( 'NONE',  ( 0.9412147342319837628, 0.1574803149606300301, 0.8833661417322832277 ) ) ;
#26598=CARTESIAN_POINT ( 'NONE',  ( 1.033464566929134687, 0.06523048226347956391, 1.350885826771654141 ) ) ;
#26602=DIRECTION ( 'NONE',  ( 1.822029033848725028E-16, 0.000000000000000000, 1.000000000000000000 ) ) ;
#26604=CARTESIAN_POINT ( 'NONE',  ( 0.9500414927467378812, 0.1787899950787401604, 0.6988188975840318173 ) ) ;
#26611=CARTESIAN_POINT ( 'NONE',  ( 0.8759842519685039353, 0.1574803149606299191, 1.072834645561763889 ) ) ;
#26612=DIRECTION ( 'NONE',  ( 0.000000000000000000, 0.000000000000000000, -1.000000000000000000 ) ) ;
#26613=ORIENTED_EDGE ( 'NONE', *, *, #5038, .T. ) ;
#26615=CARTESIAN_POINT ( 'NONE',  ( -0.7495606340400177148, -0.1264236179284866091, 1.783956692859621995 ) ) ;
#26616=CARTESIAN_POINT ( 'NONE',  ( 0.7495606340400177148, 0.1264236179284866091, 1.695374015694267822 ) ) ;
#26618=CARTESIAN_POINT ( 'NONE',  ( -0.9500414927467378812, 0.1787899950787401604, 1.446850393647023614 ) ) ;
#26620=CARTESIAN_POINT ( 'NONE',  ( -0.6971942568897648851, 0.07405724077823318263, 1.181102362150960428 ) ) ;
#26621=CARTESIAN_POINT ( 'NONE',  ( -0.6971942568897637749, 2.189545951927499583E-17, 0.9079724408911180600 ) ) ;
#26623=CARTESIAN_POINT ( 'NONE',  ( -1.002407869896990045, 0.1264236179284866091, 0.1107283464029293202 ) ) ;
#26625=CARTESIAN_POINT ( 'NONE',  ( -1.054774247047244540, 0.07405724077823318263, 1.643700787347811998 ) ) ;
#26626=CARTESIAN_POINT ( 'NONE',  ( -0.7495606340400177148, -0.1264236179284866091, 0.05167322829269323931 ) ) ;
#26628=CARTESIAN_POINT ( 'NONE',  ( -0.8107537697050253289, -0.1574803149606297803, 1.572342519685040685 ) ) ;
#26629=CARTESIAN_POINT ( 'NONE',  ( -0.7185039370078739607, 1.928577636452523993E-17, 0.9350393700787401619 ) ) ;
#26630=CARTESIAN_POINT ( 'NONE',  ( 0.6971942568897648851, -0.07405724077823297447, 1.624015747977732849 ) ) ;
#26634=ORIENTED_EDGE ( 'NONE', *, *, #15795, .F. ) ;
#26636=ORIENTED_EDGE ( 'NONE', *, *, #46737, .F. ) ;
#26637=CARTESIAN_POINT ( 'NONE',  ( -0.7495606340400177148, 0.1264236179284866091, 1.183562992072220599 ) ) ;
#26638=EDGE_LOOP ( 'NONE', ( #24537, #10644, #9734, #46109 ) ) ;
#26641=EDGE_CURVE ( 'NONE', #23712, #21986, #29106, .T. ) ;
#26643=CIRCLE ( 'NONE', #10662, 0.1787899950787401049 ) ;
#26647=EDGE_CURVE ( 'NONE', #11821, #47083, #35782, .T. ) ;
#26649=CARTESIAN_POINT ( 'NONE',  ( -0.9412147342319837628, 0.1574803149606300301, 0.1353346456692914035 ) ) ;
#26650=CARTESIAN_POINT ( 'NONE',  ( 0.9500414927467378812, 0.1787899950787401604, 0.7775590550643479704 ) ) ;
#26654=CARTESIAN_POINT ( 'NONE',  ( -0.9873396505805591694, 0.1113553986120547346, 1.264763779420031486 ) ) ;
#26656=CARTESIAN_POINT ( 'NONE',  ( 1.054774247047244540, 0.07405724077823318263, 1.840551181048599938 ) ) ;
#26657=CARTESIAN_POINT ( 'NONE',  ( 0.7185039370078739607, 1.928577636452523993E-17, 0.1476377952755905387 ) ) ;
#26662=CARTESIAN_POINT ( 'NONE',  ( 0.7495606340400177148, -0.1264236179284866091, 0.2878937007336381804 ) ) ;
#26663=CARTESIAN_POINT ( 'NONE',  ( -0.8759842519685039353, -0.1787899950787401882, 1.783956692859621995 ) ) ;
#26664=EDGE_LOOP ( 'NONE', ( #19991, #26390, #18305, #42024 ) ) ;
#26665=CARTESIAN_POINT ( 'NONE',  ( -0.6971942568897648851, 0.07405724077823318263, 1.343503936954111744 ) ) ;
#26666=CARTESIAN_POINT ( 'NONE',  ( 0.9873396505805591694, -0.1113553986120547346, 1.028543307086614123 ) ) ;
#26667=CARTESIAN_POINT ( 'NONE',  ( -0.6971942568897637749, 2.189545951927499583E-17, 0.5585629920722204877 ) ) ;
#26668=CARTESIAN_POINT ( 'NONE',  ( 1.002407869896990045, 0.1264236179284866091, 1.956200787347811110 ) ) ;
#26669=CARTESIAN_POINT ( 'NONE',  ( -0.8019270111902717657, 0.1787899950787401604, 1.136811023568283119 ) ) ;
#26670=CARTESIAN_POINT ( 'NONE',  ( 0.8759842519685039353, 0.1574803149606299191, 1.545275590443653480 ) ) ;
#26673=CARTESIAN_POINT ( 'NONE',  ( 0.8759842519685039353, -0.1787899950787401882, 0.5290354330171024300 ) ) ;
#26674=CARTESIAN_POINT ( 'NONE',  ( -0.9500414927467377701, 0.1787899950787401604, 0.3838582676627718127 ) ) ;
#26680=CARTESIAN_POINT ( 'NONE',  ( -0.7646288533564489232, -0.1113553986120547346, 0.1525590551181102428 ) ) ;
#26681=CARTESIAN_POINT ( 'NONE',  ( 0.8759842519685039353, 0.1787899950787401882, 1.178641732229700922 ) ) ;
#26682=CARTESIAN_POINT ( 'NONE',  ( -1.054774247047244096, 0.000000000000000000, 1.951279527505291433 ) ) ;
#26692=CARTESIAN_POINT ( 'NONE',  ( 0.8759842519685039353, 0.1574803149606299191, 1.594488188976378007 ) ) ;
#26693=CARTESIAN_POINT ( 'NONE',  ( 1.033464566929133799, 1.928577636452524610E-17, 4.498031496062992574 ) ) ;
#26694=( BOUNDED_CURVE ( )  B_SPLINE_CURVE ( 2, ( #8345, #15568, #22971, #30207, #1621, #45460, #44751, #4988, #19608, #12685, #11969, #45223, #34021, #27310, #9064, #1863, #41860, #23682, #27067, #38293, #30663, #19366, #44985, #26822, #41615, #8822, #23457, #30383, #4685, #44462, #37281, #12391, #11676, #27012, #12144, #23628, #41556, #8053, #23400, #19784, #38239, #5165, #16216, #20019, #34660, #27492, #17363, #12858, #32000, #31777, #21188, #24110, #13772, #42520, #28413, #24561, #13322, #35365, #6577, #35822, #9490, #31075, #39164, #35132, #6097, #2970, #16904, #28176, #2043, #13542, #42737, #42292, #6336, #17134, #45640, #42042, #31544, #38935, #16677, #9245, #46358, #38474, #5645, #9723, #31306, #45884, #552, #15448, #44634, #34140, #19009, #8232, #8707, #1034, #22623, #19728, #4621, #22857, #30328, #23096, #26712, #16158, #8467, #1271, #44400, #5104, #37715, #30551, #45114, #30790, #12332, #27195, #41748, #8953, #13722, #24055, #35314, #41981, #20672, #2452, #34846, #27904, #17079, #35547, #9436, #46069, #23804, #31719, #13273, #46308, #2690, #28127, #28359, #38658, #1991, #5831, #42927, #9187, #16620, #13496, #42686, #20438, #38420, #6284, #35073, #45826, #2222, #9671, #31249, #20907, #16842, #10138, #31482, #9901, #5590, #20197, #24513, #13037, #27673, #42467, #42233, #31017, #24287, #38882, #6045, #39110, #17317, #31955, #46539, #38179, #5341, #19962, #34602, #1753, #16396, #45583, #12805, #27439, #18495, #29579, #14210, #36259, #18264, #32189, #25477, #25220, #21865, #43893, #40283, #32910, #27, #7245, #14677, #33148, #272, #14916, #28612, #24747, #43174, #39342, #10379, #39581, #6759, #13731, #28369, #42938, #10148, #24757, #6534, #2924, #17560, #32198, #12816, #44133, #39820, #40056, #11099, #28622, #11331, #25943, #18732, #36957, #13972, #6772, #32449, #10629, #17671, #21751, #6406, #21018, #10751, #21263, #10017, #36383, #39468, #13842, #35886, #25102, #32068, #3541, #3041, #3288, #25358, #13601, #10262, #6171, #43302, #6644, #36133, #28977, #24867, #46425, #32320, #46898, #24633, #14089, #18152, #32792, #39231, #28732, #21498, #32559, #35434, #35666, #2569, #2803, #28241, #6878, #17909, #43779, #10504, #39694, #47148, #42803, #14332, #17435, #43533, #39939, #47387, #7129, #14561, #28487, #46659, #43056, #17205, #29232, #10981, #31843, #25598, #20790, #29695, #18611, #44939, #18386, #22442, #7371, #33501, #29464, #26539, #7826, #21982, #33270, #36837, #12151, #40169, #11441, #37063, #4215, #36604, #44699, #3762, #11917, #40864, #30391, #393, #30159, #18844, #8293, #33746, #614, #44468, #33027, #29923, #41099, #153, #855, #15045, #15272, #15757, #26058, #37289, #44008, #22685, #4441, #3989, #19073, #11683, #15514, #37534, #40628, #26308, #11212, #19324, #8060, #22921, #25826, #4693, #44236, #33973, #40402, #1099, #7589, #22204, #13106, #38724, #42051, #19792, #5892, #31553, #34426, #24119, #38484, #19560, #34669, #23409, #23873, #45891, #42304, #34911, #5654, #1816, #2054, #12636, #12868, #5174, #15991, #9013, #30614, #27737, #16687, #38246, #46131, #4935, #23635, #41334, #20028, #1335, #9498, #41812, #8534, #26774, #31316, #20504, #1572, #45419, #20264, #23165, #5407, #35141, #37782, #2284, #27501, #16913, #16224, #34206, #16453, #45178, #12399, #31086, #45650, #27020, #41569, #30856, #9253, #8774, #38013, #27260, #17853, #32010, #20733, #46369, #9729, #36065, #6818, #28187, #32496, #42992, #28911, #42746, #46602, #2516, #39878, #10201, #43475, #6108, #24806, #9962, #43240, #32734, #24574, #39173, #6346, #10443, #25040, #17142, #47078, #14272, #3222, #13780, #31786, #42527, #20960, #13331, #10682, #35606, #39637, #25289, #35373, #17373, #27960, #2980, #13550, #39404, #2747, #18088, #24346, #7063, #28427, #21690, #36322, #6586, #38943, #17613, #21201, #35834, #21438, #32258, #46837, #14026, #28672, #3476, #40576, #3709, #15459, #37239, #37010, #14500, #11856, #32968, #33444, #44641, #8241, #15217, #19018, #40807, #4631, #40343, #11153, #19265, #47329, #18557, #93, #14987, #14739, #29411, #7533, #36778, #33214, #338, #22631, #19736, #41275, #8716, #34149, #5597, #27207, #1277, #31028, #20205, #16627, #45836, #13045, #9448, #38671, #29457, #11205, #11433, #14551, #40858, #22680, #40394, #15507, #387, #11908, #22196, #33263, #29688, #22914, #4208, #18141, #10971, #47379, #18838, #33493, #609, #43768, #29913, #44461, #16676, #34659, #37771, #31305, #27729, #42291, #19783, #41324, #1091, #45168, #4684, #9489, #12390, #38004, #24109, #34198, #1325, #44929, #27011, #41555, #1561, #27250, #12143, #26767, #41804, #23627, #38238, #5396, #9722, #5886, #42983, #17133, #17362, #25033, #42519, #39628, #3214, #6576, #31776, #17843, #43466, #46357, #36056, #2734, #10191, #28412, #43228, #2277, #38934, #28661, #35821, #16903, #38716, #14015, #13771, #14263, #24560, #2969, #24336, #21187, #17602, #35364, #32246, #24799, #46827, #32489, #9951, #46592, #6096, #10433, #39392, #6809, #47071, #31999, #2509, #21429, #10672, #13541, #28175, #28905, #20721, #42736, #20493, #6335, #39163, #35131, #20952, #35597, #31543, #46123, #13321, #27952, #22142, #22377, #29860, #32726, #29402, #25279, #14978, #25763, #7759, #551, #43947, #18078, #40333, #11144, #29153, #7521, #7997, #4379, #43708, #36768, #40568, #4156, #7056, #10914, #21682, #25537, #47318, #25986, #37000, #15447, #3928, #18548, #18782, #14493, #33205, #21919, #33436, #44399, #40802, #15208, #11615, #82, #7299, #40105, #36312, #36540, #26236, #3467, #22622, #328, #14730, #3699, #30101, #18323, #44172, #39867, #11374, #32960, #37234, #19008, #33673, #785, #44633, #31248, #11847, #30550, #26946, #23343, #8231, #16395, #41037, #31016, #12568, #1990, #4866, #1752, #37955, #27438, #5340, #41502, #16157, #16619, #37714, #45356, #30327, #45582, #19494, #23572, #4620, #19727, #8466, #8952, #12804, #41980, #19961, #38178, #34364, #34601, #45113, #27194, #34139, #9186, #22856, #23803, #15922, #1270, #12331, #26474, #37473, #8706, #19254, #5103, #33912, #38419, #1503, #1033, #15690, #5589, #20196, #30789, #41747, #34845, #44874, #12087, #26711, #41267, #23095, #46537, #36004, #38880, #35772, #9899, #13959, #39340, #13494, #2688, #28610, #3162, #24285, #31953, #16840, #20670, #20905, #21379, #31717, #42925, #2220, #28357, #10136, #42465, #24745, #35545, #6520, #43172, #17077 ),
 .UNSPECIFIED., .F., .T. ) 
 B_SPLINE_CURVE_WITH_KNOTS ( ( 3, 2, 2, 2, 2, 2, 2, 2, 2, 2, 2, 2, 2, 2, 2, 2, 2, 2, 2, 2, 2, 2, 2, 2, 2, 2, 2, 2, 2, 2, 2, 2, 2, 2, 2, 2, 2, 2, 2, 2, 2, 2, 2, 2, 2, 2, 2, 2, 2, 2, 2, 2, 2, 2, 2, 2, 2, 2, 2, 2, 2, 2, 2, 2, 2, 2, 2, 2, 2, 2, 2, 2, 2, 2, 2, 2, 2, 2, 2, 2, 2, 2, 2, 2, 2, 2, 2, 2, 2, 2, 2, 2, 2, 2, 2, 2, 2, 2, 2, 2, 2, 2, 2, 2, 2, 2, 2, 2, 2, 2, 2, 2, 2, 2, 2, 2, 2, 2, 2, 2, 2, 2, 2, 2, 2, 2, 2, 2, 2, 2, 2, 2, 2, 2, 2, 2, 2, 2, 2, 2, 2, 2, 2, 2, 2, 2, 2, 2, 2, 2, 2, 2, 2, 2, 2, 2, 2, 2, 2, 2, 2, 2, 2, 2, 2, 2, 2, 2, 2, 2, 2, 2, 2, 2, 2, 2, 2, 2, 2, 2, 2, 2, 2, 2, 2, 2, 2, 2, 2, 2, 2, 2, 2, 2, 2, 2, 2, 2, 2, 2, 2, 2, 2, 2, 2, 2, 2, 2, 2, 2, 2, 2, 2, 2, 2, 2, 2, 2, 2, 2, 2, 2, 2, 2, 2, 2, 2, 2, 2, 2, 2, 2, 2, 2, 2, 2, 2, 2, 2, 2, 2, 2, 2, 2, 2, 2, 2, 2, 2, 2, 2, 2, 2, 2, 2, 2, 2, 2, 2, 2, 2, 2, 2, 2, 2, 2, 2, 2, 2, 2, 2, 2, 2, 2, 2, 2, 2, 2, 2, 2, 2, 2, 2, 2, 2, 2, 2, 2, 2, 2, 2, 2, 2, 2, 2, 2, 2, 2, 2, 2, 2, 2, 2, 2, 2, 2, 2, 2, 2, 2, 2, 2, 2, 2, 2, 2, 2, 2, 2, 2, 2, 2, 2, 2, 2, 2, 2, 2, 2, 2, 2, 2, 2, 2, 2, 2, 2, 2, 2, 2, 2, 2, 2, 2, 2, 2, 2, 2, 2, 2, 2, 2, 2, 2, 2, 2, 2, 2, 2, 2, 2, 2, 2, 2, 2, 2, 2, 2, 2, 2, 2, 2, 2, 2, 2, 2, 2, 2, 2, 2, 2, 2, 2, 2, 2, 2, 2, 2, 2, 2, 2, 2, 2, 2, 2, 2, 2, 3 ),
 ( 0.008749999973727599911, 0.01000000000000000021, 0.01250000000000000069, 0.01499999999999999944, 0.01750000000000000167, 0.02000000000000000042, 0.02249999999999999917, 0.02500000000000000139, 0.02750000000000000014, 0.02999999999999999889, 0.03250000000000000111, 0.03500000000000000333, 0.03749999999999999861, 0.04000000000000000083, 0.04250000000000000305, 0.04499999999999999833, 0.04750000000000000056, 0.05000000000000000278, 0.05249999999999999806, 0.05500000000000000028, 0.05750000000000000250, 0.05999999999999999778, 0.06250000000000000000, 0.06500000000000000222, 0.06750000000000000444, 0.07000000000000000666, 0.07250000000000000888, 0.07500000000000001110, 0.07750000000000001332, 0.08000000000000001554, 0.08250000000000001776, 0.08500000000000001998, 0.08749999999999999445, 0.08999999999999999667, 0.09249999999999999889, 0.09500000000000000111, 0.09750000000000000333, 0.1000000000000000056, 0.1025000000000000078, 0.1050000000000000100, 0.1075000000000000122, 0.1100000000000000144, 0.1125000000000000167, 0.1150000000000000189, 0.1174999999999999933, 0.1199999999999999956, 0.1224999999999999978, 0.1250000000000000000, 0.1275000000000000022, 0.1300000000000000044, 0.1325000000000000067, 0.1350000000000000089, 0.1375000000000000111, 0.1399999999999999856, 0.1424999999999999878, 0.1449999999999999900, 0.1474999999999999922, 0.1499999999999999944, 0.1524999999999999967, 0.1549999999999999989, 0.1575000000000000011, 0.1600000000000000033, 0.1625000000000000056, 0.1650000000000000078, 0.1675000000000000100, 0.1700000000000000122, 0.1724999999999999867, 0.1749999999999999889, 0.1774999999999999911, 0.1799999999999999933, 0.1824999999999999956, 0.1849999999999999978, 0.1875000000000000000, 0.1900000000000000022, 0.1925000000000000044, 0.1950000000000000067, 0.1975000000000000089, 0.2000000000000000111, 0.2025000000000000133, 0.2049999999999999878, 0.2074999999999999900, 0.2099999999999999922, 0.2124999999999999944, 0.2149999999999999967, 0.2174999999999999989, 0.2200000000000000011, 0.2225000000000000033, 0.2250000000000000056, 0.2275000000000000078, 0.2300000000000000100, 0.2325000000000000122, 0.2349999999999999867, 0.2374999999999999889, 0.2399999999999999911, 0.2424999999999999933, 0.2449999999999999956, 0.2474999999999999978, 0.2500000000000000000, 0.2525000000000000022, 0.2550000000000000044, 0.2575000000000000067, 0.2600000000000000089, 0.2625000000000000111, 0.2650000000000000133, 0.2675000000000000155, 0.2700000000000000178, 0.2725000000000000200, 0.2750000000000000222, 0.2775000000000000244, 0.2800000000000000266, 0.2824999999999999734, 0.2849999999999999756, 0.2874999999999999778, 0.2899999999999999800, 0.2924999999999999822, 0.2949999999999999845, 0.2974999999999999867, 0.2999999999999999889, 0.3024999999999999911, 0.3049999999999999933, 0.3074999999999999956, 0.3099999999999999978, 0.3125000000000000000, 0.3150000000000000022, 0.3175000000000000044, 0.3200000000000000067, 0.3225000000000000089, 0.3250000000000000111, 0.3275000000000000133, 0.3300000000000000155, 0.3325000000000000178, 0.3350000000000000200, 0.3375000000000000222, 0.3400000000000000244, 0.3425000000000000266, 0.3449999999999999734, 0.3474999999999999756, 0.3499999999999999778, 0.3524999999999999800, 0.3549999999999999822, 0.3574999999999999845, 0.3599999999999999867, 0.3624999999999999889, 0.3649999999999999911, 0.3674999999999999933, 0.3699999999999999956, 0.3724999999999999978, 0.3750000000000000000, 0.3775000000000000022, 0.3800000000000000044, 0.3825000000000000067, 0.3850000000000000089, 0.3875000000000000111, 0.3900000000000000133, 0.3925000000000000155, 0.3950000000000000178, 0.3975000000000000200, 0.4000000000000000222, 0.4025000000000000244, 0.4050000000000000266, 0.4074999999999999734, 0.4099999999999999756, 0.4124999999999999778, 0.4149999999999999800, 0.4174999999999999822, 0.4199999999999999845, 0.4224999999999999867, 0.4249999999999999889, 0.4274999999999999911, 0.4299999999999999933, 0.4324999999999999956, 0.4349999999999999978, 0.4375000000000000000, 0.4400000000000000022, 0.4425000000000000044, 0.4450000000000000067, 0.4475000000000000089, 0.4500000000000000111, 0.4525000000000000133, 0.4550000000000000155, 0.4575000000000000178, 0.4600000000000000200, 0.4625000000000000222, 0.4650000000000000244, 0.4675000000000000266, 0.4699999999999999734, 0.4724999999999999756, 0.4749999999999999778, 0.4774999999999999800, 0.4799999999999999822, 0.4824999999999999845, 0.4849999999999999867, 0.4874999999999999889, 0.4899999999999999911, 0.4924999999999999933, 0.4949999999999999956, 0.4974999999999999978, 0.5000000000000000000, 0.5024999999999999467, 0.5050000000000000044, 0.5074999999999999512, 0.5100000000000000089, 0.5124999999999999556, 0.5150000000000000133, 0.5174999999999999600, 0.5200000000000000178, 0.5224999999999999645, 0.5250000000000000222, 0.5274999999999999689, 0.5300000000000000266, 0.5324999999999999734, 0.5350000000000000311, 0.5374999999999999778, 0.5400000000000000355, 0.5424999999999999822, 0.5450000000000000400, 0.5474999999999999867, 0.5500000000000000444, 0.5524999999999999911, 0.5550000000000000488, 0.5574999999999999956, 0.5600000000000000533, 0.5625000000000000000, 0.5649999999999999467, 0.5675000000000000044, 0.5699999999999999512, 0.5725000000000000089, 0.5749999999999999556, 0.5775000000000000133, 0.5799999999999999600, 0.5825000000000000178, 0.5849999999999999645, 0.5875000000000000222, 0.5899999999999999689, 0.5925000000000000266, 0.5949999999999999734, 0.5975000000000000311, 0.5999999999999999778, 0.6025000000000000355, 0.6049999999999999822, 0.6075000000000000400, 0.6099999999999999867, 0.6125000000000000444, 0.6149999999999999911, 0.6175000000000000488, 0.6199999999999999956, 0.6225000000000000533, 0.6250000000000000000, 0.6274999999999999467, 0.6300000000000000044, 0.6324999999999999512, 0.6350000000000000089, 0.6374999999999999556, 0.6400000000000000133, 0.6424999999999999600, 0.6450000000000000178, 0.6474999999999999645, 0.6500000000000000222, 0.6524999999999999689, 0.6550000000000000266, 0.6574999999999999734, 0.6600000000000000311, 0.6624999999999999778, 0.6650000000000000355, 0.6674999999999999822, 0.6700000000000000400, 0.6724999999999999867, 0.6750000000000000444, 0.6774999999999999911, 0.6800000000000000488, 0.6824999999999999956, 0.6850000000000000533, 0.6875000000000000000, 0.6899999999999999467, 0.6925000000000000044, 0.6949999999999999512, 0.6975000000000000089, 0.6999999999999999556, 0.7025000000000000133, 0.7049999999999999600, 0.7075000000000000178, 0.7099999999999999645, 0.7125000000000000222, 0.7149999999999999689, 0.7175000000000000266, 0.7199999999999999734, 0.7225000000000000311, 0.7249999999999999778, 0.7275000000000000355, 0.7299999999999999822, 0.7325000000000000400, 0.7349999999999999867, 0.7375000000000000444, 0.7399999999999999911, 0.7425000000000000488, 0.7449999999999999956, 0.7474999999999999423, 0.7500000000000000000, 0.7524999999999999467, 0.7550000000000000044, 0.7574999999999999512, 0.7600000000000000089, 0.7624999999999999556, 0.7649999999999999023, 0.7674999999999999600, 0.7700000000000000178, 0.7724999999999999645, 0.7750000000000000222, 0.7774999999999999689, 0.7800000000000000266, 0.7824999999999998623, 0.7850000000000000311, 0.7874999999999999778, 0.7900000000000000355, 0.7924999999999999822, 0.7950000000000000400, 0.7974999999999999867, 0.8000000000000000444, 0.8024999999999999911, 0.8050000000000000488, 0.8074999999999999956, 0.8100000000000000533, 0.8125000000000000000, 0.8149999999999999467, 0.8175000000000000044, 0.8199999999999999512, 0.8225000000000000089, 0.8249999999999999556, 0.8275000000000000133, 0.8299999999999999600, 0.8325000000000000178, 0.8349999999999999645, 0.8375000000000000222, 0.8399999999999999689, 0.8425000000000000266, 0.8449999999999999734, 0.8475000000000000311, 0.8499999999999999778, 0.8525000000000000355, 0.8549999999999999822, 0.8575000000000000400, 0.8599999999999999867, 0.8625000000000000444, 0.8649999999999999911, 0.8675000000000000488, 0.8699999999999999956, 0.8725000000000000533, 0.8750000000000000000, 0.8774999999999999467, 0.8800000000000000044, 0.8824999999999999512, 0.8850000000000000089, 0.8874999999999999556, 0.8900000000000000133, 0.8924999999999999600, 0.8950000000000000178, 0.8974999999999999645, 0.9000000000000000222, 0.9024999999999999689, 0.9050000000000000266, 0.9074999999999999734, 0.9100000000000000311, 0.9124999999999999778, 0.9150000000000000355, 0.9174999999999999822, 0.9200000000000000400, 0.9224999999999999867, 0.9250000000000000444, 0.9274999999999999911, 0.9300000000000000488, 0.9324999999999999956, 0.9350000000000000533, 0.9375000000000000000, 0.9399999999999999467, 0.9425000000000000044, 0.9449999999999999512, 0.9475000000000000089, 0.9499999999999999556, 0.9525000000000000133, 0.9549999999999999600, 0.9575000000000000178, 0.9599999999999999645, 0.9625000000000000222, 0.9649999999999999689, 0.9675000000000000266, 0.9699999999999999734, 0.9725000000000000311, 0.9749999999999999778, 0.9775000000000000355, 0.9799999999999999822, 0.9825000000000000400, 0.9849999999999999867, 0.9875000000000000444, 0.9899999999999999911, 0.9925000000000000488, 0.9949999999999999956, 0.9975000000000000533, 1.000000000000000000 ),
 .UNSPECIFIED. ) 
 CURVE ( )  GEOMETRIC_REPRESENTATION_ITEM ( )  RATIONAL_B_SPLINE_CURVE ( ( 0.9619397662556429252, 0.9619397654556960386, 1.000000000000000000, 0.9238795325112869605, 1.000000000000000000, 0.9238795325112869605, 1.000000000000000000, 0.9238795325112869605, 1.000000000000000000, 0.9238795325112869605, 1.000000000000000000, 0.9238795325112869605, 1.000000000000000000, 0.9238795325112869605, 1.000000000000000000, 0.9238795325112869605, 1.000000000000000000, 0.9238795325112869605, 1.000000000000000000, 0.9238795325112869605, 1.000000000000000000, 0.9238795325112869605, 1.000000000000000000, 0.9238795325112869605, 1.000000000000000000, 0.9238795325112869605, 1.000000000000000000, 0.9238795325112869605, 1.000000000000000000, 0.9238795325112869605, 1.000000000000000000, 0.9238795325112869605, 1.000000000000000000, 0.9238795325112869605, 1.000000000000000000, 0.9238795325112869605, 1.000000000000000000, 0.9238795325112869605, 1.000000000000000000, 0.9238795325112869605, 1.000000000000000000, 0.9238795325112869605, 1.000000000000000000, 0.9238795325112869605, 1.000000000000000000, 0.9238795325112869605, 1.000000000000000000, 0.9238795325112869605, 1.000000000000000000, 0.9238795325112869605, 1.000000000000000000, 0.9238795325112869605, 1.000000000000000000, 0.9238795325112869605, 1.000000000000000000, 0.9238795325112869605, 1.000000000000000000, 0.9238795325112869605, 1.000000000000000000, 0.9238795325112869605, 1.000000000000000000, 0.9238795325112869605, 1.000000000000000000, 0.9238795325112869605, 1.000000000000000000, 0.9238795325112869605, 1.000000000000000000, 0.9238795325112869605, 1.000000000000000000, 0.9238795325112869605, 1.000000000000000000, 0.9238795325112869605, 1.000000000000000000, 0.9238795325112869605, 1.000000000000000000, 0.9238795325112869605, 1.000000000000000000, 0.9238795325112869605, 1.000000000000000000, 0.9238795325112869605, 1.000000000000000000, 0.9238795325112869605, 1.000000000000000000, 0.9238795325112869605, 1.000000000000000000, 0.9238795325112869605, 1.000000000000000000, 0.9238795325112869605, 1.000000000000000000, 0.9238795325112869605, 1.000000000000000000, 0.9238795325112869605, 1.000000000000000000, 0.9238795325112869605, 1.000000000000000000, 0.9238795325112869605, 1.000000000000000000, 0.9238795325112869605, 1.000000000000000000, 0.9238795325112869605, 1.000000000000000000, 0.9238795325112869605, 1.000000000000000000, 0.9238795325112869605, 1.000000000000000000, 0.9238795325112869605, 1.000000000000000000, 0.9238795325112869605, 1.000000000000000000, 0.9238795325112869605, 1.000000000000000000, 0.9238795325112869605, 1.000000000000000000, 0.9238795325112869605, 1.000000000000000000, 0.9238795325112869605, 1.000000000000000000, 0.9238795325112869605, 1.000000000000000000, 0.9238795325112869605, 1.000000000000000000, 0.9238795325112869605, 1.000000000000000000, 0.9238795325112869605, 1.000000000000000000, 0.9238795325112869605, 1.000000000000000000, 0.9238795325112869605, 1.000000000000000000, 0.9238795325112869605, 1.000000000000000000, 0.9238795325112869605, 1.000000000000000000, 0.9238795325112869605, 1.000000000000000000, 0.9238795325112869605, 1.000000000000000000, 0.9238795325112869605, 1.000000000000000000, 0.9238795325112869605, 1.000000000000000000, 0.9238795325112869605, 1.000000000000000000, 0.9238795325112869605, 1.000000000000000000, 0.9238795325112869605, 1.000000000000000000, 0.9238795325112869605, 1.000000000000000000, 0.9238795325112869605, 1.000000000000000000, 0.9238795325112869605, 1.000000000000000000, 0.9238795325112869605, 1.000000000000000000, 0.9238795325112869605, 1.000000000000000000, 0.9238795325112869605, 1.000000000000000000, 0.9238795325112869605, 1.000000000000000000, 0.9238795325112869605, 1.000000000000000000, 0.9238795325112869605, 1.000000000000000000, 0.9238795325112869605, 1.000000000000000000, 0.9238795325112869605, 1.000000000000000000, 0.9238795325112869605, 1.000000000000000000, 0.9238795325112869605, 1.000000000000000000, 0.9238795325112869605, 1.000000000000000000, 0.9238795325112869605, 1.000000000000000000, 0.9238795325112869605, 1.000000000000000000, 0.9238795325112869605, 1.000000000000000000, 0.9238795325112869605, 1.000000000000000000, 0.9238795325112869605, 1.000000000000000000, 0.9238795325112869605, 1.000000000000000000, 0.9238795325112869605, 1.000000000000000000, 0.9238795325112869605, 1.000000000000000000, 0.9238795325112869605, 1.000000000000000000, 0.9238795325112869605, 1.000000000000000000, 0.9238795325112869605, 1.000000000000000000, 0.9238795325112869605, 1.000000000000000000, 0.9238795325112869605, 1.000000000000000000, 0.9238795325112869605, 1.000000000000000000, 0.9238795325112869605, 1.000000000000000000, 0.9238795325112869605, 1.000000000000000000, 0.9238795325112869605, 1.000000000000000000, 0.9238795325112869605, 1.000000000000000000, 0.9238795325112869605, 1.000000000000000000, 0.9238795325112869605, 1.000000000000000000, 0.9238795325112869605, 1.000000000000000000, 0.9238795325112869605, 1.000000000000000000, 0.9238795325112869605, 1.000000000000000000, 0.9238795325112869605, 1.000000000000000000, 0.9238795325112869605, 1.000000000000000000, 0.9238795325112869605, 1.000000000000000000, 0.9238795325112869605, 1.000000000000000000, 0.9238795325112869605, 1.000000000000000000, 0.9238795325112869605, 1.000000000000000000, 0.9238795325112869605, 1.000000000000000000, 0.9238795325112869605, 1.000000000000000000, 0.9238795325112869605, 1.000000000000000000, 0.9238795325112869605, 1.000000000000000000, 0.9238795325112869605, 1.000000000000000000, 0.9238795325112869605, 1.000000000000000000, 0.9238795325112869605, 1.000000000000000000, 0.9238795325112869605, 1.000000000000000000, 0.9238795325112869605, 1.000000000000000000, 0.9238795325112869605, 1.000000000000000000, 0.9238795325112869605, 1.000000000000000000, 0.9238795325112869605, 1.000000000000000000, 0.9238795325112869605, 1.000000000000000000, 0.9238795325112869605, 1.000000000000000000, 0.9238795325112869605, 1.000000000000000000, 0.9238795325112869605, 1.000000000000000000, 0.9238795325112869605, 1.000000000000000000, 0.9238795325112869605, 1.000000000000000000, 0.9238795325112869605, 1.000000000000000000, 0.9238795325112869605, 1.000000000000000000, 0.9238795325112869605, 1.000000000000000000, 0.9238795325112869605, 1.000000000000000000, 0.9238795325112869605, 1.000000000000000000, 0.9238795325112869605, 1.000000000000000000, 0.9238795325112869605, 1.000000000000000000, 0.9238795325112869605, 1.000000000000000000, 0.9238795325112869605, 1.000000000000000000, 0.9238795325112869605, 1.000000000000000000, 0.9238795325112869605, 1.000000000000000000, 0.9238795325112869605, 1.000000000000000000, 0.9238795325112869605, 1.000000000000000000, 0.9238795325112869605, 1.000000000000000000, 0.9238795325112869605, 1.000000000000000000, 0.9238795325112869605, 1.000000000000000000, 0.9238795325112869605, 1.000000000000000000, 0.9238795325112869605, 1.000000000000000000, 0.9238795325112869605, 1.000000000000000000, 0.9238795325112869605, 1.000000000000000000, 0.9238795325112869605, 1.000000000000000000, 0.9238795325112869605, 1.000000000000000000, 0.9238795325112869605, 1.000000000000000000, 0.9238795325112869605, 1.000000000000000000, 0.9238795325112869605, 1.000000000000000000, 0.9238795325112869605, 1.000000000000000000, 0.9238795325112869605, 1.000000000000000000, 0.9238795325112869605, 1.000000000000000000, 0.9238795325112869605, 1.000000000000000000, 0.9238795325112869605, 1.000000000000000000, 0.9238795325112869605, 1.000000000000000000, 0.9238795325112869605, 1.000000000000000000, 0.9238795325112869605, 1.000000000000000000, 0.9238795325112869605, 1.000000000000000000, 0.9238795325112869605, 1.000000000000000000, 0.9238795325112869605, 1.000000000000000000, 0.9238795325112869605, 1.000000000000000000, 0.9238795325112869605, 1.000000000000000000, 0.9238795325112869605, 1.000000000000000000, 0.9238795325112869605, 1.000000000000000000, 0.9238795325112869605, 1.000000000000000000, 0.9238795325112869605, 1.000000000000000000, 0.9238795325112869605, 1.000000000000000000, 0.9238795325112869605, 1.000000000000000000, 0.9238795325112869605, 1.000000000000000000, 0.9238795325112869605, 1.000000000000000000, 0.9238795325112869605, 1.000000000000000000, 0.9238795325112869605, 1.000000000000000000, 0.9238795325112869605, 1.000000000000000000, 0.9238795325112869605, 1.000000000000000000, 0.9238795325112869605, 1.000000000000000000, 0.9238795325112869605, 1.000000000000000000, 0.9238795325112869605, 1.000000000000000000, 0.9238795325112869605, 1.000000000000000000, 0.9238795325112869605, 1.000000000000000000, 0.9238795325112869605, 1.000000000000000000, 0.9238795325112869605, 1.000000000000000000, 0.9238795325112869605, 1.000000000000000000, 0.9238795325112869605, 1.000000000000000000, 0.9238795325112869605, 1.000000000000000000, 0.9238795325112869605, 1.000000000000000000, 0.9238795325112869605, 1.000000000000000000, 0.9238795325112869605, 1.000000000000000000, 0.9238795325112869605, 1.000000000000000000, 0.9238795325112869605, 1.000000000000000000, 0.9238795325112869605, 1.000000000000000000, 0.9238795325112869605, 1.000000000000000000, 0.9238795325112869605, 1.000000000000000000, 0.9238795325112869605, 1.000000000000000000, 0.9238795325112869605, 1.000000000000000000, 0.9238795325112869605, 1.000000000000000000, 0.9238795325112869605, 1.000000000000000000, 0.9238795325112869605, 1.000000000000000000, 0.9238795325112869605, 1.000000000000000000, 0.9238795325112869605, 1.000000000000000000, 0.9238795325112869605, 1.000000000000000000, 0.9238795325112869605, 1.000000000000000000, 0.9238795325112869605, 1.000000000000000000, 0.9238795325112869605, 1.000000000000000000, 0.9238795325112869605, 1.000000000000000000, 0.9238795325112869605, 1.000000000000000000, 0.9238795325112869605, 1.000000000000000000, 0.9238795325112869605, 1.000000000000000000, 0.9238795325112869605, 1.000000000000000000, 0.9238795325112869605, 1.000000000000000000, 0.9238795325112869605, 1.000000000000000000, 0.9238795325112869605, 1.000000000000000000, 0.9238795325112869605, 1.000000000000000000, 0.9238795325112869605, 1.000000000000000000, 0.9238795325112869605, 1.000000000000000000, 0.9238795325112869605, 1.000000000000000000, 0.9238795325112869605, 1.000000000000000000, 0.9238795325112869605, 1.000000000000000000, 0.9238795325112869605, 1.000000000000000000, 0.9238795325112869605, 1.000000000000000000, 0.9238795325112869605, 1.000000000000000000, 0.9238795325112869605, 1.000000000000000000, 0.9238795325112869605, 1.000000000000000000, 0.9238795325112869605, 1.000000000000000000, 0.9238795325112869605, 1.000000000000000000, 0.9238795325112869605, 1.000000000000000000, 0.9238795325112869605, 1.000000000000000000, 0.9238795325112869605, 1.000000000000000000, 0.9238795325112869605, 1.000000000000000000, 0.9238795325112869605, 1.000000000000000000, 0.9238795325112869605, 1.000000000000000000, 0.9238795325112869605, 1.000000000000000000, 0.9238795325112869605, 1.000000000000000000, 0.9238795325112869605, 1.000000000000000000, 0.9238795325112869605, 1.000000000000000000, 0.9238795325112869605, 1.000000000000000000, 0.9238795325112869605, 1.000000000000000000, 0.9238795325112869605, 1.000000000000000000, 0.9238795325112869605, 1.000000000000000000, 0.9238795325112869605, 1.000000000000000000, 0.9238795325112869605, 1.000000000000000000, 0.9238795325112869605, 1.000000000000000000, 0.9238795325112869605, 1.000000000000000000, 0.9238795325112869605, 1.000000000000000000, 0.9238795325112869605, 1.000000000000000000, 0.9238795325112869605, 1.000000000000000000, 0.9238795325112869605, 1.000000000000000000, 0.9238795325112869605, 1.000000000000000000, 0.9238795325112869605, 1.000000000000000000, 0.9238795325112869605, 1.000000000000000000, 0.9238795325112869605, 1.000000000000000000, 0.9238795325112869605, 1.000000000000000000, 0.9238795325112869605, 1.000000000000000000, 0.9238795325112869605, 1.000000000000000000, 0.9238795325112869605, 1.000000000000000000, 0.9238795325112869605, 1.000000000000000000, 0.9238795325112869605, 1.000000000000000000, 0.9238795325112869605, 1.000000000000000000, 0.9238795325112869605, 1.000000000000000000, 0.9238795325112869605, 1.000000000000000000, 0.9238795325112869605, 1.000000000000000000, 0.9238795325112869605, 1.000000000000000000, 0.9238795325112869605, 1.000000000000000000, 0.9238795325112869605, 1.000000000000000000, 0.9238795325112869605, 1.000000000000000000, 0.9238795325112869605, 1.000000000000000000, 0.9238795325112869605, 1.000000000000000000, 0.9238795325112869605, 1.000000000000000000, 0.9238795325112869605, 1.000000000000000000, 0.9238795325112869605, 1.000000000000000000, 0.9238795325112869605, 1.000000000000000000, 0.9238795325112869605, 1.000000000000000000, 0.9238795325112869605, 1.000000000000000000, 0.9238795325112869605, 1.000000000000000000, 0.9238795325112869605, 1.000000000000000000, 0.9238795325112869605, 1.000000000000000000, 0.9238795325112869605, 1.000000000000000000, 0.9238795325112869605, 1.000000000000000000, 0.9238795325112869605, 1.000000000000000000, 0.9238795325112869605, 1.000000000000000000, 0.9238795325112869605, 1.000000000000000000, 0.9238795325112869605, 1.000000000000000000, 0.9238795325112869605, 1.000000000000000000, 0.9238795325112869605, 1.000000000000000000, 0.9238795325112869605, 1.000000000000000000, 0.9238795325112869605, 1.000000000000000000, 0.9238795325112869605, 1.000000000000000000, 0.9238795325112869605, 1.000000000000000000, 0.9238795325112869605, 1.000000000000000000, 0.9238795325112869605, 1.000000000000000000, 0.9238795325112869605, 1.000000000000000000, 0.9238795325112869605, 1.000000000000000000, 0.9238795325112869605, 1.000000000000000000, 0.9238795325112869605, 1.000000000000000000, 0.9238795325112869605, 1.000000000000000000, 0.9238795325112869605, 1.000000000000000000, 0.9238795325112869605, 1.000000000000000000, 0.9238795325112869605, 1.000000000000000000, 0.9238795325112869605, 1.000000000000000000, 0.9238795325112869605, 1.000000000000000000, 0.9238795325112869605, 1.000000000000000000, 0.9238795325112869605, 1.000000000000000000, 0.9238795325112869605, 1.000000000000000000, 0.9238795325112869605, 1.000000000000000000, 0.9238795325112869605, 1.000000000000000000, 0.9238795325112869605, 1.000000000000000000, 0.9238795325112869605, 1.000000000000000000, 0.9238795325112869605, 1.000000000000000000, 0.9238795325112869605, 1.000000000000000000, 0.9238795325112869605, 1.000000000000000000, 0.9238795325112869605, 1.000000000000000000, 0.9238795325112869605, 1.000000000000000000, 0.9238795325112869605, 1.000000000000000000, 0.9238795325112869605, 1.000000000000000000, 0.9238795325112869605, 1.000000000000000000, 0.9238795325112869605, 1.000000000000000000, 0.9238795325112869605, 1.000000000000000000, 0.9238795325112869605, 1.000000000000000000, 0.9238795325112869605, 1.000000000000000000, 0.9238795325112869605, 1.000000000000000000, 0.9238795325112869605, 1.000000000000000000, 0.9238795325112869605, 1.000000000000000000, 0.9238795325112869605, 1.000000000000000000, 0.9238795325112869605, 1.000000000000000000, 0.9238795325112869605, 1.000000000000000000, 0.9238795325112869605, 1.000000000000000000, 0.9238795325112869605, 1.000000000000000000, 0.9238795325112869605, 1.000000000000000000, 0.9238795325112869605, 1.000000000000000000, 0.9238795325112869605, 1.000000000000000000, 0.9238795325112869605, 1.000000000000000000, 0.9238795325112869605, 1.000000000000000000, 0.9238795325112869605, 1.000000000000000000, 0.9238795325112869605, 1.000000000000000000, 0.9238795325112869605, 1.000000000000000000, 0.9238795325112869605, 1.000000000000000000, 0.9238795325112869605, 1.000000000000000000, 0.9238795325112869605, 1.000000000000000000, 0.9238795325112869605, 1.000000000000000000, 0.9238795325112869605, 1.000000000000000000, 0.9238795325112869605, 1.000000000000000000, 0.9238795325112869605, 1.000000000000000000, 0.9238795325112869605, 1.000000000000000000, 0.9238795325112869605, 1.000000000000000000, 0.9238795325112869605, 1.000000000000000000, 0.9238795325112869605, 1.000000000000000000, 0.9238795325112869605, 1.000000000000000000, 0.9238795325112869605, 1.000000000000000000, 0.9238795325112869605, 1.000000000000000000, 0.9238795325112869605, 1.000000000000000000, 0.9238795325112869605, 1.000000000000000000, 0.9238795325112869605, 1.000000000000000000, 0.9238795325112869605, 1.000000000000000000, 0.9238795325112869605, 1.000000000000000000, 0.9238795325112869605, 1.000000000000000000, 0.9238795325112869605, 1.000000000000000000, 0.9238795325112869605, 1.000000000000000000, 0.9238795325112869605, 1.000000000000000000, 0.9238795325112869605, 1.000000000000000000, 0.9238795325112869605, 1.000000000000000000, 0.9238795325112869605, 1.000000000000000000, 0.9238795325112869605, 1.000000000000000000, 0.9238795325112869605, 1.000000000000000000, 0.9238795325112869605, 1.000000000000000000, 0.9238795325112869605, 1.000000000000000000, 0.9238795325112869605, 1.000000000000000000, 0.9238795325112869605, 1.000000000000000000, 0.9238795325112869605, 1.000000000000000000, 0.9238795325112869605, 1.000000000000000000, 0.9238795325112869605, 1.000000000000000000, 0.9238795325112869605, 1.000000000000000000, 0.9238795325112869605, 1.000000000000000000, 0.9238795325112869605, 1.000000000000000000, 0.9238795325112869605, 1.000000000000000000, 0.9238795325112869605, 1.000000000000000000, 0.9238795325112869605, 1.000000000000000000, 0.9238795325112869605, 1.000000000000000000, 0.9238795325112869605, 1.000000000000000000, 0.9238795325112869605, 1.000000000000000000, 0.9238795325112869605, 1.000000000000000000, 0.9238795325112869605, 1.000000000000000000, 0.9238795325112869605, 1.000000000000000000, 0.9238795325112869605, 1.000000000000000000, 0.9238795325112869605, 1.000000000000000000, 0.9238795325112869605, 1.000000000000000000, 0.9238795325112869605, 1.000000000000000000, 0.9238795325112869605, 1.000000000000000000, 0.9238795325112869605, 1.000000000000000000 ) ) 
 REPRESENTATION_ITEM ( '' )  ) ;
#26695=EDGE_CURVE ( 'NONE', #42967, #14779, #10558, .T. ) ;
#26696=CARTESIAN_POINT ( 'NONE',  ( 0.6971942568897626646, 0.07405724077823318263, 0.2362204723871814960 ) ) ;
#26703=CARTESIAN_POINT ( 'NONE',  ( -0.6971942568897648851, -0.07405724077823297447, 0.7185039369541108556 ) ) ;
#26710=CARTESIAN_POINT ( 'NONE',  ( 0.6971942568897637749, 2.189545951927499583E-17, 1.306594488135212728 ) ) ;
#26711=CARTESIAN_POINT ( 'NONE',  ( 1.002407869896990045, 0.1264236179284866091, 1.916830708607653477 ) ) ;
#26712=CARTESIAN_POINT ( 'NONE',  ( 0.7495606340400177148, -0.1264236179284866091, 0.2829724408911185041 ) ) ;
#26719=( BOUNDED_CURVE ( )  B_SPLINE_CURVE ( 2, ( #2703, #17330, #35787, #43184, #10394, #24998, #39594, #6775, #21391 ),
 .UNSPECIFIED., .F., .T. ) 
 B_SPLINE_CURVE_WITH_KNOTS ( ( 3, 2, 2, 2, 3 ),
 ( 0.07000000000000000666, 0.07249999999999999500, 0.07499999999999999722, 0.07749999999999999944, 0.08000000000000000167 ),
 .UNSPECIFIED. ) 
 CURVE ( )  GEOMETRIC_REPRESENTATION_ITEM ( )  RATIONAL_B_SPLINE_CURVE ( ( 1.000000000000000000, 0.9238795325112859613, 1.000000000000000000, 0.9238795325112869605, 1.000000000000000000, 0.9238795325112869605, 1.000000000000000000, 0.9238795325112869605, 1.000000000000000000 ) ) 
 REPRESENTATION_ITEM ( '' )  ) ;
#26720=CARTESIAN_POINT ( 'NONE',  ( 0.6971942568897626646, -0.07405724077823297447, 0.2805118109698587214 ) ) ;
#26723=CARTESIAN_POINT ( 'NONE',  ( -0.7646288533564489232, 0.1113553986120547346, 0.7726377952755906220 ) ) ;
#26724=CARTESIAN_POINT ( 'NONE',  ( -1.002407869896990045, 0.1264236179284866091, 1.326279527505291433 ) ) ;
#26725=CARTESIAN_POINT ( 'NONE',  ( 0.8759842519685039353, -0.1574803149606299191, 0.6594488187901103027 ) ) ;
#26727=CARTESIAN_POINT ( 'NONE',  ( -0.8759842519685039353, -0.1787899950787401882, 1.080216535379306952 ) ) ;
#26729=CARTESIAN_POINT ( 'NONE',  ( 0.8484283389429198019, 0.1740215856901604630, 0.03937008314049554591 ) ) ;
#26733=CARTESIAN_POINT ( 'NONE',  ( -0.8107537697050254399, -0.1574803149606297803, 1.218011811023622437 ) ) ;
#26734=CARTESIAN_POINT ( 'NONE',  ( 0.8107537697050254399, 0.1574803149606300301, 0.5733267716535435099 ) ) ;
#26735=CARTESIAN_POINT ( 'NONE',  ( -0.9873396505805591694, 0.1113553986120547346, 0.9202755905511811330 ) ) ;
#26737=CARTESIAN_POINT ( 'NONE',  ( 0.7747078557243284314, 0.1515708396127978252, 0.04064907242275175858 ) ) ;
#26739=DIRECTION ( 'NONE',  ( 1.000000000000000000, 0.000000000000000000, -1.822029033848725275E-16 ) ) ;
#26740=CARTESIAN_POINT ( 'NONE',  ( 0.9500414927467377701, 0.1787899950787401604, 0.9399606298674970661 ) ) ;
#26742=CARTESIAN_POINT ( 'NONE',  ( -0.6971942568897637749, 2.189545951927499583E-17, 1.267224409395055096 ) ) ;
#26745=CARTESIAN_POINT ( 'NONE',  ( -1.002407869896990045, 0.1264236179284866091, 0.3469488188438744070 ) ) ;
#26747=CARTESIAN_POINT ( 'NONE',  ( 0.7646288533564489232, 0.1113553986120547346, 0.8809055117034961802 ) ) ;
#26753=CARTESIAN_POINT ( 'NONE',  ( -0.7185039370078739607, 1.928577636452523993E-17, 0.2559055117034968463 ) ) ;
#26754=VECTOR ( 'NONE', #825, 39.37007874015748143 ) ;
#26755=DIRECTION ( 'NONE',  ( 0.000000000000000000, 0.000000000000000000, -1.000000000000000000 ) ) ;
#26761=CARTESIAN_POINT ( 'NONE',  ( -0.8759842519685039353, -0.1787899950787401882, 0.2140748030958428971 ) ) ;
#26762=CARTESIAN_POINT ( 'NONE',  ( -0.8759842519685039353, -0.1574803149606299191, 0.8661417322834645827 ) ) ;
#26766=CARTESIAN_POINT ( 'NONE',  ( 0.6971942568897648851, -0.07405724077823297447, 0.9940944881352130613 ) ) ;
#26767=CARTESIAN_POINT ( 'NONE',  ( 1.054774247047244540, 0.07405724077823318263, 1.441929133804504604 ) ) ;
#26769=CARTESIAN_POINT ( 'NONE',  ( 0.9412147342319837628, 0.1574803149606300301, 1.513287401574803681 ) ) ;
#26770=CARTESIAN_POINT ( 'NONE',  ( 0.7181698300657867184, 0.04631346878887296348, 1.982381534514537247 ) ) ;
#26774=CARTESIAN_POINT ( 'NONE',  ( 0.8759842519685039353, -0.1787899950787401882, 0.9965551180564724554 ) ) ;
#26775=CARTESIAN_POINT ( 'NONE',  ( -1.033464566929134687, -0.06523048226347956391, 1.424704724409449064 ) ) ;
#26777=CARTESIAN_POINT ( 'NONE',  ( 1.002407869896990045, 0.1264236179284866091, 1.764271653489543290 ) ) ;
#26780=CARTESIAN_POINT ( 'NONE',  ( 1.033464566929133799, 0.000000000000000000, 0.4429133858267716439 ) ) ;
#26782=CARTESIAN_POINT ( 'NONE',  ( -0.7185039370078739607, 1.928577636452523993E-17, 0.05905511800270921846 ) ) ;
#26783=CARTESIAN_POINT ( 'NONE',  ( 1.054774247047244540, -0.07405724077823318263, 1.082677165300567346 ) ) ;
#26784=DIRECTION ( 'NONE',  ( 0.000000000000000000, 0.000000000000000000, -1.000000000000000000 ) ) ;
#26789=CARTESIAN_POINT ( 'NONE',  ( -0.8759842519685039353, -0.1574803149606299191, 0.2755905511811023723 ) ) ;
#26790=CARTESIAN_POINT ( 'NONE',  ( -0.8759842519685039353, -0.1787899950787401882, 0.3272637794737956463 ) ) ;
#26791=ORIENTED_EDGE ( 'NONE', *, *, #35245, .F. ) ;
#26793=CARTESIAN_POINT ( 'NONE',  ( -0.6971942568897648851, -0.07405724077823297447, 1.855314960576157635 ) ) ;
#26794=CARTESIAN_POINT ( 'NONE',  ( -0.8019270111902716547, -0.1787899950787401604, 0.8759842519147408302 ) ) ;
#26795=CARTESIAN_POINT ( 'NONE',  ( -0.8019270111902717657, 0.1787899950787401604, 0.5905511810485987167 ) ) ;
#26802=CARTESIAN_POINT ( 'NONE',  ( -0.9873396505805591694, 0.1113553986120547346, 1.894685039262551163 ) ) ;
#26807=CARTESIAN_POINT ( 'NONE',  ( -1.054774247047244540, 0.07405724077823318263, 0.4576771653005669016 ) ) ;
#26808=CARTESIAN_POINT ( 'NONE',  ( -1.033464566929133799, 0.000000000000000000, 0.4035433070866141780 ) ) ;
#26809=EDGE_CURVE ( 'NONE', #44045, #38514, #15914, .T. ) ;
#26810=VECTOR ( 'NONE', #12879, 39.37007874015748143 ) ;
#26811=CARTESIAN_POINT ( 'NONE',  ( -0.8019270111902716547, -0.1787899950787401604, 1.550196850339938148 ) ) ;
#26816=CARTESIAN_POINT ( 'NONE',  ( 0.7185039370078739607, 1.928577636452523993E-17, 0.8464566928058583350 ) ) ;
#26818=CARTESIAN_POINT ( 'NONE',  ( 0.7185039370078746268, -0.06523048226347956391, 0.4650590551181104093 ) ) ;
#26820=CARTESIAN_POINT ( 'NONE',  ( -0.7646288533564489232, 0.1113553986120547346, 1.156496062884598608 ) ) ;
#26821=CARTESIAN_POINT ( 'NONE',  ( 0.8019270111902717657, -0.1787899950787401604, 0.6053149605761579677 ) ) ;
#26822=CARTESIAN_POINT ( 'NONE',  ( 0.9500414927467377701, -0.1787899950787401604, 0.09350393695411057804 ) ) ;
#26825=CARTESIAN_POINT ( 'NONE',  ( 1.033464566929133799, 0.000000000000000000, 2.007874015640504162 ) ) ;
#26827=CARTESIAN_POINT ( 'NONE',  ( 1.033464566929133799, 0.000000000000000000, 0.04921259842519685318 ) ) ;
#26828=CARTESIAN_POINT ( 'NONE',  ( -1.002407869896990045, -0.1264236179284866091, 1.124507873961984261 ) ) ;
#26829=CARTESIAN_POINT ( 'NONE',  ( 0.9873396505805591694, 0.1113553986120547346, 1.117125984251968518 ) ) ;
#26830=DIRECTION ( 'NONE',  ( 1.000000000000000000, 0.000000000000000000, -1.822029033848725275E-16 ) ) ;
#26833=CARTESIAN_POINT ( 'NONE',  ( 0.7646288533564489232, 0.1113553986120547346, 1.274606299105070839 ) ) ;
#26835=ORIENTED_EDGE ( 'NONE', *, *, #12298, .F. ) ;
#26837=CARTESIAN_POINT ( 'NONE',  ( 0.8107537697050254399, -0.1574803149606297803, 0.8636811023622043004 ) ) ;
#26838=ORIENTED_EDGE ( 'NONE', *, *, #41793, .T. ) ;
#26844=CARTESIAN_POINT ( 'NONE',  ( 0.9873396505805591694, 0.1113553986120547346, 1.186023621939716666 ) ) ;
#26846=CARTESIAN_POINT ( 'NONE',  ( -0.7185039370078739607, 1.928577636452523993E-17, 0.06889763779527559306 ) ) ;
#26851=CARTESIAN_POINT ( 'NONE',  ( -0.6971942568897648851, -0.07405724077823297447, 1.702755905458047003 ) ) ;
#26852=VERTEX_POINT ( 'NONE', #205 ) ;
#26854=CARTESIAN_POINT ( 'NONE',  ( 0.8019270111902717657, -0.1787899950787401604, 0.3690944881352128393 ) ) ;
#26856=CARTESIAN_POINT ( 'NONE',  ( -0.8019270111902717657, 0.1787899950787401604, 1.451771653489543290 ) ) ;
#26857=CARTESIAN_POINT ( 'NONE',  ( -0.7646288533564489232, 0.1113553986120547346, 1.510826771546015523 ) ) ;
#26858=CARTESIAN_POINT ( 'NONE',  ( -1.054774247047244540, -0.07405724077823318263, 1.279527559001355730 ) ) ;
#26860=CARTESIAN_POINT ( 'NONE',  ( -0.6971942568897626646, 0.07405724077823318263, 0.08366141726907129483 ) ) ;
#26862=CARTESIAN_POINT ( 'NONE',  ( -0.6971942568897637749, 2.189545951927499583E-17, 1.739665354276945131 ) ) ;
#26863=CARTESIAN_POINT ( 'NONE',  ( -1.033464566929133799, 0.000000000000000000, 2.007874015640504162 ) ) ;
#26864=CARTESIAN_POINT ( 'NONE',  ( -1.033464566929134687, 0.06523048226347956391, 1.744586614173228467 ) ) ;
#26866=CARTESIAN_POINT ( 'NONE',  ( 0.6971942568897648851, 0.07405724077823318263, 1.540354330654897685 ) ) ;
#26871=CARTESIAN_POINT ( 'NONE',  ( -0.8759842519685039353, -0.1787899950787401882, 1.158956692859621995 ) ) ;
#26872=ORIENTED_EDGE ( 'NONE', *, *, #28769, .T. ) ;
#26883=CARTESIAN_POINT ( 'NONE',  ( 1.054774247047244540, -0.07405724077823318263, 0.8464566928596233275 ) ) ;
#26884=AXIS2_PLACEMENT_3D ( 'NONE', #16113, #27148, #16574 ) ;
#26887=CARTESIAN_POINT ( 'NONE',  ( 0.7185039370078739607, 1.928577636452523993E-17, 0.09842519674286673292 ) ) ;
#26888=CARTESIAN_POINT ( 'NONE',  ( 0.9873396505805591694, 0.1113553986120547346, 0.1722440944881890035 ) ) ;
#26894=CARTESIAN_POINT ( 'NONE',  ( 1.002407869896990045, 0.1264236179284866091, 0.3075787401037169411 ) ) ;
#26895=CARTESIAN_POINT ( 'NONE',  ( -0.9500414927467378812, 0.1787899950787401604, 1.683070866087970074 ) ) ;
#26896=VERTEX_POINT ( 'NONE', #22256 ) ;
#26897=CARTESIAN_POINT ( 'NONE',  ( -1.054774247047244540, 0.07405724077823318263, 1.368110236166710125 ) ) ;
#26898=CARTESIAN_POINT ( 'NONE',  ( -0.9412147342319837628, 0.1574803149606300301, 1.316437007874015519 ) ) ;
#26899=CARTESIAN_POINT ( 'NONE',  ( 0.9500414927467378812, -0.1787899950787401604, 1.318897637741511364 ) ) ;
#26900=CARTESIAN_POINT ( 'NONE',  ( -0.8019270111902717657, 0.1787899950787401604, 1.215551181048599272 ) ) ;
#26902=CARTESIAN_POINT ( 'NONE',  ( 1.033464566929133799, 0.000000000000000000, 1.535433070758614127 ) ) ;
#26905=CARTESIAN_POINT ( 'NONE',  ( 0.9500414927467377701, -0.1787899950787401604, 0.4527559054580477249 ) ) ;
#26906=CARTESIAN_POINT ( 'NONE',  ( -1.054774247047244096, 0.000000000000000000, 0.3764763778989925203 ) ) ;
#26910=ORIENTED_EDGE ( 'NONE', *, *, #14466, .T. ) ;
#26912=CARTESIAN_POINT ( 'NONE',  ( -0.7185039370078739607, 1.928577636452523993E-17, 0.2263779527559055260 ) ) ;
#26914=CARTESIAN_POINT ( 'NONE',  ( 0.6971942568897648851, -0.07405724077823297447, 1.151574803095843036 ) ) ;
#26915=CARTESIAN_POINT ( 'NONE',  ( -0.7495606340400177148, -0.1264236179284866091, 1.975885826717889815 ) ) ;
#26916=CARTESIAN_POINT ( 'NONE',  ( -1.033464566929133799, 0.000000000000000000, 1.978346456692913646 ) ) ;
#26920=CARTESIAN_POINT ( 'NONE',  ( 1.054774247047244096, 0.000000000000000000, 1.990649606245448844 ) ) ;
#26922=CARTESIAN_POINT ( 'NONE',  ( -0.7495606340400177148, 0.1264236179284866091, 0.9473425196312755814 ) ) ;
#26923=CARTESIAN_POINT ( 'NONE',  ( -0.8759842519685039353, -0.1574803149606299191, 0.3149606299212598381 ) ) ;
#26924=CARTESIAN_POINT ( 'NONE',  ( 1.033464566929134687, -0.06523048226347956391, 0.3223425196850392971 ) ) ;
#26930=CARTESIAN_POINT ( 'NONE',  ( 0.9500414927467378812, -0.1787899950787401604, 1.313976377898992132 ) ) ;
#26931=CARTESIAN_POINT ( 'NONE',  ( 0.7185039370078739607, 1.928577636452523993E-17, 0.8956692913385826404 ) ) ;
#26932=CARTESIAN_POINT ( 'NONE',  ( -0.8759842519685039353, 0.000000000000000000, 0.000000000000000000 ) ) ;
#26934=CARTESIAN_POINT ( 'NONE',  ( 0.6971942568897637749, 2.189545951927499583E-17, 1.577263779473795369 ) ) ;
#26935=CARTESIAN_POINT ( 'NONE',  ( 1.054774247047244540, -0.07405724077823318263, 0.1377952755367876370 ) ) ;
#26937=CARTESIAN_POINT ( 'NONE',  ( -0.8107537697050254399, 0.1574803149606300301, 1.744586614065703145 ) ) ;
#26939=CARTESIAN_POINT ( 'NONE',  ( -0.9500414927467377701, 0.1787899950787401604, 0.6249999999462356737 ) ) ;
#26941=DIRECTION ( 'NONE',  ( 1.822029033848725028E-16, 0.000000000000000000, 1.000000000000000000 ) ) ;
#26943=CARTESIAN_POINT ( 'NONE',  ( -0.7646288533564489232, -0.1113553986120547346, 1.599409448711369919 ) ) ;
#26945=CARTESIAN_POINT ( 'NONE',  ( 0.6971942568897648851, -0.07405724077823297447, 1.309055118056472899 ) ) ;
#26946=CARTESIAN_POINT ( 'NONE',  ( 0.6971942568897637749, 2.189545951927499583E-17, 1.774114173174582643 ) ) ;
#26948=ORIENTED_EDGE ( 'NONE', *, *, #38948, .F. ) ;
#26952=ORIENTED_EDGE ( 'NONE', *, *, #9535, .F. ) ;
#26953=CARTESIAN_POINT ( 'NONE',  ( -0.7646288533564489232, 0.1113553986120547346, 1.520669291338582640 ) ) ;
#26957=CARTESIAN_POINT ( 'NONE',  ( 0.8759842519685039353, -0.1574803149606299191, 0.5019685038294811052 ) ) ;
#26958=CARTESIAN_POINT ( 'NONE',  ( 1.054774247047244540, -0.07405724077823318263, 0.4921259841982048577 ) ) ;
#26959=CARTESIAN_POINT ( 'NONE',  ( -0.8075642815980649258, 0.1651804164989427171, 0.03937007874015843040 ) ) ;
#26960=DIRECTION ( 'NONE',  ( 1.822029033848725028E-16, 0.000000000000000000, 1.000000000000000000 ) ) ;
#26961=CARTESIAN_POINT ( 'NONE',  ( -0.8759842519685039353, -0.1787899950787401882, 1.311515747977732405 ) ) ;
#26962=CARTESIAN_POINT ( 'NONE',  ( 0.8759842519685039353, -0.1574803149606299191, 0.8562992124908976876 ) ) ;
#26964=CARTESIAN_POINT ( 'NONE',  ( -1.002407869896990045, -0.1264236179284866091, 1.085137795221826629 ) ) ;
#26965=CARTESIAN_POINT ( 'NONE',  ( 1.033464566929133799, 0.000000000000000000, 0.6791338582677166613 ) ) ;
#26966=ORIENTED_EDGE ( 'NONE', *, *, #2630, .T. ) ;
#26967=CARTESIAN_POINT ( 'NONE',  ( -0.7646288533564489232, -0.1113553986120547346, 0.5757874014672763607 ) ) ;
#26969=CARTESIAN_POINT ( 'NONE',  ( 1.054774247047244096, 0.000000000000000000, 1.636318897584031484 ) ) ;
#26970=CARTESIAN_POINT ( 'NONE',  ( -1.033464566929134687, 0.06523048226347956391, 1.272145669291338432 ) ) ;
#26971=ADVANCED_FACE ( 'NONE', ( #38543 ), #9555, .T. ) ;
#26972=CARTESIAN_POINT ( 'NONE',  ( -0.7185039370078739607, 1.928577636452523993E-17, 1.043307086506645831 ) ) ;
#26973=LINE ( 'NONE', #5366, #32654 ) ;
#26974=CARTESIAN_POINT ( 'NONE',  ( 0.7646288533564489232, 0.1113553986120547346, 1.953740157480315043 ) ) ;
#26975=CARTESIAN_POINT ( 'NONE',  ( 0.9412147342319837628, -0.1574803149606297803, 1.449311023514519681 ) ) ;
#26980=ORIENTED_EDGE ( 'NONE', *, *, #36217, .F. ) ;
#26982=CARTESIAN_POINT ( 'NONE',  ( -0.9500414927467377701, -0.1787899950787401604, 1.589566929080094226 ) ) ;
#26984=CARTESIAN_POINT ( 'NONE',  ( -0.9500414927467378812, -0.1787899950787401604, 1.318897637741511364 ) ) ;
#26986=EDGE_CURVE ( 'NONE', #41944, #7400, #38068, .T. ) ;
#26988=( BOUNDED_CURVE ( )  B_SPLINE_CURVE ( 2, ( #16102, #7941, #15630, #41686, #22557, #8890, #18952, #19192, #33852 ),
 .UNSPECIFIED., .F., .T. ) 
 B_SPLINE_CURVE_WITH_KNOTS ( ( 3, 2, 2, 2, 3 ),
 ( 0.6300000000000000044, 0.6324999999999999512, 0.6350000000000000089, 0.6374999999999999556, 0.6400000000000000133 ),
 .UNSPECIFIED. ) 
 CURVE ( )  GEOMETRIC_REPRESENTATION_ITEM ( )  RATIONAL_B_SPLINE_CURVE ( ( 1.000000000000000000, 0.9238795325112869605, 1.000000000000000000, 0.9238795325112869605, 1.000000000000000000, 0.9238795325112869605, 1.000000000000000000, 0.9238795325112869605, 1.000000000000000000 ) ) 
 REPRESENTATION_ITEM ( '' )  ) ;
#26991=CARTESIAN_POINT ( 'NONE',  ( -0.6971942568897626646, -0.07405724077823297447, 0.3641732282926931630 ) ) ;
#26992=CARTESIAN_POINT ( 'NONE',  ( 0.8107537697050254399, 0.1574803149606300301, 1.862696850286174710 ) ) ;
#26993=CARTESIAN_POINT ( 'NONE',  ( 0.9412147342319837628, 0.1574803149606300301, 0.8735236219397174429 ) ) ;
#26995=ORIENTED_EDGE ( 'NONE', *, *, #11594, .F. ) ;
#26998=ORIENTED_EDGE ( 'NONE', *, *, #4210, .T. ) ;
#27000=CARTESIAN_POINT ( 'NONE',  ( 0.8107537697050254399, 0.1574803149606300301, 1.744586614065703145 ) ) ;
#27003=( BOUNDED_CURVE ( )  B_SPLINE_CURVE ( 2, ( #26965, #19508, #18795, #14995, #4641, #11864, #26489, #41051, #22875 ),
 .UNSPECIFIED., .F., .T. ) 
 B_SPLINE_CURVE_WITH_KNOTS ( ( 3, 2, 2, 2, 3 ),
 ( 0.3400000000000000244, 0.3425000000000000266, 0.3449999999999999734, 0.3474999999999999756, 0.3499999999999999778 ),
 .UNSPECIFIED. ) 
 CURVE ( )  GEOMETRIC_REPRESENTATION_ITEM ( )  RATIONAL_B_SPLINE_CURVE ( ( 1.000000000000000000, 0.9238795325112869605, 1.000000000000000000, 0.9238795325112869605, 1.000000000000000000, 0.9238795325112869605, 1.000000000000000000, 0.9238795325112849621, 1.000000000000000000 ) ) 
 REPRESENTATION_ITEM ( '' )  ) ;
#27004=CARTESIAN_POINT ( 'NONE',  ( -1.054774247047244540, -0.07405724077823318263, 0.2608267715997797387 ) ) ;
#27005=CARTESIAN_POINT ( 'NONE',  ( -0.8107537697050253289, 0.1574803149606300301, 0.9670275590551186129 ) ) ;
#27006=LINE ( 'NONE', #26525, #30050 ) ;
#27010=CARTESIAN_POINT ( 'NONE',  ( 0.9500414927467378812, 0.1787899950787401604, 0.8612204723871809131 ) ) ;
#27011=CARTESIAN_POINT ( 'NONE',  ( 0.8759842519685039353, -0.1787899950787401882, 1.429625984198204858 ) ) ;
#27012=CARTESIAN_POINT ( 'NONE',  ( 0.6971942568897626646, 0.07405724077823318263, 0.1181102361667090567 ) ) ;
#27014=CARTESIAN_POINT ( 'NONE',  ( 0.8759842519685039353, -0.1574803149606299191, 1.574803149606299302 ) ) ;
#27015=CARTESIAN_POINT ( 'NONE',  ( 0.7462404686856282110, -0.1095783846369325631, 1.985475001373030901 ) ) ;
#27020=CARTESIAN_POINT ( 'NONE',  ( 1.054774247047244096, 0.000000000000000000, 1.045767716481669440 ) ) ;
#27021=CARTESIAN_POINT ( 'NONE',  ( 0.6971942568897637749, 2.189545951927499583E-17, 1.779035433017102319 ) ) ;
#27022=CARTESIAN_POINT ( 'NONE',  ( 0.7646288533564489232, 0.1113553986120547346, 0.3297244093412917687 ) ) ;
#27027=DIRECTION ( 'NONE',  ( 1.000000000000000000, 0.000000000000000000, -4.336808689942014778E-16 ) ) ;
#27029=CARTESIAN_POINT ( 'NONE',  ( -0.7185039370078746268, -0.06523048226347956391, 0.1402559054042841202 ) ) ;
#27030=CARTESIAN_POINT ( 'NONE',  ( 0.9500414927467378812, 0.1787899950787401604, 1.131889763725763665 ) ) ;
#27031=CARTESIAN_POINT ( 'NONE',  ( -1.033464566929134687, 0.06523048226347956391, 1.035925196850394192 ) ) ;
#27035=CARTESIAN_POINT ( 'NONE',  ( -0.8019270111902717657, -0.1787899950787401604, 0.5610236219934807700 ) ) ;
#27036=CARTESIAN_POINT ( 'NONE',  ( 0.9873396505805591694, 0.1113553986120547346, 0.2509842519685039353 ) ) ;
#27037=CARTESIAN_POINT ( 'NONE',  ( -0.7495606340400177148, -0.1264236179284866091, 0.3223425196312759144 ) ) ;
#27042=CARTESIAN_POINT ( 'NONE',  ( -1.054774247047244540, -0.07405724077823318263, 0.5757874015210394658 ) ) ;
#27048=CARTESIAN_POINT ( 'NONE',  ( 0.8107537697050254399, -0.1574803149606297803, 1.926673228346456490 ) ) ;
#27051=CARTESIAN_POINT ( 'NONE',  ( -0.8019270111902717657, 0.1787899950787401604, 0.4675196849856070869 ) ) ;
#27052=CARTESIAN_POINT ( 'NONE',  ( -0.9873396505805591694, -0.1113553986120547346, 0.3986220472440945017 ) ) ;
#27061=CARTESIAN_POINT ( 'NONE',  ( 0.7646288533564489232, -0.1113553986120547346, 0.1919291338582677087 ) ) ;
#27062=CARTESIAN_POINT ( 'NONE',  ( 0.8107537697050254399, 0.1574803149606300301, 0.9670275590551187239 ) ) ;
#27063=CARTESIAN_POINT ( 'NONE',  ( 1.033464566929134687, 0.06523048226347956391, 0.4453740157480309270 ) ) ;
#27065=CARTESIAN_POINT ( 'NONE',  ( -1.033464566929133799, 0.000000000000000000, 1.299212598317669221 ) ) ;
#27066=CARTESIAN_POINT ( 'NONE',  ( 0.8019270111902717657, -0.1787899950787401604, 0.5265748030958428139 ) ) ;
#27067=CARTESIAN_POINT ( 'NONE',  ( 0.6971942568897637749, 2.189545951927499583E-17, 0.08120078734781142893 ) ) ;
#27069=DIRECTION ( 'NONE',  ( 1.000000000000000000, 0.000000000000000000, -1.822029033848725275E-16 ) ) ;
#27070=CARTESIAN_POINT ( 'NONE',  ( -0.7646288533564489232, 0.1113553986120547346, 1.195866141624756018 ) ) ;
#27071=EDGE_LOOP ( 'NONE', ( #24911, #20242, #36388, #37066 ) ) ;
#27072=LINE ( 'NONE', #16506, #27722 ) ;
#27073=CARTESIAN_POINT ( 'NONE',  ( -1.054774247047244540, -0.07405724077823318263, 1.087598425143086578 ) ) ;
#27074=CARTESIAN_POINT ( 'NONE',  ( 0.8759842519685039353, 0.1574803149606299191, 1.161417322834645605 ) ) ;
#27076=CARTESIAN_POINT ( 'NONE',  ( -0.9873396505805591694, 0.1113553986120547346, 0.7135826770578268530 ) ) ;
#27079=CARTESIAN_POINT ( 'NONE',  ( 1.033464566929133799, 0.000000000000000000, 0.3543307085538902057 ) ) ;
#27082=ORIENTED_EDGE ( 'NONE', *, *, #23162, .T. ) ;
#27084=CARTESIAN_POINT ( 'NONE',  ( -0.8759842519685039353, 0.1574803149606299191, 1.122047244094488194 ) ) ;
#27092=CARTESIAN_POINT ( 'NONE',  ( 0.9873396505805591694, 0.1113553986120547346, 1.146653543199559033 ) ) ;
#27095=CARTESIAN_POINT ( 'NONE',  ( -1.054774247047244096, 0.000000000000000000, 0.4552165353793071745 ) ) ;
#27098=CARTESIAN_POINT ( 'NONE',  ( -0.7495606340400177148, -0.1264236179284866091, 1.823326771599779406 ) ) ;
#27099=CARTESIAN_POINT ( 'NONE',  ( 0.7495606340400177148, -0.1264236179284866091, 1.862696850339937038 ) ) ;
#27100=EDGE_LOOP ( 'NONE', ( #11633, #34124, #7506, #28698 ) ) ;
#27102=CARTESIAN_POINT ( 'NONE',  ( -1.054774247047244540, -0.07405724077823318263, 0.8907480314422986378 ) ) ;
#27103=TOROIDAL_SURFACE ( 'NONE', #17111, 0.3444881889763780070, 0.1574803149606299191 ) ;
#27105=CARTESIAN_POINT ( 'NONE',  ( 0.6971942568897626646, 0.07405724077823318263, 0.4773622046706456068 ) ) ;
#27106=CARTESIAN_POINT ( 'NONE',  ( -1.054774247047244540, 0.07405724077823318263, 1.363188976324188895 ) ) ;
#27108=CARTESIAN_POINT ( 'NONE',  ( -0.8019270111902716547, 0.1787899950787401604, 1.373031496009229357 ) ) ;
#27110=CARTESIAN_POINT ( 'NONE',  ( -0.8759842519685039353, -0.1787899950787401882, 0.09596456687537047170 ) ) ;
#27111=CARTESIAN_POINT ( 'NONE',  ( 0.8759842519685039353, -0.1574803149606299191, 1.574803149606299302 ) ) ;
#27112=CARTESIAN_POINT ( 'NONE',  ( -0.6971942568897648851, 0.07405724077823318263, 1.697834645615527771 ) ) ;
#27113=CARTESIAN_POINT ( 'NONE',  ( -0.6971942568897637749, 2.189545951927499583E-17, 0.04675196845017354913 ) ) ;
#27114=CARTESIAN_POINT ( 'NONE',  ( -0.7185039370078746268, -0.06523048226347956391, 1.724901574803149762 ) ) ;
#27117=CARTESIAN_POINT ( 'NONE',  ( 0.8759842519685039353, -0.1787899950787401882, 1.592027559001354398 ) ) ;
#27120=VERTEX_POINT ( 'NONE', #16510 ) ;
#27126=CARTESIAN_POINT ( 'NONE',  ( 0.9500414927467378812, -0.1787899950787401604, 0.4084645668753704717 ) ) ;
#27128=CARTESIAN_POINT ( 'NONE',  ( -0.7185039370078746268, 0.06523048226347956391, 0.7652559054042838982 ) ) ;
#27133=CARTESIAN_POINT ( 'NONE',  ( 0.8759842519685039353, 0.1787899950787401882, 0.8981299212060788184 ) ) ;
#27134=CARTESIAN_POINT ( 'NONE',  ( -0.9412147342319837628, -0.1574803149606297803, 1.567421259734991690 ) ) ;
#27136=DIRECTION ( 'NONE',  ( 0.000000000000000000, 0.000000000000000000, -1.000000000000000000 ) ) ;
#27137=CARTESIAN_POINT ( 'NONE',  ( 0.6971942568897637749, 2.189545951927499583E-17, 1.936515747977732405 ) ) ;
#27139=CARTESIAN_POINT ( 'NONE',  ( 0.9412147342319837628, -0.1574803149606297803, 0.1993110236220472509 ) ) ;
#27144=EDGE_CURVE ( 'NONE', #460, #35241, #30439, .T. ) ;
#27145=CARTESIAN_POINT ( 'NONE',  ( -0.7495606340400177148, 0.1264236179284866091, 1.690452755851748146 ) ) ;
#27147=CARTESIAN_POINT ( 'NONE',  ( -0.7495606340400177148, -0.1264236179284866091, 1.350885826717889815 ) ) ;
#27148=DIRECTION ( 'NONE',  ( 0.000000000000000000, 0.000000000000000000, 1.000000000000000000 ) ) ;
#27149=CARTESIAN_POINT ( 'NONE',  ( 0.9500414927467378812, -0.1787899950787401604, 1.397637795221827295 ) ) ;
#27150=CARTESIAN_POINT ( 'NONE',  ( -1.002407869896990045, 0.1264236179284866091, 1.168799212544661348 ) ) ;
#27151=CARTESIAN_POINT ( 'NONE',  ( 0.9873396505805591694, 0.1113553986120547346, 1.540354330601133803 ) ) ;
#27153=CARTESIAN_POINT ( 'NONE',  ( 1.033464566929134687, 0.06523048226347956391, 0.04183070855389029591 ) ) ;
#27154=CARTESIAN_POINT ( 'NONE',  ( 1.054774247047244540, 0.07405724077823318263, 0.5807086613635594752 ) ) ;
#27155=CARTESIAN_POINT ( 'NONE',  ( -0.6971942568897648851, 0.07405724077823318263, 0.4330708660879683536 ) ) ;
#27156=ADVANCED_FACE ( 'NONE', ( #12456 ), #1155, .T. ) ;
#27158=EDGE_CURVE ( 'NONE', #17345, #11957, #7921, .T. ) ;
#27160=ORIENTED_EDGE ( 'NONE', *, *, #46629, .T. ) ;
#27161=CARTESIAN_POINT ( 'NONE',  ( -0.7185039370078746268, 0.06523048226347956391, 0.3026574803149607029 ) ) ;
#27163=CARTESIAN_POINT ( 'NONE',  ( -0.8107537697050254399, 0.1574803149606300301, 0.4847440943806614055 ) ) ;
#27166=EDGE_LOOP ( 'NONE', ( #11865, #41302, #21458, #28360 ) ) ;
#27167=CARTESIAN_POINT ( 'NONE',  ( -0.6971942568897626646, -0.07405724077823297447, 0.9153543306548987957 ) ) ;
#27168=DIRECTION ( 'NONE',  ( 0.000000000000000000, 0.000000000000000000, -1.000000000000000000 ) ) ;
#27169=CARTESIAN_POINT ( 'NONE',  ( -0.6971942568897637749, 2.189545951927499583E-17, 0.04183070860765386589 ) ) ;
#27171=DIRECTION ( 'NONE',  ( 1.822029033848725028E-16, 0.000000000000000000, 1.000000000000000000 ) ) ;
#27175=CARTESIAN_POINT ( 'NONE',  ( 0.6971942568897648851, 0.07405724077823318263, 1.299212598371432215 ) ) ;
#27176=CARTESIAN_POINT ( 'NONE',  ( 1.033464566929133799, 0.000000000000000000, 0.8759842519685039353 ) ) ;
#27179=CARTESIAN_POINT ( 'NONE',  ( 1.002407869896990045, -0.1264236179284866091, 1.592027559001354398 ) ) ;
#27185=CARTESIAN_POINT ( 'NONE',  ( 1.002407869896990045, 0.1264236179284866091, 0.5388779527021417826 ) ) ;
#27186=CARTESIAN_POINT ( 'NONE',  ( -1.002407869896990045, 0.1264236179284866091, 0.6619094487651338010 ) ) ;
#27190=FACE_OUTER_BOUND ( 'NONE', #2201, .T. ) ;
#27193=CARTESIAN_POINT ( 'NONE',  ( 1.002407869896990045, -0.1264236179284866091, 1.439468503883244210 ) ) ;
#27194=CARTESIAN_POINT ( 'NONE',  ( 0.6971942568897648851, -0.07405724077823297447, 1.855314960576157635 ) ) ;
#27195=CARTESIAN_POINT ( 'NONE',  ( 0.8019270111902716547, 0.1787899950787401604, 0.3100393700249766682 ) ) ;
#27198=VECTOR ( 'NONE', #43139, 39.37007874015748143 ) ;
#27199=CARTESIAN_POINT ( 'NONE',  ( -1.033464566929133799, 0.000000000000000000, 0.1574803148531029595 ) ) ;
#27205=CARTESIAN_POINT ( 'NONE',  ( 0.7495606340400177148, 0.1264236179284866091, 0.5093503936470236138 ) ) ;
#27206=CARTESIAN_POINT ( 'NONE',  ( 0.8759842519685039353, -0.1574803149606300579, 0.03937007874015747977 ) ) ;
#27207=CARTESIAN_POINT ( 'NONE',  ( 0.6971942568897648851, -0.07405724077823297447, 1.304133858213953667 ) ) ;
#27208=CARTESIAN_POINT ( 'NONE',  ( 0.8759842519685039353, -0.1574803149606299191, 1.958661417215307177 ) ) ;
#27209=CARTESIAN_POINT ( 'NONE',  ( -0.7646288533564489232, -0.1113553986120547346, 1.323818897530267602 ) ) ;
#27210=CARTESIAN_POINT ( 'NONE',  ( 0.9873396505805591694, 0.1113553986120547346, 0.7529527557979842634 ) ) ;
#27212=FACE_OUTER_BOUND ( 'NONE', #19767, .T. ) ;
#27213=ORIENTED_EDGE ( 'NONE', *, *, #18770, .T. ) ;
#27215=CARTESIAN_POINT ( 'NONE',  ( -0.9412147342319837628, 0.1574803149606300301, 0.5585629920184573827 ) ) ;
#27217=CARTESIAN_POINT ( 'NONE',  ( -0.8759842519685039353, 0.1574803149606299191, 1.200787401574803237 ) ) ;
#27219=CARTESIAN_POINT ( 'NONE',  ( 1.033464566929133799, 0.000000000000000000, 1.938976377952756014 ) ) ;
#27220=CARTESIAN_POINT ( 'NONE',  ( 0.8107537697050254399, 0.1574803149606300301, 0.3666338581601893964 ) ) ;
#27221=CARTESIAN_POINT ( 'NONE',  ( 1.033464566929134687, -0.06523048226347956391, 1.454232283357038691 ) ) ;
#27226=CARTESIAN_POINT ( 'NONE',  ( -0.6971942568897648851, -0.07405724077823297447, 1.540354330654897685 ) ) ;
#27228=CARTESIAN_POINT ( 'NONE',  ( -0.6971942568897637749, 2.189545951927499583E-17, 1.385334645615527549 ) ) ;
#27229=ORIENTED_EDGE ( 'NONE', *, *, #29449, .T. ) ;
#27230=CARTESIAN_POINT ( 'NONE',  ( -0.7646288533564489232, 0.1113553986120547346, 0.2509842518609771700 ) ) ;
#27239=CARTESIAN_POINT ( 'NONE',  ( 1.033464566929134687, 0.06523048226347956391, 1.734744094380662904 ) ) ;
#27240=CYLINDRICAL_SURFACE ( 'NONE', #10837, 0.1574803149606299191 ) ;
#27241=CARTESIAN_POINT ( 'NONE',  ( 0.7646288533564489232, -0.1113553986120547346, 1.806102362204724532 ) ) ;
#27244=ADVANCED_FACE ( 'NONE', ( #14087 ), #31608, .T. ) ;
#27245=CARTESIAN_POINT ( 'NONE',  ( -0.6971942568897626646, 0.07405724077823318263, 0.2411417322297010890 ) ) ;
#27246=CARTESIAN_POINT ( 'NONE',  ( -0.7185039370078746268, -0.06523048226347956391, 1.094980314960628975 ) ) ;
#27249=CARTESIAN_POINT ( 'NONE',  ( 1.054774247047244096, 0.000000000000000000, 1.129429133804503937 ) ) ;
#27250=CARTESIAN_POINT ( 'NONE',  ( 1.054774247047244540, -0.07405724077823318263, 1.437007873961985593 ) ) ;
#27251=EDGE_CURVE ( 'NONE', #8310, #7448, #12848, .T. ) ;
#27252=EDGE_CURVE ( 'NONE', #18121, #22721, #17711, .T. ) ;
#27254=CARTESIAN_POINT ( 'NONE',  ( 0.7185039370078746268, 0.06523048226347956391, 1.601870078740158077 ) ) ;
#27255=CARTESIAN_POINT ( 'NONE',  ( 0.7523722263184977610, 0.1050276425381515832, 1.981051316850578781 ) ) ;
#27260=CARTESIAN_POINT ( 'NONE',  ( 0.7495606340400177148, 0.1264236179284866091, 1.060531496009228247 ) ) ;
#27261=CARTESIAN_POINT ( 'NONE',  ( 1.054774247047244540, -0.07405724077823318263, 1.796259842465920853 ) ) ;
#27262=CARTESIAN_POINT ( 'NONE',  ( 0.9412147342319837628, 0.1574803149606300301, 0.2829724408373550104 ) ) ;
#27263=ORIENTED_EDGE ( 'NONE', *, *, #33845, .T. ) ;
#27265=CARTESIAN_POINT ( 'NONE',  ( 1.015010158765895509, 0.08643607152993285081, 0.03936569692628689304 ) ) ;
#27266=AXIS2_PLACEMENT_3D ( 'NONE', #27427, #1981, #5328 ) ;
#27267=TOROIDAL_SURFACE ( 'NONE', #33383, 0.3444881889763780070, 0.1574803149606299191 ) ;
#27269=CARTESIAN_POINT ( 'NONE',  ( -0.9412147342319837628, -0.1574803149606297803, 0.2682086613097960370 ) ) ;
#27271=CARTESIAN_POINT ( 'NONE',  ( 0.9500414927467378812, 0.1787899950787401604, 1.328740157426552049 ) ) ;
#27272=CARTESIAN_POINT ( 'NONE',  ( 0.7646288533564489232, 0.1113553986120547346, 1.235236220364913207 ) ) ;
#27274=CARTESIAN_POINT ( 'NONE',  ( -1.033464566929133355, 0.06523048226348168721, 1.862696850393700476 ) ) ;
#27275=( BOUNDED_CURVE ( )  B_SPLINE_CURVE ( 2, ( #37177, #10861, #18263, #32672, #22089, #36713, #47260, #32909, #29095 ),
 .UNSPECIFIED., .F., .T. ) 
 B_SPLINE_CURVE_WITH_KNOTS ( ( 3, 2, 2, 2, 3 ),
 ( 0.04000000000000000083, 0.04250000000000000305, 0.04499999999999999833, 0.04750000000000000056, 0.05000000000000000278 ),
 .UNSPECIFIED. ) 
 CURVE ( )  GEOMETRIC_REPRESENTATION_ITEM ( )  RATIONAL_B_SPLINE_CURVE ( ( 1.000000000000000000, 0.9238795325112869605, 1.000000000000000000, 0.9238795325112869605, 1.000000000000000000, 0.9238795325112869605, 1.000000000000000000, 0.9238795325112869605, 1.000000000000000000 ) ) 
 REPRESENTATION_ITEM ( '' )  ) ;
#27276=CARTESIAN_POINT ( 'NONE',  ( -1.054774247047244540, 0.07405724077823318263, 0.5757874015210394658 ) ) ;
#27279=FACE_OUTER_BOUND ( 'NONE', #10392, .T. ) ;
#27283=CARTESIAN_POINT ( 'NONE',  ( -0.6971942568897637749, 2.189545951927499583E-17, 1.031003936954110189 ) ) ;
#27284=CARTESIAN_POINT ( 'NONE',  ( -0.8019270111902717657, 0.1787899950787401604, 1.845472440891119392 ) ) ;
#27286=CARTESIAN_POINT ( 'NONE',  ( -0.6971942568897626646, 0.07405724077823318263, 0.6742125983714335469 ) ) ;
#27292=CARTESIAN_POINT ( 'NONE',  ( 1.033464566929133799, 0.000000000000000000, 0.4822834645669291653 ) ) ;
#27294=( BOUNDED_CURVE ( )  B_SPLINE_CURVE ( 2, ( #19277, #4893, #33934, #16414, #34164, #1774, #1056, #44899, #12111 ),
 .UNSPECIFIED., .F., .T. ) 
 B_SPLINE_CURVE_WITH_KNOTS ( ( 3, 2, 2, 2, 3 ),
 ( 0.5600000000000000533, 0.5625000000000000000, 0.5649999999999999467, 0.5675000000000000044, 0.5699999999999999512 ),
 .UNSPECIFIED. ) 
 CURVE ( )  GEOMETRIC_REPRESENTATION_ITEM ( )  RATIONAL_B_SPLINE_CURVE ( ( 1.000000000000000000, 0.9238795325112869605, 1.000000000000000000, 0.9238795325112869605, 1.000000000000000000, 0.9238795325112869605, 1.000000000000000000, 0.9238795325112829637, 1.000000000000000000 ) ) 
 REPRESENTATION_ITEM ( '' )  ) ;
#27295=CARTESIAN_POINT ( 'NONE',  ( -1.002407869896990045, -0.1264236179284866091, 0.5290354330171024300 ) ) ;
#27296=CARTESIAN_POINT ( 'NONE',  ( 1.033464566929133799, 0.000000000000000000, 1.230314960629921295 ) ) ;
#27297=ORIENTED_EDGE ( 'NONE', *, *, #38937, .T. ) ;
#27298=CARTESIAN_POINT ( 'NONE',  ( -1.054774247047244096, 0.000000000000000000, 1.523129921206078707 ) ) ;
#27304=ADVANCED_BREP_SHAPE_REPRESENTATION ( 'U-Bolt', ( #5043, #20860 ), #15520 ) ;
#27305=ORIENTED_EDGE ( 'NONE', *, *, #8162, .F. ) ;
#27308=CARTESIAN_POINT ( 'NONE',  ( -0.7646288533564489232, 0.1113553986120547346, 1.313976377845228249 ) ) ;
#27309=CARTESIAN_POINT ( 'NONE',  ( 0.7495606340400177148, 0.1264236179284866091, 0.5930118109698583329 ) ) ;
#27310=CARTESIAN_POINT ( 'NONE',  ( 0.9500414927467377701, 0.1787899950787401604, 0.06889763774151215492 ) ) ;
#27312=DIRECTION ( 'NONE',  ( 1.822029033848725028E-16, 0.000000000000000000, 1.000000000000000000 ) ) ;
#27317=CARTESIAN_POINT ( 'NONE',  ( -0.7495606340400177148, 0.1264236179284866091, 1.104822834591905556 ) ) ;
#27318=CARTESIAN_POINT ( 'NONE',  ( 0.8107537697050253289, -0.1574803149606297803, 1.099901574803150650 ) ) ;
#27319=CARTESIAN_POINT ( 'NONE',  ( -0.8905975117434016264, -0.1743539442039271081, 1.988441309659580769 ) ) ;
#27323=CARTESIAN_POINT ( 'NONE',  ( 0.7185039370078714072, 0.06523048226347728795, 1.277066929026331232 ) ) ;
#27328=CARTESIAN_POINT ( 'NONE',  ( 0.8759842519685039353, -0.1574803149606299191, 0.8661417322834645827 ) ) ;
#27329=CARTESIAN_POINT ( 'NONE',  ( 1.054774247047244096, 0.000000000000000000, 0.7308070865604093802 ) ) ;
#27330=ORIENTED_EDGE ( 'NONE', *, *, #33573, .T. ) ;
#27331=DIRECTION ( 'NONE',  ( 1.822029033848725028E-16, 0.000000000000000000, 1.000000000000000000 ) ) ;
#27337=CARTESIAN_POINT ( 'NONE',  ( 0.7185039370078746268, 0.06523048226347956391, 1.237696850286174044 ) ) ;
#27339=ORIENTED_EDGE ( 'NONE', *, *, #35575, .T. ) ;
#27341=CARTESIAN_POINT ( 'NONE',  ( -1.002407869896990045, 0.1264236179284866091, 1.961122047190330786 ) ) ;
#27342=CARTESIAN_POINT ( 'NONE',  ( 1.002407869896990045, -0.1264236179284866091, 1.911909448765133801 ) ) ;
#27344=CARTESIAN_POINT ( 'NONE',  ( -1.054774247047244540, 0.07405724077823318263, 0.8956692912848198684 ) ) ;
#27345=CARTESIAN_POINT ( 'NONE',  ( 0.7185039370078739607, 1.928577636452523993E-17, 1.486220472440944906 ) ) ;
#27346=CARTESIAN_POINT ( 'NONE',  ( 0.8759842519685039353, -0.1787899950787401882, 0.3715551180564728440 ) ) ;
#27347=CARTESIAN_POINT ( 'NONE',  ( -0.7495606340400177148, 0.1264236179284866091, 1.336122047190330786 ) ) ;
#27349=CARTESIAN_POINT ( 'NONE',  ( -0.6971942568897626646, 0.07405724077823318263, 0.9842519684501742638 ) ) ;
#27351=CARTESIAN_POINT ( 'NONE',  ( -1.002407869896990045, -0.1264236179284866091, 0.1402559054580474474 ) ) ;
#27353=CARTESIAN_POINT ( 'NONE',  ( -0.8759842519685039353, 0.1787899950787401882, 1.769192913332062966 ) ) ;
#27354=CARTESIAN_POINT ( 'NONE',  ( -0.8019270111902717657, 0.1787899950787401604, 0.03937007868639399305 ) ) ;
#27356=CARTESIAN_POINT ( 'NONE',  ( -0.8107537697050253289, -0.1574803149606297803, 1.769192913385826404 ) ) ;
#27357=CARTESIAN_POINT ( 'NONE',  ( -0.8759842519685039353, 0.1574803149606299191, 0.2952755905511810774 ) ) ;
#27358=CARTESIAN_POINT ( 'NONE',  ( 1.054774247047244540, 0.07405724077823318263, 1.722440944828126153 ) ) ;
#27360=CARTESIAN_POINT ( 'NONE',  ( -1.033464566929133799, 0.000000000000000000, 0.2362204723334177248 ) ) ;
#27369=CARTESIAN_POINT ( 'NONE',  ( 0.8759842519685039353, -0.1787899950787401882, 0.4060039369541102450 ) ) ;
#27372=CARTESIAN_POINT ( 'NONE',  ( -1.033464566929133799, 0.000000000000000000, 0.8661417321759370402 ) ) ;
#27375=EDGE_CURVE ( 'NONE', #42942, #3332, #17997, .T. ) ;
#27376=CARTESIAN_POINT ( 'NONE',  ( 0.8019270111902717657, 0.1787899950787401604, 0.8612204723871809131 ) ) ;
#27379=CARTESIAN_POINT ( 'NONE',  ( 0.8759842519685039353, 0.1787899950787401882, 1.926673228292693052 ) ) ;
#27380=ORIENTED_EDGE ( 'NONE', *, *, #38409, .F. ) ;
#27381=CARTESIAN_POINT ( 'NONE',  ( 0.8759842519685039353, -0.1574803149606299191, 0.3838582676090082635 ) ) ;
#27385=VECTOR ( 'NONE', #15460, 39.37007874015748143 ) ;
#27386=CARTESIAN_POINT ( 'NONE',  ( -0.7495606340400177148, 0.1264236179284866091, 1.847933070812378009 ) ) ;
#27388=VERTEX_POINT ( 'NONE', #42802 ) ;
#27389=CARTESIAN_POINT ( 'NONE',  ( -0.7495606340400177148, 0.1264236179284866091, 1.341043307032850462 ) ) ;
#27390=CARTESIAN_POINT ( 'NONE',  ( 0.8019270111902717657, -0.1787899950787401604, 1.392716535379308285 ) ) ;
#27391=CARTESIAN_POINT ( 'NONE',  ( -0.8019270111902717657, -0.1787899950787401604, 0.5265748030958428139 ) ) ;
#27392=CARTESIAN_POINT ( 'NONE',  ( 1.054774247047244540, 0.07405724077823318263, 0.06889763774151215492 ) ) ;
#27393=CARTESIAN_POINT ( 'NONE',  ( -1.002407869896990045, -0.1264236179284866091, 1.198326771599779628 ) ) ;
#27395=CARTESIAN_POINT ( 'NONE',  ( -0.9412147342319837628, 0.1574803149606300301, 1.345964566821607589 ) ) ;
#27396=CARTESIAN_POINT ( 'NONE',  ( 1.002407869896990045, -0.1264236179284866091, 0.6520669290800944484 ) ) ;
#27397=CARTESIAN_POINT ( 'NONE',  ( -0.9500414927467377701, 0.1787899950787401604, 0.5413385826234012876 ) ) ;
#27398=CARTESIAN_POINT ( 'NONE',  ( -0.7495606340400177148, -0.1264236179284866091, 0.8341535432533228045 ) ) ;
#27399=EDGE_CURVE ( 'NONE', #27120, #32643, #3303, .T. ) ;
#27402=DIRECTION ( 'NONE',  ( 0.000000000000000000, 0.000000000000000000, 1.000000000000000000 ) ) ;
#27405=CARTESIAN_POINT ( 'NONE',  ( -0.7185039370078746268, 0.06523048226347956391, 0.3420275590551182798 ) ) ;
#27407=CARTESIAN_POINT ( 'NONE',  ( -0.8107537697050254399, -0.1574803149606297803, 1.966043307086614567 ) ) ;
#27409=CARTESIAN_POINT ( 'NONE',  ( -1.033464566929133799, 0.000000000000000000, 1.309055118110236338 ) ) ;
#27410=( BOUNDED_CURVE ( )  B_SPLINE_CURVE ( 2, ( #38755, #39442, #6623, #28459, #17179, #16943, #31342, #27990, #5684 ),
 .UNSPECIFIED., .F., .T. ) 
 B_SPLINE_CURVE_WITH_KNOTS ( ( 3, 2, 2, 2, 3 ),
 ( 0.3099999999999999978, 0.3125000000000000000, 0.3150000000000000022, 0.3175000000000000044, 0.3200000000000000067 ),
 .UNSPECIFIED. ) 
 CURVE ( )  GEOMETRIC_REPRESENTATION_ITEM ( )  RATIONAL_B_SPLINE_CURVE ( ( 1.000000000000000000, 0.9238795325112869605, 1.000000000000000000, 0.9238795325112869605, 1.000000000000000000, 0.9238795325112869605, 1.000000000000000000, 0.9238795325112869605, 1.000000000000000000 ) ) 
 REPRESENTATION_ITEM ( '' )  ) ;
#27411=CARTESIAN_POINT ( 'NONE',  ( -1.054774247047244096, 0.000000000000000000, 0.1008858267178899676 ) ) ;
#27413=CARTESIAN_POINT ( 'NONE',  ( -0.7185039370078746268, 0.06523048226347977208, 0.1747047243019218821 ) ) ;
#27416=ORIENTED_EDGE ( 'NONE', *, *, #12746, .T. ) ;
#27417=CARTESIAN_POINT ( 'NONE',  ( 1.054774247047244540, 0.07405724077823318263, 1.323818897584032817 ) ) ;
#27418=CARTESIAN_POINT ( 'NONE',  ( 0.8759842519685039353, 0.1574803149606299191, 0.8858267716535432879 ) ) ;
#27422=CARTESIAN_POINT ( 'NONE',  ( 1.033464566929133355, 0.06523048226348168721, 1.862696850393700476 ) ) ;
#27423=CARTESIAN_POINT ( 'NONE',  ( 0.6971942568897626646, -0.07405724077823297447, 0.2411417322297011168 ) ) ;
#27427=CARTESIAN_POINT ( 'NONE',  ( -0.8759842519685039353, 0.000000000000000000, 0.000000000000000000 ) ) ;
#27429=CARTESIAN_POINT ( 'NONE',  ( 1.054774247047244096, 0.000000000000000000, 0.4552165353793071745 ) ) ;
#27430=CARTESIAN_POINT ( 'NONE',  ( -0.6971942568897637749, 2.189545951927499583E-17, 0.7947834645131652831 ) ) ;
#27432=CARTESIAN_POINT ( 'NONE',  ( -1.033464566929133799, 0.000000000000000000, 0.8366141732283465249 ) ) ;
#27434=CARTESIAN_POINT ( 'NONE',  ( -0.7750584684036548877, -0.1381424679723168569, 1.986199844405018622 ) ) ;
#27437=CARTESIAN_POINT ( 'NONE',  ( 1.054774247047244096, 0.000000000000000000, 1.523129921206078707 ) ) ;
#27438=CARTESIAN_POINT ( 'NONE',  ( 0.9500414927467377701, 0.1787899950787401604, 1.801181102308441861 ) ) ;
#27439=CARTESIAN_POINT ( 'NONE',  ( 0.6971942568897648851, 0.07405724077823318263, 0.4724409448281262636 ) ) ;
#27442=CARTESIAN_POINT ( 'NONE',  ( 1.033464566929133799, 1.928577636452524610E-17, 4.498031496062992574 ) ) ;
#27444=CARTESIAN_POINT ( 'NONE',  ( 0.9500414927467378812, 0.1787899950787401604, 0.5019685038832442103 ) ) ;
#27445=CARTESIAN_POINT ( 'NONE',  ( 0.7543354620012772127, -0.1135047374312812413, 0.03937368211677726160 ) ) ;
#27446=CARTESIAN_POINT ( 'NONE',  ( -0.8759842519685039353, -0.1574803149606299191, 0.7480314960629921295 ) ) ;
#27447=CARTESIAN_POINT ( 'NONE',  ( 0.7646288533564489232, 0.1113553986120547346, 0.8513779527559054427 ) ) ;
#27449=CARTESIAN_POINT ( 'NONE',  ( -0.6971942568897648851, 0.07405724077823318263, 1.299212598371432215 ) ) ;
#27450=CARTESIAN_POINT ( 'NONE',  ( 0.9873396505805591694, -0.1113553986120547346, 0.8612204723334173639 ) ) ;
#27453=CARTESIAN_POINT ( 'NONE',  ( 0.8759842519685039353, -0.1787899950787401882, 1.040846456639149764 ) ) ;
#27454=ORIENTED_EDGE ( 'NONE', *, *, #44389, .F. ) ;
#27456=CARTESIAN_POINT ( 'NONE',  ( -0.8107537697050253289, -0.1574803149606297803, 0.6176181101286932762 ) ) ;
#27457=CARTESIAN_POINT ( 'NONE',  ( -0.7185039370078739607, 1.928577636452523993E-17, 1.210629921259842590 ) ) ;
#27458=CARTESIAN_POINT ( 'NONE',  ( -1.033464566929133799, 0.000000000000000000, 1.062992125876724314 ) ) ;
#27460=CARTESIAN_POINT ( 'NONE',  ( 1.054774247047244540, -0.07405724077823318263, 0.1820866141194649179 ) ) ;
#27461=CARTESIAN_POINT ( 'NONE',  ( 0.8759842519685039353, -0.1574803149606299191, 1.446850393593259732 ) ) ;
#27464=CARTESIAN_POINT ( 'NONE',  ( 1.033464566929133799, 0.000000000000000000, 1.102362204616881947 ) ) ;
#27466=CARTESIAN_POINT ( 'NONE',  ( 1.002407869896990045, 0.1264236179284866091, 0.7012795275052913224 ) ) ;
#27467=CARTESIAN_POINT ( 'NONE',  ( -0.9500414927467377701, -0.1787899950787401604, 1.628937007820252303 ) ) ;
#27476=EDGE_CURVE ( 'NONE', #38318, #17227, #33498, .T. ) ;
#27482=CARTESIAN_POINT ( 'NONE',  ( 0.7185039370078746268, 0.06523048226347956391, 1.838090551181102539 ) ) ;
#27484=ADVANCED_FACE ( 'NONE', ( #10979 ), #853, .T. ) ;
#27487=CARTESIAN_POINT ( 'NONE',  ( -0.9500414927467377701, -0.1787899950787401604, 0.2952755904974176948 ) ) ;
#27488=CARTESIAN_POINT ( 'NONE',  ( -0.9412147342319837628, -0.1574803149606297803, 0.9867125984251976512 ) ) ;
#27490=CARTESIAN_POINT ( 'NONE',  ( 1.033464566929133799, 0.000000000000000000, 0.4035433070866141780 ) ) ;
#27491=CARTESIAN_POINT ( 'NONE',  ( 0.6971942568897648851, 0.07405724077823318263, 1.146653543253323582 ) ) ;
#27492=CARTESIAN_POINT ( 'NONE',  ( 0.9500414927467377701, 0.1787899950787401604, 0.1476377952218271561 ) ) ;
#27493=CARTESIAN_POINT ( 'NONE',  ( 1.033464566929134687, 0.06523048226347956391, 1.626476377952756458 ) ) ;
#27494=CARTESIAN_POINT ( 'NONE',  ( 0.8087737571802944281, 0.1451870484244744686, 1.979707226920621066 ) ) ;
#27499=CARTESIAN_POINT ( 'NONE',  ( -0.7646288533564489232, -0.1113553986120547346, 1.638779527451527551 ) ) ;
#27500=CARTESIAN_POINT ( 'NONE',  ( 0.9412147342319837628, -0.1574803149606297803, 1.656003937007873628 ) ) ;
#27501=CARTESIAN_POINT ( 'NONE',  ( 0.6971942568897648851, 0.07405724077823318263, 1.023622047190330342 ) ) ;
#27502=CARTESIAN_POINT ( 'NONE',  ( 0.8019270111902716547, 0.1787899950787401604, 1.850393700733638624 ) ) ;
#27503=CARTESIAN_POINT ( 'NONE',  ( 1.033464566929134687, 0.06523048226347956391, 0.3567913384751500994 ) ) ;
#27505=CARTESIAN_POINT ( 'NONE',  ( 0.7185039370078739607, 1.928577636452523993E-17, 1.240157480207432883 ) ) ;
#27508=CARTESIAN_POINT ( 'NONE',  ( -0.7646288533564489232, -0.1113553986120547346, 0.2608267715460165226 ) ) ;
#27509=CARTESIAN_POINT ( 'NONE',  ( 0.6971942568897648851, -0.07405724077823297447, 1.264763779473795813 ) ) ;
#27514=CARTESIAN_POINT ( 'NONE',  ( -0.8019270111902717657, -0.1787899950787401604, 0.6003937007336380693 ) ) ;
#27517=CYLINDRICAL_SURFACE ( 'NONE', #2532, 0.1787899950787401049 ) ;
#27519=CARTESIAN_POINT ( 'NONE',  ( -1.054774247047244540, 0.07405724077823318263, 1.013779527505291878 ) ) ;
#27520=CARTESIAN_POINT ( 'NONE',  ( -0.7185039370078746268, -0.06523048226347956391, 0.03198818897637801389 ) ) ;
#27522=EDGE_CURVE ( 'NONE', #2766, #4172, #22613, .T. ) ;
#27524=CARTESIAN_POINT ( 'NONE',  ( -0.9500414927467378812, 0.1787899950787401604, 0.7431102361667091261 ) ) ;
#27525=VERTEX_POINT ( 'NONE', #22202 ) ;
#27529=ORIENTED_EDGE ( 'NONE', *, *, #47454, .F. ) ;
#27531=CARTESIAN_POINT ( 'NONE',  ( 0.7185039370078739607, 1.928577636452523993E-17, 1.919291338582677309 ) ) ;
#27535=CARTESIAN_POINT ( 'NONE',  ( -0.8759842519685039353, 0.1787899950787401882, 0.4650590550643464716 ) ) ;
#27538=CARTESIAN_POINT ( 'NONE',  ( -0.9500414927467377701, 0.1787899950787401604, 1.687992125930489307 ) ) ;
#27540=CARTESIAN_POINT ( 'NONE',  ( -0.7185039370078739607, 1.928577636452523993E-17, 0.8464566928058583350 ) ) ;
#27544=CARTESIAN_POINT ( 'NONE',  ( 0.7185039370078760701, -0.06523048226348075740, 0.9375000000000002220 ) ) ;
#27545=CARTESIAN_POINT ( 'NONE',  ( -0.9412147342319837628, -0.1574803149606297803, 1.213090551073576107 ) ) ;
#27548=CARTESIAN_POINT ( 'NONE',  ( -0.8759842519685039353, 0.1574803149606299191, 1.190944881782236342 ) ) ;
#27549=ORIENTED_EDGE ( 'NONE', *, *, #23511, .F. ) ;
#27550=CARTESIAN_POINT ( 'NONE',  ( 0.9873396505805591694, 0.1113553986120547346, 1.579724409341291214 ) ) ;
#27551=CARTESIAN_POINT ( 'NONE',  ( -0.8019270111902716547, 0.1787899950787401604, 1.102362204670646495 ) ) ;
#27552=CARTESIAN_POINT ( 'NONE',  ( 1.033464566929133799, 0.000000000000000000, 1.151574803149606474 ) ) ;
#27558=( BOUNDED_CURVE ( )  B_SPLINE_CURVE ( 2, ( #25284, #334, #8002, #32730, #11380, #22627, #25991, #7303, #22380 ),
 .UNSPECIFIED., .F., .F. ) 
 B_SPLINE_CURVE_WITH_KNOTS ( ( 3, 2, 2, 2, 3 ),
 ( 0.3900000000000000133, 0.3925000000000000155, 0.3950000000000000178, 0.3975000000000000200, 0.4000000000000000222 ),
 .UNSPECIFIED. ) 
 CURVE ( )  GEOMETRIC_REPRESENTATION_ITEM ( )  RATIONAL_B_SPLINE_CURVE ( ( 1.000000000000000000, 0.9238795325112869605, 1.000000000000000000, 0.9238795325112869605, 1.000000000000000000, 0.9238795325112869605, 1.000000000000000000, 0.9238795325112869605, 1.000000000000000000 ) ) 
 REPRESENTATION_ITEM ( '' )  ) ;
#27559=CARTESIAN_POINT ( 'NONE',  ( 0.8759842519685039353, 0.1574803149606299191, 0.1771653543307086520 ) ) ;
#27561=CARTESIAN_POINT ( 'NONE',  ( 1.033464566929134687, 0.06523048226347956391, 1.262303149498772425 ) ) ;
#27563=DIRECTION ( 'NONE',  ( 0.000000000000000000, 0.000000000000000000, -1.000000000000000000 ) ) ;
#27565=CARTESIAN_POINT ( 'NONE',  ( -0.9500414927467378812, 0.1787899950787401604, 1.058070866087969186 ) ) ;
#27566=CARTESIAN_POINT ( 'NONE',  ( 0.6971942568897626646, 0.07405724077823318263, 0.8267716534895444003 ) ) ;
#27567=DIRECTION ( 'NONE',  ( 1.822029033848725028E-16, 0.000000000000000000, 1.000000000000000000 ) ) ;
#27568=CARTESIAN_POINT ( 'NONE',  ( 0.7646288533564489232, -0.1113553986120547346, 0.9005905511811023167 ) ) ;
#27574=EDGE_LOOP ( 'NONE', ( #7478, #2591, #37340, #38910 ) ) ;
#27575=CARTESIAN_POINT ( 'NONE',  ( -0.7495606340400177148, -0.1264236179284866091, 1.980807086560409491 ) ) ;
#27576=CARTESIAN_POINT ( 'NONE',  ( 0.6971942568897637749, 2.189545951927499583E-17, 1.818405511757259729 ) ) ;
#27578=CARTESIAN_POINT ( 'NONE',  ( 0.7185039370078739607, 1.928577636452523993E-17, 1.761811023622047223 ) ) ;
#27579=CARTESIAN_POINT ( 'NONE',  ( 0.7495606340400177148, 0.1264236179284866091, 0.4355314960092284138 ) ) ;
#27580=CARTESIAN_POINT ( 'NONE',  ( -0.8759842519685039353, -0.1787899950787401882, 1.311515747977732405 ) ) ;
#27581=CARTESIAN_POINT ( 'NONE',  ( 1.033464566929133799, 1.928577636452524610E-17, 4.498031496062992574 ) ) ;
#27582=EDGE_CURVE ( 'NONE', #26592, #38268, #42476, .T. ) ;
#27583=CARTESIAN_POINT ( 'NONE',  ( -0.6971942568897648851, -0.07405724077823297447, 0.9891732282926934960 ) ) ;
#27584=CARTESIAN_POINT ( 'NONE',  ( -1.054774247047244096, 0.000000000000000000, 0.3026574802611972648 ) ) ;
#27585=( BOUNDED_CURVE ( )  B_SPLINE_CURVE ( 2, ( #33406, #5073, #36972, #11818, #25958, #40539, #23301, #7728, #44370 ),
 .UNSPECIFIED., .F., .F. ) 
 B_SPLINE_CURVE_WITH_KNOTS ( ( 3, 2, 2, 2, 3 ),
 ( 0.4199999999999999845, 0.4224999999999999867, 0.4249999999999999889, 0.4274999999999999911, 0.4299999999999999933 ),
 .UNSPECIFIED. ) 
 CURVE ( )  GEOMETRIC_REPRESENTATION_ITEM ( )  RATIONAL_B_SPLINE_CURVE ( ( 1.000000000000000000, 0.9238795325112869605, 1.000000000000000000, 0.9238795325112869605, 1.000000000000000000, 0.9238795325112869605, 1.000000000000000000, 0.9238795325112869605, 1.000000000000000000 ) ) 
 REPRESENTATION_ITEM ( '' )  ) ;
#27589=CARTESIAN_POINT ( 'NONE',  ( -0.9500414927467378812, 0.1787899950787401604, 1.766732283410803461 ) ) ;
#27590=CARTESIAN_POINT ( 'NONE',  ( 0.7185039370078778465, -0.06523048226348396317, 1.400098425089323140 ) ) ;
#27591=CARTESIAN_POINT ( 'NONE',  ( -0.8107537697050253289, -0.1574803149606297803, 1.729822834645670548 ) ) ;
#27592=DIRECTION ( 'NONE',  ( 0.000000000000000000, 0.000000000000000000, -1.000000000000000000 ) ) ;
#27594=CARTESIAN_POINT ( 'NONE',  ( 0.7495606340400177148, -0.1264236179284866091, 1.705216535379307174 ) ) ;
#27596=CARTESIAN_POINT ( 'NONE',  ( -0.7646288533564489232, -0.1113553986120547346, 0.7332677164279054471 ) ) ;
#27597=EDGE_CURVE ( 'NONE', #44020, #5354, #20788, .T. ) ;
#27599=ORIENTED_EDGE ( 'NONE', *, *, #141, .T. ) ;
#27601=CARTESIAN_POINT ( 'NONE',  ( -0.7495606340400177148, -0.1264236179284866091, 1.154035433017102319 ) ) ;
#27608=CARTESIAN_POINT ( 'NONE',  ( 0.8759842519685039353, 0.1787899950787401882, 0.9768700786863937502 ) ) ;
#27609=AXIS2_PLACEMENT_3D ( 'NONE', #4824, #37913, #18345 ) ;
#27610=CARTESIAN_POINT ( 'NONE',  ( 0.8759842519685039353, 0.1574803149606299191, 0.6102362204724409711 ) ) ;
#27612=CARTESIAN_POINT ( 'NONE',  ( 0.9412147342319837628, 0.1574803149606300301, 0.04675196839640998608 ) ) ;
#27613=ORIENTED_EDGE ( 'NONE', *, *, #24792, .T. ) ;
#27614=CARTESIAN_POINT ( 'NONE',  ( 1.033464566929134687, -0.06523048226347956391, 0.2042322834645668717 ) ) ;
#27615=CARTESIAN_POINT ( 'NONE',  ( 0.7646288533564489232, 0.1113553986120547346, 0.7234251967428662056 ) ) ;
#27618=AXIS2_PLACEMENT_3D ( 'NONE', #21773, #2825, #43085 ) ;
#27620=CARTESIAN_POINT ( 'NONE',  ( 1.054774247047244096, 0.000000000000000000, 0.3813976377415121966 ) ) ;
#27621=DIRECTION ( 'NONE',  ( 1.000000000000000000, 0.000000000000000000, -1.822029033848725275E-16 ) ) ;
#27622=CARTESIAN_POINT ( 'NONE',  ( -1.002407869896990045, 0.1264236179284866091, 1.956200787347811110 ) ) ;
#27625=CARTESIAN_POINT ( 'NONE',  ( -0.8759842519685039353, 0.1787899950787401882, 1.493602362150960650 ) ) ;
#27627=CARTESIAN_POINT ( 'NONE',  ( 0.9500414927467378812, -0.1787899950787401604, 1.476377952702141449 ) ) ;
#27629=CARTESIAN_POINT ( 'NONE',  ( -0.9500414927467378812, -0.1787899950787401604, 0.6889763778989935750 ) ) ;
#27630=CARTESIAN_POINT ( 'NONE',  ( 0.6971942568897626646, 0.07405724077823318263, 0.1230314960092287191 ) ) ;
#27631=CARTESIAN_POINT ( 'NONE',  ( -0.8019270111902717657, -0.1787899950787401604, 1.190944881836001112 ) ) ;
#27634=CARTESIAN_POINT ( 'NONE',  ( 0.7495606340400177148, -0.1264236179284866091, 0.5634842519147401640 ) ) ;
#27635=CARTESIAN_POINT ( 'NONE',  ( -0.8019270111902716547, 0.1787899950787401604, 0.5462598424659214080 ) ) ;
#27636=CARTESIAN_POINT ( 'NONE',  ( -0.7185039370078739607, 1.928577636452523993E-17, 0.2952755904436539236 ) ) ;
#27638=CARTESIAN_POINT ( 'NONE',  ( 0.7185039370078692977, 0.06523048226347515077, 1.670767716427905780 ) ) ;
#27640=VERTEX_POINT ( 'NONE', #15753 ) ;
#27641=CARTESIAN_POINT ( 'NONE',  ( -1.033464566929134687, -0.06523048226347956391, 0.3223425196850393526 ) ) ;
#27642=CARTESIAN_POINT ( 'NONE',  ( 0.9500414927467377701, 0.1787899950787401604, 1.294291338528913204 ) ) ;
#27646=CARTESIAN_POINT ( 'NONE',  ( -0.7185039370078746268, -0.06523048226347956391, 0.5437992125984247860 ) ) ;
#27647=CARTESIAN_POINT ( 'NONE',  ( -0.6971942568897637749, 2.189545951927499583E-17, 0.9128937007336377363 ) ) ;
#27650=CYLINDRICAL_SURFACE ( 'NONE', #21179, 0.1574803149606299191 ) ;
#27652=CARTESIAN_POINT ( 'NONE',  ( -0.7646288533564489232, -0.1113553986120547346, 0.07381889763779526936 ) ) ;
#27653=ORIENTED_EDGE ( 'NONE', *, *, #38521, .F. ) ;
#27654=CARTESIAN_POINT ( 'NONE',  ( 0.6971942568897648851, -0.07405724077823297447, 1.461614173174583753 ) ) ;
#27655=VECTOR ( 'NONE', #32263, 39.37007874015748143 ) ;
#27659=CARTESIAN_POINT ( 'NONE',  ( 0.8759842519685039353, 0.1574803149606299191, 1.820866141624755796 ) ) ;
#27660=AXIS2_PLACEMENT_3D ( 'NONE', #32557, #18608, #11679 ) ;
#27664=CARTESIAN_POINT ( 'NONE',  ( -0.8759842519685039353, 0.1787899950787401882, 0.7455708660879684091 ) ) ;
#27668=CARTESIAN_POINT ( 'NONE',  ( -0.8039169694696064461, -0.1563771033850889780, 1.986832772479788956 ) ) ;
#27670=CARTESIAN_POINT ( 'NONE',  ( -1.033464566929134687, 0.06523048226347956391, 1.026082677057828185 ) ) ;
#27671=CARTESIAN_POINT ( 'NONE',  ( 0.8759842519685039353, 0.1787899950787401882, 1.454232283410803017 ) ) ;
#27673=CARTESIAN_POINT ( 'NONE',  ( 0.8759842519685039353, 0.1787899950787401882, 0.4256889763241890057 ) ) ;
#27676=DIRECTION ( 'NONE',  ( 1.822029033848725028E-16, 0.000000000000000000, 1.000000000000000000 ) ) ;
#27679=CARTESIAN_POINT ( 'NONE',  ( 0.6971942568897626646, 0.07405724077823318263, 0.3937007873478115538 ) ) ;
#27681=FACE_OUTER_BOUND ( 'NONE', #26018, .T. ) ;
#27684=CARTESIAN_POINT ( 'NONE',  ( -0.7495606340400177148, -0.1264236179284866091, 1.385334645615527549 ) ) ;
#27685=CARTESIAN_POINT ( 'NONE',  ( 0.7185039370078739607, 1.928577636452523993E-17, 0.8464566928058583350 ) ) ;
#27686=ORIENTED_EDGE ( 'NONE', *, *, #44499, .T. ) ;
#27687=DIRECTION ( 'NONE',  ( -1.000000000000000000, 0.000000000000000000, 0.000000000000000000 ) ) ;
#27688=CARTESIAN_POINT ( 'NONE',  ( 1.002407869896990045, -0.1264236179284866091, 1.045767716481669440 ) ) ;
#27691=CARTESIAN_POINT ( 'NONE',  ( -0.9412147342319837628, 0.1574803149606300301, 0.6373031494987718704 ) ) ;
#27694=CARTESIAN_POINT ( 'NONE',  ( 1.002407869896990045, 0.1264236179284866091, 1.680610236166708793 ) ) ;
#27695=CARTESIAN_POINT ( 'NONE',  ( -0.7646288533564489232, 0.1113553986120547346, 1.323818897637795367 ) ) ;
#27696=CYLINDRICAL_SURFACE ( 'NONE', #28831, 0.1574803149606299191 ) ;
#27698=CARTESIAN_POINT ( 'NONE',  ( 0.7495606340400177148, -0.1264236179284866091, 0.2091535432533232486 ) ) ;
#27699=CARTESIAN_POINT ( 'NONE',  ( -0.6971942568897626646, 0.07405724077823318263, 0.1181102361667090567 ) ) ;
#27700=CIRCLE ( 'NONE', #39088, 0.1574803149606300579 ) ;
#27701=CARTESIAN_POINT ( 'NONE',  ( 0.7185039370078746268, -0.06523048226347956391, 1.400098425089323140 ) ) ;
#27703=ORIENTED_EDGE ( 'NONE', *, *, #39963, .T. ) ;
#27704=( BOUNDED_CURVE ( )  B_SPLINE_CURVE ( 2, ( #34038, #12466, #40692, #40927, #1163, #44531, #1395, #30447, #16055 ),
 .UNSPECIFIED., .F., .T. ) 
 B_SPLINE_CURVE_WITH_KNOTS ( ( 3, 2, 2, 2, 3 ),
 ( 0.6400000000000000133, 0.6424999999999999600, 0.6450000000000000178, 0.6474999999999999645, 0.6500000000000000222 ),
 .UNSPECIFIED. ) 
 CURVE ( )  GEOMETRIC_REPRESENTATION_ITEM ( )  RATIONAL_B_SPLINE_CURVE ( ( 1.000000000000000000, 0.9238795325112869605, 1.000000000000000000, 0.9238795325112869605, 1.000000000000000000, 0.9238795325112869605, 1.000000000000000000, 0.9238795325112869605, 1.000000000000000000 ) ) 
 REPRESENTATION_ITEM ( '' )  ) ;
#27708=CARTESIAN_POINT ( 'NONE',  ( -0.7495606340400177148, -0.1264236179284866091, 1.660925196796630088 ) ) ;
#27709=VERTEX_POINT ( 'NONE', #12395 ) ;
#27715=CARTESIAN_POINT ( 'NONE',  ( -0.9873396505805591694, -0.1113553986120547346, 1.412401574695621997 ) ) ;
#27716=CARTESIAN_POINT ( 'NONE',  ( -1.033464566929134687, -0.06523048226347956391, 1.464074803149607140 ) ) ;
#27718=CARTESIAN_POINT ( 'NONE',  ( 0.8759842519685039353, -0.1574803149606299191, 1.850393700787401619 ) ) ;
#27722=VECTOR ( 'NONE', #42102, 39.37007874015748143 ) ;
#27724=CARTESIAN_POINT ( 'NONE',  ( -0.8759842519685039353, 0.1787899950787401882, 0.3124999999462365619 ) ) ;
#27725=CARTESIAN_POINT ( 'NONE',  ( -0.9412147342319837628, 0.1574803149606300301, 1.080216535433071501 ) ) ;
#27728=CARTESIAN_POINT ( 'NONE',  ( 0.8019270111902717657, -0.1787899950787401604, 1.077755905458048113 ) ) ;
#27729=CARTESIAN_POINT ( 'NONE',  ( 1.002407869896990045, -0.1264236179284866091, 1.395177165300567124 ) ) ;
#27730=CARTESIAN_POINT ( 'NONE',  ( 0.8107537697050234415, -0.1574803149606297803, 0.2337598425196851515 ) ) ;
#27731=CARTESIAN_POINT ( 'NONE',  ( 0.7646288533564489232, 0.1113553986120547346, 1.599409448818897683 ) ) ;
#27732=CARTESIAN_POINT ( 'NONE',  ( 0.8217027200616507931, 0.1498728102447202670, 1.979429313789683453 ) ) ;
#27734=CARTESIAN_POINT ( 'NONE',  ( -1.033464566929133799, 0.000000000000000000, 1.968503936900346529 ) ) ;
#27737=CARTESIAN_POINT ( 'NONE',  ( 1.054774247047244096, 0.000000000000000000, 0.9670275590013542866 ) ) ;
#27738=CARTESIAN_POINT ( 'NONE',  ( 0.6971942568897648851, 0.07405724077823318263, 1.973425196796630088 ) ) ;
#27739=CARTESIAN_POINT ( 'NONE',  ( -0.8759842519685039353, -0.1787899950787401882, 1.154035433017102319 ) ) ;
#27740=CARTESIAN_POINT ( 'NONE',  ( 0.8107537697050234415, -0.1574803149606297803, 0.3026574802074335491 ) ) ;
#27742=EDGE_CURVE ( 'NONE', #5728, #5617, #38009, .T. ) ;
#27743=CARTESIAN_POINT ( 'NONE',  ( -0.7185039370078739607, 0.000000000000000000, -2.869337061179095023E-17 ) ) ;
#27744=CARTESIAN_POINT ( 'NONE',  ( 1.032458411528080156, 0.03144513627025335295, 0.03936974531083359263 ) ) ;
#27745=CARTESIAN_POINT ( 'NONE',  ( 1.033464566929134687, 0.06523048226347956391, 0.2485236220472441526 ) ) ;
#27747=CARTESIAN_POINT ( 'NONE',  ( -1.033464566929134687, 0.06523048226347956391, 0.3174212597349925224 ) ) ;
#27750=ORIENTED_EDGE ( 'NONE', *, *, #32438, .T. ) ;
#27755=ADVANCED_FACE ( 'NONE', ( #9250 ), #34422, .T. ) ;
#27756=CARTESIAN_POINT ( 'NONE',  ( -0.7495606340400177148, -0.1264236179284866091, 0.5585629920722204877 ) ) ;
#27757=CARTESIAN_POINT ( 'NONE',  ( 0.7185039370078739607, 1.928577636452523993E-17, 1.240157480207432883 ) ) ;
#27759=ORIENTED_EDGE ( 'NONE', *, *, #25783, .F. ) ;
#27763=CARTESIAN_POINT ( 'NONE',  ( -1.054774247047244540, 0.07405724077823318263, 0.9350393700249758355 ) ) ;
#27765=AXIS2_PLACEMENT_3D ( 'NONE', #36722, #8178, #981 ) ;
#27767=CARTESIAN_POINT ( 'NONE',  ( -1.002407869896990045, 0.1264236179284866091, 0.6225393700249762796 ) ) ;
#27768=ORIENTED_EDGE ( 'NONE', *, *, #44860, .F. ) ;
#27778=CARTESIAN_POINT ( 'NONE',  ( -1.054774247047244540, 0.07405724077823318263, 0.6151574802611965431 ) ) ;
#27779=CARTESIAN_POINT ( 'NONE',  ( 0.7646288533564489232, 0.1113553986120547346, 1.353346456585388102 ) ) ;
#27781=CARTESIAN_POINT ( 'NONE',  ( -1.054774247047244096, 0.000000000000000000, 1.719980314906866203 ) ) ;
#27784=CARTESIAN_POINT ( 'NONE',  ( -0.7185039370078739607, 1.928577636452523993E-17, 0.5019685039370078705 ) ) ;
#27787=CARTESIAN_POINT ( 'NONE',  ( -0.9412147342319837628, 0.1574803149606300301, 1.227854330601135580 ) ) ;
#27795=CARTESIAN_POINT ( 'NONE',  ( 0.9873396505805591694, -0.1113553986120547346, 1.107283464566929165 ) ) ;
#27799=CARTESIAN_POINT ( 'NONE',  ( 1.033464566929134687, -0.06523048226347956391, 1.690452755797985152 ) ) ;
#27800=CARTESIAN_POINT ( 'NONE',  ( -0.7185039370078739607, 1.928577636452523993E-17, 0.9645669290263307882 ) ) ;
#27803=ORIENTED_EDGE ( 'NONE', *, *, #8155, .T. ) ;
#27807=CARTESIAN_POINT ( 'NONE',  ( 0.8759842519685039353, -0.1787899950787401882, 0.7603346456155274380 ) ) ;
#27809=CARTESIAN_POINT ( 'NONE',  ( 0.7646288533564489232, -0.1113553986120547346, 1.294291338582677309 ) ) ;
#27814=CARTESIAN_POINT ( 'NONE',  ( 0.7646288533564489232, 0.1113553986120547346, 1.235236220364913207 ) ) ;
#27817=CARTESIAN_POINT ( 'NONE',  ( -0.6971942568897637749, 2.189545951927499583E-17, 1.897145669237574772 ) ) ;
#27820=CARTESIAN_POINT ( 'NONE',  ( -0.8759842519685039353, -0.1787899950787401882, 1.587106299158834721 ) ) ;
#27821=CARTESIAN_POINT ( 'NONE',  ( -0.8759842519685039353, 0.1787899950787401882, 0.3124999999462365619 ) ) ;
#27825=CARTESIAN_POINT ( 'NONE',  ( -0.8759842519685039353, -0.1787899950787401882, 1.788877952702141672 ) ) ;
#27827=CARTESIAN_POINT ( 'NONE',  ( -0.8107537697050253289, 0.1574803149606300301, 1.754429133858266932 ) ) ;
#27830=CARTESIAN_POINT ( 'NONE',  ( 1.054774247047244540, -0.07405724077823318263, 1.678149606245448622 ) ) ;
#27833=CARTESIAN_POINT ( 'NONE',  ( -0.9412147342319837628, 0.1574803149606300301, 0.04675196839640998608 ) ) ;
#27836=CARTESIAN_POINT ( 'NONE',  ( -0.6971942568897648851, 0.07405724077823318263, 1.225393700733637514 ) ) ;
#27839=( BOUNDED_CURVE ( )  B_SPLINE_CURVE ( 2, ( #16911, #2975, #6582, #27957, #28668, #6341, #21433, #42525, #20955 ),
 .UNSPECIFIED., .F., .F. ) 
 B_SPLINE_CURVE_WITH_KNOTS ( ( 3, 2, 2, 2, 3 ),
 ( 0.3699999999999999956, 0.3724999999999999978, 0.3750000000000000000, 0.3775000000000000022, 0.3800000000000000044 ),
 .UNSPECIFIED. ) 
 CURVE ( )  GEOMETRIC_REPRESENTATION_ITEM ( )  RATIONAL_B_SPLINE_CURVE ( ( 1.000000000000000000, 0.9238795325112869605, 1.000000000000000000, 0.9238795325112869605, 1.000000000000000000, 0.9238795325112869605, 1.000000000000000000, 0.9238795325112869605, 1.000000000000000000 ) ) 
 REPRESENTATION_ITEM ( '' )  ) ;
#27842=CARTESIAN_POINT ( 'NONE',  ( -1.033464566929134687, -0.06523048226347956391, 0.8636811022546767580 ) ) ;
#27843=CARTESIAN_POINT ( 'NONE',  ( -1.033464566929133799, 0.000000000000000000, 0.6791338582677166613 ) ) ;
#27845=ADVANCED_FACE ( 'NONE', ( #41563 ), #34203, .T. ) ;
#27846=CARTESIAN_POINT ( 'NONE',  ( 0.6971942568897637749, 2.189545951927499583E-17, 0.9079724408911180600 ) ) ;
#27848=CARTESIAN_POINT ( 'NONE',  ( 0.6971942568897648851, -0.07405724077823297447, 1.978346456639149320 ) ) ;
#27849=ADVANCED_FACE ( 'NONE', ( #41330 ), #8531, .T. ) ;
#27850=EDGE_LOOP ( 'NONE', ( #37096, #15491, #35288, #5074 ) ) ;
#27852=CARTESIAN_POINT ( 'NONE',  ( 0.9873396505805591694, -0.1113553986120547346, 0.3887795274515282729 ) ) ;
#27855=( BOUNDED_CURVE ( )  B_SPLINE_CURVE ( 2, ( #34502, #24420, #39021, #9578, #38323, #16991, #38799, #1656, #34282 ),
 .UNSPECIFIED., .F., .F. ) 
 B_SPLINE_CURVE_WITH_KNOTS ( ( 3, 2, 2, 2, 3 ),
 ( 0.2700000000000000178, 0.2725000000000000200, 0.2750000000000000222, 0.2775000000000000244, 0.2800000000000000266 ),
 .UNSPECIFIED. ) 
 CURVE ( )  GEOMETRIC_REPRESENTATION_ITEM ( )  RATIONAL_B_SPLINE_CURVE ( ( 1.000000000000000000, 0.9238795325112869605, 1.000000000000000000, 0.9238795325112869605, 1.000000000000000000, 0.9238795325112869605, 1.000000000000000000, 0.9238795325112869605, 1.000000000000000000 ) ) 
 REPRESENTATION_ITEM ( '' )  ) ;
#27856=CARTESIAN_POINT ( 'NONE',  ( -1.002407869896990045, 0.1264236179284866091, 1.838090551127338657 ) ) ;
#27859=( BOUNDED_CURVE ( )  B_SPLINE_CURVE ( 2, ( #30125, #43972, #33464, #4411, #43736, #7551, #3494, #4181, #36798 ),
 .UNSPECIFIED., .F., .T. ) 
 B_SPLINE_CURVE_WITH_KNOTS ( ( 3, 2, 2, 2, 3 ),
 ( 0.1799999999999999933, 0.1824999999999999956, 0.1849999999999999978, 0.1875000000000000000, 0.1900000000000000022 ),
 .UNSPECIFIED. ) 
 CURVE ( )  GEOMETRIC_REPRESENTATION_ITEM ( )  RATIONAL_B_SPLINE_CURVE ( ( 1.000000000000000000, 0.9238795325112869605, 1.000000000000000000, 0.9238795325112869605, 1.000000000000000000, 0.9238795325112869605, 1.000000000000000000, 0.9238795325112869605, 1.000000000000000000 ) ) 
 REPRESENTATION_ITEM ( '' )  ) ;
#27860=CARTESIAN_POINT ( 'NONE',  ( -1.054774247047244540, 0.07405724077823318263, 1.525590551127340433 ) ) ;
#27861=CARTESIAN_POINT ( 'NONE',  ( -0.9412147342319837628, -0.1574803149606297803, 0.9079724409448817202 ) ) ;
#27862=CARTESIAN_POINT ( 'NONE',  ( -0.9500414927467378812, 0.1787899950787401604, 0.7037401574265510495 ) ) ;
#27863=DIRECTION ( 'NONE',  ( 0.000000000000000000, 0.000000000000000000, -1.000000000000000000 ) ) ;
#27864=CARTESIAN_POINT ( 'NONE',  ( 0.8019270111902716547, -0.1787899950787401604, 0.6840551180564720113 ) ) ;
#27865=CARTESIAN_POINT ( 'NONE',  ( -0.7495606340400177148, -0.1264236179284866091, 0.5979330708123780092 ) ) ;
#27869=CARTESIAN_POINT ( 'NONE',  ( -0.7185039370078739607, 1.928577636452523993E-17, 0.3444881889763780070 ) ) ;
#27870=CARTESIAN_POINT ( 'NONE',  ( 0.6971942568897637749, 2.189545951927499583E-17, 1.385334645615527549 ) ) ;
#27873=ORIENTED_EDGE ( 'NONE', *, *, #5406, .F. ) ;
#27875=FACE_OUTER_BOUND ( 'NONE', #23420, .T. ) ;
#27878=CARTESIAN_POINT ( 'NONE',  ( -0.7185039370078692977, 0.06523048226347515077, 1.395177165246803908 ) ) ;
#27880=CARTESIAN_POINT ( 'NONE',  ( 0.7185039370078746268, -0.06523048226347956391, 0.3863188976377952000 ) ) ;
#27881=VERTEX_POINT ( 'NONE', #9494 ) ;
#27882=CARTESIAN_POINT ( 'NONE',  ( 0.6971942568897648851, 0.07405724077823318263, 1.377952755851748146 ) ) ;
#27887=CARTESIAN_POINT ( 'NONE',  ( 0.7495606340400177148, -0.1264236179284866091, 1.700295275536787498 ) ) ;
#27888=CARTESIAN_POINT ( 'NONE',  ( 0.7495606340400177148, -0.1264236179284866091, 0.2436023621509610382 ) ) ;
#27892=FACE_OUTER_BOUND ( 'NONE', #40243, .T. ) ;
#27893=CARTESIAN_POINT ( 'NONE',  ( 0.9500414927467378812, -0.1787899950787401604, 0.4872047243556847929 ) ) ;
#27895=CARTESIAN_POINT ( 'NONE',  ( -1.002407869896990045, 0.1264236179284866091, 0.8587598424659212970 ) ) ;
#27897=CARTESIAN_POINT ( 'NONE',  ( 0.8759842519685039353, 0.1574803149606299191, 0.08858267705782735257 ) ) ;
#27901=CARTESIAN_POINT ( 'NONE',  ( 0.8019270111902717657, 0.1787899950787401604, 1.456692913332062744 ) ) ;
#27904=CARTESIAN_POINT ( 'NONE',  ( 1.054774247047244540, -0.07405724077823318263, 0.3346456692375752162 ) ) ;
#27906=EDGE_CURVE ( 'NONE', #8711, #13468, #9727, .T. ) ;
#27910=CARTESIAN_POINT ( 'NONE',  ( 0.9500414927467378812, 0.1787899950787401604, 0.4625984251430869665 ) ) ;
#27912=FACE_OUTER_BOUND ( 'NONE', #33281, .T. ) ;
#27913=CARTESIAN_POINT ( 'NONE',  ( -1.002407869896990045, -0.1264236179284866091, 1.395177165300567124 ) ) ;
#27914=VERTEX_POINT ( 'NONE', #27734 ) ;
#27915=DIRECTION ( 'NONE',  ( 0.000000000000000000, 0.000000000000000000, -1.000000000000000000 ) ) ;
#27916=CARTESIAN_POINT ( 'NONE',  ( 1.054774247047244096, 0.000000000000000000, 1.050688976324189117 ) ) ;
#27920=CARTESIAN_POINT ( 'NONE',  ( -0.7185039370078746268, -0.06523048226347956391, 0.4945866140657015353 ) ) ;
#27921=DIRECTION ( 'NONE',  ( -1.000000000000000000, 0.000000000000000000, 0.000000000000000000 ) ) ;
#27923=CARTESIAN_POINT ( 'NONE',  ( 0.8759842519685039353, 0.1787899950787401882, 0.1550196849856066983 ) ) ;
#27924=CARTESIAN_POINT ( 'NONE',  ( 0.9873396505805591694, -0.1113553986120547346, 1.451771653435779408 ) ) ;
#27929=CARTESIAN_POINT ( 'NONE',  ( -1.054774247047244540, 0.07405724077823318263, 1.678149606245448622 ) ) ;
#27931=ORIENTED_EDGE ( 'NONE', *, *, #20661, .F. ) ;
#27938=ORIENTED_EDGE ( 'NONE', *, *, #23511, .T. ) ;
#27940=CARTESIAN_POINT ( 'NONE',  ( -0.9873396505805591694, -0.1113553986120547346, 1.461614173228346525 ) ) ;
#27941=CARTESIAN_POINT ( 'NONE',  ( 0.7646288533564489232, 0.1113553986120547346, 1.796259842519684957 ) ) ;
#27945=ORIENTED_EDGE ( 'NONE', *, *, #28485, .F. ) ;
#27946=ADVANCED_FACE ( 'NONE', ( #24569 ), #42988, .T. ) ;
#27947=CARTESIAN_POINT ( 'NONE',  ( -0.6971942568897637749, 2.189545951927499583E-17, 0.3223425196312759144 ) ) ;
#27948=CARTESIAN_POINT ( 'NONE',  ( -1.033464566929133799, 0.000000000000000000, 0.9940944881889764995 ) ) ;
#27951=CARTESIAN_POINT ( 'NONE',  ( 0.7495606340400177148, 0.1264236179284866091, 1.104822834591905556 ) ) ;
#27952=CARTESIAN_POINT ( 'NONE',  ( 0.8019270111902716547, 0.1787899950787401604, 1.609251968450173598 ) ) ;
#27953=CYLINDRICAL_SURFACE ( 'NONE', #2390, 0.1574803149606299191 ) ;
#27955=CARTESIAN_POINT ( 'NONE',  ( 0.7625151755711149226, 0.1152071623345953810, 1.980784476798966853 ) ) ;
#27957=CARTESIAN_POINT ( 'NONE',  ( 0.8107537697050254399, -0.1574803149606297803, 0.7750984250893222516 ) ) ;
#27958=( BOUNDED_CURVE ( )  B_SPLINE_CURVE ( 2, ( #4161, #44403, #19499, #34143, #1274, #11619, #15926, #30556, #13274 ),
 .UNSPECIFIED., .F., .T. ) 
 B_SPLINE_CURVE_WITH_KNOTS ( ( 3, 2, 2, 2, 3 ),
 ( 0.7099999999999999645, 0.7125000000000000222, 0.7149999999999999689, 0.7175000000000000266, 0.7199999999999999734 ),
 .UNSPECIFIED. ) 
 CURVE ( )  GEOMETRIC_REPRESENTATION_ITEM ( )  RATIONAL_B_SPLINE_CURVE ( ( 1.000000000000000000, 0.9238795325112939549, 1.000000000000000000, 0.9238795325112869605, 1.000000000000000000, 0.9238795325112869605, 1.000000000000000000, 0.9238795325112869605, 1.000000000000000000 ) ) 
 REPRESENTATION_ITEM ( '' )  ) ;
#27959=CARTESIAN_POINT ( 'NONE',  ( -0.8759842519685039353, -0.1574803149606299191, 0.6988188975302678241 ) ) ;
#27960=CARTESIAN_POINT ( 'NONE',  ( 1.054774247047244540, 0.07405724077823318263, 1.166338582623402731 ) ) ;
#27961=CARTESIAN_POINT ( 'NONE',  ( 0.6971942568897648851, -0.07405724077823297447, 1.938976377898990799 ) ) ;
#27962=CARTESIAN_POINT ( 'NONE',  ( 0.7185039370078746268, -0.06523048226347956391, 0.3764763778452286935 ) ) ;
#27964=CARTESIAN_POINT ( 'NONE',  ( 1.002407869896990045, -0.1264236179284866091, 1.990649606245448844 ) ) ;
#27965=CARTESIAN_POINT ( 'NONE',  ( 1.033949376711145174, 0.01198047669008794891, 0.03936939612278594902 ) ) ;
#27966=CARTESIAN_POINT ( 'NONE',  ( -1.033464566929134687, 0.06523048226347956391, 0.1993110235145201248 ) ) ;
#27968=CARTESIAN_POINT ( 'NONE',  ( 1.002407869896990045, 0.1264236179284866091, 1.365649606245448844 ) ) ;
#27971=CARTESIAN_POINT ( 'NONE',  ( -0.7646288533564489232, -0.1113553986120547346, 0.2214566928058590567 ) ) ;
#27977=CARTESIAN_POINT ( 'NONE',  ( -0.7495606340400177148, -0.1264236179284866091, 1.345964566875370139 ) ) ;
#27979=CARTESIAN_POINT ( 'NONE',  ( -0.8019270111902717657, -0.1787899950787401604, 1.038385826717890259 ) ) ;
#27982=CARTESIAN_POINT ( 'NONE',  ( -1.002407869896990045, -0.1264236179284866091, 1.946358267662771757 ) ) ;
#27983=ORIENTED_EDGE ( 'NONE', *, *, #38037, .F. ) ;
#27984=CARTESIAN_POINT ( 'NONE',  ( -0.6971942568897626646, 0.07405724077823318263, 0.7135826771115916234 ) ) ;
#27985=EDGE_CURVE ( 'NONE', #27388, #44020, #46365, .T. ) ;
#27990=CARTESIAN_POINT ( 'NONE',  ( -1.033464566929134687, -0.06523048226347956391, 0.6668307085538908163 ) ) ;
#27993=CARTESIAN_POINT ( 'NONE',  ( -0.9873396505805591694, -0.1113553986120547346, 1.766732283357039135 ) ) ;
#27994=CARTESIAN_POINT ( 'NONE',  ( -0.7495606340400177148, -0.1264236179284866091, 0.6766732282926929409 ) ) ;
#27999=EDGE_CURVE ( 'NONE', #10600, #39650, #7629, .T. ) ;
#28000=CARTESIAN_POINT ( 'NONE',  ( -0.8759842519685039353, 0.1574803149606299191, 0.1279527557979848462 ) ) ;
#28004=CARTESIAN_POINT ( 'NONE',  ( -0.7646288533564489232, 0.1113553986120547346, 0.9694881889763780070 ) ) ;
#28005=CARTESIAN_POINT ( 'NONE',  ( -0.7646288533564489232, -0.1113553986120547346, 1.166338582569637961 ) ) ;
#28012=CARTESIAN_POINT ( 'NONE',  ( 0.7185039370078714072, 0.06523048226347728795, 1.592027558947592958 ) ) ;
#28014=CARTESIAN_POINT ( 'NONE',  ( 1.033464566929134687, 0.06523048226347956391, 1.193405511811024278 ) ) ;
#28016=CARTESIAN_POINT ( 'NONE',  ( -0.7185039370078739607, 1.928577636452523993E-17, 0.8956692913385826404 ) ) ;
#28022=CARTESIAN_POINT ( 'NONE',  ( 1.033464566929133799, 1.928577636452524610E-17, 4.498031496062992574 ) ) ;
#28026=CARTESIAN_POINT ( 'NONE',  ( 1.054774247047244096, 0.000000000000000000, 0.8882874015210394658 ) ) ;
#28029=CARTESIAN_POINT ( 'NONE',  ( -1.033464566929134687, 0.06523048226347956391, 0.5241141732283461918 ) ) ;
#28033=CARTESIAN_POINT ( 'NONE',  ( 0.8107537697050253289, -0.1574803149606297803, 1.286909448711370585 ) ) ;
#28036=CARTESIAN_POINT ( 'NONE',  ( -1.002407869896990045, 0.1264236179284866091, 1.843011810969858333 ) ) ;
#28037=CARTESIAN_POINT ( 'NONE',  ( 1.002407869896990045, 0.1264236179284866091, 1.921751968450173376 ) ) ;
#28038=VERTEX_POINT ( 'NONE', #14020 ) ;
#28040=CARTESIAN_POINT ( 'NONE',  ( -1.033464566929134687, 0.06523048226347956391, 0.4749015746956221085 ) ) ;
#28041=CARTESIAN_POINT ( 'NONE',  ( -0.9500414927467378812, -0.1787899950787401604, 1.471456692859622217 ) ) ;
#28044=CARTESIAN_POINT ( 'NONE',  ( -0.6971942568897637749, 2.189545951927499583E-17, 1.026082677111590513 ) ) ;
#28045=CARTESIAN_POINT ( 'NONE',  ( -0.7495606340400177148, -0.1264236179284866091, 0.2091535432533232486 ) ) ;
#28047=CARTESIAN_POINT ( 'NONE',  ( -0.9500414927467378812, -0.1787899950787401604, 1.870078740103715331 ) ) ;
#28049=CARTESIAN_POINT ( 'NONE',  ( -0.8107537697050253289, -0.1574803149606297803, 1.887303149606301078 ) ) ;
#28057=ORIENTED_EDGE ( 'NONE', *, *, #32279, .F. ) ;
#28058=EDGE_CURVE ( 'NONE', #31988, #28682, #27839, .T. ) ;
#28064=CARTESIAN_POINT ( 'NONE',  ( -0.9873396505805591694, 0.1113553986120547346, 0.8316929132782993062 ) ) ;
#28065=CARTESIAN_POINT ( 'NONE',  ( -1.033464566929134687, 0.06523048226347956391, 0.7209645669291341319 ) ) ;
#28068=CARTESIAN_POINT ( 'NONE',  ( 0.8019270111902717657, 0.1787899950787401604, 0.9793307086076531442 ) ) ;
#28072=CARTESIAN_POINT ( 'NONE',  ( 0.9412147342319837628, 0.1574803149606300301, 0.1648622046168823629 ) ) ;
#28073=CARTESIAN_POINT ( 'NONE',  ( 0.8107537697050254399, -0.1574803149606297803, 1.838090551073574774 ) ) ;
#28074=CARTESIAN_POINT ( 'NONE',  ( -0.8759842519685039353, 0.000000000000000000, 0.000000000000000000 ) ) ;
#28077=CARTESIAN_POINT ( 'NONE',  ( 0.6971942568897626646, -0.07405724077823297447, 0.3641732282926931630 ) ) ;
#28078=CARTESIAN_POINT ( 'NONE',  ( -0.8019270111902717657, 0.1787899950787401604, 1.924212598371433325 ) ) ;
#28079=VERTEX_POINT ( 'NONE', #13776 ) ;
#28081=CARTESIAN_POINT ( 'NONE',  ( -0.9500414927467378812, -0.1787899950787401604, 1.397637795221827295 ) ) ;
#28082=CARTESIAN_POINT ( 'NONE',  ( 1.054774247047244540, 0.07405724077823318263, 1.564960629867495845 ) ) ;
#28084=CARTESIAN_POINT ( 'NONE',  ( -0.8019270111902717657, 0.1787899950787401604, 0.6299212597887560161 ) ) ;
#28085=CARTESIAN_POINT ( 'NONE',  ( 0.8019270111902717657, -0.1787899950787401604, 0.1722440944344256208 ) ) ;
#28088=CARTESIAN_POINT ( 'NONE',  ( 1.002407869896990045, -0.1264236179284866091, 0.6126968503399370380 ) ) ;
#28089=CARTESIAN_POINT ( 'NONE',  ( -1.002407869896990045, -0.1264236179284866091, 0.5684055117572598403 ) ) ;
#28094=CARTESIAN_POINT ( 'NONE',  ( -1.033464566929134687, 0.06523048226347956391, 0.5241141732283461918 ) ) ;
#28095=CARTESIAN_POINT ( 'NONE',  ( 0.8019270111902716547, -0.1787899950787401604, 1.313976377898992132 ) ) ;
#28098=ADVANCED_FACE ( 'NONE', ( #31549 ), #21195, .T. ) ;
#28099=DIRECTION ( 'NONE',  ( 1.000000000000000000, 0.000000000000000000, -1.822029033848725275E-16 ) ) ;
#28104=ADVANCED_FACE ( 'NONE', ( #18552 ), #32963, .T. ) ;
#28105=CARTESIAN_POINT ( 'NONE',  ( 0.8759842519685039353, -0.1574803149606299191, 1.614173228346456712 ) ) ;
#28107=CARTESIAN_POINT ( 'NONE',  ( 0.6971942568897637749, 2.189545951927499583E-17, 1.419783464513165505 ) ) ;
#28111=CARTESIAN_POINT ( 'NONE',  ( 0.8759842519685039353, 0.000000000000000000, 4.498031496062992574 ) ) ;
#28116=CARTESIAN_POINT ( 'NONE',  ( 0.9500414927467378812, 0.1787899950787401604, 0.4625984251430869665 ) ) ;
#28118=( BOUNDED_CURVE ( )  B_SPLINE_CURVE ( 2, ( #24853, #9774, #35873, #39216, #28000, #32306, #42788, #13148, #31357 ),
 .UNSPECIFIED., .F., .T. ) 
 B_SPLINE_CURVE_WITH_KNOTS ( ( 3, 2, 2, 2, 3 ),
 ( 0.04000000000000000083, 0.04250000000000000305, 0.04499999999999999833, 0.04750000000000000056, 0.05000000000000000278 ),
 .UNSPECIFIED. ) 
 CURVE ( )  GEOMETRIC_REPRESENTATION_ITEM ( )  RATIONAL_B_SPLINE_CURVE ( ( 1.000000000000000000, 0.9238795325112869605, 1.000000000000000000, 0.9238795325112869605, 1.000000000000000000, 0.9238795325112869605, 1.000000000000000000, 0.9238795325112869605, 1.000000000000000000 ) ) 
 REPRESENTATION_ITEM ( '' )  ) ;
#28119=CARTESIAN_POINT ( 'NONE',  ( -0.9500414927467377701, -0.1787899950787401604, 0.8070866141194653620 ) ) ;
#28123=CARTESIAN_POINT ( 'NONE',  ( -0.7885580836502673607, -0.1477104740678956973, 1.986504824066490649 ) ) ;
#28124=CARTESIAN_POINT ( 'NONE',  ( 0.8019270111902717657, -0.1787899950787401604, 1.510826771599780294 ) ) ;
#28127=CARTESIAN_POINT ( 'NONE',  ( 0.6971942568897648851, -0.07405724077823297447, 0.3592519684501735422 ) ) ;
#28134=CARTESIAN_POINT ( 'NONE',  ( 1.002407869896990045, 0.1264236179284866091, 0.5782480314422993040 ) ) ;
#28138=CARTESIAN_POINT ( 'NONE',  ( -0.6971942568897637749, 2.189545951927499583E-17, 1.498523621993480326 ) ) ;
#28139=EDGE_LOOP ( 'NONE', ( #42996, #32274, #23486, #29192 ) ) ;
#28140=CARTESIAN_POINT ( 'NONE',  ( -1.002407869896990045, 0.1264236179284866091, 1.094980314906866203 ) ) ;
#28142=CARTESIAN_POINT ( 'NONE',  ( 0.6971942568897648851, -0.07405724077823297447, 1.033464566875371027 ) ) ;
#28144=CARTESIAN_POINT ( 'NONE',  ( 0.7646288533564489232, 0.1113553986120547346, 0.1033464566929133965 ) ) ;
#28145=CARTESIAN_POINT ( 'NONE',  ( -0.8107537697050253289, 0.1574803149606300301, 1.360728346456693050 ) ) ;
#28146=CARTESIAN_POINT ( 'NONE',  ( -0.6971942568897626646, -0.07405724077823297447, 0.8316929133320636325 ) ) ;
#28147=CARTESIAN_POINT ( 'NONE',  ( -0.7027069653493529522, 0.03506913149605040553, 0.03937007874015843734 ) ) ;
#28148=CARTESIAN_POINT ( 'NONE',  ( 1.054774247047244540, -0.07405724077823318263, 0.1033464566391499029 ) ) ;
#28149=CARTESIAN_POINT ( 'NONE',  ( -0.9500414927467377701, 0.1787899950787401604, 0.1476377952218271561 ) ) ;
#28150=CARTESIAN_POINT ( 'NONE',  ( 0.9873396505805591694, -0.1113553986120547346, 1.609251968396409493 ) ) ;
#28154=CARTESIAN_POINT ( 'NONE',  ( -0.6971942568897648851, -0.07405724077823297447, 1.776574803095843702 ) ) ;
#28161=ORIENTED_EDGE ( 'NONE', *, *, #22188, .F. ) ;
#28165=CARTESIAN_POINT ( 'NONE',  ( 0.6971942568897648851, -0.07405724077823297447, 1.067913385773007651 ) ) ;
#28168=CARTESIAN_POINT ( 'NONE',  ( 0.8107537697050253289, -0.1574803149606297803, 1.847933070866143002 ) ) ;
#28173=CARTESIAN_POINT ( 'NONE',  ( -0.7185039370078746268, 0.06523048226347956391, 0.2239173228346459099 ) ) ;
#28174=CARTESIAN_POINT ( 'NONE',  ( 0.8759842519685039353, 0.1787899950787401882, 1.099901574749385880 ) ) ;
#28175=CARTESIAN_POINT ( 'NONE',  ( 0.6971942568897637749, 2.189545951927499583E-17, 1.577263779473795369 ) ) ;
#28176=CARTESIAN_POINT ( 'NONE',  ( 0.6971942568897626646, -0.07405724077823297447, 0.2017716534895435399 ) ) ;
#28178=CARTESIAN_POINT ( 'NONE',  ( 0.8107537697050253289, -0.1574803149606297803, 1.690452755905512916 ) ) ;
#28179=CARTESIAN_POINT ( 'NONE',  ( 0.7954198352444098452, 0.1386465761046554446, 1.980005308839364320 ) ) ;
#28180=CARTESIAN_POINT ( 'NONE',  ( -0.8384580214048182878, 0.1542633986724651907, 1.979083352843399535 ) ) ;
#28182=CARTESIAN_POINT ( 'NONE',  ( -0.7646288533564489232, -0.1113553986120547346, 1.717519684931842594 ) ) ;
#28185=CARTESIAN_POINT ( 'NONE',  ( 0.8759842519685039353, -0.1787899950787401882, 0.2091535432533232486 ) ) ;
#28186=CARTESIAN_POINT ( 'NONE',  ( -1.033464566929133799, 0.000000000000000000, 0.7086614172153071767 ) ) ;
#28187=CARTESIAN_POINT ( 'NONE',  ( 1.002407869896990045, -0.1264236179284866091, 1.080216535379306952 ) ) ;
#28188=DIRECTION ( 'NONE',  ( 0.000000000000000000, 0.000000000000000000, -1.000000000000000000 ) ) ;
#28189=CARTESIAN_POINT ( 'NONE',  ( 0.8759842519685039353, -0.1574803149606299191, 0.4625984250893235838 ) ) ;
#28193=CARTESIAN_POINT ( 'NONE',  ( -1.033464566929134687, 0.06523048226347956391, 0.4355314959554649756 ) ) ;
#28195=CARTESIAN_POINT ( 'NONE',  ( 0.6971942568897648851, 0.07405724077823318263, 1.259842519631276359 ) ) ;
#28201=DIRECTION ( 'NONE',  ( -1.000000000000000000, 0.000000000000000000, 0.000000000000000000 ) ) ;
#28203=CARTESIAN_POINT ( 'NONE',  ( -0.7495606340400177148, 0.1264236179284866091, 1.414862204670645829 ) ) ;
#28205=CARTESIAN_POINT ( 'NONE',  ( -0.8019270111902717657, 0.1787899950787401604, 0.9842519684501742638 ) ) ;
#28206=CARTESIAN_POINT ( 'NONE',  ( -0.8759842519685039353, -0.1787899950787401882, 1.902066929080094448 ) ) ;
#28207=CARTESIAN_POINT ( 'NONE',  ( -0.8759842519685039353, -0.1787899950787401882, 1.114665354276944909 ) ) ;
#28208=CARTESIAN_POINT ( 'NONE',  ( -0.6971942568897626646, -0.07405724077823297447, 0.6397637794737947026 ) ) ;
#28211=CARTESIAN_POINT ( 'NONE',  ( 0.8759842519685039353, -0.1574803149606299191, 1.811023622047244208 ) ) ;
#28216=ORIENTED_EDGE ( 'NONE', *, *, #46512, .F. ) ;
#28219=CARTESIAN_POINT ( 'NONE',  ( -0.8019270111902717657, 0.1787899950787401604, 0.6643700786863951935 ) ) ;
#28222=CARTESIAN_POINT ( 'NONE',  ( -1.054774247047244540, -0.07405724077823318263, 1.678149606245448622 ) ) ;
#28224=( BOUNDED_CURVE ( )  B_SPLINE_CURVE ( 2, ( #6383, #17650, #13820, #3015, #14311, #36363, #21472, #42781, #20994 ),
 .UNSPECIFIED., .F., .T. ) 
 B_SPLINE_CURVE_WITH_KNOTS ( ( 3, 2, 2, 2, 3 ),
 ( 0.3800000000000000044, 0.3825000000000000067, 0.3850000000000000089, 0.3875000000000000111, 0.3900000000000000133 ),
 .UNSPECIFIED. ) 
 CURVE ( )  GEOMETRIC_REPRESENTATION_ITEM ( )  RATIONAL_B_SPLINE_CURVE ( ( 1.000000000000000000, 0.9238795325112869605, 1.000000000000000000, 0.9238795325112869605, 1.000000000000000000, 0.9238795325112869605, 1.000000000000000000, 0.9238795325112869605, 1.000000000000000000 ) ) 
 REPRESENTATION_ITEM ( '' )  ) ;
#28225=CARTESIAN_POINT ( 'NONE',  ( -0.7185039370078732945, -0.06523048226347920309, 0.1796259841444415029 ) ) ;
#28226=CARTESIAN_POINT ( 'NONE',  ( 0.8759842519685039353, 0.1574803149606299191, 0.6496062992125984925 ) ) ;
#28229=CARTESIAN_POINT ( 'NONE',  ( -0.7185039370078746268, -0.06523048226347956391, 1.321358267609009429 ) ) ;
#28230=CARTESIAN_POINT ( 'NONE',  ( 0.7495606340400177148, 0.1264236179284866091, 0.6717519684501732646 ) ) ;
#28236=CARTESIAN_POINT ( 'NONE',  ( 0.7185039370078739607, 1.928577636452523993E-17, 1.328740157480315043 ) ) ;
#28239=CARTESIAN_POINT ( 'NONE',  ( 0.8759842519685039353, -0.1574803149606299191, 1.968503937007874072 ) ) ;
#28240=EDGE_CURVE ( 'NONE', #18121, #2766, #7526, .T. ) ;
#28241=CARTESIAN_POINT ( 'NONE',  ( 1.054774247047244096, 0.000000000000000000, 0.6914370078202519698 ) ) ;
#28242=CARTESIAN_POINT ( 'NONE',  ( 0.8107537697050254399, -0.1574803149606297803, 1.680610236112946465 ) ) ;
#28244=CARTESIAN_POINT ( 'NONE',  ( 0.9412147342319837628, 0.1574803149606300301, 1.552657480314961758 ) ) ;
#28245=EDGE_LOOP ( 'NONE', ( #2773, #12888, #31562, #47273 ) ) ;
#28246=CARTESIAN_POINT ( 'NONE',  ( -1.033464566929133799, 0.000000000000000000, 1.072834645669291431 ) ) ;
#28247=CARTESIAN_POINT ( 'NONE',  ( 0.7646288533564489232, -0.1113553986120547346, 1.727362204724409489 ) ) ;
#28249=CARTESIAN_POINT ( 'NONE',  ( 1.054774247047244096, 0.000000000000000000, 0.8095472440407244230 ) ) ;
#28250=CARTESIAN_POINT ( 'NONE',  ( 0.8759842519685039353, -0.1574803149606299191, 1.299212598425196985 ) ) ;
#28256=CARTESIAN_POINT ( 'NONE',  ( 0.9412147342319837628, -0.1574803149606297803, 1.252460629813731741 ) ) ;
#28257=( BOUNDED_CURVE ( )  B_SPLINE_CURVE ( 2, ( #27505, #34430, #9259, #23877, #45423, #38488, #12640, #8778, #45894 ),
 .UNSPECIFIED., .F., .T. ) 
 B_SPLINE_CURVE_WITH_KNOTS ( ( 3, 2, 2, 2, 3 ),
 ( 0.6099999999999999867, 0.6125000000000000444, 0.6149999999999999911, 0.6175000000000000488, 0.6199999999999999956 ),
 .UNSPECIFIED. ) 
 CURVE ( )  GEOMETRIC_REPRESENTATION_ITEM ( )  RATIONAL_B_SPLINE_CURVE ( ( 1.000000000000000000, 0.9238795325112899581, 1.000000000000000000, 0.9238795325112869605, 1.000000000000000000, 0.9238795325112869605, 1.000000000000000000, 0.9238795325112869605, 1.000000000000000000 ) ) 
 REPRESENTATION_ITEM ( '' )  ) ;
#28259=CARTESIAN_POINT ( 'NONE',  ( -0.8759842519685039353, 0.1787899950787401882, 1.926673228292693052 ) ) ;
#28261=CARTESIAN_POINT ( 'NONE',  ( 1.002407869896990045, 0.1264236179284866091, 1.961122047190330786 ) ) ;
#28263=EDGE_CURVE ( 'NONE', #7400, #37374, #27558, .T. ) ;
#28264=CYLINDRICAL_SURFACE ( 'NONE', #35830, 0.1574803149606299191 ) ;
#28265=CARTESIAN_POINT ( 'NONE',  ( -1.054774247047244096, 0.000000000000000000, 1.006397637741511808 ) ) ;
#28267=CARTESIAN_POINT ( 'NONE',  ( -1.002407869896990045, -0.1264236179284866091, 0.2583661416785200671 ) ) ;
#28269=CARTESIAN_POINT ( 'NONE',  ( -0.7185039370078739607, 1.928577636452523993E-17, 1.791338582569637738 ) ) ;
#28270=CARTESIAN_POINT ( 'NONE',  ( -0.8019270111902717657, 0.1787899950787401604, 1.850393700733638624 ) ) ;
#28271=CARTESIAN_POINT ( 'NONE',  ( -0.8759842519685039353, -0.1787899950787401882, 0.1353346456155279653 ) ) ;
#28272=CARTESIAN_POINT ( 'NONE',  ( -0.9873396505805591694, 0.1113553986120547346, 1.943897637795275690 ) ) ;
#28276=CARTESIAN_POINT ( 'NONE',  ( -0.8759842519685039353, -0.1574803149606299191, 1.496062992125984259 ) ) ;
#28279=CARTESIAN_POINT ( 'NONE',  ( -0.9500414927467378812, -0.1787899950787401604, 0.09350393695411057804 ) ) ;
#28282=CARTESIAN_POINT ( 'NONE',  ( -0.6971942568897648851, -0.07405724077823297447, 1.230314960576158967 ) ) ;
#28288=CARTESIAN_POINT ( 'NONE',  ( 1.033464566929133799, 0.000000000000000000, 0.2460629921259842590 ) ) ;
#28289=CARTESIAN_POINT ( 'NONE',  ( -0.9873396505805591694, 0.1113553986120547346, 0.9498031494987716483 ) ) ;
#28290=CARTESIAN_POINT ( 'NONE',  ( -0.7646288533564489232, -0.1113553986120547346, 0.7431102362204724532 ) ) ;
#28293=CARTESIAN_POINT ( 'NONE',  ( 0.8759842519685039353, -0.1574803149606299191, 1.840551180994834501 ) ) ;
#28294=CARTESIAN_POINT ( 'NONE',  ( 0.9873396505805591694, -0.1113553986120547346, 0.7529527559055118058 ) ) ;
#28295=CARTESIAN_POINT ( 'NONE',  ( -0.9412147342319837628, 0.1574803149606300301, 1.237696850393701586 ) ) ;
#28296=CARTESIAN_POINT ( 'NONE',  ( 1.033464566929133799, 0.000000000000000000, 1.151574803149606474 ) ) ;
#28298=CARTESIAN_POINT ( 'NONE',  ( 0.9873396505805591694, -0.1113553986120547346, 1.097440944774362270 ) ) ;
#28299=CARTESIAN_POINT ( 'NONE',  ( 0.9412147342319837628, 0.1574803149606300301, 0.2436023620971974057 ) ) ;
#28300=DIRECTION ( 'NONE',  ( 0.000000000000000000, 0.000000000000000000, -1.000000000000000000 ) ) ;
#28304=CARTESIAN_POINT ( 'NONE',  ( -1.054774247047244540, 0.07405724077823318263, 1.835629921206078485 ) ) ;
#28306=CARTESIAN_POINT ( 'NONE',  ( -0.6971942568897637749, 2.189545951927499583E-17, 1.464074803095842370 ) ) ;
#28307=ADVANCED_FACE ( 'NONE', ( #5344 ), #19261, .T. ) ;
#28308=CARTESIAN_POINT ( 'NONE',  ( 0.8759842519685039353, 0.1787899950787401882, 1.532972440891118060 ) ) ;
#28309=CARTESIAN_POINT ( 'NONE',  ( -1.033464566929134687, -0.06523048226347956391, 0.9128937007874010634 ) ) ;
#28311=CARTESIAN_POINT ( 'NONE',  ( 0.7495606340400177148, 0.1264236179284866091, 0.1599409448281264023 ) ) ;
#28314=CARTESIAN_POINT ( 'NONE',  ( -1.054774247047244540, 0.07405724077823318263, 0.6151574802611965431 ) ) ;
#28319=ORIENTED_EDGE ( 'NONE', *, *, #27144, .F. ) ;
#28321=CARTESIAN_POINT ( 'NONE',  ( -0.8019270111902717657, 0.1787899950787401604, 1.456692913332062744 ) ) ;
#28322=CARTESIAN_POINT ( 'NONE',  ( -0.8759842519685039353, 0.1574803149606299191, 0.5314960629921260393 ) ) ;
#28323=CARTESIAN_POINT ( 'NONE',  ( 0.8759842519685039353, -0.1787899950787401882, 1.316437007820252081 ) ) ;
#28330=CARTESIAN_POINT ( 'NONE',  ( 0.8107537697050254399, -0.1574803149606297803, 1.611712598425196319 ) ) ;
#28331=CARTESIAN_POINT ( 'NONE',  ( 0.9412147342319837628, 0.1574803149606300301, 0.4896653543307082357 ) ) ;
#28333=CARTESIAN_POINT ( 'NONE',  ( 0.8759842519685039353, 0.1787899950787401882, 1.449311023568283341 ) ) ;
#28337=AXIS2_PLACEMENT_3D ( 'NONE', #11989, #26612, #8368 ) ;
#28340=CARTESIAN_POINT ( 'NONE',  ( 0.9500414927467378812, 0.1787899950787401604, 1.683070866087970074 ) ) ;
#28341=CARTESIAN_POINT ( 'NONE',  ( 1.002407869896990045, -0.1264236179284866091, 0.2928149605761578567 ) ) ;
#28345=DIRECTION ( 'NONE',  ( -1.000000000000000000, 0.000000000000000000, 0.000000000000000000 ) ) ;
#28346=CARTESIAN_POINT ( 'NONE',  ( -0.7185039370078739607, 1.928577636452523993E-17, 1.476377952648377789 ) ) ;
#28347=CARTESIAN_POINT ( 'NONE',  ( 0.6971942568897626646, 0.07405724077823318263, 0.5905511810485987167 ) ) ;
#28349=CARTESIAN_POINT ( 'NONE',  ( -0.8019270111902716547, -0.1787899950787401604, 0.8021653542769462408 ) ) ;
#28352=CARTESIAN_POINT ( 'NONE',  ( -0.7245660696681988089, -0.07386863617677040528, 1.984694592573497784 ) ) ;
#28355=CARTESIAN_POINT ( 'NONE',  ( -1.033464566929133799, 1.928577636452533546E-17, 2.007874015640504162 ) ) ;
#28356=CARTESIAN_POINT ( 'NONE',  ( 1.054774247047244540, 0.07405724077823318263, 1.643700787347811998 ) ) ;
#28357=CARTESIAN_POINT ( 'NONE',  ( 0.6971942568897648851, -0.07405724077823297447, 1.973425196796630088 ) ) ;
#28358=CARTESIAN_POINT ( 'NONE',  ( -0.8759842519685039353, -0.1574803149606299191, 1.811023622047244208 ) ) ;
#28359=CARTESIAN_POINT ( 'NONE',  ( 0.7495606340400177148, -0.1264236179284866091, 0.3617125983714334359 ) ) ;
#28360=ORIENTED_EDGE ( 'NONE', *, *, #7906, .F. ) ;
#28361=ADVANCED_FACE ( 'NONE', ( #26477 ), #19967, .T. ) ;
#28365=CARTESIAN_POINT ( 'NONE',  ( 1.002407869896990045, 0.1264236179284866091, 0.5388779527021417826 ) ) ;
#28367=CARTESIAN_POINT ( 'NONE',  ( 1.002407869896990045, 0.1264236179284866091, 0.03198818892261445085 ) ) ;
#28369=CARTESIAN_POINT ( 'NONE',  ( 1.002407869896990045, 0.1264236179284866091, 0.5388779527021417826 ) ) ;
#28370=CARTESIAN_POINT ( 'NONE',  ( -0.7646288533564489232, -0.1113553986120547346, 0.9793307086614173596 ) ) ;
#28371=CARTESIAN_POINT ( 'NONE',  ( -1.054774247047244096, 0.000000000000000000, 1.400098425143086800 ) ) ;
#28372=ORIENTED_EDGE ( 'NONE', *, *, #5787, .T. ) ;
#28373=CARTESIAN_POINT ( 'NONE',  ( -1.054774247047244096, 0.000000000000000000, 1.090059055064346527 ) ) ;
#28376=CARTESIAN_POINT ( 'NONE',  ( 0.6971942568897648851, -0.07405724077823297447, 1.151574803095843036 ) ) ;
#28378=CARTESIAN_POINT ( 'NONE',  ( -0.7646288533564489232, 0.1113553986120547346, 0.6446850392625511628 ) ) ;
#28380=CARTESIAN_POINT ( 'NONE',  ( 0.6971942568897637749, 2.189545951927499583E-17, 1.852854330654897685 ) ) ;
#28381=CARTESIAN_POINT ( 'NONE',  ( -0.9873396505805591694, 0.1113553986120547346, 1.432086614173228245 ) ) ;
#28382=CARTESIAN_POINT ( 'NONE',  ( -0.6971942568897626646, 0.07405724077823318263, 0.8661417322297003674 ) ) ;
#28383=CARTESIAN_POINT ( 'NONE',  ( 1.033464566929134687, -0.06523048226347956391, 1.808562992018457161 ) ) ;
#28384=CARTESIAN_POINT ( 'NONE',  ( -0.7013252071282976008, 0.02113730517513252166, 0.03937007874015843734 ) ) ;
#28385=CARTESIAN_POINT ( 'NONE',  ( 0.9500414927467377701, -0.1787899950787401604, 0.09842519679663024046 ) ) ;
#28386=CARTESIAN_POINT ( 'NONE',  ( 0.7646288533564489232, -0.1113553986120547346, 1.638779527451527551 ) ) ;
#28391=CARTESIAN_POINT ( 'NONE',  ( 1.054774247047244096, 0.000000000000000000, 0.8144685038832440993 ) ) ;
#28392=CARTESIAN_POINT ( 'NONE',  ( -1.054774247047244540, 0.07405724077823318263, 1.717519684985606476 ) ) ;
#28396=CARTESIAN_POINT ( 'NONE',  ( -1.033464566929134687, -0.06523048226347956391, 0.7947834645669290543 ) ) ;
#28398=ORIENTED_EDGE ( 'NONE', *, *, #17360, .F. ) ;
#28401=CARTESIAN_POINT ( 'NONE',  ( 0.7495606340400177148, 0.1264236179284866091, 1.099901574749385880 ) ) ;
#28403=CARTESIAN_POINT ( 'NONE',  ( -1.033464566929134687, 0.06523048226347956391, 0.9079724408373541777 ) ) ;
#28404=CARTESIAN_POINT ( 'NONE',  ( 0.7495606340400177148, -0.1264236179284866091, 0.04675196845017354913 ) ) ;
#28405=( BOUNDED_CURVE ( )  B_SPLINE_CURVE ( 2, ( #43964, #33694, #14279, #11162, #43724, #10928, #40121, #21936, #3716 ),
 .UNSPECIFIED., .F., .F. ) 
 B_SPLINE_CURVE_WITH_KNOTS ( ( 3, 2, 2, 2, 3 ),
 ( 0.4000000000000000222, 0.4025000000000000244, 0.4050000000000000266, 0.4074999999999999734, 0.4099999999999999756 ),
 .UNSPECIFIED. ) 
 CURVE ( )  GEOMETRIC_REPRESENTATION_ITEM ( )  RATIONAL_B_SPLINE_CURVE ( ( 1.000000000000000000, 0.9238795325112869605, 1.000000000000000000, 0.9238795325112869605, 1.000000000000000000, 0.9238795325112869605, 1.000000000000000000, 0.9238795325112849621, 1.000000000000000000 ) ) 
 REPRESENTATION_ITEM ( '' )  ) ;
#28409=CARTESIAN_POINT ( 'NONE',  ( -0.8759842519685039353, -0.1787899950787401882, 0.3321850393163153226 ) ) ;
#28411=CARTESIAN_POINT ( 'NONE',  ( 1.002407869896990045, 0.1264236179284866091, 1.173720472387181246 ) ) ;
#28412=CARTESIAN_POINT ( 'NONE',  ( 0.6971942568897648851, 0.07405724077823318263, 1.496062992072220599 ) ) ;
#28413=CARTESIAN_POINT ( 'NONE',  ( 0.8759842519685039353, -0.1787899950787401882, 0.1697834645131655606 ) ) ;
#28417=CARTESIAN_POINT ( 'NONE',  ( 0.8107537697050254399, -0.1574803149606297803, 1.523129921152316379 ) ) ;
#28422=CARTESIAN_POINT ( 'NONE',  ( -0.8107537697050253289, -0.1574803149606297803, 1.719980314853102321 ) ) ;
#28424=CARTESIAN_POINT ( 'NONE',  ( 1.002407869896990045, -0.1264236179284866091, 0.2140748030958428971 ) ) ;
#28426=CARTESIAN_POINT ( 'NONE',  ( 0.7646288533564489232, -0.1113553986120547346, 1.648622047244094668 ) ) ;
#28427=CARTESIAN_POINT ( 'NONE',  ( 0.6971942568897648851, -0.07405724077823297447, 1.186023621993481658 ) ) ;
#28430=CARTESIAN_POINT ( 'NONE',  ( 0.7185039370078746268, -0.06523048226347956391, 0.5339566928058587791 ) ) ;
#28431=VERTEX_POINT ( 'NONE', #44637 ) ;
#28435=CARTESIAN_POINT ( 'NONE',  ( -0.7646288533564489232, -0.1113553986120547346, 0.4183070865066456645 ) ) ;
#28437=CARTESIAN_POINT ( 'NONE',  ( 0.6971942568897648851, -0.07405724077823297447, 1.382874015694268044 ) ) ;
#28441=CARTESIAN_POINT ( 'NONE',  ( -0.6971942568897637749, 2.189545951927499583E-17, 0.04183070860765386589 ) ) ;
#28444=CARTESIAN_POINT ( 'NONE',  ( -1.033464566929133799, 0.000000000000000000, 1.771653543199558811 ) ) ;
#28445=CARTESIAN_POINT ( 'NONE',  ( 0.8759842519685039353, 0.000000000000000000, 4.498031496062992574 ) ) ;
#28446=CARTESIAN_POINT ( 'NONE',  ( 0.6971942568897637749, 2.189545951927499583E-17, 0.3617125983714334359 ) ) ;
#28448=CARTESIAN_POINT ( 'NONE',  ( -0.8759842519685039353, -0.1787899950787401882, 1.429625984198204858 ) ) ;
#28450=CARTESIAN_POINT ( 'NONE',  ( -0.7495606340400177148, -0.1264236179284866091, 1.975885826717889815 ) ) ;
#28452=CARTESIAN_POINT ( 'NONE',  ( -0.6971942568897637749, 2.189545951927499583E-17, 1.104822834591905556 ) ) ;
#28453=CARTESIAN_POINT ( 'NONE',  ( -0.6971942568897626646, -0.07405724077823297447, 0.7578740156942689321 ) ) ;
#28455=FACE_OUTER_BOUND ( 'NONE', #41015, .T. ) ;
#28459=CARTESIAN_POINT ( 'NONE',  ( -0.8107537697050254399, -0.1574803149606297803, 0.6569881888688504645 ) ) ;
#28460=VERTEX_POINT ( 'NONE', #30104 ) ;
#28461=CARTESIAN_POINT ( 'NONE',  ( -0.7185039370078746268, -0.06523048226347956391, 1.724901574803149540 ) ) ;
#28465=CARTESIAN_POINT ( 'NONE',  ( -0.8759842519685039353, 0.000000000000000000, 0.000000000000000000 ) ) ;
#28466=CARTESIAN_POINT ( 'NONE',  ( -0.6971942568897626646, -0.07405724077823297447, 0.6348425196312760255 ) ) ;
#28469=CARTESIAN_POINT ( 'NONE',  ( -0.8759842519685039353, 0.1787899950787401882, 1.611712598371433103 ) ) ;
#28470=CARTESIAN_POINT ( 'NONE',  ( -0.7185039370078739607, 1.928577636452523993E-17, 1.122047243986960652 ) ) ;
#28475=CARTESIAN_POINT ( 'NONE',  ( -0.9412147342319837628, -0.1574803149606297803, 1.409940944774363825 ) ) ;
#28476=CARTESIAN_POINT ( 'NONE',  ( 1.002407869896990045, -0.1264236179284866091, 0.6520669290800944484 ) ) ;
#28478=DIRECTION ( 'NONE',  ( 1.000000000000000000, 0.000000000000000000, 0.000000000000000000 ) ) ;
#28480=CARTESIAN_POINT ( 'NONE',  ( 0.8759842519685039353, -0.1574803149606299191, 1.220472440944881942 ) ) ;
#28482=CARTESIAN_POINT ( 'NONE',  ( 0.7574579170730053601, -0.1223940863669777251, 1.985778636841143641 ) ) ;
#28483=CARTESIAN_POINT ( 'NONE',  ( -0.5314960629921260393, 0.000000000000000000, 4.685039370078739829 ) ) ;
#28485=EDGE_CURVE ( 'NONE', #35290, #26252, #5109, .T. ) ;
#28487=CARTESIAN_POINT ( 'NONE',  ( 1.054774247047244540, -0.07405724077823318263, 0.7283464566391492090 ) ) ;
#28489=CARTESIAN_POINT ( 'NONE',  ( -0.8759842519685039353, -0.1574803149606299191, 0.3838582676090082635 ) ) ;
#28492=CARTESIAN_POINT ( 'NONE',  ( 1.033464566929134687, 0.06523048226347956391, 1.744586614173228467 ) ) ;
#28496=CARTESIAN_POINT ( 'NONE',  ( 0.9500414927467378812, 0.1787899950787401604, 1.053149606245450176 ) ) ;
#28497=VERTEX_POINT ( 'NONE', #34144 ) ;
#28499=CARTESIAN_POINT ( 'NONE',  ( -1.033464566929133799, 0.000000000000000000, 1.820866141732283561 ) ) ;
#28500=CARTESIAN_POINT ( 'NONE',  ( -0.8107537697050254399, 0.1574803149606300301, 0.5339566929133854334 ) ) ;
#28504=CARTESIAN_POINT ( 'NONE',  ( 0.8107537697050254399, 0.1574803149606300301, 1.242618110236220819 ) ) ;
#28505=CARTESIAN_POINT ( 'NONE',  ( -1.002407869896990045, -0.1264236179284866091, 0.09596456687537027741 ) ) ;
#28506=ORIENTED_EDGE ( 'NONE', *, *, #17151, .T. ) ;
#28507=CARTESIAN_POINT ( 'NONE',  ( -0.8759842519685039353, -0.1574803149606299191, 0.8169291337507401662 ) ) ;
#28509=CARTESIAN_POINT ( 'NONE',  ( -0.8019270111902716547, -0.1787899950787401604, 1.983267716481668108 ) ) ;
#28510=CARTESIAN_POINT ( 'NONE',  ( -0.7495606340400177148, -0.1264236179284866091, 1.070374015694267600 ) ) ;
#28511=CARTESIAN_POINT ( 'NONE',  ( -0.9500414927467378812, 0.1787899950787401604, 0.2706692912848194243 ) ) ;
#28512=FACE_OUTER_BOUND ( 'NONE', #10718, .T. ) ;
#28513=CARTESIAN_POINT ( 'NONE',  ( -0.8759842519685039353, -0.1787899950787401882, 1.906988188922614125 ) ) ;
#28515=CARTESIAN_POINT ( 'NONE',  ( -0.9873396505805591694, 0.1113553986120547346, 1.865157480314960647 ) ) ;
#28520=CARTESIAN_POINT ( 'NONE',  ( 0.8107537697050254399, -0.1574803149606297803, 1.050688976270426567 ) ) ;
#28522=CARTESIAN_POINT ( 'NONE',  ( -1.054774247047244540, 0.07405724077823318263, 0.2214566928596220785 ) ) ;
#28523=( BOUNDED_CURVE ( )  B_SPLINE_CURVE ( 2, ( #28930, #25307, #24588, #24820, #20745, #25058, #17629, #3238, #43492 ),
 .UNSPECIFIED., .F., .T. ) 
 B_SPLINE_CURVE_WITH_KNOTS ( ( 3, 2, 2, 2, 3 ),
 ( 0.2000000000000000111, 0.2025000000000000133, 0.2049999999999999878, 0.2074999999999999900, 0.2099999999999999922 ),
 .UNSPECIFIED. ) 
 CURVE ( )  GEOMETRIC_REPRESENTATION_ITEM ( )  RATIONAL_B_SPLINE_CURVE ( ( 1.000000000000000000, 0.9238795325112849621, 1.000000000000000000, 0.9238795325112869605, 1.000000000000000000, 0.9238795325112869605, 1.000000000000000000, 0.9238795325112869605, 1.000000000000000000 ) ) 
 REPRESENTATION_ITEM ( '' )  ) ;
#28524=ORIENTED_EDGE ( 'NONE', *, *, #1900, .F. ) ;
#28532=DIRECTION ( 'NONE',  ( 0.000000000000000000, 0.000000000000000000, -1.000000000000000000 ) ) ;
#28533=CARTESIAN_POINT ( 'NONE',  ( -1.033464566929134687, 0.06523048226347956391, 0.9867125983176702197 ) ) ;
#28535=CARTESIAN_POINT ( 'NONE',  ( -0.8107537697050253289, -0.1574803149606297803, 0.7455708661417325134 ) ) ;
#28537=CARTESIAN_POINT ( 'NONE',  ( 0.7646288533564489232, 0.1113553986120547346, 1.747047243986960652 ) ) ;
#28538=ORIENTED_EDGE ( 'NONE', *, *, #33573, .F. ) ;
#28540=CARTESIAN_POINT ( 'NONE',  ( 0.9412147342319837628, -0.1574803149606297803, 0.8292322834645677876 ) ) ;
#28542=CARTESIAN_POINT ( 'NONE',  ( -1.033464566929134687, -0.06523048226347956391, 1.611712598317669221 ) ) ;
#28543=( BOUNDED_CURVE ( )  B_SPLINE_CURVE ( 2, ( #42423, #42884, #2648, #39306, #10340, #31685, #6241, #31445, #6480 ),
 .UNSPECIFIED., .F., .T. ) 
 B_SPLINE_CURVE_WITH_KNOTS ( ( 3, 2, 2, 2, 3 ),
 ( 0.3099999999999999978, 0.3125000000000000000, 0.3150000000000000022, 0.3175000000000000044, 0.3200000000000000067 ),
 .UNSPECIFIED. ) 
 CURVE ( )  GEOMETRIC_REPRESENTATION_ITEM ( )  RATIONAL_B_SPLINE_CURVE ( ( 1.000000000000000000, 0.9238795325112869605, 1.000000000000000000, 0.9238795325112869605, 1.000000000000000000, 0.9238795325112869605, 1.000000000000000000, 0.9238795325112869605, 1.000000000000000000 ) ) 
 REPRESENTATION_ITEM ( '' )  ) ;
#28547=CARTESIAN_POINT ( 'NONE',  ( 1.033464566929134687, -0.06523048226347956391, 0.1550196849318430659 ) ) ;
#28550=FACE_OUTER_BOUND ( 'NONE', #25506, .T. ) ;
#28553=CARTESIAN_POINT ( 'NONE',  ( 0.8107537697050253289, -0.1574803149606297803, 0.9325787400499522262 ) ) ;
#28556=CARTESIAN_POINT ( 'NONE',  ( -0.6971942568897637749, 2.189545951927499583E-17, 0.4355314960092284138 ) ) ;
#28558=CARTESIAN_POINT ( 'NONE',  ( -0.7495606340400177148, 0.1264236179284866091, 1.380413385773007873 ) ) ;
#28559=CARTESIAN_POINT ( 'NONE',  ( 1.054774247047244540, -0.07405724077823318263, 1.520669291284818758 ) ) ;
#28561=DIRECTION ( 'NONE',  ( 0.000000000000000000, 0.000000000000000000, -1.000000000000000000 ) ) ;
#28562=CARTESIAN_POINT ( 'NONE',  ( -1.002407869896990045, 0.1264236179284866091, 0.6619094487651338010 ) ) ;
#28564=CARTESIAN_POINT ( 'NONE',  ( 0.6971942568897626646, 0.07405724077823318263, 0.2017716534895435399 ) ) ;
#28565=CARTESIAN_POINT ( 'NONE',  ( -0.8107537697050254399, -0.1574803149606297803, 1.680610236112946465 ) ) ;
#28566=CARTESIAN_POINT ( 'NONE',  ( 1.054774247047244096, 0.000000000000000000, 0.7357283464029290565 ) ) ;
#28567=CARTESIAN_POINT ( 'NONE',  ( -1.002407869896990045, 0.1264236179284866091, 0.6963582676627716461 ) ) ;
#28569=CARTESIAN_POINT ( 'NONE',  ( 0.9873396505805591694, 0.1113553986120547346, 1.067913385719243990 ) ) ;
#28571=CARTESIAN_POINT ( 'NONE',  ( -0.8759842519685039353, -0.1787899950787401882, 1.473917322780881722 ) ) ;
#28573=CARTESIAN_POINT ( 'NONE',  ( -1.033464566929133799, 0.000000000000000000, 1.466535433070866201 ) ) ;
#28575=CARTESIAN_POINT ( 'NONE',  ( -0.8107537697050253289, -0.1574803149606297803, 0.3912401574803148763 ) ) ;
#28576=CARTESIAN_POINT ( 'NONE',  ( 1.054774247047244096, 0.000000000000000000, 1.365649606245448844 ) ) ;
#28578=EDGE_LOOP ( 'NONE', ( #6702, #11746, #18108, #21352 ) ) ;
#28579=CARTESIAN_POINT ( 'NONE',  ( -0.7185039370078746268, -0.06523048226347956391, 0.6225393700787400508 ) ) ;
#28580=EDGE_CURVE ( 'NONE', #28431, #32335, #30557, .T. ) ;
#28583=CARTESIAN_POINT ( 'NONE',  ( 1.033464566929133799, 0.000000000000000000, 0.4035433070866141780 ) ) ;
#28586=CARTESIAN_POINT ( 'NONE',  ( -0.9873396505805591694, -0.1113553986120547346, 1.146653543307086798 ) ) ;
#28593=CARTESIAN_POINT ( 'NONE',  ( 0.7495606340400177148, 0.1264236179284866091, 0.2731299212060791515 ) ) ;
#28600=CARTESIAN_POINT ( 'NONE',  ( -0.8759842519685039353, 0.000000000000000000, 0.000000000000000000 ) ) ;
#28601=CARTESIAN_POINT ( 'NONE',  ( -0.7185039370078746268, -0.06523048226347956391, 1.685531496062991019 ) ) ;
#28602=CARTESIAN_POINT ( 'NONE',  ( 0.6971942568897637749, 2.189545951927499583E-17, 0.5930118109698583329 ) ) ;
#28603=CARTESIAN_POINT ( 'NONE',  ( -0.6971942568897648851, 0.07405724077823318263, 0.9104330708123777871 ) ) ;
#28607=CARTESIAN_POINT ( 'NONE',  ( -0.8844078933030434797, -0.1745978227235963076, 1.988329488380941479 ) ) ;
#28609=CARTESIAN_POINT ( 'NONE',  ( 0.6971942568897648851, -0.07405724077823297447, 1.624015747977732849 ) ) ;
#28610=CARTESIAN_POINT ( 'NONE',  ( 1.002407869896990045, -0.1264236179284866091, 1.946358267662771757 ) ) ;
#28612=CARTESIAN_POINT ( 'NONE',  ( 0.7495606340400177148, -0.1264236179284866091, 0.5191929133320630774 ) ) ;
#28618=CARTESIAN_POINT ( 'NONE',  ( 1.002407869896990045, 0.1264236179284866091, 0.6569881889226141247 ) ) ;
#28620=CARTESIAN_POINT ( 'NONE',  ( 1.054774247047244540, -0.07405724077823318263, 0.06397637789899228433 ) ) ;
#28622=CARTESIAN_POINT ( 'NONE',  ( 1.054774247047244540, -0.07405724077823318263, 0.5708661416785200116 ) ) ;
#28624=CARTESIAN_POINT ( 'NONE',  ( -0.8759842519685039353, -0.1574803149606299191, 0.9842519685039370358 ) ) ;
#28625=CARTESIAN_POINT ( 'NONE',  ( -0.8759842519685039353, -0.1787899950787401882, 1.390255905458047447 ) ) ;
#28628=CARTESIAN_POINT ( 'NONE',  ( 0.7495606340400177148, 0.1264236179284866091, 1.144192913332062966 ) ) ;
#28629=CARTESIAN_POINT ( 'NONE',  ( 0.8019270111902717657, 0.1787899950787401604, 1.766732283410803461 ) ) ;
#28630=CARTESIAN_POINT ( 'NONE',  ( -1.033464566929134687, 0.06523048226347956391, 1.350885826771654363 ) ) ;
#28631=CARTESIAN_POINT ( 'NONE',  ( -1.002407869896990045, 0.1264236179284866091, 0.9719488188438739629 ) ) ;
#28633=CARTESIAN_POINT ( 'NONE',  ( -0.9873396505805591694, 0.1113553986120547346, 0.5167322833570401341 ) ) ;
#28634=CARTESIAN_POINT ( 'NONE',  ( -0.7067031875023493948, 0.05524205133751965147, 0.03937007874015842346 ) ) ;
#28635=CARTESIAN_POINT ( 'NONE',  ( 0.9500414927467377701, -0.1787899950787401604, 0.2559055117572600624 ) ) ;
#28636=CARTESIAN_POINT ( 'NONE',  ( -0.6971942568897626646, 0.07405724077823318263, 0.1574803149068664809 ) ) ;
#28637=CARTESIAN_POINT ( 'NONE',  ( -0.6971942568897626646, 0.07405724077823318263, 0.5511811023084406402 ) ) ;
#28638=CARTESIAN_POINT ( 'NONE',  ( 0.7185039370078746268, -0.06523048226347956391, 1.557578740049953225 ) ) ;
#28642=CARTESIAN_POINT ( 'NONE',  ( 1.054774247047244540, 0.07405724077823318263, 0.8169291338045038264 ) ) ;
#28643=CARTESIAN_POINT ( 'NONE',  ( -1.054774247047244540, 0.07405724077823318263, 1.796259842465920853 ) ) ;
#28648=EDGE_LOOP ( 'NONE', ( #16418, #24777, #43626, #28524 ) ) ;
#28651=ORIENTED_EDGE ( 'NONE', *, *, #1954, .F. ) ;
#28655=ADVANCED_FACE ( 'NONE', ( #2458 ), #46073, .T. ) ;
#28659=CARTESIAN_POINT ( 'NONE',  ( -0.7495606340400177148, 0.1264236179284866091, 0.4749015747493858242 ) ) ;
#28661=CARTESIAN_POINT ( 'NONE',  ( 0.8019270111902716547, -0.1787899950787401604, 1.505905511757261062 ) ) ;
#28662=CONICAL_SURFACE ( 'NONE', #7971, 0.1574803149606299191, 1.047197551196598297 ) ;
#28663=CARTESIAN_POINT ( 'NONE',  ( -1.033464566929134687, 0.06523048226347956391, 0.5930118109160945616 ) ) ;
#28664=CARTESIAN_POINT ( 'NONE',  ( 0.9412147342319837628, 0.1574803149606300301, 1.710137795275592065 ) ) ;
#28667=CARTESIAN_POINT ( 'NONE',  ( -0.7185039370078746268, -0.06523048226347956391, 1.094980314960629419 ) ) ;
#28668=CARTESIAN_POINT ( 'NONE',  ( 0.8759842519685039353, -0.1574803149606299191, 0.7775590550105826448 ) ) ;
#28669=CARTESIAN_POINT ( 'NONE',  ( -0.8759842519685039353, -0.1574803149606299191, 1.722440944774362270 ) ) ;
#28670=CARTESIAN_POINT ( 'NONE',  ( 1.054774247047244096, 0.000000000000000000, 0.1008858267178899676 ) ) ;
#28671=CARTESIAN_POINT ( 'NONE',  ( 0.7073262291835020754, -0.03557810427923590452, 0.03937137958850374375 ) ) ;
#28672=CARTESIAN_POINT ( 'NONE',  ( 0.8019270111902716547, 0.1787899950787401604, 1.215551181048599272 ) ) ;
#28673=CARTESIAN_POINT ( 'NONE',  ( 0.7185039370078739607, 1.928577636452523993E-17, 0.2559055117034968463 ) ) ;
#28675=CARTESIAN_POINT ( 'NONE',  ( -0.8107537697050254399, -0.1574803149606297803, 1.916830708553890483 ) ) ;
#28676=CARTESIAN_POINT ( 'NONE',  ( 0.9412147342319837628, -0.1574803149606297803, 0.4650590550105836440 ) ) ;
#28681=CARTESIAN_POINT ( 'NONE',  ( -0.9412147342319837628, 0.1574803149606300301, 0.3617125983176697201 ) ) ;
#28682=VERTEX_POINT ( 'NONE', #24989 ) ;
#28683=CARTESIAN_POINT ( 'NONE',  ( 0.9500414927467378812, 0.1787899950787401604, 1.486220472387181690 ) ) ;
#28684=CARTESIAN_POINT ( 'NONE',  ( -0.9873396505805591694, 0.1113553986120547346, 1.628937007874015963 ) ) ;
#28685=DIRECTION ( 'NONE',  ( -1.000000000000000000, 0.000000000000000000, 0.000000000000000000 ) ) ;
#28690=CARTESIAN_POINT ( 'NONE',  ( 1.033464566929134687, -0.06523048226347956391, 1.296751968396409049 ) ) ;
#28692=CARTESIAN_POINT ( 'NONE',  ( 0.8759842519685039353, 0.1787899950787401882, 0.5880905511273386566 ) ) ;
#28694=CARTESIAN_POINT ( 'NONE',  ( -0.8759842519685039353, 0.1787899950787401882, 1.370570866087968520 ) ) ;
#28696=CARTESIAN_POINT ( 'NONE',  ( -0.9500414927467378812, -0.1787899950787401604, 1.082677165300567346 ) ) ;
#28697=CARTESIAN_POINT ( 'NONE',  ( -0.9873396505805591694, 0.1113553986120547346, 0.1722440944881890035 ) ) ;
#28698=ORIENTED_EDGE ( 'NONE', *, *, #29850, .T. ) ;
#28699=CARTESIAN_POINT ( 'NONE',  ( -0.9500414927467377701, 0.1787899950787401604, 1.131889763725763887 ) ) ;
#28700=CARTESIAN_POINT ( 'NONE',  ( -0.6971942568897637749, 2.189545951927499583E-17, 0.7947834645131652831 ) ) ;
#28701=AXIS2_PLACEMENT_3D ( 'NONE', #33724, #11417, #831 ) ;
#28703=ORIENTED_EDGE ( 'NONE', *, *, #47180, .F. ) ;
#28706=EDGE_LOOP ( 'NONE', ( #36425, #42843, #22718, #31527 ) ) ;
#28712=CARTESIAN_POINT ( 'NONE',  ( -1.054774247047244540, 0.07405724077823318263, 0.5757874015210394658 ) ) ;
#28713=DIRECTION ( 'NONE',  ( 0.000000000000000000, 0.000000000000000000, -1.000000000000000000 ) ) ;
#28714=EDGE_CURVE ( 'NONE', #3668, #21986, #31723, .T. ) ;
#28721=CARTESIAN_POINT ( 'NONE',  ( 0.9412147342319837628, 0.1574803149606300301, 0.6471456692913395425 ) ) ;
#28724=CARTESIAN_POINT ( 'NONE',  ( -0.8759842519685039353, 0.1574803149606299191, 1.427165354223181248 ) ) ;
#28725=CARTESIAN_POINT ( 'NONE',  ( 0.8019270111902717657, -0.1787899950787401604, 0.7627952755367881643 ) ) ;
#28728=CARTESIAN_POINT ( 'NONE',  ( 1.033464566929133799, 0.000000000000000000, 0.1574803148531029595 ) ) ;
#28729=CARTESIAN_POINT ( 'NONE',  ( 0.9873396505805591694, 0.1113553986120547346, 1.235236220472440971 ) ) ;
#28730=CARTESIAN_POINT ( 'NONE',  ( 0.9050986085126093705, -0.1735205885709931173, 1.988692092061036698 ) ) ;
#28731=DIRECTION ( 'NONE',  ( -1.000000000000000000, 0.000000000000000000, 0.000000000000000000 ) ) ;
#28732=CARTESIAN_POINT ( 'NONE',  ( 0.6971942568897648851, -0.07405724077823297447, 0.6742125983714336579 ) ) ;
#28734=CARTESIAN_POINT ( 'NONE',  ( -1.033464566929134687, 0.06523048226347956391, 0.6815944881889761664 ) ) ;
#28738=CARTESIAN_POINT ( 'NONE',  ( 0.9873396505805591694, 0.1113553986120547346, 1.550196850393700920 ) ) ;
#28739=EDGE_LOOP ( 'NONE', ( #5672, #12613, #40204, #36450 ) ) ;
#28740=CARTESIAN_POINT ( 'NONE',  ( -0.7185039370078739607, 1.928577636452523993E-17, 1.171259842519684957 ) ) ;
#28743=CARTESIAN_POINT ( 'NONE',  ( 0.7495606340400177148, 0.1264236179284866091, 0.9817913385289134265 ) ) ;
#28749=CARTESIAN_POINT ( 'NONE',  ( -0.7185039370078739607, 0.000000000000000000, -2.869337061179095023E-17 ) ) ;
#28750=CARTESIAN_POINT ( 'NONE',  ( -1.054774247047244096, 0.000000000000000000, 0.1402559054580474474 ) ) ;
#28751=CARTESIAN_POINT ( 'NONE',  ( -1.033464566929134687, -0.06523048226347956391, 0.8243110235145210130 ) ) ;
#28753=LINE ( 'NONE', #32579, #40176 ) ;
#28754=CARTESIAN_POINT ( 'NONE',  ( -1.002407869896990045, -0.1264236179284866091, 1.473917322780881722 ) ) ;
#28755=CARTESIAN_POINT ( 'NONE',  ( 1.002407869896990045, -0.1264236179284866091, 0.8882874015210394658 ) ) ;
#28756=CARTESIAN_POINT ( 'NONE',  ( -0.8019270111902717657, -0.1787899950787401604, 1.112204724355684959 ) ) ;
#28757=CARTESIAN_POINT ( 'NONE',  ( -1.054774247047244540, 0.07405724077823318263, 0.3838582676627718127 ) ) ;
#28759=CARTESIAN_POINT ( 'NONE',  ( -1.002407869896990045, -0.1264236179284866091, 1.911909448765133801 ) ) ;
#28760=CARTESIAN_POINT ( 'NONE',  ( -0.7185039370078739607, 1.928577636452523993E-17, 1.958661417322834719 ) ) ;
#28761=CARTESIAN_POINT ( 'NONE',  ( -0.7646288533564489232, -0.1113553986120547346, 1.884842519685039353 ) ) ;
#28766=CARTESIAN_POINT ( 'NONE',  ( -0.8759842519685039353, 0.1787899950787401882, 0.1894685038832444879 ) ) ;
#28769=EDGE_CURVE ( 'NONE', #30794, #36569, #32447, .T. ) ;
#28770=CARTESIAN_POINT ( 'NONE',  ( -0.6971942568897648851, -0.07405724077823297447, 1.427165354276944687 ) ) ;
#28773=EDGE_CURVE ( 'NONE', #13621, #16635, #36715, .T. ) ;
#28776=CARTESIAN_POINT ( 'NONE',  ( -0.8107537697050254399, 0.1574803149606300301, 1.547736220364914983 ) ) ;
#28778=CARTESIAN_POINT ( 'NONE',  ( 0.8107537697050253289, 0.1574803149606300301, 0.3764763779527559029 ) ) ;
#28780=CARTESIAN_POINT ( 'NONE',  ( -1.033464566929133799, 0.000000000000000000, 0.9055118109160944506 ) ) ;
#28781=CARTESIAN_POINT ( 'NONE',  ( -0.7185039370078746268, -0.06523048226347956391, 0.7800196850393692483 ) ) ;
#28783=CARTESIAN_POINT ( 'NONE',  ( 0.9412147342319837628, 0.1574803149606300301, 1.857775590443653257 ) ) ;
#28786=CARTESIAN_POINT ( 'NONE',  ( 0.7185039370078746268, -0.06523048226347956391, 0.7800196850393692483 ) ) ;
#28789=CARTESIAN_POINT ( 'NONE',  ( -0.8107537697050254399, -0.1574803149606297803, 0.4699803149606304742 ) ) ;
#28791=CARTESIAN_POINT ( 'NONE',  ( 0.9873396505805591694, 0.1113553986120547346, 0.2411417321759374011 ) ) ;
#28792=AXIS2_PLACEMENT_3D ( 'NONE', #30167, #29930, #403 ) ;
#28795=DIRECTION ( 'NONE',  ( 0.000000000000000000, 0.000000000000000000, -1.000000000000000000 ) ) ;
#28799=CARTESIAN_POINT ( 'NONE',  ( 0.7185039370078746268, 0.06523048226347956391, 0.9227362203649142058 ) ) ;
#28801=CARTESIAN_POINT ( 'NONE',  ( -1.054774247047244540, 0.07405724077823318263, 0.3395669290800945039 ) ) ;
#28802=ORIENTED_EDGE ( 'NONE', *, *, #42032, .T. ) ;
#28804=CARTESIAN_POINT ( 'NONE',  ( -1.002407869896990045, -0.1264236179284866091, 1.596948818843874074 ) ) ;
#28806=CARTESIAN_POINT ( 'NONE',  ( 0.9500414927467378812, 0.1787899950787401604, 1.530511810969859443 ) ) ;
#28810=CARTESIAN_POINT ( 'NONE',  ( -1.054774247047244096, 0.000000000000000000, 0.7750984251430865779 ) ) ;
#28811=CYLINDRICAL_SURFACE ( 'NONE', #39613, 0.1574803149606299191 ) ;
#28812=CARTESIAN_POINT ( 'NONE',  ( 0.8759842519685039353, 0.1787899950787401882, 0.7455708660879684091 ) ) ;
#28813=CARTESIAN_POINT ( 'NONE',  ( -1.054774247047244540, 0.07405724077823318263, 0.7726377952218266287 ) ) ;
#28815=( BOUNDED_CURVE ( )  B_SPLINE_CURVE ( 2, ( #19870, #2352, #5490, #8848, #12940, #6182, #41645, #1650, #1891 ),
 .UNSPECIFIED., .F., .F. ) 
 B_SPLINE_CURVE_WITH_KNOTS ( ( 3, 2, 2, 2, 3 ),
 ( 0.9200000000000000400, 0.9224999999999999867, 0.9250000000000000444, 0.9274999999999999911, 0.9300000000000000488 ),
 .UNSPECIFIED. ) 
 CURVE ( )  GEOMETRIC_REPRESENTATION_ITEM ( )  RATIONAL_B_SPLINE_CURVE ( ( 1.000000000000000000, 0.9238795325112869605, 1.000000000000000000, 0.9238795325112869605, 1.000000000000000000, 0.9238795325112869605, 1.000000000000000000, 0.9238795325112829637, 1.000000000000000000 ) ) 
 REPRESENTATION_ITEM ( '' )  ) ;
#28816=CARTESIAN_POINT ( 'NONE',  ( -0.9873396505805591694, -0.1113553986120547346, 0.8710629921259842590 ) ) ;
#28818=CARTESIAN_POINT ( 'NONE',  ( -1.054774247047244540, 0.07405724077823318263, 1.446850393647023614 ) ) ;
#28819=ORIENTED_EDGE ( 'NONE', *, *, #10584, .F. ) ;
#28820=CARTESIAN_POINT ( 'NONE',  ( -0.9873396505805591694, -0.1113553986120547346, 0.4379921259842519676 ) ) ;
#28821=CARTESIAN_POINT ( 'NONE',  ( 0.8019270111902716547, 0.1787899950787401604, 1.535433070812378675 ) ) ;
#28824=ORIENTED_EDGE ( 'NONE', *, *, #34931, .F. ) ;
#28831=AXIS2_PLACEMENT_3D ( 'NONE', #19753, #42004, #41770 ) ;
#28833=CARTESIAN_POINT ( 'NONE',  ( -0.8107537697050254399, -0.1574803149606297803, 1.139271653543306506 ) ) ;
#28834=( BOUNDED_CURVE ( )  B_SPLINE_CURVE ( 2, ( #4419, #33950, #19050, #26993, #5147, #16430, #26747, #41306, #34400 ),
 .UNSPECIFIED., .F., .T. ) 
 B_SPLINE_CURVE_WITH_KNOTS ( ( 3, 2, 2, 2, 3 ),
 ( 0.4199999999999999845, 0.4224999999999999867, 0.4249999999999999889, 0.4274999999999999911, 0.4299999999999999933 ),
 .UNSPECIFIED. ) 
 CURVE ( )  GEOMETRIC_REPRESENTATION_ITEM ( )  RATIONAL_B_SPLINE_CURVE ( ( 1.000000000000000000, 0.9238795325112869605, 1.000000000000000000, 0.9238795325112869605, 1.000000000000000000, 0.9238795325112869605, 1.000000000000000000, 0.9238795325112869605, 1.000000000000000000 ) ) 
 REPRESENTATION_ITEM ( '' )  ) ;
#28836=CYLINDRICAL_SURFACE ( 'NONE', #31064, 0.1574803149606299191 ) ;
#28837=CARTESIAN_POINT ( 'NONE',  ( 0.8759842519685039353, 0.1787899950787401882, 1.685531496009228469 ) ) ;
#28838=CARTESIAN_POINT ( 'NONE',  ( 1.054774247047244540, 0.07405724077823318263, 0.2608267715997796832 ) ) ;
#28842=CARTESIAN_POINT ( 'NONE',  ( 0.6971942568897626646, 0.07405724077823318263, 0.5511811023084406402 ) ) ;
#28843=CARTESIAN_POINT ( 'NONE',  ( -1.054774247047244540, 0.07405724077823318263, 0.8956692912848198684 ) ) ;
#28844=CARTESIAN_POINT ( 'NONE',  ( -0.8547977949112169904, 0.1745539855089116299, 0.03937007874015845815 ) ) ;
#28847=CARTESIAN_POINT ( 'NONE',  ( 0.8759842519685039353, 0.1787899950787401882, 1.611712598371433103 ) ) ;
#28850=ORIENTED_EDGE ( 'NONE', *, *, #14473, .T. ) ;
#28856=CARTESIAN_POINT ( 'NONE',  ( -1.054774247047244540, 0.07405724077823318263, 0.4232283464029293896 ) ) ;
#28857=CARTESIAN_POINT ( 'NONE',  ( 0.9500414927467378812, 0.1787899950787401604, 0.5807086613635594752 ) ) ;
#28860=CARTESIAN_POINT ( 'NONE',  ( 0.8759842519685039353, -0.1787899950787401882, 0.1353346456155279653 ) ) ;
#28861=CARTESIAN_POINT ( 'NONE',  ( -0.8107537697050254399, -0.1574803149606297803, 0.9325787400499523372 ) ) ;
#28862=CARTESIAN_POINT ( 'NONE',  ( -0.9500414927467378812, -0.1787899950787401604, 1.589566929080094448 ) ) ;
#28864=CARTESIAN_POINT ( 'NONE',  ( -0.9500414927467378812, -0.1787899950787401604, 1.122047244040725644 ) ) ;
#28866=CARTESIAN_POINT ( 'NONE',  ( 0.6971942568897648851, -0.07405724077823297447, 1.190944881836001112 ) ) ;
#28867=CARTESIAN_POINT ( 'NONE',  ( -0.7185039370078739607, 1.928577636452523993E-17, 0.6889763778452283605 ) ) ;
#28868=CARTESIAN_POINT ( 'NONE',  ( 1.033464566929134687, -0.06523048226347956391, 1.503444881889764995 ) ) ;
#28869=CARTESIAN_POINT ( 'NONE',  ( 0.9500414927467378812, 0.1787899950787401604, 1.879921259788756016 ) ) ;
#28870=CARTESIAN_POINT ( 'NONE',  ( -0.8759842519685039353, 0.1574803149606299191, 0.6102362204724409711 ) ) ;
#28871=CARTESIAN_POINT ( 'NONE',  ( -0.9500414927467378812, 0.1787899950787401604, 0.8562992125446617919 ) ) ;
#28873=CARTESIAN_POINT ( 'NONE',  ( 0.7185039370078739607, 0.000000000000000000, 4.498031496062992574 ) ) ;
#28874=CARTESIAN_POINT ( 'NONE',  ( 0.7495606340400177148, -0.1264236179284866091, 0.3272637794737956463 ) ) ;
#28875=CARTESIAN_POINT ( 'NONE',  ( -0.9500414927467377701, -0.1787899950787401604, 0.2116141731745827814 ) ) ;
#28876=CARTESIAN_POINT ( 'NONE',  ( -0.6971942568897626646, -0.07405724077823297447, 0.7529527558517473684 ) ) ;
#28877=CARTESIAN_POINT ( 'NONE',  ( 0.9412147342319837628, -0.1574803149606297803, 1.606791338475149766 ) ) ;
#28880=ORIENTED_EDGE ( 'NONE', *, *, #26538, .T. ) ;
#28881=CARTESIAN_POINT ( 'NONE',  ( 0.8019270111902717657, -0.1787899950787401604, 0.7234251967966300878 ) ) ;
#28882=CARTESIAN_POINT ( 'NONE',  ( 0.6971942568897648851, -0.07405724077823297447, 0.9940944881352130613 ) ) ;
#28883=CARTESIAN_POINT ( 'NONE',  ( -0.9500414927467377701, 0.1787899950787401604, 1.919291338528913649 ) ) ;
#28884=CARTESIAN_POINT ( 'NONE',  ( 0.7495606340400177148, -0.1264236179284866091, 1.936515747977732405 ) ) ;
#28885=ORIENTED_EDGE ( 'NONE', *, *, #911, .T. ) ;
#28888=CARTESIAN_POINT ( 'NONE',  ( 0.9873396505805591694, -0.1113553986120547346, 1.609251968396409493 ) ) ;
#28895=CARTESIAN_POINT ( 'NONE',  ( -0.9873396505805591694, 0.1113553986120547346, 0.9891732282389291697 ) ) ;
#28897=CARTESIAN_POINT ( 'NONE',  ( 0.8759842519685039353, 0.1787899950787401882, 0.07135826766277185429 ) ) ;
#28900=CARTESIAN_POINT ( 'NONE',  ( -1.002407869896990045, 0.1264236179284866091, 0.5437992125446614589 ) ) ;
#28902=CARTESIAN_POINT ( 'NONE',  ( -0.7174213970110099314, -0.05514141941195432883, 1.984310470025690609 ) ) ;
#28904=CARTESIAN_POINT ( 'NONE',  ( 0.6971942568897648851, -0.07405724077823297447, 1.269685039316314601 ) ) ;
#28905=CARTESIAN_POINT ( 'NONE',  ( 0.6971942568897648851, -0.07405724077823297447, 1.579724409395055318 ) ) ;
#28906=CARTESIAN_POINT ( 'NONE',  ( -0.8759842519685039353, 0.000000000000000000, 0.000000000000000000 ) ) ;
#28907=DIRECTION ( 'NONE',  ( 1.822029033848725028E-16, 0.000000000000000000, 1.000000000000000000 ) ) ;
#28908=CARTESIAN_POINT ( 'NONE',  ( -0.8759842519685039353, 0.1574803149606299191, 1.702755905404283565 ) ) ;
#28909=CARTESIAN_POINT ( 'NONE',  ( 1.002407869896990045, -0.1264236179284866091, 0.1353346456155277433 ) ) ;
#28910=CARTESIAN_POINT ( 'NONE',  ( 0.7108038354695511707, 0.06841997037041733232, 0.03937007863263043694 ) ) ;
#28911=CARTESIAN_POINT ( 'NONE',  ( 1.054774247047244540, 0.07405724077823318263, 1.087598425143086578 ) ) ;
#28913=CARTESIAN_POINT ( 'NONE',  ( 0.7185039370078739607, 1.928577636452523993E-17, 1.210629921259842590 ) ) ;
#28914=CARTESIAN_POINT ( 'NONE',  ( -0.8019270111902717657, 0.1787899950787401604, 1.176181102308441417 ) ) ;
#28915=CARTESIAN_POINT ( 'NONE',  ( 0.9873396505805591694, 0.1113553986120547346, 0.4773622046168818911 ) ) ;
#28917=CARTESIAN_POINT ( 'NONE',  ( -0.8107537697050254399, 0.1574803149606300301, 1.124507874015748810 ) ) ;
#28918=CARTESIAN_POINT ( 'NONE',  ( 0.9494468377376082957, 0.1530141113397992803, 0.03936700763878682452 ) ) ;
#28919=CARTESIAN_POINT ( 'NONE',  ( 0.9873396505805591694, 0.1113553986120547346, 0.2903543307086614012 ) ) ;
#28920=CARTESIAN_POINT ( 'NONE',  ( -1.033464566929134687, 0.06523048226347956391, 0.4749015746956221085 ) ) ;
#28922=CARTESIAN_POINT ( 'NONE',  ( 0.8759842519685039353, -0.1787899950787401882, 1.468996062938362046 ) ) ;
#28923=CARTESIAN_POINT ( 'NONE',  ( -0.9873396505805591694, -0.1113553986120547346, 1.146653543307086798 ) ) ;
#28926=CARTESIAN_POINT ( 'NONE',  ( -1.054774247047244096, 0.000000000000000000, 0.06151574797773248782 ) ) ;
#28929=AXIS2_PLACEMENT_3D ( 'NONE', #5721, #35442, #13853 ) ;
#28930=CARTESIAN_POINT ( 'NONE',  ( 1.033464566929133799, 0.000000000000000000, 0.4330708660342047489 ) ) ;
#28935=CARTESIAN_POINT ( 'NONE',  ( 0.6971942568897626646, -0.07405724077823297447, 0.6003937007336389575 ) ) ;
#28937=CARTESIAN_POINT ( 'NONE',  ( -0.6971942568897637749, 2.189545951927499583E-17, 1.498523621993480326 ) ) ;
#28939=CARTESIAN_POINT ( 'NONE',  ( -0.8759842519685039353, 0.1787899950787401882, 1.178641732229700922 ) ) ;
#28940=CARTESIAN_POINT ( 'NONE',  ( -0.9412147342319837628, 0.1574803149606300301, 0.2140748031496061687 ) ) ;
#28941=ORIENTED_EDGE ( 'NONE', *, *, #36131, .F. ) ;
#28942=CARTESIAN_POINT ( 'NONE',  ( -1.054774247047244540, -0.07405724077823318263, 1.043307086560409269 ) ) ;
#28943=CARTESIAN_POINT ( 'NONE',  ( -0.7495606340400177148, 0.1264236179284866091, 0.7898622046706456068 ) ) ;
#28945=CARTESIAN_POINT ( 'NONE',  ( -0.8019270111902717657, -0.1787899950787401604, 0.1722440944344256208 ) ) ;
#28948=ORIENTED_EDGE ( 'NONE', *, *, #40209, .T. ) ;
#28950=LINE ( 'NONE', #15253, #24163 ) ;
#28952=DIRECTION ( 'NONE',  ( 0.000000000000000000, 0.000000000000000000, -1.000000000000000000 ) ) ;
#28953=CARTESIAN_POINT ( 'NONE',  ( -0.7495606340400177148, -0.1264236179284866091, 0.7947834645131652831 ) ) ;
#28954=( BOUNDED_CURVE ( )  B_SPLINE_CURVE ( 2, ( #38923, #46582, #23851, #39384, #31294, #12847, #6085, #9481, #24096 ),
 .UNSPECIFIED., .F., .T. ) 
 B_SPLINE_CURVE_WITH_KNOTS ( ( 3, 2, 2, 2, 3 ),
 ( 0.1900000000000000022, 0.1925000000000000044, 0.1950000000000000067, 0.1975000000000000089, 0.2000000000000000111 ),
 .UNSPECIFIED. ) 
 CURVE ( )  GEOMETRIC_REPRESENTATION_ITEM ( )  RATIONAL_B_SPLINE_CURVE ( ( 1.000000000000000000, 0.9238795325112869605, 1.000000000000000000, 0.9238795325112869605, 1.000000000000000000, 0.9238795325112869605, 1.000000000000000000, 0.9238795325112869605, 1.000000000000000000 ) ) 
 REPRESENTATION_ITEM ( '' )  ) ;
#28956=ORIENTED_EDGE ( 'NONE', *, *, #13752, .T. ) ;
#28958=VECTOR ( 'NONE', #27676, 39.37007874015748143 ) ;
#28959=CARTESIAN_POINT ( 'NONE',  ( -0.8019270111902716547, 0.1787899950787401604, 1.850393700733638624 ) ) ;
#28962=VERTEX_POINT ( 'NONE', #5055 ) ;
#28963=CARTESIAN_POINT ( 'NONE',  ( 0.8107537697050253289, -0.1574803149606297803, 0.6668307086614162493 ) ) ;
#28965=CARTESIAN_POINT ( 'NONE',  ( -0.8759842519685039353, 0.000000000000000000, 0.000000000000000000 ) ) ;
#28966=CARTESIAN_POINT ( 'NONE',  ( -0.9873396505805591694, -0.1113553986120547346, 1.373031495955464587 ) ) ;
#28967=CARTESIAN_POINT ( 'NONE',  ( 0.8759842519685039353, 0.1787899950787401882, 0.7062007873478109987 ) ) ;
#28972=CARTESIAN_POINT ( 'NONE',  ( 0.8107537697050253289, 0.1574803149606300301, 1.281988188976378895 ) ) ;
#28973=CARTESIAN_POINT ( 'NONE',  ( 1.002407869896990045, -0.1264236179284866091, 1.990649606245448844 ) ) ;
#28977=CARTESIAN_POINT ( 'NONE',  ( 1.054774247047244540, -0.07405724077823318263, 0.6496062991588353874 ) ) ;
#28980=CARTESIAN_POINT ( 'NONE',  ( -0.9873396505805591694, -0.1113553986120547346, 0.3887795274515282729 ) ) ;
#28982=CARTESIAN_POINT ( 'NONE',  ( 0.7185039370078746268, -0.06523048226347956391, 0.6126968502861739330 ) ) ;
#28984=CARTESIAN_POINT ( 'NONE',  ( 0.8019270111902717657, -0.1787899950787401604, 0.9547244093950547628 ) ) ;
#28985=ADVANCED_FACE ( 'NONE', ( #18956 ), #30038, .T. ) ;
#28990=CARTESIAN_POINT ( 'NONE',  ( -0.6971942568897637749, 2.189545951927499583E-17, 0.08120078734781142893 ) ) ;
#28992=VERTEX_POINT ( 'NONE', #12752 ) ;
#28993=EDGE_CURVE ( 'NONE', #43250, #18901, #23039, .T. ) ;
#28994=CARTESIAN_POINT ( 'NONE',  ( 1.054774247047244096, 0.000000000000000000, 1.956200787347811110 ) ) ;
#28997=CARTESIAN_POINT ( 'NONE',  ( -1.002407869896990045, 0.1264236179284866091, 1.921751968450173376 ) ) ;
#28998=CARTESIAN_POINT ( 'NONE',  ( -0.7495606340400177148, -0.1264236179284866091, 1.621555118056472455 ) ) ;
#29000=CARTESIAN_POINT ( 'NONE',  ( -0.8759842519685039353, 0.1787899950787401882, 0.3912401574265515491 ) ) ;
#29001=CARTESIAN_POINT ( 'NONE',  ( -1.033464566929134687, -0.06523048226347956391, 1.808562992018457161 ) ) ;
#29002=CARTESIAN_POINT ( 'NONE',  ( -1.054774247047244096, 0.000000000000000000, 1.956200787347811110 ) ) ;
#29003=CARTESIAN_POINT ( 'NONE',  ( -0.7185039370078739607, 1.928577636452523993E-17, 1.486220472440944906 ) ) ;
#29004=CARTESIAN_POINT ( 'NONE',  ( -0.9873396505805591694, -0.1113553986120547346, 1.855314960629921295 ) ) ;
#29009=CARTESIAN_POINT ( 'NONE',  ( 0.7185039370078739607, 0.000000000000000000, 4.498031496062992574 ) ) ;
#29011=CARTESIAN_POINT ( 'NONE',  ( -0.6971942568897626646, -0.07405724077823297447, 0.1624015747493861295 ) ) ;
#29014=CARTESIAN_POINT ( 'NONE',  ( -0.7495606340400177148, 0.1264236179284866091, 1.459153543253322693 ) ) ;
#29019=DIRECTION ( 'NONE',  ( 0.000000000000000000, 0.000000000000000000, -1.000000000000000000 ) ) ;
#29021=CARTESIAN_POINT ( 'NONE',  ( -0.7646288533564489232, 0.1113553986120547346, 0.9990157479239685223 ) ) ;
#29022=CARTESIAN_POINT ( 'NONE',  ( 0.8019270111902717657, -0.1787899950787401604, 0.4084645668753704717 ) ) ;
#29024=CARTESIAN_POINT ( 'NONE',  ( 0.9873396505805591694, 0.1113553986120547346, 1.737204724301921299 ) ) ;
#29026=CARTESIAN_POINT ( 'NONE',  ( 0.7185039370078746268, -0.06523048226347956391, 0.2189960628845991353 ) ) ;
#29027=CARTESIAN_POINT ( 'NONE',  ( 1.033464566929134687, -0.06523048226347956391, 0.7160433070866151217 ) ) ;
#29033=CARTESIAN_POINT ( 'NONE',  ( 0.7185039370078739607, 1.928577636452523993E-17, 0.1377952754830242266 ) ) ;
#29037=CARTESIAN_POINT ( 'NONE',  ( -0.7185039370078739607, 1.928577636452523993E-17, 0.7677165353255432922 ) ) ;
#29040=CARTESIAN_POINT ( 'NONE',  ( -1.033464566929134687, 0.06523048226347956391, 0.08120078729404769935 ) ) ;
#29042=CARTESIAN_POINT ( 'NONE',  ( 0.9412147342319837628, -0.1574803149606297803, 0.9374999998924736788 ) ) ;
#29043=ADVANCED_FACE ( 'NONE', ( #12517 ), #8171, .T. ) ;
#29045=CARTESIAN_POINT ( 'NONE',  ( -0.9500414927467378812, 0.1787899950787401604, 0.4232283464029293896 ) ) ;
#29046=EDGE_LOOP ( 'NONE', ( #1787, #21904, #11222, #32772 ) ) ;
#29048=CARTESIAN_POINT ( 'NONE',  ( -0.7495606340400177148, 0.1264236179284866091, 1.537893700733637736 ) ) ;
#29049=ORIENTED_EDGE ( 'NONE', *, *, #34189, .F. ) ;
#29051=ORIENTED_EDGE ( 'NONE', *, *, #20877, .T. ) ;
#29052=CARTESIAN_POINT ( 'NONE',  ( -0.9500414927467378812, -0.1787899950787401604, 0.8464566928596233275 ) ) ;
#29053=CARTESIAN_POINT ( 'NONE',  ( 1.054774247047244540, -0.07405724077823318263, 0.1820866141194649179 ) ) ;
#29056=CARTESIAN_POINT ( 'NONE',  ( 1.054774247047244096, 0.000000000000000000, 0.6963582676627716461 ) ) ;
#29057=CARTESIAN_POINT ( 'NONE',  ( -0.6971942568897648851, 0.07405724077823318263, 0.7480314960092282472 ) ) ;
#29058=CYLINDRICAL_SURFACE ( 'NONE', #44452, 0.1574803149606299191 ) ;
#29060=CARTESIAN_POINT ( 'NONE',  ( -0.8759842519685039353, 0.000000000000000000, 0.000000000000000000 ) ) ;
#29062=CARTESIAN_POINT ( 'NONE',  ( -0.7185039370078746268, 0.06523048226347956391, 1.946358267609010095 ) ) ;
#29064=CARTESIAN_POINT ( 'NONE',  ( -0.7646288533564489232, -0.1113553986120547346, 0.4281496062992125595 ) ) ;
#29065=CARTESIAN_POINT ( 'NONE',  ( 1.054774247047244096, 0.000000000000000000, 1.523129921206078707 ) ) ;
#29068=ORIENTED_EDGE ( 'NONE', *, *, #9749, .F. ) ;
#29071=ORIENTED_EDGE ( 'NONE', *, *, #1262, .F. ) ;
#29077=CARTESIAN_POINT ( 'NONE',  ( 0.7646288533564489232, 0.1113553986120547346, 1.048228346456692828 ) ) ;
#29079=CARTESIAN_POINT ( 'NONE',  ( 0.7495606340400177148, -0.1264236179284866091, 1.739665354276945131 ) ) ;
#29080=CARTESIAN_POINT ( 'NONE',  ( 0.8759842519685039353, 0.1787899950787401882, 0.3075787401037169411 ) ) ;
#29085=CARTESIAN_POINT ( 'NONE',  ( 1.033464566929133799, 0.000000000000000000, 0.3641732283464567121 ) ) ;
#29086=CARTESIAN_POINT ( 'NONE',  ( 0.8019270111902717657, -0.1787899950787401604, 0.6397637794737947026 ) ) ;
#29087=CARTESIAN_POINT ( 'NONE',  ( -1.054774247047244540, 0.07405724077823318263, 0.9744094487651340231 ) ) ;
#29089=CARTESIAN_POINT ( 'NONE',  ( 0.7185039370078746268, 0.06523048226347956391, 1.001476377845229804 ) ) ;
#29091=CARTESIAN_POINT ( 'NONE',  ( -0.8628785951446895641, -0.1737776015968645615, 1.987962957907532635 ) ) ;
#29093=CARTESIAN_POINT ( 'NONE',  ( 0.6971942568897648851, 0.07405724077823318263, 1.697834645615527771 ) ) ;
#29095=CARTESIAN_POINT ( 'NONE',  ( 0.7185039370078739607, 1.928577636452523993E-17, 0.1377952754830242266 ) ) ;
#29096=ORIENTED_EDGE ( 'NONE', *, *, #39682, .F. ) ;
#29100=CARTESIAN_POINT ( 'NONE',  ( -1.002407869896990045, -0.1264236179284866091, 0.4552165353793071745 ) ) ;
#29101=DIRECTION ( 'NONE',  ( 0.000000000000000000, 0.000000000000000000, -1.000000000000000000 ) ) ;
#29103=CARTESIAN_POINT ( 'NONE',  ( 0.6971942568897626646, 0.07405724077823318263, 0.6299212597887560161 ) ) ;
#29105=CARTESIAN_POINT ( 'NONE',  ( 0.8019270111902717657, -0.1787899950787401604, 0.05413385821395302888 ) ) ;
#29106=( BOUNDED_CURVE ( )  B_SPLINE_CURVE ( 2, ( #35714, #14147, #13658, #28295, #3349, #43110, #2624, #9841, #41976 ),
 .UNSPECIFIED., .F., .T. ) 
 B_SPLINE_CURVE_WITH_KNOTS ( ( 3, 2, 2, 2, 3 ),
 ( 0.6199999999999999956, 0.6225000000000000533, 0.6250000000000000000, 0.6274999999999999467, 0.6300000000000000044 ),
 .UNSPECIFIED. ) 
 CURVE ( )  GEOMETRIC_REPRESENTATION_ITEM ( )  RATIONAL_B_SPLINE_CURVE ( ( 1.000000000000000000, 0.9238795325112869605, 1.000000000000000000, 0.9238795325112869605, 1.000000000000000000, 0.9238795325112869605, 1.000000000000000000, 0.9238795325112869605, 1.000000000000000000 ) ) 
 REPRESENTATION_ITEM ( '' )  ) ;
#29109=CARTESIAN_POINT ( 'NONE',  ( -0.7495606340400177148, 0.1264236179284866091, 1.572342519631275692 ) ) ;
#29111=CARTESIAN_POINT ( 'NONE',  ( -0.6971942568897637749, 2.189545951927499583E-17, 1.149114173174582643 ) ) ;
#29113=CARTESIAN_POINT ( 'NONE',  ( 0.8759842519685039353, -0.1787899950787401882, 1.198326771599779628 ) ) ;
#29114=CARTESIAN_POINT ( 'NONE',  ( 0.8759842519685039353, -0.1787899950787401882, 1.783956692859621995 ) ) ;
#29115=CARTESIAN_POINT ( 'NONE',  ( -0.7185039370078746268, -0.06523048226347956391, 0.5437992125984247860 ) ) ;
#29116=CARTESIAN_POINT ( 'NONE',  ( -0.8759842519685039353, -0.1787899950787401882, 0.8784448818360000022 ) ) ;
#29120=CARTESIAN_POINT ( 'NONE',  ( 0.6971942568897626646, -0.07405724077823297447, 0.3248031495525359746 ) ) ;
#29121=CARTESIAN_POINT ( 'NONE',  ( -0.8019270111902716547, -0.1787899950787401604, 0.2460629920722207653 ) ) ;
#29122=CARTESIAN_POINT ( 'NONE',  ( -0.7495606340400177148, -0.1264236179284866091, 0.6766732282926929409 ) ) ;
#29123=CARTESIAN_POINT ( 'NONE',  ( 0.7185039370078746268, 0.06523048226347956391, 1.552657480207433993 ) ) ;
#29126=CARTESIAN_POINT ( 'NONE',  ( 0.8759842519685039353, 0.1787899950787401882, 0.8636811023084409733 ) ) ;
#29127=CARTESIAN_POINT ( 'NONE',  ( 0.6971942568897637749, 2.189545951927499583E-17, 1.109744094434425232 ) ) ;
#29128=CARTESIAN_POINT ( 'NONE',  ( -0.8019270111902716547, -0.1787899950787401604, 1.781496062938362934 ) ) ;
#29129=CARTESIAN_POINT ( 'NONE',  ( 0.7495606340400177148, -0.1264236179284866091, 1.975885826717889815 ) ) ;
#29130=( BOUNDED_CURVE ( )  B_SPLINE_CURVE ( 2, ( #18906, #32199, #28370, #7646, #28624, #25881, #46785, #22263, #40928 ),
 .UNSPECIFIED., .F., .T. ) 
 B_SPLINE_CURVE_WITH_KNOTS ( ( 3, 2, 2, 2, 3 ),
 ( 0.4899999999999999911, 0.4924999999999999933, 0.4949999999999999956, 0.4974999999999999978, 0.5000000000000000000 ),
 .UNSPECIFIED. ) 
 CURVE ( )  GEOMETRIC_REPRESENTATION_ITEM ( )  RATIONAL_B_SPLINE_CURVE ( ( 1.000000000000000000, 0.9238795325112869605, 1.000000000000000000, 0.9238795325112869605, 1.000000000000000000, 0.9238795325112869605, 1.000000000000000000, 0.9238795325112869605, 1.000000000000000000 ) ) 
 REPRESENTATION_ITEM ( '' )  ) ;
#29132=CYLINDRICAL_SURFACE ( 'NONE', #6803, 0.1574803149606299191 ) ;
#29137=ORIENTED_EDGE ( 'NONE', *, *, #9538, .F. ) ;
#29138=CARTESIAN_POINT ( 'NONE',  ( 0.8019270111902717657, -0.1787899950787401604, 1.151574803095843036 ) ) ;
#29139=CARTESIAN_POINT ( 'NONE',  ( -1.033464566929133799, 0.000000000000000000, 1.456692913278299084 ) ) ;
#29142=CARTESIAN_POINT ( 'NONE',  ( 0.8019270111902717657, 0.1787899950787401604, 1.491141732229701367 ) ) ;
#29143=CARTESIAN_POINT ( 'NONE',  ( 1.054774247047244540, 0.07405724077823318263, 0.06397637789899228433 ) ) ;
#29146=CARTESIAN_POINT ( 'NONE',  ( -1.002407869896990045, 0.1264236179284866091, 0.4650590550643464716 ) ) ;
#29149=CARTESIAN_POINT ( 'NONE',  ( -0.7117020095487714970, -0.02979564497706602491, 1.983816935281811578 ) ) ;
#29150=CARTESIAN_POINT ( 'NONE',  ( -1.033464566929134687, 0.06523048226347956391, 1.193405511811024278 ) ) ;
#29151=CARTESIAN_POINT ( 'NONE',  ( -0.8107537697050253289, -0.1574803149606297803, 1.601870078632630756 ) ) ;
#29152=CARTESIAN_POINT ( 'NONE',  ( 0.6971942568897637749, 2.189545951927499583E-17, 1.267224409395055096 ) ) ;
#29153=CARTESIAN_POINT ( 'NONE',  ( 0.8759842519685039353, 0.1787899950787401882, 1.646161417269070837 ) ) ;
#29158=CARTESIAN_POINT ( 'NONE',  ( -0.9412147342319837628, -0.1574803149606297803, 1.724901574695621553 ) ) ;
#29159=CARTESIAN_POINT ( 'NONE',  ( 0.8019270111902717657, 0.1787899950787401604, 0.1919291338045042428 ) ) ;
#29160=CARTESIAN_POINT ( 'NONE',  ( 0.7063448026206018415, -0.03181611069741603626, 0.03937227967794548061 ) ) ;
#29161=EDGE_CURVE ( 'NONE', #14401, #29926, #15867, .T. ) ;
#29164=CARTESIAN_POINT ( 'NONE',  ( 0.8759842519685039353, -0.1574803149606299191, 1.220472440944881942 ) ) ;
#29165=CARTESIAN_POINT ( 'NONE',  ( -1.002407869896990045, -0.1264236179284866091, 1.237696850339937038 ) ) ;
#29166=CARTESIAN_POINT ( 'NONE',  ( 1.033464566929134687, 0.06523048226347956391, 0.5536417321759372623 ) ) ;
#29169=CARTESIAN_POINT ( 'NONE',  ( 0.9008793413134227324, 0.1712306536401314860, 0.03937060926507291586 ) ) ;
#29170=CARTESIAN_POINT ( 'NONE',  ( 1.033464566929133799, 0.000000000000000000, 0.2854330708661417804 ) ) ;
#29174=CARTESIAN_POINT ( 'NONE',  ( -1.033464566929134687, -0.06523048226347956391, 0.4306102361129448552 ) ) ;
#29177=CARTESIAN_POINT ( 'NONE',  ( 0.6971942568897648851, 0.07405724077823318263, 1.496062992072220821 ) ) ;
#29178=CARTESIAN_POINT ( 'NONE',  ( -0.8107537697050253289, -0.1574803149606297803, 1.139271653543306506 ) ) ;
#29180=CARTESIAN_POINT ( 'NONE',  ( -1.033464566929133799, 0.000000000000000000, 1.781496062992125928 ) ) ;
#29181=CARTESIAN_POINT ( 'NONE',  ( -0.9412147342319837628, -0.1574803149606297803, 1.380413385826771533 ) ) ;
#29182=CARTESIAN_POINT ( 'NONE',  ( 0.8759842519685039353, -0.1574803149606299191, 1.181102362204724310 ) ) ;
#29183=CARTESIAN_POINT ( 'NONE',  ( -1.002407869896990045, -0.1264236179284866091, 0.05659448813521283234 ) ) ;
#29187=CYLINDRICAL_SURFACE ( 'NONE', #39789, 0.1574803149606299191 ) ;
#29190=ORIENTED_EDGE ( 'NONE', *, *, #40334, .F. ) ;
#29191=CARTESIAN_POINT ( 'NONE',  ( 0.7495606340400177148, 0.1264236179284866091, 0.5930118109698583329 ) ) ;
#29192=ORIENTED_EDGE ( 'NONE', *, *, #19908, .F. ) ;
#29194=CARTESIAN_POINT ( 'NONE',  ( -1.002407869896990045, -0.1264236179284866091, 1.085137795221826629 ) ) ;
#29196=CARTESIAN_POINT ( 'NONE',  ( -0.9500414927467377701, 0.1787899950787401604, 1.092519684985606032 ) ) ;
#29197=CARTESIAN_POINT ( 'NONE',  ( -1.054774247047244540, 0.07405724077823318263, 0.8562992125446617919 ) ) ;
#29198=CARTESIAN_POINT ( 'NONE',  ( -0.9500414927467378812, -0.1787899950787401604, 0.2165354330171024577 ) ) ;
#29199=CARTESIAN_POINT ( 'NONE',  ( -1.033464566929133799, 0.000000000000000000, 0.3641732283464567121 ) ) ;
#29202=ORIENTED_EDGE ( 'NONE', *, *, #8004, .F. ) ;
#29203=CARTESIAN_POINT ( 'NONE',  ( -0.9873396505805591694, 0.1113553986120547346, 0.05413385826771653642 ) ) ;
#29204=CARTESIAN_POINT ( 'NONE',  ( 0.7646288533564489232, -0.1113553986120547346, 1.058070866141732402 ) ) ;
#29206=CYLINDRICAL_SURFACE ( 'NONE', #34813, 0.1574803149606299191 ) ;
#29208=CARTESIAN_POINT ( 'NONE',  ( -0.8759842519685039353, -0.1787899950787401882, 0.7209645668753701386 ) ) ;
#29209=CARTESIAN_POINT ( 'NONE',  ( -1.033464566929134687, -0.06523048226347956391, 0.5880905510735752184 ) ) ;
#29211=ORIENTED_EDGE ( 'NONE', *, *, #31296, .F. ) ;
#29212=CARTESIAN_POINT ( 'NONE',  ( -0.6971942568897648851, 0.07405724077823318263, 1.815944881835999780 ) ) ;
#29215=CARTESIAN_POINT ( 'NONE',  ( -0.8019270111902716547, -0.1787899950787401604, 0.05413385821395302888 ) ) ;
#29216=CARTESIAN_POINT ( 'NONE',  ( 0.8759842519685039353, -0.1574803149606299191, 0.7086614173228346081 ) ) ;
#29219=CARTESIAN_POINT ( 'NONE',  ( -0.7185039370078739607, 1.928577636452523993E-17, 1.358267716427907779 ) ) ;
#29222=CARTESIAN_POINT ( 'NONE',  ( 0.7495606340400177148, 0.1264236179284866091, 0.8292322834108031282 ) ) ;
#29223=CYLINDRICAL_SURFACE ( 'NONE', #6975, 0.1787899950787401049 ) ;
#29225=CARTESIAN_POINT ( 'NONE',  ( 0.9412147342319837628, -0.1574803149606297803, 1.459153543307085688 ) ) ;
#29227=CARTESIAN_POINT ( 'NONE',  ( 0.7647590343208214847, -0.1296210501886547739, 1.985957554512493006 ) ) ;
#29232=CARTESIAN_POINT ( 'NONE',  ( 0.9500414927467377701, 0.1787899950787401604, 0.7381889763241898939 ) ) ;
#29234=ORIENTED_EDGE ( 'NONE', *, *, #10299, .F. ) ;
#29235=CARTESIAN_POINT ( 'NONE',  ( 0.9873396505805591694, -0.1113553986120547346, 0.6249999998924724576 ) ) ;
#29236=CARTESIAN_POINT ( 'NONE',  ( -0.7185039370078739607, 0.000000000000000000, -2.869337061179095023E-17 ) ) ;
#29237=CARTESIAN_POINT ( 'NONE',  ( 0.8759842519685039353, 0.1787899950787401882, 1.055610236166708793 ) ) ;
#29244=VERTEX_POINT ( 'NONE', #8894 ) ;
#29245=CARTESIAN_POINT ( 'NONE',  ( -0.9500414927467378812, -0.1787899950787401604, 0.05413385821395302888 ) ) ;
#29248=CARTESIAN_POINT ( 'NONE',  ( -0.7646288533564489232, -0.1113553986120547346, 1.845472440944881942 ) ) ;
#29251=CARTESIAN_POINT ( 'NONE',  ( -0.7495606340400177148, 0.1264236179284866091, 1.651082677111590513 ) ) ;
#29252=CARTESIAN_POINT ( 'NONE',  ( -0.9500414927467377701, 0.1787899950787401604, 0.8169291338045038264 ) ) ;
#29253=CARTESIAN_POINT ( 'NONE',  ( -0.9500414927467378812, 0.1787899950787401604, 0.3494094487651343006 ) ) ;
#29254=( BOUNDED_CURVE ( )  B_SPLINE_CURVE ( 2, ( #14899, #29560, #3, #28833, #7449, #29326, #28586, #24725, #14423 ),
 .UNSPECIFIED., .F., .F. ) 
 B_SPLINE_CURVE_WITH_KNOTS ( ( 3, 2, 2, 2, 3 ),
 ( 0.5699999999999999512, 0.5725000000000000089, 0.5749999999999999556, 0.5775000000000000133, 0.5799999999999999600 ),
 .UNSPECIFIED. ) 
 CURVE ( )  GEOMETRIC_REPRESENTATION_ITEM ( )  RATIONAL_B_SPLINE_CURVE ( ( 1.000000000000000000, 0.9238795325112899581, 1.000000000000000000, 0.9238795325112869605, 1.000000000000000000, 0.9238795325112869605, 1.000000000000000000, 0.9238795325112869605, 1.000000000000000000 ) ) 
 REPRESENTATION_ITEM ( '' )  ) ;
#29255=CARTESIAN_POINT ( 'NONE',  ( -0.9412147342319837628, -0.1574803149606297803, 1.803641732175937706 ) ) ;
#29256=CARTESIAN_POINT ( 'NONE',  ( 0.8107537697050254399, 0.1574803149606300301, 0.4060039369003470289 ) ) ;
#29264=CARTESIAN_POINT ( 'NONE',  ( -0.7495606340400177148, 0.1264236179284866091, 0.3518700786863940833 ) ) ;
#29265=ORIENTED_EDGE ( 'NONE', *, *, #47180, .T. ) ;
#29267=CARTESIAN_POINT ( 'NONE',  ( -0.7495606340400177148, -0.1264236179284866091, 1.350885826717889815 ) ) ;
#29268=ORIENTED_EDGE ( 'NONE', *, *, #17171, .T. ) ;
#29269=ADVANCED_FACE ( 'NONE', ( #23525 ), #19909, .T. ) ;
#29273=EDGE_CURVE ( 'NONE', #38634, #31350, #17434, .T. ) ;
#29274=CARTESIAN_POINT ( 'NONE',  ( 0.8019270111902717657, 0.1787899950787401604, 0.3937007873478115538 ) ) ;
#29278=CARTESIAN_POINT ( 'NONE',  ( 0.7646288533564489232, -0.1113553986120547346, 1.756889763671999782 ) ) ;
#29281=CARTESIAN_POINT ( 'NONE',  ( 0.9412147342319837628, -0.1574803149606297803, 0.2288385825696384601 ) ) ;
#29282=CARTESIAN_POINT ( 'NONE',  ( 1.033464566929133799, 0.000000000000000000, 0.7185039370078739607 ) ) ;
#29284=DIRECTION ( 'NONE',  ( -0.8660254037844389297, 0.000000000000000000, -0.4999999999999994449 ) ) ;
#29286=CARTESIAN_POINT ( 'NONE',  ( 0.7185039370078746268, -0.06523048226347956391, 0.7800196850393691372 ) ) ;
#29288=ORIENTED_EDGE ( 'NONE', *, *, #3420, .T. ) ;
#29293=CARTESIAN_POINT ( 'NONE',  ( -0.8759842519685039353, 0.1574803149606299191, 0.1279527557979848462 ) ) ;
#29295=CARTESIAN_POINT ( 'NONE',  ( 0.8107537697050253289, -0.1574803149606297803, 0.9719488187901104137 ) ) ;
#29296=CARTESIAN_POINT ( 'NONE',  ( 0.9873396505805591694, 0.1113553986120547346, 0.5265748031496062520 ) ) ;
#29297=CARTESIAN_POINT ( 'NONE',  ( -0.7495606340400177148, 0.1264236179284866091, 0.3912401574265515491 ) ) ;
#29300=CARTESIAN_POINT ( 'NONE',  ( -1.054774247047244540, -0.07405724077823318263, 1.678149606245448622 ) ) ;
#29302=CARTESIAN_POINT ( 'NONE',  ( 0.8019270111902717657, 0.1787899950787401604, 1.692913385773008539 ) ) ;
#29303=CARTESIAN_POINT ( 'NONE',  ( -1.054774247047244096, 0.000000000000000000, 0.8538385826234016207 ) ) ;
#29304=CARTESIAN_POINT ( 'NONE',  ( 1.002407869896990045, 0.1264236179284866091, 0.3075787401037169411 ) ) ;
#29305=CARTESIAN_POINT ( 'NONE',  ( -0.7185039370078739607, 1.928577636452523993E-17, 0.4527559054042842868 ) ) ;
#29306=CARTESIAN_POINT ( 'NONE',  ( 0.7495606340400177148, -0.1264236179284866091, 0.7603346456155274380 ) ) ;
#29307=CARTESIAN_POINT ( 'NONE',  ( -1.054774247047244096, 0.000000000000000000, 0.7308070865604093802 ) ) ;
#29310=VECTOR ( 'NONE', #40459, 39.37007874015748143 ) ;
#29311=DIRECTION ( 'NONE',  ( 1.000000000000000000, 0.000000000000000000, -1.822029033848725275E-16 ) ) ;
#29312=CARTESIAN_POINT ( 'NONE',  ( -0.9500414927467378812, 0.1787899950787401604, 1.569881889710015299 ) ) ;
#29313=CARTESIAN_POINT ( 'NONE',  ( -0.7646288533564489232, -0.1113553986120547346, 1.835629921152314825 ) ) ;
#29315=CARTESIAN_POINT ( 'NONE',  ( -0.7185039370078739607, 1.928577636452523993E-17, 1.525590551181102317 ) ) ;
#29317=CARTESIAN_POINT ( 'NONE',  ( 1.054774247047244540, -0.07405724077823318263, 1.402559055064346749 ) ) ;
#29319=DIRECTION ( 'NONE',  ( 1.000000000000000000, 0.000000000000000000, -1.822029033848725275E-16 ) ) ;
#29323=EDGE_LOOP ( 'NONE', ( #29211, #40004, #43846, #21744, #20594, #39082, #40842, #11178, #29268, #4728, #31035, #46151, #14948, #39443, #41269, #41187, #28850, #35157, #27339, #4905, #43933, #32284, #28506, #43276, #45548, #35346, #11884, #25776, #45726, #311, #30750, #35838, #38378, #10518, #32262, #44371, #26966, #29556, #14885, #1852, #38662, #46417, #38276, #13179, #33892, #37326, #31498, #1992, #32650, #5012, #22963, #115, #25263, #566, #22640, #41075, #37957, #38914, #166, #9052, #41166, #17407, #31061, #11035, #18210, #20614, #16067, #15738, #5120, #4061, #40795, #16744, #6394, #39355, #39503, #20451, #10956, #37993, #7417, #9116, #10862, #7427, #10329, #43094, #9263, #17296, #24515, #22592, #13473, #34405, #44844, #27686, #38830, #1960, #38727, #17954, #42796, #6836, #32359, #7212, #3246, #9514 ) ) ;
#29325=EDGE_CURVE ( 'NONE', #43175, #3655, #47111, .T. ) ;
#29326=CARTESIAN_POINT ( 'NONE',  ( -0.9412147342319837628, -0.1574803149606297803, 1.144192913385827737 ) ) ;
#29327=ADVANCED_FACE ( 'NONE', ( #46717 ), #13216, .T. ) ;
#29331=CARTESIAN_POINT ( 'NONE',  ( 0.6971942568897648851, 0.07405724077823318263, 1.771653543253322249 ) ) ;
#29332=CARTESIAN_POINT ( 'NONE',  ( 1.054774247047244540, -0.07405724077823318263, 0.2952755904974176393 ) ) ;
#29333=CARTESIAN_POINT ( 'NONE',  ( 0.7185039370078739607, 1.928577636452523993E-17, 0.3051181102362204856 ) ) ;
#29335=ADVANCED_FACE ( 'NONE', ( #31194 ), #41924, .T. ) ;
#29341=CARTESIAN_POINT ( 'NONE',  ( 0.9500414927467378812, -0.1787899950787401604, 0.5659448818360001132 ) ) ;
#29343=DIRECTION ( 'NONE',  ( -1.000000000000000000, 0.000000000000000000, 0.000000000000000000 ) ) ;
#29344=CARTESIAN_POINT ( 'NONE',  ( -0.8759842519685039353, 0.000000000000000000, 2.007874015640504162 ) ) ;
#29345=CARTESIAN_POINT ( 'NONE',  ( 0.7185039370078739607, 1.928577636452523993E-17, 1.683070866141732402 ) ) ;
#29346=CARTESIAN_POINT ( 'NONE',  ( 1.002407869896990045, 0.1264236179284866091, 1.646161417269070837 ) ) ;
#29352=CARTESIAN_POINT ( 'NONE',  ( 0.7185039370078739607, 1.928577636452523993E-17, 1.830708661309795149 ) ) ;
#29355=CARTESIAN_POINT ( 'NONE',  ( 0.8107537697050254399, 0.1574803149606300301, 0.4847440943806614055 ) ) ;
#29357=DIRECTION ( 'NONE',  ( 0.000000000000000000, 0.000000000000000000, -1.000000000000000000 ) ) ;
#29358=CARTESIAN_POINT ( 'NONE',  ( 1.033464566929133799, 0.000000000000000000, 0.04921259842519685318 ) ) ;
#29359=CARTESIAN_POINT ( 'NONE',  ( -0.8759842519685039353, -0.1787899950787401882, 1.665846456639149764 ) ) ;
#29362=CARTESIAN_POINT ( 'NONE',  ( -0.9500414927467378812, 0.1787899950787401604, 1.136811023568283119 ) ) ;
#29363=DIRECTION ( 'NONE',  ( 1.000000000000000000, 0.000000000000000000, -1.822029033848725275E-16 ) ) ;
#29364=CARTESIAN_POINT ( 'NONE',  ( 0.6971942568897648851, 0.07405724077823318263, 1.186023621993481658 ) ) ;
#29366=CARTESIAN_POINT ( 'NONE',  ( 0.7495606340400177148, -0.1264236179284866091, 1.975885826717889815 ) ) ;
#29367=CARTESIAN_POINT ( 'NONE',  ( -1.033464566929134687, 0.06523048226347956391, 0.6422244094488182009 ) ) ;
#29368=CARTESIAN_POINT ( 'NONE',  ( -1.054774247047244540, 0.07405724077823318263, 1.008858267662772423 ) ) ;
#29371=CARTESIAN_POINT ( 'NONE',  ( 0.6971942568897626646, -0.07405724077823297447, 0.2854330708123783977 ) ) ;
#29372=CARTESIAN_POINT ( 'NONE',  ( -1.054774247047244540, -0.07405724077823318263, 0.1771653542769450751 ) ) ;
#29374=CARTESIAN_POINT ( 'NONE',  ( -0.7495606340400177148, -0.1264236179284866091, 0.7554133857730077617 ) ) ;
#29377=CARTESIAN_POINT ( 'NONE',  ( 0.9500414927467378812, -0.1787899950787401604, 0.7283464566391493200 ) ) ;
#29378=CARTESIAN_POINT ( 'NONE',  ( 0.8019270111902716547, 0.1787899950787401604, 1.023622047190330342 ) ) ;
#29379=CARTESIAN_POINT ( 'NONE',  ( -1.054774247047244540, 0.07405724077823318263, 1.874999999946236784 ) ) ;
#29380=VERTEX_POINT ( 'NONE', #42635 ) ;
#29382=CARTESIAN_POINT ( 'NONE',  ( 1.033464566929134687, -0.06523048226347956391, 1.611712598317669221 ) ) ;
#29386=ORIENTED_EDGE ( 'NONE', *, *, #41029, .T. ) ;
#29387=CARTESIAN_POINT ( 'NONE',  ( 1.054774247047244540, -0.07405724077823318263, 1.240157480261197431 ) ) ;
#29391=EDGE_CURVE ( 'NONE', #9619, #29926, #37301, .T. ) ;
#29392=CARTESIAN_POINT ( 'NONE',  ( 0.7185039370078739607, 1.928577636452523993E-17, 1.958661417322834719 ) ) ;
#29396=( BOUNDED_CURVE ( )  B_SPLINE_CURVE ( 2, ( #30334, #25541, #15455, #44177, #22863, #26479, #18553, #40110, #29865 ),
 .UNSPECIFIED., .F., .F. ) 
 B_SPLINE_CURVE_WITH_KNOTS ( ( 3, 2, 2, 2, 3 ),
 ( 0.5100000000000000089, 0.5124999999999999556, 0.5150000000000000133, 0.5174999999999999600, 0.5200000000000000178 ),
 .UNSPECIFIED. ) 
 CURVE ( )  GEOMETRIC_REPRESENTATION_ITEM ( )  RATIONAL_B_SPLINE_CURVE ( ( 1.000000000000000000, 0.9238795325112869605, 1.000000000000000000, 0.9238795325112869605, 1.000000000000000000, 0.9238795325112869605, 1.000000000000000000, 0.9238795325112869605, 1.000000000000000000 ) ) 
 REPRESENTATION_ITEM ( '' )  ) ;
#29397=CARTESIAN_POINT ( 'NONE',  ( -0.8019270111902716547, -0.1787899950787401604, 0.5659448818360001132 ) ) ;
#29401=CARTESIAN_POINT ( 'NONE',  ( 0.6971942568897648851, -0.07405724077823297447, 1.230314960576156746 ) ) ;
#29402=CARTESIAN_POINT ( 'NONE',  ( 0.7495606340400177148, -0.1264236179284866091, 1.621555118056472455 ) ) ;
#29406=DIRECTION ( 'NONE',  ( 1.000000000000000000, 0.000000000000000000, -1.822029033848725275E-16 ) ) ;
#29407=FACE_OUTER_BOUND ( 'NONE', #29497, .T. ) ;
#29408=CARTESIAN_POINT ( 'NONE',  ( -1.033464566929133799, 1.928577636452524610E-17, 2.869337061179095023E-17 ) ) ;
#29409=CARTESIAN_POINT ( 'NONE',  ( 1.054774247047244540, -0.07405724077823318263, 0.2559055117572600624 ) ) ;
#29410=CARTESIAN_POINT ( 'NONE',  ( 0.7027234418073040612, -0.01298421436181104380, 0.03936972784119035368 ) ) ;
#29411=CARTESIAN_POINT ( 'NONE',  ( 1.002407869896990045, -0.1264236179284866091, 1.277066929080094448 ) ) ;
#29413=CARTESIAN_POINT ( 'NONE',  ( -0.7646288533564489232, -0.1113553986120547346, 1.914370078632629868 ) ) ;
#29415=CARTESIAN_POINT ( 'NONE',  ( 0.7646288533564489232, 0.1113553986120547346, 0.7234251967428662056 ) ) ;
#29418=CARTESIAN_POINT ( 'NONE',  ( 0.9316794993730774799, 0.1616194352551858504, 0.03936999175310366972 ) ) ;
#29420=CARTESIAN_POINT ( 'NONE',  ( -0.9873396505805591694, 0.1113553986120547346, 1.107283464459401623 ) ) ;
#29421=CARTESIAN_POINT ( 'NONE',  ( 0.8759842519685039353, 0.1787899950787401882, 1.488681102308440751 ) ) ;
#29422=CARTESIAN_POINT ( 'NONE',  ( -0.7646288533564489232, 0.1113553986120547346, 1.835629921259842590 ) ) ;
#29424=CARTESIAN_POINT ( 'NONE',  ( -0.8019270111902716547, 0.1787899950787401604, 0.07381889758403178958 ) ) ;
#29428=( BOUNDED_CURVE ( )  B_SPLINE_CURVE ( 2, ( #7385, #44023, #8078, #22218, #15534, #33043, #170, #22456, #21994 ),
 .UNSPECIFIED., .F., .T. ) 
 B_SPLINE_CURVE_WITH_KNOTS ( ( 3, 2, 2, 2, 3 ),
 ( 0.3499999999999999778, 0.3524999999999999800, 0.3549999999999999822, 0.3574999999999999845, 0.3599999999999999867 ),
 .UNSPECIFIED. ) 
 CURVE ( )  GEOMETRIC_REPRESENTATION_ITEM ( )  RATIONAL_B_SPLINE_CURVE ( ( 1.000000000000000000, 0.9238795325112879597, 1.000000000000000000, 0.9238795325112869605, 1.000000000000000000, 0.9238795325112869605, 1.000000000000000000, 0.9238795325112869605, 1.000000000000000000 ) ) 
 REPRESENTATION_ITEM ( '' )  ) ;
#29431=CARTESIAN_POINT ( 'NONE',  ( 0.7495606340400177148, -0.1264236179284866091, 0.5241141731745827537 ) ) ;
#29432=ORIENTED_EDGE ( 'NONE', *, *, #29325, .F. ) ;
#29433=CARTESIAN_POINT ( 'NONE',  ( -1.054774247047244540, -0.07405724077823318263, 1.437007873961985593 ) ) ;
#29435=CARTESIAN_POINT ( 'NONE',  ( -1.054774247047244540, -0.07405724077823318263, 1.166338582623402509 ) ) ;
#29437=CARTESIAN_POINT ( 'NONE',  ( 0.9412147342319837628, 0.1574803149606300301, 1.306594488081449290 ) ) ;
#29438=CARTESIAN_POINT ( 'NONE',  ( -1.033464566929133799, 1.928577636452524610E-17, 2.869337061179095023E-17 ) ) ;
#29440=EDGE_LOOP ( 'NONE', ( #33247, #10575, #24014, #14783 ) ) ;
#29441=CARTESIAN_POINT ( 'NONE',  ( 0.9412147342319837628, -0.1574803149606297803, 1.065452755905511806 ) ) ;
#29444=CARTESIAN_POINT ( 'NONE',  ( -1.033464566929134687, 0.06523048226347956391, 0.5536417321759372623 ) ) ;
#29445=CARTESIAN_POINT ( 'NONE',  ( -1.002407869896990045, 0.1264236179284866091, 0.7357283464029290565 ) ) ;
#29448=CARTESIAN_POINT ( 'NONE',  ( -0.9500414927467377701, -0.1787899950787401604, 1.870078740103715331 ) ) ;
#29449=EDGE_CURVE ( 'NONE', #22273, #40732, #15645, .T. ) ;
#29451=CARTESIAN_POINT ( 'NONE',  ( 0.7185039370078739607, 1.928577636452523993E-17, 0.6594488188976378451 ) ) ;
#29453=CARTESIAN_POINT ( 'NONE',  ( -0.9412147342319837628, 0.1574803149606300301, 0.4010826770578274081 ) ) ;
#29454=CARTESIAN_POINT ( 'NONE',  ( -0.8107537697050253289, 0.1574803149606300301, 1.547736220364914983 ) ) ;
#29456=CARTESIAN_POINT ( 'NONE',  ( 0.7495606340400177148, -0.1264236179284866091, 0.7603346456155274380 ) ) ;
#29457=CARTESIAN_POINT ( 'NONE',  ( 1.002407869896990045, 0.1264236179284866091, 1.326279527505291433 ) ) ;
#29459=CARTESIAN_POINT ( 'NONE',  ( 0.7646288533564489232, -0.1113553986120547346, 1.373031496062992352 ) ) ;
#29460=CARTESIAN_POINT ( 'NONE',  ( 0.9893677384800499963, -0.1382549923011644755, 1.990360131067286487 ) ) ;
#29464=CARTESIAN_POINT ( 'NONE',  ( 1.054774247047244540, -0.07405724077823318263, 0.7677165353793073965 ) ) ;
#29467=ORIENTED_EDGE ( 'NONE', *, *, #23390, .F. ) ;
#29470=CARTESIAN_POINT ( 'NONE',  ( 1.054774247047244540, -0.07405724077823318263, 0.9251968503399374821 ) ) ;
#29471=CARTESIAN_POINT ( 'NONE',  ( 0.7185039370078739607, 1.928577636452523993E-17, 1.643700787401574992 ) ) ;
#29478=CARTESIAN_POINT ( 'NONE',  ( -0.7495606340400177148, 0.1264236179284866091, 0.1550196849856066983 ) ) ;
#29480=CARTESIAN_POINT ( 'NONE',  ( 0.8759842519685039353, 0.1574803149606299191, 1.751968503937007871 ) ) ;
#29483=CARTESIAN_POINT ( 'NONE',  ( -0.8019270111902717657, -0.1787899950787401604, 1.624015747977732849 ) ) ;
#29484=CARTESIAN_POINT ( 'NONE',  ( -0.8019270111902716547, -0.1787899950787401604, 0.8366141731745828647 ) ) ;
#29485=CARTESIAN_POINT ( 'NONE',  ( -0.6971942568897626646, 0.07405724077823318263, 0.3592519684501735977 ) ) ;
#29487=CARTESIAN_POINT ( 'NONE',  ( 0.7185039370078739607, 1.928577636452523993E-17, 0.4133858266641267654 ) ) ;
#29488=CARTESIAN_POINT ( 'NONE',  ( -0.7646288533564489232, 0.1113553986120547346, 0.3297244093412917687 ) ) ;
#29490=AXIS2_PLACEMENT_3D ( 'NONE', #45848, #13055, #8727 ) ;
#29495=CARTESIAN_POINT ( 'NONE',  ( -1.054774247047244096, 0.000000000000000000, 0.3764763778989925203 ) ) ;
#29497=EDGE_LOOP ( 'NONE', ( #8827, #12128, #14835, #21820 ) ) ;
#29499=CARTESIAN_POINT ( 'NONE',  ( -1.002407869896990045, -0.1264236179284866091, 1.439468503883244210 ) ) ;
#29500=ORIENTED_EDGE ( 'NONE', *, *, #31084, .F. ) ;
#29504=CYLINDRICAL_SURFACE ( 'NONE', #36328, 0.1574803149606299191 ) ;
#29506=CARTESIAN_POINT ( 'NONE',  ( 0.8759842519685039353, 0.1574803149606299191, 0.3740157480314960647 ) ) ;
#29509=CARTESIAN_POINT ( 'NONE',  ( -0.7185039370078739607, 1.928577636452523993E-17, 1.122047243986960652 ) ) ;
#29510=CARTESIAN_POINT ( 'NONE',  ( 0.8107537697050254399, 0.1574803149606300301, 0.5634842518609766149 ) ) ;
#29513=AXIS2_PLACEMENT_3D ( 'NONE', #42655, #2879, #40017 ) ;
#29515=DIRECTION ( 'NONE',  ( -0.8660254037844389297, 0.000000000000000000, 0.4999999999999994449 ) ) ;
#29516=CARTESIAN_POINT ( 'NONE',  ( 0.8759842519685039353, 0.1574803149606299191, 0.8858267716535432879 ) ) ;
#29517=CARTESIAN_POINT ( 'NONE',  ( 0.8107537697050254399, 0.1574803149606300301, 1.360728346456693050 ) ) ;
#29526=CARTESIAN_POINT ( 'NONE',  ( 0.7646288533564489232, -0.1113553986120547346, 1.008858267609007875 ) ) ;
#29527=( BOUNDED_CURVE ( )  B_SPLINE_CURVE ( 2, ( #46533, #43168, #13715, #47256, #36253, #10373, #39102, #40041, #6515 ),
 .UNSPECIFIED., .F., .F. ) 
 B_SPLINE_CURVE_WITH_KNOTS ( ( 3, 2, 2, 2, 3 ),
 ( 0.8399999999999999689, 0.8425000000000000266, 0.8449999999999999734, 0.8475000000000000311, 0.8499999999999999778 ),
 .UNSPECIFIED. ) 
 CURVE ( )  GEOMETRIC_REPRESENTATION_ITEM ( )  RATIONAL_B_SPLINE_CURVE ( ( 1.000000000000000000, 0.9238795325112869605, 1.000000000000000000, 0.9238795325112869605, 1.000000000000000000, 0.9238795325112869605, 1.000000000000000000, 0.9238795325112799661, 1.000000000000000000 ) ) 
 REPRESENTATION_ITEM ( '' )  ) ;
#29530=VERTEX_POINT ( 'NONE', #14395 ) ;
#29531=ORIENTED_EDGE ( 'NONE', *, *, #4859, .F. ) ;
#29532=CARTESIAN_POINT ( 'NONE',  ( -0.8759842519685039353, -0.1787899950787401882, 1.552657480261196765 ) ) ;
#29534=CARTESIAN_POINT ( 'NONE',  ( 1.002407869896990045, 0.1264236179284866091, 1.764271653489543290 ) ) ;
#29535=CARTESIAN_POINT ( 'NONE',  ( -0.7495606340400177148, -0.1264236179284866091, 0.7603346456155274380 ) ) ;
#29537=CARTESIAN_POINT ( 'NONE',  ( 0.8759842519685039353, -0.1787899950787401882, 0.3321850393163153226 ) ) ;
#29539=CARTESIAN_POINT ( 'NONE',  ( -0.9500414927467377701, 0.1787899950787401604, 1.249999999946235896 ) ) ;
#29540=CARTESIAN_POINT ( 'NONE',  ( -0.8019270111902716547, 0.1787899950787401604, 0.7431102361667091261 ) ) ;
#29541=CARTESIAN_POINT ( 'NONE',  ( 1.033464566929133799, 0.000000000000000000, 0.9055118109160944506 ) ) ;
#29542=CARTESIAN_POINT ( 'NONE',  ( -0.7646288533564489232, 0.1113553986120547346, 1.668307086506645609 ) ) ;
#29543=CARTESIAN_POINT ( 'NONE',  ( -0.7495606340400177148, 0.1264236179284866091, 1.537893700733637736 ) ) ;
#29544=CARTESIAN_POINT ( 'NONE',  ( -1.033464566929134687, -0.06523048226347956391, 1.887303149498773092 ) ) ;
#29547=CARTESIAN_POINT ( 'NONE',  ( -0.7646288533564489232, 0.1113553986120547346, 1.560039370078740273 ) ) ;
#29548=CARTESIAN_POINT ( 'NONE',  ( 0.8759842519685039353, 0.1574803149606299191, 1.633858267716535639 ) ) ;
#29550=CARTESIAN_POINT ( 'NONE',  ( 0.8759842519685039353, 0.1787899950787401882, 1.493602362150960650 ) ) ;
#29552=FACE_OUTER_BOUND ( 'NONE', #28578, .T. ) ;
#29555=ORIENTED_EDGE ( 'NONE', *, *, #34387, .F. ) ;
#29556=ORIENTED_EDGE ( 'NONE', *, *, #30909, .T. ) ;
#29559=EDGE_CURVE ( 'NONE', #3114, #10926, #42190, .T. ) ;
#29560=CARTESIAN_POINT ( 'NONE',  ( -0.7185039370078766252, -0.06523048226348168721, 1.134350393700787940 ) ) ;
#29566=CARTESIAN_POINT ( 'NONE',  ( 0.8759842519685039353, 0.1787899950787401882, 1.764271653489543290 ) ) ;
#29571=CARTESIAN_POINT ( 'NONE',  ( 0.9500414927467378812, -0.1787899950787401604, 0.7627952755367881643 ) ) ;
#29576=CARTESIAN_POINT ( 'NONE',  ( 1.054774247047244540, 0.07405724077823318263, 1.879921259788756016 ) ) ;
#29579=CARTESIAN_POINT ( 'NONE',  ( 0.6971942568897648851, -0.07405724077823297447, 0.4773622046706456068 ) ) ;
#29583=CARTESIAN_POINT ( 'NONE',  ( 0.7646288533564489232, 0.1113553986120547346, 0.1033464566929133965 ) ) ;
#29587=CARTESIAN_POINT ( 'NONE',  ( -0.8019270111902717657, -0.1787899950787401604, 0.4872047243556847929 ) ) ;
#29588=CARTESIAN_POINT ( 'NONE',  ( 0.8759842519685039353, 0.1574803149606299191, 0.4822834644594015674 ) ) ;
#29590=CARTESIAN_POINT ( 'NONE',  ( 0.8759842519685039353, 0.1787899950787401882, 0.3124999999462365619 ) ) ;
#29591=CARTESIAN_POINT ( 'NONE',  ( 0.7185039370078739607, 1.928577636452523993E-17, 1.122047243986960652 ) ) ;
#29592=CARTESIAN_POINT ( 'NONE',  ( -1.002407869896990045, 0.1264236179284866091, 1.562499999946236118 ) ) ;
#29593=ORIENTED_EDGE ( 'NONE', *, *, #7682, .F. ) ;
#29594=CARTESIAN_POINT ( 'NONE',  ( -0.6971942568897648851, 0.07405724077823318263, 1.225393700733637514 ) ) ;
#29596=CARTESIAN_POINT ( 'NONE',  ( 1.002407869896990045, 0.1264236179284866091, 1.252460629867496067 ) ) ;
#29597=CARTESIAN_POINT ( 'NONE',  ( -0.8019270111902717657, 0.1787899950787401604, 0.9793307086076531442 ) ) ;
#29601=CARTESIAN_POINT ( 'NONE',  ( 1.054774247047244096, 0.000000000000000000, 0.2632874015210397434 ) ) ;
#29602=CARTESIAN_POINT ( 'NONE',  ( -0.6971942568897626646, 0.07405724077823318263, 0.2362204723871814682 ) ) ;
#29603=CARTESIAN_POINT ( 'NONE',  ( -0.8759842519685039353, -0.1787899950787401882, 0.6815944881352126172 ) ) ;
#29604=CARTESIAN_POINT ( 'NONE',  ( 0.7646288533564489232, 0.1113553986120547346, 1.707677165246803241 ) ) ;
#29607=CARTESIAN_POINT ( 'NONE',  ( -0.9873396505805591694, 0.1113553986120547346, 1.353346456692913424 ) ) ;
#29609=EDGE_CURVE ( 'NONE', #24716, #37198, #40000, .T. ) ;
#29610=CARTESIAN_POINT ( 'NONE',  ( -0.9500414927467377701, 0.1787899950787401604, 1.801181102308441861 ) ) ;
#29611=ORIENTED_EDGE ( 'NONE', *, *, #44785, .T. ) ;
#29612=CARTESIAN_POINT ( 'NONE',  ( 0.7495606340400177148, 0.1264236179284866091, 1.926673228292693052 ) ) ;
#29615=ORIENTED_EDGE ( 'NONE', *, *, #17590, .T. ) ;
#29616=CARTESIAN_POINT ( 'NONE',  ( -0.8759842519685039353, 0.000000000000000000, 0.000000000000000000 ) ) ;
#29619=AXIS2_PLACEMENT_3D ( 'NONE', #7397, #7615, #4018 ) ;
#29621=CARTESIAN_POINT ( 'NONE',  ( 0.9500414927467378812, -0.1787899950787401604, 1.195866141678520345 ) ) ;
#29623=CARTESIAN_POINT ( 'NONE',  ( 0.9873396505805591694, 0.1113553986120547346, 1.382874015640503940 ) ) ;
#29625=CARTESIAN_POINT ( 'NONE',  ( 0.9500414927467378812, -0.1787899950787401604, 0.2116141731745827814 ) ) ;
#29628=SHAPE_DEFINITION_REPRESENTATION ( #45712, #7769 ) ;
#29629=CARTESIAN_POINT ( 'NONE',  ( -0.6971942568897648851, 0.07405724077823318263, 0.4379921259304883074 ) ) ;
#29632=CARTESIAN_POINT ( 'NONE',  ( 1.002407869896990045, 0.1264236179284866091, 1.370570866087968520 ) ) ;
#29633=LINE ( 'NONE', #44173, #3078 ) ;
#29637=CARTESIAN_POINT ( 'NONE',  ( 1.033464566929133799, 0.000000000000000000, 0.5511811022546778682 ) ) ;
#29638=CARTESIAN_POINT ( 'NONE',  ( 0.9500414927467378812, -0.1787899950787401604, 0.3297244093950552069 ) ) ;
#29639=CARTESIAN_POINT ( 'NONE',  ( 0.7038554687154958689, 0.04168604917028530255, 0.03937107934831506756 ) ) ;
#29642=DIRECTION ( 'NONE',  ( 0.000000000000000000, 0.000000000000000000, -1.000000000000000000 ) ) ;
#29643=CARTESIAN_POINT ( 'NONE',  ( -0.8759842519685039353, -0.1787899950787401882, 1.272145669237574772 ) ) ;
#29644=CARTESIAN_POINT ( 'NONE',  ( 0.7185039370078739607, 1.928577636452523993E-17, 0.6889763778452283605 ) ) ;
#29648=ORIENTED_EDGE ( 'NONE', *, *, #20233, .F. ) ;
#29650=CARTESIAN_POINT ( 'NONE',  ( -1.033464566929133799, 0.000000000000000000, 0.3149606298137326843 ) ) ;
#29651=CARTESIAN_POINT ( 'NONE',  ( -0.8759842519685039353, 0.1574803149606299191, 1.594488188976378007 ) ) ;
#29652=CARTESIAN_POINT ( 'NONE',  ( 1.054774247047244096, 0.000000000000000000, 1.596948818843874074 ) ) ;
#29654=CARTESIAN_POINT ( 'NONE',  ( -0.9873396505805591694, -0.1113553986120547346, 1.097440944774362270 ) ) ;
#29656=CARTESIAN_POINT ( 'NONE',  ( -1.033464566929133799, 0.000000000000000000, 0.1279527559055118058 ) ) ;
#29657=CARTESIAN_POINT ( 'NONE',  ( 0.9873396505805591694, -0.1113553986120547346, 1.186023622047243986 ) ) ;
#29663=CARTESIAN_POINT ( 'NONE',  ( 1.002407869896990045, 0.1264236179284866091, 0.5831692912848189803 ) ) ;
#29666=CARTESIAN_POINT ( 'NONE',  ( 1.054774247047244096, 0.000000000000000000, 0.8932086613635591421 ) ) ;
#29668=CARTESIAN_POINT ( 'NONE',  ( -1.002407869896990045, -0.1264236179284866091, 1.242618110182456714 ) ) ;
#29672=CARTESIAN_POINT ( 'NONE',  ( -1.054774247047244540, -0.07405724077823318263, 0.2608267715997796832 ) ) ;
#29673=CARTESIAN_POINT ( 'NONE',  ( 1.033464566929133799, 0.000000000000000000, 0.6791338582677166613 ) ) ;
#29677=CARTESIAN_POINT ( 'NONE',  ( -0.8107537697050254399, -0.1574803149606297803, 0.8538385825696385156 ) ) ;
#29680=CARTESIAN_POINT ( 'NONE',  ( -0.6971942568897637749, 2.189545951927499583E-17, 0.7111220471903307860 ) ) ;
#29682=CARTESIAN_POINT ( 'NONE',  ( -0.8759842519685039353, -0.1787899950787401882, 1.749507873961984483 ) ) ;
#29683=CARTESIAN_POINT ( 'NONE',  ( -0.7646288533564489232, 0.1113553986120547346, 0.8513779527559054427 ) ) ;
#29686=CARTESIAN_POINT ( 'NONE',  ( -0.7185039370078746268, 0.06523048226347956391, 1.513287401467275917 ) ) ;
#29687=CARTESIAN_POINT ( 'NONE',  ( 0.8759842519685039353, -0.1787899950787401882, 0.8833661416785196785 ) ) ;
#29688=CARTESIAN_POINT ( 'NONE',  ( 1.002407869896990045, -0.1264236179284866091, 1.355807086560409491 ) ) ;
#29690=CARTESIAN_POINT ( 'NONE',  ( 0.7646288533564489232, 0.1113553986120547346, 1.363188976377952999 ) ) ;
#29691=CARTESIAN_POINT ( 'NONE',  ( 0.7130513932977933234, -0.03761588314558831497, 1.983967136699976486 ) ) ;
#29694=( BOUNDED_CURVE ( )  B_SPLINE_CURVE ( 2, ( #21231, #39198, #6618, #32764, #14534, #13813, #3009, #21722, #29199 ),
 .UNSPECIFIED., .F., .T. ) 
 B_SPLINE_CURVE_WITH_KNOTS ( ( 3, 2, 2, 2, 3 ),
 ( 0.1700000000000000122, 0.1724999999999999867, 0.1749999999999999889, 0.1774999999999999911, 0.1799999999999999933 ),
 .UNSPECIFIED. ) 
 CURVE ( )  GEOMETRIC_REPRESENTATION_ITEM ( )  RATIONAL_B_SPLINE_CURVE ( ( 1.000000000000000000, 0.9238795325112869605, 1.000000000000000000, 0.9238795325112869605, 1.000000000000000000, 0.9238795325112869605, 1.000000000000000000, 0.9238795325112869605, 1.000000000000000000 ) ) 
 REPRESENTATION_ITEM ( '' )  ) ;
#29695=CARTESIAN_POINT ( 'NONE',  ( 0.6971942568897637749, 2.189545951927499583E-17, 0.7504921259304880854 ) ) ;
#29700=CARTESIAN_POINT ( 'NONE',  ( 0.6971942568897648851, 0.07405724077823318263, 1.181102362150960428 ) ) ;
#29701=CARTESIAN_POINT ( 'NONE',  ( -0.9873396505805591694, 0.1113553986120547346, 1.038385826771653475 ) ) ;
#29702=CARTESIAN_POINT ( 'NONE',  ( -1.033464566929134687, -0.06523048226347956391, 0.5191929133858269596 ) ) ;
#29704=ORIENTED_EDGE ( 'NONE', *, *, #40646, .T. ) ;
#29706=CARTESIAN_POINT ( 'NONE',  ( -0.8759842519685039353, -0.1787899950787401882, 0.2878937007336381804 ) ) ;
#29709=CARTESIAN_POINT ( 'NONE',  ( -1.054774247047244540, -0.07405724077823318263, 1.633858267662771313 ) ) ;
#29710=CARTESIAN_POINT ( 'NONE',  ( -0.8759842519685039353, -0.1787899950787401882, 0.9178149605761574126 ) ) ;
#29711=EDGE_CURVE ( 'NONE', #11324, #42942, #4542, .T. ) ;
#29712=CARTESIAN_POINT ( 'NONE',  ( -0.7646288533564489232, -0.1113553986120547346, 0.1033464565853864231 ) ) ;
#29715=CARTESIAN_POINT ( 'NONE',  ( 0.8759842519685039353, -0.1787899950787401882, 0.05167322829269314910 ) ) ;
#29723=CARTESIAN_POINT ( 'NONE',  ( -1.054774247047244540, 0.07405724077823318263, 0.3789370078202520253 ) ) ;
#29724=CARTESIAN_POINT ( 'NONE',  ( 0.7646288533564489232, -0.1113553986120547346, 1.609251968503937036 ) ) ;
#29726=CARTESIAN_POINT ( 'NONE',  ( -0.6971942568897637749, 2.189545951927499583E-17, 1.385334645615527549 ) ) ;
#29731=CARTESIAN_POINT ( 'NONE',  ( 0.8759842519685039353, 0.000000000000000000, 4.498031496062992574 ) ) ;
#29733=CARTESIAN_POINT ( 'NONE',  ( 0.7185039370078739607, 1.928577636452523993E-17, 0.4232283464566928832 ) ) ;
#29735=CARTESIAN_POINT ( 'NONE',  ( -0.9873396505805591694, -0.1113553986120547346, 1.058070866034204860 ) ) ;
#29736=CARTESIAN_POINT ( 'NONE',  ( 0.8759842519685039353, -0.1787899950787401882, 0.4502952755367874427 ) ) ;
#29737=CARTESIAN_POINT ( 'NONE',  ( -1.033464566929133799, 0.000000000000000000, 1.702755905511810885 ) ) ;
#29739=CARTESIAN_POINT ( 'NONE',  ( 0.8759842519685039353, -0.1574803149606299191, 1.958661417215307177 ) ) ;
#29740=VERTEX_POINT ( 'NONE', #26846 ) ;
#29741=CARTESIAN_POINT ( 'NONE',  ( 1.033464566929134687, -0.06523048226347956391, 0.04675196850393695952 ) ) ;
#29742=CARTESIAN_POINT ( 'NONE',  ( 1.033464566929134687, -0.06523048226347956391, 0.9522637795275590289 ) ) ;
#29745=CARTESIAN_POINT ( 'NONE',  ( 0.9412147342319837628, -0.1574803149606297803, 0.7504921259842517456 ) ) ;
#29755=CARTESIAN_POINT ( 'NONE',  ( 1.033464566929134687, -0.06523048226347956391, 1.178641732175937040 ) ) ;
#29758=CARTESIAN_POINT ( 'NONE',  ( -0.6971942568897637749, 2.189545951927499583E-17, 0.4749015747493858242 ) ) ;
#29760=ORIENTED_EDGE ( 'NONE', *, *, #5952, .F. ) ;
#29761=CARTESIAN_POINT ( 'NONE',  ( -0.8759842519685039353, 0.1787899950787401882, 1.532972440891118060 ) ) ;
#29762=CARTESIAN_POINT ( 'NONE',  ( 1.054774247047244096, 0.000000000000000000, 1.641240157426551161 ) ) ;
#29763=CARTESIAN_POINT ( 'NONE',  ( -1.002407869896990045, 0.1264236179284866091, 0.7406496062454487328 ) ) ;
#29764=CARTESIAN_POINT ( 'NONE',  ( 0.7185039370078739607, 1.928577636452523993E-17, 1.476377952648377789 ) ) ;
#29765=CARTESIAN_POINT ( 'NONE',  ( 1.002407869896990045, -0.1264236179284866091, 0.3371062991588349989 ) ) ;
#29766=CARTESIAN_POINT ( 'NONE',  ( -0.8107537697050254399, 0.1574803149606300301, 1.508366141624757129 ) ) ;
#29767=CARTESIAN_POINT ( 'NONE',  ( -0.6971942568897648851, -0.07405724077823297447, 1.264763779473795813 ) ) ;
#29770=CYLINDRICAL_SURFACE ( 'NONE', #9225, 0.1574803149606299191 ) ;
#29771=CARTESIAN_POINT ( 'NONE',  ( -1.002407869896990045, -0.1264236179284866091, 1.518208661363559031 ) ) ;
#29772=CARTESIAN_POINT ( 'NONE',  ( -1.033464566929133799, 0.000000000000000000, 1.889763779420031486 ) ) ;
#29773=ORIENTED_EDGE ( 'NONE', *, *, #42657, .F. ) ;
#29774=CARTESIAN_POINT ( 'NONE',  ( -0.8759842519685039353, -0.1574803149606299191, 1.574803149606299302 ) ) ;
#29775=FACE_OUTER_BOUND ( 'NONE', #43072, .T. ) ;
#29776=CARTESIAN_POINT ( 'NONE',  ( 0.8019270111902716547, 0.1787899950787401604, 1.496062992072220599 ) ) ;
#29779=EDGE_LOOP ( 'NONE', ( #13851, #32515, #17483, #17975 ) ) ;
#29787=VERTEX_POINT ( 'NONE', #18674 ) ;
#29790=CARTESIAN_POINT ( 'NONE',  ( 1.054774247047244540, -0.07405724077823318263, 1.751968503883245765 ) ) ;
#29793=CARTESIAN_POINT ( 'NONE',  ( 1.054774247047244096, 0.000000000000000000, 0.7701771653005669016 ) ) ;
#29794=( BOUNDED_CURVE ( )  B_SPLINE_CURVE ( 2, ( #8407, #20322, #26654, #24629, #20553, #38996, #31837, #16508, #35194 ),
 .UNSPECIFIED., .F., .T. ) 
 B_SPLINE_CURVE_WITH_KNOTS ( ( 3, 2, 2, 2, 3 ),
 ( 0.6199999999999999956, 0.6225000000000000533, 0.6250000000000000000, 0.6274999999999999467, 0.6300000000000000044 ),
 .UNSPECIFIED. ) 
 CURVE ( )  GEOMETRIC_REPRESENTATION_ITEM ( )  RATIONAL_B_SPLINE_CURVE ( ( 1.000000000000000000, 0.9238795325112869605, 1.000000000000000000, 0.9238795325112869605, 1.000000000000000000, 0.9238795325112869605, 1.000000000000000000, 0.9238795325112829637, 1.000000000000000000 ) ) 
 REPRESENTATION_ITEM ( '' )  ) ;
#29798=CARTESIAN_POINT ( 'NONE',  ( -0.7185039370078739607, 1.928577636452523993E-17, 1.328740157480315043 ) ) ;
#29799=CARTESIAN_POINT ( 'NONE',  ( 0.7495606340400177148, 0.1264236179284866091, 1.774114173174582643 ) ) ;
#29802=CARTESIAN_POINT ( 'NONE',  ( 0.8759842519685039353, 0.1574803149606299191, 0.05905511811023622659 ) ) ;
#29807=CARTESIAN_POINT ( 'NONE',  ( 0.7495606340400177148, -0.1264236179284866091, 0.2091535432533232486 ) ) ;
#29808=CARTESIAN_POINT ( 'NONE',  ( 0.8107537697050254399, 0.1574803149606300301, 0.06151574803149608556 ) ) ;
#29811=CARTESIAN_POINT ( 'NONE',  ( -0.6971942568897648851, 0.07405724077823318263, 1.771653543253322249 ) ) ;
#29813=CARTESIAN_POINT ( 'NONE',  ( -0.8759842519685039353, 0.1787899950787401882, 1.178641732229700922 ) ) ;
#29815=CARTESIAN_POINT ( 'NONE',  ( 1.054774247047244096, 0.000000000000000000, 1.247539370024976391 ) ) ;
#29817=CARTESIAN_POINT ( 'NONE',  ( 0.6971942568897626646, -0.07405724077823297447, 0.04921259837143338034 ) ) ;
#29818=CARTESIAN_POINT ( 'NONE',  ( -1.054774247047244540, -0.07405724077823318263, 1.003937007820251193 ) ) ;
#29819=LINE ( 'NONE', #28873, #1733 ) ;
#29820=CARTESIAN_POINT ( 'NONE',  ( 0.6971942568897648851, 0.07405724077823318263, 0.4773622046706456068 ) ) ;
#29821=CARTESIAN_POINT ( 'NONE',  ( -0.8019270111902716547, 0.1787899950787401604, 0.3494094487651343006 ) ) ;
#29822=CARTESIAN_POINT ( 'NONE',  ( -1.054774247047244540, -0.07405724077823318263, 0.7677165353793073965 ) ) ;
#29823=EDGE_LOOP ( 'NONE', ( #22774, #34873, #10175, #35102 ) ) ;
#29825=( BOUNDED_CURVE ( )  B_SPLINE_CURVE ( 2, ( #12692, #16963, #27550, #16277, #23462, #17199, #31835, #28012, #45465 ),
 .UNSPECIFIED., .F., .T. ) 
 B_SPLINE_CURVE_WITH_KNOTS ( ( 3, 2, 2, 2, 3 ),
 ( 0.7800000000000000266, 0.7824999999999999734, 0.7850000000000000311, 0.7874999999999999778, 0.7900000000000000355 ),
 .UNSPECIFIED. ) 
 CURVE ( )  GEOMETRIC_REPRESENTATION_ITEM ( )  RATIONAL_B_SPLINE_CURVE ( ( 1.000000000000000000, 0.9238795325112869605, 1.000000000000000000, 0.9238795325112869605, 1.000000000000000000, 0.9238795325112869605, 1.000000000000000000, 0.9238795325112829637, 1.000000000000000000 ) ) 
 REPRESENTATION_ITEM ( '' )  ) ;
#29828=CARTESIAN_POINT ( 'NONE',  ( 0.8759842519685039353, 0.1787899950787401882, 0.9030511810485984947 ) ) ;
#29829=CARTESIAN_POINT ( 'NONE',  ( -0.9873396505805591694, -0.1113553986120547346, 0.1624015748031496231 ) ) ;
#29830=CARTESIAN_POINT ( 'NONE',  ( 0.6971942568897648851, 0.07405724077823318263, 1.067913385773007651 ) ) ;
#29833=CARTESIAN_POINT ( 'NONE',  ( 0.8019270111902717657, 0.1787899950787401604, 1.924212598371433325 ) ) ;
#29834=CARTESIAN_POINT ( 'NONE',  ( -0.7495606340400177148, -0.1264236179284866091, 0.8784448818360000022 ) ) ;
#29835=CARTESIAN_POINT ( 'NONE',  ( 0.9412147342319837628, -0.1574803149606297803, 0.3174212598425196763 ) ) ;
#29841=CARTESIAN_POINT ( 'NONE',  ( 0.8019270111902717657, 0.1787899950787401604, 1.176181102308441417 ) ) ;
#29842=CARTESIAN_POINT ( 'NONE',  ( -1.033464566929134687, 0.06523048226347956391, 0.8292322833570401341 ) ) ;
#29843=DIRECTION ( 'NONE',  ( -1.000000000000000000, 0.000000000000000000, 0.000000000000000000 ) ) ;
#29846=CARTESIAN_POINT ( 'NONE',  ( 0.9500414927467378812, 0.1787899950787401604, 0.1082677164816695514 ) ) ;
#29850=EDGE_CURVE ( 'NONE', #29244, #25968, #43746, .T. ) ;
#29853=CARTESIAN_POINT ( 'NONE',  ( -0.6971942568897637749, 2.189545951927499583E-17, 0.7160433070328504623 ) ) ;
#29858=CARTESIAN_POINT ( 'NONE',  ( 0.8019270111902717657, -0.1787899950787401604, 1.392716535379308285 ) ) ;
#29860=CARTESIAN_POINT ( 'NONE',  ( 0.6971942568897637749, 2.189545951927499583E-17, 1.616633858213952779 ) ) ;
#29861=ADVANCED_FACE ( 'NONE', ( #30226 ), #44774, .T. ) ;
#29865=CARTESIAN_POINT ( 'NONE',  ( -1.033464566929133799, 0.000000000000000000, 1.033464566929133799 ) ) ;
#29869=CARTESIAN_POINT ( 'NONE',  ( 0.8107537697050253289, 0.1574803149606300301, 0.6028543306011346914 ) ) ;
#29870=ORIENTED_EDGE ( 'NONE', *, *, #5461, .T. ) ;
#29872=CARTESIAN_POINT ( 'NONE',  ( 0.8241499611671327941, 0.1701252295545555571, 0.03936897362612447326 ) ) ;
#29877=CARTESIAN_POINT ( 'NONE',  ( -1.033464566929133799, 0.000000000000000000, 1.102362204616881947 ) ) ;
#29878=CARTESIAN_POINT ( 'NONE',  ( 0.6971942568897648851, 0.07405724077823318263, 1.653543307032850462 ) ) ;
#29879=CARTESIAN_POINT ( 'NONE',  ( -0.9873396505805591694, 0.1113553986120547346, 1.825787401574803237 ) ) ;
#29880=CARTESIAN_POINT ( 'NONE',  ( -0.8107537697050254399, -0.1574803149606297803, 1.375492125984252745 ) ) ;
#29881=CARTESIAN_POINT ( 'NONE',  ( 1.033464566929133799, 0.000000000000000000, 1.929133858160188897 ) ) ;
#29886=FACE_OUTER_BOUND ( 'NONE', #22217, .T. ) ;
#29888=CARTESIAN_POINT ( 'NONE',  ( 1.054774247047244096, 0.000000000000000000, 0.8538385826234016207 ) ) ;
#29890=CARTESIAN_POINT ( 'NONE',  ( -1.002407869896990045, -0.1264236179284866091, 1.321358267662771757 ) ) ;
#29892=AXIS2_PLACEMENT_3D ( 'NONE', #29060, #43379, #25186 ) ;
#29893=CARTESIAN_POINT ( 'NONE',  ( -0.8759842519685039353, 0.1787899950787401882, 0.3912401574265515491 ) ) ;
#29894=CARTESIAN_POINT ( 'NONE',  ( 0.7185039370078739607, 1.928577636452523993E-17, 0.6594488188976378451 ) ) ;
#29895=CARTESIAN_POINT ( 'NONE',  ( 0.8107537697050254399, -0.1574803149606297803, 1.641240157372788389 ) ) ;
#29898=CARTESIAN_POINT ( 'NONE',  ( 0.7108038354695511707, 0.06841997037041733232, 0.03937007863263043694 ) ) ;
#29899=EDGE_LOOP ( 'NONE', ( #45507, #42596, #13901, #19115 ) ) ;
#29900=CARTESIAN_POINT ( 'NONE',  ( 0.7646288533564489232, -0.1113553986120547346, 1.205708661309795371 ) ) ;
#29902=LINE ( 'NONE', #33726, #19338 ) ;
#29904=EDGE_CURVE ( 'NONE', #24840, #40966, #9482, .T. ) ;
#29905=EDGE_CURVE ( 'NONE', #26896, #14505, #28815, .T. ) ;
#29906=CARTESIAN_POINT ( 'NONE',  ( 1.033464566929133799, 0.000000000000000000, 0.4724409447743622148 ) ) ;
#29907=CARTESIAN_POINT ( 'NONE',  ( -0.8759842519685039353, -0.1574803149606299191, 0.8267716535433071723 ) ) ;
#29910=DIRECTION ( 'NONE',  ( 0.000000000000000000, 0.000000000000000000, -1.000000000000000000 ) ) ;
#29911=CARTESIAN_POINT ( 'NONE',  ( -0.8759842519685039353, 0.1574803149606299191, 1.584645669183810890 ) ) ;
#29912=CARTESIAN_POINT ( 'NONE',  ( 0.7495606340400177148, 0.1264236179284866091, 0.9867125983714331028 ) ) ;
#29913=CARTESIAN_POINT ( 'NONE',  ( 0.6971942568897637749, 2.189545951927499583E-17, 1.380413385773007873 ) ) ;
#29918=CARTESIAN_POINT ( 'NONE',  ( 0.9412147342319837628, -0.1574803149606297803, 1.419783464566930276 ) ) ;
#29919=CARTESIAN_POINT ( 'NONE',  ( 0.7102656538334291003, 0.005844371759168983001, 1.983162255655229078 ) ) ;
#29921=VECTOR ( 'NONE', #44259, 39.37007874015748143 ) ;
#29922=CARTESIAN_POINT ( 'NONE',  ( -0.8759842519685039353, 0.000000000000000000, 0.000000000000000000 ) ) ;
#29923=CARTESIAN_POINT ( 'NONE',  ( 0.6971942568897637749, 2.189545951927499583E-17, 0.8292322834108031282 ) ) ;
#29926=VERTEX_POINT ( 'NONE', #38086 ) ;
#29927=CARTESIAN_POINT ( 'NONE',  ( 0.7185039370078741827, 0.06523048226347841205, 0.9325787401574796576 ) ) ;
#29929=CARTESIAN_POINT ( 'NONE',  ( 1.002407869896990045, -0.1264236179284866091, 1.198326771599779628 ) ) ;
#29930=DIRECTION ( 'NONE',  ( 1.822029033848725028E-16, 0.000000000000000000, 1.000000000000000000 ) ) ;
#29935=CARTESIAN_POINT ( 'NONE',  ( -0.8019270111902717657, 0.1787899950787401604, 0.1919291338045042428 ) ) ;
#29939=CARTESIAN_POINT ( 'NONE',  ( -0.8759842519685039353, 0.1787899950787401882, 1.646161417269070837 ) ) ;
#29940=CARTESIAN_POINT ( 'NONE',  ( -0.8759842519685039353, 0.1787899950787401882, 0.8981299212060788184 ) ) ;
#29941=CARTESIAN_POINT ( 'NONE',  ( -0.8759842519685039353, -0.1787899950787401882, 0.4896653542769449086 ) ) ;
#29944=CARTESIAN_POINT ( 'NONE',  ( -0.8759842519685039353, 0.1574803149606299191, 0.3248031494987720369 ) ) ;
#29946=CARTESIAN_POINT ( 'NONE',  ( -0.7185039370078739607, 0.000000000000000000, 2.007874015640504162 ) ) ;
#29952=CARTESIAN_POINT ( 'NONE',  ( -0.9412147342319837628, -0.1574803149606297803, 1.173720472333417586 ) ) ;
#29953=CARTESIAN_POINT ( 'NONE',  ( -0.6971942568897626646, 0.07405724077823318263, 0.3543307086076538659 ) ) ;
#29956=ORIENTED_EDGE ( 'NONE', *, *, #25783, .T. ) ;
#29958=CARTESIAN_POINT ( 'NONE',  ( -0.6971942568897637749, 2.189545951927499583E-17, 1.542814960576157413 ) ) ;
#29962=( BOUNDED_CURVE ( )  B_SPLINE_CURVE ( 2, ( #4536, #44798, #23263, #12493, #30013, #37629, #40720, #19654, #37879 ),
 .UNSPECIFIED., .F., .F. ) 
 B_SPLINE_CURVE_WITH_KNOTS ( ( 3, 2, 2, 2, 3 ),
 ( 0.08000000000000000167, 0.08250000000000000389, 0.08500000000000000611, 0.08749999999999999445, 0.08999999999999999667 ),
 .UNSPECIFIED. ) 
 CURVE ( )  GEOMETRIC_REPRESENTATION_ITEM ( )  RATIONAL_B_SPLINE_CURVE ( ( 1.000000000000000000, 0.9238795325112869605, 1.000000000000000000, 0.9238795325112869605, 1.000000000000000000, 0.9238795325112869605, 1.000000000000000000, 0.9238795325112869605, 1.000000000000000000 ) ) 
 REPRESENTATION_ITEM ( '' )  ) ;
#29967=CARTESIAN_POINT ( 'NONE',  ( -0.7646288533564489232, -0.1113553986120547346, 1.008858267609007875 ) ) ;
#29968=CARTESIAN_POINT ( 'NONE',  ( 0.8759842519685039353, -0.1787899950787401882, 0.5290354330171024300 ) ) ;
#29973=EDGE_CURVE ( 'NONE', #40417, #35775, #7369, .T. ) ;
#29975=CARTESIAN_POINT ( 'NONE',  ( -0.8019270111902716547, 0.1787899950787401604, 0.9055118109698584439 ) ) ;
#29976=CARTESIAN_POINT ( 'NONE',  ( 0.7646288533564489232, 0.1113553986120547346, 0.9301181102362204856 ) ) ;
#29979=CARTESIAN_POINT ( 'NONE',  ( -0.9412147342319837628, -0.1574803149606297803, 0.8292322834645677876 ) ) ;
#29985=ORIENTED_EDGE ( 'NONE', *, *, #20556, .T. ) ;
#29987=CARTESIAN_POINT ( 'NONE',  ( 0.8759842519685039353, -0.1574803149606299191, 1.377952755905512028 ) ) ;
#29992=CARTESIAN_POINT ( 'NONE',  ( 1.033464566929134687, 0.06523048226347956391, 1.144192913278300194 ) ) ;
#29993=CARTESIAN_POINT ( 'NONE',  ( -0.8759842519685039353, -0.1574803149606299191, 1.653543307086614345 ) ) ;
#29996=CARTESIAN_POINT ( 'NONE',  ( -0.8759842519685039353, 0.1787899950787401882, 1.729822834591905556 ) ) ;
#29997=CARTESIAN_POINT ( 'NONE',  ( 0.7495606340400177148, -0.1264236179284866091, 1.744586614119464807 ) ) ;
#29999=CARTESIAN_POINT ( 'NONE',  ( -0.8759842519685039353, 0.1787899950787401882, 0.9030511810485984947 ) ) ;
#30002=CARTESIAN_POINT ( 'NONE',  ( -1.054774247047244096, 0.000000000000000000, 1.163877952702141672 ) ) ;
#30003=CARTESIAN_POINT ( 'NONE',  ( -1.054774247047244096, 0.000000000000000000, 0.9276574802611967652 ) ) ;
#30004=CARTESIAN_POINT ( 'NONE',  ( -0.8019270111902717657, 0.1787899950787401604, 0.1574803149068664809 ) ) ;
#30006=CARTESIAN_POINT ( 'NONE',  ( -1.054774247047244540, 0.07405724077823318263, 1.525590551127340433 ) ) ;
#30007=CARTESIAN_POINT ( 'NONE',  ( -0.8759842519685039353, -0.1574803149606299191, 1.958661417215307177 ) ) ;
#30009=CARTESIAN_POINT ( 'NONE',  ( -1.033464566929134687, -0.06523048226347956391, 1.660925196850393526 ) ) ;
#30011=CARTESIAN_POINT ( 'NONE',  ( 1.054774247047244540, 0.07405724077823318263, 1.604330708607653921 ) ) ;
#30013=CARTESIAN_POINT ( 'NONE',  ( 0.8759842519685039353, 0.1574803149606299191, 0.2066929132782996115 ) ) ;
#30014=CARTESIAN_POINT ( 'NONE',  ( 0.7185039370078739607, 1.928577636452523993E-17, 0.2952755904436539236 ) ) ;
#30015=ORIENTED_EDGE ( 'NONE', *, *, #22614, .T. ) ;
#30018=ORIENTED_EDGE ( 'NONE', *, *, #43437, .F. ) ;
#30030=CARTESIAN_POINT ( 'NONE',  ( -0.8107537697050254399, 0.1574803149606300301, 1.075295275483024726 ) ) ;
#30031=CARTESIAN_POINT ( 'NONE',  ( 0.8759842519685039353, -0.1787899950787401882, 0.7997047243556849594 ) ) ;
#30033=DIRECTION ( 'NONE',  ( -1.000000000000000000, 0.000000000000000000, 0.000000000000000000 ) ) ;
#30034=CARTESIAN_POINT ( 'NONE',  ( -0.8107537697050234415, -0.1574803149606297803, 0.06643700776648873985 ) ) ;
#30035=CARTESIAN_POINT ( 'NONE',  ( 0.6971942568897648851, 0.07405724077823318263, 1.776574803095843924 ) ) ;
#30037=CARTESIAN_POINT ( 'NONE',  ( 0.9412147342319837628, -0.1574803149606297803, 0.04183070866141735261 ) ) ;
#30038=CYLINDRICAL_SURFACE ( 'NONE', #18346, 0.1574803149606299191 ) ;
#30042=CARTESIAN_POINT ( 'NONE',  ( 0.8019270111902717657, -0.1787899950787401604, 0.2116141731745827814 ) ) ;
#30043=CARTESIAN_POINT ( 'NONE',  ( -0.7185039370078739607, 1.928577636452523993E-17, 1.633858267609007875 ) ) ;
#30044=CARTESIAN_POINT ( 'NONE',  ( -1.002407869896990045, -0.1264236179284866091, 1.749507873961984483 ) ) ;
#30046=CARTESIAN_POINT ( 'NONE',  ( -1.054774247047244540, -0.07405724077823318263, 1.245078740103716886 ) ) ;
#30048=CARTESIAN_POINT ( 'NONE',  ( 0.9500414927467378812, 0.1787899950787401604, 1.333661417269071059 ) ) ;
#30050=VECTOR ( 'NONE', #1084, 39.37007874015748143 ) ;
#30051=AXIS2_PLACEMENT_3D ( 'NONE', #7534, #3710, #8005 ) ;
#30052=CARTESIAN_POINT ( 'NONE',  ( 1.054774247047244540, 0.07405724077823318263, 1.953740157426552715 ) ) ;
#30053=CARTESIAN_POINT ( 'NONE',  ( -0.8759842519685039353, -0.1787899950787401882, 0.9965551180564724554 ) ) ;
#30056=CARTESIAN_POINT ( 'NONE',  ( 0.6971942568897648851, 0.07405724077823318263, 0.4379921259304883074 ) ) ;
#30057=CARTESIAN_POINT ( 'NONE',  ( -0.6971942568897637749, 2.189545951927499583E-17, 0.3961614172690708924 ) ) ;
#30058=CARTESIAN_POINT ( 'NONE',  ( 1.033464566929134687, 0.06523048226347956391, 1.656003936900346085 ) ) ;
#30066=CARTESIAN_POINT ( 'NONE',  ( -1.033464566929134687, -0.06523048226347956391, 0.08612204724409450174 ) ) ;
#30068=ORIENTED_EDGE ( 'NONE', *, *, #32334, .F. ) ;
#30069=CARTESIAN_POINT ( 'NONE',  ( -1.054774247047244540, -0.07405724077823318263, 0.8907480314422986378 ) ) ;
#30070=CARTESIAN_POINT ( 'NONE',  ( -0.9873396505805591694, -0.1113553986120547346, 0.3198818897637795700 ) ) ;
#30071=LINE ( 'NONE', #45084, #14486 ) ;
#30075=EDGE_CURVE ( 'NONE', #47093, #41227, #17448, .T. ) ;
#30078=CARTESIAN_POINT ( 'NONE',  ( 0.6971942568897648851, 0.07405724077823318263, 1.181102362150960428 ) ) ;
#30079=CARTESIAN_POINT ( 'NONE',  ( 0.8107537697050254399, 0.1574803149606300301, 1.596948818897636624 ) ) ;
#30081=( BOUNDED_CURVE ( )  B_SPLINE_CURVE ( 2, ( #11170, #354, #44424, #19035, #32984, #15005, #47343, #33460, #29656 ),
 .UNSPECIFIED., .F., .F. ) 
 B_SPLINE_CURVE_WITH_KNOTS ( ( 3, 2, 2, 2, 3 ),
 ( 0.05000000000000000278, 0.05249999999999999806, 0.05500000000000000028, 0.05750000000000000250, 0.05999999999999999778 ),
 .UNSPECIFIED. ) 
 CURVE ( )  GEOMETRIC_REPRESENTATION_ITEM ( )  RATIONAL_B_SPLINE_CURVE ( ( 1.000000000000000000, 0.9238795325112859613, 1.000000000000000000, 0.9238795325112869605, 1.000000000000000000, 0.9238795325112869605, 1.000000000000000000, 0.9238795325112869605, 1.000000000000000000 ) ) 
 REPRESENTATION_ITEM ( '' )  ) ;
#30082=VECTOR ( 'NONE', #23229, 39.37007874015748143 ) ;
#30085=CARTESIAN_POINT ( 'NONE',  ( 0.7495606340400177148, -0.1264236179284866091, 1.503444881836000002 ) ) ;
#30091=DIRECTION ( 'NONE',  ( -1.000000000000000000, 0.000000000000000000, 0.000000000000000000 ) ) ;
#30094=CARTESIAN_POINT ( 'NONE',  ( -0.8019270111902716547, -0.1787899950787401604, 0.7234251967966300878 ) ) ;
#30101=CARTESIAN_POINT ( 'NONE',  ( 0.7495606340400177148, -0.1264236179284866091, 1.739665354276945131 ) ) ;
#30102=CARTESIAN_POINT ( 'NONE',  ( -0.9873396505805591694, -0.1113553986120547346, 1.648622047136566904 ) ) ;
#30104=CARTESIAN_POINT ( 'NONE',  ( -0.7185039370078739607, 1.928577636452523993E-17, 0.4625984251968504046 ) ) ;
#30106=CARTESIAN_POINT ( 'NONE',  ( 0.7185039370078739607, 1.928577636452523993E-17, 0.5314960628845992741 ) ) ;
#30107=( BOUNDED_CURVE ( )  B_SPLINE_CURVE ( 2, ( #44814, #12024, #19428, #26649, #41197, #19668, #4799, #34080, #45045 ),
 .UNSPECIFIED., .F., .F. ) 
 B_SPLINE_CURVE_WITH_KNOTS ( ( 3, 2, 2, 2, 3 ),
 ( 0.05999999999999999778, 0.06250000000000000000, 0.06500000000000000222, 0.06750000000000000444, 0.07000000000000000666 ),
 .UNSPECIFIED. ) 
 CURVE ( )  GEOMETRIC_REPRESENTATION_ITEM ( )  RATIONAL_B_SPLINE_CURVE ( ( 1.000000000000000000, 0.9238795325112869605, 1.000000000000000000, 0.9238795325112869605, 1.000000000000000000, 0.9238795325112869605, 1.000000000000000000, 0.9238795325112869605, 1.000000000000000000 ) ) 
 REPRESENTATION_ITEM ( '' )  ) ;
#30108=CARTESIAN_POINT ( 'NONE',  ( 1.002407869896990045, 0.1264236179284866091, 0.3026574802611972648 ) ) ;
#30109=CARTESIAN_POINT ( 'NONE',  ( -1.033464566929133799, 0.000000000000000000, 1.732283464459401623 ) ) ;
#30110=CARTESIAN_POINT ( 'NONE',  ( -0.9873396505805591694, -0.1113553986120547346, 1.333661417215306955 ) ) ;
#30112=CARTESIAN_POINT ( 'NONE',  ( -0.8019270111902717657, -0.1787899950787401604, 1.309055118056472899 ) ) ;
#30113=CARTESIAN_POINT ( 'NONE',  ( 0.7646288533564489232, 0.1113553986120547346, 0.6053149605223937524 ) ) ;
#30119=CARTESIAN_POINT ( 'NONE',  ( 0.9873396505805591694, 0.1113553986120547346, 0.2411417321759374011 ) ) ;
#30121=CARTESIAN_POINT ( 'NONE',  ( -1.033464566929134687, -0.06523048226347956391, 0.4404527559055117503 ) ) ;
#30122=CARTESIAN_POINT ( 'NONE',  ( 0.9873396505805591694, -0.1113553986120547346, 1.924212598317669221 ) ) ;
#30125=CARTESIAN_POINT ( 'NONE',  ( -1.033464566929133799, 0.000000000000000000, 0.3641732283464567121 ) ) ;
#30127=CARTESIAN_POINT ( 'NONE',  ( -0.6971942568897648851, -0.07405724077823297447, 1.269685039316314601 ) ) ;
#30130=CARTESIAN_POINT ( 'NONE',  ( -0.8759842519685039353, 0.1787899950787401882, 0.3518700786863940833 ) ) ;
#30137=ORIENTED_EDGE ( 'NONE', *, *, #14131, .T. ) ;
#30138=CARTESIAN_POINT ( 'NONE',  ( 0.8019270111902717657, -0.1787899950787401604, 1.033464566875371027 ) ) ;
#30141=CARTESIAN_POINT ( 'NONE',  ( 0.9412147342319837628, 0.1574803149606300301, 1.424704724301921521 ) ) ;
#30144=EDGE_CURVE ( 'NONE', #45011, #28038, #43165, .T. ) ;
#30145=CARTESIAN_POINT ( 'NONE',  ( -0.6971942568897637749, 2.189545951927499583E-17, 0.2436023621509610382 ) ) ;
#30146=CARTESIAN_POINT ( 'NONE',  ( -0.7646288533564489232, -0.1113553986120547346, 0.9005905511811023167 ) ) ;
#30147=DIRECTION ( 'NONE',  ( 1.822029033848725028E-16, 0.000000000000000000, 1.000000000000000000 ) ) ;
#30149=CARTESIAN_POINT ( 'NONE',  ( -0.9412147342319837628, 0.1574803149606300301, 1.936515747923967412 ) ) ;
#30150=CARTESIAN_POINT ( 'NONE',  ( 0.8019270111902717657, 0.1787899950787401604, 0.9448818897100165204 ) ) ;
#30154=CARTESIAN_POINT ( 'NONE',  ( 0.8107537697050253289, 0.1574803149606300301, 1.400098425196850904 ) ) ;
#30155=CARTESIAN_POINT ( 'NONE',  ( 0.7098837130843900223, -0.004402484902747280486, 1.983343479121606245 ) ) ;
#30157=CARTESIAN_POINT ( 'NONE',  ( 0.7185039370078778465, -0.06523048226348396317, 1.715059055010583089 ) ) ;
#30159=CARTESIAN_POINT ( 'NONE',  ( 1.054774247047244540, 0.07405724077823318263, 0.8120078739619844832 ) ) ;
#30163=CARTESIAN_POINT ( 'NONE',  ( 0.9873396505805591694, -0.1113553986120547346, 0.4281496061916850726 ) ) ;
#30165=CARTESIAN_POINT ( 'NONE',  ( -0.7646288533564489232, 0.1113553986120547346, 0.1722440943806619884 ) ) ;
#30166=CARTESIAN_POINT ( 'NONE',  ( 0.7495606340400177148, -0.1264236179284866091, 1.109744094434425232 ) ) ;
#30167=CARTESIAN_POINT ( 'NONE',  ( -0.8759842519685039353, 0.000000000000000000, 0.000000000000000000 ) ) ;
#30171=CARTESIAN_POINT ( 'NONE',  ( -0.8019270111902717657, 0.1787899950787401604, 0.5068897637257642197 ) ) ;
#30172=ORIENTED_EDGE ( 'NONE', *, *, #34186, .F. ) ;
#30174=CARTESIAN_POINT ( 'NONE',  ( -0.7495606340400177148, -0.1264236179284866091, 0.2829724408911185041 ) ) ;
#30175=ORIENTED_EDGE ( 'NONE', *, *, #27906, .T. ) ;
#30176=ORIENTED_EDGE ( 'NONE', *, *, #10909, .T. ) ;
#30177=CARTESIAN_POINT ( 'NONE',  ( 0.8107537697050254399, 0.1574803149606300301, 0.3371062992125987146 ) ) ;
#30180=CARTESIAN_POINT ( 'NONE',  ( -0.6971942568897637749, 2.189545951927499583E-17, 1.813484251914740053 ) ) ;
#30182=CARTESIAN_POINT ( 'NONE',  ( -0.9500414927467378812, -0.1787899950787401604, 0.4527559054580477249 ) ) ;
#30192=EDGE_CURVE ( 'NONE', #38421, #3331, #36614, .T. ) ;
#30194=CARTESIAN_POINT ( 'NONE',  ( -0.8019270111902717657, -0.1787899950787401604, 0.3248031495525355306 ) ) ;
#30195=CARTESIAN_POINT ( 'NONE',  ( -0.8759842519685039353, 0.000000000000000000, 0.000000000000000000 ) ) ;
#30197=CARTESIAN_POINT ( 'NONE',  ( -1.054774247047244540, -0.07405724077823318263, 1.481299212544662902 ) ) ;
#30203=CARTESIAN_POINT ( 'NONE',  ( 0.9873396505805591694, -0.1113553986120547346, 0.5167322834645668994 ) ) ;
#30205=CARTESIAN_POINT ( 'NONE',  ( -0.9412147342319837628, 0.1574803149606300301, 1.149114173120819427 ) ) ;
#30206=CARTESIAN_POINT ( 'NONE',  ( 0.6971942568897626646, -0.07405724077823297447, 0.5216535432533228045 ) ) ;
#30207=CARTESIAN_POINT ( 'NONE',  ( 0.6971942568897626646, -0.07405724077823297447, 0.04429133852891373180 ) ) ;
#30210=CARTESIAN_POINT ( 'NONE',  ( 0.8107537697050253289, -0.1574803149606297803, 1.916830708553890705 ) ) ;
#30211=ORIENTED_EDGE ( 'NONE', *, *, #32657, .F. ) ;
#30213=CARTESIAN_POINT ( 'NONE',  ( -0.6971942568897648851, -0.07405724077823297447, 0.9153543306548987957 ) ) ;
#30214=CARTESIAN_POINT ( 'NONE',  ( 1.033464566929133799, 0.000000000000000000, 0.9153543307086614567 ) ) ;
#30225=CARTESIAN_POINT ( 'NONE',  ( 0.9412147342319837628, 0.1574803149606300301, 1.070374015640503496 ) ) ;
#30226=FACE_OUTER_BOUND ( 'NONE', #28739, .T. ) ;
#30229=CARTESIAN_POINT ( 'NONE',  ( -1.054774247047244540, 0.07405724077823318263, 1.722440944828125930 ) ) ;
#30230=CARTESIAN_POINT ( 'NONE',  ( -0.9873396505805591694, 0.1113553986120547346, 0.6446850393700788162 ) ) ;
#30231=CARTESIAN_POINT ( 'NONE',  ( 0.6971942568897648851, 0.07405724077823318263, 1.658464566875369472 ) ) ;
#30233=CARTESIAN_POINT ( 'NONE',  ( 0.7495606340400177148, -0.1264236179284866091, 0.2878937007336381804 ) ) ;
#30234=CARTESIAN_POINT ( 'NONE',  ( -0.7495606340400177148, 0.1264236179284866091, 1.375492125930488196 ) ) ;
#30235=CARTESIAN_POINT ( 'NONE',  ( -0.8759842519685039353, 0.1574803149606299191, 1.505905511703495847 ) ) ;
#30236=CARTESIAN_POINT ( 'NONE',  ( -1.002407869896990045, 0.1264236179284866091, 1.247539370024976391 ) ) ;
#30237=CARTESIAN_POINT ( 'NONE',  ( -0.7495606340400177148, 0.1264236179284866091, 0.8636811023084409733 ) ) ;
#30239=CARTESIAN_POINT ( 'NONE',  ( -1.033464566929133355, 0.06523048226348168721, 1.656003936900346973 ) ) ;
#30240=CARTESIAN_POINT ( 'NONE',  ( -1.054774247047244540, -0.07405724077823318263, 1.638779527505292988 ) ) ;
#30241=CARTESIAN_POINT ( 'NONE',  ( -1.002407869896990045, -0.1264236179284866091, 0.1008858267178899676 ) ) ;
#30243=CARTESIAN_POINT ( 'NONE',  ( -0.7646288533564489232, 0.1113553986120547346, 1.599409448818897683 ) ) ;
#30245=CARTESIAN_POINT ( 'NONE',  ( 0.9500414927467377701, -0.1787899950787401604, 1.594488188922615457 ) ) ;
#30248=CARTESIAN_POINT ( 'NONE',  ( -0.7185039370078739607, 1.928577636452523993E-17, 0.4133858266641259882 ) ) ;
#30253=CARTESIAN_POINT ( 'NONE',  ( -0.8759842519685039353, 0.1787899950787401882, 1.178641732229700922 ) ) ;
#30260=CARTESIAN_POINT ( 'NONE',  ( 0.9500414927467378812, 0.1787899950787401604, 1.840551181048599938 ) ) ;
#30264=CARTESIAN_POINT ( 'NONE',  ( 0.8019270111902717657, 0.1787899950787401604, 0.7431102361667091261 ) ) ;
#30268=CARTESIAN_POINT ( 'NONE',  ( 0.7495606340400177148, 0.1264236179284866091, 1.813484251914740053 ) ) ;
#30270=CARTESIAN_POINT ( 'NONE',  ( 0.7646288533564489232, -0.1113553986120547346, 0.1131889763779527630 ) ) ;
#30275=CARTESIAN_POINT ( 'NONE',  ( 0.9500414927467378812, 0.1787899950787401604, 0.2706692912848194243 ) ) ;
#30276=CARTESIAN_POINT ( 'NONE',  ( -0.7495606340400177148, -0.1264236179284866091, 1.739665354276945131 ) ) ;
#30280=FACE_OUTER_BOUND ( 'NONE', #22885, .T. ) ;
#30281=VECTOR ( 'NONE', #45205, 39.37007874015748143 ) ;
#30283=CARTESIAN_POINT ( 'NONE',  ( -0.9500414927467378812, 0.1787899950787401604, 0.5462598424659214080 ) ) ;
#30284=CARTESIAN_POINT ( 'NONE',  ( 0.8019270111902717657, -0.1787899950787401604, 1.938976377898990799 ) ) ;
#30285=CARTESIAN_POINT ( 'NONE',  ( -1.002407869896990045, 0.1264236179284866091, 1.208169291284818980 ) ) ;
#30286=FACE_OUTER_BOUND ( 'NONE', #28245, .T. ) ;
#30288=CARTESIAN_POINT ( 'NONE',  ( -0.8759842519685039353, 0.1574803149606299191, 1.348425196742866206 ) ) ;
#30289=CARTESIAN_POINT ( 'NONE',  ( 1.054774247047244540, -0.07405724077823318263, 0.4970472440407249226 ) ) ;
#30290=CARTESIAN_POINT ( 'NONE',  ( -1.002407869896990045, 0.1264236179284866091, 0.3813976377415121966 ) ) ;
#30291=CARTESIAN_POINT ( 'NONE',  ( -1.054774247047244540, 0.07405724077823318263, 0.8513779527021426707 ) ) ;
#30292=ORIENTED_EDGE ( 'NONE', *, *, #27985, .T. ) ;
#30293=ORIENTED_EDGE ( 'NONE', *, *, #20877, .F. ) ;
#30296=CARTESIAN_POINT ( 'NONE',  ( -0.9412147342319837628, 0.1574803149606300301, 0.1353346456692913757 ) ) ;
#30298=ORIENTED_EDGE ( 'NONE', *, *, #42244, .T. ) ;
#30302=CARTESIAN_POINT ( 'NONE',  ( -1.054774247047244096, 0.000000000000000000, 0.06151574797773248782 ) ) ;
#30304=ORIENTED_EDGE ( 'NONE', *, *, #33152, .T. ) ;
#30306=CARTESIAN_POINT ( 'NONE',  ( -0.7185039370078746268, -0.06523048226347956391, 0.07135826771653554224 ) ) ;
#30310=CARTESIAN_POINT ( 'NONE',  ( 0.7108038354695511707, 0.06841997037041733232, 0.03937007863263043694 ) ) ;
#30311=CARTESIAN_POINT ( 'NONE',  ( 1.054774247047244540, -0.07405724077823318263, 1.555118110182455382 ) ) ;
#30312=CARTESIAN_POINT ( 'NONE',  ( 0.8019270111902717657, 0.1787899950787401604, 0.1919291338045042428 ) ) ;
#30314=VECTOR ( 'NONE', #15729, 39.37007874015748143 ) ;
#30320=CARTESIAN_POINT ( 'NONE',  ( -0.7495606340400177148, 0.1264236179284866091, 0.6717519684501732646 ) ) ;
#30324=DIRECTION ( 'NONE',  ( 0.000000000000000000, 1.000000000000000000, 0.000000000000000000 ) ) ;
#30326=CARTESIAN_POINT ( 'NONE',  ( 1.054774247047244540, 0.07405724077823318263, 1.328740157426552049 ) ) ;
#30327=CARTESIAN_POINT ( 'NONE',  ( 0.7495606340400177148, -0.1264236179284866091, 1.818405511757259729 ) ) ;
#30328=CARTESIAN_POINT ( 'NONE',  ( 0.6971942568897637749, 2.189545951927499583E-17, 0.2780511810485988278 ) ) ;
#30330=CARTESIAN_POINT ( 'NONE',  ( -0.8759842519685039353, -0.1574803149606299191, 1.643700787294047228 ) ) ;
#30334=CARTESIAN_POINT ( 'NONE',  ( -0.7185039370078739607, 1.928577636452523993E-17, 1.013779527559055094 ) ) ;
#30335=CARTESIAN_POINT ( 'NONE',  ( -0.7185039370078714072, 0.06523048226347728795, 1.237696850286174932 ) ) ;
#30337=CARTESIAN_POINT ( 'NONE',  ( -0.8759842519685039353, -0.1574803149606299191, 1.328740157372787278 ) ) ;
#30339=CARTESIAN_POINT ( 'NONE',  ( 0.9412147342319837628, 0.1574803149606300301, 0.7160433069790875793 ) ) ;
#30342=CARTESIAN_POINT ( 'NONE',  ( 0.8163103687857603541, 0.1681809448548153563, 0.03937007863263042307 ) ) ;
#30347=CARTESIAN_POINT ( 'NONE',  ( -0.7646288533564489232, 0.1113553986120547346, 0.8120078740157481434 ) ) ;
#30348=CARTESIAN_POINT ( 'NONE',  ( 0.7495606340400177148, 0.1264236179284866091, 1.611712598371433103 ) ) ;
#30349=CARTESIAN_POINT ( 'NONE',  ( -0.8107537697050253289, -0.1574803149606297803, 1.178641732283464583 ) ) ;
#30351=CARTESIAN_POINT ( 'NONE',  ( 1.033464566929133799, 0.000000000000000000, 0.2362204723334177248 ) ) ;
#30355=CARTESIAN_POINT ( 'NONE',  ( 0.7646288533564489232, -0.1113553986120547346, 1.323818897530267602 ) ) ;
#30356=ORIENTED_EDGE ( 'NONE', *, *, #33845, .F. ) ;
#30360=CARTESIAN_POINT ( 'NONE',  ( -0.8019270111902717657, 0.1787899950787401604, 1.338582677111590069 ) ) ;
#30364=( BOUNDED_CURVE ( )  B_SPLINE_CURVE ( 2, ( #46193, #28734, #6880, #3290, #13603, #42805, #36135, #13391, #21020 ),
 .UNSPECIFIED., .F., .T. ) 
 B_SPLINE_CURVE_WITH_KNOTS ( ( 3, 2, 2, 2, 3 ),
 ( 0.3400000000000000244, 0.3425000000000000266, 0.3449999999999999734, 0.3474999999999999756, 0.3499999999999999778 ),
 .UNSPECIFIED. ) 
 CURVE ( )  GEOMETRIC_REPRESENTATION_ITEM ( )  RATIONAL_B_SPLINE_CURVE ( ( 1.000000000000000000, 0.9238795325112869605, 1.000000000000000000, 0.9238795325112869605, 1.000000000000000000, 0.9238795325112869605, 1.000000000000000000, 0.9238795325112849621, 1.000000000000000000 ) ) 
 REPRESENTATION_ITEM ( '' )  ) ;
#30365=FACE_OUTER_BOUND ( 'NONE', #27071, .T. ) ;
#30366=CARTESIAN_POINT ( 'NONE',  ( -1.054774247047244540, 0.07405724077823318263, 0.3838582676627718127 ) ) ;
#30377=( BOUNDED_CURVE ( )  B_SPLINE_CURVE ( 2, ( #38194, #45842, #5844, #8722, #5356, #1284, #38436, #16407, #31264 ),
 .UNSPECIFIED., .F., .F. ) 
 B_SPLINE_CURVE_WITH_KNOTS ( ( 3, 2, 2, 2, 3 ),
 ( 0.3800000000000000044, 0.3825000000000000067, 0.3850000000000000089, 0.3875000000000000111, 0.3900000000000000133 ),
 .UNSPECIFIED. ) 
 CURVE ( )  GEOMETRIC_REPRESENTATION_ITEM ( )  RATIONAL_B_SPLINE_CURVE ( ( 1.000000000000000000, 0.9238795325112869605, 1.000000000000000000, 0.9238795325112869605, 1.000000000000000000, 0.9238795325112869605, 1.000000000000000000, 0.9238795325112869605, 1.000000000000000000 ) ) 
 REPRESENTATION_ITEM ( '' )  ) ;
#30378=CARTESIAN_POINT ( 'NONE',  ( -0.7646288533564489232, -0.1113553986120547346, 0.8218503937007874960 ) ) ;
#30380=CARTESIAN_POINT ( 'NONE',  ( -1.033464566929134687, 0.06523048226347956391, 1.931594488081448180 ) ) ;
#30381=CARTESIAN_POINT ( 'NONE',  ( -0.9873396505805591694, 0.1113553986120547346, 1.461614173120818760 ) ) ;
#30382=CARTESIAN_POINT ( 'NONE',  ( 0.8759842519685039353, 0.1787899950787401882, 0.9030511810485984947 ) ) ;
#30383=CARTESIAN_POINT ( 'NONE',  ( 1.054774247047244540, 0.07405724077823318263, 0.1033464566391499029 ) ) ;
#30385=CARTESIAN_POINT ( 'NONE',  ( 0.7646288533564489232, 0.1113553986120547346, 1.638779527559055316 ) ) ;
#30386=CARTESIAN_POINT ( 'NONE',  ( 0.7274018190141648965, -0.07989133380807623974, 1.984821033286637171 ) ) ;
#30391=CARTESIAN_POINT ( 'NONE',  ( 1.054774247047244540, -0.07405724077823318263, 0.8070866141194653620 ) ) ;
#30392=CARTESIAN_POINT ( 'NONE',  ( 0.9500414927467377701, 0.1787899950787401604, 1.845472440891119392 ) ) ;
#30396=CARTESIAN_POINT ( 'NONE',  ( -0.7185039370078739607, 1.928577636452523993E-17, 1.555118110128692832 ) ) ;
#30398=CARTESIAN_POINT ( 'NONE',  ( -1.033464566929134687, -0.06523048226347956391, 0.07627952745152805081 ) ) ;
#30399=CARTESIAN_POINT ( 'NONE',  ( 0.6971942568897637749, 2.189545951927499583E-17, 1.144192913332062966 ) ) ;
#30400=CARTESIAN_POINT ( 'NONE',  ( 0.7185039370078739607, 0.000000000000000000, 4.498031496062992574 ) ) ;
#30403=EDGE_CURVE ( 'NONE', #5296, #41905, #37038, .T. ) ;
#30404=CARTESIAN_POINT ( 'NONE',  ( 1.033464566929133799, 0.000000000000000000, 0.04921259842519685318 ) ) ;
#30405=CARTESIAN_POINT ( 'NONE',  ( -0.6971942568897626646, 0.07405724077823318263, 0.3149606298674962890 ) ) ;
#30406=EDGE_LOOP ( 'NONE', ( #4544, #40134, #32521, #6590 ) ) ;
#30408=CARTESIAN_POINT ( 'NONE',  ( -1.002407869896990045, 0.1264236179284866091, 1.759350393647023614 ) ) ;
#30409=CARTESIAN_POINT ( 'NONE',  ( -0.9500414927467377701, 0.1787899950787401604, 0.8562992125446617919 ) ) ;
#30411=CARTESIAN_POINT ( 'NONE',  ( -1.054774247047244540, 0.07405724077823318263, 0.4625984251430869665 ) ) ;
#30414=CARTESIAN_POINT ( 'NONE',  ( -0.7185039370078746268, 0.06523048226347956391, 0.3321850392625518844 ) ) ;
#30418=FACE_OUTER_BOUND ( 'NONE', #9357, .T. ) ;
#30419=CARTESIAN_POINT ( 'NONE',  ( -0.9873396505805591694, 0.1113553986120547346, 1.973425196742866206 ) ) ;
#30420=CARTESIAN_POINT ( 'NONE',  ( -0.6971942568897626646, 0.07405724077823318263, 0.5511811023084406402 ) ) ;
#30421=CARTESIAN_POINT ( 'NONE',  ( 0.9873396505805591694, 0.1113553986120547346, 1.186023621939716666 ) ) ;
#30427=CARTESIAN_POINT ( 'NONE',  ( 0.8759842519685039353, 0.1574803149606299191, 0.9645669291338583307 ) ) ;
#30428=CARTESIAN_POINT ( 'NONE',  ( 0.8107537697050253289, 0.1574803149606300301, 0.4552165354330702240 ) ) ;
#30430=CARTESIAN_POINT ( 'NONE',  ( -0.8107537697050253289, 0.1574803149606300301, 1.035925196742866650 ) ) ;
#30431=CARTESIAN_POINT ( 'NONE',  ( 0.6971942568897626646, 0.07405724077823318263, 0.5954724408911187261 ) ) ;
#30433=CARTESIAN_POINT ( 'NONE',  ( 0.7185039370078746268, -0.06523048226347956391, 0.3469488188976379561 ) ) ;
#30434=CARTESIAN_POINT ( 'NONE',  ( 0.7185039370078746268, 0.06523048226347956391, 1.985728346349167950 ) ) ;
#30438=CARTESIAN_POINT ( 'NONE',  ( 0.7646288533564489232, -0.1113553986120547346, 0.9005905511811023167 ) ) ;
#30439=LINE ( 'NONE', #19376, #44994 ) ;
#30442=ORIENTED_EDGE ( 'NONE', *, *, #37772, .T. ) ;
#30446=EDGE_LOOP ( 'NONE', ( #30736, #6564, #39020, #3193 ) ) ;
#30447=CARTESIAN_POINT ( 'NONE',  ( 0.7185039370078746268, 0.06523048226347956391, 1.286909448818897905 ) ) ;
#30452=CARTESIAN_POINT ( 'NONE',  ( 1.033464566929133799, 0.000000000000000000, 1.181102362097196989 ) ) ;
#30454=ORIENTED_EDGE ( 'NONE', *, *, #17254, .F. ) ;
#30456=CARTESIAN_POINT ( 'NONE',  ( -0.8019270111902717657, 0.1787899950787401604, 1.811023621993480548 ) ) ;
#30460=CARTESIAN_POINT ( 'NONE',  ( 0.8019270111902717657, -0.1787899950787401604, 0.4872047243556847929 ) ) ;
#30461=CARTESIAN_POINT ( 'NONE',  ( -0.7495606340400177148, 0.1264236179284866091, 1.414862204670645829 ) ) ;
#30463=CARTESIAN_POINT ( 'NONE',  ( -0.8019270111902716547, 0.1787899950787401604, 1.215551181048599272 ) ) ;
#30464=CARTESIAN_POINT ( 'NONE',  ( -0.6971942568897648851, 0.07405724077823318263, 0.7874015747493863238 ) ) ;
#30465=CARTESIAN_POINT ( 'NONE',  ( -0.8019270111902717657, -0.1787899950787401604, 0.9547244093950547628 ) ) ;
#30466=CARTESIAN_POINT ( 'NONE',  ( -0.8759842519685039353, 0.1787899950787401882, 0.1156496062454492185 ) ) ;
#30468=CARTESIAN_POINT ( 'NONE',  ( -1.002407869896990045, 0.1264236179284866091, 1.803641732229700700 ) ) ;
#30469=CARTESIAN_POINT ( 'NONE',  ( -0.7495606340400177148, -0.1264236179284866091, 0.1304133857730082613 ) ) ;
#30470=CARTESIAN_POINT ( 'NONE',  ( -0.9412147342319837628, -0.1574803149606297803, 1.577263779527559917 ) ) ;
#30471=CARTESIAN_POINT ( 'NONE',  ( 1.033464566929133799, 1.928577636452524610E-17, 4.498031496062992574 ) ) ;
#30472=CARTESIAN_POINT ( 'NONE',  ( 1.054774247047244540, -0.07405724077823318263, 1.638779527505292766 ) ) ;
#30474=CARTESIAN_POINT ( 'NONE',  ( -0.7185039370078739607, 0.000000000000000000, -2.869337061179095023E-17 ) ) ;
#30480=VECTOR ( 'NONE', #42739, 39.37007874015748143 ) ;
#30481=CARTESIAN_POINT ( 'NONE',  ( -0.7185039370078746268, 0.06523048226347956391, 1.286909448818897905 ) ) ;
#30486=CARTESIAN_POINT ( 'NONE',  ( 1.054774247047244540, 0.07405724077823318263, 0.8120078739619844832 ) ) ;
#30487=VECTOR ( 'NONE', #38372, 39.37007874015748143 ) ;
#30488=EDGE_CURVE ( 'NONE', #2757, #19564, #2170, .T. ) ;
#30490=CARTESIAN_POINT ( 'NONE',  ( -0.8759842519685039353, -0.1574803149606299191, 0.06889763768774861963 ) ) ;
#30491=CARTESIAN_POINT ( 'NONE',  ( 0.9412147342319837628, -0.1574803149606297803, 0.07135826760900840227 ) ) ;
#30493=ADVANCED_FACE ( 'NONE', ( #31327 ), #13344, .T. ) ;
#30494=CARTESIAN_POINT ( 'NONE',  ( 0.8759842519685039353, -0.1574803149606299191, 0.07874015748031495954 ) ) ;
#30499=CARTESIAN_POINT ( 'NONE',  ( 0.6971942568897626646, -0.07405724077823297447, 0.2854330708123783422 ) ) ;
#30500=CARTESIAN_POINT ( 'NONE',  ( -1.054774247047244540, -0.07405724077823318263, 1.830708661363559253 ) ) ;
#30502=CARTESIAN_POINT ( 'NONE',  ( -0.6971942568897637749, 2.189545951927499583E-17, 1.345964566875370139 ) ) ;
#30503=CARTESIAN_POINT ( 'NONE',  ( 0.8759842519685039353, 0.000000000000000000, 4.498031496062992574 ) ) ;
#30504=CARTESIAN_POINT ( 'NONE',  ( -0.6971942568897626646, 0.07405724077823318263, 0.5167322834108034613 ) ) ;
#30505=CARTESIAN_POINT ( 'NONE',  ( 0.8759842519685039353, -0.1787899950787401882, 0.09596456687537047170 ) ) ;
#30506=CARTESIAN_POINT ( 'NONE',  ( -1.054774247047244540, 0.07405724077823318263, 1.245078740103716886 ) ) ;
#30510=CARTESIAN_POINT ( 'NONE',  ( 0.9500414927467377701, 0.1787899950787401604, 0.4281496062454490659 ) ) ;
#30511=CARTESIAN_POINT ( 'NONE',  ( -1.054774247047244540, 0.07405724077823318263, 0.4576771653005669016 ) ) ;
#30512=CARTESIAN_POINT ( 'NONE',  ( -1.002407869896990045, -0.1264236179284866091, 0.8439960629383622681 ) ) ;
#30516=ORIENTED_EDGE ( 'NONE', *, *, #30403, .F. ) ;
#30517=CARTESIAN_POINT ( 'NONE',  ( -0.8759842519685039353, 0.1574803149606299191, 0.2952755905511810774 ) ) ;
#30518=CARTESIAN_POINT ( 'NONE',  ( -0.9500414927467377701, 0.1787899950787401604, 1.958661417269071947 ) ) ;
#30523=CARTESIAN_POINT ( 'NONE',  ( -0.9412147342319837628, -0.1574803149606297803, 0.3174212598425196763 ) ) ;
#30529=LINE ( 'NONE', #45089, #908 ) ;
#30530=VERTEX_POINT ( 'NONE', #23423 ) ;
#30534=CARTESIAN_POINT ( 'NONE',  ( -0.7185039370078746268, 0.06523048226347956391, 1.444389763779527991 ) ) ;
#30535=CARTESIAN_POINT ( 'NONE',  ( 0.6971942568897648851, 0.07405724077823318263, 1.614173228292692386 ) ) ;
#30536=CARTESIAN_POINT ( 'NONE',  ( 1.054774247047244540, -0.07405724077823318263, 0.1771653542769450751 ) ) ;
#30539=CARTESIAN_POINT ( 'NONE',  ( -0.9412147342319837628, 0.1574803149606300301, 1.739665354223181470 ) ) ;
#30541=EDGE_CURVE ( 'NONE', #3387, #32389, #22057, .T. ) ;
#30542=CARTESIAN_POINT ( 'NONE',  ( -1.054774247047244540, 0.07405724077823318263, 0.6200787401037166635 ) ) ;
#30543=CARTESIAN_POINT ( 'NONE',  ( -0.7646288533564489232, -0.1113553986120547346, 1.284448818790110192 ) ) ;
#30545=CARTESIAN_POINT ( 'NONE',  ( 0.7185039370078739607, 1.928577636452523993E-17, 0.3838582677165354173 ) ) ;
#30547=DIRECTION ( 'NONE',  ( 0.000000000000000000, 0.000000000000000000, -1.000000000000000000 ) ) ;
#30550=CARTESIAN_POINT ( 'NONE',  ( 0.6971942568897648851, 0.07405724077823318263, 1.771653543253322249 ) ) ;
#30551=CARTESIAN_POINT ( 'NONE',  ( 1.054774247047244540, 0.07405724077823318263, 0.3001968503399373711 ) ) ;
#30555=EDGE_CURVE ( 'NONE', #38458, #14046, #23648, .T. ) ;
#30556=CARTESIAN_POINT ( 'NONE',  ( -1.033464566929134687, -0.06523048226347956391, 1.454232283357038691 ) ) ;
#30557=LINE ( 'NONE', #27442, #7591 ) ;
#30560=CARTESIAN_POINT ( 'NONE',  ( 0.8759842519685039353, 0.1787899950787401882, 0.5044291338045039375 ) ) ;
#30562=CARTESIAN_POINT ( 'NONE',  ( -0.7185039370078739607, 1.928577636452523993E-17, 1.594488188868850242 ) ) ;
#30564=CARTESIAN_POINT ( 'NONE',  ( 0.9412147342319837628, 0.1574803149606300301, 0.7554133857192455448 ) ) ;
#30570=CARTESIAN_POINT ( 'NONE',  ( -0.9873396505805591694, 0.1113553986120547346, 0.5954724408373543998 ) ) ;
#30572=CARTESIAN_POINT ( 'NONE',  ( 0.8019270111902717657, -0.1787899950787401604, 1.624015747977732849 ) ) ;
#30573=CARTESIAN_POINT ( 'NONE',  ( -0.8107537697050253289, 0.1574803149606300301, 1.281988188976378895 ) ) ;
#30574=CARTESIAN_POINT ( 'NONE',  ( 0.8107537697050254399, 0.1574803149606300301, 0.2485236219397169988 ) ) ;
#30576=CARTESIAN_POINT ( 'NONE',  ( 0.7646288533564489232, -0.1113553986120547346, 1.363188976270427455 ) ) ;
#30578=EDGE_LOOP ( 'NONE', ( #247, #46461, #11469, #22354 ) ) ;
#30580=CARTESIAN_POINT ( 'NONE',  ( -0.7495606340400177148, -0.1264236179284866091, 1.582185039316315045 ) ) ;
#30582=CARTESIAN_POINT ( 'NONE',  ( -1.054774247047244540, 0.07405724077823318263, 1.210629921206079818 ) ) ;
#30583=ORIENTED_EDGE ( 'NONE', *, *, #7103, .T. ) ;
#30586=AXIS2_PLACEMENT_3D ( 'NONE', #15927, #37721, #41271 ) ;
#30587=CARTESIAN_POINT ( 'NONE',  ( -0.6971942568897637749, 2.189545951927499583E-17, 0.3223425196312759144 ) ) ;
#30599=CARTESIAN_POINT ( 'NONE',  ( -0.8107537697050253289, 0.1574803149606300301, 0.8882874015748027929 ) ) ;
#30602=CARTESIAN_POINT ( 'NONE',  ( 0.8759842519685039353, -0.1574803149606299191, 1.102362204724409489 ) ) ;
#30603=CARTESIAN_POINT ( 'NONE',  ( 0.9500414927467378812, 0.1787899950787401604, 0.9005905511273389896 ) ) ;
#30605=EDGE_CURVE ( 'NONE', #18242, #32474, #1828, .T. ) ;
#30606=CARTESIAN_POINT ( 'NONE',  ( 0.7185039370078739607, 1.928577636452523993E-17, 1.564960629921259949 ) ) ;
#30607=CARTESIAN_POINT ( 'NONE',  ( 0.7162330157071907788, 0.04010186468405893545, 1.982507691646586245 ) ) ;
#30609=DIRECTION ( 'NONE',  ( 1.000000000000000000, 0.000000000000000000, -1.822029033848725275E-16 ) ) ;
#30611=CARTESIAN_POINT ( 'NONE',  ( -0.9412147342319837628, 0.1574803149606300301, 1.621555118002709683 ) ) ;
#30614=CARTESIAN_POINT ( 'NONE',  ( 1.054774247047244540, -0.07405724077823318263, 0.9645669290800954476 ) ) ;
#30615=CARTESIAN_POINT ( 'NONE',  ( 1.002407869896990045, 0.1264236179284866091, 1.882381889710015743 ) ) ;
#30617=CARTESIAN_POINT ( 'NONE',  ( 0.7185039370078746268, -0.06523048226347956391, 0.2977362203649139283 ) ) ;
#30618=ORIENTED_EDGE ( 'NONE', *, *, #19305, .T. ) ;
#30619=CARTESIAN_POINT ( 'NONE',  ( 0.7185039370078746268, -0.06523048226347956391, 0.4158464565853863260 ) ) ;
#30620=CARTESIAN_POINT ( 'NONE',  ( 0.7646288533564489232, -0.1113553986120547346, 1.884842519685039353 ) ) ;
#30622=CARTESIAN_POINT ( 'NONE',  ( -0.9873396505805591694, 0.1113553986120547346, 0.1230314959554651699 ) ) ;
#30623=CARTESIAN_POINT ( 'NONE',  ( 0.7495606340400177148, 0.1264236179284866091, 1.139271653489543290 ) ) ;
#30629=CARTESIAN_POINT ( 'NONE',  ( -0.9500414927467378812, 0.1787899950787401604, 0.6594488188438737408 ) ) ;
#30630=CARTESIAN_POINT ( 'NONE',  ( -0.7185039370078739607, 1.928577636452523993E-17, 0.2657480314960630197 ) ) ;
#30631=CARTESIAN_POINT ( 'NONE',  ( -0.9500414927467378812, 0.1787899950787401604, 0.2657480314422993595 ) ) ;
#30636=CARTESIAN_POINT ( 'NONE',  ( -0.8019270111902717657, 0.1787899950787401604, 1.884842519631275026 ) ) ;
#30637=CARTESIAN_POINT ( 'NONE',  ( -1.054774247047244540, 0.07405724077823318263, 1.008858267662772423 ) ) ;
#30638=CARTESIAN_POINT ( 'NONE',  ( -0.8019270111902717657, -0.1787899950787401604, 0.4872047243556847929 ) ) ;
#30640=CARTESIAN_POINT ( 'NONE',  ( -1.033464566929133799, 0.000000000000000000, 1.663385826771653697 ) ) ;
#30643=CARTESIAN_POINT ( 'NONE',  ( 0.7646288533564489232, 0.1113553986120547346, 1.796259842519684957 ) ) ;
#30646=( BOUNDED_CURVE ( )  B_SPLINE_CURVE ( 2, ( #33329, #7889, #35784, #26369, #24758, #33091, #17327, #22747, #11748 ),
 .UNSPECIFIED., .F., .T. ) 
 B_SPLINE_CURVE_WITH_KNOTS ( ( 3, 2, 2, 2, 3 ),
 ( 0.5600000000000000533, 0.5625000000000000000, 0.5649999999999999467, 0.5675000000000000044, 0.5699999999999999512 ),
 .UNSPECIFIED. ) 
 CURVE ( )  GEOMETRIC_REPRESENTATION_ITEM ( )  RATIONAL_B_SPLINE_CURVE ( ( 1.000000000000000000, 0.9238795325112869605, 1.000000000000000000, 0.9238795325112869605, 1.000000000000000000, 0.9238795325112869605, 1.000000000000000000, 0.9238795325112829637, 1.000000000000000000 ) ) 
 REPRESENTATION_ITEM ( '' )  ) ;
#30647=CARTESIAN_POINT ( 'NONE',  ( -0.8019270111902717657, -0.1787899950787401604, 0.4822834645131655606 ) ) ;
#30648=LINE ( 'NONE', #34707, #33803 ) ;
#30652=CARTESIAN_POINT ( 'NONE',  ( -0.8019270111902716547, 0.1787899950787401604, 1.535433070812378675 ) ) ;
#30658=CARTESIAN_POINT ( 'NONE',  ( 0.9873396505805591694, 0.1113553986120547346, 0.9596456692913386544 ) ) ;
#30659=CARTESIAN_POINT ( 'NONE',  ( 0.7185039370078739607, 1.928577636452523993E-17, 0.5019685039370078705 ) ) ;
#30661=CARTESIAN_POINT ( 'NONE',  ( -0.9873396505805591694, -0.1113553986120547346, 1.176181102254677313 ) ) ;
#30662=CARTESIAN_POINT ( 'NONE',  ( 0.9500414927467378812, 0.1787899950787401604, 0.5856299212060785964 ) ) ;
#30663=CARTESIAN_POINT ( 'NONE',  ( 0.7495606340400177148, -0.1264236179284866091, 0.08612204719033110523 ) ) ;
#30665=CARTESIAN_POINT ( 'NONE',  ( -0.7185039370078746268, 0.06523048226347956391, 0.4207677165354331561 ) ) ;
#30667=CARTESIAN_POINT ( 'NONE',  ( 0.7185039370078739607, 1.928577636452523993E-17, 1.722440944881889813 ) ) ;
#30669=CARTESIAN_POINT ( 'NONE',  ( -1.054774247047244540, -0.07405724077823318263, 1.048228346402928723 ) ) ;
#30670=CARTESIAN_POINT ( 'NONE',  ( 0.8107537697050253289, -0.1574803149606297803, 1.139271653543306506 ) ) ;
#30671=CARTESIAN_POINT ( 'NONE',  ( -0.9091039872111508213, -0.1724160430076012163, 1.988772421918897360 ) ) ;
#30675=CARTESIAN_POINT ( 'NONE',  ( -0.7185039370078739607, 1.928577636452523993E-17, 1.250000000000000000 ) ) ;
#30679=CARTESIAN_POINT ( 'NONE',  ( 0.8107537697050254399, 0.1574803149606300301, 1.163877952755904666 ) ) ;
#30680=CARTESIAN_POINT ( 'NONE',  ( -0.9873396505805591694, 0.1113553986120547346, 1.117125984251968518 ) ) ;
#30681=VERTEX_POINT ( 'NONE', #8787 ) ;
#30682=CARTESIAN_POINT ( 'NONE',  ( -1.033464566929134687, 0.06523048226347956391, 1.774114173120820093 ) ) ;
#30687=CARTESIAN_POINT ( 'NONE',  ( 0.9873396505805591694, 0.1113553986120547346, 1.107283464459401623 ) ) ;
#30691=CARTESIAN_POINT ( 'NONE',  ( -1.054774247047244096, 0.000000000000000000, 1.719980314906866203 ) ) ;
#30692=CARTESIAN_POINT ( 'NONE',  ( 0.9500414927467378812, 0.1787899950787401604, 1.884842519631275026 ) ) ;
#30695=CARTESIAN_POINT ( 'NONE',  ( 0.9500414927467378812, -0.1787899950787401604, 0.4133858267178901480 ) ) ;
#30696=CARTESIAN_POINT ( 'NONE',  ( -1.002407869896990045, -0.1264236179284866091, 1.395177165300567124 ) ) ;
#30697=CARTESIAN_POINT ( 'NONE',  ( -0.7185039370078739607, 1.928577636452523993E-17, 1.791338582569637738 ) ) ;
#30698=CARTESIAN_POINT ( 'NONE',  ( -1.054774247047244096, 0.000000000000000000, 0.8882874015210394658 ) ) ;
#30699=CARTESIAN_POINT ( 'NONE',  ( -0.8019270111902717657, 0.1787899950787401604, 0.07874015742655145200 ) ) ;
#30701=CARTESIAN_POINT ( 'NONE',  ( -0.8019270111902717657, -0.1787899950787401604, 1.747047244040724312 ) ) ;
#30702=CARTESIAN_POINT ( 'NONE',  ( -0.8759842519685039353, 0.1787899950787401882, 0.07627952750529173875 ) ) ;
#30703=CARTESIAN_POINT ( 'NONE',  ( -1.033464566929134687, -0.06523048226347956391, 1.739665354330709013 ) ) ;
#30704=CARTESIAN_POINT ( 'NONE',  ( -0.9412147342319837628, -0.1574803149606297803, 0.9473425196850396857 ) ) ;
#30705=CARTESIAN_POINT ( 'NONE',  ( 1.054774247047244540, 0.07405724077823318263, 1.643700787347811998 ) ) ;
#30708=ADVANCED_FACE ( 'NONE', ( #38026 ), #5185, .T. ) ;
#30710=EDGE_CURVE ( 'NONE', #11484, #43833, #1584, .T. ) ;
#30711=CARTESIAN_POINT ( 'NONE',  ( -0.6971942568897637749, 2.189545951927499583E-17, 1.188484251914740275 ) ) ;
#30713=DIRECTION ( 'NONE',  ( 1.822029033848725028E-16, 0.000000000000000000, 1.000000000000000000 ) ) ;
#30714=CARTESIAN_POINT ( 'NONE',  ( 0.6971942568897648851, -0.07405724077823297447, 1.855314960576157635 ) ) ;
#30717=CARTESIAN_POINT ( 'NONE',  ( -0.9412147342319837628, 0.1574803149606300301, 0.7554133857192455448 ) ) ;
#30722=CARTESIAN_POINT ( 'NONE',  ( 1.054774247047244540, -0.07405724077823318263, 1.003937007820251193 ) ) ;
#30726=CARTESIAN_POINT ( 'NONE',  ( -0.7646288533564489232, 0.1113553986120547346, 1.313976377845228249 ) ) ;
#30727=CARTESIAN_POINT ( 'NONE',  ( 1.002407869896990045, -0.1264236179284866091, 1.951279527505291433 ) ) ;
#30728=ORIENTED_EDGE ( 'NONE', *, *, #6046, .F. ) ;
#30729=CARTESIAN_POINT ( 'NONE',  ( 0.8759842519685039353, 0.1574803149606299191, 0.1771653543307086520 ) ) ;
#30734=CARTESIAN_POINT ( 'NONE',  ( 0.8759842519685039353, 0.1787899950787401882, 0.3518700786863940833 ) ) ;
#30735=CARTESIAN_POINT ( 'NONE',  ( -0.6971942568897648851, -0.07405724077823297447, 1.737204724355685848 ) ) ;
#30736=ORIENTED_EDGE ( 'NONE', *, *, #36302, .F. ) ;
#30737=CARTESIAN_POINT ( 'NONE',  ( -0.7495606340400177148, -0.1264236179284866091, 1.232775590497417362 ) ) ;
#30738=CARTESIAN_POINT ( 'NONE',  ( 1.054774247047244540, 0.07405724077823318263, 1.368110236166710125 ) ) ;
#30739=CARTESIAN_POINT ( 'NONE',  ( -1.002407869896990045, 0.1264236179284866091, 0.5437992125446614589 ) ) ;
#30740=CARTESIAN_POINT ( 'NONE',  ( -0.6971942568897648851, 0.07405724077823318263, 1.220472440891118504 ) ) ;
#30743=CARTESIAN_POINT ( 'NONE',  ( 0.8019270111902716547, 0.1787899950787401604, 0.4330708660879683536 ) ) ;
#30744=CARTESIAN_POINT ( 'NONE',  ( -0.8759842519685039353, 0.1787899950787401882, 0.4256889763241890057 ) ) ;
#30745=CARTESIAN_POINT ( 'NONE',  ( -0.7495606340400177148, 0.1264236179284866091, 0.8243110235682834519 ) ) ;
#30750=ORIENTED_EDGE ( 'NONE', *, *, #2215, .T. ) ;
#30752=CARTESIAN_POINT ( 'NONE',  ( -0.9873396505805591694, -0.1113553986120547346, 0.3198818897637795700 ) ) ;
#30753=CARTESIAN_POINT ( 'NONE',  ( 1.054774247047244540, 0.07405724077823318263, 1.131889763725763887 ) ) ;
#30754=CARTESIAN_POINT ( 'NONE',  ( 1.033464566929133799, 0.000000000000000000, 1.929133858160188897 ) ) ;
#30755=LINE ( 'NONE', #12542, #31765 ) ;
#30761=CARTESIAN_POINT ( 'NONE',  ( -0.9500414927467378812, -0.1787899950787401604, 0.9251968503399374821 ) ) ;
#30765=CARTESIAN_POINT ( 'NONE',  ( -1.054774247047244540, 0.07405724077823318263, 0.02460629915883492599 ) ) ;
#30768=CARTESIAN_POINT ( 'NONE',  ( -1.033464566929133799, 1.928577636452524610E-17, 2.869337061179095023E-17 ) ) ;
#30770=ADVANCED_FACE ( 'NONE', ( #17158 ), #21216, .T. ) ;
#30772=CARTESIAN_POINT ( 'NONE',  ( 0.8019270111902717657, 0.1787899950787401604, 1.294291338528912982 ) ) ;
#30773=EDGE_CURVE ( 'NONE', #25251, #44020, #28523, .T. ) ;
#30776=CARTESIAN_POINT ( 'NONE',  ( 1.033464566929133799, 0.000000000000000000, 0.1968503935932602311 ) ) ;
#30781=CARTESIAN_POINT ( 'NONE',  ( -0.8019270111902716547, 0.1787899950787401604, 0.5905511810485987167 ) ) ;
#30783=CARTESIAN_POINT ( 'NONE',  ( 0.7185039370078739607, 0.000000000000000000, 4.498031496062992574 ) ) ;
#30788=CARTESIAN_POINT ( 'NONE',  ( 0.7495606340400177148, 0.1264236179284866091, 1.498523621993480326 ) ) ;
#30789=CARTESIAN_POINT ( 'NONE',  ( 0.9500414927467377701, -0.1787899950787401604, 1.904527559001354398 ) ) ;
#30790=CARTESIAN_POINT ( 'NONE',  ( 0.9500414927467377701, 0.1787899950787401604, 0.3051181101824569919 ) ) ;
#30794=VERTEX_POINT ( 'NONE', #10700 ) ;
#30798=CARTESIAN_POINT ( 'NONE',  ( -0.9873396505805591694, 0.1113553986120547346, 0.1722440944881890035 ) ) ;
#30799=CARTESIAN_POINT ( 'NONE',  ( 0.8759842519685039353, 0.1787899950787401882, 0.3863188975840318173 ) ) ;
#30802=CARTESIAN_POINT ( 'NONE',  ( -0.9500414927467378812, 0.1787899950787401604, 1.328740157426552049 ) ) ;
#30803=CARTESIAN_POINT ( 'NONE',  ( 1.033464566929134687, -0.06523048226347956391, 0.8243110235145187925 ) ) ;
#30806=CARTESIAN_POINT ( 'NONE',  ( 0.7495606340400177148, 0.1264236179284866091, 1.026082677111590513 ) ) ;
#30808=CARTESIAN_POINT ( 'NONE',  ( -0.7646288533564489232, 0.1113553986120547346, 0.5659448817822370081 ) ) ;
#30810=CARTESIAN_POINT ( 'NONE',  ( -1.033464566929134687, 0.06523048226347956391, 1.311515748031496509 ) ) ;
#30815=CARTESIAN_POINT ( 'NONE',  ( 0.9873396505805591694, 0.1113553986120547346, 1.382874015640503940 ) ) ;
#30819=EDGE_LOOP ( 'NONE', ( #27983, #9232, #44268, #36933 ) ) ;
#30820=CARTESIAN_POINT ( 'NONE',  ( -1.002407869896990045, -0.1264236179284866091, 1.592027559001354398 ) ) ;
#30822=CARTESIAN_POINT ( 'NONE',  ( -0.6971942568897648851, -0.07405724077823297447, 1.466535433017102763 ) ) ;
#30823=ORIENTED_EDGE ( 'NONE', *, *, #8764, .T. ) ;
#30827=AXIS2_PLACEMENT_3D ( 'NONE', #20091, #34737, #1876 ) ;
#30829=CARTESIAN_POINT ( 'NONE',  ( -0.7185039370078739607, 1.928577636452523993E-17, 0.3838582677165354173 ) ) ;
#30839=CARTESIAN_POINT ( 'NONE',  ( 0.8759842519685039353, 0.1574803149606299191, 1.751968503937007871 ) ) ;
#30842=CARTESIAN_POINT ( 'NONE',  ( -0.8019270111902716547, -0.1787899950787401604, 0.2116141731745827814 ) ) ;
#30843=CARTESIAN_POINT ( 'NONE',  ( -0.9412147342319837628, -0.1574803149606297803, 1.026082677165353729 ) ) ;
#30846=CARTESIAN_POINT ( 'NONE',  ( 1.054774247047244540, 0.07405724077823318263, 1.053149606245450176 ) ) ;
#30848=CARTESIAN_POINT ( 'NONE',  ( 0.8759842519685039353, 0.1574803149606299191, 1.555118110236220597 ) ) ;
#30849=CARTESIAN_POINT ( 'NONE',  ( 0.8622796235139646992, 0.1579280213382387443, 1.978604940233764209 ) ) ;
#30856=CARTESIAN_POINT ( 'NONE',  ( 1.002407869896990045, 0.1264236179284866091, 1.050688976324189117 ) ) ;
#30857=CARTESIAN_POINT ( 'NONE',  ( 0.8759842519685039353, -0.1787899950787401882, 1.788877952702141672 ) ) ;
#30858=CARTESIAN_POINT ( 'NONE',  ( 0.7185039370078739607, 1.928577636452523993E-17, 0.3346456691838114450 ) ) ;
#30864=CARTESIAN_POINT ( 'NONE',  ( -0.8759842519685039353, 0.1574803149606299191, 0.2460629920184571051 ) ) ;
#30866=CARTESIAN_POINT ( 'NONE',  ( 1.002407869896990045, 0.1264236179284866091, 1.247539370024976391 ) ) ;
#30870=CARTESIAN_POINT ( 'NONE',  ( -1.054774247047244540, -0.07405724077823318263, 0.6102362204186774219 ) ) ;
#30871=CARTESIAN_POINT ( 'NONE',  ( -0.8759842519685039353, 0.000000000000000000, 0.000000000000000000 ) ) ;
#30872=CARTESIAN_POINT ( 'NONE',  ( 1.033464566929133799, 0.000000000000000000, 1.811023621939716444 ) ) ;
#30876=CARTESIAN_POINT ( 'NONE',  ( -0.8019270111902717657, 0.1787899950787401604, 1.806102362150961316 ) ) ;
#30878=CARTESIAN_POINT ( 'NONE',  ( -0.8759842519685039353, -0.1787899950787401882, 0.5290354330171024300 ) ) ;
#30880=ADVANCED_FACE ( 'NONE', ( #14519 ), #29187, .T. ) ;
#30885=CARTESIAN_POINT ( 'NONE',  ( 0.7185039370078739607, 1.928577636452523993E-17, 0.4625984251968504046 ) ) ;
#30886=CARTESIAN_POINT ( 'NONE',  ( 0.7185039370078739607, 0.000000000000000000, 2.007874015640504162 ) ) ;
#30889=CARTESIAN_POINT ( 'NONE',  ( -0.8019270111902717657, -0.1787899950787401604, 0.5216535432533228045 ) ) ;
#30893=CARTESIAN_POINT ( 'NONE',  ( -1.054774247047244540, -0.07405724077823318263, 1.520669291284818758 ) ) ;
#30897=CARTESIAN_POINT ( 'NONE',  ( 0.7185039370078739607, 1.928577636452523993E-17, 0.3740157479239689664 ) ) ;
#30898=CARTESIAN_POINT ( 'NONE',  ( 0.9873396505805591694, 0.1113553986120547346, 1.028543306979086802 ) ) ;
#30899=LINE ( 'NONE', #41374, #31574 ) ;
#30901=CARTESIAN_POINT ( 'NONE',  ( -0.8759842519685039353, 0.1574803149606299191, 1.309055118002708573 ) ) ;
#30902=CARTESIAN_POINT ( 'NONE',  ( 0.8019270111902717657, 0.1787899950787401604, 0.5905511810485987167 ) ) ;
#30903=CARTESIAN_POINT ( 'NONE',  ( -0.7185039370078714072, 0.06523048226347728795, 1.631397637687748814 ) ) ;
#30906=CARTESIAN_POINT ( 'NONE',  ( 0.8107537697050253289, 0.1574803149606300301, 1.045767716535432879 ) ) ;
#30909=EDGE_CURVE ( 'NONE', #12474, #14401, #15354, .T. ) ;
#30910=( BOUNDED_CURVE ( )  B_SPLINE_CURVE ( 2, ( #5112, #45363, #30798, #1999, #12576, #32913, #44352, #33619, #26184 ),
 .UNSPECIFIED., .F., .T. ) 
 B_SPLINE_CURVE_WITH_KNOTS ( ( 3, 2, 2, 2, 3 ),
 ( 0.08000000000000000167, 0.08250000000000000389, 0.08500000000000000611, 0.08749999999999999445, 0.08999999999999999667 ),
 .UNSPECIFIED. ) 
 CURVE ( )  GEOMETRIC_REPRESENTATION_ITEM ( )  RATIONAL_B_SPLINE_CURVE ( ( 1.000000000000000000, 0.9238795325112869605, 1.000000000000000000, 0.9238795325112869605, 1.000000000000000000, 0.9238795325112869605, 1.000000000000000000, 0.9238795325112869605, 1.000000000000000000 ) ) 
 REPRESENTATION_ITEM ( '' )  ) ;
#30911=CARTESIAN_POINT ( 'NONE',  ( -0.8759842519685039353, 0.000000000000000000, 0.000000000000000000 ) ) ;
#30913=CARTESIAN_POINT ( 'NONE',  ( 0.9412147342319837628, 0.1574803149606300301, 0.5979330707586145710 ) ) ;
#30915=ORIENTED_EDGE ( 'NONE', *, *, #45532, .F. ) ;
#30916=CARTESIAN_POINT ( 'NONE',  ( 1.033464566929134687, 0.06523048226347956391, 1.154035433070866423 ) ) ;
#30918=DIRECTION ( 'NONE',  ( 1.000000000000000000, 0.000000000000000000, -1.822029033848725275E-16 ) ) ;
#30919=CARTESIAN_POINT ( 'NONE',  ( 1.033464566929133799, 0.000000000000000000, 0.9153543307086614567 ) ) ;
#30926=CARTESIAN_POINT ( 'NONE',  ( -0.7495606340400177148, -0.1264236179284866091, 1.862696850339937038 ) ) ;
#30927=CARTESIAN_POINT ( 'NONE',  ( 0.6971942568897648851, 0.07405724077823318263, 1.855314960576157635 ) ) ;
#30928=VERTEX_POINT ( 'NONE', #28444 ) ;
#30931=CARTESIAN_POINT ( 'NONE',  ( 0.6971942568897637749, 2.189545951927499583E-17, 0.4798228345919055560 ) ) ;
#30932=CARTESIAN_POINT ( 'NONE',  ( -0.8759842519685039353, -0.1787899950787401882, 1.350885826717889815 ) ) ;
#30934=CARTESIAN_POINT ( 'NONE',  ( -1.054774247047244540, -0.07405724077823318263, 0.9251968503399374821 ) ) ;
#30935=CARTESIAN_POINT ( 'NONE',  ( -0.7495606340400177148, -0.1264236179284866091, 0.1304133857730082613 ) ) ;
#30936=( BOUNDED_CURVE ( )  B_SPLINE_CURVE ( 2, ( #15120, #22522, #23004, #4288, #30235, #29766, #26857, #45020, #18919 ),
 .UNSPECIFIED., .F., .F. ) 
 B_SPLINE_CURVE_WITH_KNOTS ( ( 3, 2, 2, 2, 3 ),
 ( 0.7399999999999999911, 0.7425000000000000488, 0.7449999999999999956, 0.7475000000000000533, 0.7500000000000000000 ),
 .UNSPECIFIED. ) 
 CURVE ( )  GEOMETRIC_REPRESENTATION_ITEM ( )  RATIONAL_B_SPLINE_CURVE ( ( 1.000000000000000000, 0.9238795325112869605, 1.000000000000000000, 0.9238795325112869605, 1.000000000000000000, 0.9238795325112869605, 1.000000000000000000, 0.9238795325112829637, 1.000000000000000000 ) ) 
 REPRESENTATION_ITEM ( '' )  ) ;
#30939=CARTESIAN_POINT ( 'NONE',  ( -1.054774247047244540, 0.07405724077823318263, 1.761811023568284007 ) ) ;
#30940=CARTESIAN_POINT ( 'NONE',  ( -0.9873396505805591694, 0.1113553986120547346, 1.973425196742866206 ) ) ;
#30941=CARTESIAN_POINT ( 'NONE',  ( -0.8759842519685039353, 0.1574803149606299191, 1.673228346456693050 ) ) ;
#30943=CARTESIAN_POINT ( 'NONE',  ( 0.6971942568897648851, -0.07405724077823297447, 1.545275590497419138 ) ) ;
#30946=CARTESIAN_POINT ( 'NONE',  ( -0.9412147342319837628, 0.1574803149606300301, 1.788877952755905554 ) ) ;
#30947=EDGE_CURVE ( 'NONE', #15464, #10600, #46250, .T. ) ;
#30956=CARTESIAN_POINT ( 'NONE',  ( 0.9500414927467378812, -0.1787899950787401604, 0.8809055117572599514 ) ) ;
#30959=CARTESIAN_POINT ( 'NONE',  ( 0.9873396505805591694, 0.1113553986120547346, 0.04429133847515007855 ) ) ;
#30966=CARTESIAN_POINT ( 'NONE',  ( -0.7495606340400177148, -0.1264236179284866091, 1.897145669237574772 ) ) ;
#30968=CARTESIAN_POINT ( 'NONE',  ( -0.9500414927467378812, 0.1787899950787401604, 1.254921259788757348 ) ) ;
#30971=CARTESIAN_POINT ( 'NONE',  ( 1.054774247047244540, -0.07405724077823318263, 1.363188976324188895 ) ) ;
#30972=CARTESIAN_POINT ( 'NONE',  ( -0.9500414927467378812, 0.1787899950787401604, 0.5068897637257642197 ) ) ;
#30973=CARTESIAN_POINT ( 'NONE',  ( -1.054774247047244540, 0.07405724077823318263, 1.284448818843874740 ) ) ;
#30976=CARTESIAN_POINT ( 'NONE',  ( 0.6971942568897648851, 0.07405724077823318263, 0.6348425196312760255 ) ) ;
#30977=CARTESIAN_POINT ( 'NONE',  ( -1.002407869896990045, -0.1264236179284866091, 0.5290354330171024300 ) ) ;
#30979=CARTESIAN_POINT ( 'NONE',  ( 1.033464566929133799, 0.000000000000000000, 0.03937007863263043694 ) ) ;
#30982=CARTESIAN_POINT ( 'NONE',  ( -1.033464566929134687, 0.06523048226347956391, 0.3666338582677165503 ) ) ;
#30983=CARTESIAN_POINT ( 'NONE',  ( 0.6971942568897648851, 0.07405724077823318263, 1.146653543253323582 ) ) ;
#30985=CARTESIAN_POINT ( 'NONE',  ( 0.7646288533564489232, 0.1113553986120547346, 1.313976377845228249 ) ) ;
#30987=EDGE_LOOP ( 'NONE', ( #21471, #10004, #1060, #5751 ) ) ;
#30988=ADVANCED_FACE ( 'NONE', ( #4578 ), #34102, .T. ) ;
#30989=CARTESIAN_POINT ( 'NONE',  ( -0.7646288533564489232, -0.1113553986120547346, 1.294291338582677309 ) ) ;
#30990=CARTESIAN_POINT ( 'NONE',  ( -0.6971942568897648851, -0.07405724077823297447, 0.9940944881352130613 ) ) ;
#30991=CARTESIAN_POINT ( 'NONE',  ( -1.054774247047244540, 0.07405724077823318263, 0.1820866141194649179 ) ) ;
#30998=CARTESIAN_POINT ( 'NONE',  ( 0.6971942568897637749, 2.189545951927499583E-17, 1.301673228292692830 ) ) ;
#31004=CARTESIAN_POINT ( 'NONE',  ( 0.8019270111902717657, -0.1787899950787401604, 0.4429133857730075952 ) ) ;
#31005=CARTESIAN_POINT ( 'NONE',  ( -0.7495606340400177148, 0.1264236179284866091, 0.7898622046706456068 ) ) ;
#31007=CARTESIAN_POINT ( 'NONE',  ( 0.8759842519685039353, 0.000000000000000000, 4.498031496062992574 ) ) ;
#31009=CARTESIAN_POINT ( 'NONE',  ( -0.7541062341187345641, -0.1190279680630223907, 1.985685656426464440 ) ) ;
#31015=CARTESIAN_POINT ( 'NONE',  ( 0.9500414927467378812, 0.1787899950787401604, 1.491141732229701367 ) ) ;
#31016=CARTESIAN_POINT ( 'NONE',  ( 0.9500414927467377701, -0.1787899950787401604, 1.786417322780882388 ) ) ;
#31017=CARTESIAN_POINT ( 'NONE',  ( 0.6971942568897648851, 0.07405724077823318263, 0.4330708660879683536 ) ) ;
#31021=ADVANCED_FACE ( 'NONE', ( #30286 ), #32988, .T. ) ;
#31026=CARTESIAN_POINT ( 'NONE',  ( 1.002407869896990045, -0.1264236179284866091, 0.4896653542769449086 ) ) ;
#31028=CARTESIAN_POINT ( 'NONE',  ( 0.8019270111902716547, -0.1787899950787401604, 1.309055118056473122 ) ) ;
#31030=CARTESIAN_POINT ( 'NONE',  ( 1.033464566929134687, 0.06523048226347956391, 0.2091535433070865757 ) ) ;
#31031=CARTESIAN_POINT ( 'NONE',  ( 0.8759842519685039353, 0.1574803149606299191, 0.8366141731208189825 ) ) ;
#31032=VERTEX_POINT ( 'NONE', #37424 ) ;
#31033=EDGE_CURVE ( 'NONE', #44561, #28497, #21944, .T. ) ;
#31034=CARTESIAN_POINT ( 'NONE',  ( 0.8759842519685039353, 0.1787899950787401882, 0.9424212597887559051 ) ) ;
#31035=ORIENTED_EDGE ( 'NONE', *, *, #5081, .T. ) ;
#31037=CARTESIAN_POINT ( 'NONE',  ( -0.7185039370078739607, 1.928577636452523993E-17, 0.5708661416247566844 ) ) ;
#31038=CARTESIAN_POINT ( 'NONE',  ( 1.033464566929133799, 0.000000000000000000, 0.08858267716535432601 ) ) ;
#31039=CARTESIAN_POINT ( 'NONE',  ( -0.8759842519685039353, 0.1574803149606299191, 1.318897637795275690 ) ) ;
#31040=CARTESIAN_POINT ( 'NONE',  ( -0.7185039370078746268, -0.06523048226347956391, 1.045767716427905114 ) ) ;
#31042=CARTESIAN_POINT ( 'NONE',  ( -0.7185039370078739607, 1.928577636452523993E-17, 0.4232283464566928832 ) ) ;
#31043=CARTESIAN_POINT ( 'NONE',  ( 0.6971942568897626646, 0.07405724077823318263, 0.1230314960092287191 ) ) ;
#31044=CARTESIAN_POINT ( 'NONE',  ( 0.7185039370078739607, 1.928577636452523993E-17, 1.397637795168062969 ) ) ;
#31047=( BOUNDED_CURVE ( )  B_SPLINE_CURVE ( 2, ( #3351, #32616, #43112, #25161, #10318, #10561, #13660, #31898, #25416 ),
 .UNSPECIFIED., .F., .T. ) 
 B_SPLINE_CURVE_WITH_KNOTS ( ( 3, 2, 2, 2, 3 ),
 ( 0.7600000000000000089, 0.7624999999999999556, 0.7650000000000000133, 0.7674999999999999600, 0.7700000000000000178 ),
 .UNSPECIFIED. ) 
 CURVE ( )  GEOMETRIC_REPRESENTATION_ITEM ( )  RATIONAL_B_SPLINE_CURVE ( ( 1.000000000000000000, 0.9238795325112869605, 1.000000000000000000, 0.9238795325112869605, 1.000000000000000000, 0.9238795325112869605, 1.000000000000000000, 0.9238795325112869605, 1.000000000000000000 ) ) 
 REPRESENTATION_ITEM ( '' )  ) ;
#31049=ORIENTED_EDGE ( 'NONE', *, *, #12485, .T. ) ;
#31050=CARTESIAN_POINT ( 'NONE',  ( 1.054774247047244096, 0.000000000000000000, 0.6963582676627716461 ) ) ;
#31051=CARTESIAN_POINT ( 'NONE',  ( 1.054774247047244540, -0.07405724077823318263, 0.9694881889226145688 ) ) ;
#31052=CARTESIAN_POINT ( 'NONE',  ( -0.9500414927467377701, -0.1787899950787401604, 1.550196850339938148 ) ) ;
#31056=CARTESIAN_POINT ( 'NONE',  ( -0.8107537697050254399, 0.1574803149606300301, 0.2485236219397169988 ) ) ;
#31057=CARTESIAN_POINT ( 'NONE',  ( 0.7646288533564489232, 0.1113553986120547346, 1.865157480207432883 ) ) ;
#31059=CARTESIAN_POINT ( 'NONE',  ( -0.9412147342319837628, -0.1574803149606297803, 1.882381889656251639 ) ) ;
#31061=ORIENTED_EDGE ( 'NONE', *, *, #10849, .T. ) ;
#31064=AXIS2_PLACEMENT_3D ( 'NONE', #13944, #10363, #3392 ) ;
#31066=CARTESIAN_POINT ( 'NONE',  ( -0.8759842519685039353, -0.1574803149606299191, 1.407480314853102321 ) ) ;
#31067=CARTESIAN_POINT ( 'NONE',  ( -0.7185039370078746268, 0.06523048226347956391, 0.9227362203649142058 ) ) ;
#31068=CARTESIAN_POINT ( 'NONE',  ( 0.9412147342319837628, -0.1574803149606297803, 1.892224409448819644 ) ) ;
#31071=CARTESIAN_POINT ( 'NONE',  ( -0.9500414927467377701, 0.1787899950787401604, 0.3887795275052913224 ) ) ;
#31072=CARTESIAN_POINT ( 'NONE',  ( -0.7646288533564489232, -0.1113553986120547346, 0.9793307086614173596 ) ) ;
#31074=CARTESIAN_POINT ( 'NONE',  ( 1.054774247047244540, -0.07405724077823318263, 1.008858267662772423 ) ) ;
#31075=CARTESIAN_POINT ( 'NONE',  ( 0.9500414927467377701, 0.1787899950787401604, 0.1870078739619845110 ) ) ;
#31077=CARTESIAN_POINT ( 'NONE',  ( -0.9873396505805591694, 0.1113553986120547346, 0.6348425195775118102 ) ) ;
#31079=CARTESIAN_POINT ( 'NONE',  ( 1.033464566929134687, -0.06523048226347956391, 1.621555118110237004 ) ) ;
#31080=CARTESIAN_POINT ( 'NONE',  ( 0.7579794631033002217, 0.1108770549927829419, 1.980899420926319321 ) ) ;
#31082=DIRECTION ( 'NONE',  ( 1.000000000000000000, 0.000000000000000000, -1.822029033848725275E-16 ) ) ;
#31084=EDGE_CURVE ( 'NONE', #5177, #6537, #41903, .T. ) ;
#31086=CARTESIAN_POINT ( 'NONE',  ( 1.002407869896990045, -0.1264236179284866091, 1.040846456639149764 ) ) ;
#31087=CARTESIAN_POINT ( 'NONE',  ( 0.6971942568897637749, 2.189545951927499583E-17, 1.897145669237574772 ) ) ;
#31088=CARTESIAN_POINT ( 'NONE',  ( 0.8759842519685039353, 0.1574803149606299191, 0.3248031494987720369 ) ) ;
#31091=ADVANCED_FACE ( 'NONE', ( #37672 ), #19447, .T. ) ;
#31095=CARTESIAN_POINT ( 'NONE',  ( -0.7185039370078746268, -0.06523048226347956391, 0.1796259841444415029 ) ) ;
#31096=CARTESIAN_POINT ( 'NONE',  ( 0.8019270111902717657, -0.1787899950787401604, 1.309055118056472899 ) ) ;
#31101=CARTESIAN_POINT ( 'NONE',  ( -0.8759842519685039353, 0.1787899950787401882, 0.5831692912848189803 ) ) ;
#31102=CARTESIAN_POINT ( 'NONE',  ( 1.033464566929134687, -0.06523048226347956391, 1.375492125876724980 ) ) ;
#31103=DIRECTION ( 'NONE',  ( 0.000000000000000000, 0.000000000000000000, -1.000000000000000000 ) ) ;
#31105=CARTESIAN_POINT ( 'NONE',  ( -0.8019270111902717657, 0.1787899950787401604, 0.9448818897100165204 ) ) ;
#31106=CARTESIAN_POINT ( 'NONE',  ( -1.054774247047244096, 0.000000000000000000, 1.911909448765133801 ) ) ;
#31108=CARTESIAN_POINT ( 'NONE',  ( -0.8759842519685039353, -0.1787899950787401882, 0.6077755904974173617 ) ) ;
#31118=LINE ( 'NONE', #5201, #32598 ) ;
#31119=CARTESIAN_POINT ( 'NONE',  ( -0.6971942568897626646, 0.07405724077823318263, 0.4330708660879683536 ) ) ;
#31120=CARTESIAN_POINT ( 'NONE',  ( -0.7646288533564489232, -0.1113553986120547346, 0.3887795275590551491 ) ) ;
#31121=ORIENTED_EDGE ( 'NONE', *, *, #18710, .T. ) ;
#31122=CARTESIAN_POINT ( 'NONE',  ( -0.6971942568897648851, 0.07405724077823318263, 1.619094488135213838 ) ) ;
#31124=CARTESIAN_POINT ( 'NONE',  ( -0.7185039370078739607, 1.928577636452523993E-17, 1.761811023622047223 ) ) ;
#31126=CYLINDRICAL_SURFACE ( 'NONE', #40722, 0.1574803149606299191 ) ;
#31129=CARTESIAN_POINT ( 'NONE',  ( -0.9873396505805591694, 0.1113553986120547346, 1.304133858160188897 ) ) ;
#31131=CARTESIAN_POINT ( 'NONE',  ( 0.9412147342319837628, -0.1574803149606297803, 1.764271653435779852 ) ) ;
#31135=CARTESIAN_POINT ( 'NONE',  ( -0.9500414927467377701, 0.1787899950787401604, 1.097440944828127041 ) ) ;
#31136=CARTESIAN_POINT ( 'NONE',  ( 0.9412147342319837628, 0.1574803149606300301, 1.119586614173229577 ) ) ;
#31139=CARTESIAN_POINT ( 'NONE',  ( -0.7185039370078739607, 1.928577636452523993E-17, 0.7283464565853858819 ) ) ;
#31146=CARTESIAN_POINT ( 'NONE',  ( 0.6971942568897626646, 0.07405724077823318263, 0.9055118109698585549 ) ) ;
#31154=CARTESIAN_POINT ( 'NONE',  ( 0.7646288533564489232, -0.1113553986120547346, 1.245078740049952559 ) ) ;
#31156=ORIENTED_EDGE ( 'NONE', *, *, #37940, .F. ) ;
#31158=CARTESIAN_POINT ( 'NONE',  ( -0.7495606340400177148, -0.1264236179284866091, 1.941437007820252081 ) ) ;
#31159=CARTESIAN_POINT ( 'NONE',  ( 0.8019270111902717657, 0.1787899950787401604, 1.811023621993480548 ) ) ;
#31163=CARTESIAN_POINT ( 'NONE',  ( 0.9500414927467378812, 0.1787899950787401604, 0.5068897637257642197 ) ) ;
#31164=CARTESIAN_POINT ( 'NONE',  ( -0.9500414927467378812, 0.1787899950787401604, 1.407480314906865981 ) ) ;
#31166=CARTESIAN_POINT ( 'NONE',  ( -0.7495606340400177148, -0.1264236179284866091, 0.2878937007336381804 ) ) ;
#31168=CARTESIAN_POINT ( 'NONE',  ( -1.002407869896990045, -0.1264236179284866091, 1.754429133804503715 ) ) ;
#31169=CARTESIAN_POINT ( 'NONE',  ( -1.033464566929133799, 0.000000000000000000, 1.968503936900346529 ) ) ;
#31171=CARTESIAN_POINT ( 'NONE',  ( -0.7185039370078746268, -0.06523048226347956391, 1.803641732283465693 ) ) ;
#31173=CARTESIAN_POINT ( 'NONE',  ( 0.9500414927467377701, 0.1787899950787401604, 1.687992125930489307 ) ) ;
#31175=CARTESIAN_POINT ( 'NONE',  ( -1.033464566929134687, -0.06523048226347956391, 1.503444881889764995 ) ) ;
#31184=CARTESIAN_POINT ( 'NONE',  ( -0.7185039370078746268, 0.06523048226347956391, 0.8046259841444418637 ) ) ;
#31188=CARTESIAN_POINT ( 'NONE',  ( 0.7495606340400177148, 0.1264236179284866091, 0.9030511810485984947 ) ) ;
#31189=EDGE_CURVE ( 'NONE', #16139, #9851, #8618, .T. ) ;
#31191=CARTESIAN_POINT ( 'NONE',  ( -0.7185039370078739607, 1.928577636452523993E-17, 1.131889763779527547 ) ) ;
#31193=CARTESIAN_POINT ( 'NONE',  ( 0.9500414927467378812, -0.1787899950787401604, 1.948818897584033927 ) ) ;
#31194=FACE_OUTER_BOUND ( 'NONE', #42896, .T. ) ;
#31199=( BOUNDED_CURVE ( )  B_SPLINE_CURVE ( 2, ( #17178, #25573, #29203, #31813, #35639, #39666, #2779, #46872, #46400 ),
 .UNSPECIFIED., .F., .T. ) 
 B_SPLINE_CURVE_WITH_KNOTS ( ( 3, 2, 2, 2, 3 ),
 ( 0.02000000000000000042, 0.02249999999999999917, 0.02500000000000000139, 0.02750000000000000014, 0.02999999999999999889 ),
 .UNSPECIFIED. ) 
 CURVE ( )  GEOMETRIC_REPRESENTATION_ITEM ( )  RATIONAL_B_SPLINE_CURVE ( ( 1.000000000000000000, 0.9238795325112869605, 1.000000000000000000, 0.9238795325112869605, 1.000000000000000000, 0.9238795325112869605, 1.000000000000000000, 0.9238795325112869605, 1.000000000000000000 ) ) 
 REPRESENTATION_ITEM ( '' )  ) ;
#31200=CARTESIAN_POINT ( 'NONE',  ( 1.002407869896990045, -0.1264236179284866091, 0.3764763778989925203 ) ) ;
#31201=CARTESIAN_POINT ( 'NONE',  ( -0.9500414927467378812, -0.1787899950787401604, 1.943897637741510254 ) ) ;
#31203=CARTESIAN_POINT ( 'NONE',  ( -0.8759842519685039353, -0.1787899950787401882, 1.434547244040724534 ) ) ;
#31204=CARTESIAN_POINT ( 'NONE',  ( -0.7646288533564489232, 0.1113553986120547346, 1.323818897637795367 ) ) ;
#31205=CARTESIAN_POINT ( 'NONE',  ( 0.6971942568897637749, 2.189545951927499583E-17, 1.385334645615527549 ) ) ;
#31208=CARTESIAN_POINT ( 'NONE',  ( 0.8759842519685039353, 0.1787899950787401882, 0.1156496062454492185 ) ) ;
#31209=CARTESIAN_POINT ( 'NONE',  ( -0.7495606340400177148, 0.1264236179284866091, 1.139271653489543290 ) ) ;
#31211=CARTESIAN_POINT ( 'NONE',  ( 0.6971942568897648851, -0.07405724077823297447, 0.6003937007336389575 ) ) ;
#31212=CARTESIAN_POINT ( 'NONE',  ( -0.6971942568897648851, 0.07405724077823318263, 0.5118110235682844511 ) ) ;
#31215=CARTESIAN_POINT ( 'NONE',  ( -0.9412147342319837628, -0.1574803149606297803, 0.3174212598425196763 ) ) ;
#31216=CARTESIAN_POINT ( 'NONE',  ( 0.6971942568897648851, 0.07405724077823318263, 1.343503936954111966 ) ) ;
#31219=CARTESIAN_POINT ( 'NONE',  ( -0.9412147342319837628, -0.1574803149606297803, 0.6323818897637792924 ) ) ;
#31220=CARTESIAN_POINT ( 'NONE',  ( -0.6971942568897637749, 2.189545951927499583E-17, 0.9916338582139527791 ) ) ;
#31224=CARTESIAN_POINT ( 'NONE',  ( -0.8107537697050254399, 0.1574803149606300301, 0.1697834644594022058 ) ) ;
#31227=CARTESIAN_POINT ( 'NONE',  ( 0.8019270111902717657, 0.1787899950787401604, 1.333661417269071059 ) ) ;
#31232=CARTESIAN_POINT ( 'NONE',  ( 1.033464566929134687, 0.06523048226347956391, 1.813484251860976171 ) ) ;
#31233=CARTESIAN_POINT ( 'NONE',  ( 0.8759842519685039353, -0.1787899950787401882, 1.626476377898992132 ) ) ;
#31239=CARTESIAN_POINT ( 'NONE',  ( 0.8019270111902717657, 0.1787899950787401604, 0.4675196849856070869 ) ) ;
#31240=CARTESIAN_POINT ( 'NONE',  ( -0.8759842519685039353, -0.1787899950787401882, 0.8046259841982047467 ) ) ;
#31241=EDGE_CURVE ( 'NONE', #5433, #461, #25438, .T. ) ;
#31245=CARTESIAN_POINT ( 'NONE',  ( -0.7640572627416960527, -0.1288658717550650867, 1.985929485999813338 ) ) ;
#31247=CARTESIAN_POINT ( 'NONE',  ( 1.054774247047244540, 0.07405724077823318263, 1.564960629867495845 ) ) ;
#31248=CARTESIAN_POINT ( 'NONE',  ( 0.8019270111902716547, 0.1787899950787401604, 1.766732283410803239 ) ) ;
#31249=CARTESIAN_POINT ( 'NONE',  ( 0.7495606340400177148, -0.1264236179284866091, 0.4010826771115905687 ) ) ;
#31251=CARTESIAN_POINT ( 'NONE',  ( 0.7185039370078739607, 1.928577636452523993E-17, 0.1377952754830242266 ) ) ;
#31253=CARTESIAN_POINT ( 'NONE',  ( 0.7185039370078739607, 1.928577636452523993E-17, 0.8464566928058583350 ) ) ;
#31256=CARTESIAN_POINT ( 'NONE',  ( 1.054774247047244096, 0.000000000000000000, 0.3764763778989925203 ) ) ;
#31257=CARTESIAN_POINT ( 'NONE',  ( 0.8281979645144629254, -0.1535074065110398345, 0.03937341667646054172 ) ) ;
#31258=CARTESIAN_POINT ( 'NONE',  ( 0.9873396505805591694, -0.1113553986120547346, 1.963582677057826853 ) ) ;
#31259=EDGE_CURVE ( 'NONE', #23819, #13130, #38579, .T. ) ;
#31260=LINE ( 'NONE', #10079, #33994 ) ;
#31261=CARTESIAN_POINT ( 'NONE',  ( -1.054774247047244096, 0.000000000000000000, 1.518208661363559031 ) ) ;
#31262=CARTESIAN_POINT ( 'NONE',  ( 0.9873396505805591694, -0.1113553986120547346, 0.8218503935932598425 ) ) ;
#31263=ORIENTED_EDGE ( 'NONE', *, *, #36987, .T. ) ;
#31264=CARTESIAN_POINT ( 'NONE',  ( -0.7185039370078739607, 1.928577636452523993E-17, 0.8070866140657008136 ) ) ;
#31265=CARTESIAN_POINT ( 'NONE',  ( 0.9500414927467378812, -0.1787899950787401604, 1.003937007820251193 ) ) ;
#31268=CARTESIAN_POINT ( 'NONE',  ( -0.9873396505805591694, -0.1113553986120547346, 0.5068897636720007815 ) ) ;
#31269=CARTESIAN_POINT ( 'NONE',  ( -0.9412147342319837628, 0.1574803149606300301, 0.8046259842519695171 ) ) ;
#31270=CARTESIAN_POINT ( 'NONE',  ( 0.8759842519685039353, -0.1787899950787401882, 1.665846456639149764 ) ) ;
#31271=CARTESIAN_POINT ( 'NONE',  ( -1.033464566929133799, 0.000000000000000000, 1.387795275590551158 ) ) ;
#31275=CARTESIAN_POINT ( 'NONE',  ( 0.8759842519685039353, 0.1787899950787401882, 0.07627952750529173875 ) ) ;
#31276=CARTESIAN_POINT ( 'NONE',  ( 0.8107537697050253289, 0.1574803149606300301, 1.468996062884598830 ) ) ;
#31278=VERTEX_POINT ( 'NONE', #11482 ) ;
#31280=CARTESIAN_POINT ( 'NONE',  ( 0.8107537697050254399, -0.1574803149606297803, 0.5880905511811019837 ) ) ;
#31281=CARTESIAN_POINT ( 'NONE',  ( -0.9500414927467377701, 0.1787899950787401604, 1.683070866087970074 ) ) ;
#31283=ORIENTED_EDGE ( 'NONE', *, *, #6978, .T. ) ;
#31290=ORIENTED_EDGE ( 'NONE', *, *, #14666, .T. ) ;
#31294=CARTESIAN_POINT ( 'NONE',  ( -0.8759842519685039353, -0.1574803149606299191, 0.4232283463491653963 ) ) ;
#31295=CARTESIAN_POINT ( 'NONE',  ( 0.9412147342319837628, 0.1574803149606300301, 1.749507874015747699 ) ) ;
#31296=EDGE_CURVE ( 'NONE', #42583, #24091, #26694, .T. ) ;
#31299=CARTESIAN_POINT ( 'NONE',  ( -0.7495606340400177148, -0.1264236179284866091, 0.3666338582139531677 ) ) ;
#31300=CARTESIAN_POINT ( 'NONE',  ( -0.7646288533564489232, 0.1113553986120547346, 1.048228346456692828 ) ) ;
#31302=CARTESIAN_POINT ( 'NONE',  ( -0.7124115563218176295, 0.02371305101100566748, 1.982827744692199801 ) ) ;
#31304=CARTESIAN_POINT ( 'NONE',  ( 1.054774247047244540, 0.07405724077823318263, 1.013779527505291878 ) ) ;
#31305=CARTESIAN_POINT ( 'NONE',  ( 0.9500414927467377701, -0.1787899950787401604, 1.392716535379308285 ) ) ;
#31306=CARTESIAN_POINT ( 'NONE',  ( 0.7495606340400177148, -0.1264236179284866091, 0.2436023621509610382 ) ) ;
#31308=CARTESIAN_POINT ( 'NONE',  ( 0.9412147342319837628, -0.1574803149606297803, 1.577263779527559917 ) ) ;
#31309=CARTESIAN_POINT ( 'NONE',  ( 1.033464566929133799, 0.000000000000000000, 1.427165354330708569 ) ) ;
#31310=CARTESIAN_POINT ( 'NONE',  ( -0.8639857840511040443, 0.1575694914283039538, 1.978574434837644835 ) ) ;
#31314=( BOUNDED_CURVE ( )  B_SPLINE_CURVE ( 2, ( #2550, #15078, #13696, #42664, #11243, #6497, #22238, #4022, #9880 ),
 .UNSPECIFIED., .F., .T. ) 
 B_SPLINE_CURVE_WITH_KNOTS ( ( 3, 2, 2, 2, 3 ),
 ( 0.4000000000000000222, 0.4025000000000000244, 0.4050000000000000266, 0.4074999999999999734, 0.4099999999999999756 ),
 .UNSPECIFIED. ) 
 CURVE ( )  GEOMETRIC_REPRESENTATION_ITEM ( )  RATIONAL_B_SPLINE_CURVE ( ( 1.000000000000000000, 0.9238795325112869605, 1.000000000000000000, 0.9238795325112869605, 1.000000000000000000, 0.9238795325112869605, 1.000000000000000000, 0.9238795325112849621, 1.000000000000000000 ) ) 
 REPRESENTATION_ITEM ( '' )  ) ;
#31316=CARTESIAN_POINT ( 'NONE',  ( 0.9500414927467377701, -0.1787899950787401604, 0.9990157479777320715 ) ) ;
#31317=CARTESIAN_POINT ( 'NONE',  ( 1.033464566929134687, -0.06523048226347956391, 0.3912401573727880555 ) ) ;
#31320=CARTESIAN_POINT ( 'NONE',  ( 0.9976899381744536166, 0.1122945889148146276, 0.03936994490810627467 ) ) ;
#31322=CARTESIAN_POINT ( 'NONE',  ( -0.8759842519685039353, -0.1574803149606299191, 0.3051181101286932762 ) ) ;
#31324=CARTESIAN_POINT ( 'NONE',  ( 0.8019270111902717657, 0.1787899950787401604, 1.333661417269071059 ) ) ;
#31327=FACE_OUTER_BOUND ( 'NONE', #46471, .T. ) ;
#31328=CARTESIAN_POINT ( 'NONE',  ( -0.8759842519685039353, 0.1787899950787401882, 0.6619094487651338010 ) ) ;
#31329=CARTESIAN_POINT ( 'NONE',  ( 0.9412147342319837628, -0.1574803149606297803, 1.370570866034205748 ) ) ;
#31332=CARTESIAN_POINT ( 'NONE',  ( -1.054774247047244096, 0.000000000000000000, 1.990649606245448844 ) ) ;
#31335=ORIENTED_EDGE ( 'NONE', *, *, #38696, .F. ) ;
#31339=ORIENTED_EDGE ( 'NONE', *, *, #17744, .T. ) ;
#31342=CARTESIAN_POINT ( 'NONE',  ( -0.9873396505805591694, -0.1113553986120547346, 0.6643700786326299790 ) ) ;
#31347=CARTESIAN_POINT ( 'NONE',  ( -0.8019270111902717657, 0.1787899950787401604, 0.5068897637257642197 ) ) ;
#31350=VERTEX_POINT ( 'NONE', #24984 ) ;
#31352=CARTESIAN_POINT ( 'NONE',  ( -1.002407869896990045, -0.1264236179284866091, 1.715059055064346527 ) ) ;
#31355=CARTESIAN_POINT ( 'NONE',  ( 0.7185039370078739607, 0.000000000000000000, 4.498031496062992574 ) ) ;
#31356=AXIS2_PLACEMENT_3D ( 'NONE', #1691, #16340, #17266 ) ;
#31357=CARTESIAN_POINT ( 'NONE',  ( -0.7185039370078739607, 1.928577636452523993E-17, 0.1377952754830242266 ) ) ;
#31360=CARTESIAN_POINT ( 'NONE',  ( 0.7185039370078746268, -0.06523048226347956391, 0.5831692913385827515 ) ) ;
#31363=CARTESIAN_POINT ( 'NONE',  ( -0.7646288533564489232, -0.1113553986120547346, 1.205708661309795371 ) ) ;
#31364=CARTESIAN_POINT ( 'NONE',  ( 0.9500414927467378812, 0.1787899950787401604, 0.6643700786863929730 ) ) ;
#31367=DIRECTION ( 'NONE',  ( 1.822029033848725028E-16, 0.000000000000000000, 1.000000000000000000 ) ) ;
#31370=CARTESIAN_POINT ( 'NONE',  ( -1.002407869896990045, 0.1264236179284866091, 1.055610236166708793 ) ) ;
#31371=CARTESIAN_POINT ( 'NONE',  ( 0.8107537697050253289, 0.1574803149606300301, 1.085137795275590955 ) ) ;
#31373=CYLINDRICAL_SURFACE ( 'NONE', #38180, 0.1574803149606299191 ) ;
#31378=CARTESIAN_POINT ( 'NONE',  ( 0.9873396505805591694, 0.1113553986120547346, 0.1722440944881890035 ) ) ;
#31380=CARTESIAN_POINT ( 'NONE',  ( -0.8107537697050254399, -0.1574803149606297803, 1.257381889763780736 ) ) ;
#31386=CARTESIAN_POINT ( 'NONE',  ( 0.7185039370078739607, 1.928577636452523993E-17, 1.171259842519684957 ) ) ;
#31387=CARTESIAN_POINT ( 'NONE',  ( 1.002407869896990045, -0.1264236179284866091, 0.8439960629383622681 ) ) ;
#31394=CARTESIAN_POINT ( 'NONE',  ( 1.033464566929133799, 0.000000000000000000, 1.181102362097196989 ) ) ;
#31396=CARTESIAN_POINT ( 'NONE',  ( -0.8759842519685039353, -0.1787899950787401882, 1.867618110182456714 ) ) ;
#31397=CARTESIAN_POINT ( 'NONE',  ( 0.8759842519685039353, -0.1787899950787401882, 1.867618110182456714 ) ) ;
#31398=ORIENTED_EDGE ( 'NONE', *, *, #7736, .T. ) ;
#31399=CARTESIAN_POINT ( 'NONE',  ( 0.8759842519685039353, -0.1574803149606299191, 1.771653543307086576 ) ) ;
#31400=CARTESIAN_POINT ( 'NONE',  ( -0.6971942568897648851, -0.07405724077823297447, 1.461614173174583753 ) ) ;
#31401=DIRECTION ( 'NONE',  ( 0.000000000000000000, 0.000000000000000000, -1.000000000000000000 ) ) ;
#31402=CARTESIAN_POINT ( 'NONE',  ( -0.9500414927467378812, 0.1787899950787401604, 0.3100393700249766682 ) ) ;
#31405=CARTESIAN_POINT ( 'NONE',  ( -1.054774247047244540, -0.07405724077823318263, 1.796259842465923073 ) ) ;
#31407=CARTESIAN_POINT ( 'NONE',  ( -0.7185039370078739607, 1.928577636452523993E-17, 1.722440944881889813 ) ) ;
#31410=CARTESIAN_POINT ( 'NONE',  ( 0.8759842519685039353, 0.1787899950787401882, 1.690452755851748146 ) ) ;
#31415=EDGE_LOOP ( 'NONE', ( #43006, #9913, #20296, #37593 ) ) ;
#31416=CARTESIAN_POINT ( 'NONE',  ( -0.7495606340400177148, 0.1264236179284866091, 1.301673228292692830 ) ) ;
#31420=LINE ( 'NONE', #35475, #14872 ) ;
#31423=CARTESIAN_POINT ( 'NONE',  ( -0.8107537697050253289, -0.1574803149606297803, 0.7750984250893222516 ) ) ;
#31424=CARTESIAN_POINT ( 'NONE',  ( -0.8107537697050253289, -0.1574803149606297803, 0.6668307086614162493 ) ) ;
#31426=CARTESIAN_POINT ( 'NONE',  ( 0.7495606340400177148, -0.1264236179284866091, 0.9916338582139527791 ) ) ;
#31427=CARTESIAN_POINT ( 'NONE',  ( 1.054774247047244096, 0.000000000000000000, 1.995570866087968520 ) ) ;
#31430=CARTESIAN_POINT ( 'NONE',  ( 0.8107537697050254399, -0.1574803149606297803, 0.3813976376877488139 ) ) ;
#31434=CARTESIAN_POINT ( 'NONE',  ( -0.6971942568897648851, 0.07405724077823318263, 1.929133858213952335 ) ) ;
#31436=CARTESIAN_POINT ( 'NONE',  ( -1.054774247047244540, 0.07405724077823318263, 1.486220472387181690 ) ) ;
#31437=CARTESIAN_POINT ( 'NONE',  ( 1.002407869896990045, -0.1264236179284866091, 1.400098425143086800 ) ) ;
#31439=CARTESIAN_POINT ( 'NONE',  ( -0.8759842519685039353, -0.1787899950787401882, 0.6077755904974173617 ) ) ;
#31440=CARTESIAN_POINT ( 'NONE',  ( 1.002407869896990045, -0.1264236179284866091, 0.1008858267178899676 ) ) ;
#31443=CARTESIAN_POINT ( 'NONE',  ( 0.6971942568897637749, 2.189545951927499583E-17, 0.6373031495525354195 ) ) ;
#31444=CARTESIAN_POINT ( 'NONE',  ( -1.054774247047244540, 0.07405724077823318263, 0.5757874015210393548 ) ) ;
#31445=CARTESIAN_POINT ( 'NONE',  ( 1.033464566929134687, -0.06523048226347956391, 0.6373031496062994128 ) ) ;
#31448=CARTESIAN_POINT ( 'NONE',  ( -0.9412147342319837628, 0.1574803149606300301, 0.2928149606299214613 ) ) ;
#31449=CARTESIAN_POINT ( 'NONE',  ( 0.8019270111902716547, 0.1787899950787401604, 1.338582677111590069 ) ) ;
#31452=VERTEX_POINT ( 'NONE', #14208 ) ;
#31453=CARTESIAN_POINT ( 'NONE',  ( -0.8019270111902717657, -0.1787899950787401604, 0.9202755904974182499 ) ) ;
#31458=CARTESIAN_POINT ( 'NONE',  ( 0.8759842519685039353, 0.1574803149606299191, 1.003937007874015741 ) ) ;
#31463=AXIS2_PLACEMENT_3D ( 'NONE', #30503, #45776, #34799 ) ;
#31467=CARTESIAN_POINT ( 'NONE',  ( 0.8107537697050234415, -0.1574803149606297803, 0.1845472439869611792 ) ) ;
#31472=CARTESIAN_POINT ( 'NONE',  ( 0.8759842519685039353, 0.1787899950787401882, 0.4256889763241890057 ) ) ;
#31473=( BOUNDED_CURVE ( )  B_SPLINE_CURVE ( 2, ( #33830, #16317, #22534, #19413, #7919, #34063, #18933, #34516, #33592 ),
 .UNSPECIFIED., .F., .F. ) 
 B_SPLINE_CURVE_WITH_KNOTS ( ( 3, 2, 2, 2, 3 ),
 ( 0.4899999999999999911, 0.4924999999999999933, 0.4949999999999999956, 0.4974999999999999978, 0.5000000000000000000 ),
 .UNSPECIFIED. ) 
 CURVE ( )  GEOMETRIC_REPRESENTATION_ITEM ( )  RATIONAL_B_SPLINE_CURVE ( ( 1.000000000000000000, 0.9238795325112869605, 1.000000000000000000, 0.9238795325112869605, 1.000000000000000000, 0.9238795325112869605, 1.000000000000000000, 0.9238795325112869605, 1.000000000000000000 ) ) 
 REPRESENTATION_ITEM ( '' )  ) ;
#31474=CARTESIAN_POINT ( 'NONE',  ( -0.7495606340400177148, -0.1264236179284866091, 0.7603346456155274380 ) ) ;
#31476=CARTESIAN_POINT ( 'NONE',  ( 0.9412147342319837628, 0.1574803149606300301, 0.08612204713656733401 ) ) ;
#31479=CARTESIAN_POINT ( 'NONE',  ( 0.8759842519685039353, -0.1787899950787401882, 1.592027559001354398 ) ) ;
#31482=CARTESIAN_POINT ( 'NONE',  ( 1.002407869896990045, -0.1264236179284866091, 0.4109251967966299213 ) ) ;
#31485=ORIENTED_EDGE ( 'NONE', *, *, #15833, .T. ) ;
#31486=FACE_OUTER_BOUND ( 'NONE', #7620, .T. ) ;
#31491=CARTESIAN_POINT ( 'NONE',  ( 0.6971942568897637749, 2.189545951927499583E-17, 0.3961614172690708924 ) ) ;
#31495=CARTESIAN_POINT ( 'NONE',  ( 0.7185039370078739607, 0.000000000000000000, 2.007874015640504162 ) ) ;
#31497=CARTESIAN_POINT ( 'NONE',  ( -0.8019270111902717657, 0.1787899950787401604, 1.412401574749386990 ) ) ;
#31498=ORIENTED_EDGE ( 'NONE', *, *, #10077, .T. ) ;
#31500=CARTESIAN_POINT ( 'NONE',  ( 0.8019270111902717657, 0.1787899950787401604, 0.9448818897100165204 ) ) ;
#31501=CARTESIAN_POINT ( 'NONE',  ( -0.7185039370078739607, 1.928577636452523993E-17, 0.4921259841444416971 ) ) ;
#31502=VECTOR ( 'NONE', #28713, 39.37007874015748143 ) ;
#31503=CARTESIAN_POINT ( 'NONE',  ( 0.7495606340400177148, -0.1264236179284866091, 1.739665354276945131 ) ) ;
#31504=CARTESIAN_POINT ( 'NONE',  ( -0.9873396505805591694, -0.1113553986120547346, 1.382874015748031704 ) ) ;
#31508=CARTESIAN_POINT ( 'NONE',  ( 1.002407869896990045, -0.1264236179284866091, 0.2189960629383626012 ) ) ;
#31509=CARTESIAN_POINT ( 'NONE',  ( -1.002407869896990045, 0.1264236179284866091, 0.1058070865604098382 ) ) ;
#31511=CARTESIAN_POINT ( 'NONE',  ( 1.033464566929134687, -0.06523048226347956391, 1.414862204616882835 ) ) ;
#31512=VERTEX_POINT ( 'NONE', #3409 ) ;
#31513=VERTEX_POINT ( 'NONE', #32671 ) ;
#31517=CARTESIAN_POINT ( 'NONE',  ( -0.8019270111902716547, -0.1787899950787401604, 1.624015747977732849 ) ) ;
#31519=EDGE_CURVE ( 'NONE', #40492, #40417, #43652, .T. ) ;
#31521=CARTESIAN_POINT ( 'NONE',  ( 0.8759842519685039353, 0.000000000000000000, 4.498031496062992574 ) ) ;
#31522=DIRECTION ( 'NONE',  ( 1.822029033848725028E-16, 0.000000000000000000, 1.000000000000000000 ) ) ;
#31524=VERTEX_POINT ( 'NONE', #18025 ) ;
#31527=ORIENTED_EDGE ( 'NONE', *, *, #9766, .T. ) ;
#31528=CARTESIAN_POINT ( 'NONE',  ( 0.8019270111902717657, -0.1787899950787401604, 1.112204724355684959 ) ) ;
#31529=ADVANCED_FACE ( 'NONE', ( #47013 ), #11321, .T. ) ;
#31533=CARTESIAN_POINT ( 'NONE',  ( 0.9873396505805591694, 0.1113553986120547346, 1.904527559055118280 ) ) ;
#31534=AXIS2_PLACEMENT_3D ( 'NONE', #8689, #15908, #29843 ) ;
#31537=CARTESIAN_POINT ( 'NONE',  ( -0.7495606340400177148, 0.1264236179284866091, 0.3567913385289137596 ) ) ;
#31538=CARTESIAN_POINT ( 'NONE',  ( -0.7646288533564489232, 0.1113553986120547346, 0.9694881889763780070 ) ) ;
#31540=CARTESIAN_POINT ( 'NONE',  ( -0.7111459129584819516, 0.01515968786127315504, 1.982990166292141643 ) ) ;
#31542=CARTESIAN_POINT ( 'NONE',  ( 1.054774247047244096, 0.000000000000000000, 1.090059055064346527 ) ) ;
#31543=CARTESIAN_POINT ( 'NONE',  ( 1.002407869896990045, 0.1264236179284866091, 1.601870078686393750 ) ) ;
#31544=CARTESIAN_POINT ( 'NONE',  ( 1.002407869896990045, 0.1264236179284866091, 0.2239173227808822775 ) ) ;
#31545=DIRECTION ( 'NONE',  ( 1.822029033848725028E-16, 0.000000000000000000, 1.000000000000000000 ) ) ;
#31546=CARTESIAN_POINT ( 'NONE',  ( 0.7646288533564489232, 0.1113553986120547346, 1.678149606299212726 ) ) ;
#31548=CARTESIAN_POINT ( 'NONE',  ( -0.8370031021572473806, 0.1539506378960530386, 1.979113158066270639 ) ) ;
#31549=FACE_OUTER_BOUND ( 'NONE', #25889, .T. ) ;
#31553=CARTESIAN_POINT ( 'NONE',  ( 0.8759842519685039353, -0.1787899950787401882, 0.9178149605761574126 ) ) ;
#31554=CARTESIAN_POINT ( 'NONE',  ( 0.8759842519685039353, 0.1787899950787401882, 1.966043307032850462 ) ) ;
#31555=CARTESIAN_POINT ( 'NONE',  ( 0.8107537697050253289, 0.1574803149606300301, 0.3272637794200322636 ) ) ;
#31558=CARTESIAN_POINT ( 'NONE',  ( 1.031069757465331804, 0.04013614735736921457, 0.03937007433850867738 ) ) ;
#31559=CARTESIAN_POINT ( 'NONE',  ( -0.8759842519685039353, -0.1574803149606299191, 0.2263779526483783444 ) ) ;
#31560=CARTESIAN_POINT ( 'NONE',  ( 0.9500414927467378812, -0.1787899950787401604, 1.313976377898992132 ) ) ;
#31562=ORIENTED_EDGE ( 'NONE', *, *, #29904, .T. ) ;
#31563=DIRECTION ( 'NONE',  ( -4.336808689942014285E-16, 0.000000000000000000, -1.000000000000000000 ) ) ;
#31564=CARTESIAN_POINT ( 'NONE',  ( 0.8759842519685039353, -0.1574803149606299191, 0.06889763768774861963 ) ) ;
#31566=CARTESIAN_POINT ( 'NONE',  ( -0.7185039370078739607, 1.928577636452523993E-17, 1.003937007766488199 ) ) ;
#31567=VECTOR ( 'NONE', #13844, 39.37007874015748143 ) ;
#31570=ORIENTED_EDGE ( 'NONE', *, *, #40721, .F. ) ;
#31571=ADVANCED_FACE ( 'NONE', ( #23228 ), #271, .T. ) ;
#31574=VECTOR ( 'NONE', #44746, 39.37007874015748143 ) ;
#31576=CARTESIAN_POINT ( 'NONE',  ( -1.002407869896990045, 0.1264236179284866091, 1.916830708607653477 ) ) ;
#31577=ORIENTED_EDGE ( 'NONE', *, *, #25450, .F. ) ;
#31578=CARTESIAN_POINT ( 'NONE',  ( -0.7495606340400177148, -0.1264236179284866091, 0.6815944881352126172 ) ) ;
#31581=ORIENTED_EDGE ( 'NONE', *, *, #36215, .F. ) ;
#31587=CARTESIAN_POINT ( 'NONE',  ( -1.054774247047244096, 0.000000000000000000, 0.5733267715997795166 ) ) ;
#31589=EDGE_LOOP ( 'NONE', ( #9753, #38616, #29386, #8669 ) ) ;
#31590=CARTESIAN_POINT ( 'NONE',  ( -0.7495606340400177148, -0.1264236179284866091, 1.587106299158834721 ) ) ;
#31592=( BOUNDED_CURVE ( )  B_SPLINE_CURVE ( 2, ( #23459, #30433, #34726, #1379, #9304, #23219, #41862, #19368, #34023 ),
 .UNSPECIFIED., .F., .T. ) 
 B_SPLINE_CURVE_WITH_KNOTS ( ( 3, 2, 2, 2, 3 ),
 ( 0.1700000000000000122, 0.1724999999999999867, 0.1749999999999999889, 0.1774999999999999911, 0.1799999999999999933 ),
 .UNSPECIFIED. ) 
 CURVE ( )  GEOMETRIC_REPRESENTATION_ITEM ( )  RATIONAL_B_SPLINE_CURVE ( ( 1.000000000000000000, 0.9238795325112869605, 1.000000000000000000, 0.9238795325112869605, 1.000000000000000000, 0.9238795325112869605, 1.000000000000000000, 0.9238795325112869605, 1.000000000000000000 ) ) 
 REPRESENTATION_ITEM ( '' )  ) ;
#31594=CARTESIAN_POINT ( 'NONE',  ( 0.7646288533564489232, 0.1113553986120547346, 0.6545275590551181688 ) ) ;
#31595=EDGE_LOOP ( 'NONE', ( #46489, #33187, #44214, #33688 ) ) ;
#31596=CARTESIAN_POINT ( 'NONE',  ( 1.033464566929134687, -0.06523048226347956391, 0.5979330708661413363 ) ) ;
#31597=CARTESIAN_POINT ( 'NONE',  ( 0.9873396505805591694, 0.1113553986120547346, 0.6348425195775118102 ) ) ;
#31598=CARTESIAN_POINT ( 'NONE',  ( -0.7646288533564489232, 0.1113553986120547346, 1.235236220364913207 ) ) ;
#31605=CARTESIAN_POINT ( 'NONE',  ( 0.9873396505805591694, 0.1113553986120547346, 1.156496062992125928 ) ) ;
#31608=CYLINDRICAL_SURFACE ( 'NONE', #22066, 0.1574803149606299191 ) ;
#31609=LINE ( 'NONE', #41871, #39225 ) ;
#31610=LINE ( 'NONE', #32321, #33112 ) ;
#31617=CARTESIAN_POINT ( 'NONE',  ( 0.9500414927467378812, -0.1787899950787401604, 0.8809055117572599514 ) ) ;
#31620=CYLINDRICAL_SURFACE ( 'NONE', #19713, 0.1574803149606299191 ) ;
#31624=CARTESIAN_POINT ( 'NONE',  ( 0.7185039370078746268, 0.06523048226347956391, 1.277066929026331898 ) ) ;
#31625=( BOUNDED_CURVE ( )  B_SPLINE_CURVE ( 2, ( #36058, #18080, #39870, #25538, #21189, #2736, #6578, #43711, #24564 ),
 .UNSPECIFIED., .F., .T. ) 
 B_SPLINE_CURVE_WITH_KNOTS ( ( 3, 2, 2, 2, 3 ),
 ( 0.9599999999999999645, 0.9625000000000000222, 0.9649999999999999689, 0.9675000000000000266, 0.9699999999999999734 ),
 .UNSPECIFIED. ) 
 CURVE ( )  GEOMETRIC_REPRESENTATION_ITEM ( )  RATIONAL_B_SPLINE_CURVE ( ( 1.000000000000000000, 0.9238795325112869605, 1.000000000000000000, 0.9238795325112869605, 1.000000000000000000, 0.9238795325112869605, 1.000000000000000000, 0.9238795325112869605, 1.000000000000000000 ) ) 
 REPRESENTATION_ITEM ( '' )  ) ;
#31626=EDGE_CURVE ( 'NONE', #7863, #6761, #33715, .T. ) ;
#31628=ORIENTED_EDGE ( 'NONE', *, *, #45281, .F. ) ;
#31629=CARTESIAN_POINT ( 'NONE',  ( -1.054774247047244540, -0.07405724077823318263, 1.993110236166711013 ) ) ;
#31630=EDGE_CURVE ( 'NONE', #9851, #11117, #20232, .T. ) ;
#31634=CARTESIAN_POINT ( 'NONE',  ( -0.9500414927467378812, -0.1787899950787401604, 1.550196850339937926 ) ) ;
#31635=CARTESIAN_POINT ( 'NONE',  ( -0.7495606340400177148, 0.1264236179284866091, 1.021161417269070837 ) ) ;
#31636=CARTESIAN_POINT ( 'NONE',  ( -1.002407869896990045, 0.1264236179284866091, 0.1894685038832444879 ) ) ;
#31638=DIRECTION ( 'NONE',  ( 0.000000000000000000, 0.000000000000000000, 1.000000000000000000 ) ) ;
#31639=CARTESIAN_POINT ( 'NONE',  ( -0.6971942568897648851, 0.07405724077823318263, 1.934055118056471567 ) ) ;
#31641=CARTESIAN_POINT ( 'NONE',  ( -0.7185039370078746268, 0.06523048226347956391, 1.877460629921260393 ) ) ;
#31657=CARTESIAN_POINT ( 'NONE',  ( -0.8107537697050253289, -0.1574803149606297803, 0.8144685038294804391 ) ) ;
#31658=CARTESIAN_POINT ( 'NONE',  ( -1.033464566929134687, -0.06523048226347956391, 0.7554133858267707557 ) ) ;
#31660=CARTESIAN_POINT ( 'NONE',  ( 1.054774247047244540, 0.07405724077823318263, 0.9301181101824563813 ) ) ;
#31664=CARTESIAN_POINT ( 'NONE',  ( 0.7185039370078746268, 0.06523048226347956391, 0.2140748030420794590 ) ) ;
#31667=CARTESIAN_POINT ( 'NONE',  ( 1.033464566929133799, 0.000000000000000000, 0.2066929133858267931 ) ) ;
#31668=CARTESIAN_POINT ( 'NONE',  ( 0.9412147342319837628, -0.1574803149606297803, 0.3863188975302684347 ) ) ;
#31672=CARTESIAN_POINT ( 'NONE',  ( -0.6971942568897648851, -0.07405724077823297447, 1.973425196796630088 ) ) ;
#31673=ORIENTED_EDGE ( 'NONE', *, *, #17171, .F. ) ;
#31674=ORIENTED_EDGE ( 'NONE', *, *, #17151, .F. ) ;
#31675=CARTESIAN_POINT ( 'NONE',  ( -0.9500414927467378812, -0.1787899950787401604, 1.437007873961985371 ) ) ;
#31677=CARTESIAN_POINT ( 'NONE',  ( 0.6971942568897648851, 0.07405724077823318263, 1.422244094434426120 ) ) ;
#31679=CARTESIAN_POINT ( 'NONE',  ( -1.054774247047244096, 0.000000000000000000, 0.5782480314422993040 ) ) ;
#31680=CARTESIAN_POINT ( 'NONE',  ( 0.8759842519685039353, 0.1787899950787401882, 0.1550196849856066983 ) ) ;
#31683=CARTESIAN_POINT ( 'NONE',  ( 1.054774247047244540, -0.07405724077823318263, 0.6545275590013546196 ) ) ;
#31684=CARTESIAN_POINT ( 'NONE',  ( -0.6971942568897637749, 2.189545951927499583E-17, 0.4749015747493858242 ) ) ;
#31685=CARTESIAN_POINT ( 'NONE',  ( 0.9412147342319837628, -0.1574803149606297803, 0.6323818897637792924 ) ) ;
#31686=CYLINDRICAL_SURFACE ( 'NONE', #6084, 0.1574803149606299191 ) ;
#31688=CARTESIAN_POINT ( 'NONE',  ( -0.7495606340400177148, 0.1264236179284866091, 1.498523621993480326 ) ) ;
#31689=EDGE_LOOP ( 'NONE', ( #25394, #37431, #44012, #3346 ) ) ;
#31691=CARTESIAN_POINT ( 'NONE',  ( -0.8759842519685039353, 0.1574803149606299191, 0.4921259842519685179 ) ) ;
#31692=CARTESIAN_POINT ( 'NONE',  ( 0.6971942568897637749, 2.189545951927499583E-17, 1.345964566875370139 ) ) ;
#31695=DIRECTION ( 'NONE',  ( -1.000000000000000000, 0.000000000000000000, 0.000000000000000000 ) ) ;
#31696=CARTESIAN_POINT ( 'NONE',  ( -1.054774247047244540, -0.07405724077823318263, 0.9301181101824563813 ) ) ;
#31701=AXIS2_PLACEMENT_3D ( 'NONE', #21488, #17421, #21251 ) ;
#31703=CARTESIAN_POINT ( 'NONE',  ( 0.8759842519685039353, -0.1574803149606299191, 0.1870078739082208508 ) ) ;
#31710=CARTESIAN_POINT ( 'NONE',  ( 0.6971942568897626646, -0.07405724077823297447, 0.4379921259304882519 ) ) ;
#31712=CARTESIAN_POINT ( 'NONE',  ( -0.9500414927467377701, -0.1787899950787401604, 0.7677165353793073965 ) ) ;
#31714=FACE_OUTER_BOUND ( 'NONE', #22659, .T. ) ;
#31716=CARTESIAN_POINT ( 'NONE',  ( 0.8759842519685039353, -0.1787899950787401882, 1.552657480261196765 ) ) ;
#31717=CARTESIAN_POINT ( 'NONE',  ( 0.7495606340400177148, 0.1264236179284866091, 1.966043307032850462 ) ) ;
#31719=CARTESIAN_POINT ( 'NONE',  ( 0.8019270111902716547, 0.1787899950787401604, 0.3494094487651343006 ) ) ;
#31722=CARTESIAN_POINT ( 'NONE',  ( 0.8759842519685039353, 0.000000000000000000, 1.978346456692913646 ) ) ;
#31723=LINE ( 'NONE', #46315, #43535 ) ;
#31725=CARTESIAN_POINT ( 'NONE',  ( 0.6971942568897637749, 2.189545951927499583E-17, 0.5536417322297008115 ) ) ;
#31727=ADVANCED_FACE ( 'NONE', ( #42362 ), #38070, .T. ) ;
#31729=CARTESIAN_POINT ( 'NONE',  ( -0.7495606340400177148, -0.1264236179284866091, 1.464074803095842370 ) ) ;
#31730=ORIENTED_EDGE ( 'NONE', *, *, #28240, .F. ) ;
#31732=CARTESIAN_POINT ( 'NONE',  ( 0.6971942568897648851, -0.07405724077823297447, 0.9940944881352130613 ) ) ;
#31734=AXIS2_PLACEMENT_3D ( 'NONE', #33488, #26526, #44458 ) ;
#31737=CARTESIAN_POINT ( 'NONE',  ( -0.7646288533564489232, -0.1113553986120547346, 0.6545275589475906264 ) ) ;
#31738=CARTESIAN_POINT ( 'NONE',  ( 0.7185039370078739607, 1.928577636452523993E-17, 1.486220472440944906 ) ) ;
#31739=CARTESIAN_POINT ( 'NONE',  ( 1.002407869896990045, 0.1264236179284866091, 1.719980314906866203 ) ) ;
#31740=CARTESIAN_POINT ( 'NONE',  ( -0.7646288533564489232, 0.1113553986120547346, 1.441929133858267598 ) ) ;
#31741=CARTESIAN_POINT ( 'NONE',  ( -1.054774247047244540, -0.07405724077823318263, 0.8464566928596233275 ) ) ;
#31745=CARTESIAN_POINT ( 'NONE',  ( 1.002407869896990045, 0.1264236179284866091, 0.1107283464029293202 ) ) ;
#31746=CARTESIAN_POINT ( 'NONE',  ( 1.033464566929133799, 0.000000000000000000, 1.496062992018456494 ) ) ;
#31749=CARTESIAN_POINT ( 'NONE',  ( 1.033464566929134687, 0.06523048226347956391, 1.774114173120820093 ) ) ;
#31752=CARTESIAN_POINT ( 'NONE',  ( -1.054774247047244096, 0.000000000000000000, 1.754429133804503715 ) ) ;
#31754=CARTESIAN_POINT ( 'NONE',  ( -0.7185039370078746268, 0.06523048226347956391, 0.6569881889763780070 ) ) ;
#31760=VERTEX_POINT ( 'NONE', #38545 ) ;
#31763=CARTESIAN_POINT ( 'NONE',  ( -0.7185039370078739607, 1.928577636452523993E-17, 0.8169291338582678197 ) ) ;
#31764=CARTESIAN_POINT ( 'NONE',  ( 1.033464566929134687, -0.06523048226347956391, 1.779035433070867089 ) ) ;
#31765=VECTOR ( 'NONE', #38383, 39.37007874015748143 ) ;
#31770=CARTESIAN_POINT ( 'NONE',  ( -0.8759842519685039353, -0.1787899950787401882, 0.4109251967966299213 ) ) ;
#31771=CARTESIAN_POINT ( 'NONE',  ( -1.033464566929134687, -0.06523048226347956391, 0.9916338582677171054 ) ) ;
#31775=CARTESIAN_POINT ( 'NONE',  ( 1.002407869896990045, 0.1264236179284866091, 1.094980314906866203 ) ) ;
#31776=CARTESIAN_POINT ( 'NONE',  ( 1.054774247047244096, 0.000000000000000000, 1.478838582623401399 ) ) ;
#31777=CARTESIAN_POINT ( 'NONE',  ( 0.6971942568897626646, 0.07405724077823318263, 0.1574803149068664809 ) ) ;
#31780=LINE ( 'NONE', #46363, #30480 ) ;
#31782=CARTESIAN_POINT ( 'NONE',  ( 0.8107537697050254399, 0.1574803149606300301, 0.6815944880814486240 ) ) ;
#31783=CARTESIAN_POINT ( 'NONE',  ( -0.7646288533564489232, 0.1113553986120547346, 1.707677165246803241 ) ) ;
#31786=CARTESIAN_POINT ( 'NONE',  ( 0.6971942568897648851, 0.07405724077823318263, 1.141732283410804349 ) ) ;
#31789=CARTESIAN_POINT ( 'NONE',  ( -0.9500414927467378812, -0.1787899950787401604, 1.156496062938362046 ) ) ;
#31790=CARTESIAN_POINT ( 'NONE',  ( 1.033464566929134687, -0.06523048226347956391, 0.5093503935932609528 ) ) ;
#31791=ORIENTED_EDGE ( 'NONE', *, *, #26986, .F. ) ;
#31793=CARTESIAN_POINT ( 'NONE',  ( -1.033464566929133799, 0.000000000000000000, 0.3149606298137326843 ) ) ;
#31794=ORIENTED_EDGE ( 'NONE', *, *, #22614, .F. ) ;
#31795=CARTESIAN_POINT ( 'NONE',  ( 0.9500414927467378812, -0.1787899950787401604, 1.235236220418678199 ) ) ;
#31798=CARTESIAN_POINT ( 'NONE',  ( 0.7185039370078739607, 1.928577636452523993E-17, 0.05905511800270921846 ) ) ;
#31800=CARTESIAN_POINT ( 'NONE',  ( 0.7185039370078746268, 0.06523048226347956391, 0.7357283464566919395 ) ) ;
#31802=AXIS2_PLACEMENT_3D ( 'NONE', #34453, #9288, #41360 ) ;
#31804=ORIENTED_EDGE ( 'NONE', *, *, #22561, .T. ) ;
#31805=CARTESIAN_POINT ( 'NONE',  ( -0.6971942568897637749, 2.189545951927499583E-17, 1.380413385773007873 ) ) ;
#31807=CARTESIAN_POINT ( 'NONE',  ( -1.002407869896990045, -0.1264236179284866091, 0.9670275590013542866 ) ) ;
#31808=CARTESIAN_POINT ( 'NONE',  ( -0.9412147342319837628, -0.1574803149606297803, 0.04183070866141735261 ) ) ;
#31809=VERTEX_POINT ( 'NONE', #13389 ) ;
#31810=CARTESIAN_POINT ( 'NONE',  ( -0.6971942568897637749, 2.189545951927499583E-17, 0.6373031495525354195 ) ) ;
#31812=ORIENTED_EDGE ( 'NONE', *, *, #16805, .T. ) ;
#31813=CARTESIAN_POINT ( 'NONE',  ( -0.9412147342319837628, 0.1574803149606300301, 0.05659448818897643008 ) ) ;
#31818=CARTESIAN_POINT ( 'NONE',  ( -0.9500414927467378812, -0.1787899950787401604, 0.6053149605761579677 ) ) ;
#31821=CARTESIAN_POINT ( 'NONE',  ( -0.7495606340400177148, -0.1264236179284866091, 1.665846456639149764 ) ) ;
#31822=CARTESIAN_POINT ( 'NONE',  ( 1.033464566929133799, 1.928577636452524610E-17, 4.498031496062992574 ) ) ;
#31826=CARTESIAN_POINT ( 'NONE',  ( -0.7185039370078739607, 1.928577636452523993E-17, 1.397637795168062969 ) ) ;
#31828=CARTESIAN_POINT ( 'NONE',  ( 0.6971942568897637749, 2.189545951927499583E-17, 0.6373031495525354195 ) ) ;
#31833=CARTESIAN_POINT ( 'NONE',  ( 1.033464566929133799, 0.000000000000000000, 1.614173228238929170 ) ) ;
#31835=CARTESIAN_POINT ( 'NONE',  ( 0.7646288533564489232, 0.1113553986120547346, 1.589566929026330566 ) ) ;
#31836=CARTESIAN_POINT ( 'NONE',  ( 1.033464566929133799, 0.000000000000000000, 1.309055118110236338 ) ) ;
#31837=CARTESIAN_POINT ( 'NONE',  ( -0.7646288533564489232, 0.1113553986120547346, 1.274606299105070839 ) ) ;
#31838=CARTESIAN_POINT ( 'NONE',  ( -0.9412147342319837628, -0.1574803149606297803, 1.341043307086613456 ) ) ;
#31839=CARTESIAN_POINT ( 'NONE',  ( 0.8107537697050254399, -0.1574803149606297803, 1.966043307086614567 ) ) ;
#31843=CARTESIAN_POINT ( 'NONE',  ( 0.8019270111902716547, 0.1787899950787401604, 0.7431102361667091261 ) ) ;
#31847=VERTEX_POINT ( 'NONE', #1334 ) ;
#31848=CARTESIAN_POINT ( 'NONE',  ( -0.9873396505805591694, -0.1113553986120547346, 1.067913385826771755 ) ) ;
#31849=CARTESIAN_POINT ( 'NONE',  ( 0.7185039370078746268, -0.06523048226347956391, 1.724901574803149762 ) ) ;
#31851=CARTESIAN_POINT ( 'NONE',  ( 0.9500414927467378812, -0.1787899950787401604, 0.8021653542769460188 ) ) ;
#31853=CARTESIAN_POINT ( 'NONE',  ( 0.8759842519685039353, -0.1574803149606299191, 0.6988188975302678241 ) ) ;
#31860=CARTESIAN_POINT ( 'NONE',  ( -0.6971942568897648851, -0.07405724077823297447, 1.899606299158834943 ) ) ;
#31861=FACE_OUTER_BOUND ( 'NONE', #31595, .T. ) ;
#31863=CARTESIAN_POINT ( 'NONE',  ( -0.8759842519685039353, -0.1574803149606299191, 1.850393700787401619 ) ) ;
#31864=CARTESIAN_POINT ( 'NONE',  ( -0.7495606340400177148, 0.1264236179284866091, 1.572342519631275692 ) ) ;
#31866=CARTESIAN_POINT ( 'NONE',  ( -1.002407869896990045, 0.1264236179284866091, 1.011318897584031484 ) ) ;
#31867=CARTESIAN_POINT ( 'NONE',  ( -0.6971942568897626646, -0.07405724077823297447, 0.2066929133320631329 ) ) ;
#31869=CARTESIAN_POINT ( 'NONE',  ( -0.6971942568897648851, -0.07405724077823297447, 1.899606299158834943 ) ) ;
#31871=CARTESIAN_POINT ( 'NONE',  ( -0.9873396505805591694, -0.1113553986120547346, 1.934055118110236338 ) ) ;
#31875=CARTESIAN_POINT ( 'NONE',  ( -0.7185039370078746268, -0.06523048226347956391, 1.488681102362205300 ) ) ;
#31876=CARTESIAN_POINT ( 'NONE',  ( -0.7185039370078739607, 0.000000000000000000, -2.869337061179095023E-17 ) ) ;
#31878=CARTESIAN_POINT ( 'NONE',  ( -1.054774247047244096, 0.000000000000000000, 0.2189960629383626012 ) ) ;
#31879=( BOUNDED_CURVE ( )  B_SPLINE_CURVE ( 2, ( #24452, #13212, #41921, #46480, #20375, #35259, #28298, #10074, #2627 ),
 .UNSPECIFIED., .F., .F. ) 
 B_SPLINE_CURVE_WITH_KNOTS ( ( 3, 2, 2, 2, 3 ),
 ( 0.5300000000000000266, 0.5324999999999999734, 0.5350000000000000311, 0.5374999999999999778, 0.5400000000000000355 ),
 .UNSPECIFIED. ) 
 CURVE ( )  GEOMETRIC_REPRESENTATION_ITEM ( )  RATIONAL_B_SPLINE_CURVE ( ( 1.000000000000000000, 0.9238795325112869605, 1.000000000000000000, 0.9238795325112869605, 1.000000000000000000, 0.9238795325112869605, 1.000000000000000000, 0.9238795325112869605, 1.000000000000000000 ) ) 
 REPRESENTATION_ITEM ( '' )  ) ;
#31882=CARTESIAN_POINT ( 'NONE',  ( -0.9500414927467377701, 0.1787899950787401604, 1.254921259788757348 ) ) ;
#31884=EDGE_CURVE ( 'NONE', #2356, #5354, #9012, .T. ) ;
#31889=CARTESIAN_POINT ( 'NONE',  ( -1.033464566929133799, 0.000000000000000000, 0.7972440944881890035 ) ) ;
#31892=CARTESIAN_POINT ( 'NONE',  ( 0.8759842519685039353, 0.1574803149606299191, 1.820866141624755796 ) ) ;
#31893=CARTESIAN_POINT ( 'NONE',  ( 0.7646288533564489232, 0.1113553986120547346, 0.8513779527559054427 ) ) ;
#31896=( BOUNDED_CURVE ( )  B_SPLINE_CURVE ( 2, ( #18715, #8638, #37397, #16098, #37891, #4313, #491, #37646, #11791 ),
 .UNSPECIFIED., .F., .T. ) 
 B_SPLINE_CURVE_WITH_KNOTS ( ( 3, 2, 2, 2, 3 ),
 ( 0.4299999999999999933, 0.4324999999999999956, 0.4349999999999999978, 0.4375000000000000000, 0.4400000000000000022 ),
 .UNSPECIFIED. ) 
 CURVE ( )  GEOMETRIC_REPRESENTATION_ITEM ( )  RATIONAL_B_SPLINE_CURVE ( ( 1.000000000000000000, 0.9238795325112869605, 1.000000000000000000, 0.9238795325112869605, 1.000000000000000000, 0.9238795325112869605, 1.000000000000000000, 0.9238795325112869605, 1.000000000000000000 ) ) 
 REPRESENTATION_ITEM ( '' )  ) ;
#31898=CARTESIAN_POINT ( 'NONE',  ( 0.7185039370078746268, 0.06523048226347956391, 1.523129921259841923 ) ) ;
#31899=CARTESIAN_POINT ( 'NONE',  ( 0.7185039370078746268, -0.06523048226347956391, 0.2189960628845991353 ) ) ;
#31900=ORIENTED_EDGE ( 'NONE', *, *, #47297, .F. ) ;
#31901=ORIENTED_EDGE ( 'NONE', *, *, #1954, .T. ) ;
#31902=CARTESIAN_POINT ( 'NONE',  ( -1.033464566929133799, 0.000000000000000000, 1.190944881889763884 ) ) ;
#31905=CARTESIAN_POINT ( 'NONE',  ( -0.9500414927467378812, -0.1787899950787401604, 1.904527559001354398 ) ) ;
#31907=CARTESIAN_POINT ( 'NONE',  ( -1.002407869896990045, 0.1264236179284866091, 1.449311023568283341 ) ) ;
#31908=CARTESIAN_POINT ( 'NONE',  ( 0.6971942568897637749, 2.189545951927499583E-17, 1.542814960576157413 ) ) ;
#31909=EDGE_LOOP ( 'NONE', ( #28319, #44766, #25175, #14308 ) ) ;
#31910=CARTESIAN_POINT ( 'NONE',  ( -0.8759842519685039353, -0.1574803149606299191, 0.9055118110236221041 ) ) ;
#31911=CARTESIAN_POINT ( 'NONE',  ( -1.054774247047244540, -0.07405724077823318263, 0.6545275590013545086 ) ) ;
#31912=CARTESIAN_POINT ( 'NONE',  ( 1.054774247047244540, 0.07405724077823318263, 0.1870078739619845387 ) ) ;
#31913=CARTESIAN_POINT ( 'NONE',  ( -1.033464566929133799, 1.928577636452524610E-17, 2.869337061179095023E-17 ) ) ;
#31915=CARTESIAN_POINT ( 'NONE',  ( 0.7495606340400177148, 0.1264236179284866091, 0.7504921259304880854 ) ) ;
#31916=CARTESIAN_POINT ( 'NONE',  ( -0.6971942568897648851, 0.07405724077823318263, 0.5905511810485987167 ) ) ;
#31917=DIRECTION ( 'NONE',  ( 0.000000000000000000, 0.000000000000000000, -1.000000000000000000 ) ) ;
#31918=CARTESIAN_POINT ( 'NONE',  ( 0.7646288533564489232, -0.1113553986120547346, 1.136811023622047223 ) ) ;
#31919=ORIENTED_EDGE ( 'NONE', *, *, #2899, .T. ) ;
#31920=CARTESIAN_POINT ( 'NONE',  ( -1.033464566929133799, 1.928577636452524610E-17, 2.869337061179095023E-17 ) ) ;
#31921=CARTESIAN_POINT ( 'NONE',  ( -0.8107537697050253289, -0.1574803149606297803, 0.5093503937007877180 ) ) ;
#31922=CARTESIAN_POINT ( 'NONE',  ( 0.7495606340400177148, 0.1264236179284866091, 1.301673228292692830 ) ) ;
#31930=CARTESIAN_POINT ( 'NONE',  ( 1.054774247047244540, -0.07405724077823318263, 1.437007873961985371 ) ) ;
#31932=CARTESIAN_POINT ( 'NONE',  ( 1.033464566929133799, 1.928577636452524610E-17, 4.498031496062992574 ) ) ;
#31936=CARTESIAN_POINT ( 'NONE',  ( 1.054774247047244540, -0.07405724077823318263, 0.3740157479777325711 ) ) ;
#31937=EDGE_CURVE ( 'NONE', #43630, #14529, #33427, .T. ) ;
#31940=CYLINDRICAL_SURFACE ( 'NONE', #22658, 0.1574803149606299191 ) ;
#31943=CARTESIAN_POINT ( 'NONE',  ( 0.6971942568897637749, 2.189545951927499583E-17, 0.6323818897100157432 ) ) ;
#31945=CARTESIAN_POINT ( 'NONE',  ( -0.8019270111902716547, -0.1787899950787401604, 0.8415354330171020969 ) ) ;
#31949=CARTESIAN_POINT ( 'NONE',  ( -0.8361142526885965154, -0.1686726915505806779, 1.987473384380551877 ) ) ;
#31952=CARTESIAN_POINT ( 'NONE',  ( 0.8759842519685039353, -0.1787899950787401882, 1.749507873961984483 ) ) ;
#31953=CARTESIAN_POINT ( 'NONE',  ( 1.054774247047244540, 0.07405724077823318263, 1.953740157426552715 ) ) ;
#31955=CARTESIAN_POINT ( 'NONE',  ( 0.9500414927467377701, -0.1787899950787401604, 0.4478346456155276045 ) ) ;
#31961=CARTESIAN_POINT ( 'NONE',  ( 0.8019270111902717657, 0.1787899950787401604, 0.03937007868639399305 ) ) ;
#31962=CARTESIAN_POINT ( 'NONE',  ( -0.7646288533564489232, -0.1113553986120547346, 1.520669291231054876 ) ) ;
#31964=CARTESIAN_POINT ( 'NONE',  ( -0.6971942568897648851, -0.07405724077823297447, 1.461614173174583753 ) ) ;
#31967=CARTESIAN_POINT ( 'NONE',  ( 1.002407869896990045, 0.1264236179284866091, 1.213090551127338435 ) ) ;
#31968=CARTESIAN_POINT ( 'NONE',  ( -1.033464566929134687, -0.06523048226347956391, 0.7062007872940467834 ) ) ;
#31970=CARTESIAN_POINT ( 'NONE',  ( 0.7495606340400177148, 0.1264236179284866091, 1.769192913332062966 ) ) ;
#31971=CARTESIAN_POINT ( 'NONE',  ( -0.8107537697050253289, -0.1574803149606297803, 1.336122047244094446 ) ) ;
#31972=CARTESIAN_POINT ( 'NONE',  ( -1.002407869896990045, -0.1264236179284866091, 0.9227362204186770889 ) ) ;
#31975=CARTESIAN_POINT ( 'NONE',  ( 0.8019270111902716547, -0.1787899950787401604, 0.1328740156942679884 ) ) ;
#31976=CARTESIAN_POINT ( 'NONE',  ( 1.033464566929134687, 0.06523048226347956391, 1.616633858160190229 ) ) ;
#31978=CARTESIAN_POINT ( 'NONE',  ( 0.7185039370078739607, 1.928577636452523993E-17, 1.791338582569637738 ) ) ;
#31979=CARTESIAN_POINT ( 'NONE',  ( 0.8759842519685039353, -0.1787899950787401882, 0.7258858267178898149 ) ) ;
#31980=CARTESIAN_POINT ( 'NONE',  ( -0.8759842519685039353, -0.1787899950787401882, 1.705216535379307174 ) ) ;
#31986=EDGE_LOOP ( 'NONE', ( #37514, #19519, #25491, #44542 ) ) ;
#31988=VERTEX_POINT ( 'NONE', #32850 ) ;
#31989=CARTESIAN_POINT ( 'NONE',  ( 1.002407869896990045, 0.1264236179284866091, 1.050688976324189117 ) ) ;
#31991=CARTESIAN_POINT ( 'NONE',  ( -0.7185039370078746268, -0.06523048226347956391, 1.449311023622047445 ) ) ;
#31993=CARTESIAN_POINT ( 'NONE',  ( 0.9412147342319837628, 0.1574803149606300301, 1.906988188976377563 ) ) ;
#31996=CARTESIAN_POINT ( 'NONE',  ( -0.7495606340400177148, -0.1264236179284866091, 0.2878937007336381804 ) ) ;
#31998=CARTESIAN_POINT ( 'NONE',  ( 0.8759842519685039353, 0.1787899950787401882, 1.178641732229700922 ) ) ;
#31999=CARTESIAN_POINT ( 'NONE',  ( 0.9500414927467377701, 0.1787899950787401604, 1.564960629867495845 ) ) ;
#32000=CARTESIAN_POINT ( 'NONE',  ( 0.7495606340400177148, 0.1264236179284866091, 0.1550196849856066983 ) ) ;
#32001=CARTESIAN_POINT ( 'NONE',  ( 0.7185039370078746268, -0.06523048226347956391, 0.8882874014672752505 ) ) ;
#32005=CARTESIAN_POINT ( 'NONE',  ( -0.8107537697050253289, 0.1574803149606300301, 1.705216535325545069 ) ) ;
#32006=VECTOR ( 'NONE', #2015, 39.37007874015748143 ) ;
#32008=CARTESIAN_POINT ( 'NONE',  ( 0.7495606340400177148, 0.1264236179284866091, 0.1156496062454492185 ) ) ;
#32010=CARTESIAN_POINT ( 'NONE',  ( 0.6971942568897637749, 2.189545951927499583E-17, 1.065452755851747924 ) ) ;
#32013=CARTESIAN_POINT ( 'NONE',  ( 0.7646288533564489232, -0.1113553986120547346, 0.5364173227271189504 ) ) ;
#32014=VERTEX_POINT ( 'NONE', #209 ) ;
#32015=CARTESIAN_POINT ( 'NONE',  ( -1.033464566929133799, 0.000000000000000000, 0.4724409447743622148 ) ) ;
#32016=CARTESIAN_POINT ( 'NONE',  ( 1.023384524333779799, 0.06767030011490859920, 0.03937429509552410611 ) ) ;
#32017=CARTESIAN_POINT ( 'NONE',  ( -0.8107537697050253289, 0.1574803149606300301, 0.3666338581601894520 ) ) ;
#32019=CARTESIAN_POINT ( 'NONE',  ( 0.9500414927467378812, -0.1787899950787401604, 1.471456692859622217 ) ) ;
#32021=CARTESIAN_POINT ( 'NONE',  ( -0.8759842519685039353, -0.1574803149606299191, 0.2263779526483783444 ) ) ;
#32022=DIMENSIONAL_EXPONENTS ( 1.000000000000000000, 0.000000000000000000, 0.000000000000000000, 0.000000000000000000, 0.000000000000000000, 0.000000000000000000, 0.000000000000000000 ) ;
#32027=ORIENTED_EDGE ( 'NONE', *, *, #2578, .F. ) ;
#32029=CARTESIAN_POINT ( 'NONE',  ( 0.8759842519685039353, -0.1787899950787401882, 0.4502952755367874427 ) ) ;
#32031=CARTESIAN_POINT ( 'NONE',  ( -1.002407869896990045, 0.1264236179284866091, 1.365649606245448844 ) ) ;
#32034=CARTESIAN_POINT ( 'NONE',  ( -0.8759842519685039353, -0.1787899950787401882, 0.9621062991588346103 ) ) ;
#32035=CARTESIAN_POINT ( 'NONE',  ( -0.9500414927467378812, 0.1787899950787401604, 1.958661417269071947 ) ) ;
#32036=CARTESIAN_POINT ( 'NONE',  ( -0.8019270111902716547, 0.1787899950787401604, 1.097440944828127041 ) ) ;
#32037=CARTESIAN_POINT ( 'NONE',  ( -0.9500414927467378812, 0.1787899950787401604, 0.7037401574265510495 ) ) ;
#32038=AXIS2_PLACEMENT_3D ( 'NONE', #41096, #4690, #19788 ) ;
#32041=ORIENTED_EDGE ( 'NONE', *, *, #35453, .F. ) ;
#32045=CARTESIAN_POINT ( 'NONE',  ( -0.8107537697050254399, -0.1574803149606297803, 1.729822834645670548 ) ) ;
#32046=CYLINDRICAL_SURFACE ( 'NONE', #17275, 0.1574803149606299191 ) ;
#32047=VECTOR ( 'NONE', #31401, 39.37007874015748143 ) ;
#32048=CARTESIAN_POINT ( 'NONE',  ( -0.8019270111902717657, -0.1787899950787401604, 0.6791338582139527791 ) ) ;
#32051=ORIENTED_EDGE ( 'NONE', *, *, #966, .F. ) ;
#32053=CARTESIAN_POINT ( 'NONE',  ( -0.6971942568897648851, -0.07405724077823297447, 1.624015747977732849 ) ) ;
#32055=CARTESIAN_POINT ( 'NONE',  ( 0.7185039370078739607, 1.928577636452523993E-17, 1.043307086506645831 ) ) ;
#32056=ORIENTED_EDGE ( 'NONE', *, *, #18271, .T. ) ;
#32059=CARTESIAN_POINT ( 'NONE',  ( -0.7185039370078746268, -0.06523048226347956391, 1.360728346349165285 ) ) ;
#32060=CARTESIAN_POINT ( 'NONE',  ( 0.8019270111902717657, -0.1787899950787401604, 0.6840551180564720113 ) ) ;
#32062=CARTESIAN_POINT ( 'NONE',  ( 0.8759842519685039353, 0.000000000000000000, 4.498031496062992574 ) ) ;
#32065=CARTESIAN_POINT ( 'NONE',  ( 0.8759842519685039353, -0.1574803149606299191, 1.299212598425196985 ) ) ;
#32068=CARTESIAN_POINT ( 'NONE',  ( 0.8759842519685039353, 0.1787899950787401882, 0.6225393700249762796 ) ) ;
#32072=CARTESIAN_POINT ( 'NONE',  ( 0.7185039370078739607, 1.928577636452523993E-17, 1.673228346349165285 ) ) ;
#32074=DIRECTION ( 'NONE',  ( 0.000000000000000000, 0.000000000000000000, -1.000000000000000000 ) ) ;
#32076=CARTESIAN_POINT ( 'NONE',  ( 0.8019270111902717657, -0.1787899950787401604, 0.8759842519147408302 ) ) ;
#32084=CARTESIAN_POINT ( 'NONE',  ( -0.8759842519685039353, 0.1787899950787401882, 0.03198818892261445085 ) ) ;
#32089=CARTESIAN_POINT ( 'NONE',  ( -0.6971942568897648851, -0.07405724077823297447, 1.978346456639149098 ) ) ;
#32090=CARTESIAN_POINT ( 'NONE',  ( -0.6971942568897648851, -0.07405724077823297447, 1.067913385773007651 ) ) ;
#32091=CARTESIAN_POINT ( 'NONE',  ( -1.054774247047244540, -0.07405724077823318263, 0.2608267715997796832 ) ) ;
#32093=CARTESIAN_POINT ( 'NONE',  ( -0.8759842519685039353, 0.1787899950787401882, 1.966043307032850462 ) ) ;
#32095=CARTESIAN_POINT ( 'NONE',  ( -0.8107537697050253289, -0.1574803149606297803, 1.926673228346456490 ) ) ;
#32099=CARTESIAN_POINT ( 'NONE',  ( -1.033464566929133799, 1.928577636452524610E-17, 2.869337061179095023E-17 ) ) ;
#32101=CARTESIAN_POINT ( 'NONE',  ( -0.9500414927467378812, -0.1787899950787401604, 0.1722440944344254266 ) ) ;
#32102=EDGE_CURVE ( 'NONE', #42555, #35982, #23604, .T. ) ;
#32104=ORIENTED_EDGE ( 'NONE', *, *, #35122, .F. ) ;
#32105=ORIENTED_EDGE ( 'NONE', *, *, #1798, .F. ) ;
#32106=EDGE_CURVE ( 'NONE', #18241, #17345, #43455, .T. ) ;
#32114=CARTESIAN_POINT ( 'NONE',  ( -0.7185039370078746268, -0.06523048226347956391, 0.7406496062992133922 ) ) ;
#32116=CARTESIAN_POINT ( 'NONE',  ( 0.8759842519685039353, -0.1574803149606299191, 1.801181102254677091 ) ) ;
#32118=CARTESIAN_POINT ( 'NONE',  ( -0.8759842519685039353, 0.1574803149606299191, 1.427165354223181248 ) ) ;
#32119=CARTESIAN_POINT ( 'NONE',  ( 1.033464566929133799, 0.000000000000000000, 0.7972440944881890035 ) ) ;
#32121=CARTESIAN_POINT ( 'NONE',  ( -1.033464566929133799, 0.000000000000000000, 0.4822834645669291653 ) ) ;
#32123=CARTESIAN_POINT ( 'NONE',  ( 0.8107537697050234415, -0.1574803149606297803, 0.1058070865066461225 ) ) ;
#32124=EDGE_LOOP ( 'NONE', ( #31156, #32759, #25334, #34775 ) ) ;
#32126=CARTESIAN_POINT ( 'NONE',  ( -0.7646288533564489232, -0.1113553986120547346, 1.176181102362204633 ) ) ;
#32129=CARTESIAN_POINT ( 'NONE',  ( 0.7185039370078739607, 1.928577636452523993E-17, 0.8858267715460158565 ) ) ;
#32132=CARTESIAN_POINT ( 'NONE',  ( -0.8759842519685039353, -0.1787899950787401882, 0.4060039369541102450 ) ) ;
#32134=CARTESIAN_POINT ( 'NONE',  ( -1.002407869896990045, -0.1264236179284866091, 1.478838582623401399 ) ) ;
#32135=CARTESIAN_POINT ( 'NONE',  ( 0.6971942568897648851, 0.07405724077823318263, 1.579724409395055318 ) ) ;
#32137=CARTESIAN_POINT ( 'NONE',  ( 0.8759842519685039353, -0.1574803149606299191, 0.9350393699712126194 ) ) ;
#32138=CARTESIAN_POINT ( 'NONE',  ( -0.7495606340400177148, -0.1264236179284866091, 0.6422244093950550958 ) ) ;
#32139=CARTESIAN_POINT ( 'NONE',  ( 1.002407869896990045, -0.1264236179284866091, 0.1796259841982051075 ) ) ;
#32140=CARTESIAN_POINT ( 'NONE',  ( -0.6971942568897648851, 0.07405724077823318263, 1.299212598371432215 ) ) ;
#32143=CARTESIAN_POINT ( 'NONE',  ( 0.9500414927467377701, 0.1787899950787401604, 0.7431102361667091261 ) ) ;
#32144=CARTESIAN_POINT ( 'NONE',  ( -0.7495606340400177148, 0.1264236179284866091, 0.6668307086076534773 ) ) ;
#32146=( BOUNDED_CURVE ( )  B_SPLINE_CURVE ( 2, ( #37175, #15864, #45050, #30034, #30490, #23036, #12263, #12512, #4559 ),
 .UNSPECIFIED., .F., .T. ) 
 B_SPLINE_CURVE_WITH_KNOTS ( ( 3, 2, 2, 2, 3 ),
 ( 0.01000000000000000021, 0.01250000000000000069, 0.01499999999999999944, 0.01750000000000000167, 0.02000000000000000042 ),
 .UNSPECIFIED. ) 
 CURVE ( )  GEOMETRIC_REPRESENTATION_ITEM ( )  RATIONAL_B_SPLINE_CURVE ( ( 1.000000000000000000, 0.9238795325112869605, 1.000000000000000000, 0.9238795325112869605, 1.000000000000000000, 0.9238795325112869605, 1.000000000000000000, 0.9238795325112869605, 1.000000000000000000 ) ) 
 REPRESENTATION_ITEM ( '' )  ) ;
#32147=CARTESIAN_POINT ( 'NONE',  ( -0.9412147342319837628, -0.1574803149606297803, 0.8686023622047237547 ) ) ;
#32149=CARTESIAN_POINT ( 'NONE',  ( -0.7495606340400177148, 0.1264236179284866091, 1.380413385773007873 ) ) ;
#32151=CARTESIAN_POINT ( 'NONE',  ( -0.7185039370078739607, 1.928577636452523993E-17, 0.5019685039370078705 ) ) ;
#32153=ADVANCED_FACE ( 'NONE', ( #2745 ), #16452, .T. ) ;
#32154=CARTESIAN_POINT ( 'NONE',  ( 0.9500414927467377701, 0.1787899950787401604, 1.254921259788757348 ) ) ;
#32157=CARTESIAN_POINT ( 'NONE',  ( -1.033464566929135131, 1.928577636452536319E-17, 0.03937007874015843040 ) ) ;
#32160=ORIENTED_EDGE ( 'NONE', *, *, #34116, .F. ) ;
#32161=CARTESIAN_POINT ( 'NONE',  ( 0.9500414927467378812, -0.1787899950787401604, 1.392716535379308285 ) ) ;
#32163=( BOUNDED_CURVE ( )  B_SPLINE_CURVE ( 2, ( #12581, #4877, #27209, #41757, #30337, #23111, #30110, #22633, #8243 ),
 .UNSPECIFIED., .F., .F. ) 
 B_SPLINE_CURVE_WITH_KNOTS ( ( 3, 2, 2, 2, 3 ),
 ( 0.6500000000000000222, 0.6524999999999999689, 0.6550000000000000266, 0.6574999999999999734, 0.6600000000000000311 ),
 .UNSPECIFIED. ) 
 CURVE ( )  GEOMETRIC_REPRESENTATION_ITEM ( )  RATIONAL_B_SPLINE_CURVE ( ( 1.000000000000000000, 0.9238795325112899581, 1.000000000000000000, 0.9238795325112869605, 1.000000000000000000, 0.9238795325112869605, 1.000000000000000000, 0.9238795325112869605, 1.000000000000000000 ) ) 
 REPRESENTATION_ITEM ( '' )  ) ;
#32169=CARTESIAN_POINT ( 'NONE',  ( 0.6971942568897637749, 2.189545951927499583E-17, 1.695374015694267822 ) ) ;
#32170=CARTESIAN_POINT ( 'NONE',  ( 0.6971942568897637749, 2.189545951927499583E-17, 0.3174212597887562382 ) ) ;
#32176=CARTESIAN_POINT ( 'NONE',  ( -0.7185039370078739607, 1.928577636452523993E-17, 0.6102362203649134287 ) ) ;
#32178=CARTESIAN_POINT ( 'NONE',  ( 0.7495606340400177148, 0.1264236179284866091, 0.5487204723871811352 ) ) ;
#32180=CARTESIAN_POINT ( 'NONE',  ( -1.002407869896990045, 0.1264236179284866091, 0.9374999999462362288 ) ) ;
#32186=CARTESIAN_POINT ( 'NONE',  ( 0.8019270111902717657, 0.1787899950787401604, 1.653543307032850462 ) ) ;
#32189=CARTESIAN_POINT ( 'NONE',  ( 0.9500414927467377701, -0.1787899950787401604, 0.4872047243556847929 ) ) ;
#32190=ORIENTED_EDGE ( 'NONE', *, *, #44616, .F. ) ;
#32194=CARTESIAN_POINT ( 'NONE',  ( 0.8759842519685039353, 0.1787899950787401882, 0.5437992125446614589 ) ) ;
#32196=CARTESIAN_POINT ( 'NONE',  ( 1.054774247047244540, -0.07405724077823318263, 0.1033464566391498751 ) ) ;
#32198=CARTESIAN_POINT ( 'NONE',  ( 0.6971942568897648851, -0.07405724077823297447, 0.5561023621509617598 ) ) ;
#32199=CARTESIAN_POINT ( 'NONE',  ( -0.7185039370078746268, -0.06523048226347956391, 0.9768700787401572994 ) ) ;
#32200=CARTESIAN_POINT ( 'NONE',  ( -0.6971942568897648851, -0.07405724077823297447, 1.500984251914741607 ) ) ;
#32203=CARTESIAN_POINT ( 'NONE',  ( 0.6971942568897648851, -0.07405724077823297447, 1.230314960576156746 ) ) ;
#32204=CARTESIAN_POINT ( 'NONE',  ( -0.8107537697050253289, -0.1574803149606297803, 0.6963582676090082080 ) ) ;
#32205=CARTESIAN_POINT ( 'NONE',  ( -1.033464566929133799, 0.000000000000000000, 1.102362204616881947 ) ) ;
#32206=CARTESIAN_POINT ( 'NONE',  ( 0.8019270111902717657, 0.1787899950787401604, 1.845472440891119392 ) ) ;
#32207=CARTESIAN_POINT ( 'NONE',  ( -1.033464566929134687, -0.06523048226347956391, 1.424704724409449064 ) ) ;
#32208=CARTESIAN_POINT ( 'NONE',  ( -1.002407869896990045, -0.1264236179284866091, 0.9621062991588346103 ) ) ;
#32211=CARTESIAN_POINT ( 'NONE',  ( -0.7085582780037171791, 0.06187450949840840597, 0.03937007874015843734 ) ) ;
#32212=CARTESIAN_POINT ( 'NONE',  ( 1.054774247047244096, 0.000000000000000000, 0.3420275590013546751 ) ) ;
#32213=CARTESIAN_POINT ( 'NONE',  ( -1.054774247047244540, -0.07405724077823318263, 0.1377952755367876370 ) ) ;
#32215=CARTESIAN_POINT ( 'NONE',  ( -0.7495606340400177148, -0.1264236179284866091, 0.6373031495525354195 ) ) ;
#32216=CARTESIAN_POINT ( 'NONE',  ( 0.9873396505805591694, 0.1113553986120547346, 1.540354330601133803 ) ) ;
#32221=CARTESIAN_POINT ( 'NONE',  ( 0.7185039370078714072, 0.06523048226347728795, 1.788877952648379122 ) ) ;
#32222=CARTESIAN_POINT ( 'NONE',  ( 0.8019270111902717657, 0.1787899950787401604, 0.8267716534895444003 ) ) ;
#32223=EDGE_CURVE ( 'NONE', #38458, #34404, #34948, .T. ) ;
#32224=CARTESIAN_POINT ( 'NONE',  ( -0.8019270111902716547, -0.1787899950787401604, 1.742125984198204858 ) ) ;
#32227=VECTOR ( 'NONE', #45600, 39.37007874015748143 ) ;
#32235=CARTESIAN_POINT ( 'NONE',  ( 0.6971942568897637749, 2.189545951927499583E-17, 1.104822834591905556 ) ) ;
#32237=CARTESIAN_POINT ( 'NONE',  ( -1.033464566929134687, 0.06523048226347956391, 0.9867125983176703308 ) ) ;
#32238=CARTESIAN_POINT ( 'NONE',  ( 0.8019270111902717657, 0.1787899950787401604, 0.07381889758403178958 ) ) ;
#32241=CARTESIAN_POINT ( 'NONE',  ( -1.054774247047244540, -0.07405724077823318263, 0.4183070865604096578 ) ) ;
#32243=CARTESIAN_POINT ( 'NONE',  ( -0.7163004791323965836, -0.05128305946486693551, 1.984233574417522350 ) ) ;
#32245=CARTESIAN_POINT ( 'NONE',  ( 1.054774247047244540, -0.07405724077823318263, 1.245078740103716886 ) ) ;
#32246=CARTESIAN_POINT ( 'NONE',  ( 0.6971942568897637749, 2.189545951927499583E-17, 1.537893700733637736 ) ) ;
#32247=VECTOR ( 'NONE', #46878, 39.37007874015748143 ) ;
#32249=CARTESIAN_POINT ( 'NONE',  ( 0.9412147342319837628, -0.1574803149606297803, 1.656003937007873406 ) ) ;
#32250=FACE_OUTER_BOUND ( 'NONE', #29323, .T. ) ;
#32252=CARTESIAN_POINT ( 'NONE',  ( -0.8759842519685039353, -0.1574803149606299191, 1.102362204724409489 ) ) ;
#32254=DIRECTION ( 'NONE',  ( 1.822029033848725028E-16, 0.000000000000000000, 1.000000000000000000 ) ) ;
#32255=CARTESIAN_POINT ( 'NONE',  ( -0.9412147342319837628, 0.1574803149606300301, 1.779035432963339991 ) ) ;
#32257=CARTESIAN_POINT ( 'NONE',  ( 1.002407869896990045, -0.1264236179284866091, 0.09596456687537027741 ) ) ;
#32258=CARTESIAN_POINT ( 'NONE',  ( 1.002407869896990045, 0.1264236179284866091, 1.208169291284818980 ) ) ;
#32259=CARTESIAN_POINT ( 'NONE',  ( -0.8759842519685039353, -0.1574803149606299191, 0.5413385825696385156 ) ) ;
#32260=CARTESIAN_POINT ( 'NONE',  ( 0.6971942568897637749, 2.189545951927499583E-17, 1.936515747977732405 ) ) ;
#32261=CARTESIAN_POINT ( 'NONE',  ( 0.9873396505805591694, -0.1113553986120547346, 0.5068897636720007815 ) ) ;
#32262=ORIENTED_EDGE ( 'NONE', *, *, #6307, .T. ) ;
#32263=DIRECTION ( 'NONE',  ( 0.000000000000000000, 0.000000000000000000, -1.000000000000000000 ) ) ;
#32264=CARTESIAN_POINT ( 'NONE',  ( 0.8716041552374669266, 0.1747403318699642938, 0.03936765223768743521 ) ) ;
#32265=CARTESIAN_POINT ( 'NONE',  ( -0.8759842519685039353, -0.1574803149606299191, 0.4625984250893235838 ) ) ;
#32267=CARTESIAN_POINT ( 'NONE',  ( 0.8019270111902717657, -0.1787899950787401604, 1.387795275536786610 ) ) ;
#32268=CARTESIAN_POINT ( 'NONE',  ( 0.7185039370078739607, 1.928577636452523993E-17, 1.564960629921259949 ) ) ;
#32269=CARTESIAN_POINT ( 'NONE',  ( -1.033464566929134687, -0.06523048226347956391, 0.2337598424121580809 ) ) ;
#32271=EDGE_LOOP ( 'NONE', ( #45331, #23613, #6485, #44419 ) ) ;
#32274=ORIENTED_EDGE ( 'NONE', *, *, #36261, .T. ) ;
#32275=CARTESIAN_POINT ( 'NONE',  ( 0.9412147342319837628, -0.1574803149606297803, 1.291830708553889595 ) ) ;
#32277=CARTESIAN_POINT ( 'NONE',  ( 1.054774247047244096, 0.000000000000000000, 0.6569881889226141247 ) ) ;
#32278=VERTEX_POINT ( 'NONE', #36064 ) ;
#32279=EDGE_CURVE ( 'NONE', #42583, #1531, #20120, .T. ) ;
#32280=CARTESIAN_POINT ( 'NONE',  ( -0.7495606340400177148, 0.1264236179284866091, 1.336122047190330786 ) ) ;
#32283=CARTESIAN_POINT ( 'NONE',  ( -0.7185039370078746268, 0.06523048226347956391, 0.1845472440944883052 ) ) ;
#32284=ORIENTED_EDGE ( 'NONE', *, *, #25936, .T. ) ;
#32285=CARTESIAN_POINT ( 'NONE',  ( -1.054774247047244540, -0.07405724077823318263, 1.122047244040725422 ) ) ;
#32287=CARTESIAN_POINT ( 'NONE',  ( -1.054774247047244540, -0.07405724077823318263, 0.7726377952218265177 ) ) ;
#32288=CARTESIAN_POINT ( 'NONE',  ( -0.8759842519685039353, 0.1787899950787401882, 0.1943897637257641919 ) ) ;
#32292=ORIENTED_EDGE ( 'NONE', *, *, #40028, .F. ) ;
#32295=CARTESIAN_POINT ( 'NONE',  ( -0.7185039370078739607, 1.928577636452523993E-17, 1.712598425089322918 ) ) ;
#32300=CARTESIAN_POINT ( 'NONE',  ( -0.7495606340400177148, 0.1264236179284866091, 0.6274606298674959559 ) ) ;
#32303=VERTEX_POINT ( 'NONE', #20204 ) ;
#32305=CARTESIAN_POINT ( 'NONE',  ( -1.033464566929133799, 1.928577636452524610E-17, 2.869337061179095023E-17 ) ) ;
#32306=CARTESIAN_POINT ( 'NONE',  ( -0.8107537697050254399, 0.1574803149606300301, 0.1304133857192446289 ) ) ;
#32310=CARTESIAN_POINT ( 'NONE',  ( 1.002407869896990045, 0.1264236179284866091, 0.7012795275052913224 ) ) ;
#32315=CARTESIAN_POINT ( 'NONE',  ( 0.7185039370078739607, 1.928577636452523993E-17, 1.210629921259842590 ) ) ;
#32316=CARTESIAN_POINT ( 'NONE',  ( 0.9496616949729309587, -0.1608514975889442644, 1.989539966078783806 ) ) ;
#32317=CARTESIAN_POINT ( 'NONE',  ( 1.033464566929134687, -0.06523048226347956391, 1.739665354330709235 ) ) ;
#32320=CARTESIAN_POINT ( 'NONE',  ( 1.002407869896990045, 0.1264236179284866091, 0.6569881889226141247 ) ) ;
#32321=CARTESIAN_POINT ( 'NONE',  ( 1.033464566929133799, 1.928577636452524610E-17, 4.498031496062992574 ) ) ;
#32324=CARTESIAN_POINT ( 'NONE',  ( 0.7646288533564489232, -0.1113553986120547346, 0.6151574802074331050 ) ) ;
#32326=CARTESIAN_POINT ( 'NONE',  ( 1.002407869896990045, -0.1264236179284866091, 0.9227362204186770889 ) ) ;
#32327=ORIENTED_EDGE ( 'NONE', *, *, #7219, .T. ) ;
#32328=CARTESIAN_POINT ( 'NONE',  ( 0.7646288533564489232, 0.1113553986120547346, 1.481299212598425230 ) ) ;
#32329=CARTESIAN_POINT ( 'NONE',  ( -0.9873396505805591694, 0.1113553986120547346, 0.5265748031496062520 ) ) ;
#32333=DIRECTION ( 'NONE',  ( 1.822029033848725028E-16, 0.000000000000000000, 1.000000000000000000 ) ) ;
#32334=EDGE_CURVE ( 'NONE', #23930, #8150, #20518, .T. ) ;
#32335=VERTEX_POINT ( 'NONE', #13279 ) ;
#32336=CARTESIAN_POINT ( 'NONE',  ( -0.9500414927467378812, -0.1787899950787401604, 0.1328740156942679607 ) ) ;
#32337=CARTESIAN_POINT ( 'NONE',  ( 1.002407869896990045, -0.1264236179284866091, 1.990649606245448844 ) ) ;
#32339=CARTESIAN_POINT ( 'NONE',  ( -1.054774247047244096, 0.000000000000000000, 1.916830708607653477 ) ) ;
#32340=CARTESIAN_POINT ( 'NONE',  ( -0.6971942568897648851, -0.07405724077823297447, 1.579724409395055318 ) ) ;
#32341=CARTESIAN_POINT ( 'NONE',  ( 0.6971942568897648851, 0.07405724077823318263, 0.8316929133320636325 ) ) ;
#32342=ADVANCED_FACE ( 'NONE', ( #27912 ), #9680, .T. ) ;
#32343=CARTESIAN_POINT ( 'NONE',  ( -1.054774247047244096, 0.000000000000000000, 1.045767716481669440 ) ) ;
#32344=CARTESIAN_POINT ( 'NONE',  ( -1.002407869896990045, -0.1264236179284866091, 0.3764763778989925203 ) ) ;
#32345=CARTESIAN_POINT ( 'NONE',  ( -0.9873396505805591694, -0.1113553986120547346, 0.6742125984251968740 ) ) ;
#32346=CARTESIAN_POINT ( 'NONE',  ( -0.8759842519685039353, 0.1787899950787401882, 1.847933070812378009 ) ) ;
#32348=CARTESIAN_POINT ( 'NONE',  ( -1.033464566929134687, -0.06523048226347956391, 1.897145669291339320 ) ) ;
#32349=CARTESIAN_POINT ( 'NONE',  ( -0.8759842519685039353, 0.000000000000000000, 0.000000000000000000 ) ) ;
#32353=CARTESIAN_POINT ( 'NONE',  ( 0.7185039370078746268, -0.06523048226347956391, 1.045767716427905114 ) ) ;
#32354=CARTESIAN_POINT ( 'NONE',  ( -1.002407869896990045, -0.1264236179284866091, 0.09596456687537027741 ) ) ;
#32358=CARTESIAN_POINT ( 'NONE',  ( -1.054774247047244540, -0.07405724077823318263, 1.284448818843874518 ) ) ;
#32359=ORIENTED_EDGE ( 'NONE', *, *, #44668, .T. ) ;
#32363=ADVANCED_FACE ( 'NONE', ( #10868 ), #35781, .T. ) ;
#32365=CARTESIAN_POINT ( 'NONE',  ( -0.9412147342319837628, -0.1574803149606297803, 1.370570866034205748 ) ) ;
#32367=CARTESIAN_POINT ( 'NONE',  ( -0.9412147342319837628, -0.1574803149606297803, 0.7111220472440957785 ) ) ;
#32368=CARTESIAN_POINT ( 'NONE',  ( 0.8759842519685039353, -0.1787899950787401882, 0.4109251967966299213 ) ) ;
#32370=CARTESIAN_POINT ( 'NONE',  ( 0.8759842519685039353, 0.1574803149606299191, 1.781496062884598164 ) ) ;
#32373=CARTESIAN_POINT ( 'NONE',  ( 0.7185039370078746268, 0.06523048226347956391, 0.8538385826771660581 ) ) ;
#32378=CARTESIAN_POINT ( 'NONE',  ( 0.9412147342319837628, 0.1574803149606300301, 0.1254921258767249526 ) ) ;
#32381=CARTESIAN_POINT ( 'NONE',  ( -0.8759842519685039353, -0.1574803149606299191, 0.6200787400499527813 ) ) ;
#32385=CARTESIAN_POINT ( 'NONE',  ( 0.7185039370078746268, 0.06523048226347956391, 0.9621062991050720603 ) ) ;
#32386=CARTESIAN_POINT ( 'NONE',  ( 1.033464566929133799, 1.928577636452524610E-17, 4.498031496062992574 ) ) ;
#32387=ADVANCED_FACE ( 'NONE', ( #35 ), #2442, .F. ) ;
#32388=CARTESIAN_POINT ( 'NONE',  ( -0.8019270111902717657, 0.1787899950787401604, 0.4281496062454490659 ) ) ;
#32389=VERTEX_POINT ( 'NONE', #4490 ) ;
#32390=ORIENTED_EDGE ( 'NONE', *, *, #7103, .F. ) ;
#32391=CARTESIAN_POINT ( 'NONE',  ( -0.6971942568897648851, -0.07405724077823297447, 1.663385826717890925 ) ) ;
#32392=CARTESIAN_POINT ( 'NONE',  ( 0.9500414927467378812, 0.1787899950787401604, 1.609251968450173376 ) ) ;
#32394=CARTESIAN_POINT ( 'NONE',  ( -0.8759842519685039353, -0.1787899950787401882, 0.7652559054580472253 ) ) ;
#32396=CARTESIAN_POINT ( 'NONE',  ( 1.054774247047244540, -0.07405724077823318263, 0.2214566928596220785 ) ) ;
#32397=CARTESIAN_POINT ( 'NONE',  ( -0.7185039370078739607, 1.928577636452523993E-17, 1.673228346349165285 ) ) ;
#32398=CARTESIAN_POINT ( 'NONE',  ( 0.9500414927467377701, -0.1787899950787401604, 0.7283464566391492090 ) ) ;
#32399=CARTESIAN_POINT ( 'NONE',  ( -1.054774247047244540, -0.07405724077823318263, 0.6889763778989936860 ) ) ;
#32401=CARTESIAN_POINT ( 'NONE',  ( 0.7646288533564489232, 0.1113553986120547346, 0.9202755904436535905 ) ) ;
#32404=CARTESIAN_POINT ( 'NONE',  ( -0.7495606340400177148, -0.1264236179284866091, 1.429625984198204858 ) ) ;
#32406=CARTESIAN_POINT ( 'NONE',  ( -0.7185039370078739607, 1.928577636452523993E-17, 1.486220472440944906 ) ) ;
#32408=CARTESIAN_POINT ( 'NONE',  ( -1.033464566929134687, 0.06523048226347956391, 0.4060039370078741272 ) ) ;
#32409=CARTESIAN_POINT ( 'NONE',  ( 0.6971942568897637749, 2.189545951927499583E-17, 1.424704724355685181 ) ) ;
#32410=CARTESIAN_POINT ( 'NONE',  ( -0.7185039370078746268, 0.06523048226347956391, 0.3715551180027091283 ) ) ;
#32415=CARTESIAN_POINT ( 'NONE',  ( 0.7495606340400177148, -0.1264236179284866091, 1.424704724355685181 ) ) ;
#32428=CARTESIAN_POINT ( 'NONE',  ( 0.6971942568897626646, -0.07405724077823297447, 0.6742125983714335469 ) ) ;
#32429=CARTESIAN_POINT ( 'NONE',  ( -1.054774247047244540, -0.07405724077823318263, 0.9301181101824563813 ) ) ;
#32430=CARTESIAN_POINT ( 'NONE',  ( -0.8720834684628424593, 0.1749638022103473245, 0.03937007874015842346 ) ) ;
#32431=LINE ( 'NONE', #25214, #2514 ) ;
#32434=CARTESIAN_POINT ( 'NONE',  ( -0.7185039370078739607, 1.928577636452523993E-17, 1.486220472440944906 ) ) ;
#32435=CARTESIAN_POINT ( 'NONE',  ( 1.002407869896990045, 0.1264236179284866091, 1.685531496009228469 ) ) ;
#32438=EDGE_CURVE ( 'NONE', #12102, #19774, #40451, .T. ) ;
#32440=ORIENTED_EDGE ( 'NONE', *, *, #37498, .F. ) ;
#32443=CARTESIAN_POINT ( 'NONE',  ( -0.8019270111902717657, 0.1787899950787401604, 0.3937007873478115538 ) ) ;
#32444=CARTESIAN_POINT ( 'NONE',  ( 0.6971942568897637749, 2.189545951927499583E-17, 0.6717519684501732646 ) ) ;
#32446=CARTESIAN_POINT ( 'NONE',  ( 0.6971942568897626646, -0.07405724077823297447, 0.1279527558517483676 ) ) ;
#32447=( BOUNDED_CURVE ( )  B_SPLINE_CURVE ( 2, ( #22321, #43414, #3414, #36007, #10863, #40049, #17794, #18030, #47019 ),
 .UNSPECIFIED., .F., .T. ) 
 B_SPLINE_CURVE_WITH_KNOTS ( ( 3, 2, 2, 2, 3 ),
 ( 0.6500000000000000222, 0.6524999999999999689, 0.6550000000000000266, 0.6574999999999999734, 0.6600000000000000311 ),
 .UNSPECIFIED. ) 
 CURVE ( )  GEOMETRIC_REPRESENTATION_ITEM ( )  RATIONAL_B_SPLINE_CURVE ( ( 1.000000000000000000, 0.9238795325112899581, 1.000000000000000000, 0.9238795325112869605, 1.000000000000000000, 0.9238795325112869605, 1.000000000000000000, 0.9238795325112869605, 1.000000000000000000 ) ) 
 REPRESENTATION_ITEM ( '' )  ) ;
#32449=CARTESIAN_POINT ( 'NONE',  ( 0.7495606340400177148, 0.1264236179284866091, 0.5880905511273386566 ) ) ;
#32451=CARTESIAN_POINT ( 'NONE',  ( -0.6971942568897637749, 2.189545951927499583E-17, 1.616633858213952779 ) ) ;
#32453=CARTESIAN_POINT ( 'NONE',  ( -0.6971942568897648851, 0.07405724077823318263, 1.107283464513165949 ) ) ;
#32455=CARTESIAN_POINT ( 'NONE',  ( 1.002407869896990045, 0.1264236179284866091, 1.173720472387181246 ) ) ;
#32456=CARTESIAN_POINT ( 'NONE',  ( -0.7185039370078746268, -0.06523048226347956391, 0.6914370077664893088 ) ) ;
#32457=CARTESIAN_POINT ( 'NONE',  ( 1.002407869896990045, 0.1264236179284866091, 1.877460629867496067 ) ) ;
#32458=CARTESIAN_POINT ( 'NONE',  ( -1.033464566929134687, -0.06523048226347956391, 0.5979330708661413363 ) ) ;
#32459=CARTESIAN_POINT ( 'NONE',  ( -0.8759842519685039353, 0.1787899950787401882, 0.9374999999462362288 ) ) ;
#32461=CARTESIAN_POINT ( 'NONE',  ( 0.8759842519685039353, 0.1787899950787401882, 0.2337598424659216578 ) ) ;
#32462=CARTESIAN_POINT ( 'NONE',  ( -1.002407869896990045, 0.1264236179284866091, 0.2239173227808822775 ) ) ;
#32464=CARTESIAN_POINT ( 'NONE',  ( -0.7495606340400177148, 0.1264236179284866091, 0.7062007873478109987 ) ) ;
#32465=CARTESIAN_POINT ( 'NONE',  ( 0.9873396505805591694, -0.1113553986120547346, 1.530511810916094451 ) ) ;
#32466=ORIENTED_EDGE ( 'NONE', *, *, #24833, .T. ) ;
#32468=CARTESIAN_POINT ( 'NONE',  ( 0.8019270111902717657, -0.1787899950787401604, 0.7627952755367881643 ) ) ;
#32469=CARTESIAN_POINT ( 'NONE',  ( 0.7495606340400177148, -0.1264236179284866091, 1.035925196796629866 ) ) ;
#32470=CARTESIAN_POINT ( 'NONE',  ( -0.7495606340400177148, -0.1264236179284866091, 1.897145669237574772 ) ) ;
#32471=( BOUNDED_CURVE ( )  B_SPLINE_CURVE ( 2, ( #32397, #36917, #11056, #28565, #17508, #21579, #46974, #39546, #13918 ),
 .UNSPECIFIED., .F., .T. ) 
 B_SPLINE_CURVE_WITH_KNOTS ( ( 3, 2, 2, 2, 3 ),
 ( 0.8299999999999999600, 0.8325000000000000178, 0.8349999999999999645, 0.8375000000000000222, 0.8399999999999999689 ),
 .UNSPECIFIED. ) 
 CURVE ( )  GEOMETRIC_REPRESENTATION_ITEM ( )  RATIONAL_B_SPLINE_CURVE ( ( 1.000000000000000000, 0.9238795325112939549, 1.000000000000000000, 0.9238795325112869605, 1.000000000000000000, 0.9238795325112869605, 1.000000000000000000, 0.9238795325112869605, 1.000000000000000000 ) ) 
 REPRESENTATION_ITEM ( '' )  ) ;
#32472=DIRECTION ( 'NONE',  ( -1.000000000000000000, 0.000000000000000000, 0.000000000000000000 ) ) ;
#32474=VERTEX_POINT ( 'NONE', #42573 ) ;
#32476=ORIENTED_EDGE ( 'NONE', *, *, #29559, .F. ) ;
#32477=CARTESIAN_POINT ( 'NONE',  ( 1.054774247047244540, 0.07405724077823318263, 1.087598425143086578 ) ) ;
#32478=DIRECTION ( 'NONE',  ( 0.000000000000000000, 0.000000000000000000, 1.000000000000000000 ) ) ;
#32481=CARTESIAN_POINT ( 'NONE',  ( 0.7646288533564489232, 0.1113553986120547346, 1.953740157480315043 ) ) ;
#32485=CARTESIAN_POINT ( 'NONE',  ( -0.8019270111902716547, -0.1787899950787401604, 0.5265748030958428139 ) ) ;
#32488=CARTESIAN_POINT ( 'NONE',  ( 0.9500414927467378812, 0.1787899950787401604, 1.176181102308441417 ) ) ;
#32489=CARTESIAN_POINT ( 'NONE',  ( 0.8019270111902716547, -0.1787899950787401604, 1.545275590497419138 ) ) ;
#32493=CARTESIAN_POINT ( 'NONE',  ( 0.8759842519685039353, 0.000000000000000000, 4.498031496062992574 ) ) ;
#32494=CARTESIAN_POINT ( 'NONE',  ( -0.9873396505805591694, 0.1113553986120547346, 1.737204724301921299 ) ) ;
#32495=CARTESIAN_POINT ( 'NONE',  ( 0.8019270111902717657, 0.1787899950787401604, 0.1525590550643468046 ) ) ;
#32496=CARTESIAN_POINT ( 'NONE',  ( 1.054774247047244540, -0.07405724077823318263, 1.082677165300567346 ) ) ;
#32498=CARTESIAN_POINT ( 'NONE',  ( 0.8107537697050253289, -0.1574803149606297803, 0.4601377951680635792 ) ) ;
#32499=VERTEX_POINT ( 'NONE', #42353 ) ;
#32501=CARTESIAN_POINT ( 'NONE',  ( -0.7185039370078739607, 0.000000000000000000, -2.869337061179095023E-17 ) ) ;
#32502=CARTESIAN_POINT ( 'NONE',  ( 0.9530870782177205403, 0.1508571639167848033, 0.03936674302998629388 ) ) ;
#32503=CARTESIAN_POINT ( 'NONE',  ( -1.033464566929134687, 0.06523048226347956391, 0.3961614172153076763 ) ) ;
#32504=CARTESIAN_POINT ( 'NONE',  ( -0.9412147342319837628, -0.1574803149606297803, 1.537893700787401841 ) ) ;
#32505=CARTESIAN_POINT ( 'NONE',  ( 0.8759842519685039353, 0.1787899950787401882, 1.449311023568283341 ) ) ;
#32507=CARTESIAN_POINT ( 'NONE',  ( -0.9412147342319837628, -0.1574803149606297803, 1.774114173228345859 ) ) ;
#32508=CARTESIAN_POINT ( 'NONE',  ( -1.033464566929133799, 0.000000000000000000, 0.2362204723334177248 ) ) ;
#32510=ORIENTED_EDGE ( 'NONE', *, *, #3680, .F. ) ;
#32512=VERTEX_POINT ( 'NONE', #2335 ) ;
#32513=DIRECTION ( 'NONE',  ( 1.822029033848725028E-16, 0.000000000000000000, 1.000000000000000000 ) ) ;
#32515=ORIENTED_EDGE ( 'NONE', *, *, #30488, .F. ) ;
#32516=CARTESIAN_POINT ( 'NONE',  ( 0.8759842519685039353, -0.1787899950787401882, 0.6077755904974173617 ) ) ;
#32519=CARTESIAN_POINT ( 'NONE',  ( -0.7495606340400177148, 0.1264236179284866091, 1.104822834591905556 ) ) ;
#32520=CARTESIAN_POINT ( 'NONE',  ( -0.9873396505805591694, -0.1113553986120547346, 0.2017716535433070890 ) ) ;
#32521=ORIENTED_EDGE ( 'NONE', *, *, #44616, .T. ) ;
#32522=CARTESIAN_POINT ( 'NONE',  ( -0.7495606340400177148, 0.1264236179284866091, 1.060531496009228247 ) ) ;
#32523=CARTESIAN_POINT ( 'NONE',  ( -1.002407869896990045, -0.1264236179284866091, 0.2583661416785200671 ) ) ;
#32524=DIRECTION ( 'NONE',  ( 1.822029033848725028E-16, 0.000000000000000000, 1.000000000000000000 ) ) ;
#32532=ORIENTED_EDGE ( 'NONE', *, *, #9224, .T. ) ;
#32533=CARTESIAN_POINT ( 'NONE',  ( 1.033464566929133799, 0.000000000000000000, 0.6791338582677166613 ) ) ;
#32535=CARTESIAN_POINT ( 'NONE',  ( -0.7495606340400177148, -0.1264236179284866091, 0.6373031495525354195 ) ) ;
#32538=CARTESIAN_POINT ( 'NONE',  ( -0.6971942568897637749, 2.189545951927499583E-17, 1.818405511757259729 ) ) ;
#32543=CARTESIAN_POINT ( 'NONE',  ( -1.002407869896990045, -0.1264236179284866091, 0.06151574797773248782 ) ) ;
#32545=CARTESIAN_POINT ( 'NONE',  ( 0.7646288533564489232, 0.1113553986120547346, 0.6938976377952755792 ) ) ;
#32547=DIRECTION ( 'NONE',  ( 1.000000000000000000, 0.000000000000000000, 0.000000000000000000 ) ) ;
#32548=CARTESIAN_POINT ( 'NONE',  ( -0.7646288533564489232, -0.1113553986120547346, 1.402559055010582645 ) ) ;
#32549=CARTESIAN_POINT ( 'NONE',  ( 0.6971942568897637749, 2.189545951927499583E-17, 0.8341535432533228045 ) ) ;
#32555=CARTESIAN_POINT ( 'NONE',  ( 0.7185039370078739607, 1.928577636452523993E-17, 1.250000000000000000 ) ) ;
#32557=CARTESIAN_POINT ( 'NONE',  ( 0.8759842519685039353, 0.000000000000000000, 4.498031496062992574 ) ) ;
#32558=CARTESIAN_POINT ( 'NONE',  ( 0.8759842519685039353, -0.1574803149606299191, 1.850393700787401619 ) ) ;
#32559=CARTESIAN_POINT ( 'NONE',  ( 0.8019270111902716547, -0.1787899950787401604, 0.6791338582139527791 ) ) ;
#32563=AXIS2_PLACEMENT_3D ( 'NONE', #1423, #26150, #16082 ) ;
#32564=CARTESIAN_POINT ( 'NONE',  ( -0.8107537697050254399, -0.1574803149606297803, 0.3813976376877488139 ) ) ;
#32570=CARTESIAN_POINT ( 'NONE',  ( 0.7495606340400177148, -0.1264236179284866091, 0.9522637794737952577 ) ) ;
#32576=CARTESIAN_POINT ( 'NONE',  ( -0.6971942568897626646, 0.07405724077823318263, 0.07874015742655145200 ) ) ;
#32577=CARTESIAN_POINT ( 'NONE',  ( 0.7495606340400177148, 0.1264236179284866091, 1.970964566875370139 ) ) ;
#32579=CARTESIAN_POINT ( 'NONE',  ( -0.7185039370078739607, 0.000000000000000000, -2.869337061179095023E-17 ) ) ;
#32580=CARTESIAN_POINT ( 'NONE',  ( -1.002407869896990045, 0.1264236179284866091, 1.719980314906866203 ) ) ;
#32581=CARTESIAN_POINT ( 'NONE',  ( -0.9500414927467378812, -0.1787899950787401604, 1.117125984198206412 ) ) ;
#32582=CARTESIAN_POINT ( 'NONE',  ( -0.8759842519685039353, -0.1787899950787401882, 0.3321850393163153226 ) ) ;
#32583=( BOUNDED_CURVE ( )  B_SPLINE_CURVE ( 2, ( #21701, #36335, #6597, #43730, #10933, #7323, #21448, #17623, #24585 ),
 .UNSPECIFIED., .F., .T. ) 
 B_SPLINE_CURVE_WITH_KNOTS ( ( 3, 2, 2, 2, 3 ),
 ( 0.04000000000000000083, 0.04250000000000000305, 0.04499999999999999833, 0.04750000000000000056, 0.05000000000000000278 ),
 .UNSPECIFIED. ) 
 CURVE ( )  GEOMETRIC_REPRESENTATION_ITEM ( )  RATIONAL_B_SPLINE_CURVE ( ( 1.000000000000000000, 0.9238795325112869605, 1.000000000000000000, 0.9238795325112869605, 1.000000000000000000, 0.9238795325112869605, 1.000000000000000000, 0.9238795325112869605, 1.000000000000000000 ) ) 
 REPRESENTATION_ITEM ( '' )  ) ;
#32585=CARTESIAN_POINT ( 'NONE',  ( -1.054774247047244540, 0.07405724077823318263, 1.919291338528913871 ) ) ;
#32590=CARTESIAN_POINT ( 'NONE',  ( -1.002407869896990045, 0.1264236179284866091, 0.1451771653005673179 ) ) ;
#32592=ORIENTED_EDGE ( 'NONE', *, *, #43036, .F. ) ;
#32594=CARTESIAN_POINT ( 'NONE',  ( -1.002407869896990045, 0.1264236179284866091, 1.449311023568283341 ) ) ;
#32596=CARTESIAN_POINT ( 'NONE',  ( 0.9500414927467378812, -0.1787899950787401604, 1.471456692859622217 ) ) ;
#32598=VECTOR ( 'NONE', #23911, 39.37007874015748143 ) ;
#32602=DIRECTION ( 'NONE',  ( -1.000000000000000000, 0.000000000000000000, 0.000000000000000000 ) ) ;
#32604=CARTESIAN_POINT ( 'NONE',  ( 0.9412147342319837628, 0.1574803149606300301, 0.3321850393700786497 ) ) ;
#32606=CARTESIAN_POINT ( 'NONE',  ( -0.9873396505805591694, -0.1113553986120547346, 0.9793307085538898171 ) ) ;
#32607=CARTESIAN_POINT ( 'NONE',  ( 0.9500414927467378812, 0.1787899950787401604, 0.3887795275052913224 ) ) ;
#32609=CARTESIAN_POINT ( 'NONE',  ( 1.033464566929133799, 0.000000000000000000, 1.889763779420031486 ) ) ;
#32611=EDGE_CURVE ( 'NONE', #43027, #29787, #19845, .T. ) ;
#32613=CARTESIAN_POINT ( 'NONE',  ( 1.033464566929134687, 0.06523048226347956391, 0.7997047244094482865 ) ) ;
#32615=CARTESIAN_POINT ( 'NONE',  ( -1.033464566929134687, -0.06523048226347956391, 0.4798228346456689386 ) ) ;
#32616=CARTESIAN_POINT ( 'NONE',  ( 1.033464566929134687, 0.06523048226347956391, 1.508366141732284671 ) ) ;
#32617=CARTESIAN_POINT ( 'NONE',  ( 1.033464566929133799, 0.000000000000000000, 0.1968503935932602311 ) ) ;
#32620=CYLINDRICAL_SURFACE ( 'NONE', #5749, 0.1574803149606299191 ) ;
#32623=CARTESIAN_POINT ( 'NONE',  ( -0.9873396505805591694, -0.1113553986120547346, 0.1525590550105832555 ) ) ;
#32625=CARTESIAN_POINT ( 'NONE',  ( 0.7646288533564489232, 0.1113553986120547346, 1.038385826664126155 ) ) ;
#32626=CARTESIAN_POINT ( 'NONE',  ( 1.033464566929133799, 0.000000000000000000, 0.5216535433070865757 ) ) ;
#32628=ORIENTED_EDGE ( 'NONE', *, *, #3532, .F. ) ;
#32630=CARTESIAN_POINT ( 'NONE',  ( -0.8019270111902717657, -0.1787899950787401604, 1.668307086560410157 ) ) ;
#32631=CARTESIAN_POINT ( 'NONE',  ( 0.7495606340400177148, 0.1264236179284866091, 1.537893700733637736 ) ) ;
#32633=CARTESIAN_POINT ( 'NONE',  ( -0.6971942568897637749, 2.189545951927499583E-17, 0.7554133857730077617 ) ) ;
#32634=CARTESIAN_POINT ( 'NONE',  ( 0.8759842519685039353, 0.1787899950787401882, 0.2337598424659216578 ) ) ;
#32635=LINE ( 'NONE', #7434, #41128 ) ;
#32636=CARTESIAN_POINT ( 'NONE',  ( 0.7495606340400177148, -0.1264236179284866091, 0.7997047243556849594 ) ) ;
#32637=CARTESIAN_POINT ( 'NONE',  ( -0.8759842519685039353, 0.1787899950787401882, 0.7012795275052913224 ) ) ;
#32638=EDGE_CURVE ( 'NONE', #4710, #38209, #46817, .T. ) ;
#32642=CARTESIAN_POINT ( 'NONE',  ( -0.7646288533564489232, 0.1113553986120547346, 1.943897637687747926 ) ) ;
#32643=VERTEX_POINT ( 'NONE', #19611 ) ;
#32645=CARTESIAN_POINT ( 'NONE',  ( -0.8107537697050253289, -0.1574803149606297803, 0.4699803149606304742 ) ) ;
#32646=CARTESIAN_POINT ( 'NONE',  ( 1.054774247047244540, -0.07405724077823318263, 1.520669291284818758 ) ) ;
#32650=ORIENTED_EDGE ( 'NONE', *, *, #25450, .T. ) ;
#32652=DIRECTION ( 'NONE',  ( 0.000000000000000000, 0.000000000000000000, 1.000000000000000000 ) ) ;
#32654=VECTOR ( 'NONE', #1775, 39.37007874015748143 ) ;
#32657=EDGE_CURVE ( 'NONE', #12042, #29787, #4249, .T. ) ;
#32659=CARTESIAN_POINT ( 'NONE',  ( 0.9500414927467378812, -0.1787899950787401604, 1.707677165300566235 ) ) ;
#32660=CARTESIAN_POINT ( 'NONE',  ( 1.054774247047244540, 0.07405724077823318263, 0.3789370078202520253 ) ) ;
#32665=CARTESIAN_POINT ( 'NONE',  ( 0.7495606340400177148, -0.1264236179284866091, 0.5979330708123780092 ) ) ;
#32666=CARTESIAN_POINT ( 'NONE',  ( -0.9500414927467377701, -0.1787899950787401604, 1.003937007820253413 ) ) ;
#32667=CARTESIAN_POINT ( 'NONE',  ( 0.9873396505805591694, 0.1113553986120547346, 0.9891732282389291697 ) ) ;
#32669=CARTESIAN_POINT ( 'NONE',  ( 0.7646288533564489232, 0.1113553986120547346, 0.9596456691838111119 ) ) ;
#32670=CARTESIAN_POINT ( 'NONE',  ( 0.8759842519685039353, 0.1787899950787401882, 1.729822834591905556 ) ) ;
#32671=CARTESIAN_POINT ( 'NONE',  ( -0.7185039370078739607, 1.928577636452523993E-17, 0.8858267715460158565 ) ) ;
#32672=CARTESIAN_POINT ( 'NONE',  ( 0.9412147342319837628, 0.1574803149606300301, 0.1254921258767249526 ) ) ;
#32678=CARTESIAN_POINT ( 'NONE',  ( -0.8019270111902717657, -0.1787899950787401604, 0.4478346456155276045 ) ) ;
#32679=CARTESIAN_POINT ( 'NONE',  ( 1.054774247047244096, 0.000000000000000000, 0.5339566928596221063 ) ) ;
#32681=CARTESIAN_POINT ( 'NONE',  ( 0.6971942568897637749, 2.189545951927499583E-17, 0.08612204719033110523 ) ) ;
#32682=CARTESIAN_POINT ( 'NONE',  ( 0.9873396505805591694, 0.1113553986120547346, 1.107283464459401623 ) ) ;
#32683=CARTESIAN_POINT ( 'NONE',  ( -0.6971942568897648851, -0.07405724077823297447, 1.658464566875369472 ) ) ;
#32686=CARTESIAN_POINT ( 'NONE',  ( 0.6971942568897648851, 0.07405724077823318263, 1.146653543253323582 ) ) ;
#32687=CARTESIAN_POINT ( 'NONE',  ( 1.002407869896990045, -0.1264236179284866091, 1.828248031442299082 ) ) ;
#32688=CARTESIAN_POINT ( 'NONE',  ( -0.7185039370078746268, 0.06523048226347956391, 0.6176181102362200415 ) ) ;
#32689=CARTESIAN_POINT ( 'NONE',  ( -0.6971942568897626646, -0.07405724077823297447, 0.9498031495525356416 ) ) ;
#32690=CARTESIAN_POINT ( 'NONE',  ( -0.8759842519685039353, -0.1574803149606299191, 1.614173228346456712 ) ) ;
#32692=CARTESIAN_POINT ( 'NONE',  ( 0.8019270111902716547, 0.1787899950787401604, 0.3543307086076538659 ) ) ;
#32693=CARTESIAN_POINT ( 'NONE',  ( -0.7495606340400177148, 0.1264236179284866091, 0.2731299212060791515 ) ) ;
#32695=CARTESIAN_POINT ( 'NONE',  ( -0.7495606340400177148, 0.1264236179284866091, 0.7849409448281259305 ) ) ;
#32696=CARTESIAN_POINT ( 'NONE',  ( 0.7646288533564489232, 0.1113553986120547346, 1.550196850286173156 ) ) ;
#32697=ORIENTED_EDGE ( 'NONE', *, *, #575, .F. ) ;
#32698=EDGE_CURVE ( 'NONE', #32512, #39036, #6636, .T. ) ;
#32700=CARTESIAN_POINT ( 'NONE',  ( 0.6971942568897637749, 2.189545951927499583E-17, 0.7947834645131652831 ) ) ;
#32701=CARTESIAN_POINT ( 'NONE',  ( 0.8019270111902716547, 0.1787899950787401604, 1.102362204670646495 ) ) ;
#32702=CARTESIAN_POINT ( 'NONE',  ( -0.6971942568897648851, -0.07405724077823297447, 1.855314960576157635 ) ) ;
#32703=CARTESIAN_POINT ( 'NONE',  ( 0.9500414927467378812, 0.1787899950787401604, 1.919291338528913871 ) ) ;
#32707=EDGE_LOOP ( 'NONE', ( #27653, #35959, #31398, #37905 ) ) ;
#32709=ADVANCED_FACE ( 'NONE', ( #24624 ), #29223, .T. ) ;
#32712=CARTESIAN_POINT ( 'NONE',  ( 0.8759842519685039353, 0.1787899950787401882, 1.134350393647023614 ) ) ;
#32717=CARTESIAN_POINT ( 'NONE',  ( 1.033464566929134687, -0.06523048226347956391, 1.936515748031494955 ) ) ;
#32720=( BOUNDED_CURVE ( )  B_SPLINE_CURVE ( 2, ( #10390, #24521, #39120, #28861, #24995, #6294, #20683, #6056, #35323 ),
 .UNSPECIFIED., .F., .F. ) 
 B_SPLINE_CURVE_WITH_KNOTS ( ( 3, 2, 2, 2, 3 ),
 ( 0.4500000000000000111, 0.4525000000000000133, 0.4550000000000000155, 0.4575000000000000178, 0.4600000000000000200 ),
 .UNSPECIFIED. ) 
 CURVE ( )  GEOMETRIC_REPRESENTATION_ITEM ( )  RATIONAL_B_SPLINE_CURVE ( ( 1.000000000000000000, 0.9238795325112869605, 1.000000000000000000, 0.9238795325112869605, 1.000000000000000000, 0.9238795325112869605, 1.000000000000000000, 0.9238795325112869605, 1.000000000000000000 ) ) 
 REPRESENTATION_ITEM ( '' )  ) ;
#32721=CARTESIAN_POINT ( 'NONE',  ( -0.8019270111902716547, 0.1787899950787401604, 0.4330708660879683536 ) ) ;
#32725=CARTESIAN_POINT ( 'NONE',  ( 0.7495606340400177148, -0.1264236179284866091, 1.272145669237574772 ) ) ;
#32726=CARTESIAN_POINT ( 'NONE',  ( 0.6971942568897648851, -0.07405724077823297447, 1.619094488135213838 ) ) ;
#32727=CARTESIAN_POINT ( 'NONE',  ( -0.5314960629921260393, 0.000000000000000000, 4.498031496062992574 ) ) ;
#32729=CARTESIAN_POINT ( 'NONE',  ( -0.7672715001790547662, 0.1194512761122965006, 1.980665997130102163 ) ) ;
#32730=CARTESIAN_POINT ( 'NONE',  ( 0.8107537697050254399, -0.1574803149606297803, 0.8144685038294804391 ) ) ;
#32731=CARTESIAN_POINT ( 'NONE',  ( -0.7185039370078739607, 1.928577636452523993E-17, 1.712598425089322918 ) ) ;
#32732=CARTESIAN_POINT ( 'NONE',  ( 0.7495606340400177148, -0.1264236179284866091, 0.1648622046706460786 ) ) ;
#32733=CARTESIAN_POINT ( 'NONE',  ( 0.7010592508071858964, 0.01453562945798193839, 0.03937031133914711128 ) ) ;
#32734=CARTESIAN_POINT ( 'NONE',  ( 0.8759842519685039353, -0.1787899950787401882, 1.114665354276944909 ) ) ;
#32736=CARTESIAN_POINT ( 'NONE',  ( 1.033464566929134687, -0.06523048226347956391, 1.227854330708661124 ) ) ;
#32737=CARTESIAN_POINT ( 'NONE',  ( -0.9500414927467378812, -0.1787899950787401604, 1.235236220418678199 ) ) ;
#32738=CARTESIAN_POINT ( 'NONE',  ( 1.033464566929133799, 0.000000000000000000, 0.5118110235145204578 ) ) ;
#32741=CARTESIAN_POINT ( 'NONE',  ( 0.8636164050717508589, 0.1748576815465697487, 0.03937204453775523805 ) ) ;
#32742=CARTESIAN_POINT ( 'NONE',  ( -0.8759842519685039353, 0.1574803149606299191, 0.4035433069790866356 ) ) ;
#32743=VERTEX_POINT ( 'NONE', #21492 ) ;
#32744=CARTESIAN_POINT ( 'NONE',  ( 0.8759842519685039353, -0.1787899950787401882, 1.390255905458047447 ) ) ;
#32745=CARTESIAN_POINT ( 'NONE',  ( -0.9412147342319837628, 0.1574803149606300301, 1.631397637795275468 ) ) ;
#32746=CARTESIAN_POINT ( 'NONE',  ( 1.033464566929133799, 0.000000000000000000, 1.663385826771653697 ) ) ;
#32751=( BOUNDED_CURVE ( )  B_SPLINE_CURVE ( 2, ( #25614, #21517, #29248, #43797, #31863, #6187, #172, #15778, #40885 ),
 .UNSPECIFIED., .F., .T. ) 
 B_SPLINE_CURVE_WITH_KNOTS ( ( 3, 2, 2, 2, 3 ),
 ( 0.9300000000000000488, 0.9324999999999999956, 0.9350000000000000533, 0.9375000000000000000, 0.9399999999999999467 ),
 .UNSPECIFIED. ) 
 CURVE ( )  GEOMETRIC_REPRESENTATION_ITEM ( )  RATIONAL_B_SPLINE_CURVE ( ( 1.000000000000000000, 0.9238795325112869605, 1.000000000000000000, 0.9238795325112869605, 1.000000000000000000, 0.9238795325112869605, 1.000000000000000000, 0.9238795325112829637, 1.000000000000000000 ) ) 
 REPRESENTATION_ITEM ( '' )  ) ;
#32753=DIRECTION ( 'NONE',  ( -1.000000000000000000, 0.000000000000000000, 0.000000000000000000 ) ) ;
#32754=( BOUNDED_CURVE ( )  B_SPLINE_CURVE ( 2, ( #9326, #30916, #20333, #37849, #2115, #30679, #16745, #12703, #31386 ),
 .UNSPECIFIED., .F., .F. ) 
 B_SPLINE_CURVE_WITH_KNOTS ( ( 3, 2, 2, 2, 3 ),
 ( 0.5799999999999999600, 0.5825000000000000178, 0.5849999999999999645, 0.5875000000000000222, 0.5899999999999999689 ),
 .UNSPECIFIED. ) 
 CURVE ( )  GEOMETRIC_REPRESENTATION_ITEM ( )  RATIONAL_B_SPLINE_CURVE ( ( 1.000000000000000000, 0.9238795325112869605, 1.000000000000000000, 0.9238795325112869605, 1.000000000000000000, 0.9238795325112869605, 1.000000000000000000, 0.9238795325112869605, 1.000000000000000000 ) ) 
 REPRESENTATION_ITEM ( '' )  ) ;
#32755=CARTESIAN_POINT ( 'NONE',  ( 0.8019270111902717657, 0.1787899950787401604, 0.6299212597887560161 ) ) ;
#32758=CARTESIAN_POINT ( 'NONE',  ( -0.8019270111902717657, -0.1787899950787401604, 1.117125984198206412 ) ) ;
#32759=ORIENTED_EDGE ( 'NONE', *, *, #16203, .T. ) ;
#32760=EDGE_CURVE ( 'NONE', #20293, #14046, #7081, .T. ) ;
#32761=CARTESIAN_POINT ( 'NONE',  ( -0.8759842519685039353, -0.1787899950787401882, 1.075295275536787276 ) ) ;
#32762=CARTESIAN_POINT ( 'NONE',  ( -1.054774247047244096, 0.000000000000000000, 0.8538385826234016207 ) ) ;
#32763=CARTESIAN_POINT ( 'NONE',  ( -1.054774247047244540, 0.07405724077823318263, 0.1870078739619845387 ) ) ;
#32764=CARTESIAN_POINT ( 'NONE',  ( -0.8107537697050254399, -0.1574803149606297803, 0.3518700787401575769 ) ) ;
#32765=CARTESIAN_POINT ( 'NONE',  ( 0.7185039370078766252, -0.06523048226348168721, 1.636318897530268490 ) ) ;
#32769=CARTESIAN_POINT ( 'NONE',  ( -0.8759842519685039353, -0.1574803149606299191, 0.8562992124908976876 ) ) ;
#32772=ORIENTED_EDGE ( 'NONE', *, *, #27742, .F. ) ;
#32774=CARTESIAN_POINT ( 'NONE',  ( -0.9500414927467378812, 0.1787899950787401604, 0.7775590550643479704 ) ) ;
#32775=AXIS2_PLACEMENT_3D ( 'NONE', #42470, #8955, #37958 ) ;
#32776=CARTESIAN_POINT ( 'NONE',  ( -0.8019270111902716547, -0.1787899950787401604, 1.747047244040724312 ) ) ;
#32780=CARTESIAN_POINT ( 'NONE',  ( 0.8107537697050253289, -0.1574803149606297803, 0.7062007874015745479 ) ) ;
#32783=CARTESIAN_POINT ( 'NONE',  ( -0.7185039370078746268, 0.06523048226347956391, 1.355807086506646275 ) ) ;
#32784=CARTESIAN_POINT ( 'NONE',  ( 0.8759842519685039353, 0.1787899950787401882, 0.8243110235682834519 ) ) ;
#32788=CARTESIAN_POINT ( 'NONE',  ( 0.7185039370078739607, 1.928577636452523993E-17, 1.446850393700787274 ) ) ;
#32789=CARTESIAN_POINT ( 'NONE',  ( 0.9408631620327171374, -0.1642324321402740817, 1.989367024862866540 ) ) ;
#32790=CARTESIAN_POINT ( 'NONE',  ( 0.9412147342319837628, -0.1574803149606297803, 1.567421259734991690 ) ) ;
#32791=CARTESIAN_POINT ( 'NONE',  ( 0.7185039370078739607, 1.928577636452523993E-17, 1.712598425089322918 ) ) ;
#32792=CARTESIAN_POINT ( 'NONE',  ( 0.6971942568897648851, 0.07405724077823318263, 0.6692913385289143147 ) ) ;
#32793=CARTESIAN_POINT ( 'NONE',  ( 0.9412147342319837628, -0.1574803149606297803, 0.2682086613097960370 ) ) ;
#32796=ORIENTED_EDGE ( 'NONE', *, *, #36582, .F. ) ;
#32797=DIRECTION ( 'NONE',  ( 1.000000000000000000, 0.000000000000000000, -4.336808689942015271E-16 ) ) ;
#32799=CARTESIAN_POINT ( 'NONE',  ( 1.002407869896990045, -0.1264236179284866091, 0.9621062991588346103 ) ) ;
#32800=CARTESIAN_POINT ( 'NONE',  ( 1.033464566929133799, 0.000000000000000000, 1.496062992018456494 ) ) ;
#32804=CARTESIAN_POINT ( 'NONE',  ( -0.8759842519685039353, 0.1787899950787401882, 0.1107283464029295283 ) ) ;
#32805=CARTESIAN_POINT ( 'NONE',  ( -0.9412147342319837628, 0.1574803149606300301, 0.6077755905511815770 ) ) ;
#32809=CARTESIAN_POINT ( 'NONE',  ( -0.6971942568897637749, 2.189545951927499583E-17, 1.897145669237574772 ) ) ;
#32810=CARTESIAN_POINT ( 'NONE',  ( -0.8019270111902717657, -0.1787899950787401604, 1.742125984198204858 ) ) ;
#32811=ADVANCED_FACE ( 'NONE', ( #47381 ), #14553, .T. ) ;
#32812=CONICAL_SURFACE ( 'NONE', #10604, 0.1574803149606299191, 1.047197551196598297 ) ;
#32813=CARTESIAN_POINT ( 'NONE',  ( -0.7495606340400177148, -0.1264236179284866091, 0.4060039369541102450 ) ) ;
#32816=CARTESIAN_POINT ( 'NONE',  ( 0.9873396505805591694, 0.1113553986120547346, 0.3986220471365669038 ) ) ;
#32817=CARTESIAN_POINT ( 'NONE',  ( 1.054774247047244540, 0.07405724077823318263, 0.02460629915883492599 ) ) ;
#32825=CARTESIAN_POINT ( 'NONE',  ( -1.054774247047244540, -0.07405724077823318263, 0.3346456692375748831 ) ) ;
#32828=CARTESIAN_POINT ( 'NONE',  ( -0.6971942568897648851, -0.07405724077823297447, 1.348425196796630976 ) ) ;
#32833=CARTESIAN_POINT ( 'NONE',  ( -0.7185039370078739607, 0.000000000000000000, -2.869337061179095023E-17 ) ) ;
#32835=CARTESIAN_POINT ( 'NONE',  ( 0.9873396505805591694, 0.1113553986120547346, 0.4084645669291339098 ) ) ;
#32838=CARTESIAN_POINT ( 'NONE',  ( -0.7185039370078746268, -0.06523048226347956391, 0.9670275589475911815 ) ) ;
#32839=VECTOR ( 'NONE', #45949, 39.37007874015748143 ) ;
#32842=CARTESIAN_POINT ( 'NONE',  ( 0.9873396505805591694, -0.1113553986120547346, 1.806102362097196767 ) ) ;
#32845=CARTESIAN_POINT ( 'NONE',  ( 0.9873396505805591694, -0.1113553986120547346, 0.8316929133858268486 ) ) ;
#32849=CARTESIAN_POINT ( 'NONE',  ( -0.8107537697050254399, -0.1574803149606297803, 0.8243110236220465570 ) ) ;
#32850=CARTESIAN_POINT ( 'NONE',  ( 0.7185039370078739607, 1.928577636452523993E-17, 0.7677165353255432922 ) ) ;
#32852=ORIENTED_EDGE ( 'NONE', *, *, #43981, .T. ) ;
#32857=CARTESIAN_POINT ( 'NONE',  ( -0.8107537697050253289, 0.1574803149606300301, 0.1697834644594022058 ) ) ;
#32859=CARTESIAN_POINT ( 'NONE',  ( 0.9873396505805591694, 0.1113553986120547346, 0.9498031494987716483 ) ) ;
#32860=( BOUNDED_CURVE ( )  B_SPLINE_CURVE ( 2, ( #3514, #28461, #24606, #32045, #18125, #13579, #43032, #43282, #39670 ),
 .UNSPECIFIED., .F., .T. ) 
 B_SPLINE_CURVE_WITH_KNOTS ( ( 3, 2, 2, 2, 3 ),
 ( 0.8699999999999999956, 0.8725000000000000533, 0.8750000000000000000, 0.8774999999999999467, 0.8800000000000000044 ),
 .UNSPECIFIED. ) 
 CURVE ( )  GEOMETRIC_REPRESENTATION_ITEM ( )  RATIONAL_B_SPLINE_CURVE ( ( 1.000000000000000000, 0.9238795325112869605, 1.000000000000000000, 0.9238795325112869605, 1.000000000000000000, 0.9238795325112869605, 1.000000000000000000, 0.9238795325112869605, 1.000000000000000000 ) ) 
 REPRESENTATION_ITEM ( '' )  ) ;
#32863=CARTESIAN_POINT ( 'NONE',  ( -0.7495606340400177148, -0.1264236179284866091, 1.665846456639149764 ) ) ;
#32865=CARTESIAN_POINT ( 'NONE',  ( 0.7495606340400177148, -0.1264236179284866091, 1.547736220418677089 ) ) ;
#32867=CARTESIAN_POINT ( 'NONE',  ( -1.054774247047244540, -0.07405724077823318263, 0.8513779527021426707 ) ) ;
#32868=CARTESIAN_POINT ( 'NONE',  ( 0.8019270111902717657, 0.1787899950787401604, 0.2755905511273391006 ) ) ;
#32869=CARTESIAN_POINT ( 'NONE',  ( 0.9500414927467377701, 0.1787899950787401604, 0.7037401574265510495 ) ) ;
#32870=CARTESIAN_POINT ( 'NONE',  ( -0.8759842519685039353, -0.1787899950787401882, 0.7209645668753701386 ) ) ;
#32872=EDGE_CURVE ( 'NONE', #41698, #13201, #22854, .T. ) ;
#32873=CARTESIAN_POINT ( 'NONE',  ( -1.033464566929133799, 0.000000000000000000, 0.8759842519685039353 ) ) ;
#32874=CARTESIAN_POINT ( 'NONE',  ( -0.6971942568897648851, -0.07405724077823297447, 1.545275590497416696 ) ) ;
#32875=CARTESIAN_POINT ( 'NONE',  ( -0.7185039370078746268, -0.06523048226347956391, 1.833169291231055542 ) ) ;
#32878=LINE ( 'NONE', #14644, #46563 ) ;
#32879=CARTESIAN_POINT ( 'NONE',  ( 0.6971942568897648851, -0.07405724077823297447, 1.505905511757261062 ) ) ;
#32887=ORIENTED_EDGE ( 'NONE', *, *, #15044, .T. ) ;
#32892=CARTESIAN_POINT ( 'NONE',  ( 0.7495606340400177148, 0.1264236179284866091, 1.769192913332062966 ) ) ;
#32893=CARTESIAN_POINT ( 'NONE',  ( 0.8759842519685039353, -0.1787899950787401882, 0.3666338582139531677 ) ) ;
#32899=CARTESIAN_POINT ( 'NONE',  ( 1.054774247047244096, 0.000000000000000000, 0.6520669290800944484 ) ) ;
#32901=CARTESIAN_POINT ( 'NONE',  ( -0.9225890239890590649, 0.1652722632748837295, 0.03937007874015842346 ) ) ;
#32902=CARTESIAN_POINT ( 'NONE',  ( 0.8759842519685039353, 0.000000000000000000, 4.498031496062992574 ) ) ;
#32904=CARTESIAN_POINT ( 'NONE',  ( -0.8561525976674764227, -0.1729235199935184042, 1.987843333062883522 ) ) ;
#32906=CARTESIAN_POINT ( 'NONE',  ( 0.7185039370078741827, 0.06523048226347841205, 0.9621062991050717272 ) ) ;
#32907=CARTESIAN_POINT ( 'NONE',  ( 0.7495606340400177148, -0.1264236179284866091, 1.744586614119464807 ) ) ;
#32909=CARTESIAN_POINT ( 'NONE',  ( 0.7185039370078746268, 0.06523048226347956391, 0.1353346455617644717 ) ) ;
#32910=CARTESIAN_POINT ( 'NONE',  ( 0.9500414927467377701, 0.1787899950787401604, 0.5019685038832443214 ) ) ;
#32912=CARTESIAN_POINT ( 'NONE',  ( -0.9500414927467378812, 0.1787899950787401604, 0.4675196849856070869 ) ) ;
#32913=CARTESIAN_POINT ( 'NONE',  ( -0.8107537697050254399, 0.1574803149606300301, 0.1796259842519686567 ) ) ;
#32916=CARTESIAN_POINT ( 'NONE',  ( 1.002407869896990045, 0.1264236179284866091, 0.1107283464029293202 ) ) ;
#32918=CARTESIAN_POINT ( 'NONE',  ( -0.8019270111902717657, -0.1787899950787401604, 1.663385826717890925 ) ) ;
#32920=CARTESIAN_POINT ( 'NONE',  ( -0.7495606340400177148, -0.1264236179284866091, 1.154035433017102319 ) ) ;
#32921=CARTESIAN_POINT ( 'NONE',  ( -0.7646288533564489232, 0.1113553986120547346, 0.3395669291338583307 ) ) ;
#32923=CARTESIAN_POINT ( 'NONE',  ( 1.054774247047244540, -0.07405724077823318263, 1.166338582623402509 ) ) ;
#32925=CARTESIAN_POINT ( 'NONE',  ( 0.6971942568897648851, 0.07405724077823318263, 1.889763779473794258 ) ) ;
#32926=CARTESIAN_POINT ( 'NONE',  ( -1.002407869896990045, -0.1264236179284866091, 1.119586614119464585 ) ) ;
#32929=CARTESIAN_POINT ( 'NONE',  ( 0.8759842519685039353, -0.1787899950787401882, 0.2928149605761578567 ) ) ;
#32930=CARTESIAN_POINT ( 'NONE',  ( -0.8019270111902716547, 0.1787899950787401604, 0.1919291338045042705 ) ) ;
#32931=CARTESIAN_POINT ( 'NONE',  ( -0.9500414927467378812, 0.1787899950787401604, 0.7381889763241898939 ) ) ;
#32932=ORIENTED_EDGE ( 'NONE', *, *, #42126, .T. ) ;
#32933=EDGE_CURVE ( 'NONE', #27914, #11128, #34362, .T. ) ;
#32935=CARTESIAN_POINT ( 'NONE',  ( 0.8759842519685039353, 0.1787899950787401882, 0.7849409448281259305 ) ) ;
#32936=CARTESIAN_POINT ( 'NONE',  ( 0.6971942568897648851, -0.07405724077823297447, 1.112204724355684959 ) ) ;
#32937=CARTESIAN_POINT ( 'NONE',  ( -0.6971942568897648851, -0.07405724077823297447, 1.934055118056471567 ) ) ;
#32938=VERTEX_POINT ( 'NONE', #12329 ) ;
#32940=CARTESIAN_POINT ( 'NONE',  ( 1.002407869896990045, 0.1264236179284866091, 1.877460629867496067 ) ) ;
#32941=VECTOR ( 'NONE', #38736, 39.37007874015748143 ) ;
#32946=CARTESIAN_POINT ( 'NONE',  ( -0.9412147342319837628, 0.1574803149606300301, 1.700295275483023172 ) ) ;
#32948=CARTESIAN_POINT ( 'NONE',  ( 1.054774247047244540, 0.07405724077823318263, 1.205708661363558365 ) ) ;
#32949=CARTESIAN_POINT ( 'NONE',  ( -0.8759842519685039353, 0.1574803149606299191, 0.8366141731208189825 ) ) ;
#32951=CARTESIAN_POINT ( 'NONE',  ( -0.7185039370078739607, 0.000000000000000000, -2.869337061179095023E-17 ) ) ;
#32952=CARTESIAN_POINT ( 'NONE',  ( 0.7185039370078746268, 0.06523048226347956391, 1.956200787401575880 ) ) ;
#32954=CARTESIAN_POINT ( 'NONE',  ( -0.8759842519685039353, -0.1787899950787401882, 0.4502952755367874427 ) ) ;
#32955=CARTESIAN_POINT ( 'NONE',  ( -1.033464566929133799, 0.000000000000000000, 0.6692913384751496553 ) ) ;
#32957=CARTESIAN_POINT ( 'NONE',  ( -0.7123214566016451421, -0.03363891151877827779, 1.983890876906730716 ) ) ;
#32959=CARTESIAN_POINT ( 'NONE',  ( 0.8759842519685039353, -0.1787899950787401882, 1.198326771599779628 ) ) ;
#32960=CARTESIAN_POINT ( 'NONE',  ( 1.054774247047244540, -0.07405724077823318263, 1.751968503883245987 ) ) ;
#32963=CYLINDRICAL_SURFACE ( 'NONE', #8305, 0.1574803149606299191 ) ;
#32967=CARTESIAN_POINT ( 'NONE',  ( 0.6971942568897626646, -0.07405724077823297447, 0.2017716534895435399 ) ) ;
#32968=CARTESIAN_POINT ( 'NONE',  ( 1.002407869896990045, -0.1264236179284866091, 1.237696850339937038 ) ) ;
#32972=CARTESIAN_POINT ( 'NONE',  ( -1.054774247047244540, 0.07405724077823318263, 1.245078740103716886 ) ) ;
#32973=CARTESIAN_POINT ( 'NONE',  ( 0.8107537697050253289, 0.1574803149606300301, 0.7209645668216065895 ) ) ;
#32975=CARTESIAN_POINT ( 'NONE',  ( 0.9651916757672701630, 0.1428679945500031245, 0.03937007847211974887 ) ) ;
#32976=CARTESIAN_POINT ( 'NONE',  ( 0.7185039370078739607, 1.928577636452523993E-17, 0.2657480314960630197 ) ) ;
#32980=CARTESIAN_POINT ( 'NONE',  ( -0.9873396505805591694, -0.1113553986120547346, 0.04429133858267716300 ) ) ;
#32981=CARTESIAN_POINT ( 'NONE',  ( 1.054774247047244096, 0.000000000000000000, 1.439468503883244210 ) ) ;
#32982=CARTESIAN_POINT ( 'NONE',  ( -0.9873396505805591694, 0.1113553986120547346, 1.156496062992125928 ) ) ;
#32983=DIRECTION ( 'NONE',  ( 1.000000000000000000, 0.000000000000000000, -1.822029033848725275E-16 ) ) ;
#32984=CARTESIAN_POINT ( 'NONE',  ( -0.8759842519685039353, -0.1574803149606299191, 0.1181102362204724532 ) ) ;
#32988=CYLINDRICAL_SURFACE ( 'NONE', #3100, 0.1574803149606299191 ) ;
#32992=CARTESIAN_POINT ( 'NONE',  ( 0.6971942568897626646, 0.07405724077823318263, 0.5167322834108034613 ) ) ;
#32995=CARTESIAN_POINT ( 'NONE',  ( -0.6971942568897637749, 2.189545951927499583E-17, 1.109744094434425232 ) ) ;
#32998=CARTESIAN_POINT ( 'NONE',  ( -1.054774247047244096, 0.000000000000000000, 0.8144685038832440993 ) ) ;
#32999=ADVANCED_FACE ( 'NONE', ( #8229 ), #37471, .T. ) ;
#33000=CARTESIAN_POINT ( 'NONE',  ( -0.8759842519685039353, 0.1787899950787401882, 0.2731299212060791515 ) ) ;
#33001=CARTESIAN_POINT ( 'NONE',  ( 0.7185039370078746268, -0.06523048226347956391, 0.6619094488188971281 ) ) ;
#33005=CARTESIAN_POINT ( 'NONE',  ( 0.7185039370078746268, -0.06523048226347956391, 1.055610236220473341 ) ) ;
#33008=CARTESIAN_POINT ( 'NONE',  ( -0.6971942568897626646, -0.07405724077823297447, 0.7923228345919055560 ) ) ;
#33011=CARTESIAN_POINT ( 'NONE',  ( -0.8019270111902716547, -0.1787899950787401604, 1.786417322780882388 ) ) ;
#33012=TOROIDAL_SURFACE ( 'NONE', #18435, 0.3444881889763780070, 0.1574803149606299191 ) ;
#33014=CARTESIAN_POINT ( 'NONE',  ( 1.033464566929133799, 0.000000000000000000, 0.2755905510735752184 ) ) ;
#33015=CARTESIAN_POINT ( 'NONE',  ( 1.033464566929134687, 0.06523048226347956391, 0.6422244094488182009 ) ) ;
#33018=CARTESIAN_POINT ( 'NONE',  ( -0.9873396505805591694, -0.1113553986120547346, 1.530511810916094451 ) ) ;
#33019=CARTESIAN_POINT ( 'NONE',  ( 1.054774247047244540, -0.07405724077823318263, 0.6938976377415123631 ) ) ;
#33020=LINE ( 'NONE', #36833, #40648 ) ;
#33021=CARTESIAN_POINT ( 'NONE',  ( 1.033464566929133799, 0.000000000000000000, 1.387795275590551158 ) ) ;
#33022=CARTESIAN_POINT ( 'NONE',  ( 0.8845810845758348417, -0.1747031431852734129, 1.988336823050417035 ) ) ;
#33023=CARTESIAN_POINT ( 'NONE',  ( 0.7646288533564489232, -0.1113553986120547346, 1.560039369971212508 ) ) ;
#33024=CARTESIAN_POINT ( 'NONE',  ( 0.8107537697050254399, 0.1574803149606300301, 0.3272637794200322636 ) ) ;
#33026=( BOUNDED_CURVE ( )  B_SPLINE_CURVE ( 2, ( #19097, #22458, #44723, #40188, #40421, #37081, #7605, #22219, #18858 ),
 .UNSPECIFIED., .F., .F. ) 
 B_SPLINE_CURVE_WITH_KNOTS ( ( 3, 2, 2, 2, 3 ),
 ( 0.1499999999999999944, 0.1524999999999999967, 0.1549999999999999989, 0.1575000000000000011, 0.1600000000000000033 ),
 .UNSPECIFIED. ) 
 CURVE ( )  GEOMETRIC_REPRESENTATION_ITEM ( )  RATIONAL_B_SPLINE_CURVE ( ( 1.000000000000000000, 0.9238795325112869605, 1.000000000000000000, 0.9238795325112869605, 1.000000000000000000, 0.9238795325112869605, 1.000000000000000000, 0.9238795325112869605, 1.000000000000000000 ) ) 
 REPRESENTATION_ITEM ( '' )  ) ;
#33027=CARTESIAN_POINT ( 'NONE',  ( 0.6971942568897648851, 0.07405724077823318263, 0.8267716534895444003 ) ) ;
#33028=CARTESIAN_POINT ( 'NONE',  ( -0.9500414927467378812, -0.1787899950787401604, 1.983267716481667886 ) ) ;
#33033=CARTESIAN_POINT ( 'NONE',  ( -0.9412147342319837628, 0.1574803149606300301, 1.158956692913385655 ) ) ;
#33035=CARTESIAN_POINT ( 'NONE',  ( 0.8759842519685039353, 0.1787899950787401882, 0.9374999999462362288 ) ) ;
#33039=AXIS2_PLACEMENT_3D ( 'NONE', #3418, #29357, #43899 ) ;
#33042=CARTESIAN_POINT ( 'NONE',  ( -1.002407869896990045, 0.1264236179284866091, 0.1058070865604098382 ) ) ;
#33043=CARTESIAN_POINT ( 'NONE',  ( -0.9412147342319837628, -0.1574803149606297803, 0.7111220472440957785 ) ) ;
#33048=CARTESIAN_POINT ( 'NONE',  ( -1.054774247047244540, 0.07405724077823318263, 1.717519684985606476 ) ) ;
#33049=ORIENTED_EDGE ( 'NONE', *, *, #36965, .F. ) ;
#33051=CARTESIAN_POINT ( 'NONE',  ( -0.9500414927467378812, -0.1787899950787401604, 0.4133858267178901480 ) ) ;
#33056=CARTESIAN_POINT ( 'NONE',  ( 0.7495606340400177148, 0.1264236179284866091, 0.03690944876513417572 ) ) ;
#33060=DIRECTION ( 'NONE',  ( 1.000000000000000000, 0.000000000000000000, -1.822029033848725275E-16 ) ) ;
#33061=CARTESIAN_POINT ( 'NONE',  ( -1.054774247047244540, -0.07405724077823318263, 0.3740157479777325711 ) ) ;
#33062=ORIENTED_EDGE ( 'NONE', *, *, #20241, .F. ) ;
#33064=CARTESIAN_POINT ( 'NONE',  ( -0.9500414927467377701, -0.1787899950787401604, 1.358267716481669662 ) ) ;
#33065=ORIENTED_EDGE ( 'NONE', *, *, #8665, .F. ) ;
#33068=FACE_OUTER_BOUND ( 'NONE', #40901, .T. ) ;
#33071=CARTESIAN_POINT ( 'NONE',  ( -0.7185039370078746268, 0.06523048226347956391, 1.119586614065702035 ) ) ;
#33072=CARTESIAN_POINT ( 'NONE',  ( 0.8019270111902717657, 0.1787899950787401604, 0.4330708660879683536 ) ) ;
#33076=VERTEX_POINT ( 'NONE', #41500 ) ;
#33078=ORIENTED_EDGE ( 'NONE', *, *, #12457, .T. ) ;
#33080=CARTESIAN_POINT ( 'NONE',  ( -0.7185039370078739607, 1.928577636452523993E-17, 1.437007873908220601 ) ) ;
#33081=CARTESIAN_POINT ( 'NONE',  ( 0.8107537697050253289, -0.1574803149606297803, 0.9424212598425207865 ) ) ;
#33086=CARTESIAN_POINT ( 'NONE',  ( 1.033464566929133799, 0.000000000000000000, 0.7972440944881890035 ) ) ;
#33087=EDGE_CURVE ( 'NONE', #3668, #29530, #9178, .T. ) ;
#33091=CARTESIAN_POINT ( 'NONE',  ( 0.8107537697050254399, 0.1574803149606300301, 1.154035432963338659 ) ) ;
#33096=CARTESIAN_POINT ( 'NONE',  ( 0.8759842519685039353, -0.1574803149606299191, 0.9350393699712126194 ) ) ;
#33097=CARTESIAN_POINT ( 'NONE',  ( 0.8107537697050254399, 0.1574803149606300301, 0.5339566929133854334 ) ) ;
#33101=CARTESIAN_POINT ( 'NONE',  ( -0.9500414927467378812, 0.1787899950787401604, 1.609251968450173376 ) ) ;
#33103=CARTESIAN_POINT ( 'NONE',  ( 0.7495606340400177148, -0.1264236179284866091, 1.626476377898992132 ) ) ;
#33105=CARTESIAN_POINT ( 'NONE',  ( -0.6971942568897626646, 0.07405724077823318263, 0.8710629920722218200 ) ) ;
#33107=CARTESIAN_POINT ( 'NONE',  ( 1.054774247047244540, -0.07405724077823318263, 0.3395669290800945039 ) ) ;
#33108=CARTESIAN_POINT ( 'NONE',  ( -0.9412147342319837628, 0.1574803149606300301, 0.2534448818897638289 ) ) ;
#33109=CARTESIAN_POINT ( 'NONE',  ( -0.8759842519685039353, 0.1787899950787401882, 1.213090551127338435 ) ) ;
#33110=CARTESIAN_POINT ( 'NONE',  ( -0.6971942568897648851, -0.07405724077823297447, 0.6348425196312760255 ) ) ;
#33112=VECTOR ( 'NONE', #24868, 39.37007874015748143 ) ;
#33113=CYLINDRICAL_SURFACE ( 'NONE', #14558, 0.1574803149606299191 ) ;
#33114=CARTESIAN_POINT ( 'NONE',  ( -1.054774247047244540, -0.07405724077823318263, 1.560039370024977057 ) ) ;
#33115=CARTESIAN_POINT ( 'NONE',  ( -0.9873396505805591694, 0.1113553986120547346, 1.934055118002708573 ) ) ;
#33116=EDGE_LOOP ( 'NONE', ( #9515, #22422, #41430, #17046 ) ) ;
#33118=CARTESIAN_POINT ( 'NONE',  ( -0.9873396505805591694, -0.1113553986120547346, 1.658464566929134021 ) ) ;
#33119=CARTESIAN_POINT ( 'NONE',  ( 0.8107537697050254399, 0.1574803149606300301, 1.636318897637794922 ) ) ;
#33120=CARTESIAN_POINT ( 'NONE',  ( 0.6971942568897648851, -0.07405724077823297447, 1.466535433017102763 ) ) ;
#33124=VERTEX_POINT ( 'NONE', #28355 ) ;
#33126=ORIENTED_EDGE ( 'NONE', *, *, #8219, .F. ) ;
#33127=ORIENTED_EDGE ( 'NONE', *, *, #33675, .F. ) ;
#33128=FACE_OUTER_BOUND ( 'NONE', #27574, .T. ) ;
#33131=CARTESIAN_POINT ( 'NONE',  ( 0.8019270111902717657, 0.1787899950787401604, 1.806102362150961316 ) ) ;
#33136=EDGE_CURVE ( 'NONE', #23920, #11484, #75, .T. ) ;
#33137=CARTESIAN_POINT ( 'NONE',  ( 0.7495606340400177148, -0.1264236179284866091, 0.7160433070328504623 ) ) ;
#33138=( BOUNDED_CURVE ( )  B_SPLINE_CURVE ( 2, ( #14425, #18004, #47243, #11077, #25696, #2669, #29077, #43635, #10844 ),
 .UNSPECIFIED., .F., .T. ) 
 B_SPLINE_CURVE_WITH_KNOTS ( ( 3, 2, 2, 2, 3 ),
 ( 0.5200000000000000178, 0.5224999999999999645, 0.5250000000000000222, 0.5274999999999999689, 0.5300000000000000266 ),
 .UNSPECIFIED. ) 
 CURVE ( )  GEOMETRIC_REPRESENTATION_ITEM ( )  RATIONAL_B_SPLINE_CURVE ( ( 1.000000000000000000, 0.9238795325112869605, 1.000000000000000000, 0.9238795325112869605, 1.000000000000000000, 0.9238795325112869605, 1.000000000000000000, 0.9238795325112869605, 1.000000000000000000 ) ) 
 REPRESENTATION_ITEM ( '' )  ) ;
#33141=DIRECTION ( 'NONE',  ( -1.000000000000000000, 0.000000000000000000, 0.000000000000000000 ) ) ;
#33144=CARTESIAN_POINT ( 'NONE',  ( 0.8759842519685039353, 0.000000000000000000, 4.498031496062992574 ) ) ;
#33145=CARTESIAN_POINT ( 'NONE',  ( 0.6971942568897648851, -0.07405724077823297447, 1.781496062938362934 ) ) ;
#33147=FACE_OUTER_BOUND ( 'NONE', #46284, .T. ) ;
#33148=CARTESIAN_POINT ( 'NONE',  ( 0.6971942568897648851, 0.07405724077823318263, 0.5118110235682844511 ) ) ;
#33149=EDGE_CURVE ( 'NONE', #19564, #30530, #12274, .T. ) ;
#33150=AXIS2_PLACEMENT_3D ( 'NONE', #4109, #29101, #25486 ) ;
#33152=EDGE_CURVE ( 'NONE', #35903, #6796, #17159, .T. ) ;
#33153=CARTESIAN_POINT ( 'NONE',  ( 0.7185039370078746268, -0.06523048226347956391, 0.07135826771653554224 ) ) ;
#33156=CARTESIAN_POINT ( 'NONE',  ( -0.8019270111902717657, -0.1787899950787401604, 0.4084645668753704717 ) ) ;
#33159=CARTESIAN_POINT ( 'NONE',  ( 0.8759842519685039353, 0.1787899950787401882, 0.2337598424659216578 ) ) ;
#33161=CARTESIAN_POINT ( 'NONE',  ( -0.9500414927467378812, -0.1787899950787401604, 1.550196850339937926 ) ) ;
#33164=CARTESIAN_POINT ( 'NONE',  ( -0.7495606340400177148, 0.1264236179284866091, 1.144192913332062966 ) ) ;
#33166=CARTESIAN_POINT ( 'NONE',  ( 0.7495606340400177148, -0.1264236179284866091, 1.936515747977732405 ) ) ;
#33167=CARTESIAN_POINT ( 'NONE',  ( -0.8107537697050253289, -0.1574803149606297803, 0.6274606299212601712 ) ) ;
#33168=CARTESIAN_POINT ( 'NONE',  ( -1.054774247047244540, -0.07405724077823318263, 1.122047244040725644 ) ) ;
#33171=CARTESIAN_POINT ( 'NONE',  ( 0.8019270111902716547, -0.1787899950787401604, 0.3690944881352128393 ) ) ;
#33172=CARTESIAN_POINT ( 'NONE',  ( -0.8759842519685039353, -0.1787899950787401882, 0.1697834645131655606 ) ) ;
#33173=CARTESIAN_POINT ( 'NONE',  ( -1.054774247047244540, 0.07405724077823318263, 0.8120078739619844832 ) ) ;
#33174=ORIENTED_EDGE ( 'NONE', *, *, #4210, .F. ) ;
#33175=( BOUNDED_CURVE ( )  B_SPLINE_CURVE ( 2, ( #41658, #1662, #20355, #34992, #27111, #9583, #41895, #13414, #9347 ),
 .UNSPECIFIED., .F., .T. ) 
 B_SPLINE_CURVE_WITH_KNOTS ( ( 3, 2, 2, 2, 3 ),
 ( 0.7900000000000000355, 0.7924999999999999822, 0.7950000000000000400, 0.7974999999999999867, 0.8000000000000000444 ),
 .UNSPECIFIED. ) 
 CURVE ( )  GEOMETRIC_REPRESENTATION_ITEM ( )  RATIONAL_B_SPLINE_CURVE ( ( 1.000000000000000000, 0.9238795325112869605, 1.000000000000000000, 0.9238795325112869605, 1.000000000000000000, 0.9238795325112869605, 1.000000000000000000, 0.9238795325112869605, 1.000000000000000000 ) ) 
 REPRESENTATION_ITEM ( '' )  ) ;
#33178=CARTESIAN_POINT ( 'NONE',  ( 0.8759842519685039353, -0.1787899950787401882, 0.8833661416785196785 ) ) ;
#33179=CARTESIAN_POINT ( 'NONE',  ( 1.002407869896990045, 0.1264236179284866091, 1.055610236166708793 ) ) ;
#33180=CARTESIAN_POINT ( 'NONE',  ( -1.054774247047244540, -0.07405724077823318263, 1.791338582623401177 ) ) ;
#33187=ORIENTED_EDGE ( 'NONE', *, *, #16149, .F. ) ;
#33188=CARTESIAN_POINT ( 'NONE',  ( 0.9500414927467378812, 0.1787899950787401604, 1.249999999946235896 ) ) ;
#33192=ADVANCED_FACE ( 'NONE', ( #4099 ), #47011, .T. ) ;
#33195=CARTESIAN_POINT ( 'NONE',  ( 0.7495606340400177148, -0.1264236179284866091, 0.1254921259304885850 ) ) ;
#33198=PRODUCT_CONTEXT ( 'NONE', #1229, 'mechanical' ) ;
#33200=CARTESIAN_POINT ( 'NONE',  ( -1.002407869896990045, 0.1264236179284866091, 0.5044291338045039375 ) ) ;
#33203=CARTESIAN_POINT ( 'NONE',  ( 1.054774247047244096, 0.000000000000000000, 1.995570866087968520 ) ) ;
#33204=CARTESIAN_POINT ( 'NONE',  ( 1.054774247047244096, 0.000000000000000000, 1.365649606245448844 ) ) ;
#33205=CARTESIAN_POINT ( 'NONE',  ( 0.6971942568897637749, 2.189545951927499583E-17, 1.695374015694267822 ) ) ;
#33206=CARTESIAN_POINT ( 'NONE',  ( 0.9873396505805591694, 0.1113553986120547346, 1.500984251860976171 ) ) ;
#33208=CARTESIAN_POINT ( 'NONE',  ( -1.033464566929133799, 0.000000000000000000, 0.2066929133858267931 ) ) ;
#33212=CARTESIAN_POINT ( 'NONE',  ( 1.054774247047244540, 0.07405724077823318263, 0.3001968503399373711 ) ) ;
#33213=CARTESIAN_POINT ( 'NONE',  ( 0.7111015311219361923, -0.04729053972105573544, 0.03937016857757889149 ) ) ;
#33214=CARTESIAN_POINT ( 'NONE',  ( 1.054774247047244540, 0.07405724077823318263, 1.284448818843874518 ) ) ;
#33215=CARTESIAN_POINT ( 'NONE',  ( -0.7185039370078739607, 1.928577636452523993E-17, 1.712598425089322918 ) ) ;
#33218=CARTESIAN_POINT ( 'NONE',  ( -0.6971942568897648851, -0.07405724077823297447, 1.264763779473795813 ) ) ;
#33219=CARTESIAN_POINT ( 'NONE',  ( 0.7185039370078746268, -0.06523048226347956391, 0.6126968502861739330 ) ) ;
#33222=CARTESIAN_POINT ( 'NONE',  ( 0.8823777864880867350, 0.1740654330852410558, 0.03936977449015421904 ) ) ;
#33225=CARTESIAN_POINT ( 'NONE',  ( -0.9412147342319837628, 0.1574803149606300301, 1.592027559055119612 ) ) ;
#33226=CARTESIAN_POINT ( 'NONE',  ( 1.002407869896990045, 0.1264236179284866091, 1.641240157426551161 ) ) ;
#33228=CARTESIAN_POINT ( 'NONE',  ( 0.8107537697050254399, 0.1574803149606300301, 1.675688976377952999 ) ) ;
#33230=VERTEX_POINT ( 'NONE', #11089 ) ;
#33231=DIRECTION ( 'NONE',  ( 1.822029033848725028E-16, 0.000000000000000000, 1.000000000000000000 ) ) ;
#33234=CARTESIAN_POINT ( 'NONE',  ( 0.6971942568897626646, 0.07405724077823318263, 0.6348425196312760255 ) ) ;
#33235=ORIENTED_EDGE ( 'NONE', *, *, #7906, .T. ) ;
#33236=CARTESIAN_POINT ( 'NONE',  ( 1.054774247047244540, 0.07405724077823318263, 0.8169291338045038264 ) ) ;
#33238=CARTESIAN_POINT ( 'NONE',  ( -0.7495606340400177148, -0.1264236179284866091, 1.232775590497417362 ) ) ;
#33240=CARTESIAN_POINT ( 'NONE',  ( 1.033464566929133799, 0.000000000000000000, 1.299212598317669221 ) ) ;
#33241=CARTESIAN_POINT ( 'NONE',  ( -1.002407869896990045, 0.1264236179284866091, 0.1500984251430867999 ) ) ;
#33242=CARTESIAN_POINT ( 'NONE',  ( 0.8759842519685039353, -0.1574803149606299191, 0.6692913385826771977 ) ) ;
#33247=ORIENTED_EDGE ( 'NONE', *, *, #2899, .F. ) ;
#33248=CARTESIAN_POINT ( 'NONE',  ( 1.033464566929133799, 0.000000000000000000, 1.220472440837354400 ) ) ;
#33249=CARTESIAN_POINT ( 'NONE',  ( -0.7495606340400177148, -0.1264236179284866091, 0.7160433070328504623 ) ) ;
#33250=CARTESIAN_POINT ( 'NONE',  ( -0.9873396505805591694, -0.1113553986120547346, 0.5856299211523150472 ) ) ;
#33252=CARTESIAN_POINT ( 'NONE',  ( -0.9500414927467377701, 0.1787899950787401604, 1.766732283410803239 ) ) ;
#33258=CARTESIAN_POINT ( 'NONE',  ( -0.8107537697050253289, -0.1574803149606297803, 0.8243110236220465570 ) ) ;
#33261=CARTESIAN_POINT ( 'NONE',  ( -1.033464566929134687, 0.06523048226347956391, 1.577263779420032153 ) ) ;
#33262=CARTESIAN_POINT ( 'NONE',  ( 0.6971942568897637749, 2.189545951927499583E-17, 0.7947834645131652831 ) ) ;
#33263=CARTESIAN_POINT ( 'NONE',  ( 0.9500414927467377701, -0.1787899950787401604, 1.353346456639149986 ) ) ;
#33265=CARTESIAN_POINT ( 'NONE',  ( 0.7646288533564489232, 0.1113553986120547346, 1.402559055118110187 ) ) ;
#33266=CARTESIAN_POINT ( 'NONE',  ( 0.8335474968540336205, -0.1679597360014907503, 1.987423594222797574 ) ) ;
#33268=CARTESIAN_POINT ( 'NONE',  ( 0.8759842519685039353, -0.1574803149606299191, 1.486220472333417142 ) ) ;
#33270=CARTESIAN_POINT ( 'NONE',  ( 0.9500414927467377701, 0.1787899950787401604, 0.7775590550643457499 ) ) ;
#33271=CARTESIAN_POINT ( 'NONE',  ( -0.7646288533564489232, -0.1113553986120547346, 1.412401574803149540 ) ) ;
#33273=DIRECTION ( 'NONE',  ( 1.000000000000000000, 0.000000000000000000, -1.822029033848725275E-16 ) ) ;
#33274=VERTEX_POINT ( 'NONE', #40279 ) ;
#33275=CARTESIAN_POINT ( 'NONE',  ( 0.8107537697050254399, 0.1574803149606300301, 0.9276574803149607584 ) ) ;
#33276=CARTESIAN_POINT ( 'NONE',  ( -1.033464566929133799, 1.928577636452524610E-17, 2.869337061179095023E-17 ) ) ;
#33277=CARTESIAN_POINT ( 'NONE',  ( 0.8019270111902717657, -0.1787899950787401604, 1.033464566875371027 ) ) ;
#33281=EDGE_LOOP ( 'NONE', ( #12309, #25078, #23734 ) ) ;
#33283=FACE_OUTER_BOUND ( 'NONE', #39072, .T. ) ;
#33284=CARTESIAN_POINT ( 'NONE',  ( -1.054774247047244540, -0.07405724077823318263, 0.2559055117572600624 ) ) ;
#33285=CARTESIAN_POINT ( 'NONE',  ( -0.9873396505805591694, 0.1113553986120547346, 0.6053149606299212948 ) ) ;
#33288=CARTESIAN_POINT ( 'NONE',  ( -0.9500414927467378812, 0.1787899950787401604, 1.722440944828125930 ) ) ;
#33289=CARTESIAN_POINT ( 'NONE',  ( -0.7495606340400177148, -0.1264236179284866091, 0.3272637794737956463 ) ) ;
#33293=CARTESIAN_POINT ( 'NONE',  ( 0.8759842519685039353, 0.1787899950787401882, 0.03198818892261445085 ) ) ;
#33297=CARTESIAN_POINT ( 'NONE',  ( -0.9500414927467378812, -0.1787899950787401604, 1.043307086560409269 ) ) ;
#33298=LINE ( 'NONE', #19595, #14212 ) ;
#33299=CARTESIAN_POINT ( 'NONE',  ( -0.8759842519685039353, -0.1787899950787401882, 0.2878937007336381804 ) ) ;
#33301=CARTESIAN_POINT ( 'NONE',  ( -0.8759842519685039353, -0.1787899950787401882, 1.395177165300567124 ) ) ;
#33302=VERTEX_POINT ( 'NONE', #32434 ) ;
#33308=CARTESIAN_POINT ( 'NONE',  ( 0.9412147342319837628, -0.1574803149606297803, 0.3174212598425196763 ) ) ;
#33310=DIRECTION ( 'NONE',  ( -1.000000000000000000, 0.000000000000000000, 0.000000000000000000 ) ) ;
#33311=( BOUNDED_CURVE ( )  B_SPLINE_CURVE ( 2, ( #16467, #20519, #8789, #5670, #41826, #31329, #9271, #31102, #20279 ),
 .UNSPECIFIED., .F., .T. ) 
 B_SPLINE_CURVE_WITH_KNOTS ( ( 3, 2, 2, 2, 3 ),
 ( 0.6700000000000000400, 0.6724999999999999867, 0.6750000000000000444, 0.6774999999999999911, 0.6800000000000000488 ),
 .UNSPECIFIED. ) 
 CURVE ( )  GEOMETRIC_REPRESENTATION_ITEM ( )  RATIONAL_B_SPLINE_CURVE ( ( 1.000000000000000000, 0.9238795325112899581, 1.000000000000000000, 0.9238795325112869605, 1.000000000000000000, 0.9238795325112869605, 1.000000000000000000, 0.9238795325112869605, 1.000000000000000000 ) ) 
 REPRESENTATION_ITEM ( '' )  ) ;
#33312=CARTESIAN_POINT ( 'NONE',  ( -0.9873396505805591694, 0.1113553986120547346, 1.028543306979086802 ) ) ;
#33313=CARTESIAN_POINT ( 'NONE',  ( 0.6971942568897637749, 2.189545951927499583E-17, 0.4404527558517480901 ) ) ;
#33320=CARTESIAN_POINT ( 'NONE',  ( 0.8107537697050253289, -0.1574803149606297803, 0.9030511811023627100 ) ) ;
#33321=CARTESIAN_POINT ( 'NONE',  ( 0.7185039370078739607, 1.928577636452523993E-17, 1.368110236220472675 ) ) ;
#33323=EDGE_CURVE ( 'NONE', #13881, #20346, #25135, .T. ) ;
#33325=CARTESIAN_POINT ( 'NONE',  ( 0.7185039370078739607, 1.928577636452523993E-17, 1.043307086506645831 ) ) ;
#33328=CARTESIAN_POINT ( 'NONE',  ( 0.7646288533564489232, 0.1113553986120547346, 1.904527558947590515 ) ) ;
#33329=CARTESIAN_POINT ( 'NONE',  ( 1.033464566929133799, 0.000000000000000000, 1.141732283357039357 ) ) ;
#33333=CARTESIAN_POINT ( 'NONE',  ( 1.033464566929133799, 0.000000000000000000, 0.9055118109160944506 ) ) ;
#33338=CARTESIAN_POINT ( 'NONE',  ( -0.6971942568897648851, 0.07405724077823318263, 1.579724409395055318 ) ) ;
#33339=CARTESIAN_POINT ( 'NONE',  ( 0.9500414927467378812, 0.1787899950787401604, 1.727362204670645385 ) ) ;
#33340=CARTESIAN_POINT ( 'NONE',  ( -0.8759842519685039353, 0.1787899950787401882, 0.7849409448281259305 ) ) ;
#33342=CARTESIAN_POINT ( 'NONE',  ( 0.9500414927467378812, -0.1787899950787401604, 0.2952755904974176393 ) ) ;
#33344=CARTESIAN_POINT ( 'NONE',  ( -0.8019270111902716547, 0.1787899950787401604, 1.294291338528913204 ) ) ;
#33345=CARTESIAN_POINT ( 'NONE',  ( -0.8759842519685039353, 0.1787899950787401882, 0.7800196849856062542 ) ) ;
#33348=CARTESIAN_POINT ( 'NONE',  ( -1.054774247047244096, 0.000000000000000000, 1.601870078686393750 ) ) ;
#33349=CARTESIAN_POINT ( 'NONE',  ( -0.7646288533564489232, -0.1113553986120547346, 1.874999999892472458 ) ) ;
#33350=ORIENTED_EDGE ( 'NONE', *, *, #26158, .F. ) ;
#33354=CARTESIAN_POINT ( 'NONE',  ( -0.8107537697050253289, -0.1574803149606297803, 1.651082677165354839 ) ) ;
#33356=CARTESIAN_POINT ( 'NONE',  ( 0.6971942568897637749, 2.189545951927499583E-17, 1.464074803095842370 ) ) ;
#33358=CARTESIAN_POINT ( 'NONE',  ( -0.9412147342319837628, 0.1574803149606300301, 0.3617125983176697201 ) ) ;
#33363=EDGE_CURVE ( 'NONE', #17196, #44204, #14088, .T. ) ;
#33368=CARTESIAN_POINT ( 'NONE',  ( 0.9500414927467378812, -0.1787899950787401604, 1.747047244040724312 ) ) ;
#33373=CARTESIAN_POINT ( 'NONE',  ( 0.6971942568897626646, 0.07405724077823318263, 0.7874015747493863238 ) ) ;
#33374=EDGE_CURVE ( 'NONE', #35698, #4424, #32146, .T. ) ;
#33378=CARTESIAN_POINT ( 'NONE',  ( -0.9215977125122606362, -0.1699356664333222244, 1.989001160739882312 ) ) ;
#33379=CARTESIAN_POINT ( 'NONE',  ( 0.7646288533564489232, 0.1113553986120547346, 0.4576771653543307283 ) ) ;
#33380=CARTESIAN_POINT ( 'NONE',  ( 0.6971942568897637749, 2.189545951927499583E-17, 1.857775590497417362 ) ) ;
#33383=AXIS2_PLACEMENT_3D ( 'NONE', #17835, #21671, #32478 ) ;
#33384=CARTESIAN_POINT ( 'NONE',  ( 0.8107537697050253289, 0.1574803149606300301, 0.06151574803149607168 ) ) ;
#33387=ADVANCED_FACE ( 'NONE', ( #15154 ), #38127, .T. ) ;
#33390=CARTESIAN_POINT ( 'NONE',  ( 0.7495606340400177148, 0.1264236179284866091, 0.1993110235682838682 ) ) ;
#33392=CARTESIAN_POINT ( 'NONE',  ( -0.8019270111902717657, -0.1787899950787401604, 1.545275590497416696 ) ) ;
#33394=CARTESIAN_POINT ( 'NONE',  ( -0.9500414927467378812, -0.1787899950787401604, 1.161417322780881278 ) ) ;
#33395=CARTESIAN_POINT ( 'NONE',  ( -0.7185039370078739607, 1.928577636452523993E-17, 0.3444881889763780070 ) ) ;
#33397=CARTESIAN_POINT ( 'NONE',  ( 0.7495606340400177148, -0.1264236179284866091, 1.272145669237574772 ) ) ;
#33398=CARTESIAN_POINT ( 'NONE',  ( 0.6971942568897648851, 0.07405724077823318263, 1.968503936954110189 ) ) ;
#33399=CARTESIAN_POINT ( 'NONE',  ( -0.8019270111902717657, -0.1787899950787401604, 1.033464566875371027 ) ) ;
#33402=CARTESIAN_POINT ( 'NONE',  ( 1.054774247047244540, 0.07405724077823318263, 0.3838582676627718127 ) ) ;
#33403=CARTESIAN_POINT ( 'NONE',  ( -1.054774247047244096, 0.000000000000000000, 0.1796259841982051075 ) ) ;
#33404=CARTESIAN_POINT ( 'NONE',  ( -0.7495606340400177148, 0.1264236179284866091, 0.7455708660879684091 ) ) ;
#33405=CARTESIAN_POINT ( 'NONE',  ( 1.033464566929134687, -0.06523048226347956391, 1.729822834538142784 ) ) ;
#33406=CARTESIAN_POINT ( 'NONE',  ( -1.033464566929133799, 0.000000000000000000, 0.8661417321759370402 ) ) ;
#33408=CARTESIAN_POINT ( 'NONE',  ( 0.7495606340400177148, 0.1264236179284866091, 0.9079724408911180600 ) ) ;
#33409=CARTESIAN_POINT ( 'NONE',  ( -0.7646288533564489232, -0.1113553986120547346, 0.1131889763779527630 ) ) ;
#33410=CARTESIAN_POINT ( 'NONE',  ( 0.7495606340400177148, -0.1264236179284866091, 0.9965551180564724554 ) ) ;
#33411=CARTESIAN_POINT ( 'NONE',  ( -1.002407869896990045, -0.1264236179284866091, 1.985728346402929168 ) ) ;
#33415=CARTESIAN_POINT ( 'NONE',  ( 0.8759842519685039353, 0.1787899950787401882, 1.882381889710015743 ) ) ;
#33416=EDGE_CURVE ( 'NONE', #20097, #27388, #21783, .T. ) ;
#33417=CARTESIAN_POINT ( 'NONE',  ( -0.7495606340400177148, -0.1264236179284866091, 0.04675196845017354913 ) ) ;
#33422=ORIENTED_EDGE ( 'NONE', *, *, #35122, .T. ) ;
#33423=CARTESIAN_POINT ( 'NONE',  ( 0.9500414927467378812, -0.1787899950787401604, 1.156496062938362046 ) ) ;
#33424=EDGE_CURVE ( 'NONE', #19175, #26131, #44577, .T. ) ;
#33427=( BOUNDED_CURVE ( )  B_SPLINE_CURVE ( 2, ( #23408, #29286, #3815, #38012, #12398, #11032, #18208, #26537, #33086 ),
 .UNSPECIFIED., .F., .T. ) 
 B_SPLINE_CURVE_WITH_KNOTS ( ( 3, 2, 2, 2, 3 ),
 ( 0.3900000000000000133, 0.3925000000000000155, 0.3950000000000000178, 0.3975000000000000200, 0.4000000000000000222 ),
 .UNSPECIFIED. ) 
 CURVE ( )  GEOMETRIC_REPRESENTATION_ITEM ( )  RATIONAL_B_SPLINE_CURVE ( ( 1.000000000000000000, 0.9238795325112869605, 1.000000000000000000, 0.9238795325112869605, 1.000000000000000000, 0.9238795325112869605, 1.000000000000000000, 0.9238795325112869605, 1.000000000000000000 ) ) 
 REPRESENTATION_ITEM ( '' )  ) ;
#33428=CARTESIAN_POINT ( 'NONE',  ( 0.8759842519685039353, 0.1787899950787401882, 0.1107283464029295283 ) ) ;
#33431=LINE ( 'NONE', #32305, #7361 ) ;
#33432=CARTESIAN_POINT ( 'NONE',  ( -0.8759842519685039353, 0.1787899950787401882, 0.7062007873478109987 ) ) ;
#33435=CARTESIAN_POINT ( 'NONE',  ( 0.8019270111902717657, -0.1787899950787401604, 1.313976377898992132 ) ) ;
#33436=CARTESIAN_POINT ( 'NONE',  ( 0.7495606340400177148, -0.1264236179284866091, 1.700295275536787498 ) ) ;
#33438=CARTESIAN_POINT ( 'NONE',  ( 1.033464566929134687, -0.06523048226347956391, 0.9030511809948349455 ) ) ;
#33441=CARTESIAN_POINT ( 'NONE',  ( 1.033464566929133799, 0.000000000000000000, 0.8759842519685039353 ) ) ;
#33442=( BOUNDED_CURVE ( )  B_SPLINE_CURVE ( 2, ( #16680, #5887, #35135, #27730, #45885, #42043, #42293, #5397, #5646 ),
 .UNSPECIFIED., .F., .T. ) 
 B_SPLINE_CURVE_WITH_KNOTS ( ( 3, 2, 2, 2, 3 ),
 ( 0.1100000000000000006, 0.1125000000000000028, 0.1150000000000000050, 0.1174999999999999933, 0.1199999999999999956 ),
 .UNSPECIFIED. ) 
 CURVE ( )  GEOMETRIC_REPRESENTATION_ITEM ( )  RATIONAL_B_SPLINE_CURVE ( ( 1.000000000000000000, 0.9238795325112869605, 1.000000000000000000, 0.9238795325112869605, 1.000000000000000000, 0.9238795325112869605, 1.000000000000000000, 0.9238795325112869605, 1.000000000000000000 ) ) 
 REPRESENTATION_ITEM ( '' )  ) ;
#33443=CARTESIAN_POINT ( 'NONE',  ( 1.054774247047244540, 0.07405724077823318263, 0.2608267715997796832 ) ) ;
#33444=CARTESIAN_POINT ( 'NONE',  ( 1.054774247047244540, -0.07405724077823318263, 1.240157480261197875 ) ) ;
#33445=CARTESIAN_POINT ( 'NONE',  ( -0.9873396505805591694, 0.1113553986120547346, 1.707677165354330562 ) ) ;
#33448=CARTESIAN_POINT ( 'NONE',  ( -0.6971942568897648851, -0.07405724077823297447, 1.186023621993481658 ) ) ;
#33449=CARTESIAN_POINT ( 'NONE',  ( 1.033464566929133799, 0.000000000000000000, 0.6692913384751496553 ) ) ;
#33451=CARTESIAN_POINT ( 'NONE',  ( -0.8759842519685039353, 0.1574803149606299191, 1.751968503937007871 ) ) ;
#33452=CARTESIAN_POINT ( 'NONE',  ( -1.033464566929133799, 1.928577636452524610E-17, 2.869337061179095023E-17 ) ) ;
#33453=ORIENTED_EDGE ( 'NONE', *, *, #47018, .F. ) ;
#33455=EDGE_LOOP ( 'NONE', ( #2374, #40827, #39759, #14059 ) ) ;
#33457=CARTESIAN_POINT ( 'NONE',  ( 0.8019270111902717657, 0.1787899950787401604, 1.648622047190331230 ) ) ;
#33458=CARTESIAN_POINT ( 'NONE',  ( -1.033464566929133799, 0.000000000000000000, 1.102362204616881947 ) ) ;
#33460=CARTESIAN_POINT ( 'NONE',  ( -1.033464566929134687, -0.06523048226347956391, 0.1254921259842521064 ) ) ;
#33461=CARTESIAN_POINT ( 'NONE',  ( 0.7185039370078739607, 1.928577636452523993E-17, 0.3740157479239689664 ) ) ;
#33464=CARTESIAN_POINT ( 'NONE',  ( -0.9873396505805591694, 0.1113553986120547346, 0.3690944881889763884 ) ) ;
#33466=ORIENTED_EDGE ( 'NONE', *, *, #40725, .T. ) ;
#33467=CARTESIAN_POINT ( 'NONE',  ( 1.002407869896990045, 0.1264236179284866091, 0.8981299212060788184 ) ) ;
#33470=VECTOR ( 'NONE', #6024, 39.37007874015748143 ) ;
#33473=CARTESIAN_POINT ( 'NONE',  ( -0.6971942568897637749, 2.189545951927499583E-17, 0.2829724408911185041 ) ) ;
#33479=VERTEX_POINT ( 'NONE', #29798 ) ;
#33480=CARTESIAN_POINT ( 'NONE',  ( 0.8019270111902717657, 0.1787899950787401604, 1.018700787347811110 ) ) ;
#33482=CARTESIAN_POINT ( 'NONE',  ( 0.7185039370078746268, -0.06523048226347956391, 1.203248031388535200 ) ) ;
#33486=CARTESIAN_POINT ( 'NONE',  ( -1.054774247047244540, 0.07405724077823318263, 0.1082677164816695514 ) ) ;
#33487=CARTESIAN_POINT ( 'NONE',  ( -0.7185039370078739607, 1.928577636452523993E-17, 0.8169291338582678197 ) ) ;
#33488=CARTESIAN_POINT ( 'NONE',  ( -0.5314960629921260393, -1.928577636452524610E-17, 4.498031496062992574 ) ) ;
#33491=CARTESIAN_POINT ( 'NONE',  ( -0.9412147342319837628, 0.1574803149606300301, 1.582185039262551607 ) ) ;
#33492=CARTESIAN_POINT ( 'NONE',  ( 1.054774247047244540, 0.07405724077823318263, 0.8562992125446617919 ) ) ;
#33493=CARTESIAN_POINT ( 'NONE',  ( 0.8019270111902716547, 0.1787899950787401604, 1.373031496009229357 ) ) ;
#33494=CARTESIAN_POINT ( 'NONE',  ( 0.9412147342319837628, 0.1574803149606300301, 0.5191929132782994172 ) ) ;
#33495=CARTESIAN_POINT ( 'NONE',  ( 1.033464566929134687, -0.06523048226347956391, 1.385334645669290987 ) ) ;
#33496=CARTESIAN_POINT ( 'NONE',  ( 0.7099058204916336434, -0.002335345252131881735, 1.983306857452649341 ) ) ;
#33498=LINE ( 'NONE', #4214, #20558 ) ;
#33501=CARTESIAN_POINT ( 'NONE',  ( 1.002407869896990045, -0.1264236179284866091, 0.7652559054580472253 ) ) ;
#33505=CARTESIAN_POINT ( 'NONE',  ( 0.7185039370078739607, 1.928577636452523993E-17, 0.4133858266641267654 ) ) ;
#33507=CARTESIAN_POINT ( 'NONE',  ( 1.054774247047244096, 0.000000000000000000, 1.124507873961984261 ) ) ;
#33513=CARTESIAN_POINT ( 'NONE',  ( -0.6971942568897626646, 0.07405724077823318263, 0.2362204723871814960 ) ) ;
#33514=CARTESIAN_POINT ( 'NONE',  ( 0.7185039370078746268, 0.06523048226347956391, 0.3420275590551182798 ) ) ;
#33516=LINE ( 'NONE', #31920, #25688 ) ;
#33517=CARTESIAN_POINT ( 'NONE',  ( -0.6971942568897648851, 0.07405724077823318263, 1.692913385773008539 ) ) ;
#33518=CARTESIAN_POINT ( 'NONE',  ( -0.8759842519685039353, 0.1787899950787401882, 0.8587598424659212970 ) ) ;
#33519=CARTESIAN_POINT ( 'NONE',  ( -1.002407869896990045, -0.1264236179284866091, 0.5733267715997795166 ) ) ;
#33520=EDGE_CURVE ( 'NONE', #28038, #6061, #26988, .T. ) ;
#33521=CARTESIAN_POINT ( 'NONE',  ( -1.033464566929133799, 0.000000000000000000, 0.6791338582677166613 ) ) ;
#33522=CARTESIAN_POINT ( 'NONE',  ( -0.8759842519685039353, -0.1787899950787401882, 1.985728346402929168 ) ) ;
#33523=DIRECTION ( 'NONE',  ( -1.000000000000000000, 0.000000000000000000, 0.000000000000000000 ) ) ;
#33524=CARTESIAN_POINT ( 'NONE',  ( 0.6971942568897637749, 2.189545951927499583E-17, 0.04183070860765386589 ) ) ;
#33531=AXIS2_PLACEMENT_3D ( 'NONE', #37367, #11999, #37138 ) ;
#33532=CARTESIAN_POINT ( 'NONE',  ( -0.6971942568897626646, 0.07405724077823318263, 0.3937007873478115538 ) ) ;
#33535=CARTESIAN_POINT ( 'NONE',  ( 0.7185039370078739607, 1.928577636452523993E-17, 1.604330708661417360 ) ) ;
#33537=CARTESIAN_POINT ( 'NONE',  ( -0.6971942568897648851, 0.07405724077823318263, 1.304133858213953667 ) ) ;
#33543=CYLINDRICAL_SURFACE ( 'NONE', #10245, 0.1574803149606299191 ) ;
#33544=CARTESIAN_POINT ( 'NONE',  ( -1.033464566929133799, 0.000000000000000000, 1.023622047136567126 ) ) ;
#33545=CARTESIAN_POINT ( 'NONE',  ( 0.9500414927467378812, -0.1787899950787401604, 0.6102362204186774219 ) ) ;
#33546=CARTESIAN_POINT ( 'NONE',  ( 0.7646288533564489232, 0.1113553986120547346, 0.5659448817822370081 ) ) ;
#33548=CARTESIAN_POINT ( 'NONE',  ( 0.8759842519685039353, -0.1574803149606299191, 1.998031495955464587 ) ) ;
#33551=CARTESIAN_POINT ( 'NONE',  ( -0.9500414927467377701, 0.1787899950787401604, 1.018700787347811110 ) ) ;
#33552=CARTESIAN_POINT ( 'NONE',  ( 0.7185039370078746268, -0.06523048226347956391, 1.016240157480315487 ) ) ;
#33559=CARTESIAN_POINT ( 'NONE',  ( 0.6971942568897626646, 0.07405724077823318263, 0.7086614172690703928 ) ) ;
#33567=CARTESIAN_POINT ( 'NONE',  ( 0.7646288533564489232, 0.1113553986120547346, 1.117125984144440975 ) ) ;
#33569=CARTESIAN_POINT ( 'NONE',  ( -0.8759842519685039353, -0.1787899950787401882, 0.4847440944344252323 ) ) ;
#33572=CARTESIAN_POINT ( 'NONE',  ( -1.054774247047244540, -0.07405724077823318263, 1.835629921206078485 ) ) ;
#33573=EDGE_CURVE ( 'NONE', #1467, #14891, #31879, .T. ) ;
#33574=CARTESIAN_POINT ( 'NONE',  ( 0.6971942568897637749, 2.189545951927499583E-17, 1.700295275536787498 ) ) ;
#33576=CARTESIAN_POINT ( 'NONE',  ( -1.002407869896990045, 0.1264236179284866091, 0.8981299212060788184 ) ) ;
#33577=LINE ( 'NONE', #37136, #2653 ) ;
#33579=CARTESIAN_POINT ( 'NONE',  ( -0.8759842519685039353, 0.1787899950787401882, 1.252460629867496067 ) ) ;
#33580=CARTESIAN_POINT ( 'NONE',  ( -0.8019270111902717657, 0.1787899950787401604, 0.9399606298674970661 ) ) ;
#33582=CARTESIAN_POINT ( 'NONE',  ( -0.7495606340400177148, 0.1264236179284866091, 0.04183070860765386589 ) ) ;
#33585=CARTESIAN_POINT ( 'NONE',  ( -0.6971942568897637749, 2.189545951927499583E-17, 1.542814960576157413 ) ) ;
#33586=CARTESIAN_POINT ( 'NONE',  ( -0.9873396505805591694, -0.1113553986120547346, 1.924212598317669221 ) ) ;
#33588=CARTESIAN_POINT ( 'NONE',  ( -0.7185039370078746268, -0.06523048226347956391, 1.646161417322835385 ) ) ;
#33590=CARTESIAN_POINT ( 'NONE',  ( 0.9500414927467377701, -0.1787899950787401604, 1.555118110182457158 ) ) ;
#33592=CARTESIAN_POINT ( 'NONE',  ( 1.033464566929133799, 0.000000000000000000, 1.023622047136567126 ) ) ;
#33594=EDGE_LOOP ( 'NONE', ( #45915, #26450, #40683, #36673 ) ) ;
#33595=EDGE_CURVE ( 'NONE', #20346, #47229, #9794, .T. ) ;
#33596=AXIS2_PLACEMENT_3D ( 'NONE', #32493, #24342, #38940 ) ;
#33597=ORIENTED_EDGE ( 'NONE', *, *, #10016, .F. ) ;
#33598=ORIENTED_EDGE ( 'NONE', *, *, #3361, .F. ) ;
#33604=CARTESIAN_POINT ( 'NONE',  ( 1.054774247047244096, 0.000000000000000000, 1.715059055064346527 ) ) ;
#33610=DIRECTION ( 'NONE',  ( 0.000000000000000000, 0.000000000000000000, -1.000000000000000000 ) ) ;
#33612=CARTESIAN_POINT ( 'NONE',  ( 0.9873396505805591694, 0.1113553986120547346, 0.4478346456692913202 ) ) ;
#33613=CARTESIAN_POINT ( 'NONE',  ( 0.8019270111902717657, 0.1787899950787401604, 1.811023621993480548 ) ) ;
#33614=CARTESIAN_POINT ( 'NONE',  ( 0.7185039370078739607, 1.928577636452523993E-17, 1.870078740049952559 ) ) ;
#33616=ORIENTED_EDGE ( 'NONE', *, *, #32106, .F. ) ;
#33619=CARTESIAN_POINT ( 'NONE',  ( -0.7185039370078746268, 0.06523048226347956391, 0.1845472440944882775 ) ) ;
#33621=CARTESIAN_POINT ( 'NONE',  ( 0.6971942568897626646, -0.07405724077823297447, 0.1673228345919059168 ) ) ;
#33624=CARTESIAN_POINT ( 'NONE',  ( -0.6971942568897637749, 2.189545951927499583E-17, 1.734744094434425232 ) ) ;
#33626=CARTESIAN_POINT ( 'NONE',  ( -0.6971942568897648851, -0.07405724077823297447, 1.269685039316314601 ) ) ;
#33627=LINE ( 'NONE', #26192, #21481 ) ;
#33629=CARTESIAN_POINT ( 'NONE',  ( 1.054774247047244540, 0.07405724077823318263, 1.328740157426552049 ) ) ;
#33630=CARTESIAN_POINT ( 'NONE',  ( 0.9500414927467378812, 0.1787899950787401604, 1.919291338528913871 ) ) ;
#33631=CARTESIAN_POINT ( 'NONE',  ( -1.054774247047244096, 0.000000000000000000, 1.006397637741511808 ) ) ;
#33634=CARTESIAN_POINT ( 'NONE',  ( 0.8759842519685039353, -0.1787899950787401882, 0.4896653542769449086 ) ) ;
#33635=CARTESIAN_POINT ( 'NONE',  ( -0.8759842519685039353, 0.1787899950787401882, 0.3469488188438744070 ) ) ;
#33636=CARTESIAN_POINT ( 'NONE',  ( -0.8019270111902717657, -0.1787899950787401604, 0.8366141731745828647 ) ) ;
#33637=CARTESIAN_POINT ( 'NONE',  ( 0.7646288533564489232, -0.1113553986120547346, 1.717519684931842594 ) ) ;
#33640=CARTESIAN_POINT ( 'NONE',  ( -0.7185039370078714072, 0.06523048226347728795, 1.365649606299213614 ) ) ;
#33642=CARTESIAN_POINT ( 'NONE',  ( -0.7185039370078739607, 1.928577636452523993E-17, 0.1476377952755905387 ) ) ;
#33644=CARTESIAN_POINT ( 'NONE',  ( 0.9500414927467377701, -0.1787899950787401604, 1.200787401521039355 ) ) ;
#33645=CARTESIAN_POINT ( 'NONE',  ( 0.7646288533564489232, 0.1113553986120547346, 1.943897637687747926 ) ) ;
#33646=ORIENTED_EDGE ( 'NONE', *, *, #34767, .F. ) ;
#33650=VERTEX_POINT ( 'NONE', #5230 ) ;
#33653=CARTESIAN_POINT ( 'NONE',  ( 0.7495606340400177148, -0.1264236179284866091, 1.267224409395055096 ) ) ;
#33658=CARTESIAN_POINT ( 'NONE',  ( 0.6971942568897648851, 0.07405724077823318263, 1.496062992072220821 ) ) ;
#33659=CARTESIAN_POINT ( 'NONE',  ( 0.6971942568897637749, 2.189545951927499583E-17, 0.1993110235682838682 ) ) ;
#33663=DIRECTION ( 'NONE',  ( 1.822029033848725028E-16, 0.000000000000000000, 1.000000000000000000 ) ) ;
#33664=AXIS2_PLACEMENT_3D ( 'NONE', #2021, #45615, #5863 ) ;
#33665=CARTESIAN_POINT ( 'NONE',  ( -0.8019270111902716547, 0.1787899950787401604, 0.6299212597887560161 ) ) ;
#33667=CARTESIAN_POINT ( 'NONE',  ( 0.7185039370078739607, 1.928577636452523993E-17, 0.2952755904436539236 ) ) ;
#33669=CARTESIAN_POINT ( 'NONE',  ( -0.7185039370078739607, 1.928577636452523993E-17, 1.751968503829480106 ) ) ;
#33670=CARTESIAN_POINT ( 'NONE',  ( -1.033464566929133799, 1.928577636452524610E-17, 2.869337061179095023E-17 ) ) ;
#33671=CARTESIAN_POINT ( 'NONE',  ( 0.9500414927467378812, 0.1787899950787401604, 1.412401574749386990 ) ) ;
#33673=CARTESIAN_POINT ( 'NONE',  ( 1.002407869896990045, 0.1264236179284866091, 1.759350393647023614 ) ) ;
#33674=CARTESIAN_POINT ( 'NONE',  ( 0.7646288533564489232, 0.1113553986120547346, 0.1427165354330708902 ) ) ;
#33675=EDGE_CURVE ( 'NONE', #37113, #6940, #2113, .T. ) ;
#33676=CARTESIAN_POINT ( 'NONE',  ( 1.033464566929133799, 0.000000000000000000, 0.9055118109160944506 ) ) ;
#33680=CARTESIAN_POINT ( 'NONE',  ( 0.8759842519685039353, 0.1787899950787401882, 0.3469488188438744070 ) ) ;
#33682=CARTESIAN_POINT ( 'NONE',  ( 0.7331056760640133341, -0.08919270234511263162, 0.03937007864081804726 ) ) ;
#33685=CARTESIAN_POINT ( 'NONE',  ( -1.033464566929133799, 0.000000000000000000, 0.7578740157480314821 ) ) ;
#33686=CARTESIAN_POINT ( 'NONE',  ( -0.6971942568897648851, -0.07405724077823297447, 1.343503936954111744 ) ) ;
#33687=CARTESIAN_POINT ( 'NONE',  ( 0.8759842519685039353, 0.1574803149606299191, 0.6003937006798740761 ) ) ;
#33688=ORIENTED_EDGE ( 'NONE', *, *, #34767, .T. ) ;
#33694=CARTESIAN_POINT ( 'NONE',  ( 1.033464566929134687, 0.06523048226347956391, 0.8292322833570401341 ) ) ;
#33697=CARTESIAN_POINT ( 'NONE',  ( -0.9412147342319918675, -0.1574803149606224251, 0.04183070866141774813 ) ) ;
#33698=CARTESIAN_POINT ( 'NONE',  ( -0.7185039370078746268, 0.06523048226347956391, 1.208169291338584417 ) ) ;
#33700=CARTESIAN_POINT ( 'NONE',  ( 0.9873396505805591694, 0.1113553986120547346, 0.5659448818897637734 ) ) ;
#33701=CARTESIAN_POINT ( 'NONE',  ( -0.7646288533564489232, 0.1113553986120547346, 0.9301181102362204856 ) ) ;
#33703=CARTESIAN_POINT ( 'NONE',  ( 1.033464566929133799, 1.928577636452524610E-17, 4.498031496062992574 ) ) ;
#33706=VECTOR ( 'NONE', #32333, 39.37007874015748143 ) ;
#33707=CARTESIAN_POINT ( 'NONE',  ( 0.7185039370078739607, 1.928577636452523993E-17, 1.003937007766488199 ) ) ;
#33708=ORIENTED_EDGE ( 'NONE', *, *, #32933, .F. ) ;
#33710=CARTESIAN_POINT ( 'NONE',  ( -0.7495606340400177148, 0.1264236179284866091, 1.532972440891118060 ) ) ;
#33712=CARTESIAN_POINT ( 'NONE',  ( -0.9500414927467378812, 0.1787899950787401604, 1.294291338528912982 ) ) ;
#33715=( BOUNDED_CURVE ( )  B_SPLINE_CURVE ( 2, ( #5474, #34735, #31378, #12458, #27559, #16280, #16739, #38779, #35198 ),
 .UNSPECIFIED., .F., .F. ) 
 B_SPLINE_CURVE_WITH_KNOTS ( ( 3, 2, 2, 2, 3 ),
 ( 0.08000000000000000167, 0.08250000000000000389, 0.08500000000000000611, 0.08749999999999999445, 0.08999999999999999667 ),
 .UNSPECIFIED. ) 
 CURVE ( )  GEOMETRIC_REPRESENTATION_ITEM ( )  RATIONAL_B_SPLINE_CURVE ( ( 1.000000000000000000, 0.9238795325112869605, 1.000000000000000000, 0.9238795325112869605, 1.000000000000000000, 0.9238795325112869605, 1.000000000000000000, 0.9238795325112869605, 1.000000000000000000 ) ) 
 REPRESENTATION_ITEM ( '' )  ) ;
#33716=CARTESIAN_POINT ( 'NONE',  ( -1.054774247047244096, 0.000000000000000000, 0.3420275590013546751 ) ) ;
#33718=CARTESIAN_POINT ( 'NONE',  ( 0.8759842519685039353, 0.000000000000000000, 2.007874015640504162 ) ) ;
#33722=ORIENTED_EDGE ( 'NONE', *, *, #4640, .T. ) ;
#33724=CARTESIAN_POINT ( 'NONE',  ( -0.8759842519685039353, 0.000000000000000000, 0.000000000000000000 ) ) ;
#33726=CARTESIAN_POINT ( 'NONE',  ( 0.7185039370078739607, 0.000000000000000000, 4.498031496062992574 ) ) ;
#33728=( BOUNDED_CURVE ( )  B_SPLINE_CURVE ( 2, ( #7501, #36294, #3447, #14707, #1246, #26448, #45329, #38154, #41013 ),
 .UNSPECIFIED., .F., .T. ) 
 B_SPLINE_CURVE_WITH_KNOTS ( ( 3, 2, 2, 2, 3 ),
 ( 0.08999999999999999667, 0.09249999999999999889, 0.09500000000000000111, 0.09750000000000000333, 0.1000000000000000056 ),
 .UNSPECIFIED. ) 
 CURVE ( )  GEOMETRIC_REPRESENTATION_ITEM ( )  RATIONAL_B_SPLINE_CURVE ( ( 1.000000000000000000, 0.9238795325112869605, 1.000000000000000000, 0.9238795325112869605, 1.000000000000000000, 0.9238795325112869605, 1.000000000000000000, 0.9238795325112869605, 1.000000000000000000 ) ) 
 REPRESENTATION_ITEM ( '' )  ) ;
#33729=CARTESIAN_POINT ( 'NONE',  ( -1.054774247047244096, 0.000000000000000000, 0.1845472440407248116 ) ) ;
#33730=CARTESIAN_POINT ( 'NONE',  ( -1.033464566929134687, -0.06523048226347956391, 0.9522637795275590289 ) ) ;
#33735=CARTESIAN_POINT ( 'NONE',  ( -0.8759842519685039353, -0.1574803149606299191, 1.486220472333417142 ) ) ;
#33736=CARTESIAN_POINT ( 'NONE',  ( 0.9500414927467378812, 0.1787899950787401604, 0.9399606298674970661 ) ) ;
#33739=CARTESIAN_POINT ( 'NONE',  ( 0.8107537697050253289, 0.1574803149606300301, 1.439468503937006538 ) ) ;
#33740=CARTESIAN_POINT ( 'NONE',  ( 0.7133215388179315886, 0.02839841869291725301, 1.982739101751397781 ) ) ;
#33746=CARTESIAN_POINT ( 'NONE',  ( 0.8759842519685039353, 0.1787899950787401882, 0.8193897637257637756 ) ) ;
#33748=CARTESIAN_POINT ( 'NONE',  ( 0.7495606340400177148, 0.1264236179284866091, 1.852854330654897685 ) ) ;
#33752=CARTESIAN_POINT ( 'NONE',  ( -0.8107537697050253289, 0.1574803149606300301, 0.09104330697908720460 ) ) ;
#33753=CARTESIAN_POINT ( 'NONE',  ( 0.6971942568897637749, 2.189545951927499583E-17, 1.104822834591905556 ) ) ;
#33755=DIRECTION ( 'NONE',  ( 0.000000000000000000, 0.000000000000000000, -1.000000000000000000 ) ) ;
#33758=CARTESIAN_POINT ( 'NONE',  ( -1.002407869896990045, 0.1264236179284866091, 0.4995078739619842612 ) ) ;
#33761=CARTESIAN_POINT ( 'NONE',  ( -0.6971942568897637749, 2.189545951927499583E-17, 0.2780511810485988278 ) ) ;
#33763=CARTESIAN_POINT ( 'NONE',  ( -0.8759842519685039353, 0.1574803149606299191, 0.6102362204724409711 ) ) ;
#33765=CARTESIAN_POINT ( 'NONE',  ( -0.7495606340400177148, 0.1264236179284866091, 1.808562992072220377 ) ) ;
#33766=CARTESIAN_POINT ( 'NONE',  ( -1.054774247047244540, 0.07405724077823318263, 0.9301181101824563813 ) ) ;
#33767=CARTESIAN_POINT ( 'NONE',  ( -0.6971942568897626646, 0.07405724077823318263, 0.5561023621509617598 ) ) ;
#33769=CARTESIAN_POINT ( 'NONE',  ( 1.033464566929134687, 0.06523048226347956391, 0.3961614172153076763 ) ) ;
#33771=CARTESIAN_POINT ( 'NONE',  ( -0.8759842519685039353, 0.1574803149606299191, 1.673228346456693050 ) ) ;
#33775=CARTESIAN_POINT ( 'NONE',  ( 0.9412147342319837628, 0.1574803149606300301, 1.788877952755905554 ) ) ;
#33779=CARTESIAN_POINT ( 'NONE',  ( -1.054774247047244540, 0.07405724077823318263, 0.2608267715997796832 ) ) ;
#33785=EDGE_CURVE ( 'NONE', #25810, #38992, #3725, .T. ) ;
#33788=CARTESIAN_POINT ( 'NONE',  ( -0.8107537697050253289, -0.1574803149606297803, 1.050688976270426567 ) ) ;
#33789=CARTESIAN_POINT ( 'NONE',  ( 0.8759842519685039353, -0.1787899950787401882, 0.4896653542769449086 ) ) ;
#33795=CARTESIAN_POINT ( 'NONE',  ( -1.002407869896990045, 0.1264236179284866091, 0.8981299212060788184 ) ) ;
#33796=CARTESIAN_POINT ( 'NONE',  ( 0.8759842519685039353, -0.1574803149606299191, 0.9448818897637796255 ) ) ;
#33801=EDGE_LOOP ( 'NONE', ( #23673, #19963, #27297, #33597 ) ) ;
#33803=VECTOR ( 'NONE', #34006, 39.37007874015748143 ) ;
#33805=CARTESIAN_POINT ( 'NONE',  ( 0.7495606340400177148, -0.1264236179284866091, 0.7160433070328504623 ) ) ;
#33808=CARTESIAN_POINT ( 'NONE',  ( 1.033464566929134687, -0.06523048226347956391, 0.8341535433070870198 ) ) ;
#33813=CARTESIAN_POINT ( 'NONE',  ( 0.9873396505805591694, 0.1113553986120547346, 1.067913385719243990 ) ) ;
#33814=CARTESIAN_POINT ( 'NONE',  ( -1.033464566929133799, 0.000000000000000000, 1.663385826771653697 ) ) ;
#33816=VERTEX_POINT ( 'NONE', #32072 ) ;
#33817=CARTESIAN_POINT ( 'NONE',  ( -0.8759842519685039353, 0.1787899950787401882, 1.808562992072220377 ) ) ;
#33818=CARTESIAN_POINT ( 'NONE',  ( 0.7495606340400177148, 0.1264236179284866091, 1.656003936954110412 ) ) ;
#33819=CARTESIAN_POINT ( 'NONE',  ( -0.7185039370078739607, 0.000000000000000000, -2.869337061179095023E-17 ) ) ;
#33820=CARTESIAN_POINT ( 'NONE',  ( 1.002407869896990045, 0.1264236179284866091, 0.2682086613635594752 ) ) ;
#33821=CARTESIAN_POINT ( 'NONE',  ( -1.002407869896990045, -0.1264236179284866091, 1.434547244040724534 ) ) ;
#33822=CARTESIAN_POINT ( 'NONE',  ( -1.054774247047244540, -0.07405724077823318263, 1.318897637741511364 ) ) ;
#33824=CARTESIAN_POINT ( 'NONE',  ( -0.8019270111902717657, 0.1787899950787401604, 1.535433070812378675 ) ) ;
#33825=CARTESIAN_POINT ( 'NONE',  ( -0.7646288533564489232, -0.1113553986120547346, 1.993110236112944911 ) ) ;
#33827=CARTESIAN_POINT ( 'NONE',  ( -0.9412147342319837628, 0.1574803149606300301, 1.592027559055119390 ) ) ;
#33828=CARTESIAN_POINT ( 'NONE',  ( 1.033464566929134687, -0.06523048226347956391, 0.9817913384751512096 ) ) ;
#33830=CARTESIAN_POINT ( 'NONE',  ( 0.7185039370078739607, 1.928577636452523993E-17, 1.003937007766488199 ) ) ;
#33831=CARTESIAN_POINT ( 'NONE',  ( -0.7185039370078746268, 0.06523048226347956391, 1.798720472440944240 ) ) ;
#33837=CARTESIAN_POINT ( 'NONE',  ( -1.054774247047244540, -0.07405724077823318263, 1.166338582623402731 ) ) ;
#33839=AXIS2_PLACEMENT_3D ( 'NONE', #43631, #10841, #35984 ) ;
#33845=EDGE_CURVE ( 'NONE', #11565, #1914, #36758, .T. ) ;
#33846=CARTESIAN_POINT ( 'NONE',  ( 0.7495606340400177148, 0.1264236179284866091, 0.7455708660879684091 ) ) ;
#33848=ADVANCED_FACE ( 'NONE', ( #40173 ), #7374, .T. ) ;
#33851=CARTESIAN_POINT ( 'NONE',  ( 1.033464566929133799, 1.928577636452524610E-17, 4.498031496062992574 ) ) ;
#33852=CARTESIAN_POINT ( 'NONE',  ( 1.033464566929133799, 0.000000000000000000, 1.269685039370078705 ) ) ;
#33853=CARTESIAN_POINT ( 'NONE',  ( 0.9500414927467378812, -0.1787899950787401604, 1.791338582623401177 ) ) ;
#33856=CARTESIAN_POINT ( 'NONE',  ( 0.7185039370078746268, -0.06523048226347956391, 0.1107283464566929249 ) ) ;
#33857=DIRECTION ( 'NONE',  ( 1.000000000000000000, 0.000000000000000000, -1.822029033848725275E-16 ) ) ;
#33861=CARTESIAN_POINT ( 'NONE',  ( 1.054774247047244540, -0.07405724077823318263, 0.3001968503399373711 ) ) ;
#33862=FACE_OUTER_BOUND ( 'NONE', #29779, .T. ) ;
#33864=CARTESIAN_POINT ( 'NONE',  ( -0.7495606340400177148, 0.1264236179284866091, 1.769192913332062966 ) ) ;
#33865=ORIENTED_EDGE ( 'NONE', *, *, #9953, .T. ) ;
#33866=CARTESIAN_POINT ( 'NONE',  ( -1.054774247047244540, -0.07405724077823318263, 1.323818897584032817 ) ) ;
#33867=CARTESIAN_POINT ( 'NONE',  ( -0.7185039370078746268, 0.06523048226347956391, 0.8932086614173216921 ) ) ;
#33868=CARTESIAN_POINT ( 'NONE',  ( 0.6971942568897648851, -0.07405724077823297447, 1.309055118056472899 ) ) ;
#33869=CARTESIAN_POINT ( 'NONE',  ( -1.054774247047244540, -0.07405724077823318263, 0.4970472440407249226 ) ) ;
#33871=CARTESIAN_POINT ( 'NONE',  ( 1.054774247047244096, 0.000000000000000000, 1.990649606245448844 ) ) ;
#33872=CARTESIAN_POINT ( 'NONE',  ( -0.7495606340400177148, 0.1264236179284866091, 0.9817913385289134265 ) ) ;
#33874=CARTESIAN_POINT ( 'NONE',  ( 0.9412147342319837628, 0.1574803149606300301, 1.198326771653543732 ) ) ;
#33875=CARTESIAN_POINT ( 'NONE',  ( 0.6971942568897648851, -0.07405724077823297447, 0.5216535432533228045 ) ) ;
#33876=CARTESIAN_POINT ( 'NONE',  ( -1.002407869896990045, -0.1264236179284866091, 0.3321850393163153226 ) ) ;
#33877=CARTESIAN_POINT ( 'NONE',  ( -1.054774247047244096, 0.000000000000000000, 0.8489173227808819444 ) ) ;
#33878=ORIENTED_EDGE ( 'NONE', *, *, #37506, .F. ) ;
#33879=VECTOR ( 'NONE', #45417, 39.37007874015748143 ) ;
#33880=CARTESIAN_POINT ( 'NONE',  ( -0.7646288533564489232, 0.1113553986120547346, 0.1427165354330708902 ) ) ;
#33881=CARTESIAN_POINT ( 'NONE',  ( 0.6971942568897648851, 0.07405724077823318263, 1.186023621993481658 ) ) ;
#33882=CARTESIAN_POINT ( 'NONE',  ( -1.054774247047244096, 0.000000000000000000, 1.990649606245448844 ) ) ;
#33885=CARTESIAN_POINT ( 'NONE',  ( -0.7495606340400177148, 0.1264236179284866091, 0.8686023621509606496 ) ) ;
#33886=CARTESIAN_POINT ( 'NONE',  ( -0.7185039370078739607, 1.928577636452523993E-17, 0.3051181102362204856 ) ) ;
#33887=CARTESIAN_POINT ( 'NONE',  ( -0.9500414927467378812, -0.1787899950787401604, 0.05413385821395302888 ) ) ;
#33892=ORIENTED_EDGE ( 'NONE', *, *, #2487, .T. ) ;
#33893=CARTESIAN_POINT ( 'NONE',  ( 1.002407869896990045, -0.1264236179284866091, 1.277066929080094448 ) ) ;
#33894=VECTOR ( 'NONE', #22553, 39.37007874015748143 ) ;
#33895=CARTESIAN_POINT ( 'NONE',  ( -0.9412147342319837628, 0.1574803149606300301, 0.8341535431995593664 ) ) ;
#33899=CARTESIAN_POINT ( 'NONE',  ( 1.054774247047244540, 0.07405724077823318263, 0.2214566928596220785 ) ) ;
#33904=FACE_OUTER_BOUND ( 'NONE', #39712, .T. ) ;
#33905=CARTESIAN_POINT ( 'NONE',  ( -0.6971942568897648851, -0.07405724077823297447, 0.6397637794737947026 ) ) ;
#33910=CARTESIAN_POINT ( 'NONE',  ( 0.7185039370078739607, 1.928577636452523993E-17, 1.446850393700787274 ) ) ;
#33912=CARTESIAN_POINT ( 'NONE',  ( 0.7495606340400177148, 0.1264236179284866091, 1.887303149552535420 ) ) ;
#33913=CARTESIAN_POINT ( 'NONE',  ( 0.7185039370078746268, 0.06523048226347977208, 0.1451771653543309226 ) ) ;
#33917=CARTESIAN_POINT ( 'NONE',  ( -0.8759842519685039353, 0.1574803149606299191, 1.230314960522393752 ) ) ;
#33918=CARTESIAN_POINT ( 'NONE',  ( 0.8019270111902717657, -0.1787899950787401604, 0.3641732282926931630 ) ) ;
#33919=CARTESIAN_POINT ( 'NONE',  ( -0.8759842519685039353, -0.1574803149606299191, 1.722440944774362270 ) ) ;
#33921=DIRECTION ( 'NONE',  ( 0.000000000000000000, 0.000000000000000000, -1.000000000000000000 ) ) ;
#33922=CARTESIAN_POINT ( 'NONE',  ( 0.8107537697050253289, 0.1574803149606300301, 0.6422244093412926569 ) ) ;
#33924=CARTESIAN_POINT ( 'NONE',  ( -0.8019270111902717657, -0.1787899950787401604, 1.077755905458048113 ) ) ;
#33930=CARTESIAN_POINT ( 'NONE',  ( -0.8759842519685039353, 0.1574803149606299191, 0.4822834644594015674 ) ) ;
#33931=PLANE ( 'NONE',  #20898 ) ;
#33932=CARTESIAN_POINT ( 'NONE',  ( 1.054774247047244540, -0.07405724077823318263, 1.594488188922613237 ) ) ;
#33933=CARTESIAN_POINT ( 'NONE',  ( -1.033464566929134687, -0.06523048226347956391, 1.188484251968505268 ) ) ;
#33934=CARTESIAN_POINT ( 'NONE',  ( -0.9873396505805591694, 0.1113553986120547346, 1.146653543199559033 ) ) ;
#33941=CARTESIAN_POINT ( 'NONE',  ( -0.7495606340400177148, 0.1264236179284866091, 1.572342519631275692 ) ) ;
#33943=CARTESIAN_POINT ( 'NONE',  ( -1.002407869896990045, 0.1264236179284866091, 1.252460629867496067 ) ) ;
#33944=VECTOR ( 'NONE', #41926, 39.37007874015748143 ) ;
#33945=ORIENTED_EDGE ( 'NONE', *, *, #7736, .F. ) ;
#33948=CARTESIAN_POINT ( 'NONE',  ( -1.054774247047244096, 0.000000000000000000, 0.3813976377415121966 ) ) ;
#33950=CARTESIAN_POINT ( 'NONE',  ( 1.033464566929134687, 0.06523048226347956391, 0.8686023620971983217 ) ) ;
#33953=ORIENTED_EDGE ( 'NONE', *, *, #14257, .T. ) ;
#33957=EDGE_CURVE ( 'NONE', #14401, #19175, #44697, .T. ) ;
#33961=CARTESIAN_POINT ( 'NONE',  ( -1.002407869896990045, -0.1264236179284866091, 0.2189960629383626012 ) ) ;
#33962=CARTESIAN_POINT ( 'NONE',  ( -1.033464566929134687, -0.06523048226347956391, 0.9128937007874008414 ) ) ;
#33964=CARTESIAN_POINT ( 'NONE',  ( -0.8107537697050254399, 0.1574803149606300301, 1.941437007766490863 ) ) ;
#33965=CARTESIAN_POINT ( 'NONE',  ( 0.6971942568897626646, 0.07405724077823318263, 0.8710629920722218200 ) ) ;
#33966=CARTESIAN_POINT ( 'NONE',  ( 0.9412147342319837628, 0.1574803149606300301, 1.631397637795275468 ) ) ;
#33967=CARTESIAN_POINT ( 'NONE',  ( 0.7409552448146143888, -0.1027862860257732214, 1.985316688754235948 ) ) ;
#33973=CARTESIAN_POINT ( 'NONE',  ( 1.002407869896990045, 0.1264236179284866091, 0.8932086613635591421 ) ) ;
#33974=CARTESIAN_POINT ( 'NONE',  ( -0.8759842519685039353, -0.1574803149606299191, 1.417322834645669216 ) ) ;
#33975=CARTESIAN_POINT ( 'NONE',  ( 0.9500414927467377701, -0.1787899950787401604, 1.830708661363559253 ) ) ;
#33980=CARTESIAN_POINT ( 'NONE',  ( -0.8107537697050253289, 0.1574803149606300301, 0.05167322823892971095 ) ) ;
#33981=CARTESIAN_POINT ( 'NONE',  ( 1.054774247047244540, -0.07405724077823318263, 1.161417322780881278 ) ) ;
#33985=( BOUNDED_CURVE ( )  B_SPLINE_CURVE ( 2, ( #13433, #46467, #43101, #47193, #24680, #35930, #9835, #21547, #36185 ),
 .UNSPECIFIED., .F., .T. ) 
 B_SPLINE_CURVE_WITH_KNOTS ( ( 3, 2, 2, 2, 3 ),
 ( 0.1100000000000000006, 0.1125000000000000028, 0.1150000000000000050, 0.1174999999999999933, 0.1199999999999999956 ),
 .UNSPECIFIED. ) 
 CURVE ( )  GEOMETRIC_REPRESENTATION_ITEM ( )  RATIONAL_B_SPLINE_CURVE ( ( 1.000000000000000000, 0.9238795325112869605, 1.000000000000000000, 0.9238795325112869605, 1.000000000000000000, 0.9238795325112869605, 1.000000000000000000, 0.9238795325112869605, 1.000000000000000000 ) ) 
 REPRESENTATION_ITEM ( '' )  ) ;
#33988=CARTESIAN_POINT ( 'NONE',  ( -0.6971942568897626646, -0.07405724077823297447, 0.2411417322297011168 ) ) ;
#33992=CARTESIAN_POINT ( 'NONE',  ( -0.7495606340400177148, -0.1264236179284866091, 1.857775590497417362 ) ) ;
#33993=CARTESIAN_POINT ( 'NONE',  ( -0.6971942568897637749, 2.189545951927499583E-17, 0.9079724408911180600 ) ) ;
#33994=VECTOR ( 'NONE', #12582, 39.37007874015748143 ) ;
#33995=CARTESIAN_POINT ( 'NONE',  ( -1.054774247047244096, 0.000000000000000000, 0.5782480314422993040 ) ) ;
#34002=CARTESIAN_POINT ( 'NONE',  ( 1.033464566929134687, -0.06523048226347956391, 1.936515748031494510 ) ) ;
#34005=CARTESIAN_POINT ( 'NONE',  ( -1.002407869896990045, 0.1264236179284866091, 0.4995078739619842612 ) ) ;
#34006=DIRECTION ( 'NONE',  ( 1.822029033848725028E-16, 0.000000000000000000, 1.000000000000000000 ) ) ;
#34008=VERTEX_POINT ( 'NONE', #40688 ) ;
#34010=EDGE_CURVE ( 'NONE', #45765, #36143, #613, .T. ) ;
#34011=CARTESIAN_POINT ( 'NONE',  ( -0.9500414927467377701, -0.1787899950787401604, 1.476377952702141449 ) ) ;
#34015=CARTESIAN_POINT ( 'NONE',  ( 0.7185039370078739607, 1.928577636452523993E-17, 0.1870078740157480324 ) ) ;
#34017=CARTESIAN_POINT ( 'NONE',  ( 0.9873396505805591694, -0.1113553986120547346, 0.4379921259842519676 ) ) ;
#34019=CARTESIAN_POINT ( 'NONE',  ( -0.7185039370078746268, 0.06523048226347956391, 1.040846456585385882 ) ) ;
#34020=CARTESIAN_POINT ( 'NONE',  ( 0.7495606340400177148, 0.1264236179284866091, 0.5536417322297008115 ) ) ;
#34021=CARTESIAN_POINT ( 'NONE',  ( 1.002407869896990045, 0.1264236179284866091, 0.06643700782025216411 ) ) ;
#34023=CARTESIAN_POINT ( 'NONE',  ( 1.033464566929133799, 0.000000000000000000, 0.3641732283464567121 ) ) ;
#34024=CARTESIAN_POINT ( 'NONE',  ( 0.8759842519685039353, 0.1574803149606299191, 1.899606299105070839 ) ) ;
#34025=ORIENTED_EDGE ( 'NONE', *, *, #8528, .F. ) ;
#34027=CARTESIAN_POINT ( 'NONE',  ( -0.6971942568897648851, 0.07405724077823318263, 1.067913385773007651 ) ) ;
#34028=CARTESIAN_POINT ( 'NONE',  ( 1.033464566929134687, 0.06523048226347956391, 0.9571850393700783721 ) ) ;
#34029=CARTESIAN_POINT ( 'NONE',  ( 0.7185039370078739607, 0.000000000000000000, 4.498031496062992574 ) ) ;
#34031=DIRECTION ( 'NONE',  ( -1.000000000000000000, 0.000000000000000000, 0.000000000000000000 ) ) ;
#34036=CYLINDRICAL_SURFACE ( 'NONE', #5411, 0.1574803149606299191 ) ;
#34037=CARTESIAN_POINT ( 'NONE',  ( 0.8019270111902717657, -0.1787899950787401604, 0.7185039369541108556 ) ) ;
#34038=CARTESIAN_POINT ( 'NONE',  ( 1.033464566929133799, 0.000000000000000000, 1.269685039370078705 ) ) ;
#34039=CARTESIAN_POINT ( 'NONE',  ( -1.033464566929134687, 0.06523048226347956391, 0.4355314959554649201 ) ) ;
#34043=CARTESIAN_POINT ( 'NONE',  ( 1.033464566929134687, 0.06523048226347956391, 1.104822834538142340 ) ) ;
#34048=CARTESIAN_POINT ( 'NONE',  ( -0.6971942568897648851, 0.07405724077823318263, 1.776574803095843924 ) ) ;
#34049=CARTESIAN_POINT ( 'NONE',  ( 1.054774247047244540, 0.07405724077823318263, 1.722440944828125930 ) ) ;
#34052=CARTESIAN_POINT ( 'NONE',  ( 0.6971942568897626646, -0.07405724077823297447, 0.4429133857730075952 ) ) ;
#34053=CARTESIAN_POINT ( 'NONE',  ( -0.7495606340400177148, -0.1264236179284866091, 1.306594488135212728 ) ) ;
#34054=DIRECTION ( 'NONE',  ( 1.822029033848725028E-16, 0.000000000000000000, 1.000000000000000000 ) ) ;
#34055=CARTESIAN_POINT ( 'NONE',  ( -0.7495606340400177148, 0.1264236179284866091, 1.178641732229700922 ) ) ;
#34056=CARTESIAN_POINT ( 'NONE',  ( -0.8759842519685039353, 0.1787899950787401882, 0.07627952750529173875 ) ) ;
#34058=CARTESIAN_POINT ( 'NONE',  ( -0.6971942568897648851, -0.07405724077823297447, 1.702755905458047003 ) ) ;
#34059=CARTESIAN_POINT ( 'NONE',  ( -1.033464566929134687, 0.06523048226347956391, 1.970964566821606034 ) ) ;
#34060=CARTESIAN_POINT ( 'NONE',  ( -0.8107537697050253289, 0.1574803149606300301, 1.636318897637794700 ) ) ;
#34063=CARTESIAN_POINT ( 'NONE',  ( 0.9412147342319837628, -0.1574803149606297803, 1.016240157372787722 ) ) ;
#34073=EDGE_CURVE ( 'NONE', #38112, #25810, #41610, .T. ) ;
#34080=CARTESIAN_POINT ( 'NONE',  ( -0.7185039370078746268, 0.06523048226347977208, 0.1451771653543309226 ) ) ;
#34081=CARTESIAN_POINT ( 'NONE',  ( 0.8759842519685039353, 0.1787899950787401882, 0.8193897637257637756 ) ) ;
#34084=CARTESIAN_POINT ( 'NONE',  ( 0.8019270111902717657, 0.1787899950787401604, 1.850393700733638624 ) ) ;
#34085=CARTESIAN_POINT ( 'NONE',  ( 0.9873396505805591694, -0.1113553986120547346, 0.1624015748031496231 ) ) ;
#34088=LINE ( 'NONE', #1693, #7091 ) ;
#34090=CARTESIAN_POINT ( 'NONE',  ( 0.8019270111902717657, -0.1787899950787401604, 0.1722440944344256208 ) ) ;
#34092=CARTESIAN_POINT ( 'NONE',  ( -0.6971942568897637749, 2.189545951927499583E-17, 1.774114173174582643 ) ) ;
#34094=AXIS2_PLACEMENT_3D ( 'NONE', #47178, #21780, #14361 ) ;
#34095=CARTESIAN_POINT ( 'NONE',  ( -0.8759842519685039353, 0.1787899950787401882, 1.296751968450173154 ) ) ;
#34096=CARTESIAN_POINT ( 'NONE',  ( -0.8107537697050254399, 0.1574803149606300301, 1.321358267716534751 ) ) ;
#34097=CARTESIAN_POINT ( 'NONE',  ( 0.8759842519685039353, 0.1787899950787401882, 1.296751968450173154 ) ) ;
#34100=CARTESIAN_POINT ( 'NONE',  ( -0.7495606340400177148, 0.1264236179284866091, 0.5142716534895434011 ) ) ;
#34101=CARTESIAN_POINT ( 'NONE',  ( -0.7495606340400177148, 0.1264236179284866091, 1.218011810969858111 ) ) ;
#34102=CYLINDRICAL_SURFACE ( 'NONE', #27609, 0.1574803149606299191 ) ;
#34104=CARTESIAN_POINT ( 'NONE',  ( -0.7646288533564489232, 0.1113553986120547346, 1.353346456585388102 ) ) ;
#34105=CARTESIAN_POINT ( 'NONE',  ( 1.054774247047244096, 0.000000000000000000, 0.5388779527021417826 ) ) ;
#34106=CARTESIAN_POINT ( 'NONE',  ( -0.8759842519685039353, 0.1787899950787401882, 0.3863188975840318173 ) ) ;
#34108=CARTESIAN_POINT ( 'NONE',  ( -1.033464566929134687, 0.06523048226347956391, 1.350885826771654141 ) ) ;
#34109=ORIENTED_EDGE ( 'NONE', *, *, #13674, .F. ) ;
#34110=CARTESIAN_POINT ( 'NONE',  ( -0.9873396505805591694, 0.1113553986120547346, 0.2509842519685039353 ) ) ;
#34111=CARTESIAN_POINT ( 'NONE',  ( 0.6971942568897648851, -0.07405724077823297447, 1.190944881836001112 ) ) ;
#34115=( BOUNDED_CURVE ( )  B_SPLINE_CURVE ( 2, ( #17765, #35981, #10601, #28331, #42902, #10112, #25200, #20647, #17058 ),
 .UNSPECIFIED., .F., .F. ) 
 B_SPLINE_CURVE_WITH_KNOTS ( ( 3, 2, 2, 2, 3 ),
 ( 0.2399999999999999911, 0.2424999999999999933, 0.2449999999999999956, 0.2474999999999999978, 0.2500000000000000000 ),
 .UNSPECIFIED. ) 
 CURVE ( )  GEOMETRIC_REPRESENTATION_ITEM ( )  RATIONAL_B_SPLINE_CURVE ( ( 1.000000000000000000, 0.9238795325112869605, 1.000000000000000000, 0.9238795325112869605, 1.000000000000000000, 0.9238795325112869605, 1.000000000000000000, 0.9238795325112869605, 1.000000000000000000 ) ) 
 REPRESENTATION_ITEM ( '' )  ) ;
#34116=EDGE_CURVE ( 'NONE', #1914, #12042, #445, .T. ) ;
#34118=CARTESIAN_POINT ( 'NONE',  ( -0.8019270111902717657, 0.1787899950787401604, 0.07381889758403178958 ) ) ;
#34121=CARTESIAN_POINT ( 'NONE',  ( 0.7185039370078746268, 0.06523048226347956391, 1.011318897637796033 ) ) ;
#34123=CARTESIAN_POINT ( 'NONE',  ( -1.033464566929133799, 0.000000000000000000, 1.338582677057826853 ) ) ;
#34124=ORIENTED_EDGE ( 'NONE', *, *, #19305, .F. ) ;
#34133=CARTESIAN_POINT ( 'NONE',  ( -1.002407869896990045, -0.1264236179284866091, 0.6126968503399370380 ) ) ;
#34137=CARTESIAN_POINT ( 'NONE',  ( -0.8107537697050254399, -0.1574803149606297803, 1.601870078632630756 ) ) ;
#34138=DIRECTION ( 'NONE',  ( 1.822029033848725028E-16, 0.000000000000000000, 1.000000000000000000 ) ) ;
#34139=CARTESIAN_POINT ( 'NONE',  ( 0.7495606340400177148, -0.1264236179284866091, 1.857775590497417362 ) ) ;
#34140=CARTESIAN_POINT ( 'NONE',  ( 1.054774247047244540, -0.07405724077823318263, 0.2559055117572600624 ) ) ;
#34143=CARTESIAN_POINT ( 'NONE',  ( -0.8107537697050254399, -0.1574803149606297803, 1.444389763672000671 ) ) ;
#34144=CARTESIAN_POINT ( 'NONE',  ( -1.033464566929133799, 0.000000000000000000, 1.584645669291338654 ) ) ;
#34146=CARTESIAN_POINT ( 'NONE',  ( 0.6971942568897626646, -0.07405724077823297447, 0.4773622046706456068 ) ) ;
#34148=CARTESIAN_POINT ( 'NONE',  ( 0.7330336333443192576, -0.08909248707107361720, 0.03937010521645695205 ) ) ;
#34149=CARTESIAN_POINT ( 'NONE',  ( 0.6971942568897648851, 0.07405724077823318263, 1.299212598371434435 ) ) ;
#34153=CARTESIAN_POINT ( 'NONE',  ( -1.054774247047244096, 0.000000000000000000, 1.281988188922614125 ) ) ;
#34154=CARTESIAN_POINT ( 'NONE',  ( 0.7185039370078746268, 0.06523048226347956391, 0.7652559054042838982 ) ) ;
#34155=ORIENTED_EDGE ( 'NONE', *, *, #33136, .T. ) ;
#34156=CARTESIAN_POINT ( 'NONE',  ( -1.033464566929134687, 0.06523048226347956391, 0.1993110235145201248 ) ) ;
#34157=CARTESIAN_POINT ( 'NONE',  ( 0.8488709075541929217, 0.1740638475949229103, 0.03937009123436348290 ) ) ;
#34161=CARTESIAN_POINT ( 'NONE',  ( 0.7495606340400177148, -0.1264236179284866091, 1.621555118056472455 ) ) ;
#34162=CARTESIAN_POINT ( 'NONE',  ( -0.9412147342319837628, 0.1574803149606300301, 1.277066929133857442 ) ) ;
#34164=CARTESIAN_POINT ( 'NONE',  ( -0.8759842519685039353, 0.1574803149606299191, 1.151574803042078710 ) ) ;
#34166=CARTESIAN_POINT ( 'NONE',  ( -0.8107537697050254399, 0.1574803149606300301, 0.7603346455617647770 ) ) ;
#34167=CARTESIAN_POINT ( 'NONE',  ( -0.7646288533564489232, -0.1113553986120547346, 0.4970472439869613734 ) ) ;
#34169=VERTEX_POINT ( 'NONE', #33325 ) ;
#34174=CARTESIAN_POINT ( 'NONE',  ( -1.002407869896990045, 0.1264236179284866091, 1.291830708607653477 ) ) ;
#34176=VERTEX_POINT ( 'NONE', #15100 ) ;
#34178=CARTESIAN_POINT ( 'NONE',  ( -0.8759842519685039353, 0.1574803149606299191, 0.2460629920184571051 ) ) ;
#34179=CARTESIAN_POINT ( 'NONE',  ( -0.6971942568897626646, 0.07405724077823318263, 0.2805118109698587214 ) ) ;
#34180=CARTESIAN_POINT ( 'NONE',  ( 0.9412147342319837628, 0.1574803149606300301, 1.857775590443653480 ) ) ;
#34183=ORIENTED_EDGE ( 'NONE', *, *, #43038, .F. ) ;
#34185=ORIENTED_EDGE ( 'NONE', *, *, #9610, .T. ) ;
#34186=EDGE_CURVE ( 'NONE', #11484, #22073, #151, .T. ) ;
#34188=CARTESIAN_POINT ( 'NONE',  ( -0.8759842519685039353, 0.000000000000000000, 0.000000000000000000 ) ) ;
#34189=EDGE_CURVE ( 'NONE', #11117, #43450, #18962, .T. ) ;
#34190=DIRECTION ( 'NONE',  ( 1.000000000000000000, 0.000000000000000000, -1.822029033848725275E-16 ) ) ;
#34192=CARTESIAN_POINT ( 'NONE',  ( -1.002407869896990045, 0.1264236179284866091, 0.1500984251430867999 ) ) ;
#34193=CARTESIAN_POINT ( 'NONE',  ( -0.8759842519685039353, 0.1574803149606299191, 0.8858267716535432879 ) ) ;
#34196=CARTESIAN_POINT ( 'NONE',  ( 0.7185039370078746268, -0.06523048226347956391, 1.094980314960629419 ) ) ;
#34197=CARTESIAN_POINT ( 'NONE',  ( 0.6971942568897637749, 2.189545951927499583E-17, 0.8735236219934803259 ) ) ;
#34198=CARTESIAN_POINT ( 'NONE',  ( 0.6971942568897648851, -0.07405724077823297447, 1.422244094434425898 ) ) ;
#34199=CARTESIAN_POINT ( 'NONE',  ( -0.8759842519685039353, 0.000000000000000000, 0.000000000000000000 ) ) ;
#34200=CARTESIAN_POINT ( 'NONE',  ( 0.7185039370078746268, -0.06523048226347956391, 1.528051181102361600 ) ) ;
#34201=CARTESIAN_POINT ( 'NONE',  ( 0.7353396263524580867, -0.09417691312399201209, 1.985127456826107251 ) ) ;
#34202=DIRECTION ( 'NONE',  ( 0.000000000000000000, 0.000000000000000000, -1.000000000000000000 ) ) ;
#34203=CYLINDRICAL_SURFACE ( 'NONE', #32038, 0.1574803149606299191 ) ;
#34206=CARTESIAN_POINT ( 'NONE',  ( 0.7495606340400177148, -0.1264236179284866091, 1.031003936954110189 ) ) ;
#34208=CARTESIAN_POINT ( 'NONE',  ( 0.7495606340400177148, -0.1264236179284866091, 1.783956692859621995 ) ) ;
#34210=EDGE_LOOP ( 'NONE', ( #673, #19434, #8921, #40155 ) ) ;
#34211=CARTESIAN_POINT ( 'NONE',  ( -0.8107537697050254399, 0.1574803149606300301, 0.8489173228346468258 ) ) ;
#34214=CARTESIAN_POINT ( 'NONE',  ( -0.7185039370078746268, 0.06523048226347956391, 0.09596456682160688090 ) ) ;
#34216=CARTESIAN_POINT ( 'NONE',  ( 0.8019270111902717657, 0.1787899950787401604, 1.136811023568283119 ) ) ;
#34217=EDGE_CURVE ( 'NONE', #21986, #18116, #10749, .T. ) ;
#34222=CARTESIAN_POINT ( 'NONE',  ( 1.033464566929134687, 0.06523048226347956391, 0.2485236220472441526 ) ) ;
#34223=CARTESIAN_POINT ( 'NONE',  ( -1.054774247047244540, -0.07405724077823318263, 0.2165354330171024577 ) ) ;
#34226=CARTESIAN_POINT ( 'NONE',  ( -0.9500414927467378812, -0.1787899950787401604, 1.825787401521040243 ) ) ;
#34227=CARTESIAN_POINT ( 'NONE',  ( -0.6971942568897648851, 0.07405724077823318263, 0.8661417322297002563 ) ) ;
#34228=CARTESIAN_POINT ( 'NONE',  ( -0.8759842519685039353, 0.1787899950787401882, 0.4699803149068661479 ) ) ;
#34231=CYLINDRICAL_SURFACE ( 'NONE', #23388, 0.1574803149606299191 ) ;
#34235=CARTESIAN_POINT ( 'NONE',  ( 0.8107537697050254399, 0.1574803149606300301, 1.793799212598424342 ) ) ;
#34236=CARTESIAN_POINT ( 'NONE',  ( -0.7185039370078739607, 1.928577636452523993E-17, 0.1476377952755905387 ) ) ;
#34237=CARTESIAN_POINT ( 'NONE',  ( -1.002407869896990045, -0.1264236179284866091, 0.4502952755367874427 ) ) ;
#34238=CARTESIAN_POINT ( 'NONE',  ( 0.7185039370078746268, 0.06523048226347956391, 1.198326771546015967 ) ) ;
#34241=CARTESIAN_POINT ( 'NONE',  ( -0.7495606340400177148, -0.1264236179284866091, 1.468996062938362046 ) ) ;
#34245=LINE ( 'NONE', #41611, #7832 ) ;
#34246=DIRECTION ( 'NONE',  ( 0.000000000000000000, 0.000000000000000000, -1.000000000000000000 ) ) ;
#34247=CARTESIAN_POINT ( 'NONE',  ( -0.7646288533564489232, -0.1113553986120547346, 1.284448818790110192 ) ) ;
#34249=CARTESIAN_POINT ( 'NONE',  ( 0.7185039370078739607, 1.928577636452523993E-17, 1.751968503829480106 ) ) ;
#34250=VERTEX_POINT ( 'NONE', #12928 ) ;
#34252=CARTESIAN_POINT ( 'NONE',  ( 0.7185039370078739607, 1.928577636452523993E-17, 1.131889763779527547 ) ) ;
#34255=CARTESIAN_POINT ( 'NONE',  ( 0.7646288533564489232, -0.1113553986120547346, 0.5757874014672763607 ) ) ;
#34260=ORIENTED_EDGE ( 'NONE', *, *, #26036, .F. ) ;
#34262=CARTESIAN_POINT ( 'NONE',  ( 0.7646288533564489232, -0.1113553986120547346, 0.8612204724409449064 ) ) ;
#34263=EDGE_CURVE ( 'NONE', #12053, #8209, #3988, .T. ) ;
#34266=CARTESIAN_POINT ( 'NONE',  ( -0.8107537697050254399, 0.1574803149606300301, 0.4453740156405042727 ) ) ;
#34270=CARTESIAN_POINT ( 'NONE',  ( 0.8107537697050253289, -0.1574803149606297803, 1.050688976270426567 ) ) ;
#34273=CARTESIAN_POINT ( 'NONE',  ( -0.7495606340400177148, 0.1264236179284866091, 0.4699803149068661479 ) ) ;
#34274=ORIENTED_EDGE ( 'NONE', *, *, #8162, .T. ) ;
#34276=CARTESIAN_POINT ( 'NONE',  ( -0.9500414927467378812, 0.1787899950787401604, 1.687992125930489307 ) ) ;
#34278=EDGE_CURVE ( 'NONE', #44204, #33479, #20328, .T. ) ;
#34279=CARTESIAN_POINT ( 'NONE',  ( 1.002407869896990045, -0.1264236179284866091, 1.833169291284818758 ) ) ;
#34281=CARTESIAN_POINT ( 'NONE',  ( -0.6971942568897626646, -0.07405724077823297447, 0.9153543306548987957 ) ) ;
#34282=CARTESIAN_POINT ( 'NONE',  ( 1.033464566929133799, 0.000000000000000000, 0.5610236220472440971 ) ) ;
#34283=CARTESIAN_POINT ( 'NONE',  ( 1.054774247047244540, 0.07405724077823318263, 0.4232283464029293896 ) ) ;
#34284=CARTESIAN_POINT ( 'NONE',  ( -0.6971942568897648851, 0.07405724077823318263, 1.377952755851748146 ) ) ;
#34287=CARTESIAN_POINT ( 'NONE',  ( -1.054774247047244540, -0.07405724077823318263, 1.397637795221827517 ) ) ;
#34289=CARTESIAN_POINT ( 'NONE',  ( -1.054774247047244540, -0.07405724077823318263, 0.1427165353793072855 ) ) ;
#34290=( BOUNDED_CURVE ( )  B_SPLINE_CURVE ( 2, ( #44601, #34108, #29607, #12289, #18748, #26205, #11349, #33640, #15414 ),
 .UNSPECIFIED., .F., .T. ) 
 B_SPLINE_CURVE_WITH_KNOTS ( ( 3, 2, 2, 2, 3 ),
 ( 0.6800000000000000488, 0.6824999999999999956, 0.6850000000000000533, 0.6875000000000000000, 0.6899999999999999467 ),
 .UNSPECIFIED. ) 
 CURVE ( )  GEOMETRIC_REPRESENTATION_ITEM ( )  RATIONAL_B_SPLINE_CURVE ( ( 1.000000000000000000, 0.9238795325112869605, 1.000000000000000000, 0.9238795325112869605, 1.000000000000000000, 0.9238795325112869605, 1.000000000000000000, 0.9238795325112829637, 1.000000000000000000 ) ) 
 REPRESENTATION_ITEM ( '' )  ) ;
#34292=CARTESIAN_POINT ( 'NONE',  ( -0.7495606340400177148, -0.1264236179284866091, 1.705216535379307174 ) ) ;
#34293=CARTESIAN_POINT ( 'NONE',  ( -0.8759842519685039353, -0.1787899950787401882, 0.09596456687537047170 ) ) ;
#34294=CARTESIAN_POINT ( 'NONE',  ( -0.9873396505805591694, 0.1113553986120547346, 1.825787401574803237 ) ) ;
#34296=CARTESIAN_POINT ( 'NONE',  ( 1.002407869896990045, 0.1264236179284866091, 1.567421259788755794 ) ) ;
#34298=CARTESIAN_POINT ( 'NONE',  ( 0.8759842519685039353, 0.000000000000000000, 0.03937007874015747977 ) ) ;
#34300=ORIENTED_EDGE ( 'NONE', *, *, #20175, .F. ) ;
#34303=AXIS2_PLACEMENT_3D ( 'NONE', #34366, #34851, #1996 ) ;
#34305=CARTESIAN_POINT ( 'NONE',  ( 0.8019270111902717657, 0.1787899950787401604, 1.845472440891119392 ) ) ;
#34309=CARTESIAN_POINT ( 'NONE',  ( 1.054774247047244096, 0.000000000000000000, 0.8489173227808819444 ) ) ;
#34314=CARTESIAN_POINT ( 'NONE',  ( 1.002407869896990045, 0.1264236179284866091, 1.961122047190330786 ) ) ;
#34317=CARTESIAN_POINT ( 'NONE',  ( 1.033464566929133799, 0.000000000000000000, 0.1279527559055118058 ) ) ;
#34321=CARTESIAN_POINT ( 'NONE',  ( -0.9500414927467378812, -0.1787899950787401604, 1.747047244040724312 ) ) ;
#34322=ORIENTED_EDGE ( 'NONE', *, *, #24833, .F. ) ;
#34323=CARTESIAN_POINT ( 'NONE',  ( -0.9500414927467378812, 0.1787899950787401604, 1.373031496009229135 ) ) ;
#34325=CARTESIAN_POINT ( 'NONE',  ( 0.6971942568897637749, 2.189545951927499583E-17, 1.345964566875370139 ) ) ;
#34326=CARTESIAN_POINT ( 'NONE',  ( -0.6971942568897648851, 0.07405724077823318263, 1.141732283410804349 ) ) ;
#34328=ADVANCED_FACE ( 'NONE', ( #9077 ), #5476, .T. ) ;
#34330=DIRECTION ( 'NONE',  ( 1.822029033848725028E-16, 0.000000000000000000, 1.000000000000000000 ) ) ;
#34331=CARTESIAN_POINT ( 'NONE',  ( 0.8759842519685039353, 0.1787899950787401882, 0.5093503936470236138 ) ) ;
#34332=CARTESIAN_POINT ( 'NONE',  ( -0.9500414927467377701, 0.1787899950787401604, 0.3444881889226146243 ) ) ;
#34335=ORIENTED_EDGE ( 'NONE', *, *, #34425, .T. ) ;
#34336=CARTESIAN_POINT ( 'NONE',  ( -0.8107537697050253289, 0.1574803149606300301, 0.3371062992125987146 ) ) ;
#34337=CARTESIAN_POINT ( 'NONE',  ( 0.8019270111902716547, -0.1787899950787401604, 1.235236220418678199 ) ) ;
#34338=CARTESIAN_POINT ( 'NONE',  ( 0.8759842519685039353, 0.1574803149606299191, 1.938976377845228249 ) ) ;
#34339=CARTESIAN_POINT ( 'NONE',  ( -0.7185039370078739607, 1.928577636452523993E-17, 1.958661417322834719 ) ) ;
#34342=CARTESIAN_POINT ( 'NONE',  ( -1.054774247047244096, 0.000000000000000000, 1.011318897584031484 ) ) ;
#34344=CARTESIAN_POINT ( 'NONE',  ( -0.7185039370078739607, 1.928577636452523993E-17, 1.476377952648377789 ) ) ;
#34345=CARTESIAN_POINT ( 'NONE',  ( -0.8019270111902717657, 0.1787899950787401604, 0.03444881884387430981 ) ) ;
#34348=CARTESIAN_POINT ( 'NONE',  ( -0.9873396505805591694, 0.1113553986120547346, 0.1624015746956226358 ) ) ;
#34351=CARTESIAN_POINT ( 'NONE',  ( 0.6971942568897648851, 0.07405724077823318263, 1.338582677111590069 ) ) ;
#34352=CARTESIAN_POINT ( 'NONE',  ( 0.9412147342319837628, 0.1574803149606300301, 1.464074803042079376 ) ) ;
#34354=CARTESIAN_POINT ( 'NONE',  ( 0.6971942568897637749, 2.189545951927499583E-17, 1.616633858213952779 ) ) ;
#34358=CARTESIAN_POINT ( 'NONE',  ( -1.054774247047244540, 0.07405724077823318263, 0.5807086613635594752 ) ) ;
#34362=LINE ( 'NONE', #33670, #13134 ) ;
#34363=CARTESIAN_POINT ( 'NONE',  ( 0.7495606340400177148, 0.1264236179284866091, 1.537893700733637736 ) ) ;
#34364=CARTESIAN_POINT ( 'NONE',  ( 0.7495606340400177148, 0.1264236179284866091, 1.847933070812378009 ) ) ;
#34366=CARTESIAN_POINT ( 'NONE',  ( -0.5314960629921260393, 0.000000000000000000, 4.842519685039370358 ) ) ;
#34371=CARTESIAN_POINT ( 'NONE',  ( 0.7495606340400177148, -0.1264236179284866091, 0.4404527558517480901 ) ) ;
#34373=DIRECTION ( 'NONE',  ( 1.000000000000000000, 0.000000000000000000, -1.822029033848725275E-16 ) ) ;
#34375=CARTESIAN_POINT ( 'NONE',  ( 0.7646288533564489232, 0.1113553986120547346, 0.2214566929133858220 ) ) ;
#34376=CARTESIAN_POINT ( 'NONE',  ( -0.7495606340400177148, 0.1264236179284866091, 1.296751968450173154 ) ) ;
#34377=CARTESIAN_POINT ( 'NONE',  ( 1.033464566929133799, 0.000000000000000000, 0.7874015746956221085 ) ) ;
#34378=ORIENTED_EDGE ( 'NONE', *, *, #41188, .T. ) ;
#34380=CARTESIAN_POINT ( 'NONE',  ( 1.002407869896990045, 0.1264236179284866091, 1.016240157426551161 ) ) ;
#34383=CARTESIAN_POINT ( 'NONE',  ( -0.9873396505805591694, -0.1113553986120547346, 0.5856299211523157133 ) ) ;
#34385=CARTESIAN_POINT ( 'NONE',  ( 0.6971942568897648851, -0.07405724077823297447, 1.697834645615527771 ) ) ;
#34386=CARTESIAN_POINT ( 'NONE',  ( -0.8107537697050253289, -0.1574803149606297803, 1.296751968503936370 ) ) ;
#34387=EDGE_CURVE ( 'NONE', #41647, #35449, #35888, .T. ) ;
#34389=CARTESIAN_POINT ( 'NONE',  ( 0.8075642843603819676, 0.1651804176431314886, 0.03937007863263043694 ) ) ;
#34390=CARTESIAN_POINT ( 'NONE',  ( 0.9873396505805591694, 0.1113553986120547346, 1.343503936900346529 ) ) ;
#34391=ORIENTED_EDGE ( 'NONE', *, *, #28769, .F. ) ;
#34393=( BOUNDED_CURVE ( )  B_SPLINE_CURVE ( 2, ( #7937, #40741, #8165, #8641, #22793, #27134, #37399, #19190, #41684 ),
 .UNSPECIFIED., .F., .T. ) 
 B_SPLINE_CURVE_WITH_KNOTS ( ( 3, 2, 2, 2, 3 ),
 ( 0.7700000000000000178, 0.7724999999999999645, 0.7750000000000000222, 0.7774999999999999689, 0.7800000000000000266 ),
 .UNSPECIFIED. ) 
 CURVE ( )  GEOMETRIC_REPRESENTATION_ITEM ( )  RATIONAL_B_SPLINE_CURVE ( ( 1.000000000000000000, 0.9238795325112899581, 1.000000000000000000, 0.9238795325112869605, 1.000000000000000000, 0.9238795325112869605, 1.000000000000000000, 0.9238795325112869605, 1.000000000000000000 ) ) 
 REPRESENTATION_ITEM ( '' )  ) ;
#34394=ORIENTED_EDGE ( 'NONE', *, *, #5348, .F. ) ;
#34395=CARTESIAN_POINT ( 'NONE',  ( 0.8759842519685039353, -0.1787899950787401882, 0.9621062991588346103 ) ) ;
#34396=CARTESIAN_POINT ( 'NONE',  ( -0.6971942568897648851, 0.07405724077823318263, 1.535433070812378675 ) ) ;
#34398=CARTESIAN_POINT ( 'NONE',  ( -0.8019270111902717657, -0.1787899950787401604, 1.471456692859622217 ) ) ;
#34400=CARTESIAN_POINT ( 'NONE',  ( 0.7185039370078739607, 1.928577636452523993E-17, 0.8858267715460158565 ) ) ;
#34402=ORIENTED_EDGE ( 'NONE', *, *, #47268, .F. ) ;
#34404=VERTEX_POINT ( 'NONE', #42364 ) ;
#34405=ORIENTED_EDGE ( 'NONE', *, *, #14723, .T. ) ;
#34406=CARTESIAN_POINT ( 'NONE',  ( -1.033464566929136907, -0.06523048226347749612, 1.414862204616882835 ) ) ;
#34407=VECTOR ( 'NONE', #3306, 39.37007874015748143 ) ;
#34408=EDGE_CURVE ( 'NONE', #1638, #10984, #31610, .T. ) ;
#34409=CARTESIAN_POINT ( 'NONE',  ( 0.9412147342319837628, -0.1574803149606297803, 0.1107283463491657988 ) ) ;
#34412=CARTESIAN_POINT ( 'NONE',  ( -0.7495606340400177148, 0.1264236179284866091, 0.1599409448281264023 ) ) ;
#34413=CARTESIAN_POINT ( 'NONE',  ( -0.7646288533564489232, 0.1113553986120547346, 1.087598425196850460 ) ) ;
#34416=CARTESIAN_POINT ( 'NONE',  ( -1.033464566929133799, 0.000000000000000000, 1.929133858160188897 ) ) ;
#34417=CARTESIAN_POINT ( 'NONE',  ( 1.002407869896990045, -0.1264236179284866091, 0.9276574802611967652 ) ) ;
#34419=CARTESIAN_POINT ( 'NONE',  ( 0.9873396505805591694, -0.1113553986120547346, 1.579724409448818978 ) ) ;
#34420=CARTESIAN_POINT ( 'NONE',  ( 0.9412147342319837628, -0.1574803149606297803, 1.419783464566930054 ) ) ;
#34421=LINE ( 'NONE', #1567, #33879 ) ;
#34422=CYLINDRICAL_SURFACE ( 'NONE', #43505, 0.1574803149606299191 ) ;
#34425=EDGE_CURVE ( 'NONE', #13566, #14779, #10904, .T. ) ;
#34426=CARTESIAN_POINT ( 'NONE',  ( 0.9500414927467377701, -0.1787899950787401604, 0.9202755904974182499 ) ) ;
#34427=CARTESIAN_POINT ( 'NONE',  ( 0.7495606340400177148, -0.1264236179284866091, 1.862696850339937038 ) ) ;
#34428=CARTESIAN_POINT ( 'NONE',  ( 0.9873396505805591694, -0.1113553986120547346, 0.3494094487113705294 ) ) ;
#34430=CARTESIAN_POINT ( 'NONE',  ( 0.7185039370078766252, -0.06523048226348168721, 1.242618110128693276 ) ) ;
#34432=CARTESIAN_POINT ( 'NONE',  ( -1.033464566929133799, 0.000000000000000000, 0.2362204723334177248 ) ) ;
#34434=CARTESIAN_POINT ( 'NONE',  ( 0.9500414927467378812, -0.1787899950787401604, 1.195866141678520345 ) ) ;
#34435=EDGE_CURVE ( 'NONE', #19285, #34008, #30364, .T. ) ;
#34439=CARTESIAN_POINT ( 'NONE',  ( 1.033464566929133799, 1.928577636452524610E-17, 4.498031496062992574 ) ) ;
#34440=CARTESIAN_POINT ( 'NONE',  ( -0.6971942568897626646, -0.07405724077823297447, 0.5954724408911187261 ) ) ;
#34441=DIRECTION ( 'NONE',  ( 0.000000000000000000, 1.000000000000000000, 0.000000000000000000 ) ) ;
#34443=CARTESIAN_POINT ( 'NONE',  ( -1.002407869896990045, -0.1264236179284866091, 1.828248031442299082 ) ) ;
#34445=CARTESIAN_POINT ( 'NONE',  ( -0.6971942568897637749, 2.189545951927499583E-17, 0.9867125983714331028 ) ) ;
#34446=CARTESIAN_POINT ( 'NONE',  ( -0.6971942568897626646, 0.07405724077823318263, 0.5954724408911187261 ) ) ;
#34447=VERTEX_POINT ( 'NONE', #27800 ) ;
#34453=CARTESIAN_POINT ( 'NONE',  ( 0.8759842519685039353, 0.000000000000000000, 4.498031496062992574 ) ) ;
#34455=CARTESIAN_POINT ( 'NONE',  ( -0.8019270111902717657, 0.1787899950787401604, 0.4281496062454490659 ) ) ;
#34460=CARTESIAN_POINT ( 'NONE',  ( -1.002407869896990045, -0.1264236179284866091, 1.478838582623401399 ) ) ;
#34464=CARTESIAN_POINT ( 'NONE',  ( 1.033464566929133799, 0.000000000000000000, 1.023622047136567126 ) ) ;
#34466=CARTESIAN_POINT ( 'NONE',  ( 0.7185039370078746268, 0.06523048226347956391, 0.4601377952755902889 ) ) ;
#34469=CARTESIAN_POINT ( 'NONE',  ( -0.8107537697050253289, -0.1574803149606297803, 1.208169291231056430 ) ) ;
#34471=CARTESIAN_POINT ( 'NONE',  ( 1.054774247047244540, 0.07405724077823318263, 0.5807086613635594752 ) ) ;
#34473=CARTESIAN_POINT ( 'NONE',  ( -1.033464566929133799, 0.000000000000000000, 1.181102362097196989 ) ) ;
#34474=ORIENTED_EDGE ( 'NONE', *, *, #15044, .F. ) ;
#34476=CARTESIAN_POINT ( 'NONE',  ( -1.054774247047244096, 0.000000000000000000, 1.129429133804503937 ) ) ;
#34477=CARTESIAN_POINT ( 'NONE',  ( 0.7646288533564489232, -0.1113553986120547346, 1.176181102362204633 ) ) ;
#34482=CARTESIAN_POINT ( 'NONE',  ( -1.033464566929134687, -0.06523048226347956391, 1.267224409448818978 ) ) ;
#34486=CARTESIAN_POINT ( 'NONE',  ( -1.054774247047244540, 0.07405724077823318263, 1.053149606245450176 ) ) ;
#34487=CARTESIAN_POINT ( 'NONE',  ( -0.7646288533564489232, 0.1113553986120547346, 1.126968503937007871 ) ) ;
#34490=CARTESIAN_POINT ( 'NONE',  ( -1.033464566929133799, 0.000000000000000000, 1.771653543199558811 ) ) ;
#34494=CARTESIAN_POINT ( 'NONE',  ( 1.033464566929133799, 0.000000000000000000, 1.062992125876724314 ) ) ;
#34499=CARTESIAN_POINT ( 'NONE',  ( -1.054774247047244540, 0.07405724077823318263, 1.761811023568284007 ) ) ;
#34500=CARTESIAN_POINT ( 'NONE',  ( 0.8019270111902717657, -0.1787899950787401604, 1.786417322780882388 ) ) ;
#34501=ORIENTED_EDGE ( 'NONE', *, *, #45091, .F. ) ;
#34502=CARTESIAN_POINT ( 'NONE',  ( 0.7185039370078739607, 1.928577636452523993E-17, 0.5413385826771653919 ) ) ;
#34503=CARTESIAN_POINT ( 'NONE',  ( 0.7495606340400177148, -0.1264236179284866091, 0.4060039369541102450 ) ) ;
#34505=CARTESIAN_POINT ( 'NONE',  ( -1.054774247047244540, -0.07405724077823318263, 1.318897637741511364 ) ) ;
#34508=CARTESIAN_POINT ( 'NONE',  ( -0.8019270111902717657, -0.1787899950787401604, 0.09350393695411057804 ) ) ;
#34509=LINE ( 'NONE', #23496, #2294 ) ;
#34510=CARTESIAN_POINT ( 'NONE',  ( -0.6971942568897648851, -0.07405724077823297447, 1.781496062938362934 ) ) ;
#34511=CARTESIAN_POINT ( 'NONE',  ( -0.8107537697050253289, 0.1574803149606300301, 1.980807086506644943 ) ) ;
#34512=CARTESIAN_POINT ( 'NONE',  ( 0.9873396505805591694, -0.1113553986120547346, 1.412401574695621997 ) ) ;
#34513=CARTESIAN_POINT ( 'NONE',  ( -0.7185039370078746268, -0.06523048226347956391, 1.764271653543307838 ) ) ;
#34514=DIRECTION ( 'NONE',  ( -1.000000000000000000, 0.000000000000000000, 0.000000000000000000 ) ) ;
#34516=CARTESIAN_POINT ( 'NONE',  ( 1.033464566929134687, -0.06523048226347956391, 1.021161417215306955 ) ) ;
#34517=CARTESIAN_POINT ( 'NONE',  ( -1.033464566929134687, 0.06523048226347956391, 1.783956692913386544 ) ) ;
#34521=EDGE_CURVE ( 'NONE', #23610, #8711, #5534, .T. ) ;
#34524=CARTESIAN_POINT ( 'NONE',  ( -0.8107537697050254399, -0.1574803149606297803, 0.5880905511811019837 ) ) ;
#34525=CARTESIAN_POINT ( 'NONE',  ( 0.8019270111902717657, -0.1787899950787401604, 0.4035433070328508509 ) ) ;
#34527=CARTESIAN_POINT ( 'NONE',  ( -0.7185039370078746268, -0.06523048226347956391, 0.8489173227271192834 ) ) ;
#34528=ADVANCED_FACE ( 'NONE', ( #39417 ), #39648, .T. ) ;
#34531=CARTESIAN_POINT ( 'NONE',  ( 1.002407869896990045, -0.1264236179284866091, 0.9227362204186770889 ) ) ;
#34533=CARTESIAN_POINT ( 'NONE',  ( 0.8107537697050254399, 0.1574803149606300301, 0.6126968503937006982 ) ) ;
#34535=CARTESIAN_POINT ( 'NONE',  ( 1.054774247047244540, -0.07405724077823318263, 1.993110236166711013 ) ) ;
#34537=ORIENTED_EDGE ( 'NONE', *, *, #34186, .T. ) ;
#34538=CARTESIAN_POINT ( 'NONE',  ( 0.7185039370078746268, 0.06523048226347956391, 0.2239173228346459099 ) ) ;
#34541=DIRECTION ( 'NONE',  ( 0.000000000000000000, 0.000000000000000000, -1.000000000000000000 ) ) ;
#34543=( BOUNDED_CURVE ( )  B_SPLINE_CURVE ( 2, ( #34015, #19836, #27061, #1615, #34717, #23211, #45217, #22966, #901 ),
 .UNSPECIFIED., .F., .T. ) 
 B_SPLINE_CURVE_WITH_KNOTS ( ( 3, 2, 2, 2, 3 ),
 ( 0.08999999999999999667, 0.09249999999999999889, 0.09500000000000000111, 0.09750000000000000333, 0.1000000000000000056 ),
 .UNSPECIFIED. ) 
 CURVE ( )  GEOMETRIC_REPRESENTATION_ITEM ( )  RATIONAL_B_SPLINE_CURVE ( ( 1.000000000000000000, 0.9238795325112869605, 1.000000000000000000, 0.9238795325112869605, 1.000000000000000000, 0.9238795325112869605, 1.000000000000000000, 0.9238795325112869605, 1.000000000000000000 ) ) 
 REPRESENTATION_ITEM ( '' )  ) ;
#34544=CARTESIAN_POINT ( 'NONE',  ( -1.054774247047244540, -0.07405724077823318263, 1.712598425143087688 ) ) ;
#34546=CARTESIAN_POINT ( 'NONE',  ( -0.8019270111902717657, 0.1787899950787401604, 1.299212598371432215 ) ) ;
#34548=CARTESIAN_POINT ( 'NONE',  ( 0.6971942568897648851, -0.07405724077823297447, 1.427165354276944687 ) ) ;
#34549=CARTESIAN_POINT ( 'NONE',  ( -1.054774247047244540, 0.07405724077823318263, 0.5019685038832442103 ) ) ;
#34550=CARTESIAN_POINT ( 'NONE',  ( 0.8759842519685039353, 0.1787899950787401882, 0.07627952750529173875 ) ) ;
#34551=CARTESIAN_POINT ( 'NONE',  ( -0.8019270111902717657, -0.1787899950787401604, 1.230314960576156746 ) ) ;
#34553=CARTESIAN_POINT ( 'NONE',  ( -0.9873396505805591694, 0.1113553986120547346, 1.343503936900346529 ) ) ;
#34554=CARTESIAN_POINT ( 'NONE',  ( 0.7495606340400177148, 0.1264236179284866091, 0.5930118109698583329 ) ) ;
#34555=CARTESIAN_POINT ( 'NONE',  ( -1.054774247047244096, 0.000000000000000000, 0.4552165353793071745 ) ) ;
#34556=CARTESIAN_POINT ( 'NONE',  ( -0.6971942568897637749, 2.189545951927499583E-17, 0.8292322834108031282 ) ) ;
#34562=CARTESIAN_POINT ( 'NONE',  ( -0.9412147342319837628, 0.1574803149606300301, 0.3321850393700786497 ) ) ;
#34563=CARTESIAN_POINT ( 'NONE',  ( 1.054774247047244540, -0.07405724077823318263, 1.166338582623402731 ) ) ;
#34568=CARTESIAN_POINT ( 'NONE',  ( -0.8759842519685039353, -0.1787899950787401882, 0.9621062991588346103 ) ) ;
#34569=CARTESIAN_POINT ( 'NONE',  ( -0.7495606340400177148, 0.1264236179284866091, 0.1943897637257641919 ) ) ;
#34575=CARTESIAN_POINT ( 'NONE',  ( 0.8019270111902717657, -0.1787899950787401604, 1.348425196796630976 ) ) ;
#34576=EDGE_CURVE ( 'NONE', #32303, #21217, #23888, .T. ) ;
#34578=CARTESIAN_POINT ( 'NONE',  ( 0.7185039370078739607, 1.928577636452523993E-17, 1.919291338582677309 ) ) ;
#34581=DIRECTION ( 'NONE',  ( 1.822029033848725028E-16, 0.000000000000000000, 1.000000000000000000 ) ) ;
#34582=CARTESIAN_POINT ( 'NONE',  ( 0.7495606340400177148, 0.1264236179284866091, 1.572342519631275692 ) ) ;
#34583=ADVANCED_FACE ( 'NONE', ( #17156 ), #2991, .T. ) ;
#34588=EDGE_CURVE ( 'NONE', #19760, #22180, #39802, .T. ) ;
#34591=CARTESIAN_POINT ( 'NONE',  ( -1.002407869896990045, -0.1264236179284866091, 0.7308070865604093802 ) ) ;
#34595=CARTESIAN_POINT ( 'NONE',  ( -0.7765702477540072923, -0.1393169151461616795, 1.986236931248386517 ) ) ;
#34600=CARTESIAN_POINT ( 'NONE',  ( 0.8019270111902717657, 0.1787899950787401604, 1.574803149552536530 ) ) ;
#34601=CARTESIAN_POINT ( 'NONE',  ( 0.6971942568897648851, 0.07405724077823318263, 1.850393700733638624 ) ) ;
#34602=CARTESIAN_POINT ( 'NONE',  ( 1.002407869896990045, 0.1264236179284866091, 0.4601377952218267953 ) ) ;
#34606=CARTESIAN_POINT ( 'NONE',  ( -0.8759842519685039353, 0.000000000000000000, 1.995570866087968520 ) ) ;
#34609=CARTESIAN_POINT ( 'NONE',  ( 0.7185039370078732945, -0.06523048226347899492, 0.4945866140657012577 ) ) ;
#34610=CARTESIAN_POINT ( 'NONE',  ( 0.8759842519685039353, -0.1787899950787401882, 0.4453740156942677664 ) ) ;
#34611=CARTESIAN_POINT ( 'NONE',  ( 0.7598281768898816901, -0.1184571006790323261, 0.03937028442103207571 ) ) ;
#34613=LINE ( 'NONE', #16167, #8784 ) ;
#34614=CARTESIAN_POINT ( 'NONE',  ( -0.9500414927467378812, 0.1787899950787401604, 1.368110236166710125 ) ) ;
#34615=CARTESIAN_POINT ( 'NONE',  ( 0.8107537697050253289, -0.1574803149606297803, 0.8144685038294804391 ) ) ;
#34617=CARTESIAN_POINT ( 'NONE',  ( 0.6971942568897648851, 0.07405724077823318263, 1.067913385773007651 ) ) ;
#34620=CARTESIAN_POINT ( 'NONE',  ( -0.9412147342319837628, 0.1574803149606300301, 0.5979330707586145710 ) ) ;
#34622=CARTESIAN_POINT ( 'NONE',  ( 0.8759842519685039353, -0.1787899950787401882, 1.744586614119464807 ) ) ;
#34623=CARTESIAN_POINT ( 'NONE',  ( -0.9412147342319837628, -0.1574803149606297803, 1.262303149606299746 ) ) ;
#34627=CARTESIAN_POINT ( 'NONE',  ( 0.7495606340400177148, -0.1264236179284866091, 0.09104330703285078152 ) ) ;
#34628=CARTESIAN_POINT ( 'NONE',  ( 0.7646288533564489232, 0.1113553986120547346, 1.353346456585388102 ) ) ;
#34633=CARTESIAN_POINT ( 'NONE',  ( -0.6971942568897637749, 2.189545951927499583E-17, 1.616633858213952779 ) ) ;
#34635=ORIENTED_EDGE ( 'NONE', *, *, #31259, .F. ) ;
#34647=CARTESIAN_POINT ( 'NONE',  ( -0.8107537697050254399, -0.1574803149606297803, 1.208169291231056430 ) ) ;
#34650=CARTESIAN_POINT ( 'NONE',  ( 0.7185039370078746268, -0.06523048226347956391, 1.882381889763779181 ) ) ;
#34653=CARTESIAN_POINT ( 'NONE',  ( -1.054774247047244540, -0.07405724077823318263, 0.2214566928596221063 ) ) ;
#34654=CARTESIAN_POINT ( 'NONE',  ( -0.7646288533564489232, -0.1113553986120547346, 1.097440944881889813 ) ) ;
#34656=CARTESIAN_POINT ( 'NONE',  ( 0.9412147342319837628, -0.1574803149606297803, 1.104822834645669882 ) ) ;
#34658=CARTESIAN_POINT ( 'NONE',  ( 0.7495606340400177148, -0.1264236179284866091, 1.075295275536787276 ) ) ;
#34659=CARTESIAN_POINT ( 'NONE',  ( 0.8019270111902716547, -0.1787899950787401604, 1.387795275536786610 ) ) ;
#34660=CARTESIAN_POINT ( 'NONE',  ( 1.002407869896990045, 0.1264236179284866091, 0.1451771653005673179 ) ) ;
#34662=CARTESIAN_POINT ( 'NONE',  ( 0.8759842519685039353, 0.1574803149606299191, 1.594488188976378007 ) ) ;
#34665=CARTESIAN_POINT ( 'NONE',  ( -0.8759842519685039353, 0.000000000000000000, 0.000000000000000000 ) ) ;
#34666=( BOUNDED_CURVE ( )  B_SPLINE_CURVE ( 2, ( #45136, #42260, #19985, #20462, #24077, #16181, #12353, #38443, #8973 ),
 .UNSPECIFIED., .F., .T. ) 
 B_SPLINE_CURVE_WITH_KNOTS ( ( 3, 2, 2, 2, 3 ),
 ( 0.3599999999999999867, 0.3624999999999999889, 0.3649999999999999911, 0.3674999999999999933, 0.3699999999999999956 ),
 .UNSPECIFIED. ) 
 CURVE ( )  GEOMETRIC_REPRESENTATION_ITEM ( )  RATIONAL_B_SPLINE_CURVE ( ( 1.000000000000000000, 0.9238795325112869605, 1.000000000000000000, 0.9238795325112869605, 1.000000000000000000, 0.9238795325112869605, 1.000000000000000000, 0.9238795325112869605, 1.000000000000000000 ) ) 
 REPRESENTATION_ITEM ( '' )  ) ;
#34668=CARTESIAN_POINT ( 'NONE',  ( -0.7185039370078746268, 0.06523048226347956391, 1.562500000000000000 ) ) ;
#34669=CARTESIAN_POINT ( 'NONE',  ( 1.054774247047244540, 0.07405724077823318263, 0.9301181101824563813 ) ) ;
#34670=CARTESIAN_POINT ( 'NONE',  ( 0.6971942568897648851, 0.07405724077823318263, 1.855314960576157635 ) ) ;
#34671=CARTESIAN_POINT ( 'NONE',  ( 0.8759842519685039353, 0.1574803149606299191, 0.3641732282389295583 ) ) ;
#34676=CARTESIAN_POINT ( 'NONE',  ( -0.7185039370078746268, 0.06523048226347956391, 0.2140748030420794590 ) ) ;
#34678=CARTESIAN_POINT ( 'NONE',  ( 1.054774247047244540, 0.07405724077823318263, 1.323818897584032817 ) ) ;
#34682=EDGE_CURVE ( 'NONE', #34404, #13881, #10458, .T. ) ;
#34684=CARTESIAN_POINT ( 'NONE',  ( -0.7495606340400177148, -0.1264236179284866091, 0.5191929133320630774 ) ) ;
#34685=CARTESIAN_POINT ( 'NONE',  ( 0.8107537697050254399, 0.1574803149606300301, 0.2583661417322834497 ) ) ;
#34688=ORIENTED_EDGE ( 'NONE', *, *, #19997, .T. ) ;
#34691=CARTESIAN_POINT ( 'NONE',  ( -1.002407869896990045, 0.1264236179284866091, 1.055610236166708793 ) ) ;
#34692=CARTESIAN_POINT ( 'NONE',  ( -0.8759842519685039353, -0.1787899950787401882, 1.862696850339937038 ) ) ;
#34693=CARTESIAN_POINT ( 'NONE',  ( -0.9500414927467377701, -0.1787899950787401604, 0.9990157479777320715 ) ) ;
#34694=CARTESIAN_POINT ( 'NONE',  ( -1.054774247047244540, 0.07405724077823318263, 0.7381889763241898939 ) ) ;
#34695=( BOUNDED_CURVE ( )  B_SPLINE_CURVE ( 2, ( #23100, #16622, #20198, #41504, #45829, #8954, #42237, #8710, #27199 ),
 .UNSPECIFIED., .F., .F. ) 
 B_SPLINE_CURVE_WITH_KNOTS ( ( 3, 2, 2, 2, 3 ),
 ( 0.05000000000000000278, 0.05249999999999999806, 0.05500000000000000028, 0.05750000000000000250, 0.05999999999999999778 ),
 .UNSPECIFIED. ) 
 CURVE ( )  GEOMETRIC_REPRESENTATION_ITEM ( )  RATIONAL_B_SPLINE_CURVE ( ( 1.000000000000000000, 0.9238795325112859613, 1.000000000000000000, 0.9238795325112869605, 1.000000000000000000, 0.9238795325112869605, 1.000000000000000000, 0.9238795325112869605, 1.000000000000000000 ) ) 
 REPRESENTATION_ITEM ( '' )  ) ;
#34698=CARTESIAN_POINT ( 'NONE',  ( 0.7185039370078746268, -0.06523048226347956391, 1.803641732283465471 ) ) ;
#34706=CARTESIAN_POINT ( 'NONE',  ( -1.054774247047244540, -0.07405724077823318263, 0.5314960629383620461 ) ) ;
#34707=CARTESIAN_POINT ( 'NONE',  ( -0.7185039370078739607, 0.000000000000000000, -2.869337061179095023E-17 ) ) ;
#34708=CIRCLE ( 'NONE', #36977, 0.1787899950787401049 ) ;
#34711=CARTESIAN_POINT ( 'NONE',  ( -0.7495606340400177148, 0.1264236179284866091, 1.498523621993480326 ) ) ;
#34716=DIRECTION ( 'NONE',  ( 0.000000000000000000, 0.000000000000000000, -1.000000000000000000 ) ) ;
#34717=CARTESIAN_POINT ( 'NONE',  ( 0.8759842519685039353, -0.1574803149606299191, 0.1968503937007874127 ) ) ;
#34719=CARTESIAN_POINT ( 'NONE',  ( 0.9873396505805591694, -0.1113553986120547346, 0.5561023622047244208 ) ) ;
#34722=CARTESIAN_POINT ( 'NONE',  ( -0.7185039370078746268, -0.06523048226347956391, 1.242618110128693276 ) ) ;
#34723=CARTESIAN_POINT ( 'NONE',  ( 1.054774247047244540, -0.07405724077823318263, 0.6545275590013545086 ) ) ;
#34726=CARTESIAN_POINT ( 'NONE',  ( 0.7646288533564489232, -0.1113553986120547346, 0.3494094488188976277 ) ) ;
#34730=CARTESIAN_POINT ( 'NONE',  ( -1.054774247047244540, -0.07405724077823318263, 1.126968503883244654 ) ) ;
#34731=CARTESIAN_POINT ( 'NONE',  ( 0.7646288533564489232, 0.1113553986120547346, 1.087598425196850460 ) ) ;
#34734=CARTESIAN_POINT ( 'NONE',  ( -1.033464566929134687, 0.06523048226347956391, 0.7111220471365682361 ) ) ;
#34735=CARTESIAN_POINT ( 'NONE',  ( 1.033464566929134687, 0.06523048226347956391, 0.1697834645669291653 ) ) ;
#34736=CARTESIAN_POINT ( 'NONE',  ( -0.7646288533564489232, -0.1113553986120547346, 1.953740157372787500 ) ) ;
#34737=DIRECTION ( 'NONE',  ( 0.000000000000000000, 0.000000000000000000, -1.000000000000000000 ) ) ;
#34740=ORIENTED_EDGE ( 'NONE', *, *, #7573, .T. ) ;
#34741=CARTESIAN_POINT ( 'NONE',  ( 1.033464566929133799, 0.000000000000000000, 0.2854330708661417804 ) ) ;
#34742=CARTESIAN_POINT ( 'NONE',  ( 0.6971942568897626646, -0.07405724077823297447, 0.7529527558517473684 ) ) ;
#34744=CYLINDRICAL_SURFACE ( 'NONE', #7354, 0.1574803149606299191 ) ;
#34745=DIRECTION ( 'NONE',  ( 1.822029033848725028E-16, 0.000000000000000000, 1.000000000000000000 ) ) ;
#34749=CARTESIAN_POINT ( 'NONE',  ( -0.7185039370078739607, 1.928577636452523993E-17, 1.407480314960629864 ) ) ;
#34752=CARTESIAN_POINT ( 'NONE',  ( -0.9500414927467378812, 0.1787899950787401604, 1.884842519631275026 ) ) ;
#34753=VERTEX_POINT ( 'NONE', #21940 ) ;
#34757=CARTESIAN_POINT ( 'NONE',  ( 1.054774247047244540, 0.07405724077823318263, 0.5019685038832442103 ) ) ;
#34758=CARTESIAN_POINT ( 'NONE',  ( -1.002407869896990045, 0.1264236179284866091, 1.405019684985606476 ) ) ;
#34760=CARTESIAN_POINT ( 'NONE',  ( -0.8759842519685039353, -0.1787899950787401882, 0.1747047243556852092 ) ) ;
#34761=CARTESIAN_POINT ( 'NONE',  ( -0.8759842519685039353, 0.1574803149606299191, 0.5708661417322835607 ) ) ;
#34762=CARTESIAN_POINT ( 'NONE',  ( -0.6971942568897648851, 0.07405724077823318263, 1.737204724355685848 ) ) ;
#34763=CARTESIAN_POINT ( 'NONE',  ( -1.054774247047244540, 0.07405724077823318263, 0.1082677164816695514 ) ) ;
#34765=CARTESIAN_POINT ( 'NONE',  ( -0.7185039370078739607, 1.928577636452523993E-17, 1.801181102362204633 ) ) ;
#34767=EDGE_CURVE ( 'NONE', #20854, #46310, #30081, .T. ) ;
#34768=CARTESIAN_POINT ( 'NONE',  ( 0.7495606340400177148, -0.1264236179284866091, 1.744586614119464807 ) ) ;
#34771=EDGE_CURVE ( 'NONE', #28431, #46488, #898, .T. ) ;
#34775=ORIENTED_EDGE ( 'NONE', *, *, #20169, .F. ) ;
#34779=EDGE_CURVE ( 'NONE', #10690, #24840, #5821, .T. ) ;
#34782=CARTESIAN_POINT ( 'NONE',  ( -1.033464566929134687, -0.06523048226347956391, 0.7455708660342049710 ) ) ;
#34785=CARTESIAN_POINT ( 'NONE',  ( 0.8759842519685039353, -0.1787899950787401882, 0.9178149605761574126 ) ) ;
#34788=CARTESIAN_POINT ( 'NONE',  ( 0.6971942568897637749, 2.189545951927499583E-17, 1.975885826717889815 ) ) ;
#34790=CARTESIAN_POINT ( 'NONE',  ( 0.7646288533564489232, -0.1113553986120547346, 0.3789370077664886427 ) ) ;
#34794=CARTESIAN_POINT ( 'NONE',  ( 0.7495606340400177148, 0.1264236179284866091, 0.3567913385289137596 ) ) ;
#34796=CARTESIAN_POINT ( 'NONE',  ( -0.7495606340400177148, 0.1264236179284866091, 1.926673228292693052 ) ) ;
#34798=CARTESIAN_POINT ( 'NONE',  ( -0.8759842519685039353, -0.1787899950787401882, 1.513287401521039355 ) ) ;
#34799=DIRECTION ( 'NONE',  ( -1.000000000000000000, 0.000000000000000000, 0.000000000000000000 ) ) ;
#34800=CARTESIAN_POINT ( 'NONE',  ( 0.8019270111902717657, -0.1787899950787401604, 1.471456692859622217 ) ) ;
#34802=CARTESIAN_POINT ( 'NONE',  ( -0.9500414927467378812, -0.1787899950787401604, 0.5314960629383620461 ) ) ;
#34803=CARTESIAN_POINT ( 'NONE',  ( 1.054774247047244096, 0.000000000000000000, 0.1058070865604096300 ) ) ;
#34804=CARTESIAN_POINT ( 'NONE',  ( -0.8019270111902717657, 0.1787899950787401604, 1.254921259788757348 ) ) ;
#34805=ADVANCED_FACE ( 'NONE', ( #7076 ), #21702, .T. ) ;
#34808=CARTESIAN_POINT ( 'NONE',  ( 0.6971942568897637749, 2.189545951927499583E-17, 0.6766732282926929409 ) ) ;
#34809=CARTESIAN_POINT ( 'NONE',  ( -0.8759842519685039353, -0.1787899950787401882, 0.5241141731745827537 ) ) ;
#34813=AXIS2_PLACEMENT_3D ( 'NONE', #28465, #24610, #14312 ) ;
#34814=CARTESIAN_POINT ( 'NONE',  ( -0.8759842519685039353, -0.1574803149606299191, 0.3149606299212598381 ) ) ;
#34815=EDGE_CURVE ( 'NONE', #29787, #11192, #40093, .T. ) ;
#34816=CARTESIAN_POINT ( 'NONE',  ( 0.7495606340400177148, -0.1264236179284866091, 1.272145669237574772 ) ) ;
#34822=CARTESIAN_POINT ( 'NONE',  ( -0.7495606340400177148, -0.1264236179284866091, 0.9965551180564724554 ) ) ;
#34823=CARTESIAN_POINT ( 'NONE',  ( -0.9500414927467378812, -0.1787899950787401604, 0.2116141731745827814 ) ) ;
#34824=ORIENTED_EDGE ( 'NONE', *, *, #45495, .T. ) ;
#34827=ORIENTED_EDGE ( 'NONE', *, *, #17045, .F. ) ;
#34828=CARTESIAN_POINT ( 'NONE',  ( 1.054774247047244540, 0.07405724077823318263, 1.363188976324188895 ) ) ;
#34832=CARTESIAN_POINT ( 'NONE',  ( 1.054774247047244096, 0.000000000000000000, 1.636318897584031484 ) ) ;
#34836=CARTESIAN_POINT ( 'NONE',  ( -0.9873396505805591694, 0.1113553986120547346, 1.737204724301921299 ) ) ;
#34837=CARTESIAN_POINT ( 'NONE',  ( 1.054774247047244540, -0.07405724077823318263, 0.4921259841982048577 ) ) ;
#34838=( BOUNDED_CURVE ( )  B_SPLINE_CURVE ( 2, ( #13001, #42198, #46274, #24019, #46035, #38621, #5798, #20404, #35044 ),
 .UNSPECIFIED., .F., .T. ) 
 B_SPLINE_CURVE_WITH_KNOTS ( ( 3, 2, 2, 2, 3 ),
 ( 0.9100000000000000311, 0.9124999999999999778, 0.9150000000000000355, 0.9174999999999999822, 0.9200000000000000400 ),
 .UNSPECIFIED. ) 
 CURVE ( )  GEOMETRIC_REPRESENTATION_ITEM ( )  RATIONAL_B_SPLINE_CURVE ( ( 1.000000000000000000, 0.9238795325112899581, 1.000000000000000000, 0.9238795325112869605, 1.000000000000000000, 0.9238795325112869605, 1.000000000000000000, 0.9238795325112869605, 1.000000000000000000 ) ) 
 REPRESENTATION_ITEM ( '' )  ) ;
#34839=CARTESIAN_POINT ( 'NONE',  ( -1.054774247047244096, 0.000000000000000000, 0.8538385826234016207 ) ) ;
#34841=CARTESIAN_POINT ( 'NONE',  ( 0.7185039370078746268, 0.06523048226347956391, 0.09596456682160686702 ) ) ;
#34844=CARTESIAN_POINT ( 'NONE',  ( 0.8759842519685039353, -0.1787899950787401882, 1.473917322780881722 ) ) ;
#34845=CARTESIAN_POINT ( 'NONE',  ( 1.054774247047244540, -0.07405724077823318263, 1.909448818843873186 ) ) ;
#34846=CARTESIAN_POINT ( 'NONE',  ( 1.002407869896990045, -0.1264236179284866091, 0.3321850393163153226 ) ) ;
#34848=MECHANICAL_DESIGN_GEOMETRIC_PRESENTATION_REPRESENTATION('',(#25641),#4953);
#34850=CARTESIAN_POINT ( 'NONE',  ( -1.033464566929133799, 0.000000000000000000, 1.023622047136567126 ) ) ;
#34851=DIRECTION ( 'NONE',  ( 1.000000000000000000, 0.000000000000000000, 0.000000000000000000 ) ) ;
#34855=CARTESIAN_POINT ( 'NONE',  ( 0.8759842519685039353, -0.1787899950787401882, 0.5241141731745827537 ) ) ;
#34858=CARTESIAN_POINT ( 'NONE',  ( -0.8759842519685039353, -0.1787899950787401882, 1.508366141678519678 ) ) ;
#34859=CARTESIAN_POINT ( 'NONE',  ( 0.8759842519685039353, -0.1574803149606299191, 0.7381889762704251234 ) ) ;
#34860=ORIENTED_EDGE ( 'NONE', *, *, #45320, .F. ) ;
#34861=CARTESIAN_POINT ( 'NONE',  ( -1.033464566929133799, 1.928577636452524610E-17, 2.869337061179095023E-17 ) ) ;
#34862=CARTESIAN_POINT ( 'NONE',  ( 0.7495606340400177148, 0.1264236179284866091, 1.065452755851747924 ) ) ;
#34864=CARTESIAN_POINT ( 'NONE',  ( -1.033464566929133799, 0.000000000000000000, 0.5905511809948347235 ) ) ;
#34865=CARTESIAN_POINT ( 'NONE',  ( -0.8759842519685039353, -0.1574803149606299191, 1.377952755905512028 ) ) ;
#34867=CARTESIAN_POINT ( 'NONE',  ( 1.033464566929133799, 0.000000000000000000, 1.820866141732283561 ) ) ;
#34870=CARTESIAN_POINT ( 'NONE',  ( 1.002407869896990045, 0.1264236179284866091, 0.1500984251430867999 ) ) ;
#34871=CARTESIAN_POINT ( 'NONE',  ( -0.6971942568897626646, -0.07405724077823297447, 0.08366141726907130871 ) ) ;
#34872=CARTESIAN_POINT ( 'NONE',  ( 1.033464566929133799, 0.000000000000000000, 1.456692913278299084 ) ) ;
#34873=ORIENTED_EDGE ( 'NONE', *, *, #17211, .F. ) ;
#34876=CARTESIAN_POINT ( 'NONE',  ( 0.7185039370078739607, 1.928577636452523993E-17, 0.5807086614173228023 ) ) ;
#34879=CARTESIAN_POINT ( 'NONE',  ( -1.002407869896990045, -0.1264236179284866091, 1.631397637741511808 ) ) ;
#34881=EDGE_CURVE ( 'NONE', #7898, #32014, #12003, .T. ) ;
#34882=CARTESIAN_POINT ( 'NONE',  ( -0.7185039370078739607, 1.928577636452523993E-17, 0.2559055117034968463 ) ) ;
#34887=ORIENTED_EDGE ( 'NONE', *, *, #11343, .F. ) ;
#34890=VECTOR ( 'NONE', #34947, 39.37007874015748143 ) ;
#34893=CARTESIAN_POINT ( 'NONE',  ( -0.8107537697050254399, -0.1574803149606297803, 1.405019684931842816 ) ) ;
#34895=CARTESIAN_POINT ( 'NONE',  ( 0.7185039370078746268, -0.06523048226347956391, 1.764271653543307838 ) ) ;
#34897=CARTESIAN_POINT ( 'NONE',  ( -0.8759842519685039353, 0.1787899950787401882, 0.3518700786863940833 ) ) ;
#34898=CARTESIAN_POINT ( 'NONE',  ( -0.7185039370078739607, 1.928577636452523993E-17, 1.013779527559055094 ) ) ;
#34900=CARTESIAN_POINT ( 'NONE',  ( -0.7366659922730268706, 0.08466132560603677193, 1.981546310870151428 ) ) ;
#34902=CARTESIAN_POINT ( 'NONE',  ( 0.7495606340400177148, 0.1264236179284866091, 1.065452755851747924 ) ) ;
#34904=CARTESIAN_POINT ( 'NONE',  ( -0.8107537697050254399, 0.1574803149606300301, 0.6422244093412927679 ) ) ;
#34905=CARTESIAN_POINT ( 'NONE',  ( 0.7646288533564489232, -0.1113553986120547346, 1.491141732283464583 ) ) ;
#34908=DIRECTION ( 'NONE',  ( 1.822029033848725028E-16, 0.000000000000000000, 1.000000000000000000 ) ) ;
#34911=CARTESIAN_POINT ( 'NONE',  ( 0.7495606340400177148, 0.1264236179284866091, 0.9424212597887559051 ) ) ;
#34912=CARTESIAN_POINT ( 'NONE',  ( 0.8019270111902716547, 0.1787899950787401604, 1.929133858213952557 ) ) ;
#34913=CARTESIAN_POINT ( 'NONE',  ( 0.9412147342319837628, -0.1574803149606297803, 0.3469488187901108023 ) ) ;
#34918=CARTESIAN_POINT ( 'NONE',  ( -1.033464566929134687, -0.06523048226347956391, 0.1943897636720004762 ) ) ;
#34919=DIRECTION ( 'NONE',  ( 0.000000000000000000, 0.000000000000000000, -1.000000000000000000 ) ) ;
#34920=CARTESIAN_POINT ( 'NONE',  ( 0.7495606340400177148, 0.1264236179284866091, 1.257381889710015743 ) ) ;
#34925=CARTESIAN_POINT ( 'NONE',  ( -0.6971942568897626646, 0.07405724077823318263, 0.5905511810485987167 ) ) ;
#34928=CARTESIAN_POINT ( 'NONE',  ( -0.8759842519685039353, -0.1787899950787401882, 1.040846456639149764 ) ) ;
#34929=CARTESIAN_POINT ( 'NONE',  ( -0.6971942568897648851, -0.07405724077823297447, 1.934055118056471567 ) ) ;
#34930=VERTEX_POINT ( 'NONE', #26500 ) ;
#34931=EDGE_CURVE ( 'NONE', #8568, #8310, #46530, .T. ) ;
#34932=CARTESIAN_POINT ( 'NONE',  ( -0.7495606340400177148, 0.1264236179284866091, 0.7504921259304880854 ) ) ;
#34934=CARTESIAN_POINT ( 'NONE',  ( -0.7185039370078746268, 0.06523048226347956391, 0.09596456682160686702 ) ) ;
#34940=CARTESIAN_POINT ( 'NONE',  ( -0.7646288533564489232, -0.1113553986120547346, 1.756889763671999782 ) ) ;
#34941=CARTESIAN_POINT ( 'NONE',  ( -1.054774247047244540, -0.07405724077823318263, 0.4921259841982048577 ) ) ;
#34944=CARTESIAN_POINT ( 'NONE',  ( -0.8019270111902716547, -0.1787899950787401604, 1.668307086560410157 ) ) ;
#34947=DIRECTION ( 'NONE',  ( 0.000000000000000000, 0.000000000000000000, -1.000000000000000000 ) ) ;
#34948=( BOUNDED_CURVE ( )  B_SPLINE_CURVE ( 2, ( #46130, #13779, #28426, #20503, #6107, #27500, #42050, #16686, #17141 ),
 .UNSPECIFIED., .F., .T. ) 
 B_SPLINE_CURVE_WITH_KNOTS ( ( 3, 2, 2, 2, 3 ),
 ( 0.8299999999999999600, 0.8325000000000000178, 0.8349999999999999645, 0.8375000000000000222, 0.8399999999999999689 ),
 .UNSPECIFIED. ) 
 CURVE ( )  GEOMETRIC_REPRESENTATION_ITEM ( )  RATIONAL_B_SPLINE_CURVE ( ( 1.000000000000000000, 0.9238795325112899581, 1.000000000000000000, 0.9238795325112869605, 1.000000000000000000, 0.9238795325112869605, 1.000000000000000000, 0.9238795325112869605, 1.000000000000000000 ) ) 
 REPRESENTATION_ITEM ( '' )  ) ;
#34949=CARTESIAN_POINT ( 'NONE',  ( -0.7646288533564489232, 0.1113553986120547346, 0.4970472440944882497 ) ) ;
#34950=CARTESIAN_POINT ( 'NONE',  ( 0.7185039370078746268, 0.06523048226347956391, 0.5388779527559054427 ) ) ;
#34952=DIRECTION ( 'NONE',  ( 0.000000000000000000, 1.000000000000000000, 0.000000000000000000 ) ) ;
#34953=CARTESIAN_POINT ( 'NONE',  ( -0.7185039370078746268, -0.06523048226347956391, 1.163877952648379344 ) ) ;
#34959=CARTESIAN_POINT ( 'NONE',  ( -0.6971942568897648851, 0.07405724077823318263, 1.146653543253323582 ) ) ;
#34960=CARTESIAN_POINT ( 'NONE',  ( 0.9873396505805591694, -0.1113553986120547346, 1.028543307086614123 ) ) ;
#34963=CARTESIAN_POINT ( 'NONE',  ( -0.9410460383272908347, -0.1644621043414253858, 1.989368141162188186 ) ) ;
#34969=ORIENTED_EDGE ( 'NONE', *, *, #9556, .T. ) ;
#34972=CARTESIAN_POINT ( 'NONE',  ( 0.8759842519685039353, 0.1787899950787401882, 0.8193897637257637756 ) ) ;
#34979=CARTESIAN_POINT ( 'NONE',  ( 0.9412147342319837628, 0.1574803149606300301, 1.227854330601135580 ) ) ;
#34980=( BOUNDED_SURFACE ( )  B_SPLINE_SURFACE ( 1, 2, ( 
 ( #23723, #8863, #37619, #16307, #38097, #37370, #33582, #23255, #12002, #8377, #19165, #15843, #12722, #695, #4525, #11766, #19645, #16074, #9102, #4777, #34056, #30699, #26386, #26860, #15601, #45264, #5259, #34508, #27110, #12483, #41419, #41657, #1183, #5024, #26623, #8140, #30466, #22764, #19879, #23495, #12235, #15353, #30935, #942, #37870, #45496, #27351, #34289, #1661, #1415, #23007, #41894, #18923, #30004, #44548, #40945, #20582, #16996, #1901, #10044, #34760, #24661, #6193, #43083, #45976, #42830, #31636, #21047, #46447, #20816, #39254, #13413, #38570, #31867, #28045, #35454, #17457, #6430, #10287, #35227, #2136, #38803, #24895, #23965, #16763, #2598, #13629, #9346, #35689, #24200, #5500, #39024, #2824, #5737, #28267, #32091, #46678, #13187, #13870, #28511, #12948, #9582, #20112, #42604, #5963, #16539, #31166, #46213, #45739, #9818, #24424, #20353, #27584, #42136, #34991, #31402, #27821, #42383, #18629, #21999, #14819, #25842, #33289, #7388, #32582, #413, #44258, #47169, #36856, #3560, #10999, #29253, #44029, #3065, #21523, #29485, #36625, #17695, #39493, #14352, #36160, #14113, #32344, #46924, #11232, #28757, #40424, #43558, #29000, #10769, #11458, #43326, #21772, #6667, #32813, #10528, #15064, #33051, #25125, #3315, #25381, #39957, #7148, #36402, #3785, #18173, #47407, #14579, #40192, #18403, #15290, #22705, #7848, #30182, #11942, #37083, #37310, #30411, #41590, #18861, #34228, #44726, #5193, #40649, #635, #26328, #878, #30638, #29941, #23190, #44487, #8557, #37804, #4459, #4957, #15781, #19584, #23429, #26564, #40889, #45200, #41122, #11702, #4232, #30878, #45439, #8796, #8082, #19343, #44959, #16013, #26075, #8317, #12422, #19101, #33767, #1357, #15539, #22946, #37556, #4717, #22463, #33519, #27042, #33995, #38035, #19818, #1122, #12172, #26795, #41352, #34446, #1593, #9521, #6373, #41834, #31108, #5434, #13356, #9755, #2775, #45917, #27767, #24368, #20052, #20529, #9279, #38968, #31810, #28208, #20755, #6133, #35164, #35402, #13131, #46160, #38507, #1838, #42327, #16478, #13573, #2543, #24146, #27286, #24598, #45671, #31578, #9988, #39197, #2307, #46396, #38749, #16705, #20287, #17398, #32037, #12661, #5914, #16936, #27984, #9037, #17172, #23660, #42773, #42552, #38269, #5678, #20985, #35634, #34694, #12889, #27524, #42077, #23900, #34932, #6616, #47110, #28453, #3962, #40370, #43022, #3006, #3505, #32287, #39906, #10228, #21952, #7339, #14052, #18355, #28943, #14770, #28700, #14300, #35854, #25798, #43503, #43980, #21229, #6844, #32998, #21720, #11187, #10472, #25070, #14532, #46866, #3735, #17640, #22171, #43271, #36351, #24835, #46628, #7558, #18118, #32762, #29197, #43744, #10948, #36574, #121, #33885, #4133, #19463, #22594, #29834, #7973, #18985, #759, #15421, #30069, #22827, #37442, #4592, #1006, #41953, #24259, #38152, #5316, #27647, #27167, #41718, #31453, #9160, #30761, #37927, #31696, #46279, #42436, #45327, #20168, #45797, #16815, #26922, #23774, #13246, #8922, #19931, #9405, #34568, #1720, #38389, #12544, #41473, #8678, #9640, #5558, #38855, #6020, #16366, #23312, #31220, #30990, #34822, #1963, #16595, #20642, #19701, #42203, #34342, #24022, #38626, #17055, #5801, #20408, #35047, #1474, #2193, #35287, #2427, #16131, #40201, #33297, #2985, #17617, #3226, #34486, #1882, #27565, #47335, #8009, #21933, #36553, #20210, #19742, #26487, #33924, #26727, #45371, #26964, #8965, #28373, #10393, #28140, #42480, #25493, #40759, #3174, #32453, #21881, #18278, #14688, #47030, #7715, #28864, #22331, #18508, #25234, #43664, #40525, #29362, #18736, #25946, #33164, #36725, #29111, #39823, #32920, #7012, #4115, #33394, #43903, #21639, #15168, #36272, #22099, #511, #29813, #40294, #44358, #40, #7259, #40059, #3424, #18039, #47274, #36501, #11103, #25725, #14453, #11566, #3656, #26191, #284, #7479, #14930, #29594, #1223, #5297, #30737, #5064, #41700, #40995, #12758, #30046, #8419, #4332, #41932, #30968, #18966, #8181, #41455, #22806, #15877, #33626, #12525, #45306, #4573, #8901, #19443, #19915, #19207, #23046, #26429, #16347, #34095, #34546, #44592, #44832, #23533, #37665, #45535, #984, #15643, #37907, #37415, #33866, #38135, #4820, #12043, #741, #9140, #37188, #27389, #26665, #30502, #8656, #27147, #15402, #45064, #11808, #41214, #12278, #19681, #26897, #23292, #34323, #1454, #16112, #28558, #13669, #42417, #21092, #42874, #42176, #38365, #28081, #2174, #46017, #24005, #20622, #17503, #5539, #9386, #16573, #24464, #20855, #13913, #9621, #38836, #35498, #31203, #31675, #20385, #2638, #10085, #39297, #31907, #17271, #46254, #46490, #24239, #35026, #28306, #24697, #6471, #35730, #2868, #13451, #32134, #6002, #9853, #31436, #12985, #35269, #27625, #46725, #43127, #2404, #20151, #23756, #38603, #42643, #34798, #1939, #6231, #45775, #17037, #27860, #13226, #5779, #29761, #10331, #29048, #25430, #21821, #6713, #14873, #39538, #29532, #11052, #462, #3366, #224, #36449, #25892, #3832, #25664, #44083, #14161, #33338, #3115, #43607, #24942, #15114, #4064, #21327, #28804, #14630, #43367, #3603, #35960, #33101, #18453, #25177, #11280, #40005, #40474, #39761, #10817, #46971, #36910, #7198, #7658, #17742, #17976, #22274, #18223, #18678, #21574, #36214, #7429, #10578, #6953, #32391, #32863, #32630, #47217, #14400, #47459, #29300, #43848, #22048, #36674, #34276, #1653, #15591, #1405, #11756, #26378, #26851, #40937, #44540, #41168, #15343, #16298, #44308, #30691, #30229, #41650, #45255, #29996, #11511, #1172, #22757, #19152, #8133, #8371, #38089, #26133, #37362, #37132, #45013, #41409, #34499, #44777, #11993, #8607, #4283, #4769, #34048, #23246, #8852, #26615, #19396, #4514, #37860, #15832, #5014, #23488, #12475, #40702, #37610, #33817, #30456, #22517, #933, #12225, #19634, #27098, #690, #5248, #19873, #18914, #33572, #20808, #16530, #28036, #17225, #9808, #38564, #42595, #35447, #38320, #34985, #30926, #20575, #31396, #13407, #6184, #2128, #23713, #45966, #16757, #34752, #13180, #13620, #10034, #1894, #27817, #31860, #42821, #24416, #2587, #46439, #24653, #46206, #23958, #39247, #35681, #5729, #28259, #42376, #2354, #35217, #6420, #41885, #31158, #21038, #39018, #9092, #45488, #20345, #12943, #5493, #27341, #20106, #2818, #45727, #12715, #9575, #24193, #9339, #27575, #42125, #38795, #5955, #16988, #31629, #3777 ),
 ( #10276, #25609, #36150, #44022, #32084, #39483, #17684, #39708, #21993, #6660, #14573, #21279, #47400, #29245, #14104, #43794, #47160, #21513, #25117, #22216, #36846, #17450, #3305, #32576, #28990, #13860, #36618, #46672, #18398, #18164, #28505, #10519, #7384, #43549, #33042, #10993, #32804, #168, #35902, #40416, #24886, #17922, #43071, #3056, #11224, #32336, #46915, #21763, #28750, #10763, #43315, #40184, #14815, #6893, #29478, #14344, #25837, #25370, #39950, #7142, #36398, #3552, #19578, #44251, #11695, #23182, #37303, #1350, #15285, #29935, #4708, #4227, #18856, #8549, #19091, #7842, #15058, #8790, #23425, #34223, #22454, #44715, #22938, #41347, #4002, #22698, #37798, #33513, #627, #33988, #44480, #26321, #871, #37075, #18624, #33284, #4950, #4453, #16007, #30631, #40879, #409, #8308, #8076, #33761, #15530, #30174, #45194, #29706, #11936, #11454, #19337, #1114, #41588, #26558, #41115, #15773, #26069, #37547, #30405, #44954, #12416, #27037, #12165, #26790, #40640, #40239, #36210, #3599, #28801, #39535, #47214, #6711, #18449, #7426, #14396, #17500, #44079, #21325, #18219, #11276, #40470, #40002, #22045, #7654, #47457, #36670, #17738, #14628, #22270, #29297, #10574, #43845, #2864, #10328, #6950, #32132, #7194, #3362, #11047, #46723, #21571, #43124, #29045, #43604, #32388, #10814, #13910, #28556, #46968, #25427, #24940, #14157, #43365, #25174, #39758, #27095, #12223, #40934, #41646, #8849, #8131, #34273, #19631, #29758, #44304, #7897, #4279, #33569, #687, #15340, #22754, #4512, #19088, #33758, #18621, #40413, #30171, #19576, #44711, #26555, #41112, #34684, #9026, #36027, #8788, #12880, #45192, #23890, #5187, #17574, #24135, #12414, #2937, #13987, #28637, #23650, #1829, #27756, #27035, #45662, #21162, #3188, #46801, #19808, #27276, #41586, #16465, #31101, #38027, #41825, #34925, #43195, #34440, #38738, #27514, #10406, #1585, #16239, #30870, #5425, #35794, #45432, #42319, #38261, #13122, #9511, #42066, #6550, #20276, #32215, #25008, #9270, #38497, #5669, #39606, #2070, #6783, #21402, #30629, #31328, #45906, #14463, #3666, #7964, #36284, #29122, #14941, #29603, #21651, #4122, #36511, #21890, #7272, #43674, #22583, #43434, #14699, #32464, #11116, #39835, #18746, #11344, #47042, #36969, #521, #15179, #10884, #18290, #44145, #14234, #32931, #7725, #17817, #33404, #7026, #25504, #28876, #29374, #43913, #10642, #40072, #22109, #29822, #25247, #40535, #25735, #44368, #3436, #18049, #32695, #40307, #22341, #47285, #11575, #7489, #26202, #40768, #36736, #3894, #18521, #33173, #1708, #23057, #8666, #37429, #30745, #12536, #34556, #16355, #27398, #33636, #15888, #996, #30512, #750, #33877, #30291, #15411, #8191, #44843, #45073, #30237, #1660, #41418, #1414, #44547, #8616, #8862, #19644, #19163, #23254, #30698, #18921, #44788, #40709, #1182, #12001, #5258, #19878, #26621, #4290, #41176, #8376, #15351, #23006, #16306, #30934, #30003, #37618, #7909, #22525, #37141, #33580, #11765, #26385, #40944, #15842, #37369, #30465, #5736, #42829, #9581, #16995, #35226, #2597, #9101, #45737, #17231, #42603, #23722, #27349, #2134, #27583, #1899, #41892, #9345, #6191, #23964, #46446, #28265, #20815, #31866, #20581, #10042, #2361, #31635, #46212, #28044, #9815, #24660, #6429, #21046, #35688, #17455, #44028, #32343, #3559, #22222, #4008, #36401, #3784, #25379, #36159, #39716, #32090, #28510, #43082, #3314, #47168, #39956, #10285, #36623, #24894, #39492, #10998, #21283, #6900, #21998, #7147, #14112, #25616, #40191, #28756, #10527, #32581, #18172, #44725, #633, #22704, #37555, #1121, #35375, #43243, #2519, #25043, #13108, #6821, #16689, #17145, #27739, #31789, #42305, #18091, #21930, #39881, #15220, #18334, #4168, #28914, #43719, #22387, #36550, #33448, #47332, #14503, #36782, #36325, #3479, #40580, #3711, #7065, #14275, #40810, #36068, #564, #21693, #43958, #7537, #37014, #43477, #7311, #44410, #32737, #29165, #18561, #10924, #32972, #14743, #11157, #10685, #22149, #11628, #3938, #26247, #33218, #342, #14991, #29643, #44184, #12100, #22871, #34153, #45597, #4392, #4636, #15462, #37965, #34376, #27449, #8479, #37727, #1515, #30112, #26961, #1046, #16168, #41759, #19975, #15703, #26724, #30802, #41279, #4881, #8962, #1281, #15937, #33686, #41992, #22635, #5352, #41514, #8719, #45368, #12583, #19022, #23582, #34614, #1763, #797, #11860, #24064, #9450, #6057, #27684, #13974, #28625, #46549, #27913, #6536, #28371, #42246, #23814, #13506, #16854, #31497, #38673, #20685, #17562, #38433, #5841, #2004, #9912, #6295, #46786, #42478, #24297, #20917, #16630, #17091, #20449, #35556, #42941, #39354, #17328, #31964, #31729, #13732, #9682, #42696, #46080, #45839, #38896, #13048, #10150, #21150, #35325, #5600, #35785, #13282, #28138, #32200, #9196, #46322, #34858, #2464, #24522, #39123, #31261, #15166, #43182, #14451, #10871, #7256, #39592, #282, #24996, #14927, #43901, #33392, #36270, #33161, #21879, #11333, #36723, #11100, #29592, #47027, #18733, #36014, #29109, #10391, #508, #36958, #6773, #14221, #38, #28862, #36499, #21389, #18506, #3885, #10630, #44135, #25490, #25944, #25232, #43662, #32451, #22329, #40057, #40523, #3172, #3421, #7713, #3654, #17801, #39821, #14686, #4113, #43421, #7010, #18276, #21636, #18037, #32683, #47272, #32918, #29359, #40292, #7477, #22097, #12276, #41453, #26426, #26895, #19441, #8654, #27145, #982, #37663, #15400, #23290, #4818, #37904, #41697, #16110, #34544, #44830, #40993, #15641, #19913, #739, #8179, #5062, #19679, #33624, #30735, #30276, #1696, #15875, #34321, #30044, #1452, #45304, #12523, #37413, #8899, #23531, #37186, #33864, #29811, #34092, #12041, #38133, #5295, #26663, #22571, #41212, #8416, #44589, #23044, #44356, #11564, #11806, #1221, #26189, #40756, #7953, #4330, #18964, #22804, #45062, #4571, #19205, #30500, #24003, #28304, #27856, #35267, #6000, #2636, #27386, #16571, #6229, #13449, #41930, #16345, #38601, #45773, #38363, #12756, #23754, #24462, #9138, #17269, #20382, #5776, #42174, #21089, #5537, #46015, #30966, #9618, #20149, #31905, #9850, #45533, #46487, #42872, #10083, #9383, #35024, #28078, #34796, #31434, #24695, #35728, #39295, #1936, #12983, #31201, #2172, #16795, #6469, #42414, #27622, #13223, #24237, #2402, #38834, #20620, #17035, #31672, #46251, #42640, #39061, #33028, #14805, #42804, #14090 ) ),
 .UNSPECIFIED., .F., .F., .T. ) 
 B_SPLINE_SURFACE_WITH_KNOTS ( ( 2, 2 ),
 ( 3, 2, 2, 2, 2, 2, 2, 2, 2, 2, 2, 2, 2, 2, 2, 2, 2, 2, 2, 2, 2, 2, 2, 2, 2, 2, 2, 2, 2, 2, 2, 2, 2, 2, 2, 2, 2, 2, 2, 2, 2, 2, 2, 2, 2, 2, 2, 2, 2, 2, 2, 2, 2, 2, 2, 2, 2, 2, 2, 2, 2, 2, 2, 2, 2, 2, 2, 2, 2, 2, 2, 2, 2, 2, 2, 2, 2, 2, 2, 2, 2, 2, 2, 2, 2, 2, 2, 2, 2, 2, 2, 2, 2, 2, 2, 2, 2, 2, 2, 2, 2, 2, 2, 2, 2, 2, 2, 2, 2, 2, 2, 2, 2, 2, 2, 2, 2, 2, 2, 2, 2, 2, 2, 2, 2, 2, 2, 2, 2, 2, 2, 2, 2, 2, 2, 2, 2, 2, 2, 2, 2, 2, 2, 2, 2, 2, 2, 2, 2, 2, 2, 2, 2, 2, 2, 2, 2, 2, 2, 2, 2, 2, 2, 2, 2, 2, 2, 2, 2, 2, 2, 2, 2, 2, 2, 2, 2, 2, 2, 2, 2, 2, 2, 2, 2, 2, 2, 2, 2, 2, 2, 2, 2, 2, 2, 2, 2, 2, 2, 2, 2, 2, 2, 2, 2, 2, 2, 2, 2, 2, 2, 2, 2, 2, 2, 2, 2, 2, 2, 2, 2, 2, 2, 2, 2, 2, 2, 2, 2, 2, 2, 2, 2, 2, 2, 2, 2, 2, 2, 2, 2, 2, 2, 2, 2, 2, 2, 2, 2, 2, 2, 2, 2, 2, 2, 2, 2, 2, 2, 2, 2, 2, 2, 2, 2, 2, 2, 2, 2, 2, 2, 2, 2, 2, 2, 2, 2, 2, 2, 2, 2, 2, 2, 2, 2, 2, 2, 2, 2, 2, 2, 2, 2, 2, 2, 2, 2, 2, 2, 2, 2, 2, 2, 2, 2, 2, 2, 2, 2, 2, 2, 2, 2, 2, 2, 2, 2, 2, 2, 2, 2, 2, 2, 2, 2, 2, 2, 2, 2, 2, 2, 2, 2, 2, 2, 2, 2, 2, 2, 2, 2, 2, 2, 2, 2, 2, 2, 2, 2, 2, 2, 2, 2, 2, 2, 2, 2, 2, 2, 2, 2, 2, 2, 2, 2, 2, 2, 2, 2, 2, 2, 2, 2, 2, 2, 2, 2, 2, 2, 2, 2, 2, 2, 2, 2, 2, 2, 2, 2, 2, 2, 2, 2, 2, 2, 2, 2, 2, 2, 2, 3 ),
 ( 0.000000000000000000, 1.000000000000000000 ),
 ( 0.000000000000000000, 0.002500000000000000052, 0.005000000000000000104, 0.007499999999999999722, 0.01000000000000000021, 0.01250000000000000069, 0.01499999999999999944, 0.01750000000000000167, 0.02000000000000000042, 0.02249999999999999917, 0.02500000000000000139, 0.02750000000000000014, 0.02999999999999999889, 0.03250000000000000111, 0.03500000000000000333, 0.03749999999999999861, 0.04000000000000000083, 0.04250000000000000305, 0.04499999999999999833, 0.04750000000000000056, 0.05000000000000000278, 0.05249999999999999806, 0.05500000000000000028, 0.05750000000000000250, 0.05999999999999999778, 0.06250000000000000000, 0.06500000000000000222, 0.06750000000000000444, 0.07000000000000000666, 0.07249999999999999500, 0.07499999999999999722, 0.07749999999999999944, 0.08000000000000000167, 0.08250000000000000389, 0.08500000000000000611, 0.08749999999999999445, 0.08999999999999999667, 0.09249999999999999889, 0.09500000000000000111, 0.09750000000000000333, 0.1000000000000000056, 0.1024999999999999939, 0.1049999999999999961, 0.1074999999999999983, 0.1100000000000000006, 0.1125000000000000028, 0.1150000000000000050, 0.1174999999999999933, 0.1199999999999999956, 0.1224999999999999978, 0.1250000000000000000, 0.1275000000000000022, 0.1300000000000000044, 0.1325000000000000067, 0.1350000000000000089, 0.1375000000000000111, 0.1400000000000000133, 0.1424999999999999878, 0.1449999999999999900, 0.1474999999999999922, 0.1499999999999999944, 0.1524999999999999967, 0.1549999999999999989, 0.1575000000000000011, 0.1600000000000000033, 0.1625000000000000056, 0.1650000000000000078, 0.1675000000000000100, 0.1700000000000000122, 0.1724999999999999867, 0.1749999999999999889, 0.1774999999999999911, 0.1799999999999999933, 0.1824999999999999956, 0.1849999999999999978, 0.1875000000000000000, 0.1900000000000000022, 0.1925000000000000044, 0.1950000000000000067, 0.1975000000000000089, 0.2000000000000000111, 0.2025000000000000133, 0.2049999999999999878, 0.2074999999999999900, 0.2099999999999999922, 0.2124999999999999944, 0.2149999999999999967, 0.2174999999999999989, 0.2200000000000000011, 0.2225000000000000033, 0.2250000000000000056, 0.2275000000000000078, 0.2300000000000000100, 0.2325000000000000122, 0.2349999999999999867, 0.2374999999999999889, 0.2399999999999999911, 0.2424999999999999933, 0.2449999999999999956, 0.2474999999999999978, 0.2500000000000000000, 0.2525000000000000022, 0.2550000000000000044, 0.2575000000000000067, 0.2600000000000000089, 0.2625000000000000111, 0.2650000000000000133, 0.2675000000000000155, 0.2700000000000000178, 0.2725000000000000200, 0.2750000000000000222, 0.2775000000000000244, 0.2800000000000000266, 0.2824999999999999734, 0.2849999999999999756, 0.2874999999999999778, 0.2899999999999999800, 0.2924999999999999822, 0.2949999999999999845, 0.2974999999999999867, 0.2999999999999999889, 0.3024999999999999911, 0.3049999999999999933, 0.3074999999999999956, 0.3099999999999999978, 0.3125000000000000000, 0.3150000000000000022, 0.3175000000000000044, 0.3200000000000000067, 0.3225000000000000089, 0.3250000000000000111, 0.3275000000000000133, 0.3300000000000000155, 0.3325000000000000178, 0.3350000000000000200, 0.3375000000000000222, 0.3400000000000000244, 0.3425000000000000266, 0.3449999999999999734, 0.3474999999999999756, 0.3499999999999999778, 0.3524999999999999800, 0.3549999999999999822, 0.3574999999999999845, 0.3599999999999999867, 0.3624999999999999889, 0.3649999999999999911, 0.3674999999999999933, 0.3699999999999999956, 0.3724999999999999978, 0.3750000000000000000, 0.3775000000000000022, 0.3800000000000000044, 0.3825000000000000067, 0.3850000000000000089, 0.3875000000000000111, 0.3900000000000000133, 0.3925000000000000155, 0.3950000000000000178, 0.3975000000000000200, 0.4000000000000000222, 0.4025000000000000244, 0.4050000000000000266, 0.4074999999999999734, 0.4099999999999999756, 0.4124999999999999778, 0.4149999999999999800, 0.4174999999999999822, 0.4199999999999999845, 0.4224999999999999867, 0.4249999999999999889, 0.4274999999999999911, 0.4299999999999999933, 0.4324999999999999956, 0.4349999999999999978, 0.4375000000000000000, 0.4400000000000000022, 0.4425000000000000044, 0.4450000000000000067, 0.4475000000000000089, 0.4500000000000000111, 0.4525000000000000133, 0.4550000000000000155, 0.4575000000000000178, 0.4600000000000000200, 0.4625000000000000222, 0.4650000000000000244, 0.4675000000000000266, 0.4699999999999999734, 0.4724999999999999756, 0.4749999999999999778, 0.4774999999999999800, 0.4799999999999999822, 0.4824999999999999845, 0.4849999999999999867, 0.4874999999999999889, 0.4899999999999999911, 0.4924999999999999933, 0.4949999999999999956, 0.4974999999999999978, 0.5000000000000000000, 0.5024999999999999467, 0.5050000000000000044, 0.5074999999999999512, 0.5100000000000000089, 0.5124999999999999556, 0.5150000000000000133, 0.5174999999999999600, 0.5200000000000000178, 0.5224999999999999645, 0.5250000000000000222, 0.5274999999999999689, 0.5300000000000000266, 0.5324999999999999734, 0.5350000000000000311, 0.5374999999999999778, 0.5400000000000000355, 0.5424999999999999822, 0.5450000000000000400, 0.5474999999999999867, 0.5500000000000000444, 0.5524999999999999911, 0.5550000000000000488, 0.5574999999999999956, 0.5600000000000000533, 0.5625000000000000000, 0.5649999999999999467, 0.5675000000000000044, 0.5699999999999999512, 0.5725000000000000089, 0.5749999999999999556, 0.5775000000000000133, 0.5799999999999999600, 0.5825000000000000178, 0.5849999999999999645, 0.5875000000000000222, 0.5899999999999999689, 0.5925000000000000266, 0.5949999999999999734, 0.5975000000000000311, 0.5999999999999999778, 0.6025000000000000355, 0.6049999999999999822, 0.6075000000000000400, 0.6099999999999999867, 0.6125000000000000444, 0.6149999999999999911, 0.6175000000000000488, 0.6199999999999999956, 0.6225000000000000533, 0.6250000000000000000, 0.6274999999999999467, 0.6300000000000000044, 0.6324999999999999512, 0.6350000000000000089, 0.6374999999999999556, 0.6400000000000000133, 0.6424999999999999600, 0.6450000000000000178, 0.6474999999999999645, 0.6500000000000000222, 0.6524999999999999689, 0.6550000000000000266, 0.6574999999999999734, 0.6600000000000000311, 0.6624999999999999778, 0.6650000000000000355, 0.6674999999999999822, 0.6700000000000000400, 0.6724999999999999867, 0.6750000000000000444, 0.6774999999999999911, 0.6800000000000000488, 0.6824999999999999956, 0.6850000000000000533, 0.6875000000000000000, 0.6899999999999999467, 0.6925000000000000044, 0.6949999999999999512, 0.6975000000000000089, 0.6999999999999999556, 0.7025000000000000133, 0.7049999999999999600, 0.7075000000000000178, 0.7099999999999999645, 0.7125000000000000222, 0.7149999999999999689, 0.7175000000000000266, 0.7199999999999999734, 0.7225000000000000311, 0.7249999999999999778, 0.7275000000000000355, 0.7299999999999999822, 0.7325000000000000400, 0.7349999999999999867, 0.7375000000000000444, 0.7399999999999999911, 0.7425000000000000488, 0.7449999999999999956, 0.7475000000000000533, 0.7500000000000000000, 0.7524999999999999467, 0.7550000000000000044, 0.7574999999999999512, 0.7600000000000000089, 0.7624999999999999556, 0.7650000000000000133, 0.7674999999999999600, 0.7700000000000000178, 0.7724999999999999645, 0.7750000000000000222, 0.7774999999999999689, 0.7800000000000000266, 0.7824999999999999734, 0.7850000000000000311, 0.7874999999999999778, 0.7900000000000000355, 0.7924999999999999822, 0.7950000000000000400, 0.7974999999999999867, 0.8000000000000000444, 0.8024999999999999911, 0.8050000000000000488, 0.8074999999999999956, 0.8100000000000000533, 0.8125000000000000000, 0.8149999999999999467, 0.8175000000000000044, 0.8199999999999999512, 0.8225000000000000089, 0.8249999999999999556, 0.8275000000000000133, 0.8299999999999999600, 0.8325000000000000178, 0.8349999999999999645, 0.8375000000000000222, 0.8399999999999999689, 0.8425000000000000266, 0.8449999999999999734, 0.8475000000000000311, 0.8499999999999999778, 0.8525000000000000355, 0.8549999999999999822, 0.8575000000000000400, 0.8599999999999999867, 0.8625000000000000444, 0.8649999999999999911, 0.8675000000000000488, 0.8699999999999999956, 0.8725000000000000533, 0.8750000000000000000, 0.8774999999999999467, 0.8800000000000000044, 0.8824999999999999512, 0.8850000000000000089, 0.8874999999999999556, 0.8900000000000000133, 0.8924999999999999600, 0.8950000000000000178, 0.8974999999999999645, 0.9000000000000000222, 0.9024999999999999689, 0.9050000000000000266, 0.9074999999999999734, 0.9100000000000000311, 0.9124999999999999778, 0.9150000000000000355, 0.9174999999999999822, 0.9200000000000000400, 0.9224999999999999867, 0.9250000000000000444, 0.9274999999999999911, 0.9300000000000000488, 0.9324999999999999956, 0.9350000000000000533, 0.9375000000000000000, 0.9399999999999999467, 0.9425000000000000044, 0.9449999999999999512, 0.9475000000000000089, 0.9499999999999999556, 0.9525000000000000133, 0.9549999999999999600, 0.9575000000000000178, 0.9599999999999999645, 0.9625000000000000222, 0.9649999999999999689, 0.9675000000000000266, 0.9699999999999999734, 0.9725000000000000311, 0.9749999999999999778, 0.9775000000000000355, 0.9799999999999999822, 0.9825000000000000400, 0.9849999999999999867, 0.9875000000000000444, 0.9899999999999999911, 0.9925000000000000488, 0.9949999999999999956, 0.9975000000000000533, 1.000000000000000000 ),
 .UNSPECIFIED. ) 
 GEOMETRIC_REPRESENTATION_ITEM ( )  RATIONAL_B_SPLINE_SURFACE ( (
 ( 1.000000000000000000, 0.9238795325112869605, 1.000000000000000000, 0.9238795325112869605, 1.000000000000000000, 0.9238795325112869605, 1.000000000000000000, 0.9238795325112869605, 1.000000000000000000, 0.9238795325112869605, 1.000000000000000000, 0.9238795325112869605, 1.000000000000000000, 0.9238795325112869605, 1.000000000000000000, 0.9238795325112869605, 1.000000000000000000, 0.9238795325112869605, 1.000000000000000000, 0.9238795325112869605, 1.000000000000000000, 0.9238795325112869605, 1.000000000000000000, 0.9238795325112869605, 1.000000000000000000, 0.9238795325112869605, 1.000000000000000000, 0.9238795325112869605, 1.000000000000000000, 0.9238795325112869605, 1.000000000000000000, 0.9238795325112869605, 1.000000000000000000, 0.9238795325112869605, 1.000000000000000000, 0.9238795325112869605, 1.000000000000000000, 0.9238795325112869605, 1.000000000000000000, 0.9238795325112869605, 1.000000000000000000, 0.9238795325112869605, 1.000000000000000000, 0.9238795325112869605, 1.000000000000000000, 0.9238795325112869605, 1.000000000000000000, 0.9238795325112869605, 1.000000000000000000, 0.9238795325112869605, 1.000000000000000000, 0.9238795325112869605, 1.000000000000000000, 0.9238795325112869605, 1.000000000000000000, 0.9238795325112869605, 1.000000000000000000, 0.9238795325112869605, 1.000000000000000000, 0.9238795325112869605, 1.000000000000000000, 0.9238795325112869605, 1.000000000000000000, 0.9238795325112869605, 1.000000000000000000, 0.9238795325112869605, 1.000000000000000000, 0.9238795325112869605, 1.000000000000000000, 0.9238795325112869605, 1.000000000000000000, 0.9238795325112869605, 1.000000000000000000, 0.9238795325112869605, 1.000000000000000000, 0.9238795325112869605, 1.000000000000000000, 0.9238795325112869605, 1.000000000000000000, 0.9238795325112869605, 1.000000000000000000, 0.9238795325112869605, 1.000000000000000000, 0.9238795325112869605, 1.000000000000000000, 0.9238795325112869605, 1.000000000000000000, 0.9238795325112869605, 1.000000000000000000, 0.9238795325112869605, 1.000000000000000000, 0.9238795325112869605, 1.000000000000000000, 0.9238795325112869605, 1.000000000000000000, 0.9238795325112869605, 1.000000000000000000, 0.9238795325112869605, 1.000000000000000000, 0.9238795325112869605, 1.000000000000000000, 0.9238795325112869605, 1.000000000000000000, 0.9238795325112869605, 1.000000000000000000, 0.9238795325112869605, 1.000000000000000000, 0.9238795325112869605, 1.000000000000000000, 0.9238795325112869605, 1.000000000000000000, 0.9238795325112869605, 1.000000000000000000, 0.9238795325112869605, 1.000000000000000000, 0.9238795325112869605, 1.000000000000000000, 0.9238795325112869605, 1.000000000000000000, 0.9238795325112869605, 1.000000000000000000, 0.9238795325112869605, 1.000000000000000000, 0.9238795325112869605, 1.000000000000000000, 0.9238795325112869605, 1.000000000000000000, 0.9238795325112869605, 1.000000000000000000, 0.9238795325112869605, 1.000000000000000000, 0.9238795325112869605, 1.000000000000000000, 0.9238795325112869605, 1.000000000000000000, 0.9238795325112869605, 1.000000000000000000, 0.9238795325112869605, 1.000000000000000000, 0.9238795325112869605, 1.000000000000000000, 0.9238795325112869605, 1.000000000000000000, 0.9238795325112869605, 1.000000000000000000, 0.9238795325112869605, 1.000000000000000000, 0.9238795325112869605, 1.000000000000000000, 0.9238795325112869605, 1.000000000000000000, 0.9238795325112869605, 1.000000000000000000, 0.9238795325112869605, 1.000000000000000000, 0.9238795325112869605, 1.000000000000000000, 0.9238795325112869605, 1.000000000000000000, 0.9238795325112869605, 1.000000000000000000, 0.9238795325112869605, 1.000000000000000000, 0.9238795325112869605, 1.000000000000000000, 0.9238795325112869605, 1.000000000000000000, 0.9238795325112869605, 1.000000000000000000, 0.9238795325112869605, 1.000000000000000000, 0.9238795325112869605, 1.000000000000000000, 0.9238795325112869605, 1.000000000000000000, 0.9238795325112869605, 1.000000000000000000, 0.9238795325112869605, 1.000000000000000000, 0.9238795325112869605, 1.000000000000000000, 0.9238795325112869605, 1.000000000000000000, 0.9238795325112869605, 1.000000000000000000, 0.9238795325112869605, 1.000000000000000000, 0.9238795325112869605, 1.000000000000000000, 0.9238795325112869605, 1.000000000000000000, 0.9238795325112869605, 1.000000000000000000, 0.9238795325112869605, 1.000000000000000000, 0.9238795325112869605, 1.000000000000000000, 0.9238795325112869605, 1.000000000000000000, 0.9238795325112869605, 1.000000000000000000, 0.9238795325112869605, 1.000000000000000000, 0.9238795325112869605, 1.000000000000000000, 0.9238795325112869605, 1.000000000000000000, 0.9238795325112869605, 1.000000000000000000, 0.9238795325112869605, 1.000000000000000000, 0.9238795325112869605, 1.000000000000000000, 0.9238795325112869605, 1.000000000000000000, 0.9238795325112869605, 1.000000000000000000, 0.9238795325112869605, 1.000000000000000000, 0.9238795325112869605, 1.000000000000000000, 0.9238795325112869605, 1.000000000000000000, 0.9238795325112869605, 1.000000000000000000, 0.9238795325112869605, 1.000000000000000000, 0.9238795325112869605, 1.000000000000000000, 0.9238795325112869605, 1.000000000000000000, 0.9238795325112869605, 1.000000000000000000, 0.9238795325112869605, 1.000000000000000000, 0.9238795325112869605, 1.000000000000000000, 0.9238795325112869605, 1.000000000000000000, 0.9238795325112869605, 1.000000000000000000, 0.9238795325112869605, 1.000000000000000000, 0.9238795325112869605, 1.000000000000000000, 0.9238795325112869605, 1.000000000000000000, 0.9238795325112869605, 1.000000000000000000, 0.9238795325112869605, 1.000000000000000000, 0.9238795325112869605, 1.000000000000000000, 0.9238795325112869605, 1.000000000000000000, 0.9238795325112869605, 1.000000000000000000, 0.9238795325112869605, 1.000000000000000000, 0.9238795325112869605, 1.000000000000000000, 0.9238795325112869605, 1.000000000000000000, 0.9238795325112869605, 1.000000000000000000, 0.9238795325112869605, 1.000000000000000000, 0.9238795325112869605, 1.000000000000000000, 0.9238795325112869605, 1.000000000000000000, 0.9238795325112869605, 1.000000000000000000, 0.9238795325112869605, 1.000000000000000000, 0.9238795325112869605, 1.000000000000000000, 0.9238795325112869605, 1.000000000000000000, 0.9238795325112869605, 1.000000000000000000, 0.9238795325112869605, 1.000000000000000000, 0.9238795325112869605, 1.000000000000000000, 0.9238795325112869605, 1.000000000000000000, 0.9238795325112869605, 1.000000000000000000, 0.9238795325112869605, 1.000000000000000000, 0.9238795325112869605, 1.000000000000000000, 0.9238795325112869605, 1.000000000000000000, 0.9238795325112869605, 1.000000000000000000, 0.9238795325112869605, 1.000000000000000000, 0.9238795325112869605, 1.000000000000000000, 0.9238795325112869605, 1.000000000000000000, 0.9238795325112869605, 1.000000000000000000, 0.9238795325112869605, 1.000000000000000000, 0.9238795325112869605, 1.000000000000000000, 0.9238795325112869605, 1.000000000000000000, 0.9238795325112869605, 1.000000000000000000, 0.9238795325112869605, 1.000000000000000000, 0.9238795325112869605, 1.000000000000000000, 0.9238795325112869605, 1.000000000000000000, 0.9238795325112869605, 1.000000000000000000, 0.9238795325112869605, 1.000000000000000000, 0.9238795325112869605, 1.000000000000000000, 0.9238795325112869605, 1.000000000000000000, 0.9238795325112869605, 1.000000000000000000, 0.9238795325112869605, 1.000000000000000000, 0.9238795325112869605, 1.000000000000000000, 0.9238795325112869605, 1.000000000000000000, 0.9238795325112869605, 1.000000000000000000, 0.9238795325112869605, 1.000000000000000000, 0.9238795325112869605, 1.000000000000000000, 0.9238795325112869605, 1.000000000000000000, 0.9238795325112869605, 1.000000000000000000, 0.9238795325112869605, 1.000000000000000000, 0.9238795325112869605, 1.000000000000000000, 0.9238795325112869605, 1.000000000000000000, 0.9238795325112869605, 1.000000000000000000, 0.9238795325112869605, 1.000000000000000000, 0.9238795325112869605, 1.000000000000000000, 0.9238795325112869605, 1.000000000000000000, 0.9238795325112869605, 1.000000000000000000, 0.9238795325112869605, 1.000000000000000000, 0.9238795325112869605, 1.000000000000000000, 0.9238795325112869605, 1.000000000000000000, 0.9238795325112869605, 1.000000000000000000, 0.9238795325112869605, 1.000000000000000000, 0.9238795325112869605, 1.000000000000000000, 0.9238795325112869605, 1.000000000000000000, 0.9238795325112869605, 1.000000000000000000, 0.9238795325112869605, 1.000000000000000000, 0.9238795325112869605, 1.000000000000000000, 0.9238795325112869605, 1.000000000000000000, 0.9238795325112869605, 1.000000000000000000, 0.9238795325112869605, 1.000000000000000000, 0.9238795325112869605, 1.000000000000000000, 0.9238795325112869605, 1.000000000000000000, 0.9238795325112869605, 1.000000000000000000, 0.9238795325112869605, 1.000000000000000000, 0.9238795325112869605, 1.000000000000000000, 0.9238795325112869605, 1.000000000000000000, 0.9238795325112869605, 1.000000000000000000, 0.9238795325112869605, 1.000000000000000000, 0.9238795325112869605, 1.000000000000000000, 0.9238795325112869605, 1.000000000000000000, 0.9238795325112869605, 1.000000000000000000, 0.9238795325112869605, 1.000000000000000000, 0.9238795325112869605, 1.000000000000000000, 0.9238795325112869605, 1.000000000000000000, 0.9238795325112869605, 1.000000000000000000, 0.9238795325112869605, 1.000000000000000000, 0.9238795325112869605, 1.000000000000000000, 0.9238795325112869605, 1.000000000000000000, 0.9238795325112869605, 1.000000000000000000, 0.9238795325112869605, 1.000000000000000000, 0.9238795325112869605, 1.000000000000000000, 0.9238795325112869605, 1.000000000000000000, 0.9238795325112869605, 1.000000000000000000, 0.9238795325112869605, 1.000000000000000000, 0.9238795325112869605, 1.000000000000000000, 0.9238795325112869605, 1.000000000000000000, 0.9238795325112869605, 1.000000000000000000, 0.9238795325112869605, 1.000000000000000000, 0.9238795325112869605, 1.000000000000000000, 0.9238795325112869605, 1.000000000000000000, 0.9238795325112869605, 1.000000000000000000, 0.9238795325112869605, 1.000000000000000000, 0.9238795325112869605, 1.000000000000000000, 0.9238795325112869605, 1.000000000000000000, 0.9238795325112869605, 1.000000000000000000, 0.9238795325112869605, 1.000000000000000000, 0.9238795325112869605, 1.000000000000000000, 0.9238795325112869605, 1.000000000000000000, 0.9238795325112869605, 1.000000000000000000, 0.9238795325112869605, 1.000000000000000000, 0.9238795325112869605, 1.000000000000000000, 0.9238795325112869605, 1.000000000000000000, 0.9238795325112869605, 1.000000000000000000, 0.9238795325112869605, 1.000000000000000000, 0.9238795325112869605, 1.000000000000000000, 0.9238795325112869605, 1.000000000000000000, 0.9238795325112869605, 1.000000000000000000, 0.9238795325112869605, 1.000000000000000000, 0.9238795325112869605, 1.000000000000000000, 0.9238795325112869605, 1.000000000000000000, 0.9238795325112869605, 1.000000000000000000, 0.9238795325112869605, 1.000000000000000000, 0.9238795325112869605, 1.000000000000000000, 0.9238795325112869605, 1.000000000000000000, 0.9238795325112869605, 1.000000000000000000, 0.9238795325112869605, 1.000000000000000000, 0.9238795325112869605, 1.000000000000000000, 0.9238795325112869605, 1.000000000000000000, 0.9238795325112869605, 1.000000000000000000, 0.9238795325112869605, 1.000000000000000000, 0.9238795325112869605, 1.000000000000000000, 0.9238795325112869605, 1.000000000000000000, 0.9238795325112869605, 1.000000000000000000, 0.9238795325112869605, 1.000000000000000000, 0.9238795325112869605, 1.000000000000000000, 0.9238795325112869605, 1.000000000000000000, 0.9238795325112869605, 1.000000000000000000, 0.9238795325112869605, 1.000000000000000000, 0.9238795325112869605, 1.000000000000000000, 0.9238795325112869605, 1.000000000000000000, 0.9238795325112869605, 1.000000000000000000, 0.9238795325112869605, 1.000000000000000000, 0.9238795325112869605, 1.000000000000000000, 0.9238795325112869605, 1.000000000000000000, 0.9238795325112869605, 1.000000000000000000, 0.9238795325112869605, 1.000000000000000000, 0.9238795325112869605, 1.000000000000000000, 0.9238795325112869605, 1.000000000000000000, 0.9238795325112869605, 1.000000000000000000, 0.9238795325112869605, 1.000000000000000000, 0.9238795325112869605, 1.000000000000000000, 0.9238795325112869605, 1.000000000000000000, 0.9238795325112869605, 1.000000000000000000, 0.9238795325112869605, 1.000000000000000000, 0.9238795325112869605, 1.000000000000000000, 0.9238795325112869605, 1.000000000000000000, 0.9238795325112869605, 1.000000000000000000, 0.9238795325112869605, 1.000000000000000000, 0.9238795325112869605, 1.000000000000000000, 0.9238795325112869605, 1.000000000000000000, 0.9238795325112869605, 1.000000000000000000, 0.9238795325112869605, 1.000000000000000000, 0.9238795325112869605, 1.000000000000000000, 0.9238795325112869605, 1.000000000000000000, 0.9238795325112869605, 1.000000000000000000, 0.9238795325112869605, 1.000000000000000000, 0.9238795325112869605, 1.000000000000000000, 0.9238795325112869605, 1.000000000000000000, 0.9238795325112869605, 1.000000000000000000, 0.9238795325112869605, 1.000000000000000000, 0.9238795325112869605, 1.000000000000000000, 0.9238795325112869605, 1.000000000000000000, 0.9238795325112869605, 1.000000000000000000, 0.9238795325112869605, 1.000000000000000000, 0.9238795325112869605, 1.000000000000000000, 0.9238795325112869605, 1.000000000000000000, 0.9238795325112869605, 1.000000000000000000, 0.9238795325112869605, 1.000000000000000000, 0.9238795325112869605, 1.000000000000000000, 0.9238795325112869605, 1.000000000000000000, 0.9238795325112869605, 1.000000000000000000, 0.9238795325112869605, 1.000000000000000000, 0.9238795325112869605, 1.000000000000000000, 0.9238795325112869605, 1.000000000000000000, 0.9238795325112869605, 1.000000000000000000, 0.9238795325112869605, 1.000000000000000000, 0.9238795325112869605, 1.000000000000000000, 0.9238795325112869605, 1.000000000000000000, 0.9238795325112869605, 1.000000000000000000, 0.9238795325112869605, 1.000000000000000000, 0.9238795325112869605, 1.000000000000000000, 0.9238795325112869605, 1.000000000000000000, 0.9238795325112869605, 1.000000000000000000, 0.9238795325112869605, 1.000000000000000000, 0.9238795325112869605, 1.000000000000000000, 0.9238795325112869605, 1.000000000000000000, 0.9238795325112869605, 1.000000000000000000, 0.9238795325112869605, 1.000000000000000000, 0.9238795325112869605, 1.000000000000000000, 0.9238795325112869605, 1.000000000000000000, 0.9238795325112869605, 1.000000000000000000, 0.9238795325112869605, 1.000000000000000000, 0.9238795325112869605, 1.000000000000000000, 0.9238795325112869605, 1.000000000000000000, 0.9238795325112869605, 1.000000000000000000, 0.9238795325112869605, 1.000000000000000000, 0.9238795325112869605, 1.000000000000000000, 0.9238795325112869605, 1.000000000000000000, 0.9238795325112869605, 1.000000000000000000, 0.9238795325112869605, 1.000000000000000000, 0.9238795325112869605, 1.000000000000000000, 0.9238795325112869605, 1.000000000000000000, 0.9238795325112869605, 1.000000000000000000, 0.9238795325112869605, 1.000000000000000000, 0.9238795325112869605, 1.000000000000000000, 0.9238795325112869605, 1.000000000000000000, 0.9238795325112869605, 1.000000000000000000, 0.9238795325112869605, 1.000000000000000000, 0.9238795325112869605, 1.000000000000000000, 0.9238795325112869605, 1.000000000000000000, 0.9238795325112869605, 1.000000000000000000, 0.9238795325112869605, 1.000000000000000000, 0.9238795325112869605, 1.000000000000000000, 0.9238795325112869605, 1.000000000000000000, 0.9238795325112869605, 1.000000000000000000, 0.9238795325112869605, 1.000000000000000000, 0.9238795325112869605, 1.000000000000000000, 0.9238795325112869605, 1.000000000000000000, 0.9238795325112869605, 1.000000000000000000, 0.9238795325112869605, 1.000000000000000000, 0.9238795325112869605, 1.000000000000000000, 0.9238795325112869605, 1.000000000000000000, 0.9238795325112869605, 1.000000000000000000, 0.9238795325112869605, 1.000000000000000000, 0.9238795325112869605, 1.000000000000000000, 0.9238795325112869605, 1.000000000000000000, 0.9238795325112869605, 1.000000000000000000, 0.9238795325112869605, 1.000000000000000000, 0.9238795325112869605, 1.000000000000000000, 0.9238795325112869605, 1.000000000000000000, 0.9238795325112869605, 1.000000000000000000, 0.9238795325112869605, 1.000000000000000000, 0.9238795325112869605, 1.000000000000000000, 0.9238795325112869605, 1.000000000000000000, 0.9238795325112869605, 1.000000000000000000, 0.9238795325112869605, 1.000000000000000000, 0.9238795325112869605, 1.000000000000000000, 0.9238795325112869605, 1.000000000000000000, 0.9238795325112869605, 1.000000000000000000, 0.9238795325112869605, 1.000000000000000000, 0.9238795325112869605, 1.000000000000000000, 0.9238795325112869605, 1.000000000000000000, 0.9238795325112869605, 1.000000000000000000, 0.9238795325112869605, 1.000000000000000000, 0.9238795325112869605, 1.000000000000000000, 0.9238795325112869605, 1.000000000000000000, 0.9238795325112869605, 1.000000000000000000, 0.9238795325112869605, 1.000000000000000000, 0.9238795325112869605, 1.000000000000000000, 0.9238795325112869605, 1.000000000000000000, 0.9238795325112869605, 1.000000000000000000, 0.9238795325112869605, 1.000000000000000000, 0.9238795325112869605, 1.000000000000000000, 0.9238795325112869605, 1.000000000000000000, 0.9238795325112869605, 1.000000000000000000, 0.9238795325112869605, 1.000000000000000000, 0.9238795325112869605, 1.000000000000000000, 0.9238795325112869605, 1.000000000000000000, 0.9238795325112869605, 1.000000000000000000, 0.9238795325112869605, 1.000000000000000000, 0.9238795325112869605, 1.000000000000000000, 0.9238795325112869605, 1.000000000000000000, 0.9238795325112869605, 1.000000000000000000, 0.9238795325112869605, 1.000000000000000000, 0.9238795325112869605, 1.000000000000000000, 0.9238795325112869605, 1.000000000000000000, 0.9238795325112869605, 1.000000000000000000),
 ( 1.000000000000000000, 0.9238795325112869605, 1.000000000000000000, 0.9238795325112869605, 1.000000000000000000, 0.9238795325112869605, 1.000000000000000000, 0.9238795325112869605, 1.000000000000000000, 0.9238795325112869605, 1.000000000000000000, 0.9238795325112869605, 1.000000000000000000, 0.9238795325112869605, 1.000000000000000000, 0.9238795325112869605, 1.000000000000000000, 0.9238795325112869605, 1.000000000000000000, 0.9238795325112869605, 1.000000000000000000, 0.9238795325112869605, 1.000000000000000000, 0.9238795325112869605, 1.000000000000000000, 0.9238795325112869605, 1.000000000000000000, 0.9238795325112869605, 1.000000000000000000, 0.9238795325112869605, 1.000000000000000000, 0.9238795325112869605, 1.000000000000000000, 0.9238795325112869605, 1.000000000000000000, 0.9238795325112869605, 1.000000000000000000, 0.9238795325112869605, 1.000000000000000000, 0.9238795325112869605, 1.000000000000000000, 0.9238795325112869605, 1.000000000000000000, 0.9238795325112869605, 1.000000000000000000, 0.9238795325112869605, 1.000000000000000000, 0.9238795325112869605, 1.000000000000000000, 0.9238795325112869605, 1.000000000000000000, 0.9238795325112869605, 1.000000000000000000, 0.9238795325112869605, 1.000000000000000000, 0.9238795325112869605, 1.000000000000000000, 0.9238795325112869605, 1.000000000000000000, 0.9238795325112869605, 1.000000000000000000, 0.9238795325112869605, 1.000000000000000000, 0.9238795325112869605, 1.000000000000000000, 0.9238795325112869605, 1.000000000000000000, 0.9238795325112869605, 1.000000000000000000, 0.9238795325112869605, 1.000000000000000000, 0.9238795325112869605, 1.000000000000000000, 0.9238795325112869605, 1.000000000000000000, 0.9238795325112869605, 1.000000000000000000, 0.9238795325112869605, 1.000000000000000000, 0.9238795325112869605, 1.000000000000000000, 0.9238795325112869605, 1.000000000000000000, 0.9238795325112869605, 1.000000000000000000, 0.9238795325112869605, 1.000000000000000000, 0.9238795325112869605, 1.000000000000000000, 0.9238795325112869605, 1.000000000000000000, 0.9238795325112869605, 1.000000000000000000, 0.9238795325112869605, 1.000000000000000000, 0.9238795325112869605, 1.000000000000000000, 0.9238795325112869605, 1.000000000000000000, 0.9238795325112869605, 1.000000000000000000, 0.9238795325112869605, 1.000000000000000000, 0.9238795325112869605, 1.000000000000000000, 0.9238795325112869605, 1.000000000000000000, 0.9238795325112869605, 1.000000000000000000, 0.9238795325112869605, 1.000000000000000000, 0.9238795325112869605, 1.000000000000000000, 0.9238795325112869605, 1.000000000000000000, 0.9238795325112869605, 1.000000000000000000, 0.9238795325112869605, 1.000000000000000000, 0.9238795325112869605, 1.000000000000000000, 0.9238795325112869605, 1.000000000000000000, 0.9238795325112869605, 1.000000000000000000, 0.9238795325112869605, 1.000000000000000000, 0.9238795325112869605, 1.000000000000000000, 0.9238795325112869605, 1.000000000000000000, 0.9238795325112869605, 1.000000000000000000, 0.9238795325112869605, 1.000000000000000000, 0.9238795325112869605, 1.000000000000000000, 0.9238795325112869605, 1.000000000000000000, 0.9238795325112869605, 1.000000000000000000, 0.9238795325112869605, 1.000000000000000000, 0.9238795325112869605, 1.000000000000000000, 0.9238795325112869605, 1.000000000000000000, 0.9238795325112869605, 1.000000000000000000, 0.9238795325112869605, 1.000000000000000000, 0.9238795325112869605, 1.000000000000000000, 0.9238795325112869605, 1.000000000000000000, 0.9238795325112869605, 1.000000000000000000, 0.9238795325112869605, 1.000000000000000000, 0.9238795325112869605, 1.000000000000000000, 0.9238795325112869605, 1.000000000000000000, 0.9238795325112869605, 1.000000000000000000, 0.9238795325112869605, 1.000000000000000000, 0.9238795325112869605, 1.000000000000000000, 0.9238795325112869605, 1.000000000000000000, 0.9238795325112869605, 1.000000000000000000, 0.9238795325112869605, 1.000000000000000000, 0.9238795325112869605, 1.000000000000000000, 0.9238795325112869605, 1.000000000000000000, 0.9238795325112869605, 1.000000000000000000, 0.9238795325112869605, 1.000000000000000000, 0.9238795325112869605, 1.000000000000000000, 0.9238795325112869605, 1.000000000000000000, 0.9238795325112869605, 1.000000000000000000, 0.9238795325112869605, 1.000000000000000000, 0.9238795325112869605, 1.000000000000000000, 0.9238795325112869605, 1.000000000000000000, 0.9238795325112869605, 1.000000000000000000, 0.9238795325112869605, 1.000000000000000000, 0.9238795325112869605, 1.000000000000000000, 0.9238795325112869605, 1.000000000000000000, 0.9238795325112869605, 1.000000000000000000, 0.9238795325112869605, 1.000000000000000000, 0.9238795325112869605, 1.000000000000000000, 0.9238795325112869605, 1.000000000000000000, 0.9238795325112869605, 1.000000000000000000, 0.9238795325112869605, 1.000000000000000000, 0.9238795325112869605, 1.000000000000000000, 0.9238795325112869605, 1.000000000000000000, 0.9238795325112869605, 1.000000000000000000, 0.9238795325112869605, 1.000000000000000000, 0.9238795325112869605, 1.000000000000000000, 0.9238795325112869605, 1.000000000000000000, 0.9238795325112869605, 1.000000000000000000, 0.9238795325112869605, 1.000000000000000000, 0.9238795325112869605, 1.000000000000000000, 0.9238795325112869605, 1.000000000000000000, 0.9238795325112869605, 1.000000000000000000, 0.9238795325112869605, 1.000000000000000000, 0.9238795325112869605, 1.000000000000000000, 0.9238795325112869605, 1.000000000000000000, 0.9238795325112869605, 1.000000000000000000, 0.9238795325112869605, 1.000000000000000000, 0.9238795325112869605, 1.000000000000000000, 0.9238795325112869605, 1.000000000000000000, 0.9238795325112869605, 1.000000000000000000, 0.9238795325112869605, 1.000000000000000000, 0.9238795325112869605, 1.000000000000000000, 0.9238795325112869605, 1.000000000000000000, 0.9238795325112869605, 1.000000000000000000, 0.9238795325112869605, 1.000000000000000000, 0.9238795325112869605, 1.000000000000000000, 0.9238795325112869605, 1.000000000000000000, 0.9238795325112869605, 1.000000000000000000, 0.9238795325112869605, 1.000000000000000000, 0.9238795325112869605, 1.000000000000000000, 0.9238795325112869605, 1.000000000000000000, 0.9238795325112869605, 1.000000000000000000, 0.9238795325112869605, 1.000000000000000000, 0.9238795325112869605, 1.000000000000000000, 0.9238795325112869605, 1.000000000000000000, 0.9238795325112869605, 1.000000000000000000, 0.9238795325112869605, 1.000000000000000000, 0.9238795325112869605, 1.000000000000000000, 0.9238795325112869605, 1.000000000000000000, 0.9238795325112869605, 1.000000000000000000, 0.9238795325112869605, 1.000000000000000000, 0.9238795325112869605, 1.000000000000000000, 0.9238795325112869605, 1.000000000000000000, 0.9238795325112869605, 1.000000000000000000, 0.9238795325112869605, 1.000000000000000000, 0.9238795325112869605, 1.000000000000000000, 0.9238795325112869605, 1.000000000000000000, 0.9238795325112869605, 1.000000000000000000, 0.9238795325112869605, 1.000000000000000000, 0.9238795325112869605, 1.000000000000000000, 0.9238795325112869605, 1.000000000000000000, 0.9238795325112869605, 1.000000000000000000, 0.9238795325112869605, 1.000000000000000000, 0.9238795325112869605, 1.000000000000000000, 0.9238795325112869605, 1.000000000000000000, 0.9238795325112869605, 1.000000000000000000, 0.9238795325112869605, 1.000000000000000000, 0.9238795325112869605, 1.000000000000000000, 0.9238795325112869605, 1.000000000000000000, 0.9238795325112869605, 1.000000000000000000, 0.9238795325112869605, 1.000000000000000000, 0.9238795325112869605, 1.000000000000000000, 0.9238795325112869605, 1.000000000000000000, 0.9238795325112869605, 1.000000000000000000, 0.9238795325112869605, 1.000000000000000000, 0.9238795325112869605, 1.000000000000000000, 0.9238795325112869605, 1.000000000000000000, 0.9238795325112869605, 1.000000000000000000, 0.9238795325112869605, 1.000000000000000000, 0.9238795325112869605, 1.000000000000000000, 0.9238795325112869605, 1.000000000000000000, 0.9238795325112869605, 1.000000000000000000, 0.9238795325112869605, 1.000000000000000000, 0.9238795325112869605, 1.000000000000000000, 0.9238795325112869605, 1.000000000000000000, 0.9238795325112869605, 1.000000000000000000, 0.9238795325112869605, 1.000000000000000000, 0.9238795325112869605, 1.000000000000000000, 0.9238795325112869605, 1.000000000000000000, 0.9238795325112869605, 1.000000000000000000, 0.9238795325112869605, 1.000000000000000000, 0.9238795325112869605, 1.000000000000000000, 0.9238795325112869605, 1.000000000000000000, 0.9238795325112869605, 1.000000000000000000, 0.9238795325112869605, 1.000000000000000000, 0.9238795325112869605, 1.000000000000000000, 0.9238795325112869605, 1.000000000000000000, 0.9238795325112869605, 1.000000000000000000, 0.9238795325112869605, 1.000000000000000000, 0.9238795325112869605, 1.000000000000000000, 0.9238795325112869605, 1.000000000000000000, 0.9238795325112869605, 1.000000000000000000, 0.9238795325112869605, 1.000000000000000000, 0.9238795325112869605, 1.000000000000000000, 0.9238795325112869605, 1.000000000000000000, 0.9238795325112869605, 1.000000000000000000, 0.9238795325112869605, 1.000000000000000000, 0.9238795325112869605, 1.000000000000000000, 0.9238795325112869605, 1.000000000000000000, 0.9238795325112869605, 1.000000000000000000, 0.9238795325112869605, 1.000000000000000000, 0.9238795325112869605, 1.000000000000000000, 0.9238795325112869605, 1.000000000000000000, 0.9238795325112869605, 1.000000000000000000, 0.9238795325112869605, 1.000000000000000000, 0.9238795325112869605, 1.000000000000000000, 0.9238795325112869605, 1.000000000000000000, 0.9238795325112869605, 1.000000000000000000, 0.9238795325112869605, 1.000000000000000000, 0.9238795325112869605, 1.000000000000000000, 0.9238795325112869605, 1.000000000000000000, 0.9238795325112869605, 1.000000000000000000, 0.9238795325112869605, 1.000000000000000000, 0.9238795325112869605, 1.000000000000000000, 0.9238795325112869605, 1.000000000000000000, 0.9238795325112869605, 1.000000000000000000, 0.9238795325112869605, 1.000000000000000000, 0.9238795325112869605, 1.000000000000000000, 0.9238795325112869605, 1.000000000000000000, 0.9238795325112869605, 1.000000000000000000, 0.9238795325112869605, 1.000000000000000000, 0.9238795325112869605, 1.000000000000000000, 0.9238795325112869605, 1.000000000000000000, 0.9238795325112869605, 1.000000000000000000, 0.9238795325112869605, 1.000000000000000000, 0.9238795325112869605, 1.000000000000000000, 0.9238795325112869605, 1.000000000000000000, 0.9238795325112869605, 1.000000000000000000, 0.9238795325112869605, 1.000000000000000000, 0.9238795325112869605, 1.000000000000000000, 0.9238795325112869605, 1.000000000000000000, 0.9238795325112869605, 1.000000000000000000, 0.9238795325112869605, 1.000000000000000000, 0.9238795325112869605, 1.000000000000000000, 0.9238795325112869605, 1.000000000000000000, 0.9238795325112869605, 1.000000000000000000, 0.9238795325112869605, 1.000000000000000000, 0.9238795325112869605, 1.000000000000000000, 0.9238795325112869605, 1.000000000000000000, 0.9238795325112869605, 1.000000000000000000, 0.9238795325112869605, 1.000000000000000000, 0.9238795325112869605, 1.000000000000000000, 0.9238795325112869605, 1.000000000000000000, 0.9238795325112869605, 1.000000000000000000, 0.9238795325112869605, 1.000000000000000000, 0.9238795325112869605, 1.000000000000000000, 0.9238795325112869605, 1.000000000000000000, 0.9238795325112869605, 1.000000000000000000, 0.9238795325112869605, 1.000000000000000000, 0.9238795325112869605, 1.000000000000000000, 0.9238795325112869605, 1.000000000000000000, 0.9238795325112869605, 1.000000000000000000, 0.9238795325112869605, 1.000000000000000000, 0.9238795325112869605, 1.000000000000000000, 0.9238795325112869605, 1.000000000000000000, 0.9238795325112869605, 1.000000000000000000, 0.9238795325112869605, 1.000000000000000000, 0.9238795325112869605, 1.000000000000000000, 0.9238795325112869605, 1.000000000000000000, 0.9238795325112869605, 1.000000000000000000, 0.9238795325112869605, 1.000000000000000000, 0.9238795325112869605, 1.000000000000000000, 0.9238795325112869605, 1.000000000000000000, 0.9238795325112869605, 1.000000000000000000, 0.9238795325112869605, 1.000000000000000000, 0.9238795325112869605, 1.000000000000000000, 0.9238795325112869605, 1.000000000000000000, 0.9238795325112869605, 1.000000000000000000, 0.9238795325112869605, 1.000000000000000000, 0.9238795325112869605, 1.000000000000000000, 0.9238795325112869605, 1.000000000000000000, 0.9238795325112869605, 1.000000000000000000, 0.9238795325112869605, 1.000000000000000000, 0.9238795325112869605, 1.000000000000000000, 0.9238795325112869605, 1.000000000000000000, 0.9238795325112869605, 1.000000000000000000, 0.9238795325112869605, 1.000000000000000000, 0.9238795325112869605, 1.000000000000000000, 0.9238795325112869605, 1.000000000000000000, 0.9238795325112869605, 1.000000000000000000, 0.9238795325112869605, 1.000000000000000000, 0.9238795325112869605, 1.000000000000000000, 0.9238795325112869605, 1.000000000000000000, 0.9238795325112869605, 1.000000000000000000, 0.9238795325112869605, 1.000000000000000000, 0.9238795325112869605, 1.000000000000000000, 0.9238795325112869605, 1.000000000000000000, 0.9238795325112869605, 1.000000000000000000, 0.9238795325112869605, 1.000000000000000000, 0.9238795325112869605, 1.000000000000000000, 0.9238795325112869605, 1.000000000000000000, 0.9238795325112869605, 1.000000000000000000, 0.9238795325112869605, 1.000000000000000000, 0.9238795325112869605, 1.000000000000000000, 0.9238795325112869605, 1.000000000000000000, 0.9238795325112869605, 1.000000000000000000, 0.9238795325112869605, 1.000000000000000000, 0.9238795325112869605, 1.000000000000000000, 0.9238795325112869605, 1.000000000000000000, 0.9238795325112869605, 1.000000000000000000, 0.9238795325112869605, 1.000000000000000000, 0.9238795325112869605, 1.000000000000000000, 0.9238795325112869605, 1.000000000000000000, 0.9238795325112869605, 1.000000000000000000, 0.9238795325112869605, 1.000000000000000000, 0.9238795325112869605, 1.000000000000000000, 0.9238795325112869605, 1.000000000000000000, 0.9238795325112869605, 1.000000000000000000, 0.9238795325112869605, 1.000000000000000000, 0.9238795325112869605, 1.000000000000000000, 0.9238795325112869605, 1.000000000000000000, 0.9238795325112869605, 1.000000000000000000, 0.9238795325112869605, 1.000000000000000000, 0.9238795325112869605, 1.000000000000000000, 0.9238795325112869605, 1.000000000000000000, 0.9238795325112869605, 1.000000000000000000, 0.9238795325112869605, 1.000000000000000000, 0.9238795325112869605, 1.000000000000000000, 0.9238795325112869605, 1.000000000000000000, 0.9238795325112869605, 1.000000000000000000, 0.9238795325112869605, 1.000000000000000000, 0.9238795325112869605, 1.000000000000000000, 0.9238795325112869605, 1.000000000000000000, 0.9238795325112869605, 1.000000000000000000, 0.9238795325112869605, 1.000000000000000000, 0.9238795325112869605, 1.000000000000000000, 0.9238795325112869605, 1.000000000000000000, 0.9238795325112869605, 1.000000000000000000, 0.9238795325112869605, 1.000000000000000000, 0.9238795325112869605, 1.000000000000000000, 0.9238795325112869605, 1.000000000000000000, 0.9238795325112869605, 1.000000000000000000, 0.9238795325112869605, 1.000000000000000000, 0.9238795325112869605, 1.000000000000000000, 0.9238795325112869605, 1.000000000000000000, 0.9238795325112869605, 1.000000000000000000, 0.9238795325112869605, 1.000000000000000000, 0.9238795325112869605, 1.000000000000000000, 0.9238795325112869605, 1.000000000000000000, 0.9238795325112869605, 1.000000000000000000, 0.9238795325112869605, 1.000000000000000000, 0.9238795325112869605, 1.000000000000000000, 0.9238795325112869605, 1.000000000000000000, 0.9238795325112869605, 1.000000000000000000, 0.9238795325112869605, 1.000000000000000000, 0.9238795325112869605, 1.000000000000000000, 0.9238795325112869605, 1.000000000000000000, 0.9238795325112869605, 1.000000000000000000, 0.9238795325112869605, 1.000000000000000000, 0.9238795325112869605, 1.000000000000000000, 0.9238795325112869605, 1.000000000000000000, 0.9238795325112869605, 1.000000000000000000, 0.9238795325112869605, 1.000000000000000000, 0.9238795325112869605, 1.000000000000000000, 0.9238795325112869605, 1.000000000000000000, 0.9238795325112869605, 1.000000000000000000, 0.9238795325112869605, 1.000000000000000000, 0.9238795325112869605, 1.000000000000000000, 0.9238795325112869605, 1.000000000000000000, 0.9238795325112869605, 1.000000000000000000, 0.9238795325112869605, 1.000000000000000000, 0.9238795325112869605, 1.000000000000000000, 0.9238795325112869605, 1.000000000000000000, 0.9238795325112869605, 1.000000000000000000, 0.9238795325112869605, 1.000000000000000000, 0.9238795325112869605, 1.000000000000000000, 0.9238795325112869605, 1.000000000000000000, 0.9238795325112869605, 1.000000000000000000, 0.9238795325112869605, 1.000000000000000000, 0.9238795325112869605, 1.000000000000000000, 0.9238795325112869605, 1.000000000000000000, 0.9238795325112869605, 1.000000000000000000, 0.9238795325112869605, 1.000000000000000000, 0.9238795325112869605, 1.000000000000000000, 0.9238795325112869605, 1.000000000000000000, 0.9238795325112869605, 1.000000000000000000, 0.9238795325112869605, 1.000000000000000000, 0.9238795325112869605, 1.000000000000000000, 0.9238795325112869605, 1.000000000000000000, 0.9238795325112869605, 1.000000000000000000, 0.9238795325112869605, 1.000000000000000000, 0.9238795325112869605, 1.000000000000000000, 0.9238795325112869605, 1.000000000000000000, 0.9238795325112869605, 1.000000000000000000, 0.9238795325112869605, 1.000000000000000000, 0.9238795325112869605, 1.000000000000000000, 0.9238795325112869605, 1.000000000000000000, 0.9238795325112869605, 1.000000000000000000, 0.9238795325112869605, 1.000000000000000000, 0.9238795325112869605, 1.000000000000000000, 0.9238795325112869605, 1.000000000000000000, 0.9238795325112869605, 1.000000000000000000, 0.9238795325112869605, 1.000000000000000000, 0.9238795325112869605, 1.000000000000000000) ) ) 
 REPRESENTATION_ITEM ( '' )  SURFACE ( )  ) ;
#34985=CARTESIAN_POINT ( 'NONE',  ( -0.6971942568897648851, -0.07405724077823297447, 1.860236220418677089 ) ) ;
#34988=CARTESIAN_POINT ( 'NONE',  ( -0.8019270111902717657, -0.1787899950787401604, 1.466535433017102763 ) ) ;
#34991=CARTESIAN_POINT ( 'NONE',  ( -1.002407869896990045, 0.1264236179284866091, 0.3075787401037169411 ) ) ;
#34992=CARTESIAN_POINT ( 'NONE',  ( 0.8107537697050254399, -0.1574803149606297803, 1.572342519685040907 ) ) ;
#34993=CARTESIAN_POINT ( 'NONE',  ( -1.054774247047244540, -0.07405724077823318263, 1.756889763725764553 ) ) ;
#34995=CARTESIAN_POINT ( 'NONE',  ( -0.8107537697050253289, 0.1574803149606300301, 1.715059055118110631 ) ) ;
#34998=CARTESIAN_POINT ( 'NONE',  ( 0.7495606340400177148, 0.1264236179284866091, 1.695374015694267822 ) ) ;
#35002=ORIENTED_EDGE ( 'NONE', *, *, #38271, .F. ) ;
#35003=CARTESIAN_POINT ( 'NONE',  ( -0.9500414927467377701, 0.1787899950787401604, 1.294291338528913204 ) ) ;
#35006=CARTESIAN_POINT ( 'NONE',  ( -1.033464566929134687, 0.06523048226347956391, 1.272145669291338432 ) ) ;
#35009=CARTESIAN_POINT ( 'NONE',  ( -0.9412147342319837628, 0.1574803149606300301, 0.7947834644594014009 ) ) ;
#35010=CARTESIAN_POINT ( 'NONE',  ( -1.033464566929134687, 0.06523048226347956391, 0.7997047244094482865 ) ) ;
#35012=CARTESIAN_POINT ( 'NONE',  ( 0.6971942568897626646, 0.07405724077823318263, 0.9448818897100165204 ) ) ;
#35014=CARTESIAN_POINT ( 'NONE',  ( 1.054774247047244096, 0.000000000000000000, 1.956200787347811110 ) ) ;
#35016=CARTESIAN_POINT ( 'NONE',  ( -0.8107537697050254399, -0.1574803149606297803, 1.178641732283464583 ) ) ;
#35022=CARTESIAN_POINT ( 'NONE',  ( 0.7495606340400177148, -0.1264236179284866091, 0.3272637794737956463 ) ) ;
#35024=CARTESIAN_POINT ( 'NONE',  ( -0.8759842519685039353, 0.1787899950787401882, 1.921751968450173376 ) ) ;
#35025=ORIENTED_EDGE ( 'NONE', *, *, #45633, .F. ) ;
#35026=CARTESIAN_POINT ( 'NONE',  ( -0.6971942568897648851, 0.07405724077823318263, 1.461614173174583753 ) ) ;
#35027=CARTESIAN_POINT ( 'NONE',  ( 0.6971942568897648851, 0.07405724077823318263, 1.382874015694268044 ) ) ;
#35028=CARTESIAN_POINT ( 'NONE',  ( -0.7646288533564489232, -0.1113553986120547346, 0.9005905511811023167 ) ) ;
#35029=CARTESIAN_POINT ( 'NONE',  ( -0.6971942568897626646, 0.07405724077823318263, 0.7135826771115916234 ) ) ;
#35030=CARTESIAN_POINT ( 'NONE',  ( -0.7495606340400177148, -0.1264236179284866091, 1.149114173174582643 ) ) ;
#35031=DIRECTION ( 'NONE',  ( 1.000000000000000000, 0.000000000000000000, -1.822029033848725275E-16 ) ) ;
#35033=CARTESIAN_POINT ( 'NONE',  ( 0.6971942568897637749, 2.189545951927499583E-17, 0.5585629920722204877 ) ) ;
#35034=EDGE_CURVE ( 'NONE', #35490, #22163, #16644, .T. ) ;
#35041=CARTESIAN_POINT ( 'NONE',  ( -0.9412147342319837628, -0.1574803149606297803, 0.2386811023622048278 ) ) ;
#35042=CARTESIAN_POINT ( 'NONE',  ( 1.002407869896990045, -0.1264236179284866091, 1.360728346402929168 ) ) ;
#35044=CARTESIAN_POINT ( 'NONE',  ( -1.033464566929133799, 0.000000000000000000, 1.850393700679873854 ) ) ;
#35046=CARTESIAN_POINT ( 'NONE',  ( -1.033464566929133799, 0.000000000000000000, 0.6397637795275591399 ) ) ;
#35047=CARTESIAN_POINT ( 'NONE',  ( -0.7495606340400177148, 0.1264236179284866091, 1.026082677111590513 ) ) ;
#35053=CARTESIAN_POINT ( 'NONE',  ( 0.7495606340400177148, 0.1264236179284866091, 1.414862204670645829 ) ) ;
#35062=CARTESIAN_POINT ( 'NONE',  ( 0.7495606340400177148, 0.1264236179284866091, 0.5093503936470236138 ) ) ;
#35063=CARTESIAN_POINT ( 'NONE',  ( -0.8019270111902716547, 0.1787899950787401604, 0.8661417322297002563 ) ) ;
#35066=CARTESIAN_POINT ( 'NONE',  ( 0.7185039370078739607, 1.928577636452523993E-17, 0.09842519674286673292 ) ) ;
#35068=CARTESIAN_POINT ( 'NONE',  ( -0.8490223526853721836, -0.1715985158898769847, 1.987713034038145477 ) ) ;
#35069=CARTESIAN_POINT ( 'NONE',  ( -0.7185039370078739607, 1.928577636452523993E-17, 1.240157480207432883 ) ) ;
#35070=CARTESIAN_POINT ( 'NONE',  ( 0.6971942568897648851, -0.07405724077823297447, 1.584645669237574994 ) ) ;
#35072=CARTESIAN_POINT ( 'NONE',  ( -0.7185039370078746268, -0.06523048226347956391, 1.803641732283465471 ) ) ;
#35073=CARTESIAN_POINT ( 'NONE',  ( 0.7495606340400177148, 0.1264236179284866091, 0.3912401574265515491 ) ) ;
#35077=CARTESIAN_POINT ( 'NONE',  ( 1.033464566929134687, -0.06523048226347956391, 0.8636811022546768690 ) ) ;
#35078=DIRECTION ( 'NONE',  ( 0.000000000000000000, 0.000000000000000000, -1.000000000000000000 ) ) ;
#35081=CARTESIAN_POINT ( 'NONE',  ( 0.9412147342319837628, -0.1574803149606297803, 0.5044291337507409434 ) ) ;
#35083=CARTESIAN_POINT ( 'NONE',  ( 0.8019270111902717657, -0.1787899950787401604, 0.4429133857730075952 ) ) ;
#35085=CARTESIAN_POINT ( 'NONE',  ( 0.7925511340933090176, -0.1404228911275084979, 0.03937002898646041471 ) ) ;
#35086=CYLINDRICAL_SURFACE ( 'NONE', #20831, 0.1574803149606299191 ) ;
#35089=CARTESIAN_POINT ( 'NONE',  ( 0.7495606340400177148, -0.1264236179284866091, 1.035925196796629866 ) ) ;
#35092=CARTESIAN_POINT ( 'NONE',  ( -0.8759842519685039353, -0.1574803149606299191, 0.5019685038294811052 ) ) ;
#35093=CARTESIAN_POINT ( 'NONE',  ( 0.8759842519685039353, 0.1787899950787401882, 1.724901574749385880 ) ) ;
#35094=CARTESIAN_POINT ( 'NONE',  ( -0.7185039370078739607, 1.928577636452523993E-17, 1.407480314960629864 ) ) ;
#35098=CARTESIAN_POINT ( 'NONE',  ( 0.9500414927467377701, -0.1787899950787401604, 0.2165354330171024577 ) ) ;
#35099=CARTESIAN_POINT ( 'NONE',  ( -0.7495606340400177148, -0.1264236179284866091, 0.1254921259304885850 ) ) ;
#35100=CARTESIAN_POINT ( 'NONE',  ( 0.7185039370078739607, 1.928577636452523993E-17, 1.358267716427907779 ) ) ;
#35102=ORIENTED_EDGE ( 'NONE', *, *, #8645, .T. ) ;
#35107=CARTESIAN_POINT ( 'NONE',  ( -1.054774247047244096, 0.000000000000000000, 1.636318897584031484 ) ) ;
#35112=CARTESIAN_POINT ( 'NONE',  ( 0.7185039370078766252, -0.06523048226348168721, 1.596948818790109970 ) ) ;
#35117=EDGE_LOOP ( 'NONE', ( #24182, #283, #16195, #26791 ) ) ;
#35118=CARTESIAN_POINT ( 'NONE',  ( -0.9412147342319837628, -0.1574803149606297803, 1.409940944774363603 ) ) ;
#35120=CARTESIAN_POINT ( 'NONE',  ( 0.7185039370078746268, 0.06523048226347956391, 1.877460629921260393 ) ) ;
#35122=EDGE_CURVE ( 'NONE', #40732, #46518, #1995, .T. ) ;
#35123=EDGE_LOOP ( 'NONE', ( #41789, #4513, #13583, #2416 ) ) ;
#35125=CARTESIAN_POINT ( 'NONE',  ( -1.002407869896990045, -0.1264236179284866091, 0.3764763778989925203 ) ) ;
#35126=CARTESIAN_POINT ( 'NONE',  ( -0.7185039370078746268, -0.06523048226347956391, 1.016240157480315487 ) ) ;
#35129=DIRECTION ( 'NONE',  ( -1.000000000000000000, 0.000000000000000000, 0.000000000000000000 ) ) ;
#35130=CARTESIAN_POINT ( 'NONE',  ( 0.9500414927467378812, -0.1787899950787401604, 1.122047244040725644 ) ) ;
#35131=CARTESIAN_POINT ( 'NONE',  ( 1.054774247047244540, -0.07405724077823318263, 1.594488188922615457 ) ) ;
#35132=CARTESIAN_POINT ( 'NONE',  ( 0.8019270111902716547, 0.1787899950787401604, 0.1919291338045042705 ) ) ;
#35135=CARTESIAN_POINT ( 'NONE',  ( 0.7646288533564489232, -0.1113553986120547346, 0.2312992125984252023 ) ) ;
#35136=CARTESIAN_POINT ( 'NONE',  ( 0.7185039370078746268, -0.06523048226347956391, 1.646161417322835385 ) ) ;
#35137=CARTESIAN_POINT ( 'NONE',  ( 0.7717440911643036472, 0.1232935613849624051, 1.980556353253522861 ) ) ;
#35141=CARTESIAN_POINT ( 'NONE',  ( 0.8759842519685039353, 0.1787899950787401882, 1.016240157426551161 ) ) ;
#35142=CARTESIAN_POINT ( 'NONE',  ( 0.7495606340400177148, -0.1264236179284866091, 1.980807086560409491 ) ) ;
#35143=CARTESIAN_POINT ( 'NONE',  ( 1.033464566929133799, 0.000000000000000000, 0.3543307085538902057 ) ) ;
#35146=CARTESIAN_POINT ( 'NONE',  ( -0.9873396505805591694, 0.1113553986120547346, 0.2017716534357799352 ) ) ;
#35148=CARTESIAN_POINT ( 'NONE',  ( 1.002407869896990045, -0.1264236179284866091, 1.355807086560409491 ) ) ;
#35150=CARTESIAN_POINT ( 'NONE',  ( 0.9873396505805591694, -0.1113553986120547346, 0.07381889753026830980 ) ) ;
#35157=ORIENTED_EDGE ( 'NONE', *, *, #14833, .T. ) ;
#35158=CARTESIAN_POINT ( 'NONE',  ( -0.9500414927467377701, 0.1787899950787401604, 1.328740157426552049 ) ) ;
#35160=CARTESIAN_POINT ( 'NONE',  ( -1.054774247047244096, 0.000000000000000000, 1.011318897584031484 ) ) ;
#35161=CARTESIAN_POINT ( 'NONE',  ( -1.054774247047244540, -0.07405724077823318263, 1.909448818843873186 ) ) ;
#35164=CARTESIAN_POINT ( 'NONE',  ( -0.8759842519685039353, -0.1787899950787401882, 0.6471456692375747721 ) ) ;
#35173=CARTESIAN_POINT ( 'NONE',  ( -0.6971942568897626646, -0.07405724077823297447, 0.6742125983714335469 ) ) ;
#35174=CARTESIAN_POINT ( 'NONE',  ( -1.033464566929133799, 0.000000000000000000, 0.9153543307086614567 ) ) ;
#35176=CARTESIAN_POINT ( 'NONE',  ( -0.9500414927467377701, -0.1787899950787401604, 1.673228346402929834 ) ) ;
#35181=CARTESIAN_POINT ( 'NONE',  ( 0.9873396505805591694, 0.1113553986120547346, 0.6446850393700788162 ) ) ;
#35182=ORIENTED_EDGE ( 'NONE', *, *, #30403, .T. ) ;
#35188=CARTESIAN_POINT ( 'NONE',  ( -0.8107537697050254399, 0.1574803149606300301, 1.193405511703496957 ) ) ;
#35190=EDGE_CURVE ( 'NONE', #17345, #38222, #7961, .T. ) ;
#35193=CARTESIAN_POINT ( 'NONE',  ( 0.9873396505805591694, -0.1113553986120547346, 1.146653543307086798 ) ) ;
#35194=CARTESIAN_POINT ( 'NONE',  ( -0.7185039370078739607, 1.928577636452523993E-17, 1.279527558947590515 ) ) ;
#35196=VECTOR ( 'NONE', #4228, 39.37007874015748143 ) ;
#35197=CARTESIAN_POINT ( 'NONE',  ( 1.033464566929133799, 0.000000000000000000, 1.978346456692913646 ) ) ;
#35198=CARTESIAN_POINT ( 'NONE',  ( 0.7185039370078739607, 1.928577636452523993E-17, 0.1870078740157480324 ) ) ;
#35200=DIRECTION ( 'NONE',  ( 1.000000000000000000, 0.000000000000000000, -4.336808689942015271E-16 ) ) ;
#35203=DIRECTION ( 'NONE',  ( 0.000000000000000000, 0.000000000000000000, -1.000000000000000000 ) ) ;
#35208=CARTESIAN_POINT ( 'NONE',  ( 0.8019270111902717657, -0.1787899950787401604, 0.7972440944344250102 ) ) ;
#35214=CARTESIAN_POINT ( 'NONE',  ( 0.9873396505805591694, -0.1113553986120547346, 1.215551180994834723 ) ) ;
#35217=CARTESIAN_POINT ( 'NONE',  ( -0.6971942568897648851, 0.07405724077823318263, 1.934055118056471567 ) ) ;
#35218=CARTESIAN_POINT ( 'NONE',  ( 1.054774247047244096, 0.000000000000000000, 1.995570866087968520 ) ) ;
#35223=CARTESIAN_POINT ( 'NONE',  ( -0.8759842519685039353, 0.1787899950787401882, 1.528051181048598384 ) ) ;
#35226=CARTESIAN_POINT ( 'NONE',  ( -1.054774247047244096, 0.000000000000000000, 0.9670275590013542866 ) ) ;
#35227=CARTESIAN_POINT ( 'NONE',  ( -1.054774247047244540, -0.07405724077823318263, 0.2214566928596220785 ) ) ;
#35229=CARTESIAN_POINT ( 'NONE',  ( -0.7646288533564489232, 0.1113553986120547346, 0.5757874015748032370 ) ) ;
#35230=CARTESIAN_POINT ( 'NONE',  ( -0.9500414927467378812, 0.1787899950787401604, 1.924212598371433325 ) ) ;
#35231=CARTESIAN_POINT ( 'NONE',  ( -0.8019270111902717657, -0.1787899950787401604, 0.1328740156942679607 ) ) ;
#35233=CARTESIAN_POINT ( 'NONE',  ( -0.9412147342319837628, 0.1574803149606300301, 1.788877952755905332 ) ) ;
#35234=FACE_OUTER_BOUND ( 'NONE', #40240, .T. ) ;
#35240=( BOUNDED_CURVE ( )  B_SPLINE_CURVE ( 2, ( #18971, #27153, #4338, #8908, #37915, #12764, #23054, #37674, #4826 ),
 .UNSPECIFIED., .F., .T. ) 
 B_SPLINE_CURVE_WITH_KNOTS ( ( 3, 2, 2, 2, 3 ),
 ( 0.000000000000000000, 0.002500000000000000052, 0.005000000000000000104, 0.007499999999999998855, 0.01000000000000000021 ),
 .UNSPECIFIED. ) 
 CURVE ( )  GEOMETRIC_REPRESENTATION_ITEM ( )  RATIONAL_B_SPLINE_CURVE ( ( 1.000000000000000000, 0.9238795325112869605, 1.000000000000000000, 0.9238795325112869605, 1.000000000000000000, 0.9238795325112869605, 1.000000000000000000, 0.9238795325112869605, 1.000000000000000000 ) ) 
 REPRESENTATION_ITEM ( '' )  ) ;
#35241=VERTEX_POINT ( 'NONE', #15176 ) ;
#35245=EDGE_CURVE ( 'NONE', #13881, #33816, #29819, .T. ) ;
#35249=CARTESIAN_POINT ( 'NONE',  ( -0.7185039370078739607, 1.928577636452523993E-17, 0.7677165353255432922 ) ) ;
#35250=CARTESIAN_POINT ( 'NONE',  ( -0.7185039370078739607, 1.928577636452523993E-17, 0.6594488188976378451 ) ) ;
#35253=CARTESIAN_POINT ( 'NONE',  ( 0.8019270111902717657, -0.1787899950787401604, 0.9153543306548987957 ) ) ;
#35255=( BOUNDED_CURVE ( )  B_SPLINE_CURVE ( 2, ( #47330, #14501, #39638, #36323, #32259, #6587, #10202, #40115, #21928 ),
 .UNSPECIFIED., .F., .T. ) 
 B_SPLINE_CURVE_WITH_KNOTS ( ( 3, 2, 2, 2, 3 ),
 ( 0.2500000000000000000, 0.2525000000000000022, 0.2550000000000000044, 0.2575000000000000067, 0.2600000000000000089 ),
 .UNSPECIFIED. ) 
 CURVE ( )  GEOMETRIC_REPRESENTATION_ITEM ( )  RATIONAL_B_SPLINE_CURVE ( ( 1.000000000000000000, 0.9238795325112869605, 1.000000000000000000, 0.9238795325112869605, 1.000000000000000000, 0.9238795325112869605, 1.000000000000000000, 0.9238795325112869605, 1.000000000000000000 ) ) 
 REPRESENTATION_ITEM ( '' )  ) ;
#35257=CARTESIAN_POINT ( 'NONE',  ( 0.9412147342319837628, 0.1574803149606300301, 0.6077755905511815770 ) ) ;
#35259=CARTESIAN_POINT ( 'NONE',  ( 0.9412147342319837628, -0.1574803149606297803, 1.094980314853103653 ) ) ;
#35260=CARTESIAN_POINT ( 'NONE',  ( 1.033464566929133799, 0.000000000000000000, 0.03937007863263043694 ) ) ;
#35267=CARTESIAN_POINT ( 'NONE',  ( -0.9500414927467378812, 0.1787899950787401604, 1.840551181048599938 ) ) ;
#35269=CARTESIAN_POINT ( 'NONE',  ( -0.9500414927467378812, 0.1787899950787401604, 1.491141732229701367 ) ) ;
#35270=CARTESIAN_POINT ( 'NONE',  ( 0.8019270111902717657, -0.1787899950787401604, 1.432086614119464141 ) ) ;
#35271=CARTESIAN_POINT ( 'NONE',  ( -0.7185039370078746268, -0.06523048226347956391, 0.8981299212598432558 ) ) ;
#35272=CARTESIAN_POINT ( 'NONE',  ( -0.6971942568897626646, -0.07405724077823297447, 0.7185039369541108556 ) ) ;
#35274=CARTESIAN_POINT ( 'NONE',  ( -0.9873396505805591694, 0.1113553986120547346, 1.619094488081448846 ) ) ;
#35275=CARTESIAN_POINT ( 'NONE',  ( -0.9500414927467377701, -0.1787899950787401604, 0.6053149605761580787 ) ) ;
#35276=EDGE_CURVE ( 'NONE', #47215, #16187, #18687, .T. ) ;
#35278=CARTESIAN_POINT ( 'NONE',  ( -1.033464566929133799, 0.000000000000000000, 0.3248031496062992463 ) ) ;
#35280=CARTESIAN_POINT ( 'NONE',  ( -0.8759842519685039353, 0.1787899950787401882, 1.493602362150960650 ) ) ;
#35282=CARTESIAN_POINT ( 'NONE',  ( -0.9412147342319837628, -0.1574803149606297803, 0.5142716535433068392 ) ) ;
#35283=CARTESIAN_POINT ( 'NONE',  ( 0.8019270111902716547, 0.1787899950787401604, 1.259842519631276359 ) ) ;
#35286=FACE_OUTER_BOUND ( 'NONE', #33116, .T. ) ;
#35287=CARTESIAN_POINT ( 'NONE',  ( -0.6971942568897648851, -0.07405724077823297447, 1.033464566875371027 ) ) ;
#35288=ORIENTED_EDGE ( 'NONE', *, *, #23784, .T. ) ;
#35290=VERTEX_POINT ( 'NONE', #41000 ) ;
#35292=LINE ( 'NONE', #21115, #37669 ) ;
#35298=DIRECTION ( 'NONE',  ( 0.000000000000000000, 0.000000000000000000, -1.000000000000000000 ) ) ;
#35304=ADVANCED_FACE ( 'NONE', ( #15885 ), #8662, .T. ) ;
#35305=CARTESIAN_POINT ( 'NONE',  ( 1.002407869896990045, -0.1264236179284866091, 0.5290354330171024300 ) ) ;
#35306=CARTESIAN_POINT ( 'NONE',  ( -0.8759842519685039353, -0.1787899950787401882, 0.8439960629383622681 ) ) ;
#35308=DIRECTION ( 'NONE',  ( 1.822029033848725028E-16, 0.000000000000000000, 1.000000000000000000 ) ) ;
#35310=CARTESIAN_POINT ( 'NONE',  ( -0.7244611917879343332, -0.07363402883329660253, 1.984689699691266851 ) ) ;
#35311=CARTESIAN_POINT ( 'NONE',  ( 1.054774247047244540, 0.07405724077823318263, 1.446850393647023614 ) ) ;
#35313=DIRECTION ( 'NONE',  ( 1.822029033848725028E-16, 0.000000000000000000, 1.000000000000000000 ) ) ;
#35314=CARTESIAN_POINT ( 'NONE',  ( 0.7495606340400177148, -0.1264236179284866091, 0.3223425196312759144 ) ) ;
#35318=CARTESIAN_POINT ( 'NONE',  ( 0.8759842519685039353, -0.1574803149606299191, 0.8562992124908976876 ) ) ;
#35320=CARTESIAN_POINT ( 'NONE',  ( 0.8759842519685039353, -0.1787899950787401882, 0.6028543306548976854 ) ) ;
#35322=CARTESIAN_POINT ( 'NONE',  ( 0.7606907602897685639, -0.1191966515041183866, 0.03937009332876739015 ) ) ;
#35323=CARTESIAN_POINT ( 'NONE',  ( -1.033464566929133799, 0.000000000000000000, 0.9448818896562519720 ) ) ;
#35325=CARTESIAN_POINT ( 'NONE',  ( -0.8759842519685039353, 0.1787899950787401882, 1.488681102308440751 ) ) ;
#35326=EDGE_LOOP ( 'NONE', ( #45547, #20857, #19632, #27380 ) ) ;
#35328=CARTESIAN_POINT ( 'NONE',  ( 1.002407869896990045, 0.1264236179284866091, 0.9768700786863937502 ) ) ;
#35329=ORIENTED_EDGE ( 'NONE', *, *, #16209, .F. ) ;
#35332=CARTESIAN_POINT ( 'NONE',  ( -0.9500414927467378812, 0.1787899950787401604, 0.8956692912848198684 ) ) ;
#35335=CARTESIAN_POINT ( 'NONE',  ( 0.7495606340400177148, 0.1264236179284866091, 0.08120078734781142893 ) ) ;
#35336=CARTESIAN_POINT ( 'NONE',  ( -0.8759842519685039353, 0.1787899950787401882, 0.1107283464029295283 ) ) ;
#35338=CARTESIAN_POINT ( 'NONE',  ( 0.8759842519685039353, 0.1574803149606299191, 1.348425196742866206 ) ) ;
#35341=CARTESIAN_POINT ( 'NONE',  ( -1.002407869896990045, -0.1264236179284866091, 1.749507873961984483 ) ) ;
#35344=CARTESIAN_POINT ( 'NONE',  ( -0.9412147342319837628, -0.1574803149606297803, 0.7898622047244097111 ) ) ;
#35346=ORIENTED_EDGE ( 'NONE', *, *, #47454, .T. ) ;
#35349=EDGE_CURVE ( 'NONE', #2870, #36693, #8898, .T. ) ;
#35354=CARTESIAN_POINT ( 'NONE',  ( 0.7185039370078739607, 1.928577636452523993E-17, 1.801181102362204633 ) ) ;
#35356=AXIS2_PLACEMENT_3D ( 'NONE', #26932, #1485, #4364 ) ;
#35359=CARTESIAN_POINT ( 'NONE',  ( -0.6971942568897637749, 2.189545951927499583E-17, 0.2829724408911185041 ) ) ;
#35360=CARTESIAN_POINT ( 'NONE',  ( -0.8107537697050253289, 0.1574803149606300301, 1.085137795275590955 ) ) ;
#35363=CARTESIAN_POINT ( 'NONE',  ( 1.002407869896990045, -0.1264236179284866091, 1.045767716481669440 ) ) ;
#35364=CARTESIAN_POINT ( 'NONE',  ( 0.6971942568897648851, 0.07405724077823318263, 1.535433070812378675 ) ) ;
#35365=CARTESIAN_POINT ( 'NONE',  ( 1.054774247047244540, -0.07405724077823318263, 0.1771653542769450751 ) ) ;
#35367=CARTESIAN_POINT ( 'NONE',  ( 0.7185039370078746268, -0.06523048226347956391, 1.685531496062990797 ) ) ;
#35371=CARTESIAN_POINT ( 'NONE',  ( -0.7185039370078746268, 0.06523048226347956391, 1.670767716427906002 ) ) ;
#35373=CARTESIAN_POINT ( 'NONE',  ( 1.054774247047244540, -0.07405724077823318263, 1.161417322780881278 ) ) ;
#35374=FACE_OUTER_BOUND ( 'NONE', #41931, .T. ) ;
#35375=CARTESIAN_POINT ( 'NONE',  ( -0.8759842519685039353, 0.1787899950787401882, 1.134350393647023614 ) ) ;
#35376=CARTESIAN_POINT ( 'NONE',  ( 0.8759842519685039353, -0.1574803149606299191, 0.4232283463491653963 ) ) ;
#35377=ORIENTED_EDGE ( 'NONE', *, *, #33363, .F. ) ;
#35379=CARTESIAN_POINT ( 'NONE',  ( 0.9412147342319837628, 0.1574803149606300301, 0.2534448818897637734 ) ) ;
#35381=CARTESIAN_POINT ( 'NONE',  ( -0.7646288533564489232, 0.1113553986120547346, 0.2903543306011346359 ) ) ;
#35383=CARTESIAN_POINT ( 'NONE',  ( 0.6971942568897648851, -0.07405724077823297447, 1.225393700733637514 ) ) ;
#35384=DIRECTION ( 'NONE',  ( 1.000000000000000000, 0.000000000000000000, -4.336808689942015271E-16 ) ) ;
#35385=CARTESIAN_POINT ( 'NONE',  ( 0.7185039370078746268, -0.06523048226347956391, 0.06151574792396910518 ) ) ;
#35388=CARTESIAN_POINT ( 'NONE',  ( 1.033464566929133799, 0.000000000000000000, 0.7185039370078739607 ) ) ;
#35390=LINE ( 'NONE', #25061, #5311 ) ;
#35391=DIRECTION ( 'NONE',  ( 0.000000000000000000, 0.000000000000000000, -1.000000000000000000 ) ) ;
#35392=ORIENTED_EDGE ( 'NONE', *, *, #17851, .F. ) ;
#35393=CARTESIAN_POINT ( 'NONE',  ( -1.054774247047244540, 0.07405724077823318263, 1.323818897584032594 ) ) ;
#35395=CARTESIAN_POINT ( 'NONE',  ( -0.8019270111902717657, -0.1787899950787401604, 0.9990157479777320715 ) ) ;
#35396=AXIS2_PLACEMENT_3D ( 'NONE', #6500, #21120, #35754 ) ;
#35398=CARTESIAN_POINT ( 'NONE',  ( -0.9500414927467378812, -0.1787899950787401604, 1.983267716481667886 ) ) ;
#35401=CARTESIAN_POINT ( 'NONE',  ( -1.054774247047244096, 0.000000000000000000, 1.006397637741511808 ) ) ;
#35402=CARTESIAN_POINT ( 'NONE',  ( -0.9500414927467378812, -0.1787899950787401604, 0.6496062991588353874 ) ) ;
#35403=CARTESIAN_POINT ( 'NONE',  ( 0.9873396505805591694, -0.1113553986120547346, 1.815944881889763884 ) ) ;
#35404=DIRECTION ( 'NONE',  ( 1.000000000000000000, 0.000000000000000000, -1.822029033848725275E-16 ) ) ;
#35407=EDGE_LOOP ( 'NONE', ( #6730, #22535, #29956, #17439 ) ) ;
#35412=CARTESIAN_POINT ( 'NONE',  ( -1.002407869896990045, -0.1264236179284866091, 0.6077755904974173617 ) ) ;
#35417=EDGE_LOOP ( 'NONE', ( #11071, #24914, #28948, #42809 ) ) ;
#35418=CARTESIAN_POINT ( 'NONE',  ( 0.7646288533564489232, -0.1113553986120547346, 0.5462598425196850682 ) ) ;
#35421=CARTESIAN_POINT ( 'NONE',  ( -1.033464566929134687, -0.06523048226347956391, 1.375492125876724980 ) ) ;
#35425=CARTESIAN_POINT ( 'NONE',  ( 1.033464566929133799, 1.928577636452524610E-17, 4.498031496062992574 ) ) ;
#35428=CARTESIAN_POINT ( 'NONE',  ( 0.8107537697050253289, -0.1574803149606297803, 1.218011811023622437 ) ) ;
#35430=DIRECTION ( 'NONE',  ( -1.000000000000000000, 0.000000000000000000, 0.000000000000000000 ) ) ;
#35432=CARTESIAN_POINT ( 'NONE',  ( 1.033464566929136907, -0.06523048226347749612, 1.857775590551182798 ) ) ;
#35434=CARTESIAN_POINT ( 'NONE',  ( 0.8759842519685039353, -0.1787899950787401882, 0.6815944881352126172 ) ) ;
#35440=CARTESIAN_POINT ( 'NONE',  ( 1.002407869896990045, 0.1264236179284866091, 0.8932086613635591421 ) ) ;
#35442=DIRECTION ( 'NONE',  ( 0.000000000000000000, 0.000000000000000000, -1.000000000000000000 ) ) ;
#35447=CARTESIAN_POINT ( 'NONE',  ( -0.6971942568897648851, 0.07405724077823318263, 1.855314960576157635 ) ) ;
#35448=CARTESIAN_POINT ( 'NONE',  ( 0.8759842519685039353, -0.1787899950787401882, 1.985728346402929168 ) ) ;
#35449=VERTEX_POINT ( 'NONE', #16352 ) ;
#35450=CARTESIAN_POINT ( 'NONE',  ( -1.002407869896990045, -0.1264236179284866091, 1.872539370024976391 ) ) ;
#35451=CARTESIAN_POINT ( 'NONE',  ( -0.7495606340400177148, -0.1264236179284866091, 1.542814960576157413 ) ) ;
#35453=EDGE_CURVE ( 'NONE', #10984, #19760, #35240, .T. ) ;
#35454=CARTESIAN_POINT ( 'NONE',  ( -0.8019270111902717657, -0.1787899950787401604, 0.2116141731745827814 ) ) ;
#35455=EDGE_CURVE ( 'NONE', #18349, #8537, #45070, .T. ) ;
#35458=CARTESIAN_POINT ( 'NONE',  ( -1.054774247047244540, -0.07405724077823318263, 1.953740157426552715 ) ) ;
#35459=CARTESIAN_POINT ( 'NONE',  ( -0.7646288533564489232, 0.1113553986120547346, 1.835629921259842590 ) ) ;
#35460=CYLINDRICAL_SURFACE ( 'NONE', #16716, 0.1574803149606299191 ) ;
#35464=CARTESIAN_POINT ( 'NONE',  ( 1.033464566929133799, 0.000000000000000000, 1.062992125876724314 ) ) ;
#35466=PRODUCT_DEFINITION_FORMATION_WITH_SPECIFIED_SOURCE ( 'ANY', '', #9398, .NOT_KNOWN. ) ;
#35471=CARTESIAN_POINT ( 'NONE',  ( -1.002407869896990045, 0.1264236179284866091, 1.213090551127338435 ) ) ;
#35472=ORIENTED_EDGE ( 'NONE', *, *, #1132, .T. ) ;
#35475=CARTESIAN_POINT ( 'NONE',  ( -0.7185039370078739607, 0.000000000000000000, -2.869337061179095023E-17 ) ) ;
#35478=CARTESIAN_POINT ( 'NONE',  ( -0.8759842519685039353, -0.1574803149606299191, 0.7775590550105826448 ) ) ;
#35479=CARTESIAN_POINT ( 'NONE',  ( -0.7185039370078739607, 1.928577636452523993E-17, 0.7775590551181102983 ) ) ;
#35483=CARTESIAN_POINT ( 'NONE',  ( 0.7185039370078746268, -0.06523048226347956391, 0.8193897637795271027 ) ) ;
#35489=CARTESIAN_POINT ( 'NONE',  ( 1.033464566929134687, 0.06523048226347956391, 0.1205708660342053040 ) ) ;
#35490=VERTEX_POINT ( 'NONE', #24702 ) ;
#35498=CARTESIAN_POINT ( 'NONE',  ( -0.8019270111902717657, -0.1787899950787401604, 1.432086614119464141 ) ) ;
#35499=CARTESIAN_POINT ( 'NONE',  ( 1.054774247047244096, 0.000000000000000000, 1.601870078686393750 ) ) ;
#35502=CARTESIAN_POINT ( 'NONE',  ( -0.6971942568897626646, 0.07405724077823318263, 0.5954724408911187261 ) ) ;
#35503=CARTESIAN_POINT ( 'NONE',  ( 0.9500414927467378812, 0.1787899950787401604, 0.1525590550643468046 ) ) ;
#35506=CARTESIAN_POINT ( 'NONE',  ( 0.9500414927467377701, -0.1787899950787401604, 0.5708661416785200116 ) ) ;
#35507=CARTESIAN_POINT ( 'NONE',  ( -0.7495606340400177148, -0.1264236179284866091, 0.4798228345919055560 ) ) ;
#35509=( BOUNDED_CURVE ( )  B_SPLINE_CURVE ( 2, ( #42477, #23110, #41755, #45595, #27446, #19503, #4875, #1278, #23352 ),
 .UNSPECIFIED., .F., .T. ) 
 B_SPLINE_CURVE_WITH_KNOTS ( ( 3, 2, 2, 2, 3 ),
 ( 0.3699999999999999956, 0.3724999999999999978, 0.3750000000000000000, 0.3775000000000000022, 0.3800000000000000044 ),
 .UNSPECIFIED. ) 
 CURVE ( )  GEOMETRIC_REPRESENTATION_ITEM ( )  RATIONAL_B_SPLINE_CURVE ( ( 1.000000000000000000, 0.9238795325112869605, 1.000000000000000000, 0.9238795325112869605, 1.000000000000000000, 0.9238795325112869605, 1.000000000000000000, 0.9238795325112869605, 1.000000000000000000 ) ) 
 REPRESENTATION_ITEM ( '' )  ) ;
#35513=CARTESIAN_POINT ( 'NONE',  ( -1.054774247047244540, 0.07405724077823318263, 1.407480314906865981 ) ) ;
#35514=CARTESIAN_POINT ( 'NONE',  ( -0.7185039370078746268, -0.06523048226347956391, 0.3863188976377951445 ) ) ;
#35515=CARTESIAN_POINT ( 'NONE',  ( 0.6971942568897637749, 2.189545951927499583E-17, 1.267224409395055096 ) ) ;
#35519=CARTESIAN_POINT ( 'NONE',  ( -0.9873396505805591694, -0.1113553986120547346, 0.5561023622047244208 ) ) ;
#35524=CARTESIAN_POINT ( 'NONE',  ( 1.033464566929133799, 0.000000000000000000, 1.624015748031496287 ) ) ;
#35525=CARTESIAN_POINT ( 'NONE',  ( 0.9412147342319837628, -0.1574803149606297803, 0.3961614173228344415 ) ) ;
#35527=CARTESIAN_POINT ( 'NONE',  ( 0.8019270111902717657, -0.1787899950787401604, 1.427165354276944687 ) ) ;
#35528=CYLINDRICAL_SURFACE ( 'NONE', #23854, 0.1574803149606299191 ) ;
#35531=CARTESIAN_POINT ( 'NONE',  ( 1.033464566929134687, -0.06523048226347956391, 0.1943897636720005040 ) ) ;
#35535=CYLINDRICAL_SURFACE ( 'NONE', #16548, 0.1574803149606299191 ) ;
#35536=CARTESIAN_POINT ( 'NONE',  ( 0.9500414927467378812, -0.1787899950787401604, 0.5265748030958428139 ) ) ;
#35538=CARTESIAN_POINT ( 'NONE',  ( -1.054774247047244540, -0.07405724077823318263, 0.8120078739619844832 ) ) ;
#35540=CARTESIAN_POINT ( 'NONE',  ( 1.033464566929134687, 0.06523048226347956391, 0.9867125983176703308 ) ) ;
#35544=CARTESIAN_POINT ( 'NONE',  ( 0.9500414927467378812, 0.1787899950787401604, 1.727362204670645385 ) ) ;
#35545=CARTESIAN_POINT ( 'NONE',  ( 0.9500414927467377701, -0.1787899950787401604, 1.983267716481668108 ) ) ;
#35547=CARTESIAN_POINT ( 'NONE',  ( 1.054774247047244540, 0.07405724077823318263, 0.3395669290800949480 ) ) ;
#35552=CARTESIAN_POINT ( 'NONE',  ( 1.054774247047244540, -0.07405724077823318263, 0.6496062991588353874 ) ) ;
#35554=CARTESIAN_POINT ( 'NONE',  ( 1.033464566929133799, 0.000000000000000000, 0.08858267716535432601 ) ) ;
#35555=CARTESIAN_POINT ( 'NONE',  ( -0.8107537697050254399, -0.1574803149606297803, 1.523129921152316379 ) ) ;
#35556=CARTESIAN_POINT ( 'NONE',  ( -0.8019270111902717657, 0.1787899950787401604, 1.451771653489543290 ) ) ;
#35560=CARTESIAN_POINT ( 'NONE',  ( 0.9500414927467378812, -0.1787899950787401604, 1.200787401521039355 ) ) ;
#35563=CARTESIAN_POINT ( 'NONE',  ( -1.033464566929133799, 0.000000000000000000, 0.7086614172153071767 ) ) ;
#35564=CARTESIAN_POINT ( 'NONE',  ( 0.7495606340400177148, -0.1264236179284866091, 1.779035433017102319 ) ) ;
#35565=CARTESIAN_POINT ( 'NONE',  ( -0.9412147342319837628, -0.1574803149606297803, 1.459153543307085688 ) ) ;
#35566=CARTESIAN_POINT ( 'NONE',  ( -1.002407869896990045, 0.1264236179284866091, 0.9325787401037164415 ) ) ;
#35568=CARTESIAN_POINT ( 'NONE',  ( 0.9500414927467377701, 0.1787899950787401604, 0.07381889758403178958 ) ) ;
#35569=CARTESIAN_POINT ( 'NONE',  ( 0.9412147342319837628, -0.1574803149606297803, 1.567421259734991690 ) ) ;
#35571=EDGE_CURVE ( 'NONE', #36086, #22696, #16877, .T. ) ;
#35574=CARTESIAN_POINT ( 'NONE',  ( -1.002407869896990045, -0.1264236179284866091, 1.670767716481669440 ) ) ;
#35575=EDGE_CURVE ( 'NONE', #46991, #44026, #31592, .T. ) ;
#35577=CARTESIAN_POINT ( 'NONE',  ( -0.8759842519685039353, 0.000000000000000000, 0.000000000000000000 ) ) ;
#35579=ORIENTED_EDGE ( 'NONE', *, *, #6443, .T. ) ;
#35581=ORIENTED_EDGE ( 'NONE', *, *, #24534, .F. ) ;
#35582=CARTESIAN_POINT ( 'NONE',  ( 0.9500414927467378812, 0.1787899950787401604, 1.092519684985605810 ) ) ;
#35584=CARTESIAN_POINT ( 'NONE',  ( -1.033464566929133799, 0.000000000000000000, 1.220472440837354400 ) ) ;
#35585=CARTESIAN_POINT ( 'NONE',  ( -0.9873396505805591694, 0.1113553986120547346, 0.9104330707586141269 ) ) ;
#35586=CARTESIAN_POINT ( 'NONE',  ( 0.8107537697050253289, 0.1574803149606300301, 1.754429133858266932 ) ) ;
#35588=AXIS2_PLACEMENT_3D ( 'NONE', #5958, #45732, #45258 ) ;
#35594=CARTESIAN_POINT ( 'NONE',  ( -0.7371950664085656912, 0.08546456393164050813, 1.981527568757507130 ) ) ;
#35595=CARTESIAN_POINT ( 'NONE',  ( -0.9873396505805591694, 0.1113553986120547346, 0.2116141732283464416 ) ) ;
#35596=CARTESIAN_POINT ( 'NONE',  ( 1.002407869896990045, 0.1264236179284866091, 1.134350393647023614 ) ) ;
#35597=CARTESIAN_POINT ( 'NONE',  ( 1.054774247047244540, 0.07405724077823318263, 1.599409448765134911 ) ) ;
#35598=CARTESIAN_POINT ( 'NONE',  ( 1.033464566929133799, 0.000000000000000000, 0.7578740157480314821 ) ) ;
#35600=CARTESIAN_POINT ( 'NONE',  ( -0.9873396505805591694, -0.1113553986120547346, 1.107283464566929165 ) ) ;
#35602=CARTESIAN_POINT ( 'NONE',  ( -0.8759842519685039353, -0.1574803149606299191, 1.801181102254677091 ) ) ;
#35604=CARTESIAN_POINT ( 'NONE',  ( 1.054774247047244096, 0.000000000000000000, 0.1796259841982051075 ) ) ;
#35605=CARTESIAN_POINT ( 'NONE',  ( -0.7185039370078746268, -0.06523048226347956391, 0.6914370077664891978 ) ) ;
#35606=CARTESIAN_POINT ( 'NONE',  ( 0.8759842519685039353, -0.1787899950787401882, 1.154035433017102319 ) ) ;
#35608=CARTESIAN_POINT ( 'NONE',  ( 1.054774247047244540, 0.07405724077823318263, 1.958661417269071947 ) ) ;
#35609=CARTESIAN_POINT ( 'NONE',  ( 1.033464566929134687, 0.06523048226347956391, 0.5142716534357801850 ) ) ;
#35610=ORIENTED_EDGE ( 'NONE', *, *, #42133, .T. ) ;
#35611=EDGE_CURVE ( 'NONE', #9090, #36581, #15639, .T. ) ;
#35612=LINE ( 'NONE', #2752, #27655 ) ;
#35613=CARTESIAN_POINT ( 'NONE',  ( -0.8107537697050253289, -0.1574803149606297803, 0.4601377951680635792 ) ) ;
#35615=CARTESIAN_POINT ( 'NONE',  ( 0.6971942568897648851, -0.07405724077823297447, 1.461614173174583753 ) ) ;
#35625=CARTESIAN_POINT ( 'NONE',  ( 1.054774247047244096, 0.000000000000000000, 0.4207677164816693294 ) ) ;
#35629=CARTESIAN_POINT ( 'NONE',  ( -0.6971942568897648851, 0.07405724077823318263, 1.028543307032851795 ) ) ;
#35632=CARTESIAN_POINT ( 'NONE',  ( -0.9500414927467378812, -0.1787899950787401604, 1.904527559001354398 ) ) ;
#35633=CARTESIAN_POINT ( 'NONE',  ( -0.8759842519685039353, -0.1787899950787401882, 1.035925196796629866 ) ) ;
#35634=CARTESIAN_POINT ( 'NONE',  ( -1.054774247047244096, 0.000000000000000000, 0.7357283464029290565 ) ) ;
#35637=CARTESIAN_POINT ( 'NONE',  ( -1.033464566929134687, 0.06523048226347956391, 0.08120078729404769935 ) ) ;
#35638=ORIENTED_EDGE ( 'NONE', *, *, #21846, .T. ) ;
#35639=CARTESIAN_POINT ( 'NONE',  ( -0.8759842519685039353, 0.1574803149606299191, 0.05905511811023622659 ) ) ;
#35641=ORIENTED_EDGE ( 'NONE', *, *, #36987, .F. ) ;
#35642=CARTESIAN_POINT ( 'NONE',  ( -0.8107537697050234415, -0.1574803149606297803, 0.3420275589475912370 ) ) ;
#35643=FACE_OUTER_BOUND ( 'NONE', #2943, .T. ) ;
#35644=CARTESIAN_POINT ( 'NONE',  ( -0.6971942568897626646, -0.07405724077823297447, 0.5561023621509617598 ) ) ;
#35645=( BOUNDED_CURVE ( )  B_SPLINE_CURVE ( 2, ( #5449, #23200, #30421, #37816, #41602, #15793, #20064, #34238, #15549 ),
 .UNSPECIFIED., .F., .T. ) 
 B_SPLINE_CURVE_WITH_KNOTS ( ( 3, 2, 2, 2, 3 ),
 ( 0.5799999999999999600, 0.5825000000000000178, 0.5849999999999999645, 0.5875000000000000222, 0.5899999999999999689 ),
 .UNSPECIFIED. ) 
 CURVE ( )  GEOMETRIC_REPRESENTATION_ITEM ( )  RATIONAL_B_SPLINE_CURVE ( ( 1.000000000000000000, 0.9238795325112869605, 1.000000000000000000, 0.9238795325112869605, 1.000000000000000000, 0.9238795325112869605, 1.000000000000000000, 0.9238795325112869605, 1.000000000000000000 ) ) 
 REPRESENTATION_ITEM ( '' )  ) ;
#35647=CARTESIAN_POINT ( 'NONE',  ( -0.8019270111902716547, 0.1787899950787401604, 1.614173228292692386 ) ) ;
#35652=CARTESIAN_POINT ( 'NONE',  ( 0.8759842519685039353, 0.1574803149606299191, 0.5708661417322835607 ) ) ;
#35654=CARTESIAN_POINT ( 'NONE',  ( 0.8759842519685039353, 0.1574803149606299191, 0.6397637794200314865 ) ) ;
#35655=CARTESIAN_POINT ( 'NONE',  ( -0.7185039370078739607, 1.928577636452523993E-17, 1.437007873908220601 ) ) ;
#35659=CARTESIAN_POINT ( 'NONE',  ( 0.9873396505805591694, 0.1113553986120547346, 1.619094488081448846 ) ) ;
#35661=LINE ( 'NONE', #7122, #10840 ) ;
#35662=CARTESIAN_POINT ( 'NONE',  ( 0.7185039370078746268, -0.06523048226347956391, 1.291830708661417360 ) ) ;
#35664=CARTESIAN_POINT ( 'NONE',  ( -0.8107537697050254399, -0.1574803149606297803, 1.336122047244094446 ) ) ;
#35665=CARTESIAN_POINT ( 'NONE',  ( 0.7185039370078739607, 1.928577636452523993E-17, 1.722440944881889813 ) ) ;
#35666=CARTESIAN_POINT ( 'NONE',  ( 0.9500414927467377701, -0.1787899950787401604, 0.6840551180564720113 ) ) ;
#35668=CARTESIAN_POINT ( 'NONE',  ( 1.033464566929133799, 0.000000000000000000, 1.545275590551181244 ) ) ;
#35669=VERTEX_POINT ( 'NONE', #5216 ) ;
#35670=ADVANCED_FACE ( 'NONE', ( #45462 ), #45225, .T. ) ;
#35672=CARTESIAN_POINT ( 'NONE',  ( 1.033464566929134687, -0.06523048226347956391, 1.739665354330709013 ) ) ;
#35674=CARTESIAN_POINT ( 'NONE',  ( 0.8019270111902717657, 0.1787899950787401604, 0.8612204723871809131 ) ) ;
#35681=CARTESIAN_POINT ( 'NONE',  ( -1.002407869896990045, 0.1264236179284866091, 1.921751968450173376 ) ) ;
#35682=VERTEX_POINT ( 'NONE', #38295 ) ;
#35683=CARTESIAN_POINT ( 'NONE',  ( 0.7495606340400177148, 0.1264236179284866091, 1.931594488135212728 ) ) ;
#35685=CARTESIAN_POINT ( 'NONE',  ( -0.6971942568897637749, 2.189545951927499583E-17, 1.936515747977732405 ) ) ;
#35686=CARTESIAN_POINT ( 'NONE',  ( -0.8759842519685039353, 0.1787899950787401882, 1.567421259788755794 ) ) ;
#35687=CARTESIAN_POINT ( 'NONE',  ( 0.9500414927467377701, 0.1787899950787401604, 0.8612204723871810241 ) ) ;
#35688=CARTESIAN_POINT ( 'NONE',  ( -0.9500414927467378812, -0.1787899950787401604, 1.038385826717890259 ) ) ;
#35689=CARTESIAN_POINT ( 'NONE',  ( -0.6971942568897637749, 2.189545951927499583E-17, 0.2436023621509610382 ) ) ;
#35691=CARTESIAN_POINT ( 'NONE',  ( -0.9500414927467378812, -0.1787899950787401604, 1.948818897584033927 ) ) ;
#35694=CARTESIAN_POINT ( 'NONE',  ( -1.033464566929133799, 0.000000000000000000, 1.505905511811023612 ) ) ;
#35695=CARTESIAN_POINT ( 'NONE',  ( 1.033464566929134687, -0.06523048226347956391, 1.060531495955465031 ) ) ;
#35697=CARTESIAN_POINT ( 'NONE',  ( -0.6971942568897626646, -0.07405724077823297447, 0.1230314960092287191 ) ) ;
#35698=VERTEX_POINT ( 'NONE', #12917 ) ;
#35699=CARTESIAN_POINT ( 'NONE',  ( -0.8759842519685039353, -0.1787899950787401882, 1.277066929080094448 ) ) ;
#35703=CARTESIAN_POINT ( 'NONE',  ( -0.7185039370078739607, 1.928577636452523993E-17, 1.358267716427907779 ) ) ;
#35706=CARTESIAN_POINT ( 'NONE',  ( -0.9412147342319837628, -0.1574803149606297803, 0.8981299211523156023 ) ) ;
#35707=CARTESIAN_POINT ( 'NONE',  ( -0.8107537697050253289, 0.1574803149606300301, 0.6914370078740167402 ) ) ;
#35709=CARTESIAN_POINT ( 'NONE',  ( 0.9412147342319837628, 0.1574803149606300301, 1.739665354223181470 ) ) ;
#35711=DIRECTION ( 'NONE',  ( 1.000000000000000000, 0.000000000000000000, 0.000000000000000000 ) ) ;
#35712=CARTESIAN_POINT ( 'NONE',  ( 0.9873396505805591694, 0.1113553986120547346, 0.7234251968503936370 ) ) ;
#35714=CARTESIAN_POINT ( 'NONE',  ( -1.033464566929133799, 0.000000000000000000, 1.230314960629921295 ) ) ;
#35718=CARTESIAN_POINT ( 'NONE',  ( 0.9873396505805591694, -0.1113553986120547346, 0.1131889762704257896 ) ) ;
#35722=FACE_OUTER_BOUND ( 'NONE', #28706, .T. ) ;
#35726=CARTESIAN_POINT ( 'NONE',  ( 0.7646288533564489232, -0.1113553986120547346, 0.8513779526483780113 ) ) ;
#35727=DIRECTION ( 'NONE',  ( 0.000000000000000000, 0.000000000000000000, -1.000000000000000000 ) ) ;
#35728=CARTESIAN_POINT ( 'NONE',  ( -0.6971942568897648851, -0.07405724077823297447, 1.934055118056471567 ) ) ;
#35730=CARTESIAN_POINT ( 'NONE',  ( -0.8019270111902717657, -0.1787899950787401604, 1.471456692859622217 ) ) ;
#35731=CARTESIAN_POINT ( 'NONE',  ( 0.9500414927467378812, -0.1787899950787401604, 1.515748031442299526 ) ) ;
#35732=EDGE_LOOP ( 'NONE', ( #2313, #45790, #9230 ) ) ;
#35734=CARTESIAN_POINT ( 'NONE',  ( -1.054774247047244540, -0.07405724077823318263, 0.6151574802611974313 ) ) ;
#35735=CARTESIAN_POINT ( 'NONE',  ( 1.054774247047244096, 0.000000000000000000, 0.1451771653005673179 ) ) ;
#35736=CARTESIAN_POINT ( 'NONE',  ( 1.033464566929133799, 1.928577636452524610E-17, 4.498031496062992574 ) ) ;
#35737=CARTESIAN_POINT ( 'NONE',  ( 1.002407869896990045, 0.1264236179284866091, 0.7012795275052913224 ) ) ;
#35738=CARTESIAN_POINT ( 'NONE',  ( -1.002407869896990045, 0.1264236179284866091, 0.6569881889226141247 ) ) ;
#35739=FACE_OUTER_BOUND ( 'NONE', #21091, .T. ) ;
#35740=CARTESIAN_POINT ( 'NONE',  ( -0.8107537697050254399, -0.1574803149606297803, 0.8636811023622043004 ) ) ;
#35742=CARTESIAN_POINT ( 'NONE',  ( -1.054774247047244540, -0.07405724077823318263, 1.441929133804504604 ) ) ;
#35744=CARTESIAN_POINT ( 'NONE',  ( -0.9412147342319837628, 0.1574803149606300301, 1.473917322834645605 ) ) ;
#35745=CARTESIAN_POINT ( 'NONE',  ( -0.9412147342319837628, 0.1574803149606300301, 0.4896653543307081802 ) ) ;
#35746=CARTESIAN_POINT ( 'NONE',  ( 1.002407869896990045, 0.1264236179284866091, 1.252460629867496067 ) ) ;
#35753=CARTESIAN_POINT ( 'NONE',  ( 0.7495606340400177148, -0.1264236179284866091, 1.385334645615527549 ) ) ;
#35754=DIRECTION ( 'NONE',  ( -1.000000000000000000, 0.000000000000000000, 0.000000000000000000 ) ) ;
#35758=CARTESIAN_POINT ( 'NONE',  ( 1.002407869896990045, 0.1264236179284866091, 0.2632874015210397434 ) ) ;
#35762=CYLINDRICAL_SURFACE ( 'NONE', #12731, 0.1574803149606299191 ) ;
#35764=CARTESIAN_POINT ( 'NONE',  ( 0.7495606340400177148, 0.1264236179284866091, 0.5880905511273386566 ) ) ;
#35767=CARTESIAN_POINT ( 'NONE',  ( -0.6971942568897637749, 2.189545951927499583E-17, 0.9128937007336377363 ) ) ;
#35770=CARTESIAN_POINT ( 'NONE',  ( -0.8765439795121998667, -0.1745856626756026320, 1.988193917683002132 ) ) ;
#35771=CARTESIAN_POINT ( 'NONE',  ( 0.8019270111902717657, 0.1787899950787401604, 1.614173228292692386 ) ) ;
#35772=CARTESIAN_POINT ( 'NONE',  ( 0.6971942568897637749, 2.189545951927499583E-17, 1.931594488135212728 ) ) ;
#35775=VERTEX_POINT ( 'NONE', #45945 ) ;
#35779=CARTESIAN_POINT ( 'NONE',  ( 1.054774247047244540, 0.07405724077823318263, 0.6545275590013545086 ) ) ;
#35781=CYLINDRICAL_SURFACE ( 'NONE', #33039, 0.1574803149606299191 ) ;
#35782=( BOUNDED_CURVE ( )  B_SPLINE_CURVE ( 2, ( #24449, #7180, #17256, #17727, #36430, #20844, #3099, #47202, #24927 ),
 .UNSPECIFIED., .F., .F. ) 
 B_SPLINE_CURVE_WITH_KNOTS ( ( 3, 2, 2, 2, 3 ),
 ( 0.5400000000000000355, 0.5424999999999999822, 0.5450000000000000400, 0.5474999999999999867, 0.5500000000000000444 ),
 .UNSPECIFIED. ) 
 CURVE ( )  GEOMETRIC_REPRESENTATION_ITEM ( )  RATIONAL_B_SPLINE_CURVE ( ( 1.000000000000000000, 0.9238795325112869605, 1.000000000000000000, 0.9238795325112869605, 1.000000000000000000, 0.9238795325112869605, 1.000000000000000000, 0.9238795325112869605, 1.000000000000000000 ) ) 
 REPRESENTATION_ITEM ( '' )  ) ;
#35784=CARTESIAN_POINT ( 'NONE',  ( 0.9873396505805591694, 0.1113553986120547346, 1.146653543199559033 ) ) ;
#35785=CARTESIAN_POINT ( 'NONE',  ( -0.7495606340400177148, 0.1264236179284866091, 1.493602362150960650 ) ) ;
#35787=CARTESIAN_POINT ( 'NONE',  ( 0.7646288533564489232, -0.1113553986120547346, 0.1525590551181102428 ) ) ;
#35788=CARTESIAN_POINT ( 'NONE',  ( 1.002407869896990045, 0.1264236179284866091, 1.094980314906866203 ) ) ;
#35789=CARTESIAN_POINT ( 'NONE',  ( 1.002407869896990045, 0.1264236179284866091, 1.838090551127338657 ) ) ;
#35790=CARTESIAN_POINT ( 'NONE',  ( -1.054774247047244540, 0.07405724077823318263, 0.9694881889226144578 ) ) ;
#35791=CARTESIAN_POINT ( 'NONE',  ( 0.8759842519685039353, 0.000000000000000000, 4.498031496062992574 ) ) ;
#35792=CARTESIAN_POINT ( 'NONE',  ( -0.7012869015610273538, 0.0004423858256796530677, 0.03937007874015843734 ) ) ;
#35793=CARTESIAN_POINT ( 'NONE',  ( 0.9500414927467377701, 0.1787899950787401604, 0.3494094487651343006 ) ) ;
#35794=CARTESIAN_POINT ( 'NONE',  ( -1.054774247047244540, 0.07405724077823318263, 0.6151574802611965431 ) ) ;
#35795=CARTESIAN_POINT ( 'NONE',  ( 1.033464566929133799, 0.000000000000000000, 1.535433070758614127 ) ) ;
#35798=CARTESIAN_POINT ( 'NONE',  ( 0.7646288533564489232, 0.1113553986120547346, 1.786417322727117840 ) ) ;
#35800=CARTESIAN_POINT ( 'NONE',  ( 0.7495606340400177148, -0.1264236179284866091, 0.7997047243556849594 ) ) ;
#35801=CARTESIAN_POINT ( 'NONE',  ( -0.6971942568897648851, -0.07405724077823297447, 1.737204724355685626 ) ) ;
#35803=( BOUNDED_CURVE ( )  B_SPLINE_CURVE ( 2, ( #4761, #34039, #19865, #1164, #37600, #34266, #8363, #42116, #9330 ),
 .UNSPECIFIED., .F., .F. ) 
 B_SPLINE_CURVE_WITH_KNOTS ( ( 3, 2, 2, 2, 3 ),
 ( 0.2000000000000000111, 0.2025000000000000133, 0.2049999999999999878, 0.2074999999999999900, 0.2099999999999999922 ),
 .UNSPECIFIED. ) 
 CURVE ( )  GEOMETRIC_REPRESENTATION_ITEM ( )  RATIONAL_B_SPLINE_CURVE ( ( 1.000000000000000000, 0.9238795325112869605, 1.000000000000000000, 0.9238795325112869605, 1.000000000000000000, 0.9238795325112869605, 1.000000000000000000, 0.9238795325112869605, 1.000000000000000000 ) ) 
 REPRESENTATION_ITEM ( '' )  ) ;
#35804=CARTESIAN_POINT ( 'NONE',  ( -0.7185039370078739607, 1.928577636452523993E-17, 0.6594488188976378451 ) ) ;
#35810=CARTESIAN_POINT ( 'NONE',  ( 0.6971942568897637749, 2.189545951927499583E-17, 1.065452755851747924 ) ) ;
#35812=CARTESIAN_POINT ( 'NONE',  ( 0.9873396505805591694, -0.1113553986120547346, 1.973425196850393970 ) ) ;
#35816=CARTESIAN_POINT ( 'NONE',  ( -0.6971942568897648851, 0.07405724077823318263, 0.3592519684501735422 ) ) ;
#35820=CARTESIAN_POINT ( 'NONE',  ( 0.6971942568897648851, 0.07405724077823318263, 1.225393700733637514 ) ) ;
#35821=CARTESIAN_POINT ( 'NONE',  ( 0.8759842519685039353, -0.1787899950787401882, 1.508366141678519678 ) ) ;
#35822=CARTESIAN_POINT ( 'NONE',  ( 1.054774247047244540, 0.07405724077823318263, 0.1820866141194649179 ) ) ;
#35824=CARTESIAN_POINT ( 'NONE',  ( 0.7646288533564489232, -0.1113553986120547346, 1.687992125984252079 ) ) ;
#35826=CARTESIAN_POINT ( 'NONE',  ( -1.033464566929134687, 0.06523048226347956391, 0.9965551181102363376 ) ) ;
#35827=CARTESIAN_POINT ( 'NONE',  ( 1.033464566929133799, 0.000000000000000000, 1.535433070758614127 ) ) ;
#35829=CARTESIAN_POINT ( 'NONE',  ( -0.9873396505805591694, -0.1113553986120547346, 1.727362204616881947 ) ) ;
#35830=AXIS2_PLACEMENT_3D ( 'NONE', #45735, #24422, #2133 ) ;
#35832=CARTESIAN_POINT ( 'NONE',  ( 1.002407869896990045, -0.1264236179284866091, 0.1747047243556852092 ) ) ;
#35833=CARTESIAN_POINT ( 'NONE',  ( 0.7302202526404721894, -0.08507351211645501621, 0.03937197694971072970 ) ) ;
#35834=CARTESIAN_POINT ( 'NONE',  ( 1.054774247047244096, 0.000000000000000000, 1.203248031442299304 ) ) ;
#35835=FACE_OUTER_BOUND ( 'NONE', #19455, .T. ) ;
#35836=CARTESIAN_POINT ( 'NONE',  ( 1.002407869896990045, 0.1264236179284866091, 1.921751968450173376 ) ) ;
#35837=CARTESIAN_POINT ( 'NONE',  ( 0.7646288533564489232, -0.1113553986120547346, 0.4576771652468039631 ) ) ;
#35838=ORIENTED_EDGE ( 'NONE', *, *, #37129, .T. ) ;
#35839=CARTESIAN_POINT ( 'NONE',  ( -0.8107537697050253289, -0.1574803149606297803, 0.4207677164279059467 ) ) ;
#35841=CARTESIAN_POINT ( 'NONE',  ( 1.054774247047244540, -0.07405724077823318263, 1.515748031442299526 ) ) ;
#35842=CARTESIAN_POINT ( 'NONE',  ( -0.7646288533564489232, 0.1113553986120547346, 0.2903543306011346359 ) ) ;
#35844=ORIENTED_EDGE ( 'NONE', *, *, #4516, .F. ) ;
#35846=ORIENTED_EDGE ( 'NONE', *, *, #42294, .F. ) ;
#35847=DIRECTION ( 'NONE',  ( 1.000000000000000000, 0.000000000000000000, -1.822029033848725275E-16 ) ) ;
#35851=CARTESIAN_POINT ( 'NONE',  ( -0.6971942568897637749, 2.189545951927499583E-17, 1.970964566875370139 ) ) ;
#35853=CARTESIAN_POINT ( 'NONE',  ( -0.6971942568897648851, -0.07405724077823297447, 1.067913385773007651 ) ) ;
#35854=CARTESIAN_POINT ( 'NONE',  ( -0.7495606340400177148, -0.1264236179284866091, 0.7997047243556849594 ) ) ;
#35864=LINE ( 'NONE', #10723, #24875 ) ;
#35867=CARTESIAN_POINT ( 'NONE',  ( -1.054774247047244096, 0.000000000000000000, 0.6914370078202519698 ) ) ;
#35868=CARTESIAN_POINT ( 'NONE',  ( 1.033464566929134687, 0.06523048226347956391, 1.341043306979086358 ) ) ;
#35870=CARTESIAN_POINT ( 'NONE',  ( -0.9500414927467377701, -0.1787899950787401604, 1.791338582623401177 ) ) ;
#35871=CARTESIAN_POINT ( 'NONE',  ( 1.033464566929134687, -0.06523048226347956391, 1.345964566929133133 ) ) ;
#35873=CARTESIAN_POINT ( 'NONE',  ( -0.9873396505805591694, 0.1113553986120547346, 0.1230314959554651699 ) ) ;
#35877=CARTESIAN_POINT ( 'NONE',  ( -0.9873396505805591694, -0.1113553986120547346, 1.333661417215306955 ) ) ;
#35878=CARTESIAN_POINT ( 'NONE',  ( 0.8019270111902717657, 0.1787899950787401604, 0.7874015747493863238 ) ) ;
#35881=DIRECTION ( 'NONE',  ( 1.822029033848725028E-16, 0.000000000000000000, 1.000000000000000000 ) ) ;
#35883=CARTESIAN_POINT ( 'NONE',  ( 0.7185039370078746268, 0.06523048226347956391, 1.247539370078740273 ) ) ;
#35884=CARTESIAN_POINT ( 'NONE',  ( 0.7469364138422923682, -0.1104497288306852537, 1.985496003449917390 ) ) ;
#35886=CARTESIAN_POINT ( 'NONE',  ( 1.002407869896990045, 0.1264236179284866091, 0.6176181101824566033 ) ) ;
#35888=LINE ( 'NONE', #24402, #31567 ) ;
#35889=CARTESIAN_POINT ( 'NONE',  ( -0.7185039370078746268, -0.06523048226347956391, 0.3764763778452288046 ) ) ;
#35892=CARTESIAN_POINT ( 'NONE',  ( 0.9412147342319837628, -0.1574803149606297803, 0.7111220472440957785 ) ) ;
#35893=CARTESIAN_POINT ( 'NONE',  ( 0.6971942568897648851, 0.07405724077823318263, 1.062992125930488418 ) ) ;
#35895=CARTESIAN_POINT ( 'NONE',  ( 0.9412147342319837628, 0.1574803149606300301, 1.473917322834645605 ) ) ;
#35896=DIRECTION ( 'NONE',  ( -1.000000000000000000, 0.000000000000000000, 0.000000000000000000 ) ) ;
#35902=CARTESIAN_POINT ( 'NONE',  ( -0.7495606340400177148, 0.1264236179284866091, 0.1156496062454492185 ) ) ;
#35903=VERTEX_POINT ( 'NONE', #39862 ) ;
#35906=CARTESIAN_POINT ( 'NONE',  ( -0.7495606340400177148, 0.1264236179284866091, 1.931594488135212728 ) ) ;
#35907=CARTESIAN_POINT ( 'NONE',  ( -1.002407869896990045, 0.1264236179284866091, 1.523129921206078707 ) ) ;
#35908=CARTESIAN_POINT ( 'NONE',  ( 0.8019270111902716547, -0.1787899950787401604, 0.8415354330171020969 ) ) ;
#35909=( BOUNDED_CURVE ( )  B_SPLINE_CURVE ( 2, ( #45294, #38125, #40978 ),
 .UNSPECIFIED., .F., .T. ) 
 B_SPLINE_CURVE_WITH_KNOTS ( ( 3, 3 ),
 ( 0.9975000000000000533, 1.000000000000000000 ),
 .UNSPECIFIED. ) 
 CURVE ( )  GEOMETRIC_REPRESENTATION_ITEM ( )  RATIONAL_B_SPLINE_CURVE ( ( 1.000000000000000000, 0.9238795325112869605, 1.000000000000000000 ) ) 
 REPRESENTATION_ITEM ( '' )  ) ;
#35911=CARTESIAN_POINT ( 'NONE',  ( -0.7495606340400177148, -0.1264236179284866091, 1.823326771599779406 ) ) ;
#35913=CARTESIAN_POINT ( 'NONE',  ( -0.7185039370078739607, 1.928577636452523993E-17, 0.3051181102362204856 ) ) ;
#35916=FACE_OUTER_BOUND ( 'NONE', #6568, .T. ) ;
#35917=CARTESIAN_POINT ( 'NONE',  ( 0.9412147342319837628, -0.1574803149606297803, 1.055610236112945577 ) ) ;
#35918=CARTESIAN_POINT ( 'NONE',  ( -0.6971942568897626646, 0.07405724077823318263, 0.1574803149068664809 ) ) ;
#35920=ORIENTED_EDGE ( 'NONE', *, *, #37498, .T. ) ;
#35922=CARTESIAN_POINT ( 'NONE',  ( -0.8019270111902716547, -0.1787899950787401604, 1.274606299158834277 ) ) ;
#35926=EDGE_CURVE ( 'NONE', #26852, #18241, #36483, .T. ) ;
#35930=CARTESIAN_POINT ( 'NONE',  ( -0.9412147342319837628, -0.1574803149606297803, 0.2386811023622048278 ) ) ;
#35931=CARTESIAN_POINT ( 'NONE',  ( -1.033464566929134687, -0.06523048226347956391, 0.9424212597349932441 ) ) ;
#35932=CARTESIAN_POINT ( 'NONE',  ( -0.8759842519685039353, -0.1574803149606299191, 0.7480314960629921295 ) ) ;
#35935=CARTESIAN_POINT ( 'NONE',  ( 0.7646288533564489232, -0.1113553986120547346, 1.835629921152314825 ) ) ;
#35939=CARTESIAN_POINT ( 'NONE',  ( 0.9412147342319837628, -0.1574803149606297803, 0.7898622047244097111 ) ) ;
#35941=CARTESIAN_POINT ( 'NONE',  ( -0.9412147342319837628, -0.1574803149606297803, 1.606791338475149766 ) ) ;
#35942=DIRECTION ( 'NONE',  ( 0.000000000000000000, 0.000000000000000000, -1.000000000000000000 ) ) ;
#35943=DIRECTION ( 'NONE',  ( 1.000000000000000000, 0.000000000000000000, -1.822029033848725275E-16 ) ) ;
#35944=CARTESIAN_POINT ( 'NONE',  ( 1.033464566929133799, 0.000000000000000000, 0.1574803148531029595 ) ) ;
#35945=ORIENTED_EDGE ( 'NONE', *, *, #20053, .T. ) ;
#35947=CARTESIAN_POINT ( 'NONE',  ( 0.8107537697050234415, -0.1574803149606297803, 0.2337598425196852070 ) ) ;
#35950=CARTESIAN_POINT ( 'NONE',  ( 0.7185039370078739607, 0.000000000000000000, 4.498031496062992574 ) ) ;
#35954=CARTESIAN_POINT ( 'NONE',  ( 1.033464566929134687, 0.06523048226347956391, 0.9867125983176702197 ) ) ;
#35955=CARTESIAN_POINT ( 'NONE',  ( 0.7185039370078739607, 1.928577636452523993E-17, 0.5413385826771653919 ) ) ;
#35957=ORIENTED_EDGE ( 'NONE', *, *, #19796, .T. ) ;
#35959=ORIENTED_EDGE ( 'NONE', *, *, #14563, .T. ) ;
#35960=CARTESIAN_POINT ( 'NONE',  ( -1.002407869896990045, 0.1264236179284866091, 1.606791338528913426 ) ) ;
#35961=CARTESIAN_POINT ( 'NONE',  ( 0.7495606340400177148, -0.1264236179284866091, 1.587106299158834721 ) ) ;
#35962=CARTESIAN_POINT ( 'NONE',  ( -1.002407869896990045, 0.1264236179284866091, 0.6225393700249762796 ) ) ;
#35963=CARTESIAN_POINT ( 'NONE',  ( 1.002407869896990045, -0.1264236179284866091, 0.2189960629383626012 ) ) ;
#35964=DIRECTION ( 'NONE',  ( 0.000000000000000000, 0.000000000000000000, -1.000000000000000000 ) ) ;
#35965=CARTESIAN_POINT ( 'NONE',  ( 1.054774247047244540, -0.07405724077823318263, 0.7726377952218266287 ) ) ;
#35966=CARTESIAN_POINT ( 'NONE',  ( -0.6971942568897637749, 2.189545951927499583E-17, 0.7111220471903307860 ) ) ;
#35969=CARTESIAN_POINT ( 'NONE',  ( 1.033464566929133799, 0.000000000000000000, 1.151574803149606474 ) ) ;
#35971=CARTESIAN_POINT ( 'NONE',  ( -0.6971942568897648851, -0.07405724077823297447, 1.427165354276944687 ) ) ;
#35972=CARTESIAN_POINT ( 'NONE',  ( -0.7646288533564489232, -0.1113553986120547346, 0.3887795275590551491 ) ) ;
#35973=CARTESIAN_POINT ( 'NONE',  ( 0.9500414927467377701, 0.1787899950787401604, 1.530511810969859221 ) ) ;
#35974=CARTESIAN_POINT ( 'NONE',  ( -0.7646288533564489232, 0.1113553986120547346, 0.3690944880814492901 ) ) ;
#35975=ORIENTED_EDGE ( 'NONE', *, *, #45978, .T. ) ;
#35979=ORIENTED_EDGE ( 'NONE', *, *, #15840, .F. ) ;
#35980=EDGE_CURVE ( 'NONE', #44026, #9783, #44976, .T. ) ;
#35981=CARTESIAN_POINT ( 'NONE',  ( 1.033464566929134687, 0.06523048226347956391, 0.4847440944881890590 ) ) ;
#35982=VERTEX_POINT ( 'NONE', #15442 ) ;
#35983=CARTESIAN_POINT ( 'NONE',  ( 0.9500414927467378812, 0.1787899950787401604, 1.446850393647023614 ) ) ;
#35984=DIRECTION ( 'NONE',  ( 1.000000000000000000, 0.000000000000000000, -1.822029033848725275E-16 ) ) ;
#35989=CARTESIAN_POINT ( 'NONE',  ( 0.6971942568897626646, -0.07405724077823297447, 0.3198818897100162983 ) ) ;
#35995=CARTESIAN_POINT ( 'NONE',  ( -0.8107537697050254399, -0.1574803149606297803, 1.690452755905512916 ) ) ;
#35996=CARTESIAN_POINT ( 'NONE',  ( 1.054774247047244540, -0.07405724077823318263, 0.6496062991588353874 ) ) ;
#35998=CARTESIAN_POINT ( 'NONE',  ( -0.6971942568897648851, -0.07405724077823297447, 1.033464566875371027 ) ) ;
#35999=CARTESIAN_POINT ( 'NONE',  ( -1.014932596384295227, 0.08658232834094778396, 0.03937007874015843040 ) ) ;
#36003=CARTESIAN_POINT ( 'NONE',  ( 0.7495606340400177148, 0.1264236179284866091, 1.656003936954110412 ) ) ;
#36004=CARTESIAN_POINT ( 'NONE',  ( 0.7495606340400177148, 0.1264236179284866091, 1.926673228292693052 ) ) ;
#36007=CARTESIAN_POINT ( 'NONE',  ( 0.8107537697050254399, -0.1574803149606297803, 1.326279527451528661 ) ) ;
#36010=CARTESIAN_POINT ( 'NONE',  ( 1.002407869896990045, -0.1264236179284866091, 0.5290354330171024300 ) ) ;
#36012=CARTESIAN_POINT ( 'NONE',  ( 0.9500414927467378812, 0.1787899950787401604, 0.1525590550643468046 ) ) ;
#36014=CARTESIAN_POINT ( 'NONE',  ( -0.8019270111902717657, 0.1787899950787401604, 1.569881889710015299 ) ) ;
#36015=ORIENTED_EDGE ( 'NONE', *, *, #3680, .T. ) ;
#36017=CARTESIAN_POINT ( 'NONE',  ( 1.054774247047244096, 0.000000000000000000, 1.168799212544661348 ) ) ;
#36019=CARTESIAN_POINT ( 'NONE',  ( 0.8759842519685039353, -0.1574803149606299191, 1.496062992125984259 ) ) ;
#36020=CARTESIAN_POINT ( 'NONE',  ( 0.8759842519685039353, -0.1787899950787401882, 1.823326771599779406 ) ) ;
#36021=CARTESIAN_POINT ( 'NONE',  ( -0.7185039370078746268, 0.06523048226347956391, 0.5782480314960627421 ) ) ;
#36022=CARTESIAN_POINT ( 'NONE',  ( -1.054774247047244540, 0.07405724077823318263, 0.9301181101824563813 ) ) ;
#36023=CARTESIAN_POINT ( 'NONE',  ( -1.033464566929136907, -0.06523048226347749612, 1.621555118110237670 ) ) ;
#36025=CARTESIAN_POINT ( 'NONE',  ( 0.7495606340400177148, -0.1264236179284866091, 0.2485236219934806867 ) ) ;
#36026=CARTESIAN_POINT ( 'NONE',  ( -1.054774247047244096, 0.000000000000000000, 0.2583661416785200671 ) ) ;
#36027=CARTESIAN_POINT ( 'NONE',  ( -0.8759842519685039353, -0.1787899950787401882, 0.5241141731745827537 ) ) ;
#36028=CARTESIAN_POINT ( 'NONE',  ( 0.8107537697050253289, -0.1574803149606297803, 1.562499999892472458 ) ) ;
#36029=ORIENTED_EDGE ( 'NONE', *, *, #36038, .F. ) ;
#36033=CARTESIAN_POINT ( 'NONE',  ( 0.7495606340400177148, -0.1264236179284866091, 0.7603346456155274380 ) ) ;
#36034=CARTESIAN_POINT ( 'NONE',  ( -1.002407869896990045, -0.1264236179284866091, 1.867618110182456714 ) ) ;
#36038=EDGE_CURVE ( 'NONE', #17227, #27120, #13797, .T. ) ;
#36049=CARTESIAN_POINT ( 'NONE',  ( 0.8759842519685039353, 0.1574803149606299191, 1.948818897637795367 ) ) ;
#36053=CARTESIAN_POINT ( 'NONE',  ( -1.002407869896990045, -0.1264236179284866091, 0.4158464566391496531 ) ) ;
#36054=CARTESIAN_POINT ( 'NONE',  ( -0.8107537697050254399, 0.1574803149606300301, 1.203248031496062520 ) ) ;
#36055=CARTESIAN_POINT ( 'NONE',  ( 1.002407869896990045, -0.1264236179284866091, 1.203248031442299304 ) ) ;
#36056=CARTESIAN_POINT ( 'NONE',  ( 0.8759842519685039353, 0.1787899950787401882, 1.488681102308440751 ) ) ;
#36058=CARTESIAN_POINT ( 'NONE',  ( -1.033464566929133799, 0.000000000000000000, 1.899606299212598604 ) ) ;
#36059=CARTESIAN_POINT ( 'NONE',  ( -1.033464566929133799, 0.000000000000000000, 0.5905511809948347235 ) ) ;
#36061=CARTESIAN_POINT ( 'NONE',  ( -0.8759842519685039353, 0.000000000000000000, 0.000000000000000000 ) ) ;
#36062=CARTESIAN_POINT ( 'NONE',  ( -1.033464566929134687, 0.06523048226347956391, 1.734744094380662904 ) ) ;
#36063=CARTESIAN_POINT ( 'NONE',  ( 0.6971942568897637749, 2.189545951927499583E-17, 0.2386811023084413619 ) ) ;
#36064=CARTESIAN_POINT ( 'NONE',  ( -1.033464566929133799, 0.000000000000000000, 1.348425196850393748 ) ) ;
#36065=CARTESIAN_POINT ( 'NONE',  ( 0.8759842519685039353, -0.1787899950787401882, 1.075295275536787276 ) ) ;
#36067=DIRECTION ( 'NONE',  ( 0.000000000000000000, 0.000000000000000000, -1.000000000000000000 ) ) ;
#36068=CARTESIAN_POINT ( 'NONE',  ( -0.8759842519685039353, 0.1787899950787401882, 1.213090551127338435 ) ) ;
#36069=CARTESIAN_POINT ( 'NONE',  ( 0.7185039370078746268, 0.06523048226347956391, 0.5290354329633386588 ) ) ;
#36072=CARTESIAN_POINT ( 'NONE',  ( 0.9294026713671079687, 0.1625504865516811670, 0.03937007694543066122 ) ) ;
#36073=CARTESIAN_POINT ( 'NONE',  ( 0.7646288533564489232, -0.1113553986120547346, 0.2706692913385826960 ) ) ;
#36074=CARTESIAN_POINT ( 'NONE',  ( -0.9873396505805591694, -0.1113553986120547346, 0.3887795274515282729 ) ) ;
#36076=CARTESIAN_POINT ( 'NONE',  ( 0.9500414927467378812, 0.1787899950787401604, 1.407480314906865981 ) ) ;
#36078=CARTESIAN_POINT ( 'NONE',  ( -0.7185039370078739607, 1.928577636452523993E-17, 0.2952755904436539236 ) ) ;
#36081=ORIENTED_EDGE ( 'NONE', *, *, #4516, .T. ) ;
#36085=( BOUNDED_CURVE ( )  B_SPLINE_CURVE ( 2, ( #17389, #46386, #24590, #39898, #39187, #46152, #46618, #13346, #9978 ),
 .UNSPECIFIED., .F., .T. ) 
 B_SPLINE_CURVE_WITH_KNOTS ( ( 3, 2, 2, 2, 3 ),
 ( 0.2500000000000000000, 0.2525000000000000022, 0.2550000000000000044, 0.2575000000000000067, 0.2600000000000000089 ),
 .UNSPECIFIED. ) 
 CURVE ( )  GEOMETRIC_REPRESENTATION_ITEM ( )  RATIONAL_B_SPLINE_CURVE ( ( 1.000000000000000000, 0.9238795325112869605, 1.000000000000000000, 0.9238795325112869605, 1.000000000000000000, 0.9238795325112869605, 1.000000000000000000, 0.9238795325112869605, 1.000000000000000000 ) ) 
 REPRESENTATION_ITEM ( '' )  ) ;
#36086=VERTEX_POINT ( 'NONE', #19487 ) ;
#36088=CARTESIAN_POINT ( 'NONE',  ( 0.6971942568897626646, -0.07405724077823297447, 0.5610236219934807700 ) ) ;
#36090=CARTESIAN_POINT ( 'NONE',  ( -0.6971942568897648851, 0.07405724077823318263, 1.496062992072220599 ) ) ;
#36092=CARTESIAN_POINT ( 'NONE',  ( -1.002407869896990045, 0.1264236179284866091, 1.134350393647023614 ) ) ;
#36093=CARTESIAN_POINT ( 'NONE',  ( -1.033464566929133799, 0.000000000000000000, 0.1279527559055118058 ) ) ;
#36094=CARTESIAN_POINT ( 'NONE',  ( -0.7495606340400177148, -0.1264236179284866091, 1.031003936954110189 ) ) ;
#36098=DIRECTION ( 'NONE',  ( 1.822029033848725028E-16, 0.000000000000000000, 1.000000000000000000 ) ) ;
#36102=CARTESIAN_POINT ( 'NONE',  ( 0.7628455132511623438, 0.1385261779602319776, 0.03937407183360309981 ) ) ;
#36110=CYLINDRICAL_SURFACE ( 'NONE', #37943, 0.1574803149606299191 ) ;
#36111=CARTESIAN_POINT ( 'NONE',  ( -0.6971942568897637749, 2.189545951927499583E-17, 0.6717519684501732646 ) ) ;
#36112=DIRECTION ( 'NONE',  ( 0.000000000000000000, 0.000000000000000000, -1.000000000000000000 ) ) ;
#36113=CARTESIAN_POINT ( 'NONE',  ( -0.7495606340400177148, -0.1264236179284866091, 1.744586614119464807 ) ) ;
#36114=EDGE_LOOP ( 'NONE', ( #14060, #45841, #4103, #29648 ) ) ;
#36115=CARTESIAN_POINT ( 'NONE',  ( 0.7185039370078739607, 1.928577636452523993E-17, 0.6102362203649134287 ) ) ;
#36116=CARTESIAN_POINT ( 'NONE',  ( -0.6971942568897637749, 2.189545951927499583E-17, 0.1254921259304885850 ) ) ;
#36118=CARTESIAN_POINT ( 'NONE',  ( 0.8107537697050253289, 0.1574803149606300301, 0.6520669291338586637 ) ) ;
#36121=CARTESIAN_POINT ( 'NONE',  ( -0.9412147342319837628, -0.1574803149606297803, 1.449311023514519681 ) ) ;
#36122=CARTESIAN_POINT ( 'NONE',  ( 1.002407869896990045, -0.1264236179284866091, 0.7701771653005669016 ) ) ;
#36124=CARTESIAN_POINT ( 'NONE',  ( 0.9412147342319837628, 0.1574803149606300301, 1.621555118002709683 ) ) ;
#36127=CARTESIAN_POINT ( 'NONE',  ( 1.033464566929134687, -0.06523048226347956391, 1.227854330708661124 ) ) ;
#36129=CARTESIAN_POINT ( 'NONE',  ( 0.7759784704967711555, -0.1388558036440012133, 1.986221128314594742 ) ) ;
#36131=EDGE_CURVE ( 'NONE', #22180, #47216, #41332, .T. ) ;
#36133=CARTESIAN_POINT ( 'NONE',  ( 1.002407869896990045, -0.1264236179284866091, 0.6471456692375747721 ) ) ;
#36134=CARTESIAN_POINT ( 'NONE',  ( 0.9873396505805591694, -0.1113553986120547346, 0.2706692912310554866 ) ) ;
#36135=CARTESIAN_POINT ( 'NONE',  ( -0.7646288533564489232, 0.1113553986120547346, 0.6938976377952755792 ) ) ;
#36138=CARTESIAN_POINT ( 'NONE',  ( 0.8759842519685039353, 0.000000000000000000, 4.498031496062992574 ) ) ;
#36142=CARTESIAN_POINT ( 'NONE',  ( 0.9500414927467378812, -0.1787899950787401604, 1.038385826717890259 ) ) ;
#36143=VERTEX_POINT ( 'NONE', #27432 ) ;
#36148=DIRECTION ( 'NONE',  ( 0.000000000000000000, 0.000000000000000000, -1.000000000000000000 ) ) ;
#36149=VERTEX_POINT ( 'NONE', #16836 ) ;
#36150=CARTESIAN_POINT ( 'NONE',  ( -1.002407869896990045, 0.1264236179284866091, 0.02706692908009476414 ) ) ;
#36153=CARTESIAN_POINT ( 'NONE',  ( 1.054774247047244540, -0.07405724077823318263, 1.953740157426552715 ) ) ;
#36156=CARTESIAN_POINT ( 'NONE',  ( -0.7495606340400177148, -0.1264236179284866091, 1.980807086560409491 ) ) ;
#36157=CARTESIAN_POINT ( 'NONE',  ( -0.8019270111902717657, -0.1787899950787401604, 1.702755905458047003 ) ) ;
#36158=CARTESIAN_POINT ( 'NONE',  ( 0.7495606340400177148, 0.1264236179284866091, 0.9079724408911180600 ) ) ;
#36159=CARTESIAN_POINT ( 'NONE',  ( -0.6971942568897648851, 0.07405724077823318263, 1.062992125930488418 ) ) ;
#36160=CARTESIAN_POINT ( 'NONE',  ( -0.8759842519685039353, -0.1787899950787401882, 0.3715551180564728440 ) ) ;
#36161=EDGE_CURVE ( 'NONE', #26252, #15853, #34708, .T. ) ;
#36162=CARTESIAN_POINT ( 'NONE',  ( -0.7646288533564489232, -0.1113553986120547346, 0.6643700787401575214 ) ) ;
#36163=CARTESIAN_POINT ( 'NONE',  ( -0.8759842519685039353, -0.1787899950787401882, 1.867618110182456714 ) ) ;
#36164=CARTESIAN_POINT ( 'NONE',  ( -0.8107537697050254399, 0.1574803149606300301, 1.478838582677165059 ) ) ;
#36165=CARTESIAN_POINT ( 'NONE',  ( -0.8759842519685039353, -0.1574803149606299191, 1.889763779527559251 ) ) ;
#36166=CARTESIAN_POINT ( 'NONE',  ( -1.033464566929134687, -0.06523048226347956391, 1.897145669291339543 ) ) ;
#36171=EDGE_CURVE ( 'NONE', #32743, #27640, #38170, .T. ) ;
#36172=CARTESIAN_POINT ( 'NONE',  ( -0.8019270111902717657, 0.1787899950787401604, 0.1525590550643468046 ) ) ;
#36174=CARTESIAN_POINT ( 'NONE',  ( 0.7185039370078739607, 0.000000000000000000, 4.498031496062992574 ) ) ;
#36177=CARTESIAN_POINT ( 'NONE',  ( -1.054774247047244540, 0.07405724077823318263, 1.368110236166710125 ) ) ;
#36184=CARTESIAN_POINT ( 'NONE',  ( 1.033464566929134687, -0.06523048226347956391, 0.3617125984251968740 ) ) ;
#36185=CARTESIAN_POINT ( 'NONE',  ( -1.033464566929133799, 0.000000000000000000, 0.2460629921259842590 ) ) ;
#36186=CARTESIAN_POINT ( 'NONE',  ( -0.8759842519685039353, 0.1574803149606299191, 0.9153543306011338032 ) ) ;
#36188=CARTESIAN_POINT ( 'NONE',  ( 0.6971942568897626646, -0.07405724077823297447, 0.4822834645131655606 ) ) ;
#36189=CARTESIAN_POINT ( 'NONE',  ( 0.9412147342319837628, -0.1574803149606297803, 1.882381889656251861 ) ) ;
#36191=CARTESIAN_POINT ( 'NONE',  ( 1.033464566929133799, 0.000000000000000000, 1.624015748031496287 ) ) ;
#36192=CARTESIAN_POINT ( 'NONE',  ( 0.7185039370078746268, 0.06523048226347956391, 0.7357283464566919395 ) ) ;
#36195=CYLINDRICAL_SURFACE ( 'NONE', #41550, 0.1574803149606299191 ) ;
#36197=CARTESIAN_POINT ( 'NONE',  ( 0.8107537697050253289, 0.1574803149606300301, 0.2485236219397170265 ) ) ;
#36198=ORIENTED_EDGE ( 'NONE', *, *, #14473, .F. ) ;
#36202=CARTESIAN_POINT ( 'NONE',  ( 0.8759842519685039353, -0.1574803149606299191, 1.840551180994834501 ) ) ;
#36205=CARTESIAN_POINT ( 'NONE',  ( -0.9412147342319837628, -0.1574803149606297803, 0.1500984250893234451 ) ) ;
#36207=CARTESIAN_POINT ( 'NONE',  ( 0.9412147342319837628, 0.1574803149606300301, 0.9916338581601894520 ) ) ;
#36208=( BOUNDED_CURVE ( )  B_SPLINE_CURVE ( 2, ( #46144, #46380, #9266, #5421, #42062, #13559, #27272, #20040, #5901 ),
 .UNSPECIFIED., .F., .T. ) 
 B_SPLINE_CURVE_WITH_KNOTS ( ( 3, 2, 2, 2, 3 ),
 ( 0.5999999999999999778, 0.6025000000000000355, 0.6049999999999999822, 0.6075000000000000400, 0.6099999999999999867 ),
 .UNSPECIFIED. ) 
 CURVE ( )  GEOMETRIC_REPRESENTATION_ITEM ( )  RATIONAL_B_SPLINE_CURVE ( ( 1.000000000000000000, 0.9238795325112869605, 1.000000000000000000, 0.9238795325112869605, 1.000000000000000000, 0.9238795325112869605, 1.000000000000000000, 0.9238795325112829637, 1.000000000000000000 ) ) 
 REPRESENTATION_ITEM ( '' )  ) ;
#36210=CARTESIAN_POINT ( 'NONE',  ( -1.054774247047244540, -0.07405724077823318263, 0.3346456692375748831 ) ) ;
#36212=ORIENTED_EDGE ( 'NONE', *, *, #8645, .F. ) ;
#36214=CARTESIAN_POINT ( 'NONE',  ( -0.8019270111902717657, 0.1787899950787401604, 1.653543307032850462 ) ) ;
#36215=EDGE_CURVE ( 'NONE', #5433, #33302, #24049, .T. ) ;
#36216=CARTESIAN_POINT ( 'NONE',  ( 0.6971942568897637749, 2.189545951927499583E-17, 1.621555118056472455 ) ) ;
#36217=EDGE_CURVE ( 'NONE', #2118, #34930, #10964, .T. ) ;
#36218=CARTESIAN_POINT ( 'NONE',  ( -0.9500414927467378812, -0.1787899950787401604, 0.8070866141194653620 ) ) ;
#36221=CARTESIAN_POINT ( 'NONE',  ( 1.054774247047244096, 0.000000000000000000, 0.1845472440407248116 ) ) ;
#36222=CARTESIAN_POINT ( 'NONE',  ( -0.8107537697050254399, -0.1574803149606297803, 0.4601377951680635792 ) ) ;
#36223=CARTESIAN_POINT ( 'NONE',  ( -0.9500414927467377701, -0.1787899950787401604, 0.6840551180564720113 ) ) ;
#36224=LINE ( 'NONE', #6962, #11617 ) ;
#36228=ORIENTED_EDGE ( 'NONE', *, *, #43595, .F. ) ;
#36229=CARTESIAN_POINT ( 'NONE',  ( -0.9412147342319837628, 0.1574803149606300301, 1.513287401574803681 ) ) ;
#36230=CARTESIAN_POINT ( 'NONE',  ( -0.9412147342319837628, -0.1574803149606297803, 0.3961614173228344971 ) ) ;
#36231=CARTESIAN_POINT ( 'NONE',  ( 0.9500414927467377701, -0.1787899950787401604, 1.397637795221827517 ) ) ;
#36234=ADVANCED_FACE ( 'NONE', ( #31714 ), #19953, .T. ) ;
#36238=ORIENTED_EDGE ( 'NONE', *, *, #1961, .F. ) ;
#36239=CARTESIAN_POINT ( 'NONE',  ( -0.7185039370078739607, 0.000000000000000000, -2.869337061179095023E-17 ) ) ;
#36250=CARTESIAN_POINT ( 'NONE',  ( 1.054774247047244540, 0.07405724077823318263, 0.5757874015210394658 ) ) ;
#36251=CARTESIAN_POINT ( 'NONE',  ( -0.8759842519685039353, -0.1787899950787401882, 0.9621062991588346103 ) ) ;
#36252=DIRECTION ( 'NONE',  ( 1.822029033848725028E-16, 0.000000000000000000, 1.000000000000000000 ) ) ;
#36253=CARTESIAN_POINT ( 'NONE',  ( 0.8759842519685039353, 0.1574803149606299191, 1.702755905404283565 ) ) ;
#36255=CARTESIAN_POINT ( 'NONE',  ( 0.9873396505805591694, -0.1113553986120547346, 1.697834645669291209 ) ) ;
#36256=CARTESIAN_POINT ( 'NONE',  ( 1.054774247047244540, -0.07405724077823318263, 1.717519684985606476 ) ) ;
#36259=CARTESIAN_POINT ( 'NONE',  ( 0.8019270111902716547, -0.1787899950787401604, 0.4822834645131655606 ) ) ;
#36261=EDGE_CURVE ( 'NONE', #26896, #3387, #45576, .T. ) ;
#36265=CARTESIAN_POINT ( 'NONE',  ( -0.6971942568897626646, 0.07405724077823318263, 0.3986220471903312301 ) ) ;
#36266=CARTESIAN_POINT ( 'NONE',  ( 0.6971942568897626646, -0.07405724077823297447, 0.6348425196312760255 ) ) ;
#36268=CARTESIAN_POINT ( 'NONE',  ( 1.054774247047244540, 0.07405724077823318263, 0.06889763774151215492 ) ) ;
#36270=CARTESIAN_POINT ( 'NONE',  ( -0.8759842519685039353, -0.1787899950787401882, 1.547736220418677089 ) ) ;
#36272=CARTESIAN_POINT ( 'NONE',  ( -1.054774247047244540, 0.07405724077823318263, 1.171259842465921741 ) ) ;
#36275=CARTESIAN_POINT ( 'NONE',  ( 1.054774247047244096, 0.000000000000000000, 1.208169291284818980 ) ) ;
#36276=CARTESIAN_POINT ( 'NONE',  ( -0.7185039370078746268, -0.06523048226347956391, 0.7308070865066471633 ) ) ;
#36277=CARTESIAN_POINT ( 'NONE',  ( 1.054774247047244540, -0.07405724077823318263, 1.751968503883245765 ) ) ;
#36278=CARTESIAN_POINT ( 'NONE',  ( -0.9412147342319837628, 0.1574803149606300301, 0.5684055118110235005 ) ) ;
#36279=CARTESIAN_POINT ( 'NONE',  ( -0.7495606340400177148, -0.1264236179284866091, 0.9128937007336377363 ) ) ;
#36280=CARTESIAN_POINT ( 'NONE',  ( -0.9412147342319837628, -0.1574803149606297803, 1.616633858267715773 ) ) ;
#36282=CARTESIAN_POINT ( 'NONE',  ( 0.8759842519685039353, -0.1787899950787401882, 0.3321850393163153226 ) ) ;
#36283=CARTESIAN_POINT ( 'NONE',  ( -1.054774247047244540, 0.07405724077823318263, 0.2608267715997797387 ) ) ;
#36284=CARTESIAN_POINT ( 'NONE',  ( -0.6971942568897626646, -0.07405724077823297447, 0.6742125983714335469 ) ) ;
#36285=CARTESIAN_POINT ( 'NONE',  ( 0.8759842519685039353, -0.1574803149606299191, 1.564960629813732185 ) ) ;
#36289=CARTESIAN_POINT ( 'NONE',  ( 1.054774247047244540, -0.07405724077823318263, 0.7332677164816707727 ) ) ;
#36290=CARTESIAN_POINT ( 'NONE',  ( 0.7495606340400177148, -0.1264236179284866091, 1.075295275536787276 ) ) ;
#36291=CARTESIAN_POINT ( 'NONE',  ( -1.054774247047244540, -0.07405724077823318263, 1.909448818843873186 ) ) ;
#36294=CARTESIAN_POINT ( 'NONE',  ( -0.7185039370078746268, -0.06523048226347956391, 0.1894685039370079815 ) ) ;
#36296=CONICAL_SURFACE ( 'NONE', #14832, 0.1787899950787401049, 1.047197551196598297 ) ;
#36300=CARTESIAN_POINT ( 'NONE',  ( 0.6971942568897637749, 2.189545951927499583E-17, 1.222933070812378009 ) ) ;
#36302=EDGE_CURVE ( 'NONE', #36580, #5319, #16616, .T. ) ;
#36304=CARTESIAN_POINT ( 'NONE',  ( 0.8759842519685039353, -0.1574803149606299191, 1.968503937007874072 ) ) ;
#36307=CARTESIAN_POINT ( 'NONE',  ( -0.8019270111902716547, 0.1787899950787401604, 0.5118110235682844511 ) ) ;
#36310=CARTESIAN_POINT ( 'NONE',  ( 1.033464566929133799, 0.000000000000000000, 1.427165354330708569 ) ) ;
#36311=CARTESIAN_POINT ( 'NONE',  ( 1.054774247047244540, 0.07405724077823318263, 1.289370078686393750 ) ) ;
#36312=CARTESIAN_POINT ( 'NONE',  ( 1.002407869896990045, 0.1264236179284866091, 1.719980314906866203 ) ) ;
#36314=CARTESIAN_POINT ( 'NONE',  ( 0.9873396505805591694, 0.1113553986120547346, 0.01476377952755905665 ) ) ;
#36315=LINE ( 'NONE', #10435, #45827 ) ;
#36316=CARTESIAN_POINT ( 'NONE',  ( -0.7633311516264269514, 0.1159584800571472618, 1.980764034584741706 ) ) ;
#36318=CARTESIAN_POINT ( 'NONE',  ( -0.9873396505805591694, 0.1113553986120547346, 1.658464566821606256 ) ) ;
#36319=CARTESIAN_POINT ( 'NONE',  ( 0.9500414927467378812, -0.1787899950787401604, 0.09350393695411057804 ) ) ;
#36320=EDGE_CURVE ( 'NONE', #39036, #1915, #21483, .T. ) ;
#36321=CARTESIAN_POINT ( 'NONE',  ( 0.7027381063308457687, 0.03433744138758834663, 0.03937047675465409763 ) ) ;
#36322=CARTESIAN_POINT ( 'NONE',  ( 0.8019270111902716547, -0.1787899950787401604, 1.190944881836001112 ) ) ;
#36323=CARTESIAN_POINT ( 'NONE',  ( -0.8107537697050254399, -0.1574803149606297803, 0.5388779526483779003 ) ) ;
#36324=CARTESIAN_POINT ( 'NONE',  ( -0.8759842519685039353, -0.1574803149606299191, 1.919291338475149544 ) ) ;
#36325=CARTESIAN_POINT ( 'NONE',  ( -0.9500414927467378812, -0.1787899950787401604, 1.195866141678520345 ) ) ;
#36326=CARTESIAN_POINT ( 'NONE',  ( 1.033464566929134687, 0.06523048226347956391, 0.4749015746956221085 ) ) ;
#36328=AXIS2_PLACEMENT_3D ( 'NONE', #29731, #29019, #44273 ) ;
#36330=CARTESIAN_POINT ( 'NONE',  ( 0.9213771321876901288, 0.1657552102673074401, 0.03937007882159332395 ) ) ;
#36331=CARTESIAN_POINT ( 'NONE',  ( -1.033464566929133799, 0.000000000000000000, 0.3937007872940480047 ) ) ;
#36333=CARTESIAN_POINT ( 'NONE',  ( 1.054774247047244540, 0.07405724077823318263, 1.481299212544662680 ) ) ;
#36334=EDGE_CURVE ( 'NONE', #13902, #28460, #32431, .T. ) ;
#36335=CARTESIAN_POINT ( 'NONE',  ( -1.033464566929134687, 0.06523048226347956391, 0.09104330708661413640 ) ) ;
#36336=CARTESIAN_POINT ( 'NONE',  ( 0.8759842519685039353, 0.000000000000000000, 4.498031496062992574 ) ) ;
#36340=EDGE_LOOP ( 'NONE', ( #35392, #20977, #19038, #28398 ) ) ;
#36343=CARTESIAN_POINT ( 'NONE',  ( 0.8019270111902717657, 0.1787899950787401604, 0.5118110235682844511 ) ) ;
#36345=CARTESIAN_POINT ( 'NONE',  ( -0.6971942568897648851, -0.07405724077823297447, 1.500984251914741829 ) ) ;
#36347=CARTESIAN_POINT ( 'NONE',  ( -0.6971942568897637749, 2.189545951927499583E-17, 1.188484251914740275 ) ) ;
#36348=CARTESIAN_POINT ( 'NONE',  ( -0.7185039370078739607, 1.928577636452523993E-17, 0.1082677165354330728 ) ) ;
#36350=CARTESIAN_POINT ( 'NONE',  ( -0.6971942568897648851, 0.07405724077823318263, 1.023622047190330342 ) ) ;
#36351=CARTESIAN_POINT ( 'NONE',  ( -0.8019270111902717657, -0.1787899950787401604, 0.8415354330171019859 ) ) ;
#36352=CARTESIAN_POINT ( 'NONE',  ( -1.054774247047244096, 0.000000000000000000, 0.1845472440407248116 ) ) ;
#36360=AXIS2_PLACEMENT_3D ( 'NONE', #17054, #9874, #28099 ) ;
#36363=CARTESIAN_POINT ( 'NONE',  ( 0.8107537697050254399, 0.1574803149606300301, 0.7701771653543307838 ) ) ;
#36365=CARTESIAN_POINT ( 'NONE',  ( -0.8759842519685039353, -0.1787899950787401882, 0.7603346456155274380 ) ) ;
#36367=CARTESIAN_POINT ( 'NONE',  ( -1.002407869896990045, 0.1264236179284866091, 1.843011810969858333 ) ) ;
#36368=CARTESIAN_POINT ( 'NONE',  ( 0.7646288533564489232, -0.1113553986120547346, 0.7037401574803149318 ) ) ;
#36371=CARTESIAN_POINT ( 'NONE',  ( -1.033464566929133799, 0.000000000000000000, 1.338582677057826853 ) ) ;
#36372=CARTESIAN_POINT ( 'NONE',  ( 0.6971942568897626646, -0.07405724077823297447, 0.7972440944344250102 ) ) ;
#36376=CARTESIAN_POINT ( 'NONE',  ( 1.033464566929133799, 0.000000000000000000, 1.574803149498771537 ) ) ;
#36377=CARTESIAN_POINT ( 'NONE',  ( 1.033464566929134687, 0.06523048226347956391, 1.232775590551179912 ) ) ;
#36378=CARTESIAN_POINT ( 'NONE',  ( 0.8528693833544092051, -0.1722797369867551665, 1.987786336861242287 ) ) ;
#36380=DIRECTION ( 'NONE',  ( 1.000000000000000000, 0.000000000000000000, -1.822029033848725275E-16 ) ) ;
#36383=CARTESIAN_POINT ( 'NONE',  ( 1.054774247047244540, -0.07405724077823318263, 0.6102362204186774219 ) ) ;
#36384=CYLINDRICAL_SURFACE ( 'NONE', #22334, 0.1574803149606299191 ) ;
#36387=( BOUNDED_CURVE ( )  B_SPLINE_CURVE ( 2, ( #37023, #22154, #15000, #33225, #29651, #26009, #7780, #22395, #4174 ),
 .UNSPECIFIED., .F., .T. ) 
 B_SPLINE_CURVE_WITH_KNOTS ( ( 3, 2, 2, 2, 3 ),
 ( 0.8000000000000000444, 0.8024999999999999911, 0.8050000000000000488, 0.8074999999999999956, 0.8100000000000000533 ),
 .UNSPECIFIED. ) 
 CURVE ( )  GEOMETRIC_REPRESENTATION_ITEM ( )  RATIONAL_B_SPLINE_CURVE ( ( 1.000000000000000000, 0.9238795325112869605, 1.000000000000000000, 0.9238795325112869605, 1.000000000000000000, 0.9238795325112869605, 1.000000000000000000, 0.9238795325112869605, 1.000000000000000000 ) ) 
 REPRESENTATION_ITEM ( '' )  ) ;
#36388=ORIENTED_EDGE ( 'NONE', *, *, #18537, .T. ) ;
#36389=CARTESIAN_POINT ( 'NONE',  ( -0.8759842519685039353, 0.1574803149606299191, 1.161417322834645605 ) ) ;
#36392=CARTESIAN_POINT ( 'NONE',  ( 0.8759842519685039353, 0.1787899950787401882, 1.016240157426551161 ) ) ;
#36394=CARTESIAN_POINT ( 'NONE',  ( 0.7185039370078739607, 1.928577636452523993E-17, 1.604330708661417360 ) ) ;
#36398=CARTESIAN_POINT ( 'NONE',  ( -0.8759842519685039353, -0.1787899950787401882, 0.1697834645131655606 ) ) ;
#36399=CARTESIAN_POINT ( 'NONE',  ( -0.6971942568897648851, 0.07405724077823318263, 1.934055118056471567 ) ) ;
#36400=CARTESIAN_POINT ( 'NONE',  ( -0.6971942568897648851, -0.07405724077823297447, 1.737204724355685848 ) ) ;
#36401=CARTESIAN_POINT ( 'NONE',  ( -0.8759842519685039353, 0.1787899950787401882, 1.055610236166708793 ) ) ;
#36402=CARTESIAN_POINT ( 'NONE',  ( -0.9500414927467378812, 0.1787899950787401604, 0.4281496062454490659 ) ) ;
#36405=CARTESIAN_POINT ( 'NONE',  ( -1.033464566929133799, 0.000000000000000000, 1.899606299212598604 ) ) ;
#36411=CARTESIAN_POINT ( 'NONE',  ( -1.054774247047244540, -0.07405724077823318263, 0.2952755904974176393 ) ) ;
#36413=CARTESIAN_POINT ( 'NONE',  ( -0.6971942568897637749, 2.189545951927499583E-17, 1.306594488135212728 ) ) ;
#36415=AXIS2_PLACEMENT_3D ( 'NONE', #10229, #32524, #43749 ) ;
#36419=CARTESIAN_POINT ( 'NONE',  ( 0.8759842519685039353, -0.1574803149606299191, 0.3543307086614173040 ) ) ;
#36422=CARTESIAN_POINT ( 'NONE',  ( -0.7185039370078739607, 1.928577636452523993E-17, 0.9251968502861732668 ) ) ;
#36423=CARTESIAN_POINT ( 'NONE',  ( 0.8759842519685039353, 0.1787899950787401882, 0.4306102361667086820 ) ) ;
#36425=ORIENTED_EDGE ( 'NONE', *, *, #21041, .F. ) ;
#36426=CARTESIAN_POINT ( 'NONE',  ( 0.7646288533564489232, -0.1113553986120547346, 1.796259842412157415 ) ) ;
#36428=CARTESIAN_POINT ( 'NONE',  ( 0.9873396505805591694, -0.1113553986120547346, 0.2312992124908980207 ) ) ;
#36429=CARTESIAN_POINT ( 'NONE',  ( 0.9873396505805591694, 0.1113553986120547346, 0.7627952755905511584 ) ) ;
#36430=CARTESIAN_POINT ( 'NONE',  ( -0.8759842519685039353, 0.1574803149606299191, 1.082677165354330784 ) ) ;
#36431=EDGE_CURVE ( 'NONE', #47229, #2766, #29527, .T. ) ;
#36432=FACE_OUTER_BOUND ( 'NONE', #23102, .T. ) ;
#36433=CARTESIAN_POINT ( 'NONE',  ( 0.8759842519685039353, 0.1574803149606299191, 0.2066929132782996115 ) ) ;
#36443=CARTESIAN_POINT ( 'NONE',  ( -1.033464566929134687, 0.06523048226347956391, 0.1599409447743626866 ) ) ;
#36445=CARTESIAN_POINT ( 'NONE',  ( 0.9873396505805591694, 0.1113553986120547346, 0.9891732282389291697 ) ) ;
#36447=ORIENTED_EDGE ( 'NONE', *, *, #18770, .F. ) ;
#36449=CARTESIAN_POINT ( 'NONE',  ( -1.054774247047244540, 0.07405724077823318263, 1.564960629867495845 ) ) ;
#36450=ORIENTED_EDGE ( 'NONE', *, *, #32438, .F. ) ;
#36451=CARTESIAN_POINT ( 'NONE',  ( 0.8759842519685039353, -0.1787899950787401882, 1.552657480261196765 ) ) ;
#36452=CARTESIAN_POINT ( 'NONE',  ( -0.8019270111902717657, 0.1787899950787401604, 0.7874015747493863238 ) ) ;
#36454=CARTESIAN_POINT ( 'NONE',  ( 1.002407869896990045, -0.1264236179284866091, 0.7308070865604093802 ) ) ;
#36455=CARTESIAN_POINT ( 'NONE',  ( -0.7495606340400177148, -0.1264236179284866091, 0.6766732282926929409 ) ) ;
#36457=CARTESIAN_POINT ( 'NONE',  ( -1.002407869896990045, 0.1264236179284866091, 1.646161417269070837 ) ) ;
#36458=CARTESIAN_POINT ( 'NONE',  ( -0.8107537697050253289, -0.1574803149606297803, 1.956200787294048338 ) ) ;
#36460=CARTESIAN_POINT ( 'NONE',  ( 0.7185039370078760701, -0.06523048226348075740, 0.9670275589475921807 ) ) ;
#36461=CARTESIAN_POINT ( 'NONE',  ( 0.9500414927467377701, 0.1787899950787401604, 1.491141732229701145 ) ) ;
#36463=CARTESIAN_POINT ( 'NONE',  ( -0.8107537697050254399, 0.1574803149606300301, 0.3666338581601893964 ) ) ;
#36465=EDGE_CURVE ( 'NONE', #10105, #38268, #10615, .T. ) ;
#36467=ORIENTED_EDGE ( 'NONE', *, *, #41740, .F. ) ;
#36469=ORIENTED_EDGE ( 'NONE', *, *, #43149, .F. ) ;
#36472=FACE_OUTER_BOUND ( 'NONE', #16928, .T. ) ;
#36474=CARTESIAN_POINT ( 'NONE',  ( 0.9500414927467378812, 0.1787899950787401604, 1.761811023568284007 ) ) ;
#36475=CARTESIAN_POINT ( 'NONE',  ( 0.6971942568897626646, 0.07405724077823318263, 0.3543307086076538659 ) ) ;
#36476=CARTESIAN_POINT ( 'NONE',  ( 0.7646288533564489232, 0.1113553986120547346, 0.3001968503937008093 ) ) ;
#36482=CARTESIAN_POINT ( 'NONE',  ( 1.054774247047244540, 0.07405724077823318263, 0.6545275590013545086 ) ) ;
#36483=( BOUNDED_CURVE ( )  B_SPLINE_CURVE ( 2, ( #32955, #13379, #14488, #43703, #13156, #42572, #38534, #21677, #6160 ),
 .UNSPECIFIED., .F., .T. ) 
 B_SPLINE_CURVE_WITH_KNOTS ( ( 3, 2, 2, 2, 3 ),
 ( 0.3200000000000000067, 0.3225000000000000089, 0.3250000000000000111, 0.3275000000000000133, 0.3300000000000000155 ),
 .UNSPECIFIED. ) 
 CURVE ( )  GEOMETRIC_REPRESENTATION_ITEM ( )  RATIONAL_B_SPLINE_CURVE ( ( 1.000000000000000000, 0.9238795325112869605, 1.000000000000000000, 0.9238795325112869605, 1.000000000000000000, 0.9238795325112869605, 1.000000000000000000, 0.9238795325112869605, 1.000000000000000000 ) ) 
 REPRESENTATION_ITEM ( '' )  ) ;
#36485=CARTESIAN_POINT ( 'NONE',  ( 0.8759842519685039353, 0.1574803149606299191, 1.122047244094488194 ) ) ;
#36488=CARTESIAN_POINT ( 'NONE',  ( 0.6971942568897648851, -0.07405724077823297447, 1.702755905458047003 ) ) ;
#36494=CARTESIAN_POINT ( 'NONE',  ( 0.7185039370078739607, 1.928577636452523993E-17, 0.4921259841444416971 ) ) ;
#36496=CARTESIAN_POINT ( 'NONE',  ( 1.002407869896990045, 0.1264236179284866091, 0.07135826766277185429 ) ) ;
#36498=EDGE_CURVE ( 'NONE', #21060, #7011, #9883, .T. ) ;
#36499=CARTESIAN_POINT ( 'NONE',  ( -1.002407869896990045, -0.1264236179284866091, 1.592027559001354398 ) ) ;
#36501=CARTESIAN_POINT ( 'NONE',  ( -0.9500414927467378812, -0.1787899950787401604, 1.200787401521039355 ) ) ;
#36502=CARTESIAN_POINT ( 'NONE',  ( 0.9412147342319837628, -0.1574803149606297803, 1.026082677165353729 ) ) ;
#36503=CARTESIAN_POINT ( 'NONE',  ( 0.8019270111902717657, 0.1787899950787401604, 1.102362204670646495 ) ) ;
#36504=CARTESIAN_POINT ( 'NONE',  ( 0.8019270111902717657, -0.1787899950787401604, 1.860236220418677089 ) ) ;
#36505=CARTESIAN_POINT ( 'NONE',  ( -0.7646288533564489232, -0.1113553986120547346, 0.5462598425196850682 ) ) ;
#36506=CARTESIAN_POINT ( 'NONE',  ( -1.054774247047244096, 0.000000000000000000, 1.045767716481669440 ) ) ;
#36509=CARTESIAN_POINT ( 'NONE',  ( 0.8759842519685039353, 0.1787899950787401882, 0.2731299212060791515 ) ) ;
#36510=CARTESIAN_POINT ( 'NONE',  ( -1.054774247047244096, 0.000000000000000000, 0.2977362204186775885 ) ) ;
#36511=CARTESIAN_POINT ( 'NONE',  ( -1.054774247047244540, -0.07405724077823318263, 0.6889763778989935750 ) ) ;
#36512=CARTESIAN_POINT ( 'NONE',  ( 0.9412147342319837628, -0.1574803149606297803, 1.685531495955465697 ) ) ;
#36514=( BOUNDED_CURVE ( )  B_SPLINE_CURVE ( 2, ( #5501, #12486, #24202, #13188, #34761, #37871, #35229, #8864, #42137 ),
 .UNSPECIFIED., .F., .T. ) 
 B_SPLINE_CURVE_WITH_KNOTS ( ( 3, 2, 2, 2, 3 ),
 ( 0.2800000000000000266, 0.2824999999999999734, 0.2849999999999999756, 0.2874999999999999778, 0.2899999999999999800 ),
 .UNSPECIFIED. ) 
 CURVE ( )  GEOMETRIC_REPRESENTATION_ITEM ( )  RATIONAL_B_SPLINE_CURVE ( ( 1.000000000000000000, 0.9238795325112869605, 1.000000000000000000, 0.9238795325112869605, 1.000000000000000000, 0.9238795325112869605, 1.000000000000000000, 0.9238795325112869605, 1.000000000000000000 ) ) 
 REPRESENTATION_ITEM ( '' )  ) ;
#36516=CARTESIAN_POINT ( 'NONE',  ( 0.9500414927467378812, 0.1787899950787401604, 0.7431102361667091261 ) ) ;
#36517=CARTESIAN_POINT ( 'NONE',  ( 0.8019270111902716547, -0.1787899950787401604, 0.9990157479777320715 ) ) ;
#36518=CARTESIAN_POINT ( 'NONE',  ( -0.8019270111902716547, 0.1787899950787401604, 1.884842519631275026 ) ) ;
#36519=CARTESIAN_POINT ( 'NONE',  ( 1.054774247047244540, 0.07405724077823318263, 1.874999999946236784 ) ) ;
#36521=CARTESIAN_POINT ( 'NONE',  ( 0.7185039370078739607, 1.928577636452523993E-17, 1.328740157480315043 ) ) ;
#36525=CARTESIAN_POINT ( 'NONE',  ( -0.7185039370078692977, 0.06523048226347515077, 1.710137795168064079 ) ) ;
#36527=CARTESIAN_POINT ( 'NONE',  ( 0.7495606340400177148, 0.1264236179284866091, 1.139271653489543290 ) ) ;
#36531=CARTESIAN_POINT ( 'NONE',  ( 0.9412147342319837628, -0.1574803149606297803, 1.970964566929134021 ) ) ;
#36535=CARTESIAN_POINT ( 'NONE',  ( -0.9500414927467377701, 0.1787899950787401604, 0.4675196849856070314 ) ) ;
#36539=CARTESIAN_POINT ( 'NONE',  ( 0.6971942568897648851, 0.07405724077823318263, 1.186023621993481658 ) ) ;
#36540=CARTESIAN_POINT ( 'NONE',  ( 0.9500414927467377701, 0.1787899950787401604, 1.722440944828126153 ) ) ;
#36541=DIRECTION ( 'NONE',  ( 1.822029033848725028E-16, 0.000000000000000000, 1.000000000000000000 ) ) ;
#36545=CARTESIAN_POINT ( 'NONE',  ( 1.033464566929133799, 0.000000000000000000, 0.7480314959554645871 ) ) ;
#36546=CARTESIAN_POINT ( 'NONE',  ( 1.054774247047244540, -0.07405724077823318263, 0.2165354330171024577 ) ) ;
#36547=CARTESIAN_POINT ( 'NONE',  ( 0.7287427869149385451, -0.08289353061996172778, 0.03937277022166233570 ) ) ;
#36550=CARTESIAN_POINT ( 'NONE',  ( -0.6971942568897637749, 2.189545951927499583E-17, 1.183562992072220599 ) ) ;
#36551=CARTESIAN_POINT ( 'NONE',  ( 0.9412147342319837628, 0.1574803149606300301, 0.6766732282389293918 ) ) ;
#36553=CARTESIAN_POINT ( 'NONE',  ( -0.6971942568897648851, 0.07405724077823318263, 1.067913385773007651 ) ) ;
#36555=CARTESIAN_POINT ( 'NONE',  ( 0.8518726721728578921, 0.1743242345900581913, 0.03937026678633583771 ) ) ;
#36557=CARTESIAN_POINT ( 'NONE',  ( -0.7185039370078746268, 0.06523048226347956391, 0.4502952754830242266 ) ) ;
#36559=CARTESIAN_POINT ( 'NONE',  ( 0.6971942568897648851, -0.07405724077823297447, 1.422244094434426120 ) ) ;
#36560=FACE_OUTER_BOUND ( 'NONE', #19206, .T. ) ;
#36561=CARTESIAN_POINT ( 'NONE',  ( -0.9500414927467377701, 0.1787899950787401604, 0.06889763774151215492 ) ) ;
#36565=CARTESIAN_POINT ( 'NONE',  ( 0.8759842519685039353, -0.1574803149606299191, 0.6594488187901103027 ) ) ;
#36568=CARTESIAN_POINT ( 'NONE',  ( 1.054774247047244540, 0.07405724077823318263, 0.6594488188438737408 ) ) ;
#36569=VERTEX_POINT ( 'NONE', #11316 ) ;
#36570=CARTESIAN_POINT ( 'NONE',  ( -1.054774247047244096, 0.000000000000000000, 1.439468503883244210 ) ) ;
#36572=CARTESIAN_POINT ( 'NONE',  ( -0.6971942568897637749, 2.189545951927499583E-17, 1.070374015694267600 ) ) ;
#36574=CARTESIAN_POINT ( 'NONE',  ( -0.8759842519685039353, 0.1787899950787401882, 0.8636811023084409733 ) ) ;
#36576=CARTESIAN_POINT ( 'NONE',  ( -1.033464566929133799, 0.000000000000000000, 1.889763779420031486 ) ) ;
#36578=VERTEX_POINT ( 'NONE', #15627 ) ;
#36579=CARTESIAN_POINT ( 'NONE',  ( 0.7167570750452111339, 0.08279236175412563181, 0.03937007863263047164 ) ) ;
#36580=VERTEX_POINT ( 'NONE', #40510 ) ;
#36581=VERTEX_POINT ( 'NONE', #4096 ) ;
#36582=EDGE_CURVE ( 'NONE', #5868, #6940, #18133, .T. ) ;
#36583=CARTESIAN_POINT ( 'NONE',  ( -0.8107537697050254399, 0.1574803149606300301, 0.5634842518609766149 ) ) ;
#36584=CARTESIAN_POINT ( 'NONE',  ( -1.054774247047244540, 0.07405724077823318263, 0.7726377952218265177 ) ) ;
#36587=AXIS2_PLACEMENT_3D ( 'NONE', #28906, #3701, #18082 ) ;
#36590=CARTESIAN_POINT ( 'NONE',  ( -1.054774247047244096, 0.000000000000000000, 1.759350393647023614 ) ) ;
#36592=CARTESIAN_POINT ( 'NONE',  ( -0.9500414927467377701, -0.1787899950787401604, 0.09842519679663024046 ) ) ;
#36593=CARTESIAN_POINT ( 'NONE',  ( 0.9873396505805591694, 0.1113553986120547346, 0.6446850393700788162 ) ) ;
#36596=CARTESIAN_POINT ( 'NONE',  ( -0.9873396505805591694, -0.1113553986120547346, 1.491141732175936818 ) ) ;
#36597=CARTESIAN_POINT ( 'NONE',  ( 1.054774247047244540, -0.07405724077823318263, 0.8120078739619844832 ) ) ;
#36598=CARTESIAN_POINT ( 'NONE',  ( 0.9412147342319837628, 0.1574803149606300301, 0.1648622046168823629 ) ) ;
#36599=CARTESIAN_POINT ( 'NONE',  ( 0.8759842519685039353, 0.1574803149606299191, 1.397637795275590511 ) ) ;
#36600=CARTESIAN_POINT ( 'NONE',  ( 0.9315392539442560738, -0.1672740577352537228, 1.989187881297329152 ) ) ;
#36602=CARTESIAN_POINT ( 'NONE',  ( 1.033464566929133799, 0.000000000000000000, 1.496062992018456494 ) ) ;
#36604=CARTESIAN_POINT ( 'NONE',  ( 0.7495606340400177148, -0.1264236179284866091, 0.7947834645131652831 ) ) ;
#36607=DIRECTION ( 'NONE',  ( 1.822029033848725028E-16, 0.000000000000000000, 1.000000000000000000 ) ) ;
#36608=ORIENTED_EDGE ( 'NONE', *, *, #19997, .F. ) ;
#36609=CARTESIAN_POINT ( 'NONE',  ( 0.9412147342319837628, -0.1574803149606297803, 0.6225393699712132856 ) ) ;
#36610=LINE ( 'NONE', #18391, #2236 ) ;
#36611=CARTESIAN_POINT ( 'NONE',  ( 1.054774247047244540, 0.07405724077823318263, 0.9694881889226144578 ) ) ;
#36614=LINE ( 'NONE', #21511, #47456 ) ;
#36617=FACE_OUTER_BOUND ( 'NONE', #43628, .T. ) ;
#36618=CARTESIAN_POINT ( 'NONE',  ( -0.7495606340400177148, -0.1264236179284866091, 0.08612204719033110523 ) ) ;
#36620=LINE ( 'NONE', #37077, #35196 ) ;
#36621=CARTESIAN_POINT ( 'NONE',  ( -1.054774247047244096, 0.000000000000000000, 1.636318897584031484 ) ) ;
#36623=CARTESIAN_POINT ( 'NONE',  ( -1.054774247047244096, 0.000000000000000000, 1.085137795221826629 ) ) ;
#36625=CARTESIAN_POINT ( 'NONE',  ( -0.6971942568897637749, 2.189545951927499583E-17, 0.3617125983714334359 ) ) ;
#36626=CARTESIAN_POINT ( 'NONE',  ( 0.7646288533564489232, 0.1113553986120547346, 0.4084645668216063119 ) ) ;
#36627=CARTESIAN_POINT ( 'NONE',  ( 0.7495606340400177148, 0.1264236179284866091, 0.07627952750529173875 ) ) ;
#36632=CARTESIAN_POINT ( 'NONE',  ( -0.7495606340400177148, -0.1264236179284866091, 0.3617125983714334359 ) ) ;
#36633=ADVANCED_FACE ( 'NONE', ( #41200 ), #8406, .T. ) ;
#36634=ORIENTED_EDGE ( 'NONE', *, *, #17360, .T. ) ;
#36637=CARTESIAN_POINT ( 'NONE',  ( -0.9500414927467377701, 0.1787899950787401604, 1.333661417269071281 ) ) ;
#36638=EDGE_LOOP ( 'NONE', ( #10087, #536, #34378, #2856 ) ) ;
#36644=CARTESIAN_POINT ( 'NONE',  ( 1.033464566929134687, 0.06523048226347956391, 0.3666338582677165503 ) ) ;
#36646=CARTESIAN_POINT ( 'NONE',  ( -0.9412147342319837628, -0.1574803149606297803, 0.9374999998924736788 ) ) ;
#36649=CARTESIAN_POINT ( 'NONE',  ( 0.7185039370078746268, 0.06523048226347956391, 1.788877952648378233 ) ) ;
#36650=ORIENTED_EDGE ( 'NONE', *, *, #6974, .T. ) ;
#36652=CARTESIAN_POINT ( 'NONE',  ( 0.7646288533564489232, -0.1113553986120547346, 0.9399606299212598381 ) ) ;
#36654=CARTESIAN_POINT ( 'NONE',  ( 0.8759842519685039353, 0.1574803149606299191, 1.358267716535433323 ) ) ;
#36656=CARTESIAN_POINT ( 'NONE',  ( 0.8107537697050254399, -0.1574803149606297803, 1.532972440944882386 ) ) ;
#36661=DIRECTION ( 'NONE',  ( -1.000000000000000000, 0.000000000000000000, 0.000000000000000000 ) ) ;
#36666=CARTESIAN_POINT ( 'NONE',  ( -1.033464566929133799, 0.000000000000000000, 0.07874015737278799998 ) ) ;
#36668=CARTESIAN_POINT ( 'NONE',  ( 0.7185039370078746268, 0.06523048226347956391, 1.001476377845228027 ) ) ;
#36670=CARTESIAN_POINT ( 'NONE',  ( -1.002407869896990045, 0.1264236179284866091, 0.3813976377415121966 ) ) ;
#36672=EDGE_LOOP ( 'NONE', ( #14316, #17318, #25918, #47220 ) ) ;
#36673=ORIENTED_EDGE ( 'NONE', *, *, #29273, .T. ) ;
#36674=CARTESIAN_POINT ( 'NONE',  ( -1.002407869896990045, 0.1264236179284866091, 1.685531496009228469 ) ) ;
#36675=CARTESIAN_POINT ( 'NONE',  ( 1.002407869896990045, -0.1264236179284866091, 1.754429133804503715 ) ) ;
#36676=CARTESIAN_POINT ( 'NONE',  ( -0.8019270111902717657, 0.1787899950787401604, 0.8661417322297003674 ) ) ;
#36677=CARTESIAN_POINT ( 'NONE',  ( 0.6971942568897626646, -0.07405724077823297447, 0.3248031495525359746 ) ) ;
#36678=CARTESIAN_POINT ( 'NONE',  ( -0.7646288533564489232, 0.1113553986120547346, 0.2608267716535432879 ) ) ;
#36679=CARTESIAN_POINT ( 'NONE',  ( -0.7495606340400177148, -0.1264236179284866091, 0.7160433070328504623 ) ) ;
#36682=FACE_OUTER_BOUND ( 'NONE', #27850, .T. ) ;
#36683=CARTESIAN_POINT ( 'NONE',  ( -1.002407869896990045, 0.1264236179284866091, 1.606791338528913426 ) ) ;
#36684=CARTESIAN_POINT ( 'NONE',  ( -0.8107537697050253289, 0.1574803149606300301, 1.902066929026330788 ) ) ;
#36685=VERTEX_POINT ( 'NONE', #1212 ) ;
#36686=CARTESIAN_POINT ( 'NONE',  ( -0.7646288533564489232, -0.1113553986120547346, 1.648622047244094668 ) ) ;
#36688=CARTESIAN_POINT ( 'NONE',  ( 1.002407869896990045, -0.1264236179284866091, 1.400098425143086800 ) ) ;
#36689=CARTESIAN_POINT ( 'NONE',  ( -0.7646288533564489232, -0.1113553986120547346, 1.569881889763779625 ) ) ;
#36693=VERTEX_POINT ( 'NONE', #37894 ) ;
#36696=VERTEX_POINT ( 'NONE', #12262 ) ;
#36702=CARTESIAN_POINT ( 'NONE',  ( 1.054774247047244096, 0.000000000000000000, 1.793799212544661348 ) ) ;
#36706=CARTESIAN_POINT ( 'NONE',  ( 0.6971942568897626646, -0.07405724077823297447, 0.5561023621509617598 ) ) ;
#36711=CARTESIAN_POINT ( 'NONE',  ( 0.6971942568897648851, -0.07405724077823297447, 1.899606299158834943 ) ) ;
#36712=DIRECTION ( 'NONE',  ( 1.000000000000000000, 0.000000000000000000, -1.822029033848725275E-16 ) ) ;
#36713=CARTESIAN_POINT ( 'NONE',  ( 0.8107537697050254399, 0.1574803149606300301, 0.1304133857192446289 ) ) ;
#36715=LINE ( 'NONE', #11325, #22894 ) ;
#36717=CARTESIAN_POINT ( 'NONE',  ( -0.7495606340400177148, 0.1264236179284866091, 0.4355314960092284138 ) ) ;
#36718=AXIS2_PLACEMENT_3D ( 'NONE', #10824, #21338, #29311 ) ;
#36721=CARTESIAN_POINT ( 'NONE',  ( 0.6971942568897626646, 0.07405724077823318263, 0.1230314960092287191 ) ) ;
#36722=CARTESIAN_POINT ( 'NONE',  ( -0.8759842519685039353, 0.000000000000000000, 0.000000000000000000 ) ) ;
#36723=CARTESIAN_POINT ( 'NONE',  ( -1.054774247047244096, 0.000000000000000000, 1.557578740103716441 ) ) ;
#36725=CARTESIAN_POINT ( 'NONE',  ( -0.6971942568897648851, 0.07405724077823318263, 1.146653543253323582 ) ) ;
#36726=LINE ( 'NONE', #25947, #12314 ) ;
#36727=AXIS2_PLACEMENT_3D ( 'NONE', #6715, #37302, #11223 ) ;
#36728=CARTESIAN_POINT ( 'NONE',  ( 1.054774247047244540, -0.07405724077823318263, 1.245078740103716886 ) ) ;
#36730=CARTESIAN_POINT ( 'NONE',  ( -0.7646288533564489232, -0.1113553986120547346, 0.5856299212598424786 ) ) ;
#36731=CARTESIAN_POINT ( 'NONE',  ( -1.054774247047244096, 0.000000000000000000, 1.085137795221826629 ) ) ;
#36734=CARTESIAN_POINT ( 'NONE',  ( 0.7495606340400177148, 0.1264236179284866091, 0.3567913385289137596 ) ) ;
#36735=CARTESIAN_POINT ( 'NONE',  ( -0.6971942568897637749, 2.189545951927499583E-17, 0.1993110235682838682 ) ) ;
#36736=CARTESIAN_POINT ( 'NONE',  ( -1.002407869896990045, -0.1264236179284866091, 0.8046259841982047467 ) ) ;
#36737=CARTESIAN_POINT ( 'NONE',  ( 1.033464566929134687, -0.06523048226347956391, 1.690452755797984929 ) ) ;
#36740=CARTESIAN_POINT ( 'NONE',  ( 0.6971942568897637749, 2.189545951927499583E-17, 0.7554133857730077617 ) ) ;
#36741=CARTESIAN_POINT ( 'NONE',  ( 0.8759842519685039353, -0.1787899950787401882, 1.119586614119464585 ) ) ;
#36742=CARTESIAN_POINT ( 'NONE',  ( -1.054774247047244096, 0.000000000000000000, 1.833169291284818758 ) ) ;
#36743=ORIENTED_EDGE ( 'NONE', *, *, #11703, .T. ) ;
#36744=EDGE_CURVE ( 'NONE', #35290, #22349, #13198, .T. ) ;
#36745=CARTESIAN_POINT ( 'NONE',  ( 0.7495606340400177148, -0.1264236179284866091, 1.897145669237574772 ) ) ;
#36746=ADVANCED_FACE ( 'NONE', ( #19430 ), #46239, .T. ) ;
#36748=CARTESIAN_POINT ( 'NONE',  ( 0.8759842519685039353, -0.1574803149606299191, 1.604330708553889595 ) ) ;
#36752=CARTESIAN_POINT ( 'NONE',  ( -0.8759842519685039353, 0.1574803149606299191, 1.702755905404283565 ) ) ;
#36754=CARTESIAN_POINT ( 'NONE',  ( 0.6971942568897648851, -0.07405724077823297447, 1.186023621993481658 ) ) ;
#36757=CARTESIAN_POINT ( 'NONE',  ( 0.8107537697050254399, 0.1574803149606300301, 1.390255905404285119 ) ) ;
#36758=( BOUNDED_CURVE ( )  B_SPLINE_CURVE ( 2, ( #18388, #35889, #3043, #32564, #28489, #14335, #28980, #25360, #25601 ),
 .UNSPECIFIED., .F., .T. ) 
 B_SPLINE_CURVE_WITH_KNOTS ( ( 3, 2, 2, 2, 3 ),
 ( 0.1700000000000000122, 0.1724999999999999867, 0.1749999999999999889, 0.1774999999999999911, 0.1799999999999999933 ),
 .UNSPECIFIED. ) 
 CURVE ( )  GEOMETRIC_REPRESENTATION_ITEM ( )  RATIONAL_B_SPLINE_CURVE ( ( 1.000000000000000000, 0.9238795325112869605, 1.000000000000000000, 0.9238795325112869605, 1.000000000000000000, 0.9238795325112869605, 1.000000000000000000, 0.9238795325112869605, 1.000000000000000000 ) ) 
 REPRESENTATION_ITEM ( '' )  ) ;
#36759=CARTESIAN_POINT ( 'NONE',  ( 1.002407869896990045, -0.1264236179284866091, 1.473917322780881722 ) ) ;
#36760=CARTESIAN_POINT ( 'NONE',  ( 0.7495606340400177148, 0.1264236179284866091, 0.1156496062454492185 ) ) ;
#36763=CARTESIAN_POINT ( 'NONE',  ( -1.002407869896990045, 0.1264236179284866091, 0.4256889763241890057 ) ) ;
#36766=CARTESIAN_POINT ( 'NONE',  ( 0.8107537697050254399, 0.1574803149606300301, 1.439468503937006760 ) ) ;
#36767=CARTESIAN_POINT ( 'NONE',  ( 0.8019270111902717657, 0.1787899950787401604, 1.377952755851748146 ) ) ;
#36768=CARTESIAN_POINT ( 'NONE',  ( 0.6971942568897648851, -0.07405724077823297447, 1.658464566875369472 ) ) ;
#36769=DIRECTION ( 'NONE',  ( 1.000000000000000000, 0.000000000000000000, -1.822029033848725275E-16 ) ) ;
#36773=CARTESIAN_POINT ( 'NONE',  ( 0.8759842519685039353, 0.000000000000000000, 4.498031496062992574 ) ) ;
#36776=CARTESIAN_POINT ( 'NONE',  ( 0.9500414927467378812, -0.1787899950787401604, 0.2509842519147403861 ) ) ;
#36777=CARTESIAN_POINT ( 'NONE',  ( 0.7182464370288005329, -0.06544858470024300656, 0.03937008086776665194 ) ) ;
#36778=CARTESIAN_POINT ( 'NONE',  ( 1.054774247047244096, 0.000000000000000000, 1.281988188922614125 ) ) ;
#36782=CARTESIAN_POINT ( 'NONE',  ( -0.8759842519685039353, -0.1787899950787401882, 1.193405511757259951 ) ) ;
#36783=CARTESIAN_POINT ( 'NONE',  ( 0.7185039370078746268, -0.06523048226347956391, 0.7308070865066471633 ) ) ;
#36786=CARTESIAN_POINT ( 'NONE',  ( 0.8915560649286792261, 0.1728905949868962677, 0.03937011864913666365 ) ) ;
#36787=CARTESIAN_POINT ( 'NONE',  ( -0.9412147342319837628, -0.1574803149606297803, 0.3075787400499532809 ) ) ;
#36790=CARTESIAN_POINT ( 'NONE',  ( 0.7185039370078739607, 1.928577636452523993E-17, 0.4133858266641267654 ) ) ;
#36791=CARTESIAN_POINT ( 'NONE',  ( -0.7185039370078746268, -0.06523048226347956391, 1.173720472440945573 ) ) ;
#36794=CARTESIAN_POINT ( 'NONE',  ( -0.8759842519685039353, -0.1574803149606299191, 1.377952755905512028 ) ) ;
#36798=CARTESIAN_POINT ( 'NONE',  ( -0.7185039370078739607, 1.928577636452523993E-17, 0.3838582677165354173 ) ) ;
#36801=CARTESIAN_POINT ( 'NONE',  ( 1.054774247047244096, 0.000000000000000000, 0.5388779527021417826 ) ) ;
#36805=CARTESIAN_POINT ( 'NONE',  ( -0.7495606340400177148, 0.1264236179284866091, 1.144192913332062966 ) ) ;
#36808=EDGE_CURVE ( 'NONE', #10105, #38112, #31047, .T. ) ;
#36809=CARTESIAN_POINT ( 'NONE',  ( -0.8019270111902717657, -0.1787899950787401604, 0.2116141731745827814 ) ) ;
#36810=LINE ( 'NONE', #824, #30314 ) ;
#36816=B_SPLINE_CURVE_WITH_KNOTS ( 'NONE', 3,
 ( #46102, #13301, #27965, #2523, #17378, #27744, #42309, #46375, #1821, #31558, #23878, #13556, #24581, #2753, #32016, #46608, #46137, #27265, #5897, #5413, #20268, #42056, #16692, #31320, #45895, #3228, #39643, #18565, #39410, #43482, #42998, #7069, #2987, #100, #7316, #10207, #32975, #43963, #11161, #21443, #32502, #28918, #25296, #24812, #14746, #6593, #29418, #14507, #3942, #36072, #3715, #36330, #25779, #21935, #29169, #40349, #17619, #36786, #21206, #10689, #7541, #22153, #33222, #3482, #10449, #47085, #32264, #46843, #25048, #10927, #43723, #14032, #18095, #32741, #47337, #25549, #40120, #36555, #44891, #34157, #26729, #5119, #19025, #37730, #15225, #29872, #30342, #44414 ),
 .UNSPECIFIED., .F., .F.,
 ( 4, 2, 2, 1, 1, 2, 2, 2, 2, 2, 2, 2, 2, 2, 2, 2, 1, 1, 1, 1, 1, 2, 2, 2, 2, 2, 1, 1, 1, 2, 2, 2, 2, 1, 1, 2, 2, 2, 2, 1, 1, 1, 2, 2, 2, 2, 1, 1, 1, 2, 2, 2, 4 ),
 ( 0.000000000000000000, 0.06249999999922203897, 0.09374999999883308621, 0.1093749999986385890, 0.1171874999985414306, 0.1210937499984927890, 0.1249999999984441335, 0.1874999999976660059, 0.2187499999972769282, 0.2499999999968878228, 0.3124999999961092234, 0.3437499999957202568, 0.3593749999955259122, 0.3749999999953315122, 0.4374999999945541895, 0.4687499999941655004, 0.4843749999939712669, 0.4921874999938741224, 0.4960937499938254946, 0.4980468749938006257, 0.4990234374937876360, 0.4995117187437816964, 0.4999999999937758122, 0.5624999999945692331, 0.5937499999949663598, 0.6093749999951645346, 0.6171874999952633445, 0.6210937499953124163, 0.6230468749953369523, 0.6240234374953490537, 0.6249999999953610441, 0.6874999999961505237, 0.7187499999965453190, 0.7343749999967427167, 0.7421874999968420816, 0.7460937499968910425, 0.7499999999969400033, 0.7812499999973340215, 0.7968749999975310860, 0.8046874999976295628, 0.8085937499976788567, 0.8105468749977035037, 0.8115234374977157161, 0.8124999999977280396, 0.8437499999980859755, 0.8593749999982649435, 0.8671874999983544274, 0.8710937499983996135, 0.8730468749984222621, 0.8740234374984335863, 0.8749999999984447996, 0.9374999999992223998, 1.000000000000000000 ),
 .UNSPECIFIED. ) ;
#36817=EDGE_CURVE ( 'NONE', #45011, #8121, #43355, .T. ) ;
#36818=CARTESIAN_POINT ( 'NONE',  ( -0.8019270111902717657, 0.1787899950787401604, 0.7431102361667091261 ) ) ;
#36821=VERTEX_POINT ( 'NONE', #21314 ) ;
#36825=CARTESIAN_POINT ( 'NONE',  ( -0.7495606340400177148, 0.1264236179284866091, 0.08120078734781142893 ) ) ;
#36826=CARTESIAN_POINT ( 'NONE',  ( -0.8759842519685039353, -0.1574803149606299191, 0.9055118110236221041 ) ) ;
#36827=CARTESIAN_POINT ( 'NONE',  ( 1.033464566929133799, 0.000000000000000000, 0.6397637795275591399 ) ) ;
#36830=CARTESIAN_POINT ( 'NONE',  ( -0.9412147342319837628, -0.1574803149606297803, 1.488681102254677535 ) ) ;
#36831=CIRCLE ( 'NONE', #15390, 0.1574803149606299191 ) ;
#36832=CARTESIAN_POINT ( 'NONE',  ( 0.8019270111902717657, 0.1787899950787401604, 0.8267716534895444003 ) ) ;
#36833=CARTESIAN_POINT ( 'NONE',  ( -1.054774247047244096, 0.000000000000000000, 1.993110236166708793 ) ) ;
#36834=CARTESIAN_POINT ( 'NONE',  ( 0.7185039370078746268, 0.06523048226347956391, 1.444389763779527991 ) ) ;
#36835=CARTESIAN_POINT ( 'NONE',  ( 0.7767998692430261309, -0.1394856968632323391, 1.986240030985245264 ) ) ;
#36837=CARTESIAN_POINT ( 'NONE',  ( 0.8759842519685039353, 0.1787899950787401882, 0.7800196849856062542 ) ) ;
#36840=CARTESIAN_POINT ( 'NONE',  ( 0.7495606340400177148, -0.1264236179284866091, 1.031003936954110189 ) ) ;
#36843=CARTESIAN_POINT ( 'NONE',  ( -0.9412147342319837628, -0.1574803149606297803, 0.5142716535433068392 ) ) ;
#36846=CARTESIAN_POINT ( 'NONE',  ( -0.8759842519685039353, 0.1787899950787401882, 0.07135826766277185429 ) ) ;
#36853=CARTESIAN_POINT ( 'NONE',  ( -1.054774247047244096, 0.000000000000000000, 1.754429133804503715 ) ) ;
#36854=CARTESIAN_POINT ( 'NONE',  ( -1.054774247047244096, 0.000000000000000000, 0.8489173227808819444 ) ) ;
#36856=CARTESIAN_POINT ( 'NONE',  ( -1.054774247047244096, 0.000000000000000000, 0.3420275590013546751 ) ) ;
#36857=CARTESIAN_POINT ( 'NONE',  ( -0.7185039370078732945, -0.06523048226347920309, 0.1500984251968504879 ) ) ;
#36863=CYLINDRICAL_SURFACE ( 'NONE', #1142, 0.1574803149606299191 ) ;
#36867=CARTESIAN_POINT ( 'NONE',  ( -0.8759842519685039353, 0.1787899950787401882, 0.2682086613635594752 ) ) ;
#36869=CARTESIAN_POINT ( 'NONE',  ( -1.054774247047244540, 0.07405724077823318263, 1.328740157426552049 ) ) ;
#36877=CARTESIAN_POINT ( 'NONE',  ( 0.9873396505805591694, -0.1113553986120547346, 0.3592519685039369803 ) ) ;
#36880=CARTESIAN_POINT ( 'NONE',  ( -0.7185039370078746268, -0.06523048226347956391, 1.006397637687749036 ) ) ;
#36886=CARTESIAN_POINT ( 'NONE',  ( 0.9873396505805591694, -0.1113553986120547346, 2.002952755797984263 ) ) ;
#36889=CARTESIAN_POINT ( 'NONE',  ( 1.033464566929134687, 0.06523048226347956391, 0.9178149606299221830 ) ) ;
#36890=CARTESIAN_POINT ( 'NONE',  ( 0.7185039370078714072, 0.06523048226347728795, 1.365649606299213614 ) ) ;
#36899=CARTESIAN_POINT ( 'NONE',  ( -0.7185039370078746268, -0.06523048226347956391, 0.6126968502861739330 ) ) ;
#36904=CARTESIAN_POINT ( 'NONE',  ( 0.8107537697050253289, 0.1574803149606300301, 1.035925196742866650 ) ) ;
#36905=ADVANCED_FACE ( 'NONE', ( #13953 ), #18488, .T. ) ;
#36906=CARTESIAN_POINT ( 'NONE',  ( 0.8107537697050254399, 0.1574803149606300301, 1.833169291338582640 ) ) ;
#36907=ORIENTED_EDGE ( 'NONE', *, *, #23701, .F. ) ;
#36908=ORIENTED_EDGE ( 'NONE', *, *, #31189, .T. ) ;
#36910=CARTESIAN_POINT ( 'NONE',  ( -0.8759842519685039353, -0.1787899950787401882, 1.631397637741511808 ) ) ;
#36912=CARTESIAN_POINT ( 'NONE',  ( 0.6971942568897648851, 0.07405724077823318263, 1.776574803095843924 ) ) ;
#36913=CARTESIAN_POINT ( 'NONE',  ( -0.7495606340400177148, 0.1264236179284866091, 0.7504921259304880854 ) ) ;
#36914=DIRECTION ( 'NONE',  ( 0.000000000000000000, 0.000000000000000000, -1.000000000000000000 ) ) ;
#36915=CARTESIAN_POINT ( 'NONE',  ( 0.9500414927467378812, 0.1787899950787401604, 0.3494094487651343006 ) ) ;
#36917=CARTESIAN_POINT ( 'NONE',  ( -0.7185039370078778465, -0.06523048226348396317, 1.675688976270425457 ) ) ;
#36918=CARTESIAN_POINT ( 'NONE',  ( -0.7495606340400177148, 0.1264236179284866091, 1.218011810969858111 ) ) ;
#36919=VECTOR ( 'NONE', #39805, 39.37007874015748143 ) ;
#36921=AXIS2_PLACEMENT_3D ( 'NONE', #2530, #21212, #28685 ) ;
#36922=CARTESIAN_POINT ( 'NONE',  ( -0.6971942568897648851, -0.07405724077823297447, 1.584645669237574994 ) ) ;
#36923=CARTESIAN_POINT ( 'NONE',  ( -0.7646288533564489232, -0.1113553986120547346, 1.953740157372787500 ) ) ;
#36925=CARTESIAN_POINT ( 'NONE',  ( -0.7185039370078746268, 0.06523048226347956391, 1.562500000000000000 ) ) ;
#36927=CARTESIAN_POINT ( 'NONE',  ( 1.054774247047244540, 0.07405724077823318263, 1.407480314906865981 ) ) ;
#36929=CARTESIAN_POINT ( 'NONE',  ( 1.033464566929133799, 0.000000000000000000, 1.062992125876724314 ) ) ;
#36933=ORIENTED_EDGE ( 'NONE', *, *, #18399, .F. ) ;
#36940=CARTESIAN_POINT ( 'NONE',  ( 0.9873396505805591694, -0.1113553986120547346, 0.1525590550105832555 ) ) ;
#36941=CARTESIAN_POINT ( 'NONE',  ( 1.002407869896990045, 0.1264236179284866091, 0.6963582676627716461 ) ) ;
#36945=LINE ( 'NONE', #42106, #39236 ) ;
#36946=CARTESIAN_POINT ( 'NONE',  ( 0.6971942568897648851, -0.07405724077823297447, 1.820866141678520789 ) ) ;
#36947=DIRECTION ( 'NONE',  ( 1.000000000000000000, 0.000000000000000000, -1.822029033848725275E-16 ) ) ;
#36954=CARTESIAN_POINT ( 'NONE',  ( 0.8759842519685039353, -0.1787899950787401882, 0.2140748030958428971 ) ) ;
#36955=ADVANCED_FACE ( 'NONE', ( #11315 ), #25928, .T. ) ;
#36957=CARTESIAN_POINT ( 'NONE',  ( 0.9500414927467377701, 0.1787899950787401604, 0.5807086613635594752 ) ) ;
#36958=CARTESIAN_POINT ( 'NONE',  ( -0.6971942568897648851, -0.07405724077823297447, 1.579724409395055318 ) ) ;
#36961=CARTESIAN_POINT ( 'NONE',  ( -0.8759842519685039353, 0.1574803149606299191, 0.8858267716535432879 ) ) ;
#36962=CARTESIAN_POINT ( 'NONE',  ( 1.054774247047244540, 0.07405724077823318263, 1.249999999946235896 ) ) ;
#36963=CARTESIAN_POINT ( 'NONE',  ( 0.6971942568897637749, 2.189545951927499583E-17, 1.970964566875370139 ) ) ;
#36964=CARTESIAN_POINT ( 'NONE',  ( -0.8019270111902717657, 0.1787899950787401604, 1.097440944828127041 ) ) ;
#36965=EDGE_CURVE ( 'NONE', #41784, #22273, #39502, .T. ) ;
#36967=CARTESIAN_POINT ( 'NONE',  ( 0.8019270111902716547, -0.1787899950787401604, 0.4084645668753704162 ) ) ;
#36968=CARTESIAN_POINT ( 'NONE',  ( -0.8759842519685039353, 0.1787899950787401882, 0.2682086613635594752 ) ) ;
#36969=CARTESIAN_POINT ( 'NONE',  ( -0.8759842519685039353, -0.1787899950787401882, 0.7209645668753701386 ) ) ;
#36970=CARTESIAN_POINT ( 'NONE',  ( 0.9873396505805591694, -0.1113553986120547346, 1.727362204616881947 ) ) ;
#36972=CARTESIAN_POINT ( 'NONE',  ( -0.9873396505805591694, 0.1113553986120547346, 0.8710629920184568276 ) ) ;
#36973=CARTESIAN_POINT ( 'NONE',  ( 1.054774247047244540, -0.07405724077823318263, 1.048228346402928723 ) ) ;
#36974=CARTESIAN_POINT ( 'NONE',  ( -1.002407869896990045, -0.1264236179284866091, 1.828248031442299082 ) ) ;
#36976=CARTESIAN_POINT ( 'NONE',  ( 0.6971942568897648851, -0.07405724077823297447, 1.894685039316315489 ) ) ;
#36977=AXIS2_PLACEMENT_3D ( 'NONE', #2217, #12325, #5824 ) ;
#36980=ORIENTED_EDGE ( 'NONE', *, *, #30144, .F. ) ;
#36987=EDGE_CURVE ( 'NONE', #22073, #758, #35909, .T. ) ;
#36988=CYLINDRICAL_SURFACE ( 'NONE', #13932, 0.1574803149606299191 ) ;
#36990=CARTESIAN_POINT ( 'NONE',  ( 1.054774247047244096, 0.000000000000000000, 0.2189960629383626012 ) ) ;
#36994=CARTESIAN_POINT ( 'NONE',  ( 0.9873396505805591694, -0.1113553986120547346, 1.343503937007874072 ) ) ;
#36996=CARTESIAN_POINT ( 'NONE',  ( -0.7495606340400177148, 0.1264236179284866091, 0.5142716534895434011 ) ) ;
#36999=CARTESIAN_POINT ( 'NONE',  ( 1.054774247047244540, -0.07405724077823318263, 1.363188976324188895 ) ) ;
#37000=CARTESIAN_POINT ( 'NONE',  ( 1.002407869896990045, 0.1264236179284866091, 1.680610236166708793 ) ) ;
#37001=CARTESIAN_POINT ( 'NONE',  ( 1.033464566929134687, 0.06523048226347956391, 0.1304133858267717272 ) ) ;
#37005=CARTESIAN_POINT ( 'NONE',  ( -1.033464566929134687, -0.06523048226347956391, 1.936515748031494510 ) ) ;
#37006=CARTESIAN_POINT ( 'NONE',  ( 0.7646288533564489232, -0.1113553986120547346, 0.5364173227271189504 ) ) ;
#37007=CARTESIAN_POINT ( 'NONE',  ( 0.9500414927467378812, 0.1787899950787401604, 0.3444881889226146243 ) ) ;
#37008=CARTESIAN_POINT ( 'NONE',  ( 0.7331235663779919198, -0.08921757803951906041, 0.03937007923342519117 ) ) ;
#37010=CARTESIAN_POINT ( 'NONE',  ( 0.8019270111902716547, -0.1787899950787401604, 1.230314960576158967 ) ) ;
#37012=CARTESIAN_POINT ( 'NONE',  ( -0.7185039370078778465, -0.06523048226348396317, 1.911909448711369697 ) ) ;
#37014=CARTESIAN_POINT ( 'NONE',  ( -0.6971942568897648851, -0.07405724077823297447, 1.225393700733637514 ) ) ;
#37015=CARTESIAN_POINT ( 'NONE',  ( 0.8107537697050253289, -0.1574803149606297803, 0.6176181101286932762 ) ) ;
#37016=VERTEX_POINT ( 'NONE', #4315 ) ;
#37019=ORIENTED_EDGE ( 'NONE', *, *, #17859, .T. ) ;
#37022=CARTESIAN_POINT ( 'NONE',  ( -0.7646288533564489232, 0.1113553986120547346, 0.4872047243019220208 ) ) ;
#37023=CARTESIAN_POINT ( 'NONE',  ( -1.033464566929133799, 0.000000000000000000, 1.584645669291338654 ) ) ;
#37024=CARTESIAN_POINT ( 'NONE',  ( 0.6971942568897648851, -0.07405724077823297447, 1.540354330654897685 ) ) ;
#37025=EDGE_CURVE ( 'NONE', #7448, #12067, #15385, .T. ) ;
#37026=CARTESIAN_POINT ( 'NONE',  ( -0.7185039370078739607, 1.928577636452523993E-17, 1.840551181102362266 ) ) ;
#37027=CARTESIAN_POINT ( 'NONE',  ( 0.7646288533564489232, 0.1113553986120547346, 1.678149606299212726 ) ) ;
#37029=ORIENTED_EDGE ( 'NONE', *, *, #44927, .T. ) ;
#37030=CARTESIAN_POINT ( 'NONE',  ( -1.033464566929133799, 0.000000000000000000, 0.3937007872940476716 ) ) ;
#37032=ORIENTED_EDGE ( 'NONE', *, *, #1900, .T. ) ;
#37033=CARTESIAN_POINT ( 'NONE',  ( 1.002407869896990045, -0.1264236179284866091, 0.8095472440407244230 ) ) ;
#37034=CARTESIAN_POINT ( 'NONE',  ( -0.8019270111902716547, 0.1787899950787401604, 1.491141732229701145 ) ) ;
#37036=CARTESIAN_POINT ( 'NONE',  ( -0.8759842519685039353, 0.1787899950787401882, 1.336122047190330786 ) ) ;
#37038=( BOUNDED_CURVE ( )  B_SPLINE_CURVE ( 2, ( #25834, #8073, #37544, #165, #15771, #36843, #11451, #29702, #4225 ),
 .UNSPECIFIED., .F., .F. ) 
 B_SPLINE_CURVE_WITH_KNOTS ( ( 3, 2, 2, 2, 3 ),
 ( 0.2500000000000000000, 0.2525000000000000022, 0.2550000000000000044, 0.2575000000000000067, 0.2600000000000000089 ),
 .UNSPECIFIED. ) 
 CURVE ( )  GEOMETRIC_REPRESENTATION_ITEM ( )  RATIONAL_B_SPLINE_CURVE ( ( 1.000000000000000000, 0.9238795325112869605, 1.000000000000000000, 0.9238795325112869605, 1.000000000000000000, 0.9238795325112869605, 1.000000000000000000, 0.9238795325112869605, 1.000000000000000000 ) ) 
 REPRESENTATION_ITEM ( '' )  ) ;
#37039=CARTESIAN_POINT ( 'NONE',  ( -0.6971942568897626646, 0.07405724077823318263, 0.3592519684501735977 ) ) ;
#37043=CARTESIAN_POINT ( 'NONE',  ( -0.7185039370078739607, 1.928577636452523993E-17, 0.8464566928058583350 ) ) ;
#37048=( BOUNDED_CURVE ( )  B_SPLINE_CURVE ( 2, ( #12763, #44089, #47222, #33108, #10338, #39768, #36678, #3373, #14878 ),
 .UNSPECIFIED., .F., .F. ) 
 B_SPLINE_CURVE_WITH_KNOTS ( ( 3, 2, 2, 2, 3 ),
 ( 0.1199999999999999956, 0.1224999999999999978, 0.1250000000000000000, 0.1275000000000000022, 0.1300000000000000044 ),
 .UNSPECIFIED. ) 
 CURVE ( )  GEOMETRIC_REPRESENTATION_ITEM ( )  RATIONAL_B_SPLINE_CURVE ( ( 1.000000000000000000, 0.9238795325112869605, 1.000000000000000000, 0.9238795325112869605, 1.000000000000000000, 0.9238795325112869605, 1.000000000000000000, 0.9238795325112869605, 1.000000000000000000 ) ) 
 REPRESENTATION_ITEM ( '' )  ) ;
#37049=CARTESIAN_POINT ( 'NONE',  ( -0.8759842519685039353, -0.1787899950787401882, 0.05659448813521291560 ) ) ;
#37050=CARTESIAN_POINT ( 'NONE',  ( -0.9873396505805591694, 0.1113553986120547346, 0.9596456692913386544 ) ) ;
#37052=CARTESIAN_POINT ( 'NONE',  ( -0.9873396505805591694, 0.1113553986120547346, 0.3986220471365669038 ) ) ;
#37053=CARTESIAN_POINT ( 'NONE',  ( -1.033464566929133799, 0.000000000000000000, 1.535433070758614127 ) ) ;
#37054=AXIS2_PLACEMENT_3D ( 'NONE', #18885, #14839, #32602 ) ;
#37056=CARTESIAN_POINT ( 'NONE',  ( 0.6971942568897626646, -0.07405724077823297447, 0.9153543306548987957 ) ) ;
#37057=CARTESIAN_POINT ( 'NONE',  ( -0.7185039370078739607, 1.928577636452523993E-17, 1.673228346349165285 ) ) ;
#37058=CARTESIAN_POINT ( 'NONE',  ( 0.8759842519685039353, 0.1574803149606299191, 1.437007874015747921 ) ) ;
#37059=CARTESIAN_POINT ( 'NONE',  ( 0.7099245333373607192, -0.01040492030921760271, 1.983451210857912761 ) ) ;
#37060=CARTESIAN_POINT ( 'NONE',  ( 1.033464566929133799, 0.000000000000000000, 0.9547244094488189781 ) ) ;
#37061=CARTESIAN_POINT ( 'NONE',  ( 0.7185039370078746268, 0.06523048226347956391, 0.3321850392625518844 ) ) ;
#37062=EDGE_CURVE ( 'NONE', #20228, #44561, #34393, .T. ) ;
#37063=CARTESIAN_POINT ( 'NONE',  ( 0.6971942568897637749, 2.189545951927499583E-17, 0.7898622046706456068 ) ) ;
#37066=ORIENTED_EDGE ( 'NONE', *, *, #44107, .T. ) ;
#37068=CARTESIAN_POINT ( 'NONE',  ( 0.7495606340400177148, -0.1264236179284866091, 1.188484251914740275 ) ) ;
#37070=LINE ( 'NONE', #4946, #10413 ) ;
#37075=CARTESIAN_POINT ( 'NONE',  ( -0.9500414927467378812, -0.1787899950787401604, 0.2509842519147403861 ) ) ;
#37077=CARTESIAN_POINT ( 'NONE',  ( 1.054774247047244096, 0.000000000000000000, 1.993110236166708793 ) ) ;
#37081=CARTESIAN_POINT ( 'NONE',  ( 0.9412147342319837628, -0.1574803149606297803, 0.3469488187901108023 ) ) ;
#37082=CARTESIAN_POINT ( 'NONE',  ( -0.9500414927467378812, -0.1787899950787401604, 1.628937007820252303 ) ) ;
#37083=CARTESIAN_POINT ( 'NONE',  ( -1.054774247047244540, -0.07405724077823318263, 0.4576771653005669016 ) ) ;
#37087=CARTESIAN_POINT ( 'NONE',  ( 0.8019270111902717657, -0.1787899950787401604, 0.08858267711159097113 ) ) ;
#37093=CARTESIAN_POINT ( 'NONE',  ( -0.8759842519685039353, 0.1787899950787401882, 0.3863188975840318173 ) ) ;
#37095=CARTESIAN_POINT ( 'NONE',  ( -1.054774247047244096, 0.000000000000000000, 1.444389763725763665 ) ) ;
#37096=ORIENTED_EDGE ( 'NONE', *, *, #9522, .F. ) ;
#37104=FACE_OUTER_BOUND ( 'NONE', #26215, .T. ) ;
#37105=CARTESIAN_POINT ( 'NONE',  ( -0.9412147342319837628, 0.1574803149606300301, 1.031003936900347639 ) ) ;
#37107=CARTESIAN_POINT ( 'NONE',  ( 1.002407869896990045, -0.1264236179284866091, 0.5339566928596221063 ) ) ;
#37112=CARTESIAN_POINT ( 'NONE',  ( 1.033464566929134687, 0.06523048226347956391, 1.970964566821606034 ) ) ;
#37113=VERTEX_POINT ( 'NONE', #28296 ) ;
#37115=CARTESIAN_POINT ( 'NONE',  ( -0.8019270111902716547, -0.1787899950787401604, 0.9990157479777320715 ) ) ;
#37116=CARTESIAN_POINT ( 'NONE',  ( 0.9412147342319837628, -0.1574803149606297803, 0.9079724409448818312 ) ) ;
#37122=VERTEX_POINT ( 'NONE', #31191 ) ;
#37123=CARTESIAN_POINT ( 'NONE',  ( -1.033464566929133799, 0.000000000000000000, 1.309055118110236338 ) ) ;
#37124=CARTESIAN_POINT ( 'NONE',  ( 0.7185039370078739607, 1.928577636452523993E-17, 1.368110236220472675 ) ) ;
#37127=CARTESIAN_POINT ( 'NONE',  ( 0.8107537697050253289, -0.1574803149606297803, 1.129429133750740277 ) ) ;
#37129=EDGE_CURVE ( 'NONE', #4590, #47236, #40778, .T. ) ;
#37130=EDGE_LOOP ( 'NONE', ( #16365, #39423, #43735, #8876 ) ) ;
#37131=EDGE_LOOP ( 'NONE', ( #44415, #15192, #10320, #35844 ) ) ;
#37132=CARTESIAN_POINT ( 'NONE',  ( -1.002407869896990045, -0.1264236179284866091, 1.754429133804503715 ) ) ;
#37133=CARTESIAN_POINT ( 'NONE',  ( 0.7495606340400177148, -0.1264236179284866091, 1.665846456639149764 ) ) ;
#37135=CARTESIAN_POINT ( 'NONE',  ( -1.054774247047244096, 0.000000000000000000, 0.7357283464029290565 ) ) ;
#37136=CARTESIAN_POINT ( 'NONE',  ( 0.7185039370078739607, 0.000000000000000000, 4.498031496062992574 ) ) ;
#37137=CARTESIAN_POINT ( 'NONE',  ( 0.7495606340400177148, -0.1264236179284866091, 0.3272637794737956463 ) ) ;
#37138=DIRECTION ( 'NONE',  ( -1.000000000000000000, 0.000000000000000000, 0.000000000000000000 ) ) ;
#37139=CARTESIAN_POINT ( 'NONE',  ( -1.054774247047244540, 0.07405724077823318263, 1.245078740103716886 ) ) ;
#37140=CARTESIAN_POINT ( 'NONE',  ( -0.8759842519685039353, -0.1787899950787401882, 0.7997047243556849594 ) ) ;
#37141=CARTESIAN_POINT ( 'NONE',  ( -0.8759842519685039353, 0.1787899950787401882, 0.9374999999462362288 ) ) ;
#37144=CARTESIAN_POINT ( 'NONE',  ( -0.6971942568897648851, 0.07405724077823318263, 1.658464566875369472 ) ) ;
#37145=CARTESIAN_POINT ( 'NONE',  ( -1.033464566929134687, 0.06523048226347956391, 1.931594488081448180 ) ) ;
#37148=CARTESIAN_POINT ( 'NONE',  ( -1.033464566929134687, 0.06523048226347956391, 1.626476377952756458 ) ) ;
#37150=CARTESIAN_POINT ( 'NONE',  ( 0.9500414927467377701, 0.1787899950787401604, 1.569881889710015299 ) ) ;
#37155=ORIENTED_EDGE ( 'NONE', *, *, #27399, .F. ) ;
#37160=( BOUNDED_CURVE ( )  B_SPLINE_CURVE ( 2, ( #47307, #40555, #29623, #25971, #40092, #36757, #7287, #3914, #43454 ),
 .UNSPECIFIED., .F., .T. ) 
 B_SPLINE_CURVE_WITH_KNOTS ( ( 3, 2, 2, 2, 3 ),
 ( 0.6800000000000000488, 0.6824999999999999956, 0.6850000000000000533, 0.6875000000000000000, 0.6899999999999999467 ),
 .UNSPECIFIED. ) 
 CURVE ( )  GEOMETRIC_REPRESENTATION_ITEM ( )  RATIONAL_B_SPLINE_CURVE ( ( 1.000000000000000000, 0.9238795325112869605, 1.000000000000000000, 0.9238795325112869605, 1.000000000000000000, 0.9238795325112869605, 1.000000000000000000, 0.9238795325112799661, 1.000000000000000000 ) ) 
 REPRESENTATION_ITEM ( '' )  ) ;
#37163=CARTESIAN_POINT ( 'NONE',  ( 1.002407869896990045, -0.1264236179284866091, 1.788877952702141672 ) ) ;
#37170=CARTESIAN_POINT ( 'NONE',  ( 0.7495606340400177148, 0.1264236179284866091, 0.7062007873478109987 ) ) ;
#37172=CARTESIAN_POINT ( 'NONE',  ( 0.9873396505805591694, -0.1113553986120547346, 1.136811023514519681 ) ) ;
#37174=DIRECTION ( 'NONE',  ( 1.822029033848725028E-16, 0.000000000000000000, 1.000000000000000000 ) ) ;
#37175=CARTESIAN_POINT ( 'NONE',  ( -0.7185039370078739607, 1.928577636452523993E-17, 0.05905511800270921846 ) ) ;
#37176=CARTESIAN_POINT ( 'NONE',  ( 0.8019270111902717657, -0.1787899950787401604, 1.865157480261195877 ) ) ;
#37177=CARTESIAN_POINT ( 'NONE',  ( 1.033464566929133799, 0.000000000000000000, 0.1181102361129454797 ) ) ;
#37179=CARTESIAN_POINT ( 'NONE',  ( 0.9412147342319837628, 0.1574803149606300301, 0.1353346456692913757 ) ) ;
#37184=CARTESIAN_POINT ( 'NONE',  ( 0.8759842519685039353, 0.1787899950787401882, 0.1943897637257641919 ) ) ;
#37186=CARTESIAN_POINT ( 'NONE',  ( -0.8019270111902717657, 0.1787899950787401604, 1.766732283410803461 ) ) ;
#37188=CARTESIAN_POINT ( 'NONE',  ( -0.8019270111902717657, 0.1787899950787401604, 1.338582677111590069 ) ) ;
#37189=DIRECTION ( 'NONE',  ( 1.822029033848725028E-16, 0.000000000000000000, 1.000000000000000000 ) ) ;
#37190=CARTESIAN_POINT ( 'NONE',  ( 0.9500414927467378812, -0.1787899950787401604, 1.279527559001355286 ) ) ;
#37192=CARTESIAN_POINT ( 'NONE',  ( -0.7495606340400177148, 0.1264236179284866091, 1.021161417269070837 ) ) ;
#37194=DIRECTION ( 'NONE',  ( 1.822029033848725028E-16, 0.000000000000000000, 1.000000000000000000 ) ) ;
#37195=CARTESIAN_POINT ( 'NONE',  ( 0.6971942568897648851, -0.07405724077823297447, 0.4035433070328507954 ) ) ;
#37196=CARTESIAN_POINT ( 'NONE',  ( -1.054774247047244540, -0.07405724077823318263, 0.4133858267178901480 ) ) ;
#37197=CARTESIAN_POINT ( 'NONE',  ( 0.8107537697050253289, 0.1574803149606300301, 1.665846456585386548 ) ) ;
#37198=VERTEX_POINT ( 'NONE', #10317 ) ;
#37199=VERTEX_POINT ( 'NONE', #25647 ) ;
#37201=CARTESIAN_POINT ( 'NONE',  ( 1.002407869896990045, -0.1264236179284866091, 0.8882874015210394658 ) ) ;
#37202=CARTESIAN_POINT ( 'NONE',  ( -1.033464566929134687, -0.06523048226347956391, 0.1648622047244094890 ) ) ;
#37203=CARTESIAN_POINT ( 'NONE',  ( 1.002407869896990045, -0.1264236179284866091, 1.006397637741511808 ) ) ;
#37204=CARTESIAN_POINT ( 'NONE',  ( -0.7495606340400177148, -0.1264236179284866091, 1.936515747977732405 ) ) ;
#37206=AXIS2_PLACEMENT_3D ( 'NONE', #29344, #4558, #30033 ) ;
#37207=CARTESIAN_POINT ( 'NONE',  ( 0.8019270111902717657, 0.1787899950787401604, 1.884842519631275026 ) ) ;
#37208=CARTESIAN_POINT ( 'NONE',  ( -0.8107537697050234415, -0.1574803149606297803, 0.3125000000000000000 ) ) ;
#37209=CARTESIAN_POINT ( 'NONE',  ( 0.7185039370078746268, -0.06523048226347956391, 0.3075787401574803792 ) ) ;
#37214=CARTESIAN_POINT ( 'NONE',  ( 0.8019270111902717657, -0.1787899950787401604, 1.190944881836001112 ) ) ;
#37216=CARTESIAN_POINT ( 'NONE',  ( 0.8759842519685039353, -0.1574803149606299191, 0.7381889762704251234 ) ) ;
#37219=CARTESIAN_POINT ( 'NONE',  ( 1.054774247047244096, 0.000000000000000000, 1.518208661363559031 ) ) ;
#37220=CARTESIAN_POINT ( 'NONE',  ( 0.8759842519685039353, 0.1787899950787401882, 0.1500984251430870220 ) ) ;
#37225=CARTESIAN_POINT ( 'NONE',  ( 0.8759842519685039353, -0.1574803149606299191, 1.338582677165354395 ) ) ;
#37227=CARTESIAN_POINT ( 'NONE',  ( -0.8019270111902716547, -0.1787899950787401604, 0.6840551180564720113 ) ) ;
#37231=CARTESIAN_POINT ( 'NONE',  ( 1.033464566929133799, 1.928577636452524610E-17, 4.498031496062992574 ) ) ;
#37233=CARTESIAN_POINT ( 'NONE',  ( 0.7495606340400177148, -0.1264236179284866091, 1.311515747977732405 ) ) ;
#37234=CARTESIAN_POINT ( 'NONE',  ( 1.054774247047244096, 0.000000000000000000, 1.754429133804503715 ) ) ;
#37236=CARTESIAN_POINT ( 'NONE',  ( 1.033464566929133799, 0.000000000000000000, 0.1181102361129454797 ) ) ;
#37237=DIRECTION ( 'NONE',  ( 1.000000000000000000, 0.000000000000000000, -1.822029033848725275E-16 ) ) ;
#37239=CARTESIAN_POINT ( 'NONE',  ( 0.7495606340400177148, -0.1264236179284866091, 1.227854330654897685 ) ) ;
#37241=CARTESIAN_POINT ( 'NONE',  ( 0.9412147342319837628, -0.1574803149606297803, 0.7012795274515276622 ) ) ;
#37251=CARTESIAN_POINT ( 'NONE',  ( -0.7185039370078746268, -0.06523048226347956391, 1.252460629921259061 ) ) ;
#37254=CARTESIAN_POINT ( 'NONE',  ( 0.7185039370078739607, 1.928577636452523993E-17, 1.919291338582677309 ) ) ;
#37255=DIRECTION ( 'NONE',  ( 0.000000000000000000, 0.000000000000000000, -1.000000000000000000 ) ) ;
#37258=LINE ( 'NONE', #40361, #12998 ) ;
#37260=CARTESIAN_POINT ( 'NONE',  ( 0.7495606340400177148, -0.1264236179284866091, 0.8390748030958424808 ) ) ;
#37262=CARTESIAN_POINT ( 'NONE',  ( -0.7495606340400177148, 0.1264236179284866091, 1.222933070812378009 ) ) ;
#37263=VECTOR ( 'NONE', #27171, 39.37007874015748143 ) ;
#37265=CARTESIAN_POINT ( 'NONE',  ( 0.8759842519685039353, 0.000000000000000000, 4.498031496062992574 ) ) ;
#37270=CARTESIAN_POINT ( 'NONE',  ( 1.033464566929134687, -0.06523048226347956391, 1.218011810916094895 ) ) ;
#37273=ADVANCED_FACE ( 'NONE', ( #39748 ), #36195, .T. ) ;
#37274=CARTESIAN_POINT ( 'NONE',  ( -0.8019270111902716547, -0.1787899950787401604, 0.1328740156942679884 ) ) ;
#37275=CARTESIAN_POINT ( 'NONE',  ( -0.7185039370078739607, 1.928577636452523993E-17, 0.8956692913385826404 ) ) ;
#37279=CARTESIAN_POINT ( 'NONE',  ( -0.9873396505805591694, 0.1113553986120547346, 1.500984251860976171 ) ) ;
#37280=CARTESIAN_POINT ( 'NONE',  ( 0.7495606340400177148, 0.1264236179284866091, 0.9079724408911180600 ) ) ;
#37281=CARTESIAN_POINT ( 'NONE',  ( 0.8759842519685039353, 0.1787899950787401882, 0.1107283464029295283 ) ) ;
#37282=CARTESIAN_POINT ( 'NONE',  ( -1.033464566929133799, 0.000000000000000000, 0.08858267716535432601 ) ) ;
#37283=CARTESIAN_POINT ( 'NONE',  ( 0.9873396505805591694, 0.1113553986120547346, 1.392716535433070835 ) ) ;
#37284=CARTESIAN_POINT ( 'NONE',  ( 0.7176825515505187436, 0.04481503542554400588, 1.982412129522283406 ) ) ;
#37286=CARTESIAN_POINT ( 'NONE',  ( 0.8759842519685039353, 0.1574803149606299191, 0.3248031494987720369 ) ) ;
#37289=CARTESIAN_POINT ( 'NONE',  ( 1.054774247047244096, 0.000000000000000000, 0.8489173227808819444 ) ) ;
#37291=CARTESIAN_POINT ( 'NONE',  ( 0.7495606340400177148, 0.1264236179284866091, 1.774114173174582643 ) ) ;
#37293=EDGE_LOOP ( 'NONE', ( #33708, #27549, #16807, #34274 ) ) ;
#37294=CARTESIAN_POINT ( 'NONE',  ( -0.7185039370078739607, 1.928577636452523993E-17, 0.8562992125984251190 ) ) ;
#37296=CARTESIAN_POINT ( 'NONE',  ( 0.8759842519685039353, -0.1787899950787401882, 1.154035433017102319 ) ) ;
#37299=ADVANCED_FACE ( 'NONE', ( #36432 ), #14856, .T. ) ;
#37301=( BOUNDED_CURVE ( )  B_SPLINE_CURVE ( 2, ( #9614, #24234, #12977, #5994, #10080, #6465, #27615, #20615, #42865 ),
 .UNSPECIFIED., .F., .T. ) 
 B_SPLINE_CURVE_WITH_KNOTS ( ( 3, 2, 2, 2, 3 ),
 ( 0.3400000000000000244, 0.3425000000000000266, 0.3449999999999999734, 0.3474999999999999756, 0.3499999999999999778 ),
 .UNSPECIFIED. ) 
 CURVE ( )  GEOMETRIC_REPRESENTATION_ITEM ( )  RATIONAL_B_SPLINE_CURVE ( ( 1.000000000000000000, 0.9238795325112869605, 1.000000000000000000, 0.9238795325112869605, 1.000000000000000000, 0.9238795325112869605, 1.000000000000000000, 0.9238795325112849621, 1.000000000000000000 ) ) 
 REPRESENTATION_ITEM ( '' )  ) ;
#37302=DIRECTION ( 'NONE',  ( 0.000000000000000000, 0.000000000000000000, -1.000000000000000000 ) ) ;
#37303=CARTESIAN_POINT ( 'NONE',  ( -1.002407869896990045, 0.1264236179284866091, 0.1845472440407248116 ) ) ;
#37308=CARTESIAN_POINT ( 'NONE',  ( -0.7495606340400177148, 0.1264236179284866091, 1.887303149552535420 ) ) ;
#37309=CARTESIAN_POINT ( 'NONE',  ( -0.8019270111902716547, 0.1787899950787401604, 0.9399606298674970661 ) ) ;
#37310=CARTESIAN_POINT ( 'NONE',  ( -1.054774247047244096, 0.000000000000000000, 0.4601377952218267953 ) ) ;
#37311=LINE ( 'NONE', #15291, #3079 ) ;
#37315=CARTESIAN_POINT ( 'NONE',  ( 1.054774247047244540, -0.07405724077823318263, 0.05905511805647267048 ) ) ;
#37322=( BOUNDED_CURVE ( )  B_SPLINE_CURVE ( 2, ( #23704, #37852, #27568, #23480, #41878, #5006, #16289, #5484, #30919 ),
 .UNSPECIFIED., .F., .T. ) 
 B_SPLINE_CURVE_WITH_KNOTS ( ( 3, 2, 2, 2, 3 ),
 ( 0.4500000000000000111, 0.4525000000000000133, 0.4550000000000000155, 0.4575000000000000178, 0.4600000000000000200 ),
 .UNSPECIFIED. ) 
 CURVE ( )  GEOMETRIC_REPRESENTATION_ITEM ( )  RATIONAL_B_SPLINE_CURVE ( ( 1.000000000000000000, 0.9238795325112869605, 1.000000000000000000, 0.9238795325112869605, 1.000000000000000000, 0.9238795325112869605, 1.000000000000000000, 0.9238795325112869605, 1.000000000000000000 ) ) 
 REPRESENTATION_ITEM ( '' )  ) ;
#37323=CARTESIAN_POINT ( 'NONE',  ( -0.7495606340400177148, 0.1264236179284866091, 0.3124999999462365619 ) ) ;
#37324=FACE_OUTER_BOUND ( 'NONE', #707, .T. ) ;
#37326=ORIENTED_EDGE ( 'NONE', *, *, #7682, .T. ) ;
#37329=CARTESIAN_POINT ( 'NONE',  ( -1.054774247047244540, 0.07405724077823318263, 1.564960629867495845 ) ) ;
#37334=DIRECTION ( 'NONE',  ( 1.822029033848725028E-16, 0.000000000000000000, 1.000000000000000000 ) ) ;
#37336=CARTESIAN_POINT ( 'NONE',  ( -1.033464566929133799, 0.000000000000000000, 1.141732283357039357 ) ) ;
#37337=CARTESIAN_POINT ( 'NONE',  ( 0.8019270111902717657, -0.1787899950787401604, 0.5659448818360001132 ) ) ;
#37339=CARTESIAN_POINT ( 'NONE',  ( 0.8107537697050253289, 0.1574803149606300301, 1.980807086506644943 ) ) ;
#37340=ORIENTED_EDGE ( 'NONE', *, *, #45159, .T. ) ;
#37342=CARTESIAN_POINT ( 'NONE',  ( -0.8019270111902716547, -0.1787899950787401604, 1.038385826717890259 ) ) ;
#37343=CARTESIAN_POINT ( 'NONE',  ( 0.8759842519685039353, 0.1574803149606299191, 0.9251968503937008093 ) ) ;
#37346=CARTESIAN_POINT ( 'NONE',  ( 0.7646288533564489232, -0.1113553986120547346, 0.7431102362204724532 ) ) ;
#37348=ORIENTED_EDGE ( 'NONE', *, *, #3411, .T. ) ;
#37350=EDGE_LOOP ( 'NONE', ( #13353, #16369, #17940, #2336 ) ) ;
#37358=CARTESIAN_POINT ( 'NONE',  ( 0.8759842519685039353, -0.1574803149606299191, 1.092519684931842594 ) ) ;
#37361=ORIENTED_EDGE ( 'NONE', *, *, #33374, .T. ) ;
#37362=CARTESIAN_POINT ( 'NONE',  ( -0.9500414927467378812, -0.1787899950787401604, 1.751968503883245765 ) ) ;
#37363=CARTESIAN_POINT ( 'NONE',  ( 0.8019270111902717657, -0.1787899950787401604, 1.668307086560410157 ) ) ;
#37365=LINE ( 'NONE', #33819, #12651 ) ;
#37366=CARTESIAN_POINT ( 'NONE',  ( -1.054774247047244096, 0.000000000000000000, 1.360728346402929168 ) ) ;
#37367=CARTESIAN_POINT ( 'NONE',  ( 0.8759842519685039353, 0.000000000000000000, 4.498031496062992574 ) ) ;
#37368=CARTESIAN_POINT ( 'NONE',  ( -1.054774247047244540, 0.07405724077823318263, 1.166338582623402731 ) ) ;
#37369=CARTESIAN_POINT ( 'NONE',  ( -0.7495606340400177148, -0.1264236179284866091, 0.9522637794737952577 ) ) ;
#37370=CARTESIAN_POINT ( 'NONE',  ( -0.8019270111902717657, 0.1787899950787401604, 0.03937007868639399305 ) ) ;
#37372=EDGE_CURVE ( 'NONE', #28460, #1520, #358, .T. ) ;
#37373=CARTESIAN_POINT ( 'NONE',  ( -0.9500414927467378812, -0.1787899950787401604, 1.633858267662771313 ) ) ;
#37374=VERTEX_POINT ( 'NONE', #46710 ) ;
#37376=CARTESIAN_POINT ( 'NONE',  ( -0.7185039370078739607, 1.928577636452523993E-17, 1.564960629921259949 ) ) ;
#37379=CARTESIAN_POINT ( 'NONE',  ( 1.002407869896990045, 0.1264236179284866091, 1.646161417269070837 ) ) ;
#37381=CARTESIAN_POINT ( 'NONE',  ( 1.033464566929133799, 0.000000000000000000, 1.938976377952756014 ) ) ;
#37382=ORIENTED_EDGE ( 'NONE', *, *, #9440, .T. ) ;
#37383=EDGE_CURVE ( 'NONE', #24091, #7448, #7181, .T. ) ;
#37392=DIRECTION ( 'NONE',  ( 0.000000000000000000, 0.000000000000000000, 1.000000000000000000 ) ) ;
#37394=CARTESIAN_POINT ( 'NONE',  ( 0.7495606340400177148, -0.1264236179284866091, 1.818405511757259729 ) ) ;
#37397=CARTESIAN_POINT ( 'NONE',  ( -0.7646288533564489232, -0.1113553986120547346, 0.8907480313885355327 ) ) ;
#37398=CARTESIAN_POINT ( 'NONE',  ( 0.8019270111902717657, 0.1787899950787401604, 0.8218503936470251681 ) ) ;
#37399=CARTESIAN_POINT ( 'NONE',  ( -0.9873396505805591694, -0.1113553986120547346, 1.569881889656251861 ) ) ;
#37400=CARTESIAN_POINT ( 'NONE',  ( 0.7185039370078714072, 0.06523048226347728795, 1.129429133858268708 ) ) ;
#37403=CARTESIAN_POINT ( 'NONE',  ( 0.8019270111902717657, 0.1787899950787401604, 1.889763779473794258 ) ) ;
#37404=CARTESIAN_POINT ( 'NONE',  ( 1.033464566929133799, 0.000000000000000000, 0.08858267716535432601 ) ) ;
#37405=CARTESIAN_POINT ( 'NONE',  ( 0.8759842519685039353, 0.000000000000000000, 4.498031496062992574 ) ) ;
#37408=FACE_OUTER_BOUND ( 'NONE', #24153, .T. ) ;
#37410=CARTESIAN_POINT ( 'NONE',  ( 1.054774247047244540, -0.07405724077823318263, 0.1820866141194649179 ) ) ;
#37413=CARTESIAN_POINT ( 'NONE',  ( -1.002407869896990045, 0.1264236179284866091, 1.759350393647023614 ) ) ;
#37415=CARTESIAN_POINT ( 'NONE',  ( -1.002407869896990045, -0.1264236179284866091, 1.321358267662771757 ) ) ;
#37416=CARTESIAN_POINT ( 'NONE',  ( -1.033464566929133799, 0.000000000000000000, 1.299212598317669221 ) ) ;
#37418=CARTESIAN_POINT ( 'NONE',  ( 0.8759842519685039353, 0.1787899950787401882, 1.336122047190330786 ) ) ;
#37420=CARTESIAN_POINT ( 'NONE',  ( -0.8759842519685039353, -0.1787899950787401882, 0.5290354330171024300 ) ) ;
#37421=CARTESIAN_POINT ( 'NONE',  ( 1.054774247047244540, 0.07405724077823318263, 1.914370078686394860 ) ) ;
#37422=CARTESIAN_POINT ( 'NONE',  ( -0.9500414927467378812, -0.1787899950787401604, 1.077755905458048113 ) ) ;
#37424=CARTESIAN_POINT ( 'NONE',  ( 1.033464566929133799, 0.000000000000000000, 0.5610236220472440971 ) ) ;
#37427=CARTESIAN_POINT ( 'NONE',  ( 1.002407869896990045, 0.1264236179284866091, 0.4650590550643464716 ) ) ;
#37428=CARTESIAN_POINT ( 'NONE',  ( -0.6971942568897637749, 2.189545951927499583E-17, 0.3567913385289137596 ) ) ;
#37429=CARTESIAN_POINT ( 'NONE',  ( -0.8019270111902717657, 0.1787899950787401604, 0.8218503936470251681 ) ) ;
#37430=CARTESIAN_POINT ( 'NONE',  ( 0.7185039370078746268, 0.06523048226347956391, 1.710137795168064079 ) ) ;
#37431=ORIENTED_EDGE ( 'NONE', *, *, #38591, .T. ) ;
#37435=CARTESIAN_POINT ( 'NONE',  ( 1.054774247047244540, -0.07405724077823318263, 0.9301181101824563813 ) ) ;
#37436=CARTESIAN_POINT ( 'NONE',  ( -0.8107537697050253289, 0.1574803149606300301, 0.1402559055118110520 ) ) ;
#37438=EDGE_CURVE ( 'NONE', #17112, #46310, #22499, .T. ) ;
#37439=CARTESIAN_POINT ( 'NONE',  ( 1.054774247047244540, -0.07405724077823318263, 1.205708661363558365 ) ) ;
#37440=CARTESIAN_POINT ( 'NONE',  ( -0.9500414927467377701, -0.1787899950787401604, 1.983267716481668108 ) ) ;
#37442=CARTESIAN_POINT ( 'NONE',  ( -1.054774247047244540, 0.07405724077823318263, 0.8956692912848198684 ) ) ;
#37443=( BOUNDED_CURVE ( )  B_SPLINE_CURVE ( 2, ( #12112, #4653, #29879, #18571, #25784, #22397, #29422, #41290, #37026 ),
 .UNSPECIFIED., .F., .T. ) 
 B_SPLINE_CURVE_WITH_KNOTS ( ( 3, 2, 2, 2, 3 ),
 ( 0.9200000000000000400, 0.9224999999999999867, 0.9250000000000000444, 0.9274999999999999911, 0.9300000000000000488 ),
 .UNSPECIFIED. ) 
 CURVE ( )  GEOMETRIC_REPRESENTATION_ITEM ( )  RATIONAL_B_SPLINE_CURVE ( ( 1.000000000000000000, 0.9238795325112869605, 1.000000000000000000, 0.9238795325112869605, 1.000000000000000000, 0.9238795325112869605, 1.000000000000000000, 0.9238795325112869605, 1.000000000000000000 ) ) 
 REPRESENTATION_ITEM ( '' )  ) ;
#37445=CARTESIAN_POINT ( 'NONE',  ( -1.054774247047244540, -0.07405724077823318263, 0.05905511805647267048 ) ) ;
#37452=CARTESIAN_POINT ( 'NONE',  ( 1.054774247047244096, 0.000000000000000000, 1.321358267662771757 ) ) ;
#37457=CARTESIAN_POINT ( 'NONE',  ( 0.6971942568897648851, -0.07405724077823297447, 1.540354330654897685 ) ) ;
#37458=CARTESIAN_POINT ( 'NONE',  ( 1.002407869896990045, -0.1264236179284866091, 0.1353346456155277433 ) ) ;
#37463=DIMENSIONAL_EXPONENTS ( 1.000000000000000000, 0.000000000000000000, 0.000000000000000000, 0.000000000000000000, 0.000000000000000000, 0.000000000000000000, 0.000000000000000000 ) ;
#37465=CARTESIAN_POINT ( 'NONE',  ( -0.6971942568897637749, 2.189545951927499583E-17, 0.5979330708123780092 ) ) ;
#37470=CARTESIAN_POINT ( 'NONE',  ( -0.8759842519685039353, -0.1574803149606299191, 1.604330708553889595 ) ) ;
#37471=CYLINDRICAL_SURFACE ( 'NONE', #45996, 0.1574803149606299191 ) ;
#37472=CARTESIAN_POINT ( 'NONE',  ( 0.9500414927467378812, 0.1787899950787401604, 1.373031496009229135 ) ) ;
#37473=CARTESIAN_POINT ( 'NONE',  ( 1.002407869896990045, 0.1264236179284866091, 1.877460629867496067 ) ) ;
#37474=CARTESIAN_POINT ( 'NONE',  ( -0.8759842519685039353, 0.000000000000000000, 0.000000000000000000 ) ) ;
#37476=CARTESIAN_POINT ( 'NONE',  ( -0.7185039370078746268, 0.06523048226347956391, 1.523129921259841923 ) ) ;
#37479=CARTESIAN_POINT ( 'NONE',  ( -1.033464566929134687, 0.06523048226347956391, 1.222933070758614127 ) ) ;
#37480=CARTESIAN_POINT ( 'NONE',  ( 0.7495606340400177148, -0.1264236179284866091, 0.3223425196312759144 ) ) ;
#37481=CYLINDRICAL_SURFACE ( 'NONE', #30051, 0.1574803149606299191 ) ;
#37483=CARTESIAN_POINT ( 'NONE',  ( -0.8759842519685039353, 0.000000000000000000, 2.007874015640504162 ) ) ;
#37484=CARTESIAN_POINT ( 'NONE',  ( 0.9873396505805591694, 0.1113553986120547346, 0.6742125983176693316 ) ) ;
#37486=DIRECTION ( 'NONE',  ( 0.000000000000000000, 0.000000000000000000, -1.000000000000000000 ) ) ;
#37492=CARTESIAN_POINT ( 'NONE',  ( -0.9412147342319837628, 0.1574803149606300301, 1.198326771653543510 ) ) ;
#37494=CARTESIAN_POINT ( 'NONE',  ( -1.033464566929133799, 0.000000000000000000, 0.4429133858267716439 ) ) ;
#37495=CARTESIAN_POINT ( 'NONE',  ( -0.7185039370078739607, 1.928577636452523993E-17, 0.09842519674286673292 ) ) ;
#37496=CARTESIAN_POINT ( 'NONE',  ( 0.9873396505805591694, 0.1113553986120547346, 1.943897637795275690 ) ) ;
#37498=EDGE_CURVE ( 'NONE', #7863, #24526, #31260, .T. ) ;
#37502=CARTESIAN_POINT ( 'NONE',  ( 0.7495606340400177148, 0.1264236179284866091, 0.9867125983714331028 ) ) ;
#37504=CARTESIAN_POINT ( 'NONE',  ( -0.7495606340400177148, -0.1264236179284866091, 1.272145669237574772 ) ) ;
#37506=EDGE_CURVE ( 'NONE', #44561, #14442, #42870, .T. ) ;
#37508=CARTESIAN_POINT ( 'NONE',  ( -0.7495606340400177148, -0.1264236179284866091, 0.3272637794737956463 ) ) ;
#37514=ORIENTED_EDGE ( 'NONE', *, *, #40291, .F. ) ;
#37515=CARTESIAN_POINT ( 'NONE',  ( 1.002407869896990045, -0.1264236179284866091, 1.040846456639149764 ) ) ;
#37521=CARTESIAN_POINT ( 'NONE',  ( -1.054774247047244540, 0.07405724077823318263, 0.2657480314422993595 ) ) ;
#37522=CARTESIAN_POINT ( 'NONE',  ( -0.7185039370078746268, -0.06523048226347956391, 0.8193897637795271027 ) ) ;
#37525=CARTESIAN_POINT ( 'NONE',  ( 1.033464566929134687, -0.06523048226347956391, 1.109744094488189115 ) ) ;
#37526=CARTESIAN_POINT ( 'NONE',  ( -0.8759842519685039353, 0.1574803149606299191, 1.545275590443653480 ) ) ;
#37527=CARTESIAN_POINT ( 'NONE',  ( 1.054774247047244540, 0.07405724077823318263, 0.9744094487651340231 ) ) ;
#37529=CARTESIAN_POINT ( 'NONE',  ( 0.9873396505805591694, -0.1113553986120547346, 1.461614173228346525 ) ) ;
#37530=CARTESIAN_POINT ( 'NONE',  ( 0.7139362040247607677, -0.04189616717365371446, 1.984049518046542504 ) ) ;
#37534=CARTESIAN_POINT ( 'NONE',  ( 0.6971942568897637749, 2.189545951927499583E-17, 0.8686023621509606496 ) ) ;
#37535=CARTESIAN_POINT ( 'NONE',  ( 1.002407869896990045, 0.1264236179284866091, 1.803641732229700700 ) ) ;
#37539=CARTESIAN_POINT ( 'NONE',  ( -0.7185039370078739607, 0.000000000000000000, -2.869337061179095023E-17 ) ) ;
#37541=CARTESIAN_POINT ( 'NONE',  ( 0.7495606340400177148, 0.1264236179284866091, 1.218011810969858111 ) ) ;
#37542=CARTESIAN_POINT ( 'NONE',  ( -0.7185039370078739607, 1.928577636452523993E-17, 1.053149606299212504 ) ) ;
#37544=CARTESIAN_POINT ( 'NONE',  ( -0.7646288533564489232, -0.1113553986120547346, 0.5068897637795275468 ) ) ;
#37547=CARTESIAN_POINT ( 'NONE',  ( -0.7495606340400177148, 0.1264236179284866091, 0.3124999999462365619 ) ) ;
#37552=CARTESIAN_POINT ( 'NONE',  ( -0.8019270111902717657, -0.1787899950787401604, 1.820866141678520789 ) ) ;
#37553=CARTESIAN_POINT ( 'NONE',  ( -1.054774247047244540, 0.07405724077823318263, 0.8513779527021426707 ) ) ;
#37555=CARTESIAN_POINT ( 'NONE',  ( -1.002407869896990045, 0.1264236179284866091, 1.129429133804503937 ) ) ;
#37556=CARTESIAN_POINT ( 'NONE',  ( -0.8019270111902717657, -0.1787899950787401604, 0.5659448818360001132 ) ) ;
#37564=CYLINDRICAL_SURFACE ( 'NONE', #11920, 0.1574803149606299191 ) ;
#37567=DIRECTION ( 'NONE',  ( 0.000000000000000000, 0.000000000000000000, -1.000000000000000000 ) ) ;
#37568=CARTESIAN_POINT ( 'NONE',  ( -0.6971942568897626646, -0.07405724077823297447, 0.4773622046706456068 ) ) ;
#37572=ADVANCED_FACE ( 'NONE', ( #35722 ), #2857, .T. ) ;
#37575=CARTESIAN_POINT ( 'NONE',  ( 0.9412147342319837628, -0.1574803149606297803, 0.4749015748031497064 ) ) ;
#37577=CARTESIAN_POINT ( 'NONE',  ( -1.033464566929134687, -0.06523048226347956391, 1.099901574695622886 ) ) ;
#37578=CARTESIAN_POINT ( 'NONE',  ( 1.054774247047244096, 0.000000000000000000, 0.5388779527021417826 ) ) ;
#37582=CARTESIAN_POINT ( 'NONE',  ( 1.033464566929134687, 0.06523048226347956391, 1.931594488081448180 ) ) ;
#37585=CARTESIAN_POINT ( 'NONE',  ( -0.9500414927467377701, 0.1787899950787401604, 1.058070866087969186 ) ) ;
#37586=CARTESIAN_POINT ( 'NONE',  ( 0.7646288533564489232, 0.1113553986120547346, 0.8907480314960629642 ) ) ;
#37588=( BOUNDED_CURVE ( )  B_SPLINE_CURVE ( 2, ( #40194, #7609, #18631, #19104, #22225, #7850, #7391, #26078, #22467 ),
 .UNSPECIFIED., .F., .T. ) 
 B_SPLINE_CURVE_WITH_KNOTS ( ( 3, 2, 2, 2, 3 ),
 ( 0.4899999999999999911, 0.4924999999999999933, 0.4949999999999999956, 0.4974999999999999978, 0.5000000000000000000 ),
 .UNSPECIFIED. ) 
 CURVE ( )  GEOMETRIC_REPRESENTATION_ITEM ( )  RATIONAL_B_SPLINE_CURVE ( ( 1.000000000000000000, 0.9238795325112869605, 1.000000000000000000, 0.9238795325112869605, 1.000000000000000000, 0.9238795325112869605, 1.000000000000000000, 0.9238795325112869605, 1.000000000000000000 ) ) 
 REPRESENTATION_ITEM ( '' )  ) ;
#37589=VECTOR ( 'NONE', #45110, 39.37007874015748143 ) ;
#37593=ORIENTED_EDGE ( 'NONE', *, *, #32611, .F. ) ;
#37597=CARTESIAN_POINT ( 'NONE',  ( 1.054774247047244540, -0.07405724077823318263, 0.7283464566391493200 ) ) ;
#37600=CARTESIAN_POINT ( 'NONE',  ( -0.8759842519685039353, 0.1574803149606299191, 0.4429133857192448787 ) ) ;
#37605=CARTESIAN_POINT ( 'NONE',  ( 0.8759842519685039353, -0.1574803149606299191, 1.171259842412157637 ) ) ;
#37610=CARTESIAN_POINT ( 'NONE',  ( -0.9500414927467378812, 0.1787899950787401604, 1.806102362150961316 ) ) ;
#37611=CARTESIAN_POINT ( 'NONE',  ( 0.8759842519685039353, 0.1787899950787401882, 1.769192913332062966 ) ) ;
#37614=CARTESIAN_POINT ( 'NONE',  ( 0.6971942568897626646, 0.07405724077823318263, 0.3592519684501735977 ) ) ;
#37615=CARTESIAN_POINT ( 'NONE',  ( -0.6971942568897648851, -0.07405724077823297447, 1.382874015694268044 ) ) ;
#37617=CARTESIAN_POINT ( 'NONE',  ( -0.8019270111902716547, 0.1787899950787401604, 1.176181102308441195 ) ) ;
#37618=CARTESIAN_POINT ( 'NONE',  ( -1.054774247047244540, 0.07405724077823318263, 0.9301181101824563813 ) ) ;
#37619=CARTESIAN_POINT ( 'NONE',  ( -1.002407869896990045, 0.1264236179284866091, 0.03198818892261445085 ) ) ;
#37620=( BOUNDED_CURVE ( )  B_SPLINE_CURVE ( 2, ( #38219, #5379, #16192, #34180, #15964, #26992, #31057, #45622, #12839 ),
 .UNSPECIFIED., .F., .F. ) 
 B_SPLINE_CURVE_WITH_KNOTS ( ( 3, 2, 2, 2, 3 ),
 ( 0.9200000000000000400, 0.9224999999999999867, 0.9250000000000000444, 0.9274999999999999911, 0.9300000000000000488 ),
 .UNSPECIFIED. ) 
 CURVE ( )  GEOMETRIC_REPRESENTATION_ITEM ( )  RATIONAL_B_SPLINE_CURVE ( ( 1.000000000000000000, 0.9238795325112869605, 1.000000000000000000, 0.9238795325112869605, 1.000000000000000000, 0.9238795325112869605, 1.000000000000000000, 0.9238795325112829637, 1.000000000000000000 ) ) 
 REPRESENTATION_ITEM ( '' )  ) ;
#37622=CARTESIAN_POINT ( 'NONE',  ( -1.054774247047244540, 0.07405724077823318263, 1.722440944828125930 ) ) ;
#37623=CARTESIAN_POINT ( 'NONE',  ( -1.054774247047244096, 0.000000000000000000, 0.1058070865604096300 ) ) ;
#37625=CARTESIAN_POINT ( 'NONE',  ( -0.8759842519685039353, -0.1574803149606299191, 1.614173228346456712 ) ) ;
#37626=( BOUNDED_CURVE ( )  B_SPLINE_CURVE ( 2, ( #19577, #34222, #27036, #5426, #20045, #34685, #16700, #23891, #9512 ),
 .UNSPECIFIED., .F., .F. ) 
 B_SPLINE_CURVE_WITH_KNOTS ( ( 3, 2, 2, 2, 3 ),
 ( 0.1199999999999999956, 0.1224999999999999978, 0.1250000000000000000, 0.1275000000000000022, 0.1300000000000000044 ),
 .UNSPECIFIED. ) 
 CURVE ( )  GEOMETRIC_REPRESENTATION_ITEM ( )  RATIONAL_B_SPLINE_CURVE ( ( 1.000000000000000000, 0.9238795325112869605, 1.000000000000000000, 0.9238795325112869605, 1.000000000000000000, 0.9238795325112869605, 1.000000000000000000, 0.9238795325112869605, 1.000000000000000000 ) ) 
 REPRESENTATION_ITEM ( '' )  ) ;
#37627=CARTESIAN_POINT ( 'NONE',  ( 0.9500414927467377701, -0.1787899950787401604, 1.633858267662771091 ) ) ;
#37629=CARTESIAN_POINT ( 'NONE',  ( 0.8107537697050254399, 0.1574803149606300301, 0.2091535431995598104 ) ) ;
#37635=CARTESIAN_POINT ( 'NONE',  ( -1.054774247047244540, 0.07405724077823318263, 1.171259842465921741 ) ) ;
#37636=ORIENTED_EDGE ( 'NONE', *, *, #25666, .F. ) ;
#37640=ORIENTED_EDGE ( 'NONE', *, *, #19360, .T. ) ;
#37641=CARTESIAN_POINT ( 'NONE',  ( -1.033464566929133799, 0.000000000000000000, 1.269685039370078705 ) ) ;
#37646=CARTESIAN_POINT ( 'NONE',  ( -1.033464566929134687, -0.06523048226347956391, 0.9030511809948349455 ) ) ;
#37647=CARTESIAN_POINT ( 'NONE',  ( 0.6971942568897637749, 2.189545951927499583E-17, 0.7111220471903307860 ) ) ;
#37652=CARTESIAN_POINT ( 'NONE',  ( 0.9500414927467378812, 0.1787899950787401604, 1.845472440891119392 ) ) ;
#37653=EDGE_CURVE ( 'NONE', #46488, #8877, #34613, .T. ) ;
#37656=CARTESIAN_POINT ( 'NONE',  ( 0.7646288533564489232, -0.1113553986120547346, 0.07381889763779526936 ) ) ;
#37659=CARTESIAN_POINT ( 'NONE',  ( 0.8107537697050234415, -0.1574803149606297803, 0.1156496062992125873 ) ) ;
#37661=CARTESIAN_POINT ( 'NONE',  ( 1.054774247047244540, -0.07405724077823318263, 0.2214566928596220785 ) ) ;
#37662=EDGE_CURVE ( 'NONE', #13298, #45388, #24572, .T. ) ;
#37663=CARTESIAN_POINT ( 'NONE',  ( -0.6971942568897637749, 2.189545951927499583E-17, 1.695374015694267822 ) ) ;
#37665=CARTESIAN_POINT ( 'NONE',  ( -0.6971942568897648851, -0.07405724077823297447, 1.309055118056472899 ) ) ;
#37666=CARTESIAN_POINT ( 'NONE',  ( -0.8759842519685039353, 0.1574803149606299191, 1.318897637795275690 ) ) ;
#37667=CARTESIAN_POINT ( 'NONE',  ( 0.8019270111902717657, 0.1787899950787401604, 1.259842519631276359 ) ) ;
#37668=CARTESIAN_POINT ( 'NONE',  ( -0.8759842519685039353, 0.1787899950787401882, 0.5487204723871811352 ) ) ;
#37669=VECTOR ( 'NONE', #6498, 39.37007874015748143 ) ;
#37671=CARTESIAN_POINT ( 'NONE',  ( -1.054774247047244540, -0.07405724077823318263, 1.200787401521039355 ) ) ;
#37672=FACE_OUTER_BOUND ( 'NONE', #22151, .T. ) ;
#37674=CARTESIAN_POINT ( 'NONE',  ( 0.7185039370078746268, 0.06523048226347956391, 0.05659448808144944970 ) ) ;
#37675=CARTESIAN_POINT ( 'NONE',  ( 1.054774247047244540, -0.07405724077823318263, 0.5364173227808820554 ) ) ;
#37676=CARTESIAN_POINT ( 'NONE',  ( -0.8759842519685039353, -0.1787899950787401882, 0.4453740156942677664 ) ) ;
#37679=ORIENTED_EDGE ( 'NONE', *, *, #41029, .F. ) ;
#37681=CARTESIAN_POINT ( 'NONE',  ( -0.8759842519685039353, 0.1574803149606299191, 0.1771653543307086520 ) ) ;
#37682=CARTESIAN_POINT ( 'NONE',  ( 0.6971942568897637749, 2.189545951927499583E-17, 1.149114173174582643 ) ) ;
#37683=CARTESIAN_POINT ( 'NONE',  ( 0.9412147342319837628, 0.1574803149606300301, 1.936515747923967412 ) ) ;
#37687=CYLINDRICAL_SURFACE ( 'NONE', #18884, 0.1574803149606299191 ) ;
#37688=CARTESIAN_POINT ( 'NONE',  ( 0.7646288533564489232, -0.1113553986120547346, 0.3100393700787401619 ) ) ;
#37693=ORIENTED_EDGE ( 'NONE', *, *, #3786, .T. ) ;
#37694=CARTESIAN_POINT ( 'NONE',  ( 0.7495606340400177148, -0.1264236179284866091, 1.306594488135212728 ) ) ;
#37696=CARTESIAN_POINT ( 'NONE',  ( 1.033464566929134687, -0.06523048226347956391, 0.7455708660342049710 ) ) ;
#37698=CARTESIAN_POINT ( 'NONE',  ( 0.9500414927467378812, 0.1787899950787401604, 1.564960629867495845 ) ) ;
#37699=CARTESIAN_POINT ( 'NONE',  ( 0.9500414927467378812, -0.1787899950787401604, 0.1328740156942679607 ) ) ;
#37703=EDGE_CURVE ( 'NONE', #11244, #26454, #14785, .T. ) ;
#37705=CARTESIAN_POINT ( 'NONE',  ( -0.6971942568897648851, -0.07405724077823297447, 0.6791338582139527791 ) ) ;
#37709=CARTESIAN_POINT ( 'NONE',  ( -0.7185039370078766252, -0.06523048226348168721, 1.596948818790109970 ) ) ;
#37713=CARTESIAN_POINT ( 'NONE',  ( 0.8759842519685039353, -0.1787899950787401882, 1.395177165300567124 ) ) ;
#37714=CARTESIAN_POINT ( 'NONE',  ( 0.6971942568897637749, 2.189545951927499583E-17, 1.813484251914740053 ) ) ;
#37715=CARTESIAN_POINT ( 'NONE',  ( 1.054774247047244096, 0.000000000000000000, 0.2977362204186775885 ) ) ;
#37719=CARTESIAN_POINT ( 'NONE',  ( 0.8759842519685039353, 0.000000000000000000, 4.498031496062992574 ) ) ;
#37720=CARTESIAN_POINT ( 'NONE',  ( -0.7466676322263418042, 0.09839106858983247272, 1.981216915731769612 ) ) ;
#37721=DIRECTION ( 'NONE',  ( 1.822029033848725028E-16, 0.000000000000000000, 1.000000000000000000 ) ) ;
#37723=CARTESIAN_POINT ( 'NONE',  ( 0.6971942568897626646, -0.07405724077823297447, 0.3592519684501735977 ) ) ;
#37724=CARTESIAN_POINT ( 'NONE',  ( 0.9412147342319837628, 0.1574803149606300301, 1.975885826664125711 ) ) ;
#37725=CARTESIAN_POINT ( 'NONE',  ( 0.7185039370078746268, 0.06523048226347956391, 0.8538385826771661691 ) ) ;
#37727=CARTESIAN_POINT ( 'NONE',  ( -0.6971942568897648851, -0.07405724077823297447, 1.304133858213953667 ) ) ;
#37728=CARTESIAN_POINT ( 'NONE',  ( 0.7646288533564489232, -0.1113553986120547346, 0.7332677164279054471 ) ) ;
#37730=CARTESIAN_POINT ( 'NONE',  ( 0.8432997816974205918, 0.1735131131385767855, 0.03937007914154261323 ) ) ;
#37734=CARTESIAN_POINT ( 'NONE',  ( -0.8759842519685039353, 0.1574803149606299191, 0.8070866141732283561 ) ) ;
#37735=CARTESIAN_POINT ( 'NONE',  ( 0.8759842519685039353, -0.1787899950787401882, 1.547736220418677089 ) ) ;
#37736=CARTESIAN_POINT ( 'NONE',  ( -0.8107537697050253289, 0.1574803149606300301, 1.203248031496062520 ) ) ;
#37741=ORIENTED_EDGE ( 'NONE', *, *, #37772, .F. ) ;
#37742=ORIENTED_EDGE ( 'NONE', *, *, #8812, .F. ) ;
#37743=( BOUNDED_CURVE ( )  B_SPLINE_CURVE ( 2, ( #7110, #21734, #22612, #39451, #37225, #4371, #36994, #35871, #19001 ),
 .UNSPECIFIED., .F., .T. ) 
 B_SPLINE_CURVE_WITH_KNOTS ( ( 3, 2, 2, 2, 3 ),
 ( 0.6700000000000000400, 0.6724999999999999867, 0.6750000000000000444, 0.6774999999999999911, 0.6800000000000000488 ),
 .UNSPECIFIED. ) 
 CURVE ( )  GEOMETRIC_REPRESENTATION_ITEM ( )  RATIONAL_B_SPLINE_CURVE ( ( 1.000000000000000000, 0.9238795325112869605, 1.000000000000000000, 0.9238795325112869605, 1.000000000000000000, 0.9238795325112869605, 1.000000000000000000, 0.9238795325112869605, 1.000000000000000000 ) ) 
 REPRESENTATION_ITEM ( '' )  ) ;
#37746=CARTESIAN_POINT ( 'NONE',  ( -1.054774247047244540, -0.07405724077823318263, 1.245078740103716886 ) ) ;
#37748=CIRCLE ( 'NONE', #17065, 0.1574803149606299191 ) ;
#37751=CYLINDRICAL_SURFACE ( 'NONE', #13828, 0.1574803149606299191 ) ;
#37752=CARTESIAN_POINT ( 'NONE',  ( -1.002407869896990045, 0.1264236179284866091, 0.3075787401037169411 ) ) ;
#37754=CARTESIAN_POINT ( 'NONE',  ( -0.7185039370078739607, 1.928577636452523993E-17, 1.210629921259842590 ) ) ;
#37759=EDGE_LOOP ( 'NONE', ( #45684, #30175, #45653, #4658 ) ) ;
#37761=DIRECTION ( 'NONE',  ( 0.000000000000000000, 0.000000000000000000, -1.000000000000000000 ) ) ;
#37762=CYLINDRICAL_SURFACE ( 'NONE', #17838, 0.1574803149606299191 ) ;
#37765=ADVANCED_FACE ( 'NONE', ( #43359 ), #32620, .T. ) ;
#37766=CARTESIAN_POINT ( 'NONE',  ( -0.9412147342319837628, -0.1574803149606297803, 0.8686023622047237547 ) ) ;
#37769=DIRECTION ( 'NONE',  ( -1.000000000000000000, 0.000000000000000000, 0.000000000000000000 ) ) ;
#37770=CARTESIAN_POINT ( 'NONE',  ( 0.8759842519685039353, -0.1787899950787401882, 1.001476377898992132 ) ) ;
#37771=CARTESIAN_POINT ( 'NONE',  ( 0.8759842519685039353, -0.1787899950787401882, 1.390255905458047447 ) ) ;
#37772=EDGE_CURVE ( 'NONE', #15853, #26252, #24129, .T. ) ;
#37775=DIRECTION ( 'NONE',  ( 0.000000000000000000, 0.000000000000000000, -1.000000000000000000 ) ) ;
#37776=CARTESIAN_POINT ( 'NONE',  ( 0.9873396505805591694, -0.1113553986120547346, 1.500984251968503935 ) ) ;
#37777=CARTESIAN_POINT ( 'NONE',  ( 0.7100468655899934145, 0.001942326053023950760, 1.983232204919558761 ) ) ;
#37782=CARTESIAN_POINT ( 'NONE',  ( 0.8019270111902716547, 0.1787899950787401604, 1.018700787347811110 ) ) ;
#37783=CARTESIAN_POINT ( 'NONE',  ( 1.033464566929133799, 1.928577636452524610E-17, 4.498031496062992574 ) ) ;
#37784=CARTESIAN_POINT ( 'NONE',  ( 1.054774247047244096, 0.000000000000000000, 1.798720472387181024 ) ) ;
#37788=CARTESIAN_POINT ( 'NONE',  ( 0.8107537697050254399, 0.1574803149606300301, 1.085137795275590955 ) ) ;
#37791=CARTESIAN_POINT ( 'NONE',  ( -0.7646288533564489232, 0.1113553986120547346, 0.09350393690034704275 ) ) ;
#37793=CARTESIAN_POINT ( 'NONE',  ( 0.6971942568897648851, 0.07405724077823318263, 1.102362204670646495 ) ) ;
#37798=CARTESIAN_POINT ( 'NONE',  ( -0.7495606340400177148, 0.1264236179284866091, 0.2337598424659216578 ) ) ;
#37801=CARTESIAN_POINT ( 'NONE',  ( -0.9500414927467378812, 0.1787899950787401604, 1.879921259788756016 ) ) ;
#37802=CARTESIAN_POINT ( 'NONE',  ( -1.054774247047244096, 0.000000000000000000, 0.9670275590013542866 ) ) ;
#37803=ADVANCED_FACE ( 'NONE', ( #28550 ), #18439, .T. ) ;
#37804=CARTESIAN_POINT ( 'NONE',  ( -1.054774247047244096, 0.000000000000000000, 0.4995078739619842612 ) ) ;
#37807=DIRECTION ( 'NONE',  ( -1.000000000000000000, 0.000000000000000000, 0.000000000000000000 ) ) ;
#37808=CARTESIAN_POINT ( 'NONE',  ( -0.7646288533564489232, 0.1113553986120547346, 1.678149606299212726 ) ) ;
#37812=CARTESIAN_POINT ( 'NONE',  ( 0.8759842519685039353, 0.1574803149606299191, 1.791338582677165281 ) ) ;
#37813=CARTESIAN_POINT ( 'NONE',  ( 0.7185039370078739607, 0.000000000000000000, 4.498031496062992574 ) ) ;
#37814=CARTESIAN_POINT ( 'NONE',  ( -0.7185039370078766252, -0.06523048226348168721, 1.163877952648377567 ) ) ;
#37815=CARTESIAN_POINT ( 'NONE',  ( -0.8759842519685039353, -0.1787899950787401882, 0.4453740156942677664 ) ) ;
#37816=CARTESIAN_POINT ( 'NONE',  ( 0.9412147342319837628, 0.1574803149606300301, 1.188484251860977503 ) ) ;
#37820=CARTESIAN_POINT ( 'NONE',  ( -0.6971942568897648851, -0.07405724077823297447, 1.584645669237574994 ) ) ;
#37827=CARTESIAN_POINT ( 'NONE',  ( 0.7646288533564489232, 0.1113553986120547346, 0.4970472440944882497 ) ) ;
#37828=LINE ( 'NONE', #1375, #18665 ) ;
#37829=CARTESIAN_POINT ( 'NONE',  ( -0.8759842519685039353, 0.1574803149606299191, 1.269685039262551163 ) ) ;
#37830=CARTESIAN_POINT ( 'NONE',  ( 0.9500414927467378812, -0.1787899950787401604, 0.5708661416785201226 ) ) ;
#37832=CARTESIAN_POINT ( 'NONE',  ( 0.8107537697050254399, -0.1574803149606297803, 1.759350393593260842 ) ) ;
#37833=CARTESIAN_POINT ( 'NONE',  ( 0.9412147342319837628, 0.1574803149606300301, 1.897145669183811778 ) ) ;
#37834=ORIENTED_EDGE ( 'NONE', *, *, #23762, .T. ) ;
#37837=CARTESIAN_POINT ( 'NONE',  ( -1.054774247047244540, 0.07405724077823318263, 1.053149606245450176 ) ) ;
#37838=CARTESIAN_POINT ( 'NONE',  ( 0.7646288533564489232, 0.1113553986120547346, 1.166338582677165281 ) ) ;
#37839=CARTESIAN_POINT ( 'NONE',  ( -0.7646288533564489232, 0.1113553986120547346, 0.7234251967428662056 ) ) ;
#37849=CARTESIAN_POINT ( 'NONE',  ( 0.9412147342319837628, 0.1574803149606300301, 1.158956692913385655 ) ) ;
#37851=CARTESIAN_POINT ( 'NONE',  ( -0.7185039370078714072, 0.06523048226347728795, 1.788877952648379122 ) ) ;
#37852=CARTESIAN_POINT ( 'NONE',  ( 0.7185039370078746268, -0.06523048226347956391, 0.8981299212598432558 ) ) ;
#37855=CARTESIAN_POINT ( 'NONE',  ( 1.033464566929134687, -0.06523048226347956391, 1.139271653435780962 ) ) ;
#37860=CARTESIAN_POINT ( 'NONE',  ( -0.9500414927467378812, -0.1787899950787401604, 1.791338582623401177 ) ) ;
#37861=CARTESIAN_POINT ( 'NONE',  ( 1.002407869896990045, 0.1264236179284866091, 1.803641732229700700 ) ) ;
#37862=ORIENTED_EDGE ( 'NONE', *, *, #23048, .T. ) ;
#37864=CARTESIAN_POINT ( 'NONE',  ( -0.8759842519685039353, -0.1787899950787401882, 0.8833661416785196785 ) ) ;
#37866=CARTESIAN_POINT ( 'NONE',  ( 1.002407869896990045, 0.1264236179284866091, 0.3863188975840318173 ) ) ;
#37867=CARTESIAN_POINT ( 'NONE',  ( -1.002407869896990045, 0.1264236179284866091, 1.365649606245448844 ) ) ;
#37869=CARTESIAN_POINT ( 'NONE',  ( -0.7495606340400177148, 0.1264236179284866091, 1.257381889710015743 ) ) ;
#37870=CARTESIAN_POINT ( 'NONE',  ( -0.8759842519685039353, -0.1787899950787401882, 0.1353346456155279653 ) ) ;
#37871=CARTESIAN_POINT ( 'NONE',  ( -0.8107537697050254399, 0.1574803149606300301, 0.5733267716535435099 ) ) ;
#37872=CARTESIAN_POINT ( 'NONE',  ( -0.8759842519685039353, 0.1787899950787401882, 1.808562992072220377 ) ) ;
#37873=CARTESIAN_POINT ( 'NONE',  ( -0.8019270111902717657, -0.1787899950787401604, 0.09350393695411057804 ) ) ;
#37875=CARTESIAN_POINT ( 'NONE',  ( -1.033464566929133799, 0.000000000000000000, 1.781496062992125928 ) ) ;
#37876=CARTESIAN_POINT ( 'NONE',  ( -0.9873396505805591694, 0.1113553986120547346, 0.2903543307086614012 ) ) ;
#37877=CARTESIAN_POINT ( 'NONE',  ( 0.6971942568897637749, 2.189545951927499583E-17, 1.542814960576157413 ) ) ;
#37879=CARTESIAN_POINT ( 'NONE',  ( 0.7185039370078739607, 1.928577636452523993E-17, 0.2165354329633393804 ) ) ;
#37885=EDGE_CURVE ( 'NONE', #32335, #8877, #45682, .T. ) ;
#37890=EDGE_CURVE ( 'NONE', #43867, #11471, #44429, .T. ) ;
#37891=CARTESIAN_POINT ( 'NONE',  ( -0.8759842519685039353, -0.1574803149606299191, 0.8956692912310552090 ) ) ;
#37892=CARTESIAN_POINT ( 'NONE',  ( 0.8759842519685039353, 0.1787899950787401882, 0.7012795275052913224 ) ) ;
#37894=CARTESIAN_POINT ( 'NONE',  ( 0.7185039370078739607, 1.928577636452523993E-17, 1.210629921259842590 ) ) ;
#37895=CARTESIAN_POINT ( 'NONE',  ( 1.033464566929133799, 0.000000000000000000, 0.4429133858267716439 ) ) ;
#37896=CARTESIAN_POINT ( 'NONE',  ( 0.8019270111902717657, 0.1787899950787401604, 1.968503936954110189 ) ) ;
#37897=CARTESIAN_POINT ( 'NONE',  ( 0.9873396505805591694, -0.1113553986120547346, 0.04429133858267716300 ) ) ;
#37900=CARTESIAN_POINT ( 'NONE',  ( 1.033464566929134687, -0.06523048226347956391, 0.1254921259842521064 ) ) ;
#37902=( BOUNDED_CURVE ( )  B_SPLINE_CURVE ( 2, ( #38641, #31232, #45810, #44922, #27659, #8279, #8517, #833, #11668 ),
 .UNSPECIFIED., .F., .F. ) 
 B_SPLINE_CURVE_WITH_KNOTS ( ( 3, 2, 2, 2, 3 ),
 ( 0.9000000000000000222, 0.9024999999999999689, 0.9050000000000000266, 0.9074999999999999734, 0.9100000000000000311 ),
 .UNSPECIFIED. ) 
 CURVE ( )  GEOMETRIC_REPRESENTATION_ITEM ( )  RATIONAL_B_SPLINE_CURVE ( ( 1.000000000000000000, 0.9238795325112869605, 1.000000000000000000, 0.9238795325112869605, 1.000000000000000000, 0.9238795325112869605, 1.000000000000000000, 0.9238795325112829637, 1.000000000000000000 ) ) 
 REPRESENTATION_ITEM ( '' )  ) ;
#37903=CARTESIAN_POINT ( 'NONE',  ( 0.9500414927467378812, -0.1787899950787401604, 0.2165354330171024577 ) ) ;
#37904=CARTESIAN_POINT ( 'NONE',  ( -0.8759842519685039353, -0.1787899950787401882, 1.705216535379307174 ) ) ;
#37905=ORIENTED_EDGE ( 'NONE', *, *, #43280, .F. ) ;
#37907=CARTESIAN_POINT ( 'NONE',  ( -0.9500414927467378812, -0.1787899950787401604, 1.318897637741511364 ) ) ;
#37908=CARTESIAN_POINT ( 'NONE',  ( -1.033464566929133799, 0.000000000000000000, 1.309055118110236338 ) ) ;
#37909=CARTESIAN_POINT ( 'NONE',  ( 0.6971942568897648851, 0.07405724077823318263, 1.461614173174583753 ) ) ;
#37910=AXIS2_PLACEMENT_3D ( 'NONE', #5813, #35298, #20422 ) ;
#37912=CARTESIAN_POINT ( 'NONE',  ( -0.8759842519685039353, -0.1787899950787401882, 1.193405511757259951 ) ) ;
#37913=DIRECTION ( 'NONE',  ( 0.000000000000000000, 0.000000000000000000, -1.000000000000000000 ) ) ;
#37915=CARTESIAN_POINT ( 'NONE',  ( 0.8759842519685039353, 0.1574803149606299191, 0.04921259831766984505 ) ) ;
#37916=CARTESIAN_POINT ( 'NONE',  ( 0.9500414927467377701, -0.1787899950787401604, 0.4921259841982049132 ) ) ;
#37917=CARTESIAN_POINT ( 'NONE',  ( -0.9500414927467377701, -0.1787899950787401604, 0.3297244093950555954 ) ) ;
#37918=EDGE_CURVE ( 'NONE', #41944, #13298, #19670, .T. ) ;
#37921=CARTESIAN_POINT ( 'NONE',  ( -0.7185039370078746268, -0.06523048226347956391, 0.3075787401574804347 ) ) ;
#37922=CARTESIAN_POINT ( 'NONE',  ( 1.054774247047244540, 0.07405724077823318263, 1.210629921206079818 ) ) ;
#37923=CARTESIAN_POINT ( 'NONE',  ( -0.8759842519685039353, 0.1787899950787401882, 1.961122047190330786 ) ) ;
#37926=FACE_OUTER_BOUND ( 'NONE', #24083, .T. ) ;
#37927=CARTESIAN_POINT ( 'NONE',  ( -1.002407869896990045, -0.1264236179284866091, 0.9276574802611967652 ) ) ;
#37932=CARTESIAN_POINT ( 'NONE',  ( -1.033464566929134687, 0.06523048226347956391, 1.380413385719244435 ) ) ;
#37934=CARTESIAN_POINT ( 'NONE',  ( -1.033464566929133799, 0.000000000000000000, 0.08858267716535432601 ) ) ;
#37936=CARTESIAN_POINT ( 'NONE',  ( 1.054774247047244540, -0.07405724077823318263, 1.318897637741511364 ) ) ;
#37937=CIRCLE ( 'NONE', #47126, 0.1574803149606299191 ) ;
#37938=CARTESIAN_POINT ( 'NONE',  ( 0.8107537697050254399, 0.1574803149606300301, 0.8882874015748026819 ) ) ;
#37940=EDGE_CURVE ( 'NONE', #30928, #12054, #3145, .T. ) ;
#37941=CARTESIAN_POINT ( 'NONE',  ( 1.002407869896990045, 0.1264236179284866091, 1.641240157426551161 ) ) ;
#37943=AXIS2_PLACEMENT_3D ( 'NONE', #20996, #2782, #46876 ) ;
#37948=CARTESIAN_POINT ( 'NONE',  ( -0.7495606340400177148, -0.1264236179284866091, 0.6815944881352126172 ) ) ;
#37950=CARTESIAN_POINT ( 'NONE',  ( -1.033464566929133799, 1.928577636452524610E-17, 2.869337061179095023E-17 ) ) ;
#37952=CARTESIAN_POINT ( 'NONE',  ( -0.8759842519685039353, 0.000000000000000000, 0.000000000000000000 ) ) ;
#37953=CARTESIAN_POINT ( 'NONE',  ( -0.8759842519685039353, 0.000000000000000000, 0.000000000000000000 ) ) ;
#37954=CARTESIAN_POINT ( 'NONE',  ( 1.002407869896990045, 0.1264236179284866091, 1.567421259788755794 ) ) ;
#37955=CARTESIAN_POINT ( 'NONE',  ( 1.002407869896990045, 0.1264236179284866091, 1.798720472387181024 ) ) ;
#37957=ORIENTED_EDGE ( 'NONE', *, *, #25911, .T. ) ;
#37958=DIRECTION ( 'NONE',  ( -1.000000000000000000, 0.000000000000000000, 0.000000000000000000 ) ) ;
#37959=CARTESIAN_POINT ( 'NONE',  ( -0.7413037127160185813, 0.09138582755367204158, 1.981387379239460289 ) ) ;
#37962=CARTESIAN_POINT ( 'NONE',  ( 1.054774247047244540, 0.07405724077823318263, 0.3789370078202520253 ) ) ;
#37965=CARTESIAN_POINT ( 'NONE',  ( -0.8019270111902717657, 0.1787899950787401604, 1.294291338528912982 ) ) ;
#37966=CARTESIAN_POINT ( 'NONE',  ( 0.7185039370078746268, -0.06523048226347956391, 0.7701771652468031304 ) ) ;
#37968=LINE ( 'NONE', #33452, #32227 ) ;
#37970=CARTESIAN_POINT ( 'NONE',  ( -1.033464566929133799, 0.000000000000000000, 0.6299212597349921339 ) ) ;
#37971=CARTESIAN_POINT ( 'NONE',  ( -1.033464566929134687, 0.06523048226347956391, 0.7997047244094481755 ) ) ;
#37972=CARTESIAN_POINT ( 'NONE',  ( 0.7495606340400177148, 0.1264236179284866091, 1.690452755851748146 ) ) ;
#37977=CARTESIAN_POINT ( 'NONE',  ( -0.8759842519685039353, -0.1574803149606299191, 0.5019685038294811052 ) ) ;
#37978=CARTESIAN_POINT ( 'NONE',  ( 0.9412147342319837628, -0.1574803149606297803, 1.488681102254677535 ) ) ;
#37979=VERTEX_POINT ( 'NONE', #19864 ) ;
#37983=VERTEX_POINT ( 'NONE', #44767 ) ;
#37985=CARTESIAN_POINT ( 'NONE',  ( -0.9500414927467378812, 0.1787899950787401604, 1.254921259788757348 ) ) ;
#37993=ORIENTED_EDGE ( 'NONE', *, *, #36808, .T. ) ;
#37995=CARTESIAN_POINT ( 'NONE',  ( -0.7185039370078739607, 1.928577636452523993E-17, 1.200787401467275695 ) ) ;
#37996=CARTESIAN_POINT ( 'NONE',  ( 0.7185039370078739607, 0.000000000000000000, 4.498031496062992574 ) ) ;
#37998=EDGE_CURVE ( 'NONE', #33230, #3623, #7888, .T. ) ;
#37999=CARTESIAN_POINT ( 'NONE',  ( -0.8759842519685039353, 0.1787899950787401882, 0.2731299212060791515 ) ) ;
#38000=CARTESIAN_POINT ( 'NONE',  ( -0.9412147342319837628, 0.1574803149606300301, 1.040846456692913424 ) ) ;
#38002=CARTESIAN_POINT ( 'NONE',  ( 0.7185039370078739607, 1.928577636452523993E-17, 0.4232283464566928832 ) ) ;
#38003=CARTESIAN_POINT ( 'NONE',  ( 0.9500414927467378812, -0.1787899950787401604, 0.9645669290800953366 ) ) ;
#38004=CARTESIAN_POINT ( 'NONE',  ( 0.6971942568897648851, 0.07405724077823318263, 1.417322834591906444 ) ) ;
#38005=CARTESIAN_POINT ( 'NONE',  ( -1.033464566929133799, 0.000000000000000000, 0.6299212597349921339 ) ) ;
#38006=CARTESIAN_POINT ( 'NONE',  ( 0.7185039370078746268, -0.06523048226347956391, 1.606791338582677309 ) ) ;
#38007=CARTESIAN_POINT ( 'NONE',  ( 0.7230964962832268084, 0.05970772165639868373, 1.982102096445605310 ) ) ;
#38009=LINE ( 'NONE', #20025, #23618 ) ;
#38011=( BOUNDED_CURVE ( )  B_SPLINE_CURVE ( 2, ( #15419, #11823, #30989, #26446, #45553, #8439, #41234, #12773, #27409 ),
 .UNSPECIFIED., .F., .T. ) 
 B_SPLINE_CURVE_WITH_KNOTS ( ( 3, 2, 2, 2, 3 ),
 ( 0.6500000000000000222, 0.6524999999999999689, 0.6550000000000000266, 0.6574999999999999734, 0.6600000000000000311 ),
 .UNSPECIFIED. ) 
 CURVE ( )  GEOMETRIC_REPRESENTATION_ITEM ( )  RATIONAL_B_SPLINE_CURVE ( ( 1.000000000000000000, 0.9238795325112869605, 1.000000000000000000, 0.9238795325112869605, 1.000000000000000000, 0.9238795325112869605, 1.000000000000000000, 0.9238795325112869605, 1.000000000000000000 ) ) 
 REPRESENTATION_ITEM ( '' )  ) ;
#38012=CARTESIAN_POINT ( 'NONE',  ( 0.8107537697050254399, -0.1574803149606297803, 0.7849409448818904789 ) ) ;
#38013=CARTESIAN_POINT ( 'NONE',  ( 0.8019270111902716547, 0.1787899950787401604, 1.058070866087969186 ) ) ;
#38014=CARTESIAN_POINT ( 'NONE',  ( 0.9500414927467377701, 0.1787899950787401604, 1.884842519631275026 ) ) ;
#38015=CARTESIAN_POINT ( 'NONE',  ( 0.9873396505805591694, 0.1113553986120547346, 0.3592519683964098820 ) ) ;
#38018=CARTESIAN_POINT ( 'NONE',  ( 0.7185039370078739607, 1.928577636452523993E-17, 1.879921259842519676 ) ) ;
#38020=CARTESIAN_POINT ( 'NONE',  ( -0.7646288533564489232, -0.1113553986120547346, 0.2214566928058590567 ) ) ;
#38022=CARTESIAN_POINT ( 'NONE',  ( 1.054774247047244540, 0.07405724077823318263, 1.166338582623402509 ) ) ;
#38026=FACE_OUTER_BOUND ( 'NONE', #37350, .T. ) ;
#38027=CARTESIAN_POINT ( 'NONE',  ( -0.8019270111902717657, 0.1787899950787401604, 0.5856299212060785964 ) ) ;
#38028=CARTESIAN_POINT ( 'NONE',  ( -0.9873396505805591694, -0.1113553986120547346, 0.2805118110236220486 ) ) ;
#38032=CARTESIAN_POINT ( 'NONE',  ( -0.7495606340400177148, -0.1264236179284866091, 1.818405511757259729 ) ) ;
#38034=CARTESIAN_POINT ( 'NONE',  ( -0.9500414927467377701, 0.1787899950787401604, 1.013779527505291878 ) ) ;
#38035=CARTESIAN_POINT ( 'NONE',  ( -1.054774247047244540, 0.07405724077823318263, 0.5807086613635594752 ) ) ;
#38036=( BOUNDED_CURVE ( )  B_SPLINE_CURVE ( 2, ( #4261, #15095, #8113, #29741, #26827 ),
 .UNSPECIFIED., .F., .T. ) 
 B_SPLINE_CURVE_WITH_KNOTS ( ( 3, 2, 3 ),
 ( 0.01499999999999999944, 0.01750000000000000167, 0.02000000000000000042 ),
 .UNSPECIFIED. ) 
 CURVE ( )  GEOMETRIC_REPRESENTATION_ITEM ( )  RATIONAL_B_SPLINE_CURVE ( ( 1.000000000000000000, 0.9238795325112869605, 1.000000000000000000, 0.9238795325112869605, 1.000000000000000000 ) ) 
 REPRESENTATION_ITEM ( '' )  ) ;
#38037=EDGE_CURVE ( 'NONE', #6061, #31524, #27704, .T. ) ;
#38044=CARTESIAN_POINT ( 'NONE',  ( -1.033464566929133799, 0.000000000000000000, 0.5216535433070865757 ) ) ;
#38045=CARTESIAN_POINT ( 'NONE',  ( -1.054774247047244096, 0.000000000000000000, 0.4552165353793071745 ) ) ;
#38046=CARTESIAN_POINT ( 'NONE',  ( -1.033464566929133799, 1.928577636452524610E-17, 2.869337061179095023E-17 ) ) ;
#38049=CARTESIAN_POINT ( 'NONE',  ( -1.002407869896990045, 0.1264236179284866091, 1.528051181048598384 ) ) ;
#38056=CARTESIAN_POINT ( 'NONE',  ( 1.033464566929133799, 0.000000000000000000, 0.4429133858267716439 ) ) ;
#38058=CARTESIAN_POINT ( 'NONE',  ( -1.033464566929134687, 0.06523048226347956391, 1.262303149498772425 ) ) ;
#38059=CARTESIAN_POINT ( 'NONE',  ( 1.054774247047244540, -0.07405724077823318263, 0.5757874015210394658 ) ) ;
#38065=CARTESIAN_POINT ( 'NONE',  ( -1.054774247047244540, 0.07405724077823318263, 1.092519684985606032 ) ) ;
#38066=CARTESIAN_POINT ( 'NONE',  ( 1.033464566929134687, -0.06523048226347956391, 1.031003937007875182 ) ) ;
#38068=LINE ( 'NONE', #34029, #601 ) ;
#38070=CYLINDRICAL_SURFACE ( 'NONE', #16166, 0.1574803149606299191 ) ;
#38072=CARTESIAN_POINT ( 'NONE',  ( 0.9412147342319837628, 0.1574803149606300301, 1.267224409341291436 ) ) ;
#38075=VERTEX_POINT ( 'NONE', #37123 ) ;
#38078=CARTESIAN_POINT ( 'NONE',  ( 0.9500414927467378812, -0.1787899950787401604, 0.7234251967966300878 ) ) ;
#38085=CARTESIAN_POINT ( 'NONE',  ( 0.8107537697050253289, 0.1574803149606300301, 1.193405511703496957 ) ) ;
#38086=CARTESIAN_POINT ( 'NONE',  ( 0.7185039370078739607, 1.928577636452523993E-17, 0.7283464565853858819 ) ) ;
#38089=CARTESIAN_POINT ( 'NONE',  ( -0.8019270111902717657, -0.1787899950787401604, 1.747047244040724312 ) ) ;
#38090=CARTESIAN_POINT ( 'NONE',  ( 0.7495606340400177148, -0.1264236179284866091, 1.902066929080094448 ) ) ;
#38092=CARTESIAN_POINT ( 'NONE',  ( 0.6971942568897626646, 0.07405724077823318263, 0.4379921259304882519 ) ) ;
#38093=CARTESIAN_POINT ( 'NONE',  ( -0.6971942568897648851, 0.07405724077823318263, 1.456692913332062744 ) ) ;
#38094=LINE ( 'NONE', #27581, #32047 ) ;
#38097=CARTESIAN_POINT ( 'NONE',  ( -0.8759842519685039353, 0.1787899950787401882, 0.03690944876513417572 ) ) ;
#38099=LINE ( 'NONE', #5261, #13794 ) ;
#38100=CARTESIAN_POINT ( 'NONE',  ( -1.054774247047244096, 0.000000000000000000, 1.680610236166708793 ) ) ;
#38101=CARTESIAN_POINT ( 'NONE',  ( -1.002407869896990045, 0.1264236179284866091, 0.03198818892261445085 ) ) ;
#38102=CARTESIAN_POINT ( 'NONE',  ( -0.8759842519685039353, -0.1574803149606299191, 1.732283464566929165 ) ) ;
#38104=CARTESIAN_POINT ( 'NONE',  ( 0.8019270111902716547, -0.1787899950787401604, 1.668307086560410157 ) ) ;
#38106=CARTESIAN_POINT ( 'NONE',  ( -0.7185039370078739607, 1.928577636452523993E-17, 1.722440944881889813 ) ) ;
#38108=CARTESIAN_POINT ( 'NONE',  ( 0.8107537697050254399, 0.1574803149606300301, 0.2878937006798746312 ) ) ;
#38109=EDGE_CURVE ( 'NONE', #12102, #2430, #23033, .T. ) ;
#38112=VERTEX_POINT ( 'NONE', #2119 ) ;
#38119=CARTESIAN_POINT ( 'NONE',  ( 0.7495606340400177148, -0.1264236179284866091, 1.857775590497417362 ) ) ;
#38121=CARTESIAN_POINT ( 'NONE',  ( -0.9412147342319837628, -0.1574803149606297803, 0.8193897636719996713 ) ) ;
#38123=CARTESIAN_POINT ( 'NONE',  ( 0.8019270111902717657, 0.1787899950787401604, 0.9005905511273389896 ) ) ;
#38125=CARTESIAN_POINT ( 'NONE',  ( -1.054774247047244540, -0.07405724077823318263, 1.993110236166711013 ) ) ;
#38127=CYLINDRICAL_SURFACE ( 'NONE', #21584, 0.1574803149606299191 ) ;
#38128=CARTESIAN_POINT ( 'NONE',  ( 0.8019270111902717657, -0.1787899950787401604, 1.983267716481667886 ) ) ;
#38133=CARTESIAN_POINT ( 'NONE',  ( -0.7495606340400177148, -0.1264236179284866091, 1.779035433017102319 ) ) ;
#38134=ORIENTED_EDGE ( 'NONE', *, *, #43280, .T. ) ;
#38135=CARTESIAN_POINT ( 'NONE',  ( -1.054774247047244096, 0.000000000000000000, 1.326279527505291433 ) ) ;
#38137=CARTESIAN_POINT ( 'NONE',  ( 0.8019270111902717657, 0.1787899950787401604, 1.338582677111590069 ) ) ;
#38138=CARTESIAN_POINT ( 'NONE',  ( -0.7495606340400177148, 0.1264236179284866091, 1.257381889710015743 ) ) ;
#38140=CARTESIAN_POINT ( 'NONE',  ( 1.033464566929133799, 0.000000000000000000, 1.190944881889763884 ) ) ;
#38141=CARTESIAN_POINT ( 'NONE',  ( 1.054774247047244540, -0.07405724077823318263, 0.6151574802611973203 ) ) ;
#38142=CARTESIAN_POINT ( 'NONE',  ( -0.9500414927467377701, 0.1787899950787401604, 0.4625984251430869665 ) ) ;
#38144=CARTESIAN_POINT ( 'NONE',  ( -0.7185039370078739607, 1.928577636452523993E-17, 1.604330708661417360 ) ) ;
#38147=CARTESIAN_POINT ( 'NONE',  ( -0.8107537697050234415, -0.1574803149606297803, 0.2731299212598424231 ) ) ;
#38148=CARTESIAN_POINT ( 'NONE',  ( -0.8759842519685039353, -0.1787899950787401882, 1.941437007820252081 ) ) ;
#38149=CARTESIAN_POINT ( 'NONE',  ( -0.8759842519685039353, 0.1574803149606299191, 0.4822834644594015674 ) ) ;
#38151=ADVANCED_FACE ( 'NONE', ( #24408 ), #41877, .T. ) ;
#38152=CARTESIAN_POINT ( 'NONE',  ( -0.7495606340400177148, 0.1264236179284866091, 0.9079724408911180600 ) ) ;
#38154=CARTESIAN_POINT ( 'NONE',  ( -1.033464566929134687, -0.06523048226347956391, 0.2042322834645668717 ) ) ;
#38155=ORIENTED_EDGE ( 'NONE', *, *, #7219, .F. ) ;
#38156=CARTESIAN_POINT ( 'NONE',  ( 0.9412147342319837628, 0.1574803149606300301, 1.001476377952755348 ) ) ;
#38158=CARTESIAN_POINT ( 'NONE',  ( -0.7185039370078739607, 1.928577636452523993E-17, 0.06889763779527559306 ) ) ;
#38161=LINE ( 'NONE', #31932, #46819 ) ;
#38163=CARTESIAN_POINT ( 'NONE',  ( 0.9412147342319837628, 0.1574803149606300301, 1.867618110236221707 ) ) ;
#38167=CARTESIAN_POINT ( 'NONE',  ( -1.002407869896990045, 0.1264236179284866091, 0.7800196849856062542 ) ) ;
#38170=LINE ( 'NONE', #30783, #219 ) ;
#38172=LINE ( 'NONE', #37231, #10310 ) ;
#38174=( BOUNDED_CURVE ( )  B_SPLINE_CURVE ( 2, ( #30630, #42067, #45193, #12415, #26789, #23651, #38028, #41346, #2071 ),
 .UNSPECIFIED., .F., .F. ) 
 B_SPLINE_CURVE_WITH_KNOTS ( ( 3, 2, 2, 2, 3 ),
 ( 0.1300000000000000044, 0.1325000000000000067, 0.1350000000000000089, 0.1375000000000000111, 0.1400000000000000133 ),
 .UNSPECIFIED. ) 
 CURVE ( )  GEOMETRIC_REPRESENTATION_ITEM ( )  RATIONAL_B_SPLINE_CURVE ( ( 1.000000000000000000, 0.9238795325112869605, 1.000000000000000000, 0.9238795325112869605, 1.000000000000000000, 0.9238795325112869605, 1.000000000000000000, 0.9238795325112869605, 1.000000000000000000 ) ) 
 REPRESENTATION_ITEM ( '' )  ) ;
#38177=CARTESIAN_POINT ( 'NONE',  ( 0.6971942568897648851, -0.07405724077823297447, 1.545275590497416696 ) ) ;
#38178=CARTESIAN_POINT ( 'NONE',  ( 0.8019270111902716547, 0.1787899950787401604, 1.845472440891119392 ) ) ;
#38179=CARTESIAN_POINT ( 'NONE',  ( 1.054774247047244540, -0.07405724077823318263, 0.4527559054580477249 ) ) ;
#38180=AXIS2_PLACEMENT_3D ( 'NONE', #16736, #21015, #35430 ) ;
#38181=CARTESIAN_POINT ( 'NONE',  ( 1.033464566929133799, 0.000000000000000000, 1.072834645669291431 ) ) ;
#38182=ORIENTED_EDGE ( 'NONE', *, *, #37890, .T. ) ;
#38186=CARTESIAN_POINT ( 'NONE',  ( 0.7185039370078739607, 1.928577636452523993E-17, 0.4921259841444416971 ) ) ;
#38187=VECTOR ( 'NONE', #7154, 39.37007874015748143 ) ;
#38188=CARTESIAN_POINT ( 'NONE',  ( 0.6971942568897637749, 2.189545951927499583E-17, 0.4749015747493858242 ) ) ;
#38189=CARTESIAN_POINT ( 'NONE',  ( 0.8759842519685039353, -0.1574803149606299191, 0.07874015748031495954 ) ) ;
#38192=CARTESIAN_POINT ( 'NONE',  ( 0.8107537697050253289, 0.1574803149606300301, 0.7603346455617647770 ) ) ;
#38194=CARTESIAN_POINT ( 'NONE',  ( -1.033464566929133799, 0.000000000000000000, 0.7874015746956221085 ) ) ;
#38196=CARTESIAN_POINT ( 'NONE',  ( 1.054774247047244540, 0.07405724077823318263, 0.9744094487651340231 ) ) ;
#38199=CARTESIAN_POINT ( 'NONE',  ( -0.7646288533564489232, 0.1113553986120547346, 0.6053149605223937524 ) ) ;
#38201=CARTESIAN_POINT ( 'NONE',  ( 0.6971942568897637749, 2.189545951927499583E-17, 1.734744094434425232 ) ) ;
#38202=CARTESIAN_POINT ( 'NONE',  ( -0.7646288533564489232, -0.1113553986120547346, 1.215551181102362266 ) ) ;
#38203=CARTESIAN_POINT ( 'NONE',  ( 0.9412147342319837628, 0.1574803149606300301, 0.5684055118110233895 ) ) ;
#38205=CARTESIAN_POINT ( 'NONE',  ( 0.7185039370078739607, 1.928577636452523993E-17, 1.958661417322834719 ) ) ;
#38206=CARTESIAN_POINT ( 'NONE',  ( 0.6971942568897637749, 2.189545951927499583E-17, 0.2042322834108035723 ) ) ;
#38207=ADVANCED_FACE ( 'NONE', ( #20800 ), #34744, .T. ) ;
#38208=CARTESIAN_POINT ( 'NONE',  ( 0.7185039370078739607, 1.928577636452523993E-17, 1.476377952648377789 ) ) ;
#38209=VERTEX_POINT ( 'NONE', #45479 ) ;
#38212=CARTESIAN_POINT ( 'NONE',  ( 1.002407869896990045, -0.1264236179284866091, 0.9670275590013542866 ) ) ;
#38213=CARTESIAN_POINT ( 'NONE',  ( -0.8019270111902716547, 0.1787899950787401604, 1.609251968450173598 ) ) ;
#38215=CARTESIAN_POINT ( 'NONE',  ( -0.6971942568897648851, 0.07405724077823318263, 1.422244094434426120 ) ) ;
#38216=ORIENTED_EDGE ( 'NONE', *, *, #17416, .F. ) ;
#38217=DIRECTION ( 'NONE',  ( -1.000000000000000000, 0.000000000000000000, 0.000000000000000000 ) ) ;
#38219=CARTESIAN_POINT ( 'NONE',  ( 1.033464566929133799, 0.000000000000000000, 1.850393700679873854 ) ) ;
#38220=CARTESIAN_POINT ( 'NONE',  ( -0.7185039370078739607, 1.928577636452523993E-17, 0.4527559054042842868 ) ) ;
#38222=VERTEX_POINT ( 'NONE', #21030 ) ;
#38224=ORIENTED_EDGE ( 'NONE', *, *, #34278, .T. ) ;
#38225=ORIENTED_EDGE ( 'NONE', *, *, #9828, .F. ) ;
#38227=CONICAL_SURFACE ( 'NONE', #23691, 0.1574803149606299191, 1.047197551196598297 ) ;
#38230=CARTESIAN_POINT ( 'NONE',  ( 0.8107537697050253289, -0.1574803149606297803, 1.887303149606301078 ) ) ;
#38233=CARTESIAN_POINT ( 'NONE',  ( -0.6971942568897626646, -0.07405724077823297447, 0.2066929133320631329 ) ) ;
#38234=CARTESIAN_POINT ( 'NONE',  ( -0.8759842519685039353, -0.1574803149606299191, 1.023622047244094446 ) ) ;
#38237=CARTESIAN_POINT ( 'NONE',  ( 0.6971942568897637749, 2.189545951927499583E-17, 1.149114173174582643 ) ) ;
#38238=CARTESIAN_POINT ( 'NONE',  ( 0.8759842519685039353, 0.1787899950787401882, 1.449311023568283341 ) ) ;
#38239=CARTESIAN_POINT ( 'NONE',  ( 1.002407869896990045, -0.1264236179284866091, 0.1353346456155277433 ) ) ;
#38240=CARTESIAN_POINT ( 'NONE',  ( 1.033464566929133799, 0.000000000000000000, 1.505905511811023612 ) ) ;
#38241=CARTESIAN_POINT ( 'NONE',  ( 0.7902745575623760788, 0.1357881168358097967, 1.980121974491770409 ) ) ;
#38244=CARTESIAN_POINT ( 'NONE',  ( -0.8107537697050253289, 0.1574803149606300301, 1.626476377845228694 ) ) ;
#38246=CARTESIAN_POINT ( 'NONE',  ( 1.002407869896990045, 0.1264236179284866091, 0.9719488188438739629 ) ) ;
#38247=CARTESIAN_POINT ( 'NONE',  ( 1.054774247047244540, 0.07405724077823318263, 1.801181102308441861 ) ) ;
#38248=CARTESIAN_POINT ( 'NONE',  ( 0.7185039370078739607, 1.928577636452523993E-17, 0.3740157479239689664 ) ) ;
#38250=EDGE_CURVE ( 'NONE', #31524, #47261, #39255, .T. ) ;
#38252=LINE ( 'NONE', #37539, #12212 ) ;
#38254=CARTESIAN_POINT ( 'NONE',  ( -1.033464566929133799, 0.000000000000000000, 0.2755905510735752184 ) ) ;
#38255=CARTESIAN_POINT ( 'NONE',  ( 1.054774247047244540, -0.07405724077823318263, 1.358267716481669662 ) ) ;
#38256=CYLINDRICAL_SURFACE ( 'NONE', #25703, 0.1574803149606300579 ) ;
#38257=ADVANCED_FACE ( 'NONE', ( #10025 ), #24645, .T. ) ;
#38259=CARTESIAN_POINT ( 'NONE',  ( -0.9412147342319837628, -0.1574803149606297803, 1.016240157372787722 ) ) ;
#38261=CARTESIAN_POINT ( 'NONE',  ( -0.8759842519685039353, 0.1787899950787401882, 0.6225393700249762796 ) ) ;
#38266=CARTESIAN_POINT ( 'NONE',  ( -1.054774247047244540, 0.07405724077823318263, 1.053149606245450176 ) ) ;
#38267=CARTESIAN_POINT ( 'NONE',  ( -0.7495606340400177148, 0.1264236179284866091, 1.847933070812378009 ) ) ;
#38268=VERTEX_POINT ( 'NONE', #32800 ) ;
#38269=CARTESIAN_POINT ( 'NONE',  ( -0.9500414927467378812, -0.1787899950787401604, 0.7283464566391493200 ) ) ;
#38271=EDGE_CURVE ( 'NONE', #11128, #36578, #37937, .T. ) ;
#38276=ORIENTED_EDGE ( 'NONE', *, *, #37918, .T. ) ;
#38278=CARTESIAN_POINT ( 'NONE',  ( -0.8759842519685039353, 0.1787899950787401882, 0.5044291338045039375 ) ) ;
#38288=CARTESIAN_POINT ( 'NONE',  ( 0.7185039370078739607, 1.928577636452523993E-17, 0.9744094488188976833 ) ) ;
#38289=CARTESIAN_POINT ( 'NONE',  ( 0.8107537697050253289, -0.1574803149606297803, 0.5880905511811019837 ) ) ;
#38290=FACE_OUTER_BOUND ( 'NONE', #4788, .T. ) ;
#38291=CARTESIAN_POINT ( 'NONE',  ( -0.7646288533564489232, 0.1113553986120547346, 1.195866141624756018 ) ) ;
#38292=CARTESIAN_POINT ( 'NONE',  ( 1.054774247047244540, 0.07405724077823318263, 0.6594488188438737408 ) ) ;
#38293=CARTESIAN_POINT ( 'NONE',  ( 0.6971942568897626646, -0.07405724077823297447, 0.08366141726907130871 ) ) ;
#38295=CARTESIAN_POINT ( 'NONE',  ( 1.033464566929133799, 0.000000000000000000, 1.929133858160188897 ) ) ;
#38297=ORIENTED_EDGE ( 'NONE', *, *, #40601, .T. ) ;
#38300=CARTESIAN_POINT ( 'NONE',  ( 0.7185039370078746268, -0.06523048226347956391, 1.134350393700787052 ) ) ;
#38302=CARTESIAN_POINT ( 'NONE',  ( -0.7185039370078741827, 0.06523048226347841205, 0.7258858266641272650 ) ) ;
#38308=CARTESIAN_POINT ( 'NONE',  ( 0.9412147342319837628, -0.1574803149606297803, 0.2780511811023620439 ) ) ;
#38309=CARTESIAN_POINT ( 'NONE',  ( 1.054774247047244540, -0.07405724077823318263, 0.8464566928596233275 ) ) ;
#38315=( BOUNDED_CURVE ( )  B_SPLINE_CURVE ( 2, ( #10771, #17459, #36162, #3067, #3316, #17697, #32345, #26329, #33521 ),
 .UNSPECIFIED., .F., .F. ) 
 B_SPLINE_CURVE_WITH_KNOTS ( ( 3, 2, 2, 2, 3 ),
 ( 0.3300000000000000155, 0.3325000000000000178, 0.3350000000000000200, 0.3375000000000000222, 0.3400000000000000244 ),
 .UNSPECIFIED. ) 
 CURVE ( )  GEOMETRIC_REPRESENTATION_ITEM ( )  RATIONAL_B_SPLINE_CURVE ( ( 1.000000000000000000, 0.9238795325112869605, 1.000000000000000000, 0.9238795325112869605, 1.000000000000000000, 0.9238795325112869605, 1.000000000000000000, 0.9238795325112869605, 1.000000000000000000 ) ) 
 REPRESENTATION_ITEM ( '' )  ) ;
#38316=CARTESIAN_POINT ( 'NONE',  ( 0.7185039370078766252, -0.06523048226348168721, 1.163877952648377567 ) ) ;
#38317=VECTOR ( 'NONE', #4751, 39.37007874015748143 ) ;
#38318=VERTEX_POINT ( 'NONE', #14340 ) ;
#38319=ORIENTED_EDGE ( 'NONE', *, *, #31296, .T. ) ;
#38320=CARTESIAN_POINT ( 'NONE',  ( -0.6971942568897637749, 2.189545951927499583E-17, 1.857775590497417362 ) ) ;
#38321=CARTESIAN_POINT ( 'NONE',  ( 0.6971942568897648851, -0.07405724077823297447, 1.820866141678520789 ) ) ;
#38322=ORIENTED_EDGE ( 'NONE', *, *, #46408, .F. ) ;
#38323=CARTESIAN_POINT ( 'NONE',  ( 0.8759842519685039353, -0.1574803149606299191, 0.5511811023622047445 ) ) ;
#38324=CARTESIAN_POINT ( 'NONE',  ( 1.002407869896990045, -0.1264236179284866091, 0.4945866141194645849 ) ) ;
#38326=CARTESIAN_POINT ( 'NONE',  ( -0.6971942568897648851, -0.07405724077823297447, 1.343503936954111744 ) ) ;
#38329=DIRECTION ( 'NONE',  ( 0.000000000000000000, 1.000000000000000000, 0.000000000000000000 ) ) ;
#38330=CARTESIAN_POINT ( 'NONE',  ( -0.6971942568897637749, 2.189545951927499583E-17, 1.818405511757259729 ) ) ;
#38331=CARTESIAN_POINT ( 'NONE',  ( -1.054774247047244096, 0.000000000000000000, 0.06643700782025216411 ) ) ;
#38332=CARTESIAN_POINT ( 'NONE',  ( -0.9412147342319837628, 0.1574803149606300301, 1.710137795275592065 ) ) ;
#38333=FACE_OUTER_BOUND ( 'NONE', #26664, .T. ) ;
#38334=CARTESIAN_POINT ( 'NONE',  ( 1.054774247047244540, 0.07405724077823318263, 1.683070866087970074 ) ) ;
#38337=CARTESIAN_POINT ( 'NONE',  ( -0.7185039370078739607, 1.928577636452523993E-17, 1.801181102362204633 ) ) ;
#38342=AXIS2_PLACEMENT_3D ( 'NONE', #41151, #15812, #12208 ) ;
#38346=CARTESIAN_POINT ( 'NONE',  ( -1.033464566929133799, 0.000000000000000000, 0.7480314959554645871 ) ) ;
#38351=CARTESIAN_POINT ( 'NONE',  ( 1.054774247047244540, -0.07405724077823318263, 0.9251968503399374821 ) ) ;
#38353=EDGE_CURVE ( 'NONE', #24091, #26106, #5808, .T. ) ;
#38356=CARTESIAN_POINT ( 'NONE',  ( 0.7185039370078746268, -0.06523048226347956391, 0.06151574792396910518 ) ) ;
#38359=CARTESIAN_POINT ( 'NONE',  ( -0.7859119931880654830, 0.1562117447626044375, 0.03937007874015843040 ) ) ;
#38363=CARTESIAN_POINT ( 'NONE',  ( -1.002407869896990045, -0.1264236179284866091, 1.867618110182456714 ) ) ;
#38365=CARTESIAN_POINT ( 'NONE',  ( -0.8759842519685039353, -0.1787899950787401882, 1.395177165300567124 ) ) ;
#38366=DIRECTION ( 'NONE',  ( 1.822029033848725028E-16, 0.000000000000000000, 1.000000000000000000 ) ) ;
#38367=CARTESIAN_POINT ( 'NONE',  ( 0.7495606340400177148, -0.1264236179284866091, 1.468996062938362046 ) ) ;
#38368=CARTESIAN_POINT ( 'NONE',  ( -0.7185039370078739607, 1.928577636452523993E-17, 0.8956692913385826404 ) ) ;
#38369=CARTESIAN_POINT ( 'NONE',  ( -0.8759842519685039353, 0.1787899950787401882, 0.5093503936470236138 ) ) ;
#38370=CARTESIAN_POINT ( 'NONE',  ( 1.054774247047244540, -0.07405724077823318263, 0.1033464566391498751 ) ) ;
#38371=CARTESIAN_POINT ( 'NONE',  ( -1.002407869896990045, -0.1264236179284866091, 1.237696850339937038 ) ) ;
#38372=DIRECTION ( 'NONE',  ( 0.000000000000000000, 0.000000000000000000, -1.000000000000000000 ) ) ;
#38374=CARTESIAN_POINT ( 'NONE',  ( 0.8759842519685039353, 0.1787899950787401882, 0.6668307086076534773 ) ) ;
#38375=CARTESIAN_POINT ( 'NONE',  ( -0.6971942568897648851, -0.07405724077823297447, 0.5954724408911187261 ) ) ;
#38378=ORIENTED_EDGE ( 'NONE', *, *, #21177, .T. ) ;
#38380=CARTESIAN_POINT ( 'NONE',  ( -0.9412147342319837628, 0.1574803149606300301, 0.3715551181102361711 ) ) ;
#38381=CARTESIAN_POINT ( 'NONE',  ( 1.054774247047244096, 0.000000000000000000, 1.168799212544661348 ) ) ;
#38383=DIRECTION ( 'NONE',  ( 1.822029033848725028E-16, 0.000000000000000000, 1.000000000000000000 ) ) ;
#38385=ORIENTED_EDGE ( 'NONE', *, *, #34010, .T. ) ;
#38387=CARTESIAN_POINT ( 'NONE',  ( -0.8759842519685039353, -0.1574803149606299191, 0.5511811023622047445 ) ) ;
#38389=CARTESIAN_POINT ( 'NONE',  ( -1.002407869896990045, -0.1264236179284866091, 0.9670275590013542866 ) ) ;
#38390=CARTESIAN_POINT ( 'NONE',  ( -1.054774247047244540, -0.07405724077823318263, 0.1377952755367876370 ) ) ;
#38397=CARTESIAN_POINT ( 'NONE',  ( 1.054774247047244540, -0.07405724077823318263, 1.358267716481669662 ) ) ;
#38402=CARTESIAN_POINT ( 'NONE',  ( 0.9500414927467378812, -0.1787899950787401604, 1.589566929080094448 ) ) ;
#38406=CARTESIAN_POINT ( 'NONE',  ( 0.8759842519685039353, 0.000000000000000000, 4.498031496062992574 ) ) ;
#38408=CARTESIAN_POINT ( 'NONE',  ( 0.8759842519685039353, 0.1787899950787401882, 0.4650590550643464716 ) ) ;
#38409=EDGE_CURVE ( 'NONE', #43867, #13799, #43790, .T. ) ;
#38411=CARTESIAN_POINT ( 'NONE',  ( -0.9500414927467377701, -0.1787899950787401604, 0.8464566928596233275 ) ) ;
#38413=DIRECTION ( 'NONE',  ( 0.000000000000000000, 0.000000000000000000, -1.000000000000000000 ) ) ;
#38415=CARTESIAN_POINT ( 'NONE',  ( -0.8475445883371663935, -0.1713140434220985220, 1.987685975326619836 ) ) ;
#38417=CARTESIAN_POINT ( 'NONE',  ( -1.033464566929133799, 0.000000000000000000, 1.023622047136567126 ) ) ;
#38418=CARTESIAN_POINT ( 'NONE',  ( 0.8019270111902717657, -0.1787899950787401604, 1.471456692859622217 ) ) ;
#38419=CARTESIAN_POINT ( 'NONE',  ( 0.6971942568897648851, 0.07405724077823318263, 1.889763779473794481 ) ) ;
#38420=CARTESIAN_POINT ( 'NONE',  ( 0.8759842519685039353, 0.1787899950787401882, 0.3863188975840318173 ) ) ;
#38421=VERTEX_POINT ( 'NONE', #36394 ) ;
#38429=CARTESIAN_POINT ( 'NONE',  ( 0.7495606340400177148, -0.1264236179284866091, 0.4798228345919055560 ) ) ;
#38430=CARTESIAN_POINT ( 'NONE',  ( 0.8019661270514706342, -0.1449744270584123751, 0.03937007223081739893 ) ) ;
#38431=CARTESIAN_POINT ( 'NONE',  ( 0.9412147342319837628, -0.1574803149606297803, 1.961122047136568014 ) ) ;
#38432=CARTESIAN_POINT ( 'NONE',  ( -1.033464566929134687, 0.06523048226347956391, 1.577263779420032153 ) ) ;
#38433=CARTESIAN_POINT ( 'NONE',  ( -0.6971942568897648851, -0.07405724077823297447, 1.422244094434426120 ) ) ;
#38434=CARTESIAN_POINT ( 'NONE',  ( 1.033464566929134687, 0.06523048226347956391, 0.8292322833570401341 ) ) ;
#38436=CARTESIAN_POINT ( 'NONE',  ( -0.7646288533564489232, 0.1113553986120547346, 0.8021653542231811373 ) ) ;
#38437=CARTESIAN_POINT ( 'NONE',  ( 1.002407869896990045, -0.1264236179284866091, 1.006397637741511808 ) ) ;
#38440=CARTESIAN_POINT ( 'NONE',  ( -0.7646288533564489232, -0.1113553986120547346, 0.5364173227271189504 ) ) ;
#38441=CARTESIAN_POINT ( 'NONE',  ( -0.8759842519685039353, -0.1574803149606299191, 1.417322834645669216 ) ) ;
#38443=CARTESIAN_POINT ( 'NONE',  ( -0.7185039370078746268, 0.06523048226347956391, 0.7357283464566919395 ) ) ;
#38445=CARTESIAN_POINT ( 'NONE',  ( 1.054774247047244096, 0.000000000000000000, 0.1845472440407248116 ) ) ;
#38446=CARTESIAN_POINT ( 'NONE',  ( 0.9873396505805591694, 0.1113553986120547346, 1.422244094380661572 ) ) ;
#38450=ORIENTED_EDGE ( 'NONE', *, *, #11231, .F. ) ;
#38451=CARTESIAN_POINT ( 'NONE',  ( -0.8759842519685039353, 0.1787899950787401882, 1.764271653489543290 ) ) ;
#38458=VERTEX_POINT ( 'NONE', #29471 ) ;
#38460=ORIENTED_EDGE ( 'NONE', *, *, #14669, .T. ) ;
#38466=CARTESIAN_POINT ( 'NONE',  ( 0.7646288533564489232, -0.1113553986120547346, 1.884842519685039353 ) ) ;
#38468=VERTEX_POINT ( 'NONE', #28499 ) ;
#38470=CARTESIAN_POINT ( 'NONE',  ( -0.6971942568897648851, -0.07405724077823297447, 0.4035433070328507954 ) ) ;
#38471=CARTESIAN_POINT ( 'NONE',  ( -0.8759842519685039353, -0.1574803149606299191, 1.062992125984252079 ) ) ;
#38473=CARTESIAN_POINT ( 'NONE',  ( -0.7646288533564489232, 0.1113553986120547346, 0.2214566929133858220 ) ) ;
#38474=CARTESIAN_POINT ( 'NONE',  ( 0.6971942568897626646, 0.07405724077823318263, 0.2362204723871814682 ) ) ;
#38475=CARTESIAN_POINT ( 'NONE',  ( -0.9412147342319837628, 0.1574803149606300301, 0.6373031494987716483 ) ) ;
#38477=CARTESIAN_POINT ( 'NONE',  ( 0.7646288533564489232, -0.1113553986120547346, 1.530511811023621993 ) ) ;
#38478=CARTESIAN_POINT ( 'NONE',  ( 0.7932464814172374146, 0.1374651347690867276, 1.980054407178728937 ) ) ;
#38480=CARTESIAN_POINT ( 'NONE',  ( 0.7185039370078746268, -0.06523048226347956391, 0.4552165353255435698 ) ) ;
#38481=CARTESIAN_POINT ( 'NONE',  ( -0.8759842519685039353, -0.1574803149606299191, 1.643700787294047228 ) ) ;
#38483=CARTESIAN_POINT ( 'NONE',  ( -1.033464566929134687, -0.06523048226347956391, 0.7062007872940467834 ) ) ;
#38484=CARTESIAN_POINT ( 'NONE',  ( 1.054774247047244540, -0.07405724077823318263, 0.9251968503399373711 ) ) ;
#38485=CARTESIAN_POINT ( 'NONE',  ( 0.9500414927467377701, 0.1787899950787401604, 1.924212598371433325 ) ) ;
#38486=CARTESIAN_POINT ( 'NONE',  ( 0.8759842519685039353, -0.1574803149606299191, 0.2657480313885358103 ) ) ;
#38488=CARTESIAN_POINT ( 'NONE',  ( 0.9412147342319837628, -0.1574803149606297803, 1.252460629813731519 ) ) ;
#38489=CARTESIAN_POINT ( 'NONE',  ( 0.9873396505805591694, -0.1113553986120547346, 0.2411417322834645827 ) ) ;
#38493=CARTESIAN_POINT ( 'NONE',  ( -1.033464566929134687, -0.06523048226347956391, 0.2731299211523157133 ) ) ;
#38494=CARTESIAN_POINT ( 'NONE',  ( 1.054774247047244540, -0.07405724077823318263, 1.318897637741511364 ) ) ;
#38496=CARTESIAN_POINT ( 'NONE',  ( -0.7185039370078739607, 1.928577636452523993E-17, 1.879921259842519676 ) ) ;
#38497=CARTESIAN_POINT ( 'NONE',  ( -0.9500414927467378812, -0.1787899950787401604, 0.6446850393163160442 ) ) ;
#38504=CARTESIAN_POINT ( 'NONE',  ( -0.6971942568897648851, -0.07405724077823297447, 1.033464566875371027 ) ) ;
#38505=CARTESIAN_POINT ( 'NONE',  ( -1.002407869896990045, -0.1264236179284866091, 1.906988188922614125 ) ) ;
#38507=CARTESIAN_POINT ( 'NONE',  ( -1.054774247047244096, 0.000000000000000000, 0.6569881889226141247 ) ) ;
#38508=EDGE_CURVE ( 'NONE', #461, #30681, #25832, .T. ) ;
#38509=ORIENTED_EDGE ( 'NONE', *, *, #26647, .F. ) ;
#38511=CARTESIAN_POINT ( 'NONE',  ( -0.9412147342319837628, 0.1574803149606300301, 1.670767716535433545 ) ) ;
#38514=VERTEX_POINT ( 'NONE', #14570 ) ;
#38517=CARTESIAN_POINT ( 'NONE',  ( -0.7495606340400177148, 0.1264236179284866091, 0.4699803149068661479 ) ) ;
#38521=EDGE_CURVE ( 'NONE', #2430, #8074, #6502, .T. ) ;
#38522=CARTESIAN_POINT ( 'NONE',  ( -0.8019270111902716547, -0.1787899950787401604, 1.589566929080094226 ) ) ;
#38523=CARTESIAN_POINT ( 'NONE',  ( 1.054774247047244096, 0.000000000000000000, 0.3026574802611972648 ) ) ;
#38528=CARTESIAN_POINT ( 'NONE',  ( -0.7185039370078739607, 1.928577636452523993E-17, 0.1771653542231816925 ) ) ;
#38530=CARTESIAN_POINT ( 'NONE',  ( 1.033464566929133799, 0.000000000000000000, 0.9547244094488189781 ) ) ;
#38531=CARTESIAN_POINT ( 'NONE',  ( -0.7185039370078739607, 1.928577636452523993E-17, 1.161417322727118284 ) ) ;
#38532=CARTESIAN_POINT ( 'NONE',  ( 0.8759842519685039353, 0.1787899950787401882, 0.6274606298674959559 ) ) ;
#38534=CARTESIAN_POINT ( 'NONE',  ( -0.7646288533564489232, 0.1113553986120547346, 0.6840551180027086842 ) ) ;
#38537=CARTESIAN_POINT ( 'NONE',  ( -1.033464566929133799, 0.000000000000000000, 0.7874015746956221085 ) ) ;
#38539=CARTESIAN_POINT ( 'NONE',  ( -1.054774247047244540, 0.07405724077823318263, 1.131889763725763887 ) ) ;
#38540=CARTESIAN_POINT ( 'NONE',  ( 0.8759842519685039353, -0.1574803149606299191, 1.062992125984252079 ) ) ;
#38542=CARTESIAN_POINT ( 'NONE',  ( -0.9129482065544513025, -0.1717787576874445776, 1.988841906250625291 ) ) ;
#38543=FACE_OUTER_BOUND ( 'NONE', #6680, .T. ) ;
#38545=CARTESIAN_POINT ( 'NONE',  ( 1.033464566929133799, 0.000000000000000000, 1.299212598317669221 ) ) ;
#38547=CARTESIAN_POINT ( 'NONE',  ( 0.8107537697050254399, 0.1574803149606300301, 1.272145669183810668 ) ) ;
#38552=CARTESIAN_POINT ( 'NONE',  ( 1.033464566929134687, -0.06523048226347956391, 0.8735236220472449853 ) ) ;
#38553=CARTESIAN_POINT ( 'NONE',  ( 1.002407869896990045, 0.1264236179284866091, 0.8144685038832440993 ) ) ;
#38555=CARTESIAN_POINT ( 'NONE',  ( 0.7646288533564489232, -0.1113553986120547346, 1.451771653543306950 ) ) ;
#38560=CARTESIAN_POINT ( 'NONE',  ( 0.7646288533564489232, -0.1113553986120547346, 1.205708661309795371 ) ) ;
#38564=CARTESIAN_POINT ( 'NONE',  ( -0.8019270111902717657, 0.1787899950787401604, 1.850393700733638624 ) ) ;
#38565=CARTESIAN_POINT ( 'NONE',  ( 1.054774247047244540, 0.07405724077823318263, 1.840551181048599938 ) ) ;
#38569=CARTESIAN_POINT ( 'NONE',  ( -1.054774247047244540, -0.07405724077823318263, 1.515748031442299526 ) ) ;
#38570=CARTESIAN_POINT ( 'NONE',  ( -0.6971942568897637749, 2.189545951927499583E-17, 0.2042322834108035723 ) ) ;
#38572=CARTESIAN_POINT ( 'NONE',  ( -0.9500414927467378812, 0.1787899950787401604, 1.687992125930489307 ) ) ;
#38573=CARTESIAN_POINT ( 'NONE',  ( -0.9873396505805591694, -0.1113553986120547346, 1.815944881889763884 ) ) ;
#38576=CARTESIAN_POINT ( 'NONE',  ( 1.002407869896990045, 0.1264236179284866091, 1.724901574749385880 ) ) ;
#38579=( BOUNDED_CURVE ( )  B_SPLINE_CURVE ( 2, ( #17540, #28601, #15090, #35995, #3154, #47005, #25866, #40448, #29737 ),
 .UNSPECIFIED., .F., .T. ) 
 B_SPLINE_CURVE_WITH_KNOTS ( ( 3, 2, 2, 2, 3 ),
 ( 0.8499999999999999778, 0.8525000000000000355, 0.8549999999999999822, 0.8575000000000000400, 0.8599999999999999867 ),
 .UNSPECIFIED. ) 
 CURVE ( )  GEOMETRIC_REPRESENTATION_ITEM ( )  RATIONAL_B_SPLINE_CURVE ( ( 1.000000000000000000, 0.9238795325112869605, 1.000000000000000000, 0.9238795325112869605, 1.000000000000000000, 0.9238795325112869605, 1.000000000000000000, 0.9238795325112869605, 1.000000000000000000 ) ) 
 REPRESENTATION_ITEM ( '' )  ) ;
#38582=CARTESIAN_POINT ( 'NONE',  ( -1.002407869896990045, 0.1264236179284866091, 1.291830708607653477 ) ) ;
#38585=CARTESIAN_POINT ( 'NONE',  ( -1.033464566929133799, 0.000000000000000000, 0.6003937007874016185 ) ) ;
#38588=CARTESIAN_POINT ( 'NONE',  ( -0.7646288533564489232, -0.1113553986120547346, 0.8120078739082204899 ) ) ;
#38589=CARTESIAN_POINT ( 'NONE',  ( -1.033464566929134687, -0.06523048226347956391, 0.7947834645669291653 ) ) ;
#38591=EDGE_CURVE ( 'NONE', #18156, #38980, #37070, .T. ) ;
#38592=CARTESIAN_POINT ( 'NONE',  ( 1.002407869896990045, -0.1264236179284866091, 0.8833661416785196785 ) ) ;
#38594=CARTESIAN_POINT ( 'NONE',  ( 0.7646288533564489232, 0.1113553986120547346, 0.09350393690034704275 ) ) ;
#38601=CARTESIAN_POINT ( 'NONE',  ( -0.8759842519685039353, -0.1787899950787401882, 1.862696850339937038 ) ) ;
#38603=CARTESIAN_POINT ( 'NONE',  ( -0.7495606340400177148, -0.1264236179284866091, 1.508366141678519678 ) ) ;
#38604=CARTESIAN_POINT ( 'NONE',  ( 1.002407869896990045, 0.1264236179284866091, 1.370570866087968520 ) ) ;
#38607=CARTESIAN_POINT ( 'NONE',  ( -1.054774247047244096, 0.000000000000000000, 0.6963582676627716461 ) ) ;
#38608=CARTESIAN_POINT ( 'NONE',  ( 0.6971942568897637749, 2.189545951927499583E-17, 0.1254921259304885850 ) ) ;
#38609=CARTESIAN_POINT ( 'NONE',  ( -1.054774247047244540, -0.07405724077823318263, 1.279527559001355286 ) ) ;
#38611=CARTESIAN_POINT ( 'NONE',  ( 1.054774247047244096, 0.000000000000000000, 0.6569881889226141247 ) ) ;
#38612=CARTESIAN_POINT ( 'NONE',  ( -0.7495606340400177148, 0.1264236179284866091, 0.5487204723871811352 ) ) ;
#38614=CARTESIAN_POINT ( 'NONE',  ( 1.033464566929133355, 0.06523048226348168721, 1.656003936900346973 ) ) ;
#38616=ORIENTED_EDGE ( 'NONE', *, *, #2630, .F. ) ;
#38618=CARTESIAN_POINT ( 'NONE',  ( -0.7185039370078746268, -0.06523048226347956391, 0.2288385826771656140 ) ) ;
#38619=CARTESIAN_POINT ( 'NONE',  ( 0.8019270111902716547, -0.1787899950787401604, 1.274606299158834277 ) ) ;
#38621=CARTESIAN_POINT ( 'NONE',  ( -0.9412147342319837628, -0.1574803149606297803, 1.843011810916095783 ) ) ;
#38623=AXIS2_PLACEMENT_3D ( 'NONE', #22853, #4617, #19251 ) ;
#38626=CARTESIAN_POINT ( 'NONE',  ( -1.002407869896990045, 0.1264236179284866091, 1.016240157426551161 ) ) ;
#38633=CARTESIAN_POINT ( 'NONE',  ( -0.9412147342319837628, -0.1574803149606297803, 0.08120078740157483932 ) ) ;
#38634=VERTEX_POINT ( 'NONE', #8544 ) ;
#38635=CARTESIAN_POINT ( 'NONE',  ( 0.8759842519685039353, -0.1787899950787401882, 1.468996062938362046 ) ) ;
#38641=CARTESIAN_POINT ( 'NONE',  ( 1.033464566929133799, 0.000000000000000000, 1.811023621939716444 ) ) ;
#38642=CARTESIAN_POINT ( 'NONE',  ( 1.054774247047244540, -0.07405724077823318263, 1.594488188922613237 ) ) ;
#38646=CARTESIAN_POINT ( 'NONE',  ( 0.6971942568897637749, 2.189545951927499583E-17, 0.4749015747493858242 ) ) ;
#38647=CARTESIAN_POINT ( 'NONE',  ( -0.7495606340400177148, -0.1264236179284866091, 0.8390748030958424808 ) ) ;
#38649=CARTESIAN_POINT ( 'NONE',  ( 0.7646288533564489232, 0.1113553986120547346, 0.09350393690034704275 ) ) ;
#38651=CARTESIAN_POINT ( 'NONE',  ( -0.7299953799755746209, -0.08597721908260566592, 1.984947195527895225 ) ) ;
#38652=VECTOR ( 'NONE', #12896, 39.37007874015748143 ) ;
#38655=CARTESIAN_POINT ( 'NONE',  ( -0.7646288533564489232, 0.1113553986120547346, 1.038385826664126155 ) ) ;
#38656=CARTESIAN_POINT ( 'NONE',  ( 0.9500414927467378812, -0.1787899950787401604, 1.515748031442299526 ) ) ;
#38658=CARTESIAN_POINT ( 'NONE',  ( 0.8019270111902716547, -0.1787899950787401604, 0.3641732282926931630 ) ) ;
#38662=ORIENTED_EDGE ( 'NONE', *, *, #31937, .T. ) ;
#38663=CARTESIAN_POINT ( 'NONE',  ( -0.8759842519685039353, 0.000000000000000000, 0.000000000000000000 ) ) ;
#38668=CARTESIAN_POINT ( 'NONE',  ( 1.002407869896990045, -0.1264236179284866091, 0.3715551180564728440 ) ) ;
#38670=CARTESIAN_POINT ( 'NONE',  ( 0.8484761801896820721, -0.1575117747672026836, 0.03936098705002191028 ) ) ;
#38671=CARTESIAN_POINT ( 'NONE',  ( 1.054774247047244540, 0.07405724077823318263, 1.323818897584032594 ) ) ;
#38673=CARTESIAN_POINT ( 'NONE',  ( -0.7495606340400177148, 0.1264236179284866091, 1.414862204670645829 ) ) ;
#38674=CARTESIAN_POINT ( 'NONE',  ( 0.8759842519685039353, 0.1574803149606299191, 0.7972440943806614611 ) ) ;
#38677=CARTESIAN_POINT ( 'NONE',  ( 0.8759842519685039353, -0.1787899950787401882, 1.080216535379306952 ) ) ;
#38678=ORIENTED_EDGE ( 'NONE', *, *, #8615, .F. ) ;
#38680=ORIENTED_EDGE ( 'NONE', *, *, #40868, .T. ) ;
#38681=CARTESIAN_POINT ( 'NONE',  ( -0.9873396505805591694, -0.1113553986120547346, 0.5462598424121581919 ) ) ;
#38683=CARTESIAN_POINT ( 'NONE',  ( 0.6971942568897637749, 2.189545951927499583E-17, 1.695374015694267822 ) ) ;
#38684=CARTESIAN_POINT ( 'NONE',  ( -1.033464566929134687, -0.06523048226347956391, 1.385334645669290987 ) ) ;
#38685=CARTESIAN_POINT ( 'NONE',  ( 1.033464566929133799, 0.000000000000000000, 1.811023621939716444 ) ) ;
#38687=CARTESIAN_POINT ( 'NONE',  ( 0.8759842519685039353, -0.1787899950787401882, 0.1747047243556852092 ) ) ;
#38688=CARTESIAN_POINT ( 'NONE',  ( -0.8759842519685039353, -0.1787899950787401882, 0.1304133857730082613 ) ) ;
#38689=CARTESIAN_POINT ( 'NONE',  ( 1.033464566929134687, 0.06523048226347956391, 1.419783464459402289 ) ) ;
#38693=LINE ( 'NONE', #17346, #43551 ) ;
#38694=CARTESIAN_POINT ( 'NONE',  ( -1.002407869896990045, 0.1264236179284866091, 1.759350393647023614 ) ) ;
#38696=EDGE_CURVE ( 'NONE', #45388, #5152, #19083, .T. ) ;
#38705=ADVANCED_FACE ( 'NONE', ( #15525 ), #44950, .T. ) ;
#38706=CARTESIAN_POINT ( 'NONE',  ( 1.033464566929133799, 1.928577636452524610E-17, 4.498031496062992574 ) ) ;
#38708=CARTESIAN_POINT ( 'NONE',  ( 1.033464566929133799, 0.000000000000000000, 1.860236220472440971 ) ) ;
#38710=( BOUNDED_CURVE ( )  B_SPLINE_CURVE ( 2, ( #15191, #26453, #40784, #32946, #36752, #43691, #40551, #36525, #41018 ),
 .UNSPECIFIED., .F., .T. ) 
 B_SPLINE_CURVE_WITH_KNOTS ( ( 3, 2, 2, 2, 3 ),
 ( 0.8399999999999999689, 0.8425000000000000266, 0.8449999999999999734, 0.8475000000000000311, 0.8499999999999999778 ),
 .UNSPECIFIED. ) 
 CURVE ( )  GEOMETRIC_REPRESENTATION_ITEM ( )  RATIONAL_B_SPLINE_CURVE ( ( 1.000000000000000000, 0.9238795325112869605, 1.000000000000000000, 0.9238795325112869605, 1.000000000000000000, 0.9238795325112869605, 1.000000000000000000, 0.9238795325112799661, 1.000000000000000000 ) ) 
 REPRESENTATION_ITEM ( '' )  ) ;
#38711=CARTESIAN_POINT ( 'NONE',  ( -0.8019270111902716547, -0.1787899950787401604, 0.3297244093950555954 ) ) ;
#38712=CARTESIAN_POINT ( 'NONE',  ( -0.7185039370078746268, 0.06523048226347956391, 1.011318897637796033 ) ) ;
#38715=CARTESIAN_POINT ( 'NONE',  ( 0.7495606340400177148, 0.1264236179284866091, 1.144192913332062966 ) ) ;
#38716=CARTESIAN_POINT ( 'NONE',  ( 1.002407869896990045, -0.1264236179284866091, 1.513287401521039355 ) ) ;
#38718=CARTESIAN_POINT ( 'NONE',  ( 0.7185039370078746268, 0.06523048226347956391, 1.562500000000000000 ) ) ;
#38720=CARTESIAN_POINT ( 'NONE',  ( 0.7646288533564489232, 0.1113553986120547346, 1.717519685039369914 ) ) ;
#38723=DIRECTION ( 'NONE',  ( 1.822029033848725028E-16, 0.000000000000000000, 1.000000000000000000 ) ) ;
#38724=CARTESIAN_POINT ( 'NONE',  ( 0.6971942568897637749, 2.189545951927499583E-17, 0.9079724408911180600 ) ) ;
#38725=CARTESIAN_POINT ( 'NONE',  ( 1.002407869896990045, -0.1264236179284866091, 1.951279527505291433 ) ) ;
#38726=CARTESIAN_POINT ( 'NONE',  ( 0.9873396505805591694, 0.1113553986120547346, 0.2805118109160948947 ) ) ;
#38727=ORIENTED_EDGE ( 'NONE', *, *, #27375, .T. ) ;
#38728=LINE ( 'NONE', #12872, #42904 ) ;
#38730=CARTESIAN_POINT ( 'NONE',  ( -0.7185039370078746268, -0.06523048226347956391, 0.2189960628845991353 ) ) ;
#38732=CARTESIAN_POINT ( 'NONE',  ( 0.9500414927467378812, -0.1787899950787401604, 1.353346456639149986 ) ) ;
#38734=CARTESIAN_POINT ( 'NONE',  ( -0.8759842519685039353, 0.1574803149606299191, 0.2854330707586145710 ) ) ;
#38736=DIRECTION ( 'NONE',  ( 0.000000000000000000, 0.000000000000000000, -1.000000000000000000 ) ) ;
#38738=CARTESIAN_POINT ( 'NONE',  ( -0.7495606340400177148, -0.1264236179284866091, 0.5979330708123780092 ) ) ;
#38741=EDGE_LOOP ( 'NONE', ( #29593, #41637, #28956, #32190 ) ) ;
#38742=EDGE_LOOP ( 'NONE', ( #11980, #35945, #45435, #25137 ) ) ;
#38743=CARTESIAN_POINT ( 'NONE',  ( -1.054774247047244540, 0.07405724077823318263, 1.363188976324188673 ) ) ;
#38746=CARTESIAN_POINT ( 'NONE',  ( -0.9500414927467378812, -0.1787899950787401604, 1.003937007820251193 ) ) ;
#38747=CARTESIAN_POINT ( 'NONE',  ( -0.8019270111902717657, -0.1787899950787401604, 1.899606299158834943 ) ) ;
#38749=CARTESIAN_POINT ( 'NONE',  ( -1.054774247047244540, -0.07405724077823318263, 0.6938976377415123631 ) ) ;
#38750=EDGE_CURVE ( 'NONE', #25854, #3057, #8329, .T. ) ;
#38752=CARTESIAN_POINT ( 'NONE',  ( -0.8107537697050254399, 0.1574803149606300301, 0.09104330697908723236 ) ) ;
#38755=CARTESIAN_POINT ( 'NONE',  ( -0.7185039370078739607, 1.928577636452523993E-17, 0.6496062991050708391 ) ) ;
#38758=EDGE_CURVE ( 'NONE', #8121, #1697, #36208, .T. ) ;
#38759=CARTESIAN_POINT ( 'NONE',  ( -0.9412147342319837628, -0.1574803149606297803, 1.764271653435779852 ) ) ;
#38760=CARTESIAN_POINT ( 'NONE',  ( -0.7495606340400177148, 0.1264236179284866091, 0.6668307086076534773 ) ) ;
#38763=CARTESIAN_POINT ( 'NONE',  ( -0.9500414927467377701, 0.1787899950787401604, 1.727362204670645385 ) ) ;
#38768=CARTESIAN_POINT ( 'NONE',  ( -1.033464566929133799, 0.000000000000000000, 1.259842519577511810 ) ) ;
#38771=CARTESIAN_POINT ( 'NONE',  ( -0.8759842519685039353, 0.1574803149606299191, 0.4133858267716535861 ) ) ;
#38774=CARTESIAN_POINT ( 'NONE',  ( 0.8107537697050253289, 0.1574803149606300301, 1.124507874015748810 ) ) ;
#38779=CARTESIAN_POINT ( 'NONE',  ( 0.7185039370078746268, 0.06523048226347956391, 0.1845472440944882775 ) ) ;
#38785=VERTEX_POINT ( 'NONE', #45428 ) ;
#38787=CARTESIAN_POINT ( 'NONE',  ( 0.7495606340400177148, 0.1264236179284866091, 0.8243110235682834519 ) ) ;
#38789=CARTESIAN_POINT ( 'NONE',  ( 0.9412147342319837628, -0.1574803149606297803, 0.7012795274515276622 ) ) ;
#38793=CARTESIAN_POINT ( 'NONE',  ( 0.9873396505805591694, 0.1113553986120547346, 1.264763779420031486 ) ) ;
#38795=CARTESIAN_POINT ( 'NONE',  ( -0.8759842519685039353, -0.1787899950787401882, 1.985728346402929168 ) ) ;
#38796=CARTESIAN_POINT ( 'NONE',  ( 0.6971942568897637749, 2.189545951927499583E-17, 1.857775590497417362 ) ) ;
#38799=CARTESIAN_POINT ( 'NONE',  ( 0.9873396505805591694, -0.1113553986120547346, 0.5561023622047244208 ) ) ;
#38800=CARTESIAN_POINT ( 'NONE',  ( -0.6971942568897648851, 0.07405724077823318263, 1.496062992072220821 ) ) ;
#38801=DIRECTION ( 'NONE',  ( -1.000000000000000000, 0.000000000000000000, 0.000000000000000000 ) ) ;
#38803=CARTESIAN_POINT ( 'NONE',  ( -1.054774247047244540, 0.07405724077823318263, 0.2263779527021421711 ) ) ;
#38806=CARTESIAN_POINT ( 'NONE',  ( -0.9500414927467378812, 0.1787899950787401604, 1.963582677111591401 ) ) ;
#38808=CARTESIAN_POINT ( 'NONE',  ( -0.9412147342319837628, -0.1574803149606297803, 1.774114173228345859 ) ) ;
#38812=CARTESIAN_POINT ( 'NONE',  ( -0.7185039370078746268, 0.06523048226347956391, 0.05659448808144944970 ) ) ;
#38815=ORIENTED_EDGE ( 'NONE', *, *, #17964, .T. ) ;
#38822=CARTESIAN_POINT ( 'NONE',  ( -1.033464566929134687, 0.06523048226347956391, 0.6815944881889761664 ) ) ;
#38824=CARTESIAN_POINT ( 'NONE',  ( 0.9500414927467378812, 0.1787899950787401604, 0.8956692912848198684 ) ) ;
#38829=CARTESIAN_POINT ( 'NONE',  ( 0.9873396505805591694, -0.1113553986120547346, 0.07381889753026830980 ) ) ;
#38830=ORIENTED_EDGE ( 'NONE', *, *, #6046, .T. ) ;
#38831=CARTESIAN_POINT ( 'NONE',  ( -0.9412147342319837628, -0.1574803149606297803, 1.183562992125983593 ) ) ;
#38834=CARTESIAN_POINT ( 'NONE',  ( -0.7495606340400177148, 0.1264236179284866091, 1.966043307032850462 ) ) ;
#38836=CARTESIAN_POINT ( 'NONE',  ( -0.7495606340400177148, -0.1264236179284866091, 1.429625984198204858 ) ) ;
#38838=CARTESIAN_POINT ( 'NONE',  ( 0.7495606340400177148, -0.1264236179284866091, 1.390255905458047447 ) ) ;
#38840=CARTESIAN_POINT ( 'NONE',  ( -0.6971942568897637749, 2.189545951927499583E-17, 0.6373031495525354195 ) ) ;
#38842=CARTESIAN_POINT ( 'NONE',  ( 0.9500414927467377701, -0.1787899950787401604, 0.6496062991588353874 ) ) ;
#38843=CARTESIAN_POINT ( 'NONE',  ( -0.9500414927467377701, 0.1787899950787401604, 0.5807086613635594752 ) ) ;
#38845=( BOUNDED_CURVE ( )  B_SPLINE_CURVE ( 2, ( #20545, #10492, #13591, #46887, #24165, #10007, #28004, #13833, #3275 ),
 .UNSPECIFIED., .F., .F. ) 
 B_SPLINE_CURVE_WITH_KNOTS ( ( 3, 2, 2, 2, 3 ),
 ( 0.4799999999999999822, 0.4824999999999999845, 0.4849999999999999867, 0.4874999999999999889, 0.4899999999999999911 ),
 .UNSPECIFIED. ) 
 CURVE ( )  GEOMETRIC_REPRESENTATION_ITEM ( )  RATIONAL_B_SPLINE_CURVE ( ( 1.000000000000000000, 0.9238795325112869605, 1.000000000000000000, 0.9238795325112869605, 1.000000000000000000, 0.9238795325112869605, 1.000000000000000000, 0.9238795325112869605, 1.000000000000000000 ) ) 
 REPRESENTATION_ITEM ( '' )  ) ;
#38846=ADVANCED_FACE ( 'NONE', ( #12647 ), #38953, .T. ) ;
#38850=CARTESIAN_POINT ( 'NONE',  ( -0.9873396505805591694, -0.1113553986120547346, 0.4773622047244094890 ) ) ;
#38851=CARTESIAN_POINT ( 'NONE',  ( 1.054774247047244540, -0.07405724077823318263, 1.245078740103716886 ) ) ;
#38854=CARTESIAN_POINT ( 'NONE',  ( -0.7185039370078739607, 1.928577636452523993E-17, 0.9251968502861732668 ) ) ;
#38855=CARTESIAN_POINT ( 'NONE',  ( -0.8759842519685039353, 0.1787899950787401882, 0.9817913385289134265 ) ) ;
#38856=ADVANCED_FACE ( 'NONE', ( #2291 ), #38256, .T. ) ;
#38860=DIRECTION ( 'NONE',  ( 1.000000000000000000, 0.000000000000000000, -1.822029033848725275E-16 ) ) ;
#38862=DIRECTION ( 'NONE',  ( 1.822029033848725028E-16, 0.000000000000000000, 1.000000000000000000 ) ) ;
#38863=VECTOR ( 'NONE', #25672, 39.37007874015748143 ) ;
#38864=( BOUNDED_CURVE ( )  B_SPLINE_CURVE ( 2, ( #20893, #13925, #28569, #17986, #2876, #17512, #7209, #17756, #6482 ),
 .UNSPECIFIED., .F., .T. ) 
 B_SPLINE_CURVE_WITH_KNOTS ( ( 3, 2, 2, 2, 3 ),
 ( 0.5200000000000000178, 0.5224999999999999645, 0.5250000000000000222, 0.5274999999999999689, 0.5300000000000000266 ),
 .UNSPECIFIED. ) 
 CURVE ( )  GEOMETRIC_REPRESENTATION_ITEM ( )  RATIONAL_B_SPLINE_CURVE ( ( 1.000000000000000000, 0.9238795325112869605, 1.000000000000000000, 0.9238795325112869605, 1.000000000000000000, 0.9238795325112869605, 1.000000000000000000, 0.9238795325112869605, 1.000000000000000000 ) ) 
 REPRESENTATION_ITEM ( '' )  ) ;
#38872=CARTESIAN_POINT ( 'NONE',  ( 1.054774247047244540, -0.07405724077823318263, 0.4527559054580477249 ) ) ;
#38873=CARTESIAN_POINT ( 'NONE',  ( -0.7495606340400177148, -0.1264236179284866091, 0.7997047243556849594 ) ) ;
#38875=DIRECTION ( 'NONE',  ( -1.000000000000000000, 0.000000000000000000, 0.000000000000000000 ) ) ;
#38877=CARTESIAN_POINT ( 'NONE',  ( -0.7243157012892635915, -0.07330675423201983565, 1.984682877753522590 ) ) ;
#38879=CARTESIAN_POINT ( 'NONE',  ( 0.7495606340400177148, -0.1264236179284866091, 1.508366141678519678 ) ) ;
#38880=CARTESIAN_POINT ( 'NONE',  ( 0.6971942568897648851, 0.07405724077823318263, 1.929133858213952557 ) ) ;
#38882=CARTESIAN_POINT ( 'NONE',  ( 0.6971942568897648851, -0.07405724077823297447, 0.4379921259304883074 ) ) ;
#38883=ORIENTED_EDGE ( 'NONE', *, *, #15099, .F. ) ;
#38886=ORIENTED_EDGE ( 'NONE', *, *, #23605, .T. ) ;
#38887=DIRECTION ( 'NONE',  ( 0.000000000000000000, 0.000000000000000000, 1.000000000000000000 ) ) ;
#38891=CARTESIAN_POINT ( 'NONE',  ( 1.054774247047244540, 0.07405724077823318263, 0.4183070865604097133 ) ) ;
#38893=DIRECTION ( 'NONE',  ( 0.000000000000000000, 0.000000000000000000, -1.000000000000000000 ) ) ;
#38896=CARTESIAN_POINT ( 'NONE',  ( -1.054774247047244096, 0.000000000000000000, 1.478838582623401399 ) ) ;
#38897=VERTEX_POINT ( 'NONE', #13792 ) ;
#38898=DIRECTION ( 'NONE',  ( 1.000000000000000000, 0.000000000000000000, -1.822029033848725275E-16 ) ) ;
#38900=CARTESIAN_POINT ( 'NONE',  ( 0.9500414927467378812, 0.1787899950787401604, 0.9793307086076531442 ) ) ;
#38902=CARTESIAN_POINT ( 'NONE',  ( -1.033464566929134687, 0.06523048226347956391, 0.5930118109160945616 ) ) ;
#38903=CARTESIAN_POINT ( 'NONE',  ( 0.9500414927467378812, -0.1787899950787401604, 1.707677165300566235 ) ) ;
#38904=CARTESIAN_POINT ( 'NONE',  ( -0.8107537697050253289, -0.1574803149606297803, 1.414862204724410377 ) ) ;
#38905=CARTESIAN_POINT ( 'NONE',  ( -0.6971942568897637749, 2.189545951927499583E-17, 0.8292322834108031282 ) ) ;
#38908=CARTESIAN_POINT ( 'NONE',  ( 0.8759842519685039353, -0.1787899950787401882, 0.09596456687537047170 ) ) ;
#38909=CARTESIAN_POINT ( 'NONE',  ( 0.7646288533564489232, 0.1113553986120547346, 1.471456692805858113 ) ) ;
#38910=ORIENTED_EDGE ( 'NONE', *, *, #6572, .F. ) ;
#38913=CARTESIAN_POINT ( 'NONE',  ( -0.9500414927467377701, 0.1787899950787401604, 1.722440944828126153 ) ) ;
#38914=ORIENTED_EDGE ( 'NONE', *, *, #36498, .T. ) ;
#38918=ORIENTED_EDGE ( 'NONE', *, *, #3841, .T. ) ;
#38920=ORIENTED_EDGE ( 'NONE', *, *, #39785, .T. ) ;
#38921=ORIENTED_EDGE ( 'NONE', *, *, #36582, .T. ) ;
#38923=CARTESIAN_POINT ( 'NONE',  ( -0.7185039370078739607, 1.928577636452523993E-17, 0.4133858266641259882 ) ) ;
#38925=CARTESIAN_POINT ( 'NONE',  ( 0.7646288533564489232, 0.1113553986120547346, 1.756889763779527547 ) ) ;
#38929=CARTESIAN_POINT ( 'NONE',  ( -0.7495606340400177148, -0.1264236179284866091, 0.4060039369541102450 ) ) ;
#38930=CARTESIAN_POINT ( 'NONE',  ( -0.7185039370078746268, 0.06523048226347956391, 1.050688976377951889 ) ) ;
#38932=CARTESIAN_POINT ( 'NONE',  ( -0.7185039370078739607, 1.928577636452523993E-17, 0.2263779527559055260 ) ) ;
#38933=CARTESIAN_POINT ( 'NONE',  ( 0.8019270111902717657, 0.1787899950787401604, 1.023622047190330342 ) ) ;
#38934=CARTESIAN_POINT ( 'NONE',  ( 0.7495606340400177148, -0.1264236179284866091, 1.503444881836000002 ) ) ;
#38935=CARTESIAN_POINT ( 'NONE',  ( 0.9500414927467377701, 0.1787899950787401604, 0.2263779527021421711 ) ) ;
#38937=EDGE_CURVE ( 'NONE', #11894, #29244, #26128, .T. ) ;
#38938=CARTESIAN_POINT ( 'NONE',  ( 0.7646288533564489232, -0.1113553986120547346, 1.412401574803149540 ) ) ;
#38940=DIRECTION ( 'NONE',  ( -1.000000000000000000, 0.000000000000000000, 0.000000000000000000 ) ) ;
#38943=CARTESIAN_POINT ( 'NONE',  ( 0.9500414927467377701, -0.1787899950787401604, 1.195866141678520345 ) ) ;
#38944=CARTESIAN_POINT ( 'NONE',  ( 1.054774247047244540, 0.07405724077823318263, 1.919291338528913649 ) ) ;
#38945=CARTESIAN_POINT ( 'NONE',  ( 0.8107537697050253289, -0.1574803149606297803, 0.3813976376877488139 ) ) ;
#38948=EDGE_CURVE ( 'NONE', #43205, #44478, #45977, .T. ) ;
#38949=CARTESIAN_POINT ( 'NONE',  ( -0.7646288533564489232, 0.1113553986120547346, 0.2116141731208196763 ) ) ;
#38950=ORIENTED_EDGE ( 'NONE', *, *, #46512, .T. ) ;
#38951=CARTESIAN_POINT ( 'NONE',  ( 0.6971942568897648851, 0.07405724077823318263, 1.299212598371432215 ) ) ;
#38952=EDGE_CURVE ( 'NONE', #18622, #20854, #32583, .T. ) ;
#38953=CYLINDRICAL_SURFACE ( 'NONE', #19551, 0.1574803149606300579 ) ;
#38954=CARTESIAN_POINT ( 'NONE',  ( -0.7185039370078746268, 0.06523048226347956391, 0.2928149605223942520 ) ) ;
#38956=CARTESIAN_POINT ( 'NONE',  ( -0.9412147342319837628, 0.1574803149606300301, 1.867618110236221707 ) ) ;
#38958=CARTESIAN_POINT ( 'NONE',  ( 0.8759842519685039353, -0.1574803149606299191, 1.289370078632629868 ) ) ;
#38959=CARTESIAN_POINT ( 'NONE',  ( -0.7646288533564489232, 0.1113553986120547346, 0.2116141731208196763 ) ) ;
#38961=CARTESIAN_POINT ( 'NONE',  ( -0.8759842519685039353, 0.1787899950787401882, 1.331200787347811110 ) ) ;
#38963=CARTESIAN_POINT ( 'NONE',  ( -1.054774247047244096, 0.000000000000000000, 0.9719488188438739629 ) ) ;
#38964=CARTESIAN_POINT ( 'NONE',  ( -0.7646288533564489232, 0.1113553986120547346, 0.02460629921259842659 ) ) ;
#38966=CARTESIAN_POINT ( 'NONE',  ( -0.8019270111902716547, -0.1787899950787401604, 0.9940944881352130613 ) ) ;
#38968=CARTESIAN_POINT ( 'NONE',  ( -0.6971942568897626646, 0.07405724077823318263, 0.6348425196312760255 ) ) ;
#38969=CARTESIAN_POINT ( 'NONE',  ( -1.033464566929133799, 0.000000000000000000, 0.07874015737278799998 ) ) ;
#38973=CARTESIAN_POINT ( 'NONE',  ( 0.7185039370078739607, 1.928577636452523993E-17, 0.6594488188976378451 ) ) ;
#38976=CARTESIAN_POINT ( 'NONE',  ( -0.8107537697050254399, -0.1574803149606297803, 1.759350393593260842 ) ) ;
#38977=CARTESIAN_POINT ( 'NONE',  ( -1.002407869896990045, 0.1264236179284866091, 0.6963582676627716461 ) ) ;
#38978=( BOUNDED_CURVE ( )  B_SPLINE_CURVE ( 2, ( #2200, #27880, #13939, #2887, #24491, #35525, #17528, #46992, #28583 ),
 .UNSPECIFIED., .F., .T. ) 
 B_SPLINE_CURVE_WITH_KNOTS ( ( 3, 2, 2, 2, 3 ),
 ( 0.1900000000000000022, 0.1925000000000000044, 0.1950000000000000067, 0.1975000000000000089, 0.2000000000000000111 ),
 .UNSPECIFIED. ) 
 CURVE ( )  GEOMETRIC_REPRESENTATION_ITEM ( )  RATIONAL_B_SPLINE_CURVE ( ( 1.000000000000000000, 0.9238795325112869605, 1.000000000000000000, 0.9238795325112869605, 1.000000000000000000, 0.9238795325112869605, 1.000000000000000000, 0.9238795325112869605, 1.000000000000000000 ) ) 
 REPRESENTATION_ITEM ( '' )  ) ;
#38980=VERTEX_POINT ( 'NONE', #3487 ) ;
#38981=CARTESIAN_POINT ( 'NONE',  ( -0.8019270111902716547, -0.1787899950787401604, 1.707677165300568456 ) ) ;
#38984=CARTESIAN_POINT ( 'NONE',  ( -0.7185039370078739607, 1.928577636452523993E-17, 0.5019685039370078705 ) ) ;
#38985=CARTESIAN_POINT ( 'NONE',  ( 0.9873396505805591694, 0.1113553986120547346, 0.6053149606299212948 ) ) ;
#38988=CARTESIAN_POINT ( 'NONE',  ( -1.033464566929133799, 0.000000000000000000, 1.417322834538141674 ) ) ;
#38992=VERTEX_POINT ( 'NONE', #32268 ) ;
#38994=CARTESIAN_POINT ( 'NONE',  ( 0.9873396505805591694, -0.1113553986120547346, 1.186023622047243986 ) ) ;
#38996=CARTESIAN_POINT ( 'NONE',  ( -0.8107537697050254399, 0.1574803149606300301, 1.272145669183810668 ) ) ;
#38997=CARTESIAN_POINT ( 'NONE',  ( -0.9873396505805591694, -0.1113553986120547346, 1.343503937007874072 ) ) ;
#38999=CARTESIAN_POINT ( 'NONE',  ( 0.8759842519685039353, -0.1574803149606299191, 1.732283464566929165 ) ) ;
#39000=ADVANCED_FACE ( 'NONE', ( #36560 ), #3721, .T. ) ;
#39001=CARTESIAN_POINT ( 'NONE',  ( 1.033464566929133799, 0.000000000000000000, 0.5905511809948347235 ) ) ;
#39002=CARTESIAN_POINT ( 'NONE',  ( 0.8759842519685039353, -0.1574803149606299191, 1.683070866034204638 ) ) ;
#39006=ORIENTED_EDGE ( 'NONE', *, *, #35455, .F. ) ;
#39009=CARTESIAN_POINT ( 'NONE',  ( 0.7495606340400177148, -0.1264236179284866091, 0.8735236219934803259 ) ) ;
#39018=CARTESIAN_POINT ( 'NONE',  ( -0.8759842519685039353, -0.1787899950787401882, 1.946358267662771757 ) ) ;
#39019=CARTESIAN_POINT ( 'NONE',  ( 0.8019270111902717657, 0.1787899950787401604, 1.929133858213952335 ) ) ;
#39020=ORIENTED_EDGE ( 'NONE', *, *, #46745, .T. ) ;
#39021=CARTESIAN_POINT ( 'NONE',  ( 0.7646288533564489232, -0.1113553986120547346, 0.5462598425196850682 ) ) ;
#39022=CARTESIAN_POINT ( 'NONE',  ( -0.9500414927467378812, 0.1787899950787401604, 1.564960629867495845 ) ) ;
#39024=CARTESIAN_POINT ( 'NONE',  ( -0.8019270111902717657, -0.1787899950787401604, 0.2509842519147403861 ) ) ;
#39027=CARTESIAN_POINT ( 'NONE',  ( -0.7495606340400177148, 0.1264236179284866091, 1.931594488135212728 ) ) ;
#39028=CARTESIAN_POINT ( 'NONE',  ( -0.8759842519685039353, -0.1574803149606299191, 1.929133858267716661 ) ) ;
#39029=DIRECTION ( 'NONE',  ( 1.822029033848725028E-16, 0.000000000000000000, 1.000000000000000000 ) ) ;
#39033=CARTESIAN_POINT ( 'NONE',  ( 0.8759842519685039353, -0.1574803149606299191, 1.053149606191685184 ) ) ;
#39036=VERTEX_POINT ( 'NONE', #20970 ) ;
#39041=( CONVERSION_BASED_UNIT ( 'INCH', #25144 ) LENGTH_UNIT ( ) NAMED_UNIT ( #32022 ) ) ;
#39044=CARTESIAN_POINT ( 'NONE',  ( -0.8759842519685039353, -0.1574803149606299191, 0.8562992124908976876 ) ) ;
#39045=CARTESIAN_POINT ( 'NONE',  ( -0.8759842519685039353, -0.1574803149606299191, 0.7086614173228346081 ) ) ;
#39047=CARTESIAN_POINT ( 'NONE',  ( 1.033464566929134687, 0.06523048226347956391, 0.7603346456692923194 ) ) ;
#39049=EDGE_CURVE ( 'NONE', #45154, #13201, #44154, .T. ) ;
#39053=CARTESIAN_POINT ( 'NONE',  ( 0.8107537697050234415, -0.1574803149606297803, 0.1845472439869611236 ) ) ;
#39056=CARTESIAN_POINT ( 'NONE',  ( -1.033464566929134687, -0.06523048226347956391, 0.7849409447743629364 ) ) ;
#39061=CARTESIAN_POINT ( 'NONE',  ( -0.8759842519685039353, -0.1787899950787401882, 1.980807086560409491 ) ) ;
#39062=ORIENTED_EDGE ( 'NONE', *, *, #35571, .T. ) ;
#39063=CARTESIAN_POINT ( 'NONE',  ( 0.6971942568897648851, -0.07405724077823297447, 1.545275590497416696 ) ) ;
#39064=CARTESIAN_POINT ( 'NONE',  ( 0.7185039370078739607, 1.928577636452523993E-17, 0.9251968502861732668 ) ) ;
#39065=CARTESIAN_POINT ( 'NONE',  ( -1.054774247047244540, 0.07405724077823318263, 0.6988188975840318173 ) ) ;
#39068=CARTESIAN_POINT ( 'NONE',  ( 1.002407869896990045, 0.1264236179284866091, 0.6225393700249762796 ) ) ;
#39069=CARTESIAN_POINT ( 'NONE',  ( -1.002407869896990045, 0.1264236179284866091, 0.4995078739619842612 ) ) ;
#39072=EDGE_LOOP ( 'NONE', ( #12361, #39558, #11012, #5908 ) ) ;
#39073=CARTESIAN_POINT ( 'NONE',  ( -0.9500414927467378812, -0.1787899950787401604, 1.358267716481669662 ) ) ;
#39075=CARTESIAN_POINT ( 'NONE',  ( -1.033464566929134687, -0.06523048226347956391, 0.4404527559055117503 ) ) ;
#39076=CARTESIAN_POINT ( 'NONE',  ( 0.8759842519685039353, 0.1787899950787401882, 1.375492125930488196 ) ) ;
#39082=ORIENTED_EDGE ( 'NONE', *, *, #321, .T. ) ;
#39084=CYLINDRICAL_SURFACE ( 'NONE', #13202, 0.1574803149606299191 ) ;
#39085=VERTEX_POINT ( 'NONE', #37495 ) ;
#39086=CARTESIAN_POINT ( 'NONE',  ( 0.6971942568897637749, 2.189545951927499583E-17, 1.380413385773007873 ) ) ;
#39088=AXIS2_PLACEMENT_3D ( 'NONE', #17955, #35711, #203 ) ;
#39091=FACE_OUTER_BOUND ( 'NONE', #46694, .T. ) ;
#39093=CARTESIAN_POINT ( 'NONE',  ( 0.8019270111902717657, -0.1787899950787401604, 0.3248031495525355306 ) ) ;
#39097=DIRECTION ( 'NONE',  ( 1.000000000000000000, 0.000000000000000000, -1.822029033848725275E-16 ) ) ;
#39098=CARTESIAN_POINT ( 'NONE',  ( 0.8759842519685039353, 0.1787899950787401882, 0.5044291338045039375 ) ) ;
#39099=CARTESIAN_POINT ( 'NONE',  ( -1.002407869896990045, 0.1264236179284866091, 0.7406496062454487328 ) ) ;
#39102=CARTESIAN_POINT ( 'NONE',  ( 0.7646288533564489232, 0.1113553986120547346, 1.707677165246803241 ) ) ;
#39104=CARTESIAN_POINT ( 'NONE',  ( -0.7981378442724675892, -0.1533582279231914536, 1.986711164195015034 ) ) ;
#39106=CARTESIAN_POINT ( 'NONE',  ( -0.8107537697050254399, -0.1574803149606297803, 1.247539369971212508 ) ) ;
#39107=CARTESIAN_POINT ( 'NONE',  ( 0.7495606340400177148, 0.1264236179284866091, 1.695374015694267822 ) ) ;
#39109=CARTESIAN_POINT ( 'NONE',  ( -0.9412147342319837628, -0.1574803149606297803, 1.813484251968503935 ) ) ;
#39110=CARTESIAN_POINT ( 'NONE',  ( 0.8019270111902716547, -0.1787899950787401604, 0.4429133857730084833 ) ) ;
#39112=EDGE_CURVE ( 'NONE', #38468, #5617, #37443, .T. ) ;
#39116=CARTESIAN_POINT ( 'NONE',  ( 0.8759842519685039353, 0.1787899950787401882, 0.6225393700249762796 ) ) ;
#39119=( BOUNDED_CURVE ( )  B_SPLINE_CURVE ( 2, ( #12698, #19855, #13602, #28242, #39002, #9075, #45953, #27799, #9791 ),
 .UNSPECIFIED., .F., .T. ) 
 B_SPLINE_CURVE_WITH_KNOTS ( ( 3, 2, 2, 2, 3 ),
 ( 0.8299999999999999600, 0.8325000000000000178, 0.8349999999999999645, 0.8375000000000000222, 0.8399999999999999689 ),
 .UNSPECIFIED. ) 
 CURVE ( )  GEOMETRIC_REPRESENTATION_ITEM ( )  RATIONAL_B_SPLINE_CURVE ( ( 1.000000000000000000, 0.9238795325112939549, 1.000000000000000000, 0.9238795325112869605, 1.000000000000000000, 0.9238795325112869605, 1.000000000000000000, 0.9238795325112869605, 1.000000000000000000 ) ) 
 REPRESENTATION_ITEM ( '' )  ) ;
#39120=CARTESIAN_POINT ( 'NONE',  ( -0.7646288533564489232, -0.1113553986120547346, 0.9301181101286929431 ) ) ;
#39123=CARTESIAN_POINT ( 'NONE',  ( -1.054774247047244540, -0.07405724077823318263, 1.515748031442299526 ) ) ;
#39126=CARTESIAN_POINT ( 'NONE',  ( 0.8019270111902717657, -0.1787899950787401604, 1.038385826717890259 ) ) ;
#39128=CARTESIAN_POINT ( 'NONE',  ( 0.9500414927467378812, -0.1787899950787401604, 1.747047244040724312 ) ) ;
#39129=CARTESIAN_POINT ( 'NONE',  ( -0.7646288533564489232, -0.1113553986120547346, 1.333661417322834719 ) ) ;
#39130=CARTESIAN_POINT ( 'NONE',  ( -1.054774247047244096, 0.000000000000000000, 0.9276574802611967652 ) ) ;
#39132=CARTESIAN_POINT ( 'NONE',  ( -0.8484364047846082446, -0.1575219822776003920, 0.03937007874015843040 ) ) ;
#39133=CARTESIAN_POINT ( 'NONE',  ( 0.8019270111902716547, -0.1787899950787401604, 0.1722440944344256208 ) ) ;
#39134=CARTESIAN_POINT ( 'NONE',  ( -0.7495606340400177148, 0.1264236179284866091, 0.07627952750529173875 ) ) ;
#39136=CARTESIAN_POINT ( 'NONE',  ( 0.8759842519685039353, 0.1574803149606299191, 1.624015747923968522 ) ) ;
#39139=CARTESIAN_POINT ( 'NONE',  ( 1.033464566929133799, 0.000000000000000000, 0.6003937007874016185 ) ) ;
#39142=CARTESIAN_POINT ( 'NONE',  ( -0.6971942568897637749, 2.189545951927499583E-17, 1.656003936954110412 ) ) ;
#39143=( BOUNDED_CURVE ( )  B_SPLINE_CURVE ( 2, ( #19755, #45138, #19518, #8733, #8019, #27220, #44425, #1059, #33461 ),
 .UNSPECIFIED., .F., .T. ) 
 B_SPLINE_CURVE_WITH_KNOTS ( ( 3, 2, 2, 2, 3 ),
 ( 0.1600000000000000033, 0.1625000000000000056, 0.1650000000000000078, 0.1675000000000000100, 0.1700000000000000122 ),
 .UNSPECIFIED. ) 
 CURVE ( )  GEOMETRIC_REPRESENTATION_ITEM ( )  RATIONAL_B_SPLINE_CURVE ( ( 1.000000000000000000, 0.9238795325112869605, 1.000000000000000000, 0.9238795325112869605, 1.000000000000000000, 0.9238795325112869605, 1.000000000000000000, 0.9238795325112879597, 1.000000000000000000 ) ) 
 REPRESENTATION_ITEM ( '' )  ) ;
#39145=CARTESIAN_POINT ( 'NONE',  ( -0.7646288533564489232, -0.1113553986120547346, 0.7824803149606299746 ) ) ;
#39151=CARTESIAN_POINT ( 'NONE',  ( 0.8759842519685039353, 0.1787899950787401882, 1.055610236166708793 ) ) ;
#39154=CARTESIAN_POINT ( 'NONE',  ( -1.033464566929133799, 0.000000000000000000, 0.9940944881889764995 ) ) ;
#39157=CARTESIAN_POINT ( 'NONE',  ( 0.9873396505805591694, 0.1113553986120547346, 1.865157480314960647 ) ) ;
#39160=CARTESIAN_POINT ( 'NONE',  ( -0.8019270111902716547, -0.1787899950787401604, 0.3690944881352128393 ) ) ;
#39162=CARTESIAN_POINT ( 'NONE',  ( 0.8019270111902717657, -0.1787899950787401604, 1.117125984198206412 ) ) ;
#39163=CARTESIAN_POINT ( 'NONE',  ( 1.002407869896990045, -0.1264236179284866091, 1.592027559001354398 ) ) ;
#39164=CARTESIAN_POINT ( 'NONE',  ( 0.8759842519685039353, 0.1787899950787401882, 0.1894685038832444879 ) ) ;
#39166=CARTESIAN_POINT ( 'NONE',  ( 1.033464566929133799, 0.000000000000000000, 1.702755905511810885 ) ) ;
#39167=CARTESIAN_POINT ( 'NONE',  ( 0.7623055800743335775, 0.1150132697384864122, 1.980789724883672998 ) ) ;
#39168=CARTESIAN_POINT ( 'NONE',  ( -0.8107537697050254399, -0.1574803149606297803, 1.099901574803150650 ) ) ;
#39170=CARTESIAN_POINT ( 'NONE',  ( -0.7646288533564489232, -0.1113553986120547346, 1.756889763671999782 ) ) ;
#39171=CARTESIAN_POINT ( 'NONE',  ( 0.8759842519685039353, -0.1787899950787401882, 0.1697834645131655606 ) ) ;
#39173=CARTESIAN_POINT ( 'NONE',  ( 1.002407869896990045, -0.1264236179284866091, 1.119586614119464585 ) ) ;
#39174=CARTESIAN_POINT ( 'NONE',  ( -0.8759842519685039353, 0.1574803149606299191, 1.820866141624755796 ) ) ;
#39175=CARTESIAN_POINT ( 'NONE',  ( 0.6971942568897648851, 0.07405724077823318263, 1.934055118056471567 ) ) ;
#39176=CARTESIAN_POINT ( 'NONE',  ( 0.8107537697050253289, -0.1574803149606297803, 0.4207677164279059467 ) ) ;
#39179=CARTESIAN_POINT ( 'NONE',  ( -0.7646288533564489232, 0.1113553986120547346, 0.3297244093412917687 ) ) ;
#39180=CARTESIAN_POINT ( 'NONE',  ( -0.7185039370078746268, -0.06523048226347956391, 1.528051181102361378 ) ) ;
#39181=CARTESIAN_POINT ( 'NONE',  ( 0.6971942568897648851, 0.07405724077823318263, 1.338582677111590069 ) ) ;
#39183=CARTESIAN_POINT ( 'NONE',  ( 1.033464566929133799, 0.000000000000000000, 0.07874015737278799998 ) ) ;
#39185=DIRECTION ( 'NONE',  ( 0.000000000000000000, 0.000000000000000000, 1.000000000000000000 ) ) ;
#39187=CARTESIAN_POINT ( 'NONE',  ( 0.8759842519685039353, -0.1574803149606299191, 0.5118110236220472231 ) ) ;
#39190=CARTESIAN_POINT ( 'NONE',  ( -0.9500414927467377701, -0.1787899950787401604, 1.392716535379308285 ) ) ;
#39192=CARTESIAN_POINT ( 'NONE',  ( -0.9500414927467378812, 0.1787899950787401604, 1.018700787347811110 ) ) ;
#39195=CARTESIAN_POINT ( 'NONE',  ( -1.033464566929134687, 0.06523048226347956391, 0.05167322834645668439 ) ) ;
#39196=CARTESIAN_POINT ( 'NONE',  ( -0.6971942568897637749, 2.189545951927499583E-17, 1.144192913332062966 ) ) ;
#39197=CARTESIAN_POINT ( 'NONE',  ( -0.8759842519685039353, -0.1787899950787401882, 0.6865157479777322935 ) ) ;
#39198=CARTESIAN_POINT ( 'NONE',  ( -0.7185039370078746268, -0.06523048226347956391, 0.3469488188976379561 ) ) ;
#39206=CARTESIAN_POINT ( 'NONE',  ( -0.7185039370078739607, 1.928577636452523993E-17, 0.5708661416247566844 ) ) ;
#39207=CARTESIAN_POINT ( 'NONE',  ( -0.9500414927467378812, 0.1787899950787401604, 0.5807086613635594752 ) ) ;
#39209=ADVANCED_FACE ( 'NONE', ( #5612 ), #13059, .T. ) ;
#39211=EDGE_CURVE ( 'NONE', #38222, #27881, #34666, .T. ) ;
#39212=CARTESIAN_POINT ( 'NONE',  ( -0.9500414927467377701, -0.1787899950787401604, 1.594488188922615457 ) ) ;
#39213=ADVANCED_FACE ( 'NONE', ( #45609 ), #27696, .T. ) ;
#39215=VECTOR ( 'NONE', #49, 39.37007874015748143 ) ;
#39216=CARTESIAN_POINT ( 'NONE',  ( -0.9412147342319837628, 0.1574803149606300301, 0.1254921258767249526 ) ) ;
#39218=CARTESIAN_POINT ( 'NONE',  ( 0.7185039370078739607, 1.928577636452523993E-17, 0.5413385826771653919 ) ) ;
#39221=CARTESIAN_POINT ( 'NONE',  ( -1.033464566929134687, 0.06523048226347956391, 1.419783464459402289 ) ) ;
#39222=CARTESIAN_POINT ( 'NONE',  ( 0.6971942568897637749, 2.189545951927499583E-17, 0.6766732282926929409 ) ) ;
#39225=VECTOR ( 'NONE', #46192, 39.37007874015748143 ) ;
#39226=CARTESIAN_POINT ( 'NONE',  ( 0.7185039370078739607, 1.928577636452523993E-17, 1.633858267609007875 ) ) ;
#39228=CARTESIAN_POINT ( 'NONE',  ( 0.8107537697050253289, -0.1574803149606297803, 1.257381889763780736 ) ) ;
#39231=CARTESIAN_POINT ( 'NONE',  ( 0.6971942568897637749, 2.189545951927499583E-17, 0.6717519684501732646 ) ) ;
#39232=CARTESIAN_POINT ( 'NONE',  ( 1.033464566929133799, 0.000000000000000000, 0.2755905510735752184 ) ) ;
#39235=ORIENTED_EDGE ( 'NONE', *, *, #36334, .T. ) ;
#39236=VECTOR ( 'NONE', #37174, 39.37007874015748143 ) ;
#39238=CARTESIAN_POINT ( 'NONE',  ( 0.9500414927467378812, -0.1787899950787401604, 0.7627952755367881643 ) ) ;
#39239=CARTESIAN_POINT ( 'NONE',  ( 1.033464566929133799, 0.000000000000000000, 1.466535433070866201 ) ) ;
#39240=CARTESIAN_POINT ( 'NONE',  ( 1.033464566929133799, 0.000000000000000000, 0.7086614172153071767 ) ) ;
#39244=CARTESIAN_POINT ( 'NONE',  ( 0.8759842519685039353, -0.1574803149606299191, 1.210629921152315047 ) ) ;
#39246=ORIENTED_EDGE ( 'NONE', *, *, #5293, .F. ) ;
#39247=CARTESIAN_POINT ( 'NONE',  ( -1.054774247047244540, 0.07405724077823318263, 1.919291338528913871 ) ) ;
#39249=DIRECTION ( 'NONE',  ( 1.822029033848725028E-16, 0.000000000000000000, 1.000000000000000000 ) ) ;
#39251=CARTESIAN_POINT ( 'NONE',  ( -1.054774247047244540, -0.07405724077823318263, 1.914370078686394860 ) ) ;
#39252=CARTESIAN_POINT ( 'NONE',  ( -1.054774247047244096, 0.000000000000000000, 1.596948818843874074 ) ) ;
#39253=CARTESIAN_POINT ( 'NONE',  ( 0.8019270111902716547, 0.1787899950787401604, 0.8661417322297002563 ) ) ;
#39254=CARTESIAN_POINT ( 'NONE',  ( -0.7495606340400177148, 0.1264236179284866091, 0.1993110235682838682 ) ) ;
#39255=( BOUNDED_CURVE ( )  B_SPLINE_CURVE ( 2, ( #13610, #6413, #27809, #42369, #28250, #12934, #9567, #9329, #42813 ),
 .UNSPECIFIED., .F., .T. ) 
 B_SPLINE_CURVE_WITH_KNOTS ( ( 3, 2, 2, 2, 3 ),
 ( 0.6500000000000000222, 0.6524999999999999689, 0.6550000000000000266, 0.6574999999999999734, 0.6600000000000000311 ),
 .UNSPECIFIED. ) 
 CURVE ( )  GEOMETRIC_REPRESENTATION_ITEM ( )  RATIONAL_B_SPLINE_CURVE ( ( 1.000000000000000000, 0.9238795325112869605, 1.000000000000000000, 0.9238795325112869605, 1.000000000000000000, 0.9238795325112869605, 1.000000000000000000, 0.9238795325112869605, 1.000000000000000000 ) ) 
 REPRESENTATION_ITEM ( '' )  ) ;
#39258=CARTESIAN_POINT ( 'NONE',  ( -0.7495606340400177148, -0.1264236179284866091, 1.862696850339937038 ) ) ;
#39259=CARTESIAN_POINT ( 'NONE',  ( -0.8759842519685039353, 0.1574803149606299191, 1.870078740157480324 ) ) ;
#39262=CARTESIAN_POINT ( 'NONE',  ( 0.7185039370078739607, 1.928577636452523993E-17, 1.909448818790110192 ) ) ;
#39266=CARTESIAN_POINT ( 'NONE',  ( -0.6971942568897626646, 0.07405724077823318263, 0.1181102361667090567 ) ) ;
#39271=EDGE_CURVE ( 'NONE', #42434, #23712, #26973, .T. ) ;
#39277=CARTESIAN_POINT ( 'NONE',  ( -1.033464566929133799, 0.000000000000000000, 0.9842519683964094934 ) ) ;
#39278=CARTESIAN_POINT ( 'NONE',  ( -0.9412147342319837628, 0.1574803149606300301, 0.8046259842519695171 ) ) ;
#39280=CARTESIAN_POINT ( 'NONE',  ( 0.7185039370078746268, -0.06523048226347956391, 1.833169291231055542 ) ) ;
#39281=CARTESIAN_POINT ( 'NONE',  ( 1.033464566929133799, 0.000000000000000000, 0.2362204723334177248 ) ) ;
#39282=CARTESIAN_POINT ( 'NONE',  ( 0.9412147342319837628, 0.1574803149606300301, 0.8046259842519695171 ) ) ;
#39287=CARTESIAN_POINT ( 'NONE',  ( 0.7185039370078746268, -0.06523048226347956391, 0.1796259841444415029 ) ) ;
#39289=EDGE_LOOP ( 'NONE', ( #28703, #8686, #43049, #24605 ) ) ;
#39290=CARTESIAN_POINT ( 'NONE',  ( -0.8107537697050254399, 0.1574803149606300301, 1.587106299105070839 ) ) ;
#39291=CARTESIAN_POINT ( 'NONE',  ( 0.9412147342319837628, -0.1574803149606297803, 1.843011810916095783 ) ) ;
#39292=CARTESIAN_POINT ( 'NONE',  ( -0.7185039370078746268, -0.06523048226347956391, 1.173720472440945350 ) ) ;
#39295=CARTESIAN_POINT ( 'NONE',  ( -0.7495606340400177148, -0.1264236179284866091, 1.936515747977732405 ) ) ;
#39296=EDGE_LOOP ( 'NONE', ( #20288, #14996, #25752, #38680 ) ) ;
#39297=CARTESIAN_POINT ( 'NONE',  ( -1.054774247047244540, 0.07405724077823318263, 1.446850393647023614 ) ) ;
#39298=CARTESIAN_POINT ( 'NONE',  ( 1.054774247047244540, 0.07405724077823318263, 1.525590551127340433 ) ) ;
#39299=CARTESIAN_POINT ( 'NONE',  ( -0.9873396505805591694, -0.1113553986120547346, 0.9104330708661417804 ) ) ;
#39301=CARTESIAN_POINT ( 'NONE',  ( -0.7495606340400177148, 0.1264236179284866091, 0.5930118109698583329 ) ) ;
#39302=CARTESIAN_POINT ( 'NONE',  ( 0.6971942568897626646, 0.07405724077823318263, 0.1624015747493861295 ) ) ;
#39304=CARTESIAN_POINT ( 'NONE',  ( 0.6971942568897648851, -0.07405724077823297447, 0.7972440944344248992 ) ) ;
#39305=CARTESIAN_POINT ( 'NONE',  ( -1.054774247047244540, -0.07405724077823318263, 0.5708661416785200116 ) ) ;
#39306=CARTESIAN_POINT ( 'NONE',  ( 0.8107537697050254399, -0.1574803149606297803, 0.6274606299212601712 ) ) ;
#39310=CARTESIAN_POINT ( 'NONE',  ( -0.7495606340400177148, 0.1264236179284866091, 1.459153543253322693 ) ) ;
#39312=CARTESIAN_POINT ( 'NONE',  ( -0.7646288533564489232, -0.1113553986120547346, 1.530511811023621993 ) ) ;
#39313=CARTESIAN_POINT ( 'NONE',  ( -1.033464566929134687, 0.06523048226347956391, 0.4453740157480309270 ) ) ;
#39314=CARTESIAN_POINT ( 'NONE',  ( 0.7495606340400177148, 0.1264236179284866091, 1.262303149552535420 ) ) ;
#39317=DIRECTION ( 'NONE',  ( 0.000000000000000000, 0.000000000000000000, -1.000000000000000000 ) ) ;
#39332=CARTESIAN_POINT ( 'NONE',  ( -1.033464566929133799, 0.000000000000000000, 1.496062992018456494 ) ) ;
#39333=CARTESIAN_POINT ( 'NONE',  ( 1.054774247047244096, 0.000000000000000000, 0.6126968503399370380 ) ) ;
#39335=CARTESIAN_POINT ( 'NONE',  ( -0.6971942568897648851, 0.07405724077823318263, 1.028543307032851573 ) ) ;
#39337=CARTESIAN_POINT ( 'NONE',  ( 0.7185039370078739607, 1.928577636452523993E-17, 1.003937007766488199 ) ) ;
#39339=CARTESIAN_POINT ( 'NONE',  ( 0.8759842519685039353, -0.1787899950787401882, 1.631397637741511808 ) ) ;
#39340=CARTESIAN_POINT ( 'NONE',  ( 0.8019270111902716547, -0.1787899950787401604, 1.938976377898990799 ) ) ;
#39342=CARTESIAN_POINT ( 'NONE',  ( 0.9500414927467377701, -0.1787899950787401604, 0.5265748030958428139 ) ) ;
#39345=CARTESIAN_POINT ( 'NONE',  ( 0.7646288533564489232, 0.1113553986120547346, 0.02460629921259842659 ) ) ;
#39348=CARTESIAN_POINT ( 'NONE',  ( 0.8019270111902717657, -0.1787899950787401604, 0.6397637794737947026 ) ) ;
#39351=CARTESIAN_POINT ( 'NONE',  ( 1.002407869896990045, -0.1264236179284866091, 0.1008858267178899676 ) ) ;
#39354=CARTESIAN_POINT ( 'NONE',  ( -0.6971942568897648851, 0.07405724077823318263, 1.456692913332062744 ) ) ;
#39355=ORIENTED_EDGE ( 'NONE', *, *, #26289, .T. ) ;
#39357=CARTESIAN_POINT ( 'NONE',  ( 0.9412147342319837628, -0.1574803149606297803, 0.4355314960629916299 ) ) ;
#39358=CARTESIAN_POINT ( 'NONE',  ( 0.8759842519685039353, 0.1787899950787401882, 1.178641732229700922 ) ) ;
#39360=CIRCLE ( 'NONE', #1880, 0.1870078740157481989 ) ;
#39361=CARTESIAN_POINT ( 'NONE',  ( -1.033464566929134687, 0.06523048226347956391, 0.6717519683964102706 ) ) ;
#39362=CARTESIAN_POINT ( 'NONE',  ( 1.033464566929133799, 0.000000000000000000, 1.505905511811023612 ) ) ;
#39363=CARTESIAN_POINT ( 'NONE',  ( 0.9500414927467378812, 0.1787899950787401604, 1.801181102308441861 ) ) ;
#39364=CARTESIAN_POINT ( 'NONE',  ( -0.7495606340400177148, -0.1264236179284866091, 0.9522637794737952577 ) ) ;
#39367=CARTESIAN_POINT ( 'NONE',  ( 1.002407869896990045, 0.1264236179284866091, 0.3075787401037169411 ) ) ;
#39369=CARTESIAN_POINT ( 'NONE',  ( 0.7646288533564489232, 0.1113553986120547346, 1.510826771546015523 ) ) ;
#39372=CARTESIAN_POINT ( 'NONE',  ( 0.7495606340400177148, -0.1264236179284866091, 0.8390748030958424808 ) ) ;
#39373=CARTESIAN_POINT ( 'NONE',  ( -0.8759842519685039353, -0.1787899950787401882, 1.626476377898992132 ) ) ;
#39374=ORIENTED_EDGE ( 'NONE', *, *, #8219, .T. ) ;
#39383=FACE_OUTER_BOUND ( 'NONE', #36638, .T. ) ;
#39384=CARTESIAN_POINT ( 'NONE',  ( -0.8107537697050254399, -0.1574803149606297803, 0.4207677164279060578 ) ) ;
#39385=CARTESIAN_POINT ( 'NONE',  ( 1.054774247047244096, 0.000000000000000000, 0.02214566923757503927 ) ) ;
#39389=CARTESIAN_POINT ( 'NONE',  ( -0.9500414927467377701, -0.1787899950787401604, 0.3740157479777325711 ) ) ;
#39391=CARTESIAN_POINT ( 'NONE',  ( 0.8019270111902717657, 0.1787899950787401604, 1.220472440891118504 ) ) ;
#39392=CARTESIAN_POINT ( 'NONE',  ( 1.054774247047244096, 0.000000000000000000, 1.557578740103716441 ) ) ;
#39393=CARTESIAN_POINT ( 'NONE',  ( -0.7185039370078746268, 0.06523048226347956391, 0.6471456691838118891 ) ) ;
#39394=CARTESIAN_POINT ( 'NONE',  ( 0.7646288533564489232, -0.1113553986120547346, 1.648622047244094668 ) ) ;
#39396=CARTESIAN_POINT ( 'NONE',  ( -0.8759842519685039353, 0.1574803149606299191, 1.003937007874015741 ) ) ;
#39397=CARTESIAN_POINT ( 'NONE',  ( 0.8759842519685039353, 0.1574803149606299191, 1.712598425196850238 ) ) ;
#39398=CARTESIAN_POINT ( 'NONE',  ( 0.7185039370078778465, -0.06523048226348396317, 1.439468503829480772 ) ) ;
#39401=CARTESIAN_POINT ( 'NONE',  ( -1.033464566929133799, 0.000000000000000000, 1.692913385719244213 ) ) ;
#39402=CARTESIAN_POINT ( 'NONE',  ( 0.6971942568897637749, 2.189545951927499583E-17, 0.1993110235682838682 ) ) ;
#39403=CARTESIAN_POINT ( 'NONE',  ( 0.7025635012355225806, 0.03299281671818125178, 0.03937034708046514841 ) ) ;
#39404=CARTESIAN_POINT ( 'NONE',  ( 0.8759842519685039353, 0.1787899950787401882, 1.173720472387181246 ) ) ;
#39405=CARTESIAN_POINT ( 'NONE',  ( -1.033464566929133799, 0.000000000000000000, 1.811023621939716444 ) ) ;
#39407=CARTESIAN_POINT ( 'NONE',  ( 0.9412147342319837628, -0.1574803149606297803, 0.5437992124908979097 ) ) ;
#39410=CARTESIAN_POINT ( 'NONE',  ( 0.9755857380299564063, 0.1348144502090965480, 0.03936793015238081866 ) ) ;
#39412=CARTESIAN_POINT ( 'NONE',  ( -0.7185039370078739607, 1.928577636452523993E-17, 0.3740157479239689664 ) ) ;
#39414=CARTESIAN_POINT ( 'NONE',  ( 0.6971942568897637749, 2.189545951927499583E-17, 1.419783464513165505 ) ) ;
#39416=CARTESIAN_POINT ( 'NONE',  ( -0.7185039370078714072, 0.06523048226347728795, 1.641240157480314377 ) ) ;
#39417=FACE_OUTER_BOUND ( 'NONE', #16410, .T. ) ;
#39420=ORIENTED_EDGE ( 'NONE', *, *, #39211, .T. ) ;
#39421=CARTESIAN_POINT ( 'NONE',  ( -0.8759842519685039353, 0.000000000000000000, 0.000000000000000000 ) ) ;
#39422=( BOUNDED_CURVE ( )  B_SPLINE_CURVE ( 2, ( #8683, #5085, #34348, #1479, #1967, #31224, #16136, #27413, #45800 ),
 .UNSPECIFIED., .F., .T. ) 
 B_SPLINE_CURVE_WITH_KNOTS ( ( 3, 2, 2, 2, 3 ),
 ( 0.05999999999999999778, 0.06250000000000000000, 0.06500000000000000222, 0.06750000000000000444, 0.07000000000000000666 ),
 .UNSPECIFIED. ) 
 CURVE ( )  GEOMETRIC_REPRESENTATION_ITEM ( )  RATIONAL_B_SPLINE_CURVE ( ( 1.000000000000000000, 0.9238795325112869605, 1.000000000000000000, 0.9238795325112869605, 1.000000000000000000, 0.9238795325112869605, 1.000000000000000000, 0.9238795325112869605, 1.000000000000000000 ) ) 
 REPRESENTATION_ITEM ( '' )  ) ;
#39423=ORIENTED_EDGE ( 'NONE', *, *, #40837, .T. ) ;
#39424=AXIS2_PLACEMENT_3D ( 'NONE', #8801, #19592, #1599 ) ;
#39427=CARTESIAN_POINT ( 'NONE',  ( 0.9500414927467378812, 0.1787899950787401604, 0.6249999999462356737 ) ) ;
#39430=CARTESIAN_POINT ( 'NONE',  ( -0.8019270111902716547, -0.1787899950787401604, 1.348425196796630976 ) ) ;
#39432=CARTESIAN_POINT ( 'NONE',  ( -0.9500414927467378812, 0.1787899950787401604, 1.136811023568283119 ) ) ;
#39435=CARTESIAN_POINT ( 'NONE',  ( -0.6971942568897648851, 0.07405724077823318263, 1.968503936954110189 ) ) ;
#39436=EDGE_LOOP ( 'NONE', ( #32476, #12837, #31121, #26636 ) ) ;
#39437=CARTESIAN_POINT ( 'NONE',  ( -0.9500414927467377701, 0.1787899950787401604, 1.053149606245450176 ) ) ;
#39441=VERTEX_POINT ( 'NONE', #15145 ) ;
#39442=CARTESIAN_POINT ( 'NONE',  ( -0.7185039370078746268, -0.06523048226347956391, 0.6520669290263312323 ) ) ;
#39443=ORIENTED_EDGE ( 'NONE', *, *, #1721, .T. ) ;
#39445=CARTESIAN_POINT ( 'NONE',  ( -0.7185039370078746268, 0.06523048226347956391, 0.5684055117034967353 ) ) ;
#39446=CARTESIAN_POINT ( 'NONE',  ( -0.6971942568897626646, 0.07405724077823318263, 0.7086614172690703928 ) ) ;
#39449=CARTESIAN_POINT ( 'NONE',  ( -0.8759842519685039353, -0.1787899950787401882, 1.670767716481669440 ) ) ;
#39450=AXIS2_PLACEMENT_3D ( 'NONE', #6177, #27567, #30918 ) ;
#39451=CARTESIAN_POINT ( 'NONE',  ( 0.8107537697050254399, -0.1574803149606297803, 1.336122047244094446 ) ) ;
#39452=CARTESIAN_POINT ( 'NONE',  ( 0.7185039370078746268, 0.06523048226347956391, 1.040846456585385882 ) ) ;
#39454=ORIENTED_EDGE ( 'NONE', *, *, #22404, .T. ) ;
#39457=CARTESIAN_POINT ( 'NONE',  ( -0.7185039370078746268, 0.06523048226347956391, 1.316437007766489975 ) ) ;
#39458=CARTESIAN_POINT ( 'NONE',  ( 0.8759842519685039353, -0.1787899950787401882, 0.7652559054580472253 ) ) ;
#39464=CARTESIAN_POINT ( 'NONE',  ( 0.9412147342319837628, -0.1574803149606297803, 1.301673228346455602 ) ) ;
#39465=CARTESIAN_POINT ( 'NONE',  ( 0.7498931371579079519, -0.1140439591228732952, 1.985582266786952488 ) ) ;
#39467=CARTESIAN_POINT ( 'NONE',  ( 0.7646288533564489232, -0.1113553986120547346, 1.727362204724409489 ) ) ;
#39468=CARTESIAN_POINT ( 'NONE',  ( 1.054774247047244096, 0.000000000000000000, 0.6126968503399370380 ) ) ;
#39473=CARTESIAN_POINT ( 'NONE',  ( 0.8759842519685039353, -0.1787899950787401882, 0.9571850393163149340 ) ) ;
#39476=DIRECTION ( 'NONE',  ( 1.822029033848725028E-16, 0.000000000000000000, 1.000000000000000000 ) ) ;
#39483=CARTESIAN_POINT ( 'NONE',  ( -0.8019270111902717657, 0.1787899950787401604, 0.03444881884387430981 ) ) ;
#39488=CARTESIAN_POINT ( 'NONE',  ( -1.054774247047244096, 0.000000000000000000, 1.877460629867496067 ) ) ;
#39489=CARTESIAN_POINT ( 'NONE',  ( -0.8759842519685039353, -0.1787899950787401882, 1.468996062938362046 ) ) ;
#39491=CARTESIAN_POINT ( 'NONE',  ( 1.054774247047244540, -0.07405724077823318263, 0.8513779527021426707 ) ) ;
#39492=CARTESIAN_POINT ( 'NONE',  ( -1.002407869896990045, 0.1264236179284866091, 1.090059055064346527 ) ) ;
#39493=CARTESIAN_POINT ( 'NONE',  ( -0.7495606340400177148, -0.1264236179284866091, 0.3666338582139531677 ) ) ;
#39495=CARTESIAN_POINT ( 'NONE',  ( -0.9500414927467378812, 0.1787899950787401604, 1.845472440891119392 ) ) ;
#39496=CARTESIAN_POINT ( 'NONE',  ( -0.9412147342319837628, 0.1574803149606300301, 1.946358267716538082 ) ) ;
#39501=CARTESIAN_POINT ( 'NONE',  ( -1.002407869896990045, -0.1264236179284866091, 0.1747047243556852092 ) ) ;
#39502=B_SPLINE_CURVE_WITH_KNOTS ( 'NONE', 3,
 ( #10372, #40040, #40509, #7698, #25705, #35999, #22312, #3403, #24979, #3638, #4095, #3157, #40276, #18016, #10856, #32901, #25469, #7463, #17782, #18717, #32430, #47009, #28844, #7237, #21857, #18258, #14670 ),
 .UNSPECIFIED., .F., .F.,
 ( 4, 2, 2, 2, 2, 2, 2, 2, 2, 2, 1, 2, 2, 4 ),
 ( 0.000000000000000000, 0.1249999999999987232, 0.2499999999999974465, 0.3124999999999967804, 0.3749999999999961697, 0.4374999999999955591, 0.4999999999999948930, 0.6249999999999946709, 0.6874999999999952260, 0.7499999999999956701, 0.8124999999999961142, 0.8437499999999963363, 0.8749999999999965583, 1.000000000000000000 ),
 .UNSPECIFIED. ) ;
#39503=ORIENTED_EDGE ( 'NONE', *, *, #38109, .T. ) ;
#39504=CARTESIAN_POINT ( 'NONE',  ( -0.8019270111902716547, -0.1787899950787401604, 1.195866141678520345 ) ) ;
#39508=CARTESIAN_POINT ( 'NONE',  ( -0.8759842519685039353, 0.1574803149606299191, 1.545275590443653480 ) ) ;
#39512=CARTESIAN_POINT ( 'NONE',  ( -0.7185039370078739607, 1.928577636452523993E-17, 0.9645669290263307882 ) ) ;
#39513=CARTESIAN_POINT ( 'NONE',  ( -0.9873396505805591694, 0.1113553986120547346, 0.7627952755905511584 ) ) ;
#39515=CARTESIAN_POINT ( 'NONE',  ( 0.7646288533564489232, 0.1113553986120547346, 1.825787401467275473 ) ) ;
#39517=CARTESIAN_POINT ( 'NONE',  ( 0.8759842519685039353, -0.1574803149606299191, 0.2263779526483783444 ) ) ;
#39518=CARTESIAN_POINT ( 'NONE',  ( 1.033464566929134687, 0.06523048226347956391, 0.7209645669291341319 ) ) ;
#39523=CARTESIAN_POINT ( 'NONE',  ( 0.8759842519685039353, 0.1574803149606299191, 0.2460629920184571051 ) ) ;
#39525=ADVANCED_FACE ( 'NONE', ( #22555 ), #11796, .T. ) ;
#39527=CARTESIAN_POINT ( 'NONE',  ( 1.033464566929134687, -0.06523048226347956391, 1.847933070758615237 ) ) ;
#39531=CARTESIAN_POINT ( 'NONE',  ( 0.8759842519685039353, 0.1574803149606299191, 1.033464566821606478 ) ) ;
#39532=( BOUNDED_CURVE ( )  B_SPLINE_CURVE ( 2, ( #29037, #10807, #25420, #7187, #2396, #46245, #13444, #39056, #42634 ),
 .UNSPECIFIED., .F., .T. ) 
 B_SPLINE_CURVE_WITH_KNOTS ( ( 3, 2, 2, 2, 3 ),
 ( 0.3699999999999999956, 0.3724999999999999978, 0.3750000000000000000, 0.3775000000000000022, 0.3800000000000000044 ),
 .UNSPECIFIED. ) 
 CURVE ( )  GEOMETRIC_REPRESENTATION_ITEM ( )  RATIONAL_B_SPLINE_CURVE ( ( 1.000000000000000000, 0.9238795325112869605, 1.000000000000000000, 0.9238795325112869605, 1.000000000000000000, 0.9238795325112869605, 1.000000000000000000, 0.9238795325112869605, 1.000000000000000000 ) ) 
 REPRESENTATION_ITEM ( '' )  ) ;
#39535=CARTESIAN_POINT ( 'NONE',  ( -1.002407869896990045, 0.1264236179284866091, 0.3420275590013546751 ) ) ;
#39537=ORIENTED_EDGE ( 'NONE', *, *, #23872, .F. ) ;
#39538=CARTESIAN_POINT ( 'NONE',  ( -0.8019270111902717657, -0.1787899950787401604, 1.550196850339937926 ) ) ;
#39540=CARTESIAN_POINT ( 'NONE',  ( 0.6971942568897637749, 2.189545951927499583E-17, 1.582185039316315045 ) ) ;
#39542=CARTESIAN_POINT ( 'NONE',  ( -0.7185039370078739607, 1.928577636452523993E-17, 0.4921259841444416971 ) ) ;
#39543=CARTESIAN_POINT ( 'NONE',  ( -0.8759842519685039353, 0.1787899950787401882, 0.6668307086076534773 ) ) ;
#39544=CARTESIAN_POINT ( 'NONE',  ( 0.8019270111902717657, -0.1787899950787401604, 0.2116141731745827814 ) ) ;
#39545=EDGE_CURVE ( 'NONE', #34176, #33124, #10434, .T. ) ;
#39546=CARTESIAN_POINT ( 'NONE',  ( -1.033464566929134687, -0.06523048226347956391, 1.690452755797985152 ) ) ;
#39547=CARTESIAN_POINT ( 'NONE',  ( -0.6971942568897648851, 0.07405724077823318263, 0.6299212597887560161 ) ) ;
#39551=CARTESIAN_POINT ( 'NONE',  ( -0.8759842519685039353, -0.1787899950787401882, 1.434547244040724534 ) ) ;
#39553=CARTESIAN_POINT ( 'NONE',  ( -0.8107537697050253289, 0.1574803149606300301, 0.5339566929133855444 ) ) ;
#39554=CARTESIAN_POINT ( 'NONE',  ( 1.054774247047244540, 0.07405724077823318263, 1.486220472387181912 ) ) ;
#39556=CARTESIAN_POINT ( 'NONE',  ( 0.7185039370078739607, 1.928577636452523993E-17, 1.515748031388535200 ) ) ;
#39558=ORIENTED_EDGE ( 'NONE', *, *, #47352, .F. ) ;
#39559=FACE_OUTER_BOUND ( 'NONE', #45509, .T. ) ;
#39564=CYLINDRICAL_SURFACE ( 'NONE', #14211, 0.1574803149606299191 ) ;
#39566=CARTESIAN_POINT ( 'NONE',  ( 0.9500414927467378812, -0.1787899950787401604, 0.3690944881352128393 ) ) ;
#39572=CARTESIAN_POINT ( 'NONE',  ( 0.7495606340400177148, 0.1264236179284866091, 0.6274606298674959559 ) ) ;
#39573=CARTESIAN_POINT ( 'NONE',  ( -0.8759842519685039353, 0.1787899950787401882, 0.9817913385289134265 ) ) ;
#39578=CARTESIAN_POINT ( 'NONE',  ( 0.9500414927467378812, 0.1787899950787401604, 1.609251968450173376 ) ) ;
#39580=DIRECTION ( 'NONE',  ( 1.822029033848725028E-16, 0.000000000000000000, 1.000000000000000000 ) ) ;
#39581=CARTESIAN_POINT ( 'NONE',  ( 1.054774247047244540, -0.07405724077823318263, 0.5314960629383620461 ) ) ;
#39587=CARTESIAN_POINT ( 'NONE',  ( 0.8019270111902717657, 0.1787899950787401604, 0.5462598424659214080 ) ) ;
#39589=CARTESIAN_POINT ( 'NONE',  ( 0.8019270111902717657, -0.1787899950787401604, 0.09350393695411057804 ) ) ;
#39592=CARTESIAN_POINT ( 'NONE',  ( -0.7495606340400177148, 0.1264236179284866091, 1.532972440891118060 ) ) ;
#39594=CARTESIAN_POINT ( 'NONE',  ( 0.9873396505805591694, -0.1113553986120547346, 0.1624015748031496231 ) ) ;
#39595=CARTESIAN_POINT ( 'NONE',  ( 1.002407869896990045, -0.1264236179284866091, 1.124507873961984261 ) ) ;
#39596=CARTESIAN_POINT ( 'NONE',  ( -0.9873396505805591694, -0.1113553986120547346, 0.6643700786326299790 ) ) ;
#39597=CARTESIAN_POINT ( 'NONE',  ( 0.7185039370078739607, 1.928577636452523993E-17, 0.1082677165354330728 ) ) ;
#39598=CARTESIAN_POINT ( 'NONE',  ( 1.002407869896990045, 0.1264236179284866091, 1.759350393647023614 ) ) ;
#39599=CARTESIAN_POINT ( 'NONE',  ( -0.9412147342319837628, -0.1574803149606297803, 0.5536417322834641386 ) ) ;
#39600=CARTESIAN_POINT ( 'NONE',  ( -0.9500414927467378812, 0.1787899950787401604, 0.9350393700249758355 ) ) ;
#39602=CARTESIAN_POINT ( 'NONE',  ( -1.033464566929133799, 0.000000000000000000, 0.6299212597349921339 ) ) ;
#39604=CARTESIAN_POINT ( 'NONE',  ( 0.7495606340400177148, -0.1264236179284866091, 0.2878937007336381804 ) ) ;
#39605=CARTESIAN_POINT ( 'NONE',  ( -0.9500414927467377701, 0.1787899950787401604, 0.1870078739619845110 ) ) ;
#39606=CARTESIAN_POINT ( 'NONE',  ( -1.054774247047244540, -0.07405724077823318263, 0.6496062991588353874 ) ) ;
#39607=CARTESIAN_POINT ( 'NONE',  ( 0.8759842519685039353, -0.1574803149606299191, 1.525590551073574774 ) ) ;
#39609=AXIS2_PLACEMENT_3D ( 'NONE', #31722, #38887, #20677 ) ;
#39611=CARTESIAN_POINT ( 'NONE',  ( 0.9500414927467378812, -0.1787899950787401604, 0.8070866141194653620 ) ) ;
#39612=CARTESIAN_POINT ( 'NONE',  ( -0.6971942568897637749, 2.189545951927499583E-17, 1.852854330654897685 ) ) ;
#39613=AXIS2_PLACEMENT_3D ( 'NONE', #14636, #24730, #21333 ) ;
#39614=CYLINDRICAL_SURFACE ( 'NONE', #10780, 0.1574803149606299191 ) ;
#39617=ORIENTED_EDGE ( 'NONE', *, *, #31519, .F. ) ;
#39623=CARTESIAN_POINT ( 'NONE',  ( 1.002407869896990045, 0.1264236179284866091, 0.06643700782025216411 ) ) ;
#39625=CARTESIAN_POINT ( 'NONE',  ( -0.9500414927467377701, -0.1787899950787401604, 0.4921259841982049132 ) ) ;
#39627=CARTESIAN_POINT ( 'NONE',  ( 1.054774247047244540, -0.07405724077823318263, 1.166338582623402509 ) ) ;
#39628=CARTESIAN_POINT ( 'NONE',  ( 0.9500414927467377701, -0.1787899950787401604, 1.471456692859622217 ) ) ;
#39629=CARTESIAN_POINT ( 'NONE',  ( -0.8107537697050254399, 0.1574803149606300301, 0.6028543306011346914 ) ) ;
#39630=CARTESIAN_POINT ( 'NONE',  ( -0.7185039370078739607, 1.928577636452523993E-17, 1.013779527559055094 ) ) ;
#39631=DIRECTION ( 'NONE',  ( 0.000000000000000000, 0.000000000000000000, -1.000000000000000000 ) ) ;
#39632=CARTESIAN_POINT ( 'NONE',  ( -0.9412147342319837628, -0.1574803149606297803, 1.803641732175937484 ) ) ;
#39634=CARTESIAN_POINT ( 'NONE',  ( 0.8019270111902717657, 0.1787899950787401604, 0.2312992125446618197 ) ) ;
#39635=CARTESIAN_POINT ( 'NONE',  ( 0.7020141857328450197, -0.007037461325149993799, 0.03936291678462715965 ) ) ;
#39637=CARTESIAN_POINT ( 'NONE',  ( 0.9500414927467377701, -0.1787899950787401604, 1.156496062938362046 ) ) ;
#39638=CARTESIAN_POINT ( 'NONE',  ( -0.7646288533564489232, -0.1113553986120547346, 0.5364173227271189504 ) ) ;
#39640=CARTESIAN_POINT ( 'NONE',  ( 0.9873396505805591694, 0.1113553986120547346, 0.5167322833570401341 ) ) ;
#39643=CARTESIAN_POINT ( 'NONE',  ( 0.9858132855136036987, 0.1256053033721491741, 0.03936520543643565878 ) ) ;
#39644=CARTESIAN_POINT ( 'NONE',  ( -1.033464566929133799, 0.000000000000000000, 0.4330708660342047489 ) ) ;
#39646=CARTESIAN_POINT ( 'NONE',  ( 0.8019270111902717657, 0.1787899950787401604, 1.451771653489543290 ) ) ;
#39647=CARTESIAN_POINT ( 'NONE',  ( -1.033464566929133799, 0.000000000000000000, 1.624015748031496287 ) ) ;
#39648=CYLINDRICAL_SURFACE ( 'NONE', #36921, 0.1574803149606299191 ) ;
#39650=VERTEX_POINT ( 'NONE', #22085 ) ;
#39653=CARTESIAN_POINT ( 'NONE',  ( 0.9500414927467378812, -0.1787899950787401604, 0.5314960629383620461 ) ) ;
#39655=CARTESIAN_POINT ( 'NONE',  ( -1.002407869896990045, -0.1264236179284866091, 1.434547244040724534 ) ) ;
#39657=CARTESIAN_POINT ( 'NONE',  ( -0.8759842519685039353, -0.1787899950787401882, 1.119586614119464585 ) ) ;
#39658=CARTESIAN_POINT ( 'NONE',  ( -0.7646288533564489232, -0.1113553986120547346, 0.1919291338582677087 ) ) ;
#39659=ORIENTED_EDGE ( 'NONE', *, *, #11323, .T. ) ;
#39660=CARTESIAN_POINT ( 'NONE',  ( -0.9500414927467377701, -0.1787899950787401604, 1.156496062938362046 ) ) ;
#39662=CARTESIAN_POINT ( 'NONE',  ( -0.8759842519685039353, 0.1787899950787401882, 0.2337598424659216578 ) ) ;
#39666=CARTESIAN_POINT ( 'NONE',  ( -0.8107537697050254399, 0.1574803149606300301, 0.06151574803149608556 ) ) ;
#39670=CARTESIAN_POINT ( 'NONE',  ( -1.033464566929133799, 0.000000000000000000, 1.742125984251968518 ) ) ;
#39673=CARTESIAN_POINT ( 'NONE',  ( -0.8019270111902717657, 0.1787899950787401604, 0.5856299212060785964 ) ) ;
#39676=CARTESIAN_POINT ( 'NONE',  ( -1.002407869896990045, 0.1264236179284866091, 1.803641732229700700 ) ) ;
#39678=ORIENTED_EDGE ( 'NONE', *, *, #20409, .T. ) ;
#39680=CARTESIAN_POINT ( 'NONE',  ( 1.033464566929134687, 0.06523048226347956391, 0.6323818896562525271 ) ) ;
#39681=CARTESIAN_POINT ( 'NONE',  ( -0.8107537697050253289, 0.1574803149606300301, 1.350885826664126821 ) ) ;
#39682=EDGE_CURVE ( 'NONE', #8568, #35682, #494, .T. ) ;
#39683=CARTESIAN_POINT ( 'NONE',  ( 1.054774247047244540, 0.07405724077823318263, 0.7381889763241898939 ) ) ;
#39685=CARTESIAN_POINT ( 'NONE',  ( 0.7185039370078714072, 0.06523048226347728795, 1.631397637687748814 ) ) ;
#39687=CARTESIAN_POINT ( 'NONE',  ( 0.7185039370078746268, 0.06523048226347956391, 1.208169291338584417 ) ) ;
#39688=CARTESIAN_POINT ( 'NONE',  ( 0.9653553125466671769, -0.1534803737003100077, 1.989856878449740352 ) ) ;
#39690=CARTESIAN_POINT ( 'NONE',  ( 0.9873396505805591694, -0.1113553986120547346, 1.737204724409448842 ) ) ;
#39692=( BOUNDED_CURVE ( )  B_SPLINE_CURVE ( 2, ( #19070, #24340, #2739, #2048, #39397, #20954, #38720, #21193, #42298 ),
 .UNSPECIFIED., .F., .T. ) 
 B_SPLINE_CURVE_WITH_KNOTS ( ( 3, 2, 2, 2, 3 ),
 ( 0.8599999999999999867, 0.8625000000000000444, 0.8649999999999999911, 0.8675000000000000488, 0.8699999999999999956 ),
 .UNSPECIFIED. ) 
 CURVE ( )  GEOMETRIC_REPRESENTATION_ITEM ( )  RATIONAL_B_SPLINE_CURVE ( ( 1.000000000000000000, 0.9238795325112869605, 1.000000000000000000, 0.9238795325112869605, 1.000000000000000000, 0.9238795325112869605, 1.000000000000000000, 0.9238795325112869605, 1.000000000000000000 ) ) 
 REPRESENTATION_ITEM ( '' )  ) ;
#39694=CARTESIAN_POINT ( 'NONE',  ( 0.8019270111902716547, 0.1787899950787401604, 0.7037401574265510495 ) ) ;
#39698=AXIS2_PLACEMENT_3D ( 'NONE', #37719, #4381, #12335 ) ;
#39699=CARTESIAN_POINT ( 'NONE',  ( 0.9500414927467378812, -0.1787899950787401604, 0.9596456692375764375 ) ) ;
#39708=CARTESIAN_POINT ( 'NONE',  ( -0.6971942568897626646, 0.07405724077823318263, 0.03937007868639404856 ) ) ;
#39710=VECTOR ( 'NONE', #401, 39.37007874015748143 ) ;
#39711=CARTESIAN_POINT ( 'NONE',  ( 0.7495606340400177148, -0.1264236179284866091, 1.980807086560409491 ) ) ;
#39712=EDGE_LOOP ( 'NONE', ( #3225, #26283, #27160, #15303 ) ) ;
#39713=CARTESIAN_POINT ( 'NONE',  ( -0.9500414927467377701, 0.1787899950787401604, 1.963582677111591401 ) ) ;
#39714=CARTESIAN_POINT ( 'NONE',  ( -0.8019270111902717657, -0.1787899950787401604, 1.663385826717890925 ) ) ;
#39715=CARTESIAN_POINT ( 'NONE',  ( 1.054774247047244540, 0.07405724077823318263, 0.8562992125446617919 ) ) ;
#39716=CARTESIAN_POINT ( 'NONE',  ( -0.6971942568897637749, 2.189545951927499583E-17, 1.065452755851747924 ) ) ;
#39718=CARTESIAN_POINT ( 'NONE',  ( -0.8019270111902717657, -0.1787899950787401604, 1.865157480261195877 ) ) ;
#39719=CARTESIAN_POINT ( 'NONE',  ( -0.8759842519685039353, -0.1574803149606299191, 1.968503937007874072 ) ) ;
#39723=DIRECTION ( 'NONE',  ( 1.822029033848725028E-16, 0.000000000000000000, 1.000000000000000000 ) ) ;
#39725=CARTESIAN_POINT ( 'NONE',  ( -0.8759842519685039353, 0.1787899950787401882, 0.1500984251430870220 ) ) ;
#39729=CARTESIAN_POINT ( 'NONE',  ( -0.8019270111902716547, -0.1787899950787401604, 1.353346456639149986 ) ) ;
#39736=DIRECTION ( 'NONE',  ( 0.000000000000000000, 0.000000000000000000, 1.000000000000000000 ) ) ;
#39737=CARTESIAN_POINT ( 'NONE',  ( -0.7646288533564489232, -0.1113553986120547346, 0.9694881888688504645 ) ) ;
#39738=CARTESIAN_POINT ( 'NONE',  ( -1.033464566929134687, 0.06523048226347956391, 0.9178149606299221830 ) ) ;
#39740=CARTESIAN_POINT ( 'NONE',  ( 0.7495606340400177148, 0.1264236179284866091, 0.4355314960092284138 ) ) ;
#39742=CARTESIAN_POINT ( 'NONE',  ( 0.8759842519685039353, -0.1574803149606299191, 1.761811023514519459 ) ) ;
#39745=CARTESIAN_POINT ( 'NONE',  ( 0.9412147342319837628, -0.1574803149606297803, 0.8686023622047237547 ) ) ;
#39746=CARTESIAN_POINT ( 'NONE',  ( 1.033464566929133799, 0.000000000000000000, 0.4822834645669291653 ) ) ;
#39748=FACE_OUTER_BOUND ( 'NONE', #1895, .T. ) ;
#39750=CARTESIAN_POINT ( 'NONE',  ( 0.9873396505805591694, -0.1113553986120547346, 0.2312992124908980207 ) ) ;
#39756=CARTESIAN_POINT ( 'NONE',  ( 0.7185039370078746268, -0.06523048226347956391, 0.9670275589475911815 ) ) ;
#39758=CARTESIAN_POINT ( 'NONE',  ( -1.054774247047244540, -0.07405724077823318263, 0.4527559054580477249 ) ) ;
#39759=ORIENTED_EDGE ( 'NONE', *, *, #19315, .T. ) ;
#39761=CARTESIAN_POINT ( 'NONE',  ( -0.6971942568897648851, -0.07405724077823297447, 1.624015747977732849 ) ) ;
#39763=CARTESIAN_POINT ( 'NONE',  ( 0.7495606340400177148, 0.1264236179284866091, 1.616633858213952779 ) ) ;
#39764=VERTEX_POINT ( 'NONE', #40742 ) ;
#39766=CARTESIAN_POINT ( 'NONE',  ( -1.054774247047244540, 0.07405724077823318263, 0.7775590550643479704 ) ) ;
#39767=CARTESIAN_POINT ( 'NONE',  ( 1.054774247047244540, -0.07405724077823318263, 0.1427165353793072855 ) ) ;
#39768=CARTESIAN_POINT ( 'NONE',  ( -0.8107537697050254399, 0.1574803149606300301, 0.2583661417322834497 ) ) ;
#39769=CARTESIAN_POINT ( 'NONE',  ( 0.8759842519685039353, 0.1787899950787401882, 0.7849409448281259305 ) ) ;
#39770=CARTESIAN_POINT ( 'NONE',  ( -1.002407869896990045, -0.1264236179284866091, 0.6471456692375747721 ) ) ;
#39772=FACE_OUTER_BOUND ( 'NONE', #46037, .T. ) ;
#39773=FACE_OUTER_BOUND ( 'NONE', #43513, .T. ) ;
#39775=CARTESIAN_POINT ( 'NONE',  ( -0.6971942568897637749, 2.189545951927499583E-17, 1.464074803095842370 ) ) ;
#39776=CARTESIAN_POINT ( 'NONE',  ( -0.7646288533564489232, 0.1113553986120547346, 1.520669291338582640 ) ) ;
#39777=CARTESIAN_POINT ( 'NONE',  ( -1.033464566929133799, 0.000000000000000000, 0.4429133858267716439 ) ) ;
#39778=CARTESIAN_POINT ( 'NONE',  ( 1.054774247047244096, 0.000000000000000000, 1.444389763725763665 ) ) ;
#39784=EDGE_LOOP ( 'NONE', ( #41433, #6470, #6607, #17883 ) ) ;
#39785=EDGE_CURVE ( 'NONE', #1000, #11821, #7938, .T. ) ;
#39789=AXIS2_PLACEMENT_3D ( 'NONE', #39421, #6358, #43257 ) ;
#39793=CARTESIAN_POINT ( 'NONE',  ( 0.7495606340400177148, -0.1264236179284866091, 0.2829724408911185041 ) ) ;
#39800=CARTESIAN_POINT ( 'NONE',  ( 1.054774247047244540, 0.07405724077823318263, 0.6151574802611965431 ) ) ;
#39802=( BOUNDED_CURVE ( )  B_SPLINE_CURVE ( 2, ( #31798, #35385, #16922, #20515, #31564, #47091, #35150, #24131, #39183 ),
 .UNSPECIFIED., .F., .T. ) 
 B_SPLINE_CURVE_WITH_KNOTS ( ( 3, 2, 2, 2, 3 ),
 ( 0.01000000000000000021, 0.01250000000000000069, 0.01499999999999999944, 0.01750000000000000167, 0.02000000000000000042 ),
 .UNSPECIFIED. ) 
 CURVE ( )  GEOMETRIC_REPRESENTATION_ITEM ( )  RATIONAL_B_SPLINE_CURVE ( ( 1.000000000000000000, 0.9238795325112869605, 1.000000000000000000, 0.9238795325112869605, 1.000000000000000000, 0.9238795325112869605, 1.000000000000000000, 0.9238795325112869605, 1.000000000000000000 ) ) 
 REPRESENTATION_ITEM ( '' )  ) ;
#39803=CARTESIAN_POINT ( 'NONE',  ( -0.7495606340400177148, 0.1264236179284866091, 0.9079724408911180600 ) ) ;
#39805=DIRECTION ( 'NONE',  ( 0.000000000000000000, 0.000000000000000000, -1.000000000000000000 ) ) ;
#39807=CARTESIAN_POINT ( 'NONE',  ( 0.8759842519685039353, -0.1574803149606299191, 1.692913385826771533 ) ) ;
#39808=CARTESIAN_POINT ( 'NONE',  ( 0.9500414927467378812, -0.1787899950787401604, 1.633858267662771313 ) ) ;
#39812=CARTESIAN_POINT ( 'NONE',  ( 0.7185039370078739607, 1.928577636452523993E-17, 0.02952755905511811330 ) ) ;
#39815=CARTESIAN_POINT ( 'NONE',  ( -0.8759842519685039353, 0.1787899950787401882, 0.4306102361667086820 ) ) ;
#39816=CARTESIAN_POINT ( 'NONE',  ( 1.002407869896990045, 0.1264236179284866091, 0.6176181101824566033 ) ) ;
#39818=CARTESIAN_POINT ( 'NONE',  ( 0.7495606340400177148, 0.1264236179284866091, 0.1599409448281264023 ) ) ;
#39819=CARTESIAN_POINT ( 'NONE',  ( -1.033464566929134687, -0.06523048226347956391, 1.532972440837355066 ) ) ;
#39820=CARTESIAN_POINT ( 'NONE',  ( 0.8759842519685039353, -0.1787899950787401882, 0.5634842519147401640 ) ) ;
#39821=CARTESIAN_POINT ( 'NONE',  ( -1.054774247047244540, 0.07405724077823318263, 1.638779527505292988 ) ) ;
#39822=EDGE_LOOP ( 'NONE', ( #29068, #13733, #46491, #31581 ) ) ;
#39823=CARTESIAN_POINT ( 'NONE',  ( -0.6971942568897648851, -0.07405724077823297447, 1.151574803095843036 ) ) ;
#39825=CARTESIAN_POINT ( 'NONE',  ( 0.6971942568897648851, 0.07405724077823318263, 1.225393700733637514 ) ) ;
#39826=CARTESIAN_POINT ( 'NONE',  ( -0.7185039370078746268, 0.06523048226347956391, 0.7258858266641259327 ) ) ;
#39828=CARTESIAN_POINT ( 'NONE',  ( 0.7495606340400177148, 0.1264236179284866091, 1.887303149552535420 ) ) ;
#39829=CARTESIAN_POINT ( 'NONE',  ( -0.9412147342319837628, -0.1574803149606297803, 0.5930118110236219930 ) ) ;
#39830=CARTESIAN_POINT ( 'NONE',  ( -0.8759842519685039353, 0.1787899950787401882, 0.8587598424659212970 ) ) ;
#39832=CARTESIAN_POINT ( 'NONE',  ( 0.8019270111902716547, 0.1787899950787401604, 0.2362204723871814682 ) ) ;
#39833=CARTESIAN_POINT ( 'NONE',  ( -0.8019270111902716547, 0.1787899950787401604, 0.2312992125446618197 ) ) ;
#39835=CARTESIAN_POINT ( 'NONE',  ( -0.6971942568897637749, 2.189545951927499583E-17, 0.7111220471903307860 ) ) ;
#39836=CARTESIAN_POINT ( 'NONE',  ( 0.8759842519685039353, -0.1574803149606299191, 1.604330708553889595 ) ) ;
#39838=( BOUNDED_CURVE ( )  B_SPLINE_CURVE ( 2, ( #17143, #6819, #42993, #24807, #2748, #46838, #43718, #13551, #20961 ),
 .UNSPECIFIED., .F., .T. ) 
 B_SPLINE_CURVE_WITH_KNOTS ( ( 3, 2, 2, 2, 3 ),
 ( 0.9799999999999999822, 0.9825000000000000400, 0.9849999999999999867, 0.9875000000000000444, 0.9899999999999999911 ),
 .UNSPECIFIED. ) 
 CURVE ( )  GEOMETRIC_REPRESENTATION_ITEM ( )  RATIONAL_B_SPLINE_CURVE ( ( 1.000000000000000000, 0.9238795325112869605, 1.000000000000000000, 0.9238795325112869605, 1.000000000000000000, 0.9238795325112869605, 1.000000000000000000, 0.9238795325112869605, 1.000000000000000000 ) ) 
 REPRESENTATION_ITEM ( '' )  ) ;
#39841=CARTESIAN_POINT ( 'NONE',  ( 1.054774247047244540, 0.07405724077823318263, 0.8562992125446617919 ) ) ;
#39842=CARTESIAN_POINT ( 'NONE',  ( 0.6971942568897648851, 0.07405724077823318263, 0.9891732282926936071 ) ) ;
#39843=CARTESIAN_POINT ( 'NONE',  ( -0.8019270111902716547, 0.1787899950787401604, 1.806102362150961094 ) ) ;
#39844=VECTOR ( 'NONE', #37486, 39.37007874015748143 ) ;
#39845=CARTESIAN_POINT ( 'NONE',  ( 0.9500414927467378812, -0.1787899950787401604, 1.904527559001354398 ) ) ;
#39847=ORIENTED_EDGE ( 'NONE', *, *, #1349, .F. ) ;
#39848=CARTESIAN_POINT ( 'NONE',  ( 1.033464566929134687, 0.06523048226347956391, 1.311515748031496509 ) ) ;
#39852=VERTEX_POINT ( 'NONE', #10014 ) ;
#39853=CARTESIAN_POINT ( 'NONE',  ( 0.9500414927467378812, 0.1787899950787401604, 1.210629921206079818 ) ) ;
#39856=ADVANCED_FACE ( 'NONE', ( #6403 ), #31373, .T. ) ;
#39857=CARTESIAN_POINT ( 'NONE',  ( 0.9412147342319837628, -0.1574803149606297803, 1.931594488188976166 ) ) ;
#39861=CARTESIAN_POINT ( 'NONE',  ( -0.8019270111902716547, -0.1787899950787401604, 0.4872047243556847929 ) ) ;
#39862=CARTESIAN_POINT ( 'NONE',  ( 1.033464566929133799, 0.000000000000000000, 0.9448818896562519720 ) ) ;
#39864=CARTESIAN_POINT ( 'NONE',  ( -0.7226522770000863849, -0.06944897243561021227, 1.984602698732675918 ) ) ;
#39866=CARTESIAN_POINT ( 'NONE',  ( 1.054774247047244096, 0.000000000000000000, 1.247539370024976391 ) ) ;
#39867=CARTESIAN_POINT ( 'NONE',  ( 0.9500414927467377701, -0.1787899950787401604, 1.747047244040724312 ) ) ;
#39870=CARTESIAN_POINT ( 'NONE',  ( -0.9873396505805591694, 0.1113553986120547346, 1.904527559055118280 ) ) ;
#39872=CIRCLE ( 'NONE', #26884, 0.1574803149606299191 ) ;
#39874=CARTESIAN_POINT ( 'NONE',  ( -0.9412147342319837628, -0.1574803149606297803, 1.764271653435779630 ) ) ;
#39876=CARTESIAN_POINT ( 'NONE',  ( 0.6971942568897626646, 0.07405724077823318263, 0.2362204723871814960 ) ) ;
#39877=CARTESIAN_POINT ( 'NONE',  ( 0.7020737121823690252, 0.02867620229676474952, 0.03937008399637639128 ) ) ;
#39878=CARTESIAN_POINT ( 'NONE',  ( 0.8019270111902716547, 0.1787899950787401604, 1.097440944828127041 ) ) ;
#39880=CARTESIAN_POINT ( 'NONE',  ( 0.8107537697050254399, -0.1574803149606297803, 1.218011811023622437 ) ) ;
#39881=CARTESIAN_POINT ( 'NONE',  ( -1.054774247047244540, 0.07405724077823318263, 1.166338582623402509 ) ) ;
#39882=CARTESIAN_POINT ( 'NONE',  ( 0.7646288533564489232, -0.1113553986120547346, 0.4183070865066456645 ) ) ;
#39883=EDGE_LOOP ( 'NONE', ( #17649, #11595, #625, #12374 ) ) ;
#39885=ORIENTED_EDGE ( 'NONE', *, *, #34576, .T. ) ;
#39886=CARTESIAN_POINT ( 'NONE',  ( -0.7185039370078746268, 0.06523048226347956391, 0.3715551180027090727 ) ) ;
#39888=CARTESIAN_POINT ( 'NONE',  ( 0.8019270111902717657, 0.1787899950787401604, 1.491141732229701367 ) ) ;
#39889=CARTESIAN_POINT ( 'NONE',  ( -0.7185039370078746268, -0.06523048226347956391, 1.134350393700787052 ) ) ;
#39891=CARTESIAN_POINT ( 'NONE',  ( -0.7185039370078739607, 1.928577636452523993E-17, 1.761811023622047223 ) ) ;
#39892=CARTESIAN_POINT ( 'NONE',  ( -1.033464566929133799, 0.000000000000000000, 1.387795275590551158 ) ) ;
#39893=CARTESIAN_POINT ( 'NONE',  ( 1.033464566929134687, -0.06523048226347956391, 1.188484251968505268 ) ) ;
#39898=CARTESIAN_POINT ( 'NONE',  ( 0.8107537697050254399, -0.1574803149606297803, 0.5093503937007877180 ) ) ;
#39899=CARTESIAN_POINT ( 'NONE',  ( 0.8019270111902717657, -0.1787899950787401604, 0.5265748030958428139 ) ) ;
#39900=ORIENTED_EDGE ( 'NONE', *, *, #11434, .T. ) ;
#39902=CARTESIAN_POINT ( 'NONE',  ( -0.7495606340400177148, 0.1264236179284866091, 1.065452755851747924 ) ) ;
#39903=CARTESIAN_POINT ( 'NONE',  ( -0.8759842519685039353, -0.1574803149606299191, 0.1574803149606299191 ) ) ;
#39905=CARTESIAN_POINT ( 'NONE',  ( -0.8019270111902716547, -0.1787899950787401604, 1.033464566875371027 ) ) ;
#39906=CARTESIAN_POINT ( 'NONE',  ( -1.054774247047244096, 0.000000000000000000, 0.7750984251430865779 ) ) ;
#39907=CARTESIAN_POINT ( 'NONE',  ( -1.054774247047244540, -0.07405724077823318263, 0.1820866141194649179 ) ) ;
#39914=ORIENTED_EDGE ( 'NONE', *, *, #35611, .F. ) ;
#39915=CARTESIAN_POINT ( 'NONE',  ( -0.8759842519685039353, -0.1574803149606299191, 0.3444881888688507976 ) ) ;
#39919=CARTESIAN_POINT ( 'NONE',  ( -1.002407869896990045, -0.1264236179284866091, 0.8046259841982047467 ) ) ;
#39922=CARTESIAN_POINT ( 'NONE',  ( -1.002407869896990045, -0.1264236179284866091, 1.793799212544661348 ) ) ;
#39924=CARTESIAN_POINT ( 'NONE',  ( -1.033464566929133799, 0.000000000000000000, 1.141732283357039357 ) ) ;
#39925=CARTESIAN_POINT ( 'NONE',  ( -0.8759842519685039353, -0.1787899950787401882, 0.09596456687537047170 ) ) ;
#39926=CARTESIAN_POINT ( 'NONE',  ( 0.7185039370078739607, 1.928577636452523993E-17, 0.6200787401574803237 ) ) ;
#39929=CARTESIAN_POINT ( 'NONE',  ( -0.8759842519685039353, -0.1574803149606299191, 1.407480314853102321 ) ) ;
#39930=CARTESIAN_POINT ( 'NONE',  ( 0.7495606340400177148, -0.1264236179284866091, 0.7209645668753701386 ) ) ;
#39934=VECTOR ( 'NONE', #20611, 39.37007874015748143 ) ;
#39935=CARTESIAN_POINT ( 'NONE',  ( 0.8759842519685039353, 0.1574803149606299191, 1.318897637795275690 ) ) ;
#39936=CARTESIAN_POINT ( 'NONE',  ( 0.9320460955907311495, -0.1671224838594336515, 1.989197504597622679 ) ) ;
#39938=CARTESIAN_POINT ( 'NONE',  ( 0.8107537697050254399, -0.1574803149606297803, 1.483759842412158747 ) ) ;
#39939=CARTESIAN_POINT ( 'NONE',  ( 0.8019270111902716547, -0.1787899950787401604, 0.7185039369541108556 ) ) ;
#39942=DIRECTION ( 'NONE',  ( 1.822029033848725028E-16, 0.000000000000000000, 1.000000000000000000 ) ) ;
#39946=CARTESIAN_POINT ( 'NONE',  ( 1.054774247047244540, 0.07405724077823318263, 0.9301181101824563813 ) ) ;
#39947=DIRECTION ( 'NONE',  ( 0.000000000000000000, 0.000000000000000000, -1.000000000000000000 ) ) ;
#39950=CARTESIAN_POINT ( 'NONE',  ( -0.7495606340400177148, -0.1264236179284866091, 0.1648622046706460786 ) ) ;
#39952=CARTESIAN_POINT ( 'NONE',  ( 0.8759842519685039353, 0.1787899950787401882, 1.966043307032850462 ) ) ;
#39954=CARTESIAN_POINT ( 'NONE',  ( -1.054774247047244096, 0.000000000000000000, 1.956200787347811110 ) ) ;
#39955=CARTESIAN_POINT ( 'NONE',  ( -0.8019270111902717657, 0.1787899950787401604, 1.727362204670645385 ) ) ;
#39956=CARTESIAN_POINT ( 'NONE',  ( -1.002407869896990045, -0.1264236179284866091, 1.080216535379306952 ) ) ;
#39957=CARTESIAN_POINT ( 'NONE',  ( -1.054774247047244540, 0.07405724077823318263, 0.4232283464029293896 ) ) ;
#39958=CYLINDRICAL_SURFACE ( 'NONE', #27618, 0.1574803149606299191 ) ;
#39960=CARTESIAN_POINT ( 'NONE',  ( -0.8759842519685039353, 0.1574803149606299191, 1.909448818897637956 ) ) ;
#39963=EDGE_CURVE ( 'NONE', #29530, #28079, #29794, .T. ) ;
#39967=CARTESIAN_POINT ( 'NONE',  ( -0.8759842519685039353, -0.1787899950787401882, 0.2091535432533232486 ) ) ;
#39969=VERTEX_POINT ( 'NONE', #16966 ) ;
#39971=CARTESIAN_POINT ( 'NONE',  ( -0.8759842519685039353, -0.1787899950787401882, 1.355807086560409491 ) ) ;
#39980=CARTESIAN_POINT ( 'NONE',  ( -0.7185039370078746268, 0.06523048226347956391, 0.8833661416247557963 ) ) ;
#39982=CARTESIAN_POINT ( 'NONE',  ( 1.054774247047244540, 0.07405724077823318263, 0.4232283464029293896 ) ) ;
#39984=CARTESIAN_POINT ( 'NONE',  ( 0.9873396505805591694, -0.1113553986120547346, 1.766732283357039135 ) ) ;
#39987=CARTESIAN_POINT ( 'NONE',  ( 0.8107537697050253289, -0.1574803149606297803, 0.7455708661417325134 ) ) ;
#39990=CARTESIAN_POINT ( 'NONE',  ( -1.033464566929133799, 0.000000000000000000, 0.8366141732283465249 ) ) ;
#39991=CARTESIAN_POINT ( 'NONE',  ( 1.033464566929134687, -0.06523048226347956391, 0.2337598424121580809 ) ) ;
#39993=ORIENTED_EDGE ( 'NONE', *, *, #16256, .F. ) ;
#39994=CARTESIAN_POINT ( 'NONE',  ( 0.8107537697050254399, 0.1574803149606300301, 1.902066929026330566 ) ) ;
#39997=CARTESIAN_POINT ( 'NONE',  ( -0.9873396505805591694, 0.1113553986120547346, 0.04429133847515007855 ) ) ;
#39999=CARTESIAN_POINT ( 'NONE',  ( 0.7185039370078739607, 1.928577636452523993E-17, 0.9251968502861732668 ) ) ;
#40000=LINE ( 'NONE', #32386, #2995 ) ;
#40002=CARTESIAN_POINT ( 'NONE',  ( -1.002407869896990045, -0.1264236179284866091, 0.3715551180564728440 ) ) ;
#40004=ORIENTED_EDGE ( 'NONE', *, *, #32279, .T. ) ;
#40005=CARTESIAN_POINT ( 'NONE',  ( -0.6971942568897648851, 0.07405724077823318263, 1.619094488135213838 ) ) ;
#40006=CARTESIAN_POINT ( 'NONE',  ( 1.002407869896990045, -0.1264236179284866091, 1.518208661363559031 ) ) ;
#40008=CARTESIAN_POINT ( 'NONE',  ( -1.054774247047244540, 0.07405724077823318263, 0.7381889763241898939 ) ) ;
#40010=CARTESIAN_POINT ( 'NONE',  ( 0.8019270111902716547, -0.1787899950787401604, 0.7234251967966300878 ) ) ;
#40011=CARTESIAN_POINT ( 'NONE',  ( -1.054774247047244096, 0.000000000000000000, 0.6914370078202519698 ) ) ;
#40015=CARTESIAN_POINT ( 'NONE',  ( -1.033464566929134687, -0.06523048226347956391, 1.847933070758615015 ) ) ;
#40016=ORIENTED_EDGE ( 'NONE', *, *, #26374, .T. ) ;
#40017=DIRECTION ( 'NONE',  ( 1.000000000000000000, 0.000000000000000000, -1.822029033848725275E-16 ) ) ;
#40018=CARTESIAN_POINT ( 'NONE',  ( -0.8107537697050253289, 0.1574803149606300301, 1.478838582677164615 ) ) ;
#40028=EDGE_CURVE ( 'NONE', #31809, #10459, #16331, .T. ) ;
#40033=CARTESIAN_POINT ( 'NONE',  ( 1.002407869896990045, 0.1264236179284866091, 1.719980314906866203 ) ) ;
#40034=CARTESIAN_POINT ( 'NONE',  ( 0.9500414927467378812, -0.1787899950787401604, 0.2509842519147403861 ) ) ;
#40036=AXIS2_PLACEMENT_3D ( 'NONE', #25863, #903, #40213 ) ;
#40039=CARTESIAN_POINT ( 'NONE',  ( 0.6971942568897626646, -0.07405724077823297447, 0.6348425196312760255 ) ) ;
#40040=CARTESIAN_POINT ( 'NONE',  ( -1.034367163161600489, 0.01381456667479016159, 0.03937007874015843734 ) ) ;
#40041=CARTESIAN_POINT ( 'NONE',  ( 0.7185039370078692977, 0.06523048226347515077, 1.710137795168064079 ) ) ;
#40043=CARTESIAN_POINT ( 'NONE',  ( 1.033464566929134687, -0.06523048226347956391, 1.700295275590550936 ) ) ;
#40044=CARTESIAN_POINT ( 'NONE',  ( 0.7495606340400177148, 0.1264236179284866091, 1.616633858213952779 ) ) ;
#40047=ORIENTED_EDGE ( 'NONE', *, *, #17793, .T. ) ;
#40049=CARTESIAN_POINT ( 'NONE',  ( 0.9412147342319837628, -0.1574803149606297803, 1.331200787294047672 ) ) ;
#40051=CARTESIAN_POINT ( 'NONE',  ( -1.054774247047244540, -0.07405724077823318263, 0.4576771653005669016 ) ) ;
#40054=CARTESIAN_POINT ( 'NONE',  ( 1.054774247047244096, 0.000000000000000000, 0.06643700782025216411 ) ) ;
#40056=CARTESIAN_POINT ( 'NONE',  ( 0.9500414927467377701, -0.1787899950787401604, 0.5659448818360001132 ) ) ;
#40057=CARTESIAN_POINT ( 'NONE',  ( -0.7495606340400177148, -0.1264236179284866091, 1.621555118056472455 ) ) ;
#40059=CARTESIAN_POINT ( 'NONE',  ( -0.6971942568897648851, -0.07405724077823297447, 1.190944881836001112 ) ) ;
#40060=CARTESIAN_POINT ( 'NONE',  ( 1.033464566929133799, 0.000000000000000000, 0.4429133858267716439 ) ) ;
#40062=CARTESIAN_POINT ( 'NONE',  ( 0.9500414927467378812, 0.1787899950787401604, 1.097440944828127041 ) ) ;
#40064=CARTESIAN_POINT ( 'NONE',  ( 1.002407869896990045, -0.1264236179284866091, 1.788877952702141672 ) ) ;
#40065=CARTESIAN_POINT ( 'NONE',  ( -0.8107537697050253289, -0.1574803149606297803, 0.5487204724409447953 ) ) ;
#40066=CARTESIAN_POINT ( 'NONE',  ( -0.8019270111902717657, -0.1787899950787401604, 1.112204724355684959 ) ) ;
#40067=EDGE_CURVE ( 'NONE', #40994, #31847, #12973, .T. ) ;
#40069=CARTESIAN_POINT ( 'NONE',  ( -1.033464566929133799, 1.928577636452524610E-17, 2.869337061179095023E-17 ) ) ;
#40070=CARTESIAN_POINT ( 'NONE',  ( 1.054774247047244096, 0.000000000000000000, 0.3813976377415121966 ) ) ;
#40071=CARTESIAN_POINT ( 'NONE',  ( -0.7495606340400177148, -0.1264236179284866091, 0.1648622046706460786 ) ) ;
#40072=CARTESIAN_POINT ( 'NONE',  ( -0.9500414927467378812, -0.1787899950787401604, 0.7627952755367881643 ) ) ;
#40073=CARTESIAN_POINT ( 'NONE',  ( 0.9412147342319837628, 0.1574803149606300301, 1.503444881782235232 ) ) ;
#40078=CARTESIAN_POINT ( 'NONE',  ( 0.6971942568897626646, 0.07405724077823318263, 0.8710629920722218200 ) ) ;
#40080=CARTESIAN_POINT ( 'NONE',  ( 0.6971942568897648851, 0.07405724077823318263, 1.028543307032851573 ) ) ;
#40081=CARTESIAN_POINT ( 'NONE',  ( -0.9500414927467377701, -0.1787899950787401604, 1.786417322780882388 ) ) ;
#40082=CARTESIAN_POINT ( 'NONE',  ( 1.002407869896990045, -0.1264236179284866091, 1.867618110182456714 ) ) ;
#40090=CARTESIAN_POINT ( 'NONE',  ( 1.054774247047244540, 0.07405724077823318263, 1.245078740103716886 ) ) ;
#40092=CARTESIAN_POINT ( 'NONE',  ( 0.8759842519685039353, 0.1574803149606299191, 1.387795275483023616 ) ) ;
#40093=( BOUNDED_CURVE ( )  B_SPLINE_CURVE ( 2, ( #31042, #19517, #4895, #41291, #20220, #41060, #45137, #30121, #8732 ),
 .UNSPECIFIED., .F., .F. ) 
 B_SPLINE_CURVE_WITH_KNOTS ( ( 3, 2, 2, 2, 3 ),
 ( 0.2099999999999999922, 0.2124999999999999944, 0.2149999999999999967, 0.2174999999999999989, 0.2200000000000000011 ),
 .UNSPECIFIED. ) 
 CURVE ( )  GEOMETRIC_REPRESENTATION_ITEM ( )  RATIONAL_B_SPLINE_CURVE ( ( 1.000000000000000000, 0.9238795325112869605, 1.000000000000000000, 0.9238795325112869605, 1.000000000000000000, 0.9238795325112869605, 1.000000000000000000, 0.9238795325112869605, 1.000000000000000000 ) ) 
 REPRESENTATION_ITEM ( '' )  ) ;
#40094=CARTESIAN_POINT ( 'NONE',  ( 1.054774247047244540, 0.07405724077823318263, 1.520669291284818758 ) ) ;
#40095=CARTESIAN_POINT ( 'NONE',  ( 1.002407869896990045, 0.1264236179284866091, 0.02706692908009476414 ) ) ;
#40098=AXIS2_PLACEMENT_3D ( 'NONE', #1279, #26960, #19974 ) ;
#40099=CARTESIAN_POINT ( 'NONE',  ( -0.8019270111902716547, 0.1787899950787401604, 0.5511811023084406402 ) ) ;
#40102=CARTESIAN_POINT ( 'NONE',  ( -0.7103445921227516946, 0.006968863322258890200, 1.983141774271510727 ) ) ;
#40103=CARTESIAN_POINT ( 'NONE',  ( -0.7185039370078746268, 0.06523048226347956391, 1.208169291338584417 ) ) ;
#40104=CARTESIAN_POINT ( 'NONE',  ( 1.002407869896990045, 0.1264236179284866091, 1.213090551127338435 ) ) ;
#40105=CARTESIAN_POINT ( 'NONE',  ( 1.054774247047244540, 0.07405724077823318263, 1.717519684985606476 ) ) ;
#40107=CARTESIAN_POINT ( 'NONE',  ( 0.8759842519685039353, 0.1574803149606299191, 1.505905511703495847 ) ) ;
#40110=CARTESIAN_POINT ( 'NONE',  ( -1.033464566929134687, -0.06523048226347956391, 1.031003937007875182 ) ) ;
#40112=( BOUNDED_CURVE ( )  B_SPLINE_CURVE ( 2, ( #13848, #28982, #32324, #18157, #40175, #36609, #29235, #47392, #43541 ),
 .UNSPECIFIED., .F., .T. ) 
 B_SPLINE_CURVE_WITH_KNOTS ( ( 3, 2, 2, 2, 3 ),
 ( 0.2899999999999999800, 0.2924999999999999822, 0.2949999999999999845, 0.2974999999999999867, 0.2999999999999999889 ),
 .UNSPECIFIED. ) 
 CURVE ( )  GEOMETRIC_REPRESENTATION_ITEM ( )  RATIONAL_B_SPLINE_CURVE ( ( 1.000000000000000000, 0.9238795325112869605, 1.000000000000000000, 0.9238795325112869605, 1.000000000000000000, 0.9238795325112869605, 1.000000000000000000, 0.9238795325112869605, 1.000000000000000000 ) ) 
 REPRESENTATION_ITEM ( '' )  ) ;
#40113=CARTESIAN_POINT ( 'NONE',  ( 0.8019270111902717657, 0.1787899950787401604, 0.1131889763241894359 ) ) ;
#40114=CARTESIAN_POINT ( 'NONE',  ( 0.7129069480552276961, -0.05209332317552755470, 0.03937008009371578687 ) ) ;
#40115=CARTESIAN_POINT ( 'NONE',  ( -1.033464566929134687, -0.06523048226347956391, 0.5487204723334181411 ) ) ;
#40117=CARTESIAN_POINT ( 'NONE',  ( 0.8107537697050253289, -0.1574803149606297803, 0.5388779526483779003 ) ) ;
#40118=ORIENTED_EDGE ( 'NONE', *, *, #37383, .T. ) ;
#40120=CARTESIAN_POINT ( 'NONE',  ( 0.8534778653333370269, 0.1744360945806266716, 0.03937047372765634795 ) ) ;
#40121=CARTESIAN_POINT ( 'NONE',  ( 0.7646288533564489232, 0.1113553986120547346, 0.8415354329633386588 ) ) ;
#40122=CARTESIAN_POINT ( 'NONE',  ( -0.9412147342319837628, 0.1574803149606300301, 0.4010826770578274081 ) ) ;
#40123=CARTESIAN_POINT ( 'NONE',  ( 1.002407869896990045, -0.1264236179284866091, 1.473917322780881722 ) ) ;
#40124=CARTESIAN_POINT ( 'NONE',  ( -0.8759842519685039353, 0.1574803149606299191, 1.161417322834645605 ) ) ;
#40125=CARTESIAN_POINT ( 'NONE',  ( 0.8107537697050254399, 0.1574803149606300301, 1.911909448818897017 ) ) ;
#40127=ORIENTED_EDGE ( 'NONE', *, *, #12957, .T. ) ;
#40128=CARTESIAN_POINT ( 'NONE',  ( 0.9412147342319837628, 0.1574803149606300301, 0.7258858267716534751 ) ) ;
#40132=EDGE_LOOP ( 'NONE', ( #20686, #2259, #38918, #39454 ) ) ;
#40133=CARTESIAN_POINT ( 'NONE',  ( 0.9500414927467378812, -0.1787899950787401604, 0.6102362204186774219 ) ) ;
#40134=ORIENTED_EDGE ( 'NONE', *, *, #10077, .F. ) ;
#40137=CARTESIAN_POINT ( 'NONE',  ( -1.054774247047244540, 0.07405724077823318263, 1.171259842465921741 ) ) ;
#40138=CARTESIAN_POINT ( 'NONE',  ( -0.6971942568897648851, -0.07405724077823297447, 1.028543307032851573 ) ) ;
#40141=CARTESIAN_POINT ( 'NONE',  ( 0.7646288533564489232, -0.1113553986120547346, 1.638779527451527551 ) ) ;
#40148=AXIS2_PLACEMENT_3D ( 'NONE', #44688, #19549, #37769 ) ;
#40150=CARTESIAN_POINT ( 'NONE',  ( 1.054774247047244540, -0.07405724077823318263, 1.043307086560409269 ) ) ;
#40152=CARTESIAN_POINT ( 'NONE',  ( -1.002407869896990045, -0.1264236179284866091, 0.7258858267178898149 ) ) ;
#40154=CARTESIAN_POINT ( 'NONE',  ( -0.6971942568897648851, 0.07405724077823318263, 1.737204724355685626 ) ) ;
#40155=ORIENTED_EDGE ( 'NONE', *, *, #10909, .F. ) ;
#40157=CARTESIAN_POINT ( 'NONE',  ( 1.033464566929134687, 0.06523048226347956391, 0.6815944881889761664 ) ) ;
#40159=CARTESIAN_POINT ( 'NONE',  ( -1.033464566929134687, 0.06523048226347956391, 0.3961614172153076763 ) ) ;
#40160=CARTESIAN_POINT ( 'NONE',  ( -1.033464566929134687, -0.06523048226347956391, 1.454232283357038691 ) ) ;
#40161=CARTESIAN_POINT ( 'NONE',  ( 0.6971942568897626646, 0.07405724077823318263, 0.7923228345919055560 ) ) ;
#40164=CARTESIAN_POINT ( 'NONE',  ( 0.8107537697050253289, 0.1574803149606300301, 1.478838582677164615 ) ) ;
#40165=CARTESIAN_POINT ( 'NONE',  ( 0.8170104114768506065, -0.1622629120985071838, 1.987100449027034088 ) ) ;
#40167=CARTESIAN_POINT ( 'NONE',  ( 0.7185039370078778465, -0.06523048226348396317, 1.478838582569639071 ) ) ;
#40168=ORIENTED_EDGE ( 'NONE', *, *, #4049, .F. ) ;
#40169=CARTESIAN_POINT ( 'NONE',  ( 0.7495606340400177148, 0.1264236179284866091, 0.7849409448281259305 ) ) ;
#40173=FACE_OUTER_BOUND ( 'NONE', #3604, .T. ) ;
#40175=CARTESIAN_POINT ( 'NONE',  ( 0.8759842519685039353, -0.1574803149606299191, 0.6200787400499527813 ) ) ;
#40176=VECTOR ( 'NONE', #3310, 39.37007874015748143 ) ;
#40178=CARTESIAN_POINT ( 'NONE',  ( 0.9500414927467378812, -0.1787899950787401604, 0.9990157479777320715 ) ) ;
#40179=CARTESIAN_POINT ( 'NONE',  ( -0.8759842519685039353, 0.000000000000000000, 1.978346456692913646 ) ) ;
#40181=CARTESIAN_POINT ( 'NONE',  ( 0.8759842519685039353, 0.1574803149606299191, 1.240157480314960647 ) ) ;
#40182=EDGE_CURVE ( 'NONE', #44763, #15464, #31780, .T. ) ;
#40184=CARTESIAN_POINT ( 'NONE',  ( -0.9500414927467378812, 0.1787899950787401604, 0.1476377952218271561 ) ) ;
#40185=CARTESIAN_POINT ( 'NONE',  ( 0.5314960629921260393, 1.928577636452522761E-17, 5.000000000000000000 ) ) ;
#40186=ORIENTED_EDGE ( 'NONE', *, *, #21920, .T. ) ;
#40188=CARTESIAN_POINT ( 'NONE',  ( 0.8107537697050234415, -0.1574803149606297803, 0.3420275589475912370 ) ) ;
#40189=CARTESIAN_POINT ( 'NONE',  ( -0.9500414927467378812, 0.1787899950787401604, 1.604330708607653921 ) ) ;
#40191=CARTESIAN_POINT ( 'NONE',  ( -0.7495606340400177148, -0.1264236179284866091, 1.109744094434425232 ) ) ;
#40192=CARTESIAN_POINT ( 'NONE',  ( -0.6971942568897637749, 2.189545951927499583E-17, 0.4404527558517480901 ) ) ;
#40194=CARTESIAN_POINT ( 'NONE',  ( 0.7185039370078739607, 1.928577636452523993E-17, 0.9744094488188976833 ) ) ;
#40195=CARTESIAN_POINT ( 'NONE',  ( -0.9873396505805591694, -0.1113553986120547346, 1.973425196850393970 ) ) ;
#40199=DIRECTION ( 'NONE',  ( -1.000000000000000000, 0.000000000000000000, 0.000000000000000000 ) ) ;
#40201=CARTESIAN_POINT ( 'NONE',  ( -0.8759842519685039353, -0.1787899950787401882, 1.040846456639149764 ) ) ;
#40202=VECTOR ( 'NONE', #33755, 39.37007874015748143 ) ;
#40203=CARTESIAN_POINT ( 'NONE',  ( -1.002407869896990045, 0.1264236179284866091, 0.3420275590013546751 ) ) ;
#40204=ORIENTED_EDGE ( 'NONE', *, *, #4131, .T. ) ;
#40205=CARTESIAN_POINT ( 'NONE',  ( -0.7495606340400177148, -0.1264236179284866091, 1.311515747977732405 ) ) ;
#40209=EDGE_CURVE ( 'NONE', #45828, #19233, #8043, .T. ) ;
#40213=DIRECTION ( 'NONE',  ( 1.000000000000000000, 0.000000000000000000, -1.822029033848725275E-16 ) ) ;
#40214=CARTESIAN_POINT ( 'NONE',  ( -1.033464566929134687, -0.06523048226347956391, 0.9817913384751510986 ) ) ;
#40217=CARTESIAN_POINT ( 'NONE',  ( 0.8107537697050253289, -0.1574803149606297803, 1.838090551073574774 ) ) ;
#40220=CARTESIAN_POINT ( 'NONE',  ( 0.8107537697050253289, 0.1574803149606300301, 0.9670275590551186129 ) ) ;
#40223=CARTESIAN_POINT ( 'NONE',  ( 1.033464566929133799, 0.000000000000000000, 0.7578740157480314821 ) ) ;
#40236=CARTESIAN_POINT ( 'NONE',  ( 1.033464566929133799, 0.000000000000000000, 0.9842519683964094934 ) ) ;
#40239=CARTESIAN_POINT ( 'NONE',  ( -1.002407869896990045, -0.1264236179284866091, 0.3321850393163153226 ) ) ;
#40240=EDGE_LOOP ( 'NONE', ( #13912, #4295, #32887, #24962 ) ) ;
#40241=ORIENTED_EDGE ( 'NONE', *, *, #19179, .T. ) ;
#40242=CARTESIAN_POINT ( 'NONE',  ( 0.8019270111902717657, -0.1787899950787401604, 1.747047244040724312 ) ) ;
#40243=EDGE_LOOP ( 'NONE', ( #19398, #23221, #45968, #8927 ) ) ;
#40245=CARTESIAN_POINT ( 'NONE',  ( -1.002407869896990045, 0.1264236179284866091, 0.8587598424659212970 ) ) ;
#40246=CARTESIAN_POINT ( 'NONE',  ( 1.054774247047244540, 0.07405724077823318263, 0.2657480314422993595 ) ) ;
#40247=CARTESIAN_POINT ( 'NONE',  ( 0.8019270111902716547, 0.1787899950787401604, 0.7874015747493863238 ) ) ;
#40248=CARTESIAN_POINT ( 'NONE',  ( -0.6971942568897648851, 0.07405724077823318263, 0.6692913385289143147 ) ) ;
#40250=LINE ( 'NONE', #21669, #18476 ) ;
#40251=CARTESIAN_POINT ( 'NONE',  ( 1.033464566929134687, -0.06523048226347956391, 1.149114173228346969 ) ) ;
#40252=CARTESIAN_POINT ( 'NONE',  ( -0.6971942568897637749, 2.189545951927499583E-17, 1.582185039316315045 ) ) ;
#40253=CARTESIAN_POINT ( 'NONE',  ( -0.8759842519685039353, 0.1574803149606299191, 1.860236220364913207 ) ) ;
#40256=CARTESIAN_POINT ( 'NONE',  ( 1.054774247047244540, -0.07405724077823318263, 1.441929133804504604 ) ) ;
#40260=ORIENTED_EDGE ( 'NONE', *, *, #2224, .F. ) ;
#40270=CARTESIAN_POINT ( 'NONE',  ( 1.054774247047244540, -0.07405724077823318263, 1.712598425143087688 ) ) ;
#40275=CARTESIAN_POINT ( 'NONE',  ( 1.054774247047244540, 0.07405724077823318263, 0.6938976377415123631 ) ) ;
#40276=CARTESIAN_POINT ( 'NONE',  ( -0.9707163768693443107, 0.1389002614476533559, 0.03937007874015844427 ) ) ;
#40277=CARTESIAN_POINT ( 'NONE',  ( 0.8107537697050254399, -0.1574803149606297803, 1.129429133750740277 ) ) ;
#40279=CARTESIAN_POINT ( 'NONE',  ( -0.7185039370078739607, 0.000000000000000000, 4.498031496062992574 ) ) ;
#40280=CARTESIAN_POINT ( 'NONE',  ( 1.054774247047244096, 0.000000000000000000, 1.838090551127338657 ) ) ;
#40283=CARTESIAN_POINT ( 'NONE',  ( 1.002407869896990045, 0.1264236179284866091, 0.4995078739619842612 ) ) ;
#40287=CARTESIAN_POINT ( 'NONE',  ( -0.6971942568897626646, 0.07405724077823318263, 0.4379921259304882519 ) ) ;
#40290=CARTESIAN_POINT ( 'NONE',  ( 0.8019270111902717657, 0.1787899950787401604, 0.1181102361667090567 ) ) ;
#40291=EDGE_CURVE ( 'NONE', #44104, #10582, #36315, .T. ) ;
#40292=CARTESIAN_POINT ( 'NONE',  ( -0.9500414927467378812, -0.1787899950787401604, 1.668307086560410157 ) ) ;
#40293=ORIENTED_EDGE ( 'NONE', *, *, #26647, .T. ) ;
#40294=CARTESIAN_POINT ( 'NONE',  ( -0.8019270111902717657, 0.1787899950787401604, 1.181102362150960428 ) ) ;
#40295=CARTESIAN_POINT ( 'NONE',  ( -0.8759842519685039353, 0.1574803149606299191, 0.3346456692913385988 ) ) ;
#40296=CARTESIAN_POINT ( 'NONE',  ( 0.8019270111902717657, -0.1787899950787401604, 1.195866141678520345 ) ) ;
#40299=CARTESIAN_POINT ( 'NONE',  ( 1.054774247047244540, -0.07405724077823318263, 1.988188976324187562 ) ) ;
#40300=CARTESIAN_POINT ( 'NONE',  ( -0.7185039370078739607, 1.928577636452523993E-17, 0.5807086614173228023 ) ) ;
#40301=CARTESIAN_POINT ( 'NONE',  ( -1.054774247047244096, 0.000000000000000000, 1.124507873961984261 ) ) ;
#40304=CARTESIAN_POINT ( 'NONE',  ( 1.002407869896990045, 0.1264236179284866091, 0.2288385826234019815 ) ) ;
#40305=CARTESIAN_POINT ( 'NONE',  ( -0.8759842519685039353, 0.1787899950787401882, 0.2288385826234019815 ) ) ;
#40307=CARTESIAN_POINT ( 'NONE',  ( -0.6971942568897626646, 0.07405724077823318263, 0.7874015747493863238 ) ) ;
#40309=ADVANCED_FACE ( 'NONE', ( #7058 ), #14267, .T. ) ;
#40312=CARTESIAN_POINT ( 'NONE',  ( 0.8019270111902717657, -0.1787899950787401604, 0.8021653542769460188 ) ) ;
#40313=CARTESIAN_POINT ( 'NONE',  ( 1.054774247047244540, 0.07405724077823318263, 1.092519684985606032 ) ) ;
#40314=CARTESIAN_POINT ( 'NONE',  ( -1.054774247047244096, 0.000000000000000000, 1.793799212544661348 ) ) ;
#40316=CARTESIAN_POINT ( 'NONE',  ( -0.7185039370078739607, 1.928577636452523993E-17, 1.594488188868850242 ) ) ;
#40320=CARTESIAN_POINT ( 'NONE',  ( -0.7185039370078739607, 1.928577636452523993E-17, 1.092519685039370136 ) ) ;
#40322=CARTESIAN_POINT ( 'NONE',  ( 0.6971942568897648851, 0.07405724077823318263, 1.259842519631276359 ) ) ;
#40326=CARTESIAN_POINT ( 'NONE',  ( 0.8759842519685039353, 0.1787899950787401882, 0.03198818892261445085 ) ) ;
#40329=CARTESIAN_POINT ( 'NONE',  ( -0.6971942568897648851, -0.07405724077823297447, 0.4429133857730084833 ) ) ;
#40331=CARTESIAN_POINT ( 'NONE',  ( 0.9412147342319837628, 0.1574803149606300301, 1.434547244094487972 ) ) ;
#40332=CARTESIAN_POINT ( 'NONE',  ( 1.054774247047244096, 0.000000000000000000, 1.286909448765133801 ) ) ;
#40333=CARTESIAN_POINT ( 'NONE',  ( 1.002407869896990045, 0.1264236179284866091, 1.641240157426551161 ) ) ;
#40334=EDGE_CURVE ( 'NONE', #12322, #22163, #16334, .T. ) ;
#40335=CARTESIAN_POINT ( 'NONE',  ( -1.033464566929136907, -0.06523048226347749612, 1.651082677057827519 ) ) ;
#40337=CARTESIAN_POINT ( 'NONE',  ( -0.7646288533564489232, 0.1113553986120547346, 1.008858267716535417 ) ) ;
#40341=CARTESIAN_POINT ( 'NONE',  ( 0.7495606340400177148, 0.1264236179284866091, 0.2731299212060791515 ) ) ;
#40342=CARTESIAN_POINT ( 'NONE',  ( 0.7132025946407314354, -0.05284032427092102274, 0.03937007868462530369 ) ) ;
#40343=CARTESIAN_POINT ( 'NONE',  ( 0.7495606340400177148, 0.1264236179284866091, 1.257381889710015743 ) ) ;
#40346=CARTESIAN_POINT ( 'NONE',  ( 1.033464566929133799, 0.000000000000000000, 1.190944881889763884 ) ) ;
#40347=CARTESIAN_POINT ( 'NONE',  ( 0.9873396505805591694, 0.1113553986120547346, 0.7135826770578268530 ) ) ;
#40348=ORIENTED_EDGE ( 'NONE', *, *, #1349, .T. ) ;
#40349=CARTESIAN_POINT ( 'NONE',  ( 0.8962961640049118550, 0.1721048943457904046, 0.03937035593878661366 ) ) ;
#40350=CARTESIAN_POINT ( 'NONE',  ( -0.7185039370078746268, 0.06523048226347956391, 1.119586614065702035 ) ) ;
#40351=CARTESIAN_POINT ( 'NONE',  ( 0.6971942568897648851, 0.07405724077823318263, 1.456692913332062744 ) ) ;
#40352=CARTESIAN_POINT ( 'NONE',  ( -0.7646288533564489232, -0.1113553986120547346, 1.136811023622047223 ) ) ;
#40356=LINE ( 'NONE', #26014, #9772 ) ;
#40360=CARTESIAN_POINT ( 'NONE',  ( 1.033464566929134687, -0.06523048226347956391, 0.6668307085538908163 ) ) ;
#40361=CARTESIAN_POINT ( 'NONE',  ( -0.7185039370078739607, 0.000000000000000000, -2.869337061179095023E-17 ) ) ;
#40363=CARTESIAN_POINT ( 'NONE',  ( 1.002407869896990045, 0.1264236179284866091, 0.5437992125446614589 ) ) ;
#40365=CARTESIAN_POINT ( 'NONE',  ( -0.8759842519685039353, -0.1787899950787401882, 1.468996062938362046 ) ) ;
#40367=CARTESIAN_POINT ( 'NONE',  ( -1.054774247047244096, 0.000000000000000000, 1.129429133804503937 ) ) ;
#40368=ORIENTED_EDGE ( 'NONE', *, *, #26641, .F. ) ;
#40369=CARTESIAN_POINT ( 'NONE',  ( -0.7646288533564489232, -0.1113553986120547346, 1.963582677165354395 ) ) ;
#40370=CARTESIAN_POINT ( 'NONE',  ( -0.8019270111902717657, -0.1787899950787401604, 0.7627952755367881643 ) ) ;
#40371=( BOUNDED_CURVE ( )  B_SPLINE_CURVE ( 2, ( #8174, #22800, #10866, #14446, #29588, #29355, #21874, #43658, #36494 ),
 .UNSPECIFIED., .F., .T. ) 
 B_SPLINE_CURVE_WITH_KNOTS ( ( 3, 2, 2, 2, 3 ),
 ( 0.2200000000000000011, 0.2225000000000000033, 0.2250000000000000056, 0.2275000000000000078, 0.2300000000000000100 ),
 .UNSPECIFIED. ) 
 CURVE ( )  GEOMETRIC_REPRESENTATION_ITEM ( )  RATIONAL_B_SPLINE_CURVE ( ( 1.000000000000000000, 0.9238795325112869605, 1.000000000000000000, 0.9238795325112869605, 1.000000000000000000, 0.9238795325112869605, 1.000000000000000000, 0.9238795325112879597, 1.000000000000000000 ) ) 
 REPRESENTATION_ITEM ( '' )  ) ;
#40372=CARTESIAN_POINT ( 'NONE',  ( -1.033464566929133799, 0.000000000000000000, 0.6003937007874016185 ) ) ;
#40373=CARTESIAN_POINT ( 'NONE',  ( -0.6971942568897637749, 2.189545951927499583E-17, 0.1648622046706460786 ) ) ;
#40377=ORIENTED_EDGE ( 'NONE', *, *, #14788, .F. ) ;
#40378=CARTESIAN_POINT ( 'NONE',  ( 0.7238228411891962644, 0.09459845738158538520, 0.03936480202592971406 ) ) ;
#40379=VERTEX_POINT ( 'NONE', #37236 ) ;
#40381=CARTESIAN_POINT ( 'NONE',  ( -0.9500414927467378812, 0.1787899950787401604, 0.8169291338045038264 ) ) ;
#40383=CARTESIAN_POINT ( 'NONE',  ( -0.6971942568897648851, 0.07405724077823318263, 1.776574803095843702 ) ) ;
#40387=ADVANCED_FACE ( 'NONE', ( #40570 ), #15211, .T. ) ;
#40388=CARTESIAN_POINT ( 'NONE',  ( -0.8019270111902716547, 0.1787899950787401604, 0.07874015742655143812 ) ) ;
#40389=CARTESIAN_POINT ( 'NONE',  ( 0.8107537697050253289, -0.1574803149606297803, 0.6274606299212601712 ) ) ;
#40392=CARTESIAN_POINT ( 'NONE',  ( -0.7185039370078746268, 0.06523048226347956391, 1.592027558947591848 ) ) ;
#40393=CARTESIAN_POINT ( 'NONE',  ( 0.6971942568897626646, -0.07405724077823297447, 0.7185039369541108556 ) ) ;
#40394=CARTESIAN_POINT ( 'NONE',  ( 0.6971942568897637749, 2.189545951927499583E-17, 1.341043307032850462 ) ) ;
#40396=EDGE_CURVE ( 'NONE', #30681, #36685, #1902, .T. ) ;
#40398=CARTESIAN_POINT ( 'NONE',  ( 0.7185039370078746268, 0.06523048226347956391, 1.405019685039369914 ) ) ;
#40399=CARTESIAN_POINT ( 'NONE',  ( 0.8118511125780327742, -0.1600945206353099892, 1.986996213762715069 ) ) ;
#40400=CARTESIAN_POINT ( 'NONE',  ( 0.8107537697050254399, -0.1574803149606297803, 1.562499999892472013 ) ) ;
#40402=CARTESIAN_POINT ( 'NONE',  ( 0.9500414927467377701, 0.1787899950787401604, 0.8956692912848198684 ) ) ;
#40403=CARTESIAN_POINT ( 'NONE',  ( -0.7185039370078739607, 1.928577636452523993E-17, 1.407480314960629864 ) ) ;
#40408=CARTESIAN_POINT ( 'NONE',  ( 0.6971942568897637749, 2.189545951927499583E-17, 1.026082677111590513 ) ) ;
#40409=DIRECTION ( 'NONE',  ( 1.822029033848725028E-16, 0.000000000000000000, 1.000000000000000000 ) ) ;
#40413=CARTESIAN_POINT ( 'NONE',  ( -0.8759842519685039353, 0.1787899950787401882, 0.5044291338045039375 ) ) ;
#40416=CARTESIAN_POINT ( 'NONE',  ( -0.6971942568897626646, 0.07405724077823318263, 0.1181102361667090567 ) ) ;
#40417=VERTEX_POINT ( 'NONE', #44636 ) ;
#40421=CARTESIAN_POINT ( 'NONE',  ( 0.8759842519685039353, -0.1574803149606299191, 0.3444881888688507976 ) ) ;
#40422=CARTESIAN_POINT ( 'NONE',  ( -0.9500414927467378812, -0.1787899950787401604, 1.747047244040724312 ) ) ;
#40423=CARTESIAN_POINT ( 'NONE',  ( -0.7495606340400177148, -0.1264236179284866091, 0.8341535432533228045 ) ) ;
#40424=CARTESIAN_POINT ( 'NONE',  ( -1.002407869896990045, 0.1264236179284866091, 0.3863188975840318173 ) ) ;
#40425=CARTESIAN_POINT ( 'NONE',  ( -0.7185039370078746268, -0.06523048226347935574, 0.1008858266641264878 ) ) ;
#40426=CARTESIAN_POINT ( 'NONE',  ( 0.7185039370078739607, 1.928577636452523993E-17, 0.1771653542231816925 ) ) ;
#40427=DIRECTION ( 'NONE',  ( 1.822029033848725028E-16, 0.000000000000000000, 1.000000000000000000 ) ) ;
#40428=CARTESIAN_POINT ( 'NONE',  ( -0.9412147342319837628, -0.1574803149606297803, 1.970964566929134021 ) ) ;
#40435=CARTESIAN_POINT ( 'NONE',  ( -0.9500414927467378812, -0.1787899950787401604, 0.3297244093950552069 ) ) ;
#40436=ORIENTED_EDGE ( 'NONE', *, *, #40396, .T. ) ;
#40437=CARTESIAN_POINT ( 'NONE',  ( -0.6971942568897648851, 0.07405724077823318263, 1.382874015694267822 ) ) ;
#40444=CARTESIAN_POINT ( 'NONE',  ( 1.033464566929134687, 0.06523048226347956391, 0.3272637795275589734 ) ) ;
#40446=CARTESIAN_POINT ( 'NONE',  ( -0.8759842519685039353, 0.1574803149606299191, 1.033464566821606478 ) ) ;
#40448=CARTESIAN_POINT ( 'NONE',  ( -1.033464566929134687, -0.06523048226347956391, 1.700295275590550936 ) ) ;
#40450=ORIENTED_EDGE ( 'NONE', *, *, #34073, .F. ) ;
#40451=LINE ( 'NONE', #18658, #21544 ) ;
#40455=CARTESIAN_POINT ( 'NONE',  ( 1.033464566929134687, 0.06523048226347956391, 0.9965551181102363376 ) ) ;
#40456=AXIS2_PLACEMENT_3D ( 'NONE', #24371, #10230, #20531 ) ;
#40459=DIRECTION ( 'NONE',  ( 1.822029033848725028E-16, 0.000000000000000000, 1.000000000000000000 ) ) ;
#40462=CARTESIAN_POINT ( 'NONE',  ( 1.033464566929133799, 0.000000000000000000, 1.889763779420031486 ) ) ;
#40468=CARTESIAN_POINT ( 'NONE',  ( 1.033464566929134687, 0.06523048226347956391, 1.026082677057828185 ) ) ;
#40469=CARTESIAN_POINT ( 'NONE',  ( 1.033464566929133799, 0.000000000000000000, 1.820866141732283561 ) ) ;
#40470=CARTESIAN_POINT ( 'NONE',  ( -0.9500414927467378812, -0.1787899950787401604, 0.3690944881352128393 ) ) ;
#40472=ORIENTED_EDGE ( 'NONE', *, *, #28263, .T. ) ;
#40474=CARTESIAN_POINT ( 'NONE',  ( -0.6971942568897637749, 2.189545951927499583E-17, 1.621555118056472455 ) ) ;
#40475=CARTESIAN_POINT ( 'NONE',  ( 1.002407869896990045, -0.1264236179284866091, 1.675688976324189117 ) ) ;
#40476=CARTESIAN_POINT ( 'NONE',  ( -1.002407869896990045, 0.1264236179284866091, 0.7800196849856062542 ) ) ;
#40477=CARTESIAN_POINT ( 'NONE',  ( 0.8759842519685039353, 0.000000000000000000, 4.498031496062992574 ) ) ;
#40478=CARTESIAN_POINT ( 'NONE',  ( 1.002407869896990045, -0.1264236179284866091, 0.2977362204186775885 ) ) ;
#40480=CARTESIAN_POINT ( 'NONE',  ( -0.6971942568897648851, -0.07405724077823297447, 1.225393700733637514 ) ) ;
#40481=CARTESIAN_POINT ( 'NONE',  ( -0.7495606340400177148, 0.1264236179284866091, 0.6274606298674959559 ) ) ;
#40482=DIRECTION ( 'NONE',  ( 1.822029033848725028E-16, 0.000000000000000000, 1.000000000000000000 ) ) ;
#40485=CARTESIAN_POINT ( 'NONE',  ( -1.054774247047244540, 0.07405724077823318263, 1.564960629867495845 ) ) ;
#40486=CARTESIAN_POINT ( 'NONE',  ( -0.9873396505805591694, 0.1113553986120547346, 1.894685039262551163 ) ) ;
#40492=VERTEX_POINT ( 'NONE', #19260 ) ;
#40508=CARTESIAN_POINT ( 'NONE',  ( 1.002407869896990045, -0.1264236179284866091, 0.7652559054580472253 ) ) ;
#40509=CARTESIAN_POINT ( 'NONE',  ( -1.033507323347888418, 0.02751628197221928779, 0.03937007874015842346 ) ) ;
#40510=CARTESIAN_POINT ( 'NONE',  ( -1.033464566929133799, 0.000000000000000000, 1.417322834538141674 ) ) ;
#40514=CARTESIAN_POINT ( 'NONE',  ( 1.002407869896990045, -0.1264236179284866091, 1.754429133804503715 ) ) ;
#40515=CARTESIAN_POINT ( 'NONE',  ( 0.7646288533564489232, -0.1113553986120547346, 1.874999999892472458 ) ) ;
#40516=CARTESIAN_POINT ( 'NONE',  ( 0.7185039370078739607, 1.928577636452523993E-17, 0.1082677165354330728 ) ) ;
#40517=DIRECTION ( 'NONE',  ( 1.822029033848725028E-16, 0.000000000000000000, 1.000000000000000000 ) ) ;
#40519=CARTESIAN_POINT ( 'NONE',  ( -0.8759842519685039353, 0.000000000000000000, 0.000000000000000000 ) ) ;
#40521=CARTESIAN_POINT ( 'NONE',  ( 0.7495606340400177148, 0.1264236179284866091, 0.3174212597887562382 ) ) ;
#40523=CARTESIAN_POINT ( 'NONE',  ( -0.8019270111902717657, -0.1787899950787401604, 1.624015747977732849 ) ) ;
#40525=CARTESIAN_POINT ( 'NONE',  ( -1.002407869896990045, 0.1264236179284866091, 1.134350393647023614 ) ) ;
#40526=CARTESIAN_POINT ( 'NONE',  ( -1.033464566929134687, 0.06523048226347956391, 0.8784448818897643285 ) ) ;
#40528=CARTESIAN_POINT ( 'NONE',  ( 1.002407869896990045, -0.1264236179284866091, 1.281988188922614125 ) ) ;
#40529=CARTESIAN_POINT ( 'NONE',  ( 0.6971942568897637749, 2.189545951927499583E-17, 0.04675196845017354913 ) ) ;
#40530=CARTESIAN_POINT ( 'NONE',  ( -1.002407869896990045, 0.1264236179284866091, 1.050688976324189117 ) ) ;
#40533=CARTESIAN_POINT ( 'NONE',  ( 1.002407869896990045, 0.1264236179284866091, 0.4256889763241890057 ) ) ;
#40534=CARTESIAN_POINT ( 'NONE',  ( -1.002407869896990045, 0.1264236179284866091, 0.2632874015210397434 ) ) ;
#40535=CARTESIAN_POINT ( 'NONE',  ( -1.054774247047244540, 0.07405724077823318263, 0.7726377952218265177 ) ) ;
#40536=CARTESIAN_POINT ( 'NONE',  ( 0.9873396505805591694, 0.1113553986120547346, 1.658464566821606256 ) ) ;
#40539=CARTESIAN_POINT ( 'NONE',  ( -0.8107537697050254399, 0.1574803149606300301, 0.8784448817822366751 ) ) ;
#40540=CARTESIAN_POINT ( 'NONE',  ( 0.6971942568897626646, -0.07405724077823297447, 0.9153543306548987957 ) ) ;
#40541=CARTESIAN_POINT ( 'NONE',  ( -0.6971942568897648851, 0.07405724077823318263, 1.889763779473794481 ) ) ;
#40543=CARTESIAN_POINT ( 'NONE',  ( 1.054774247047244540, 0.07405724077823318263, 1.914370078686394860 ) ) ;
#40551=CARTESIAN_POINT ( 'NONE',  ( -0.7646288533564489232, 0.1113553986120547346, 1.707677165246803241 ) ) ;
#40552=VERTEX_POINT ( 'NONE', #33208 ) ;
#40553=CARTESIAN_POINT ( 'NONE',  ( 1.054774247047244096, 0.000000000000000000, 1.124507873961984261 ) ) ;
#40555=CARTESIAN_POINT ( 'NONE',  ( 1.033464566929134687, 0.06523048226347956391, 1.380413385719244435 ) ) ;
#40557=CARTESIAN_POINT ( 'NONE',  ( 0.6971942568897637749, 2.189545951927499583E-17, 1.498523621993480326 ) ) ;
#40558=CARTESIAN_POINT ( 'NONE',  ( 1.054774247047244540, -0.07405724077823318263, 0.2165354330171024577 ) ) ;
#40563=CARTESIAN_POINT ( 'NONE',  ( -0.6971942568897648851, -0.07405724077823297447, 0.5610236219934807700 ) ) ;
#40564=CARTESIAN_POINT ( 'NONE',  ( 1.033464566929134687, 0.06523048226347956391, 0.3666338582677165503 ) ) ;
#40567=CARTESIAN_POINT ( 'NONE',  ( 1.002407869896990045, 0.1264236179284866091, 1.331200787347811110 ) ) ;
#40568=CARTESIAN_POINT ( 'NONE',  ( 0.7495606340400177148, -0.1264236179284866091, 1.660925196796630088 ) ) ;
#40570=FACE_OUTER_BOUND ( 'NONE', #15023, .T. ) ;
#40571=CARTESIAN_POINT ( 'NONE',  ( -0.7845359159668372495, 0.1324275479413869194, 1.980250702907100369 ) ) ;
#40574=CARTESIAN_POINT ( 'NONE',  ( 0.9873396505805591694, 0.1113553986120547346, 0.7529527557979842634 ) ) ;
#40575=CARTESIAN_POINT ( 'NONE',  ( 0.8019270111902717657, 0.1787899950787401604, 0.3100393700249766682 ) ) ;
#40576=CARTESIAN_POINT ( 'NONE',  ( 0.6971942568897648851, 0.07405724077823318263, 1.220472440891118504 ) ) ;
#40577=LINE ( 'NONE', #3935, #10876 ) ;
#40579=CARTESIAN_POINT ( 'NONE',  ( -1.033464566929133799, 0.000000000000000000, 0.9448818896562519720 ) ) ;
#40580=CARTESIAN_POINT ( 'NONE',  ( -1.054774247047244540, -0.07405724077823318263, 1.200787401521039355 ) ) ;
#40581=CARTESIAN_POINT ( 'NONE',  ( 0.7185039370078746268, 0.06523048226347956391, 0.6077755904436538126 ) ) ;
#40582=ORIENTED_EDGE ( 'NONE', *, *, #11167, .F. ) ;
#40587=CARTESIAN_POINT ( 'NONE',  ( -0.8107537697050253289, 0.1574803149606300301, 0.4847440943806614055 ) ) ;
#40590=CARTESIAN_POINT ( 'NONE',  ( 0.6971942568897637749, 2.189545951927499583E-17, 1.577263779473795369 ) ) ;
#40594=CARTESIAN_POINT ( 'NONE',  ( 0.9412147342319837628, -0.1574803149606297803, 1.331200787294047672 ) ) ;
#40597=CARTESIAN_POINT ( 'NONE',  ( 0.6971942568897648851, -0.07405724077823297447, 0.9153543306548987957 ) ) ;
#40599=CARTESIAN_POINT ( 'NONE',  ( -0.8759842519685039353, 0.1787899950787401882, 1.296751968450173154 ) ) ;
#40601=EDGE_CURVE ( 'NONE', #29380, #7257, #27958, .T. ) ;
#40603=CARTESIAN_POINT ( 'NONE',  ( -0.9500414927467378812, -0.1787899950787401604, 0.1771653542769452139 ) ) ;
#40608=CARTESIAN_POINT ( 'NONE',  ( 1.033464566929133799, 0.000000000000000000, 1.072834645669291431 ) ) ;
#40611=CARTESIAN_POINT ( 'NONE',  ( 0.7495606340400177148, 0.1264236179284866091, 1.021161417269070837 ) ) ;
#40612=CARTESIAN_POINT ( 'NONE',  ( -0.7495606340400177148, -0.1264236179284866091, 0.7554133857730077617 ) ) ;
#40613=CARTESIAN_POINT ( 'NONE',  ( -1.033464566929133799, 0.000000000000000000, 0.5905511809948347235 ) ) ;
#40615=CARTESIAN_POINT ( 'NONE',  ( -1.054774247047244540, 0.07405724077823318263, 1.761811023568284229 ) ) ;
#40617=VECTOR ( 'NONE', #26169, 39.37007874015748143 ) ;
#40619=CARTESIAN_POINT ( 'NONE',  ( -0.9873396505805591694, -0.1113553986120547346, 0.9498031496062993018 ) ) ;
#40622=DIRECTION ( 'NONE',  ( 1.822029033848725028E-16, 0.000000000000000000, 1.000000000000000000 ) ) ;
#40623=CARTESIAN_POINT ( 'NONE',  ( -0.7646288533564489232, -0.1113553986120547346, 1.520669291231054876 ) ) ;
#40624=CARTESIAN_POINT ( 'NONE',  ( 0.6971942568897626646, -0.07405724077823297447, 0.9547244093950547628 ) ) ;
#40625=CARTESIAN_POINT ( 'NONE',  ( 0.8759842519685039353, -0.1574803149606299191, 1.417322834645669216 ) ) ;
#40626=CARTESIAN_POINT ( 'NONE',  ( 0.7107006069439822937, 0.01204446385459368753, 1.983049284763879427 ) ) ;
#40628=CARTESIAN_POINT ( 'NONE',  ( 0.6971942568897648851, -0.07405724077823297447, 0.8710629920722218200 ) ) ;
#40632=DIRECTION ( 'NONE',  ( 1.822029033848725028E-16, 0.000000000000000000, 1.000000000000000000 ) ) ;
#40633=CARTESIAN_POINT ( 'NONE',  ( 0.7495606340400177148, 0.1264236179284866091, 1.178641732229700922 ) ) ;
#40637=( BOUNDED_CURVE ( )  B_SPLINE_CURVE ( 2, ( #36545, #44178, #40574, #3705, #3933, #18554, #90, #15456, #337 ),
 .UNSPECIFIED., .F., .T. ) 
 B_SPLINE_CURVE_WITH_KNOTS ( ( 3, 2, 2, 2, 3 ),
 ( 0.3599999999999999867, 0.3624999999999999889, 0.3649999999999999911, 0.3674999999999999933, 0.3699999999999999956 ),
 .UNSPECIFIED. ) 
 CURVE ( )  GEOMETRIC_REPRESENTATION_ITEM ( )  RATIONAL_B_SPLINE_CURVE ( ( 1.000000000000000000, 0.9238795325112869605, 1.000000000000000000, 0.9238795325112869605, 1.000000000000000000, 0.9238795325112869605, 1.000000000000000000, 0.9238795325112869605, 1.000000000000000000 ) ) 
 REPRESENTATION_ITEM ( '' )  ) ;
#40638=ORIENTED_EDGE ( 'NONE', *, *, #19536, .T. ) ;
#40640=CARTESIAN_POINT ( 'NONE',  ( -0.9500414927467378812, -0.1787899950787401604, 0.3297244093950552069 ) ) ;
#40642=CARTESIAN_POINT ( 'NONE',  ( -0.7646288533564489232, 0.1113553986120547346, 0.6151574803149606474 ) ) ;
#40645=CARTESIAN_POINT ( 'NONE',  ( -1.002407869896990045, 0.1264236179284866091, 1.680610236166708793 ) ) ;
#40646=EDGE_CURVE ( 'NONE', #43833, #758, #26643, .T. ) ;
#40647=CARTESIAN_POINT ( 'NONE',  ( -1.054774247047244096, 0.000000000000000000, 0.9276574802611967652 ) ) ;
#40648=VECTOR ( 'NONE', #41091, 39.37007874015748143 ) ;
#40649=CARTESIAN_POINT ( 'NONE',  ( -0.6971942568897626646, 0.07405724077823318263, 0.4773622046706456068 ) ) ;
#40650=EDGE_CURVE ( 'NONE', #19533, #8469, #8712, .T. ) ;
#40652=CARTESIAN_POINT ( 'NONE',  ( -0.9500414927467378812, -0.1787899950787401604, 1.988188976324187562 ) ) ;
#40654=CARTESIAN_POINT ( 'NONE',  ( 0.8759842519685039353, 0.1787899950787401882, 0.07135826766277185429 ) ) ;
#40658=CARTESIAN_POINT ( 'NONE',  ( -0.7646288533564489232, 0.1113553986120547346, 1.904527558947590515 ) ) ;
#40663=( BOUNDED_CURVE ( )  B_SPLINE_CURVE ( 2, ( #7343, #32765, #40141, #29895, #25322, #47362, #18585, #22175, #7096 ),
 .UNSPECIFIED., .F., .F. ) 
 B_SPLINE_CURVE_WITH_KNOTS ( ( 3, 2, 2, 2, 3 ),
 ( 0.8100000000000000533, 0.8125000000000000000, 0.8149999999999999467, 0.8175000000000000044, 0.8199999999999999512 ),
 .UNSPECIFIED. ) 
 CURVE ( )  GEOMETRIC_REPRESENTATION_ITEM ( )  RATIONAL_B_SPLINE_CURVE ( ( 1.000000000000000000, 0.9238795325112899581, 1.000000000000000000, 0.9238795325112869605, 1.000000000000000000, 0.9238795325112869605, 1.000000000000000000, 0.9238795325112829637, 1.000000000000000000 ) ) 
 REPRESENTATION_ITEM ( '' )  ) ;
#40664=CARTESIAN_POINT ( 'NONE',  ( -0.9500414927467378812, 0.1787899950787401604, 0.3838582676627718127 ) ) ;
#40666=CARTESIAN_POINT ( 'NONE',  ( -1.054774247047244540, 0.07405724077823318263, 1.407480314906865981 ) ) ;
#40672=CARTESIAN_POINT ( 'NONE',  ( 0.8759842519685039353, -0.1574803149606299191, 0.3937007874015748254 ) ) ;
#40673=CARTESIAN_POINT ( 'NONE',  ( 0.8759842519685039353, 0.000000000000000000, 4.498031496062992574 ) ) ;
#40674=CARTESIAN_POINT ( 'NONE',  ( -0.9412147342319837628, 0.1574803149606300301, 1.109744094380661572 ) ) ;
#40675=CARTESIAN_POINT ( 'NONE',  ( 0.9500414927467378812, 0.1787899950787401604, 0.4675196849856070869 ) ) ;
#40676=CARTESIAN_POINT ( 'NONE',  ( 0.8759842519685039353, 0.1574803149606299191, 0.5610236219397165547 ) ) ;
#40681=ORIENTED_EDGE ( 'NONE', *, *, #32698, .T. ) ;
#40682=CARTESIAN_POINT ( 'NONE',  ( 0.8759842519685039353, 0.1574803149606299191, 1.938976377845228249 ) ) ;
#40683=ORIENTED_EDGE ( 'NONE', *, *, #20363, .T. ) ;
#40685=CARTESIAN_POINT ( 'NONE',  ( -0.7495606340400177148, -0.1264236179284866091, 0.9965551180564724554 ) ) ;
#40686=CARTESIAN_POINT ( 'NONE',  ( 1.033464566929133799, 0.000000000000000000, 0.8759842519685039353 ) ) ;
#40688=CARTESIAN_POINT ( 'NONE',  ( -0.7185039370078739607, 1.928577636452523993E-17, 0.6988188976377952555 ) ) ;
#40689=CARTESIAN_POINT ( 'NONE',  ( -0.7185039370078739607, 1.928577636452523993E-17, 1.003937007766488199 ) ) ;
#40690=CARTESIAN_POINT ( 'NONE',  ( 0.6971942568897626646, -0.07405724077823297447, 0.5954724408911187261 ) ) ;
#40692=CARTESIAN_POINT ( 'NONE',  ( 0.9873396505805591694, 0.1113553986120547346, 1.274606299212598604 ) ) ;
#40697=CARTESIAN_POINT ( 'NONE',  ( 0.7185039370078739607, 1.928577636452523993E-17, 1.200787401467275695 ) ) ;
#40702=CARTESIAN_POINT ( 'NONE',  ( -1.002407869896990045, 0.1264236179284866091, 1.803641732229700700 ) ) ;
#40703=CARTESIAN_POINT ( 'NONE',  ( 0.8759842519685039353, 0.1787899950787401882, 1.729822834591905556 ) ) ;
#40704=CARTESIAN_POINT ( 'NONE',  ( -0.6971942568897626646, -0.07405724077823297447, 0.8366141731745828647 ) ) ;
#40706=CARTESIAN_POINT ( 'NONE',  ( 0.8019270111902717657, 0.1787899950787401604, 0.3543307086076538659 ) ) ;
#40707=CARTESIAN_POINT ( 'NONE',  ( -0.6971942568897648851, 0.07405724077823318263, 1.299212598371434435 ) ) ;
#40708=AXIS2_PLACEMENT_3D ( 'NONE', #32902, #19, #29343 ) ;
#40709=CARTESIAN_POINT ( 'NONE',  ( -0.9500414927467378812, 0.1787899950787401604, 0.8956692912848198684 ) ) ;
#40710=CARTESIAN_POINT ( 'NONE',  ( 0.9873396505805591694, 0.1113553986120547346, 0.9104330707586141269 ) ) ;
#40713=CARTESIAN_POINT ( 'NONE',  ( -1.002407869896990045, -0.1264236179284866091, 1.636318897584031484 ) ) ;
#40714=CARTESIAN_POINT ( 'NONE',  ( -0.8107537697050253289, -0.1574803149606297803, 1.877460629813732407 ) ) ;
#40715=EDGE_LOOP ( 'NONE', ( #43988, #10408, #595, #24954 ) ) ;
#40717=CARTESIAN_POINT ( 'NONE',  ( 0.7646288533564489232, -0.1113553986120547346, 0.9694881888688504645 ) ) ;
#40718=CARTESIAN_POINT ( 'NONE',  ( 0.9500414927467377701, 0.1787899950787401604, 1.609251968450173598 ) ) ;
#40720=CARTESIAN_POINT ( 'NONE',  ( 0.7646288533564489232, 0.1113553986120547346, 0.2116141731208196763 ) ) ;
#40721=EDGE_CURVE ( 'NONE', #7257, #46851, #9189, .T. ) ;
#40722=AXIS2_PLACEMENT_3D ( 'NONE', #41141, #4482, #19122 ) ;
#40725=EDGE_CURVE ( 'NONE', #7448, #10459, #5953, .T. ) ;
#40728=VERTEX_POINT ( 'NONE', #16398 ) ;
#40732=VERTEX_POINT ( 'NONE', #16845 ) ;
#40734=CARTESIAN_POINT ( 'NONE',  ( 1.054774247047244540, 0.07405724077823318263, 1.717519684985606476 ) ) ;
#40739=CARTESIAN_POINT ( 'NONE',  ( 1.054774247047244096, 0.000000000000000000, 0.8095472440407244230 ) ) ;
#40741=CARTESIAN_POINT ( 'NONE',  ( -0.7185039370078766252, -0.06523048226348168721, 1.557578740049954558 ) ) ;
#40742=CARTESIAN_POINT ( 'NONE',  ( 0.7185039370078739607, 1.928577636452523993E-17, 0.1476377952755905387 ) ) ;
#40744=CARTESIAN_POINT ( 'NONE',  ( 0.7495606340400177148, -0.1264236179284866091, 1.862696850339937038 ) ) ;
#40745=CARTESIAN_POINT ( 'NONE',  ( 0.9873396505805591694, -0.1113553986120547346, 1.884842519577511810 ) ) ;
#40747=AXIS2_PLACEMENT_3D ( 'NONE', #40519, #7708, #18728 ) ;
#40748=CARTESIAN_POINT ( 'NONE',  ( 1.033464566929134687, 0.06523048226347956391, 0.09104330708661413640 ) ) ;
#40751=CARTESIAN_POINT ( 'NONE',  ( -0.7495606340400177148, -0.1264236179284866091, 0.4060039369541102450 ) ) ;
#40754=CARTESIAN_POINT ( 'NONE',  ( 0.7495606340400177148, -0.1264236179284866091, 0.2485236219934806867 ) ) ;
#40756=CARTESIAN_POINT ( 'NONE',  ( -0.6971942568897648851, 0.07405724077823318263, 1.811023621993480548 ) ) ;
#40758=VECTOR ( 'NONE', #19303, 39.37007874015748143 ) ;
#40759=CARTESIAN_POINT ( 'NONE',  ( -0.8019270111902717657, 0.1787899950787401604, 1.102362204670646495 ) ) ;
#40762=CARTESIAN_POINT ( 'NONE',  ( 0.9500414927467378812, -0.1787899950787401604, 1.943897637741510254 ) ) ;
#40763=CARTESIAN_POINT ( 'NONE',  ( -0.6971942568897648851, -0.07405724077823297447, 0.9891732282926934960 ) ) ;
#40766=CARTESIAN_POINT ( 'NONE',  ( 1.002407869896990045, 0.1264236179284866091, 0.5044291338045039375 ) ) ;
#40767=CARTESIAN_POINT ( 'NONE',  ( -0.8019270111902716547, -0.1787899950787401604, 0.4035433070328507954 ) ) ;
#40768=CARTESIAN_POINT ( 'NONE',  ( -0.9500414927467378812, -0.1787899950787401604, 0.8021653542769460188 ) ) ;
#40770=ADVANCED_FACE ( 'NONE', ( #31486 ), #41751, .T. ) ;
#40772=CARTESIAN_POINT ( 'NONE',  ( -0.8107537697050253289, 0.1574803149606300301, 0.2189960629921262614 ) ) ;
#40773=CARTESIAN_POINT ( 'NONE',  ( 1.002407869896990045, 0.1264236179284866091, 1.094980314906866203 ) ) ;
#40774=CARTESIAN_POINT ( 'NONE',  ( -0.8019270111902716547, 0.1787899950787401604, 1.963582677111591401 ) ) ;
#40775=ORIENTED_EDGE ( 'NONE', *, *, #8109, .F. ) ;
#40778=( BOUNDED_CURVE ( )  B_SPLINE_CURVE ( 2, ( #23744, #2625, #42859, #35257, #27610, #34533, #9128, #42165, #5526 ),
 .UNSPECIFIED., .F., .T. ) 
 B_SPLINE_CURVE_WITH_KNOTS ( ( 3, 2, 2, 2, 3 ),
 ( 0.2999999999999999889, 0.3024999999999999911, 0.3049999999999999933, 0.3074999999999999956, 0.3099999999999999978 ),
 .UNSPECIFIED. ) 
 CURVE ( )  GEOMETRIC_REPRESENTATION_ITEM ( )  RATIONAL_B_SPLINE_CURVE ( ( 1.000000000000000000, 0.9238795325112869605, 1.000000000000000000, 0.9238795325112869605, 1.000000000000000000, 0.9238795325112869605, 1.000000000000000000, 0.9238795325112869605, 1.000000000000000000 ) ) 
 REPRESENTATION_ITEM ( '' )  ) ;
#40779=AXIS2_PLACEMENT_3D ( 'NONE', #24280, #38413, #38875 ) ;
#40780=CARTESIAN_POINT ( 'NONE',  ( -0.7495606340400177148, 0.1264236179284866091, 0.07627952750529173875 ) ) ;
#40784=CARTESIAN_POINT ( 'NONE',  ( -0.9873396505805591694, 0.1113553986120547346, 1.697834645561763889 ) ) ;
#40785=CARTESIAN_POINT ( 'NONE',  ( 0.8759842519685039353, 0.1787899950787401882, 1.173720472387181246 ) ) ;
#40788=CARTESIAN_POINT ( 'NONE',  ( 1.033464566929133799, 0.000000000000000000, 1.584645669291338654 ) ) ;
#40790=CARTESIAN_POINT ( 'NONE',  ( 0.8759842519685039353, 0.1787899950787401882, 0.2288385826234019815 ) ) ;
#40794=CARTESIAN_POINT ( 'NONE',  ( -0.9873396505805591694, -0.1113553986120547346, 1.136811023514519681 ) ) ;
#40795=ORIENTED_EDGE ( 'NONE', *, *, #9828, .T. ) ;
#40797=CARTESIAN_POINT ( 'NONE',  ( -0.6971942568897648851, 0.07405724077823318263, 0.6348425196312760255 ) ) ;
#40801=CARTESIAN_POINT ( 'NONE',  ( 0.9500414927467378812, -0.1787899950787401604, 1.437007873961985371 ) ) ;
#40802=CARTESIAN_POINT ( 'NONE',  ( 0.8759842519685039353, -0.1787899950787401882, 1.705216535379307174 ) ) ;
#40804=CARTESIAN_POINT ( 'NONE',  ( 0.7185039370078739607, 0.000000000000000000, 4.498031496062992574 ) ) ;
#40807=CARTESIAN_POINT ( 'NONE',  ( 0.8759842519685039353, 0.1787899950787401882, 1.252460629867496067 ) ) ;
#40808=CARTESIAN_POINT ( 'NONE',  ( -1.033464566929133799, 0.000000000000000000, 0.1968503935932602311 ) ) ;
#40809=CARTESIAN_POINT ( 'NONE',  ( 1.033464566929133799, 0.000000000000000000, 0.2854330708661417804 ) ) ;
#40810=CARTESIAN_POINT ( 'NONE',  ( -0.9500414927467378812, 0.1787899950787401604, 1.210629921206079818 ) ) ;
#40811=CARTESIAN_POINT ( 'NONE',  ( 0.7185039370078739607, 1.928577636452523993E-17, 0.6102362203649134287 ) ) ;
#40817=CARTESIAN_POINT ( 'NONE',  ( -0.9873396505805591694, -0.1113553986120547346, 0.3100393699712130080 ) ) ;
#40820=CARTESIAN_POINT ( 'NONE',  ( 0.7495606340400177148, -0.1264236179284866091, 1.660925196796630088 ) ) ;
#40821=CARTESIAN_POINT ( 'NONE',  ( -0.7646288533564489232, -0.1113553986120547346, 1.087598425089322918 ) ) ;
#40823=CARTESIAN_POINT ( 'NONE',  ( -0.9873396505805591694, -0.1113553986120547346, 1.382874015748031704 ) ) ;
#40824=CARTESIAN_POINT ( 'NONE',  ( 0.8019270111902716547, -0.1787899950787401604, 0.05413385821395302888 ) ) ;
#40825=CARTESIAN_POINT ( 'NONE',  ( -1.054774247047244540, -0.07405724077823318263, 0.05905511805647267048 ) ) ;
#40827=ORIENTED_EDGE ( 'NONE', *, *, #36465, .T. ) ;
#40828=ADVANCED_FACE ( 'NONE', ( #23807 ), #45589, .T. ) ;
#40832=CARTESIAN_POINT ( 'NONE',  ( 0.6971942568897626646, -0.07405724077823297447, 0.6791338582139527791 ) ) ;
#40833=CARTESIAN_POINT ( 'NONE',  ( 0.8019270111902716547, 0.1787899950787401604, 0.8267716534895444003 ) ) ;
#40834=CARTESIAN_POINT ( 'NONE',  ( -1.054774247047244096, 0.000000000000000000, 1.557578740103716441 ) ) ;
#40836=CARTESIAN_POINT ( 'NONE',  ( -0.6971942568897648851, 0.07405724077823318263, 1.225393700733637514 ) ) ;
#40837=EDGE_CURVE ( 'NONE', #42967, #3817, #7492, .T. ) ;
#40838=CARTESIAN_POINT ( 'NONE',  ( -0.6971942568897626646, -0.07405724077823297447, 0.3248031495525359746 ) ) ;
#40840=FACE_OUTER_BOUND ( 'NONE', #39296, .T. ) ;
#40842=ORIENTED_EDGE ( 'NONE', *, *, #24157, .T. ) ;
#40844=VERTEX_POINT ( 'NONE', #46072 ) ;
#40846=CARTESIAN_POINT ( 'NONE',  ( 0.9412147342319837628, -0.1574803149606297803, 1.213090551073575662 ) ) ;
#40847=FACE_OUTER_BOUND ( 'NONE', #23232, .T. ) ;
#40848=CARTESIAN_POINT ( 'NONE',  ( 1.033464566929133799, 0.000000000000000000, 1.417322834538141674 ) ) ;
#40850=CARTESIAN_POINT ( 'NONE',  ( -0.9500414927467377701, -0.1787899950787401604, 0.1771653542769452416 ) ) ;
#40851=CARTESIAN_POINT ( 'NONE',  ( -0.8759842519685039353, 0.1574803149606299191, 0.8464566929133857665 ) ) ;
#40855=CARTESIAN_POINT ( 'NONE',  ( -0.8107537697050253289, -0.1574803149606297803, 1.523129921152316379 ) ) ;
#40857=CARTESIAN_POINT ( 'NONE',  ( 0.6971942568897637749, 2.189545951927499583E-17, 0.9916338582139527791 ) ) ;
#40858=CARTESIAN_POINT ( 'NONE',  ( 0.7495606340400177148, 0.1264236179284866091, 1.336122047190330786 ) ) ;
#40860=CARTESIAN_POINT ( 'NONE',  ( 0.9412147342319837628, -0.1574803149606297803, 1.341043307086615455 ) ) ;
#40861=CARTESIAN_POINT ( 'NONE',  ( 0.7265838559950141828, -0.07822853150185864191, 1.984785922399904701 ) ) ;
#40862=CARTESIAN_POINT ( 'NONE',  ( -1.033464566929133799, 0.000000000000000000, 0.04921259842519685318 ) ) ;
#40864=CARTESIAN_POINT ( 'NONE',  ( 1.002407869896990045, -0.1264236179284866091, 0.8046259841982047467 ) ) ;
#40868=EDGE_CURVE ( 'NONE', #5152, #22068, #6790, .T. ) ;
#40871=CARTESIAN_POINT ( 'NONE',  ( 1.002407869896990045, 0.1264236179284866091, 1.208169291284818980 ) ) ;
#40879=CARTESIAN_POINT ( 'NONE',  ( -0.8759842519685039353, 0.1787899950787401882, 0.2682086613635594752 ) ) ;
#40882=CARTESIAN_POINT ( 'NONE',  ( 1.033464566929134687, 0.06523048226347956391, 1.744586614173228245 ) ) ;
#40885=CARTESIAN_POINT ( 'NONE',  ( -1.033464566929133799, 0.000000000000000000, 1.860236220472440971 ) ) ;
#40886=CARTESIAN_POINT ( 'NONE',  ( -1.002407869896990045, 0.1264236179284866091, 1.877460629867496067 ) ) ;
#40887=CARTESIAN_POINT ( 'NONE',  ( -1.002407869896990045, -0.1264236179284866091, 0.8833661416785196785 ) ) ;
#40889=CARTESIAN_POINT ( 'NONE',  ( -0.6971942568897626646, 0.07405724077823318263, 0.5167322834108034613 ) ) ;
#40890=CARTESIAN_POINT ( 'NONE',  ( -0.9873396505805591694, -0.1113553986120547346, 0.1131889762704257896 ) ) ;
#40897=CARTESIAN_POINT ( 'NONE',  ( 1.033464566929133799, 0.000000000000000000, 1.781496062992125928 ) ) ;
#40899=CARTESIAN_POINT ( 'NONE',  ( -1.054774247047244096, 0.000000000000000000, 0.2977362204186775885 ) ) ;
#40901=EDGE_LOOP ( 'NONE', ( #44538, #25176, #4474, #21296 ) ) ;
#40903=ORIENTED_EDGE ( 'NONE', *, *, #8277, .T. ) ;
#40907=CARTESIAN_POINT ( 'NONE',  ( 1.033464566929134687, -0.06523048226347956391, 0.4404527559055117503 ) ) ;
#40910=CARTESIAN_POINT ( 'NONE',  ( -0.9412147342319837628, -0.1574803149606297803, 1.134350393593259509 ) ) ;
#40911=CARTESIAN_POINT ( 'NONE',  ( 0.8019270111902717657, -0.1787899950787401604, 0.4872047243556847929 ) ) ;
#40913=CIRCLE ( 'NONE', #10381, 0.1574803149606299191 ) ;
#40915=CARTESIAN_POINT ( 'NONE',  ( 0.8107537697050253289, 0.1574803149606300301, 1.941437007766490863 ) ) ;
#40916=ORIENTED_EDGE ( 'NONE', *, *, #27742, .T. ) ;
#40919=CARTESIAN_POINT ( 'NONE',  ( -0.8019270111902716547, -0.1787899950787401604, 0.9202755904974182499 ) ) ;
#40920=CARTESIAN_POINT ( 'NONE',  ( 1.033464566929134687, 0.06523048226347956391, 0.8784448818897642175 ) ) ;
#40927=CARTESIAN_POINT ( 'NONE',  ( 0.9412147342319837628, 0.1574803149606300301, 1.277066929133857442 ) ) ;
#40928=CARTESIAN_POINT ( 'NONE',  ( -1.033464566929133799, 0.000000000000000000, 0.9940944881889764995 ) ) ;
#40932=CARTESIAN_POINT ( 'NONE',  ( 0.8759842519685039353, 0.1574803149606299191, 1.112204724301921299 ) ) ;
#40934=CARTESIAN_POINT ( 'NONE',  ( -1.002407869896990045, 0.1264236179284866091, 0.4601377952218267953 ) ) ;
#40936=ORIENTED_EDGE ( 'NONE', *, *, #2376, .F. ) ;
#40937=CARTESIAN_POINT ( 'NONE',  ( -0.7495606340400177148, -0.1264236179284866091, 1.705216535379307174 ) ) ;
#40938=CARTESIAN_POINT ( 'NONE',  ( 0.8019270111902717657, 0.1787899950787401604, 1.653543307032850462 ) ) ;
#40940=CARTESIAN_POINT ( 'NONE',  ( -0.7495606340400177148, -0.1264236179284866091, 0.8784448818360000022 ) ) ;
#40943=CARTESIAN_POINT ( 'NONE',  ( -0.9500414927467377701, -0.1787899950787401604, 1.313976377898992132 ) ) ;
#40944=CARTESIAN_POINT ( 'NONE',  ( -0.6971942568897637749, 2.189545951927499583E-17, 0.9473425196312755814 ) ) ;
#40945=CARTESIAN_POINT ( 'NONE',  ( -0.6971942568897626646, 0.07405724077823318263, 0.1624015747493861295 ) ) ;
#40946=( BOUNDED_CURVE ( )  B_SPLINE_CURVE ( 2, ( #26753, #23145, #15027, #11666, #44919, #8514, #41079, #19301, #41314 ),
 .UNSPECIFIED., .F., .F. ) 
 B_SPLINE_CURVE_WITH_KNOTS ( ( 3, 2, 2, 2, 3 ),
 ( 0.1100000000000000006, 0.1125000000000000028, 0.1150000000000000050, 0.1174999999999999933, 0.1199999999999999956 ),
 .UNSPECIFIED. ) 
 CURVE ( )  GEOMETRIC_REPRESENTATION_ITEM ( )  RATIONAL_B_SPLINE_CURVE ( ( 1.000000000000000000, 0.9238795325112869605, 1.000000000000000000, 0.9238795325112869605, 1.000000000000000000, 0.9238795325112869605, 1.000000000000000000, 0.9238795325112869605, 1.000000000000000000 ) ) 
 REPRESENTATION_ITEM ( '' )  ) ;
#40948=CARTESIAN_POINT ( 'NONE',  ( -0.6971942568897637749, 2.189545951927499583E-17, 1.621555118056472455 ) ) ;
#40949=CARTESIAN_POINT ( 'NONE',  ( -0.6971942568897626646, 0.07405724077823318263, 0.04429133852891373180 ) ) ;
#40953=CARTESIAN_POINT ( 'NONE',  ( -0.9873396505805591694, -0.1113553986120547346, 1.540354330708661568 ) ) ;
#40954=( BOUNDED_CURVE ( )  B_SPLINE_CURVE ( 2, ( #16517, #16052, #34262, #26837, #27328, #12464, #9565, #38552, #5233 ),
 .UNSPECIFIED., .F., .T. ) 
 B_SPLINE_CURVE_WITH_KNOTS ( ( 3, 2, 2, 2, 3 ),
 ( 0.4299999999999999933, 0.4324999999999999956, 0.4349999999999999978, 0.4375000000000000000, 0.4400000000000000022 ),
 .UNSPECIFIED. ) 
 CURVE ( )  GEOMETRIC_REPRESENTATION_ITEM ( )  RATIONAL_B_SPLINE_CURVE ( ( 1.000000000000000000, 0.9238795325112869605, 1.000000000000000000, 0.9238795325112869605, 1.000000000000000000, 0.9238795325112869605, 1.000000000000000000, 0.9238795325112869605, 1.000000000000000000 ) ) 
 REPRESENTATION_ITEM ( '' )  ) ;
#40955=DIRECTION ( 'NONE',  ( 0.000000000000000000, 0.000000000000000000, -1.000000000000000000 ) ) ;
#40956=CARTESIAN_POINT ( 'NONE',  ( 1.054774247047244096, 0.000000000000000000, 1.641240157426551161 ) ) ;
#40963=EDGE_LOOP ( 'NONE', ( #29555, #18625, #42490, #12871 ) ) ;
#40966=VERTEX_POINT ( 'NONE', #47262 ) ;
#40969=CARTESIAN_POINT ( 'NONE',  ( 0.8759842519685039353, -0.1787899950787401882, 1.705216535379307174 ) ) ;
#40976=CARTESIAN_POINT ( 'NONE',  ( 0.8759842519685039353, -0.1787899950787401882, 0.8390748030958424808 ) ) ;
#40978=CARTESIAN_POINT ( 'NONE',  ( -1.054774247047244096, 0.000000000000000000, 1.995570866087968520 ) ) ;
#40981=CARTESIAN_POINT ( 'NONE',  ( -0.8107537697050254399, 0.1574803149606300301, 1.311515747923968744 ) ) ;
#40982=CARTESIAN_POINT ( 'NONE',  ( 1.054774247047244540, -0.07405724077823318263, 1.756889763725764553 ) ) ;
#40985=EDGE_CURVE ( 'NONE', #39852, #17493, #21198, .T. ) ;
#40986=CARTESIAN_POINT ( 'NONE',  ( 1.033464566929133799, 0.000000000000000000, 0.1279527559055118058 ) ) ;
#40991=CARTESIAN_POINT ( 'NONE',  ( 0.8019270111902717657, 0.1787899950787401604, 0.2755905511273391006 ) ) ;
#40993=CARTESIAN_POINT ( 'NONE',  ( -1.054774247047244540, 0.07405724077823318263, 1.717519684985606476 ) ) ;
#40994=VERTEX_POINT ( 'NONE', #43118 ) ;
#40995=CARTESIAN_POINT ( 'NONE',  ( -0.9500414927467378812, -0.1787899950787401604, 1.240157480261197431 ) ) ;
#40997=CARTESIAN_POINT ( 'NONE',  ( -1.002407869896990045, 0.1264236179284866091, 0.5044291338045039375 ) ) ;
#40998=CARTESIAN_POINT ( 'NONE',  ( -0.8759842519685039353, -0.1787899950787401882, 1.075295275536787276 ) ) ;
#41000=CARTESIAN_POINT ( 'NONE',  ( 1.033464566929133799, 1.928577636452524610E-17, 2.007874015640504162 ) ) ;
#41001=CARTESIAN_POINT ( 'NONE',  ( 0.8759842519685039353, -0.1787899950787401882, 0.4109251967966299213 ) ) ;
#41002=CARTESIAN_POINT ( 'NONE',  ( -0.6971942568897648851, 0.07405724077823318263, 0.3543307086076538659 ) ) ;
#41003=CARTESIAN_POINT ( 'NONE',  ( 0.9873396505805591694, -0.1113553986120547346, 1.687992125876724536 ) ) ;
#41005=DIRECTION ( 'NONE',  ( 1.822029033848725028E-16, 0.000000000000000000, 1.000000000000000000 ) ) ;
#41006=CARTESIAN_POINT ( 'NONE',  ( 0.6971942568897626646, 0.07405724077823318263, 0.9104330708123776761 ) ) ;
#41007=CARTESIAN_POINT ( 'NONE',  ( -0.7185039370078746268, 0.06523048226347956391, 0.1058070866141733041 ) ) ;
#41008=CARTESIAN_POINT ( 'NONE',  ( 0.9500414927467377701, 0.1787899950787401604, 1.215551181048599272 ) ) ;
#41009=CARTESIAN_POINT ( 'NONE',  ( -0.6971942568897648851, -0.07405724077823297447, 1.973425196796630088 ) ) ;
#41013=CARTESIAN_POINT ( 'NONE',  ( -1.033464566929133799, 0.000000000000000000, 0.2066929133858267931 ) ) ;
#41015=EDGE_LOOP ( 'NONE', ( #11297, #25737, #30304, #42378 ) ) ;
#41018=CARTESIAN_POINT ( 'NONE',  ( -0.7185039370078739607, 1.928577636452523993E-17, 1.712598425089322918 ) ) ;
#41020=CARTESIAN_POINT ( 'NONE',  ( 1.002407869896990045, -0.1264236179284866091, 1.355807086560409491 ) ) ;
#41022=CARTESIAN_POINT ( 'NONE',  ( -1.033464566929133799, 0.000000000000000000, 0.1279527559055118058 ) ) ;
#41023=CARTESIAN_POINT ( 'NONE',  ( 0.6971942568897648851, 0.07405724077823318263, 1.535433070812378675 ) ) ;
#41024=CARTESIAN_POINT ( 'NONE',  ( 1.054774247047244540, 0.07405724077823318263, 0.1033464566391498751 ) ) ;
#41029=EDGE_CURVE ( 'NONE', #12184, #39650, #21319, .T. ) ;
#41030=CARTESIAN_POINT ( 'NONE',  ( -0.9500414927467377701, -0.1787899950787401604, 0.7283464566391492090 ) ) ;
#41034=FACE_OUTER_BOUND ( 'NONE', #35407, .T. ) ;
#41036=CARTESIAN_POINT ( 'NONE',  ( 0.7495606340400177148, -0.1264236179284866091, 1.350885826717889815 ) ) ;
#41037=CARTESIAN_POINT ( 'NONE',  ( 0.8759842519685039353, -0.1787899950787401882, 1.783956692859621995 ) ) ;
#41038=CARTESIAN_POINT ( 'NONE',  ( -0.7185039370078739607, 1.928577636452523993E-17, 1.909448818790110192 ) ) ;
#41040=EDGE_CURVE ( 'NONE', #32014, #18349, #39532, .T. ) ;
#41043=CARTESIAN_POINT ( 'NONE',  ( -0.9412147342319837628, -0.1574803149606297803, 1.931594488188976166 ) ) ;
#41045=CARTESIAN_POINT ( 'NONE',  ( 0.7495606340400177148, -0.1264236179284866091, 0.3617125983714334359 ) ) ;
#41046=CARTESIAN_POINT ( 'NONE',  ( 0.7411008755701128381, -0.09968592455682778741, 0.03937258286176098521 ) ) ;
#41048=CARTESIAN_POINT ( 'NONE',  ( 0.7185039370078746268, 0.06523048226347956391, 0.6471456691838121111 ) ) ;
#41050=CARTESIAN_POINT ( 'NONE',  ( 1.033464566929131356, 0.06523048226348168721, 1.390255905511812218 ) ) ;
#41051=CARTESIAN_POINT ( 'NONE',  ( 0.7185039370078741827, 0.06523048226347841205, 0.6963582677165353063 ) ) ;
#41055=CARTESIAN_POINT ( 'NONE',  ( -1.033464566929133799, 0.000000000000000000, 1.545275590551181244 ) ) ;
#41056=CARTESIAN_POINT ( 'NONE',  ( 1.054774247047244540, 0.07405724077823318263, 1.599409448765135133 ) ) ;
#41057=CARTESIAN_POINT ( 'NONE',  ( -0.8107537697050253289, -0.1574803149606297803, 1.218011811023622437 ) ) ;
#41060=CARTESIAN_POINT ( 'NONE',  ( -0.9412147342319837628, -0.1574803149606297803, 0.4355314960629916299 ) ) ;
#41061=CARTESIAN_POINT ( 'NONE',  ( 0.9412147342319837628, -0.1574803149606297803, 1.921751968396409493 ) ) ;
#41063=CARTESIAN_POINT ( 'NONE',  ( 0.7646288533564489232, 0.1113553986120547346, 1.313976377845228249 ) ) ;
#41066=CARTESIAN_POINT ( 'NONE',  ( -0.6971942568897637749, 2.189545951927499583E-17, 1.577263779473795369 ) ) ;
#41068=CARTESIAN_POINT ( 'NONE',  ( -0.7495606340400177148, 0.1264236179284866091, 1.301673228292692830 ) ) ;
#41069=ORIENTED_EDGE ( 'NONE', *, *, #37062, .F. ) ;
#41071=CARTESIAN_POINT ( 'NONE',  ( -0.6971942568897626646, -0.07405724077823297447, 0.2854330708123783422 ) ) ;
#41075=ORIENTED_EDGE ( 'NONE', *, *, #20175, .T. ) ;
#41078=CARTESIAN_POINT ( 'NONE',  ( 0.9500414927467378812, -0.1787899950787401604, 1.038385826717890259 ) ) ;
#41079=CARTESIAN_POINT ( 'NONE',  ( -0.9873396505805591694, -0.1113553986120547346, 0.2706692912310554866 ) ) ;
#41080=CARTESIAN_POINT ( 'NONE',  ( 0.7646288533564489232, -0.1113553986120547346, 0.1033464565853864231 ) ) ;
#41081=CARTESIAN_POINT ( 'NONE',  ( -1.033464566929133799, 1.928577636452524610E-17, 2.869337061179095023E-17 ) ) ;
#41084=CARTESIAN_POINT ( 'NONE',  ( -0.6971942568897626646, -0.07405724077823297447, 0.2460629920722207653 ) ) ;
#41085=CARTESIAN_POINT ( 'NONE',  ( -0.9873396505805591694, 0.1113553986120547346, 0.8809055118110236116 ) ) ;
#41088=CARTESIAN_POINT ( 'NONE',  ( 0.9412147342319837628, 0.1574803149606300301, 0.4109251968503938590 ) ) ;
#41089=CARTESIAN_POINT ( 'NONE',  ( -0.9412147342319837628, 0.1574803149606300301, 1.542814960522393308 ) ) ;
#41090=CARTESIAN_POINT ( 'NONE',  ( 1.002407869896990045, -0.1264236179284866091, 0.8489173227808819444 ) ) ;
#41091=DIRECTION ( 'NONE',  ( 0.000000000000000000, 0.000000000000000000, 1.000000000000000000 ) ) ;
#41093=CARTESIAN_POINT ( 'NONE',  ( 1.033464566929134687, 0.06523048226347956391, 1.429625984251968074 ) ) ;
#41094=CARTESIAN_POINT ( 'NONE',  ( 0.7179901938900657976, 0.04576715322243130046, 1.982392704978442666 ) ) ;
#41095=CARTESIAN_POINT ( 'NONE',  ( -1.033464566929133799, 0.000000000000000000, 1.860236220472440971 ) ) ;
#41096=CARTESIAN_POINT ( 'NONE',  ( 0.8759842519685039353, 0.000000000000000000, 4.498031496062992574 ) ) ;
#41098=CARTESIAN_POINT ( 'NONE',  ( -1.033464566929133799, 0.000000000000000000, 1.545275590551181244 ) ) ;
#41099=CARTESIAN_POINT ( 'NONE',  ( 0.6971942568897648851, -0.07405724077823297447, 0.8316929133320636325 ) ) ;
#41100=DIRECTION ( 'NONE',  ( 1.000000000000000000, 0.000000000000000000, -1.822029033848725275E-16 ) ) ;
#41101=CARTESIAN_POINT ( 'NONE',  ( 0.6971942568897648851, -0.07405724077823297447, 1.781496062938362934 ) ) ;
#41103=CARTESIAN_POINT ( 'NONE',  ( 0.7185039370078739607, 1.928577636452523993E-17, 0.7381889763779527769 ) ) ;
#41106=CARTESIAN_POINT ( 'NONE',  ( 1.033464566929133799, 0.000000000000000000, 1.899606299212598604 ) ) ;
#41107=CARTESIAN_POINT ( 'NONE',  ( -1.033464566929133799, 0.000000000000000000, 0.03937007863263043694 ) ) ;
#41108=CARTESIAN_POINT ( 'NONE',  ( 1.054774247047244096, 0.000000000000000000, 1.203248031442299304 ) ) ;
#41109=CARTESIAN_POINT ( 'NONE',  ( -0.7646288533564489232, 0.1113553986120547346, 1.048228346456692828 ) ) ;
#41112=CARTESIAN_POINT ( 'NONE',  ( -0.6971942568897626646, -0.07405724077823297447, 0.5167322834108034613 ) ) ;
#41113=ORIENTED_EDGE ( 'NONE', *, *, #27906, .F. ) ;
#41115=CARTESIAN_POINT ( 'NONE',  ( -0.9500414927467378812, 0.1787899950787401604, 0.3051181101824569919 ) ) ;
#41120=CARTESIAN_POINT ( 'NONE',  ( -0.9500414927467378812, 0.1787899950787401604, 1.801181102308441861 ) ) ;
#41121=CARTESIAN_POINT ( 'NONE',  ( -0.8759842519685039353, -0.1787899950787401882, 0.9571850393163149340 ) ) ;
#41122=CARTESIAN_POINT ( 'NONE',  ( -0.6971942568897626646, -0.07405724077823297447, 0.5216535432533228045 ) ) ;
#41127=CARTESIAN_POINT ( 'NONE',  ( 0.9412147342319837628, -0.1574803149606297803, 1.931594488188976166 ) ) ;
#41128=VECTOR ( 'NONE', #35964, 39.37007874015748143 ) ;
#41129=CARTESIAN_POINT ( 'NONE',  ( -0.6971942568897637749, 2.189545951927499583E-17, 0.4355314960092284138 ) ) ;
#41135=CARTESIAN_POINT ( 'NONE',  ( -0.8759842519685039353, -0.1787899950787401882, 1.513287401521039355 ) ) ;
#41139=ADVANCED_FACE ( 'NONE', ( #15261 ), #604, .T. ) ;
#41140=SURFACE_SIDE_STYLE ('',( #15562 ) ) ;
#41141=CARTESIAN_POINT ( 'NONE',  ( -0.8759842519685039353, 0.000000000000000000, 0.000000000000000000 ) ) ;
#41143=CARTESIAN_POINT ( 'NONE',  ( -0.8759842519685039353, -0.1574803149606299191, 1.092519684931842594 ) ) ;
#41144=CARTESIAN_POINT ( 'NONE',  ( 0.8759842519685039353, -0.1574803149606299191, 1.761811023514519459 ) ) ;
#41145=CARTESIAN_POINT ( 'NONE',  ( 0.7646288533564489232, -0.1113553986120547346, 1.914370078632629868 ) ) ;
#41147=CARTESIAN_POINT ( 'NONE',  ( 1.033464566929133799, 0.000000000000000000, 1.033464566929133799 ) ) ;
#41148=CARTESIAN_POINT ( 'NONE',  ( -0.9500414927467377701, -0.1787899950787401604, 1.082677165300567346 ) ) ;
#41149=CARTESIAN_POINT ( 'NONE',  ( 0.8107537697050253289, 0.1574803149606300301, 0.8882874015748027929 ) ) ;
#41150=CARTESIAN_POINT ( 'NONE',  ( 0.9412147342319837628, 0.1574803149606300301, 1.355807086614173596 ) ) ;
#41151=CARTESIAN_POINT ( 'NONE',  ( 0.8759842519685039353, 0.000000000000000000, 4.498031496062992574 ) ) ;
#41153=CARTESIAN_POINT ( 'NONE',  ( -0.9873396505805591694, -0.1113553986120547346, 1.264763779527559029 ) ) ;
#41159=DIRECTION ( 'NONE',  ( 1.822029033848725028E-16, 0.000000000000000000, 1.000000000000000000 ) ) ;
#41164=CARTESIAN_POINT ( 'NONE',  ( 0.9412147342319837628, -0.1574803149606297803, 1.134350393593259509 ) ) ;
#41166=ORIENTED_EDGE ( 'NONE', *, *, #10414, .T. ) ;
#41167=ORIENTED_EDGE ( 'NONE', *, *, #25337, .T. ) ;
#41168=CARTESIAN_POINT ( 'NONE',  ( -0.8759842519685039353, -0.1787899950787401882, 1.710137795221826851 ) ) ;
#41169=CARTESIAN_POINT ( 'NONE',  ( 0.7495606340400177148, -0.1264236179284866091, 1.705216535379307174 ) ) ;
#41171=CARTESIAN_POINT ( 'NONE',  ( -0.8019270111902717657, -0.1787899950787401604, 0.8809055117572599514 ) ) ;
#41173=CARTESIAN_POINT ( 'NONE',  ( -1.054774247047244540, 0.07405724077823318263, 1.323818897584032817 ) ) ;
#41175=CARTESIAN_POINT ( 'NONE',  ( -0.7495606340400177148, -0.1264236179284866091, 1.188484251914740275 ) ) ;
#41176=CARTESIAN_POINT ( 'NONE',  ( -0.7495606340400177148, -0.1264236179284866091, 0.9128937007336377363 ) ) ;
#41177=CARTESIAN_POINT ( 'NONE',  ( -0.9412147342319837628, 0.1574803149606300301, 1.660925196742867982 ) ) ;
#41178=CARTESIAN_POINT ( 'NONE',  ( -0.7495606340400177148, -0.1264236179284866091, 1.508366141678519678 ) ) ;
#41179=CARTESIAN_POINT ( 'NONE',  ( -0.8759842519685039353, 0.1787899950787401882, 0.1156496062454492185 ) ) ;
#41180=CARTESIAN_POINT ( 'NONE',  ( -0.9873396505805591694, 0.1113553986120547346, 1.589566929133858331 ) ) ;
#41181=CARTESIAN_POINT ( 'NONE',  ( -1.033464566929134687, -0.06523048226347956391, 0.9522637795275589179 ) ) ;
#41182=CARTESIAN_POINT ( 'NONE',  ( 0.8019270111902716547, -0.1787899950787401604, 1.550196850339938148 ) ) ;
#41187=ORIENTED_EDGE ( 'NONE', *, *, #5867, .T. ) ;
#41188=EDGE_CURVE ( 'NONE', #33274, #3817, #8753, .T. ) ;
#41197=CARTESIAN_POINT ( 'NONE',  ( -0.8759842519685039353, 0.1574803149606299191, 0.1377952755905511861 ) ) ;
#41198=CARTESIAN_POINT ( 'NONE',  ( 0.9500414927467378812, -0.1787899950787401604, 0.8415354330171019859 ) ) ;
#41199=CARTESIAN_POINT ( 'NONE',  ( 1.033464566929133799, 1.928577636452524610E-17, 4.498031496062992574 ) ) ;
#41200=FACE_OUTER_BOUND ( 'NONE', #18847, .T. ) ;
#41203=CARTESIAN_POINT ( 'NONE',  ( 0.9500414927467378812, 0.1787899950787401604, 1.806102362150961316 ) ) ;
#41204=CARTESIAN_POINT ( 'NONE',  ( 0.8107537697050234415, -0.1574803149606297803, 0.1550196850393702197 ) ) ;
#41207=CARTESIAN_POINT ( 'NONE',  ( 0.7185039370078739607, 1.928577636452523993E-17, 0.1082677165354330728 ) ) ;
#41209=( BOUNDED_CURVE ( )  B_SPLINE_CURVE ( 2, ( #38528, #28225, #2326, #13372, #24161, #20775, #17658, #5697, #42343 ),
 .UNSPECIFIED., .F., .F. ) 
 B_SPLINE_CURVE_WITH_KNOTS ( ( 3, 2, 2, 2, 3 ),
 ( 0.07000000000000000666, 0.07249999999999999500, 0.07499999999999999722, 0.07749999999999999944, 0.08000000000000000167 ),
 .UNSPECIFIED. ) 
 CURVE ( )  GEOMETRIC_REPRESENTATION_ITEM ( )  RATIONAL_B_SPLINE_CURVE ( ( 1.000000000000000000, 0.9238795325112859613, 1.000000000000000000, 0.9238795325112869605, 1.000000000000000000, 0.9238795325112869605, 1.000000000000000000, 0.9238795325112869605, 1.000000000000000000 ) ) 
 REPRESENTATION_ITEM ( '' )  ) ;
#41210=CARTESIAN_POINT ( 'NONE',  ( 0.8019270111902717657, -0.1787899950787401604, 0.2903543306548980185 ) ) ;
#41211=VECTOR ( 'NONE', #1757, 39.37007874015748143 ) ;
#41212=CARTESIAN_POINT ( 'NONE',  ( -1.002407869896990045, -0.1264236179284866091, 1.788877952702141672 ) ) ;
#41214=CARTESIAN_POINT ( 'NONE',  ( -1.002407869896990045, -0.1264236179284866091, 1.360728346402929168 ) ) ;
#41215=CARTESIAN_POINT ( 'NONE',  ( -0.7646288533564489232, 0.1113553986120547346, 0.8907480314960629642 ) ) ;
#41217=CARTESIAN_POINT ( 'NONE',  ( -0.8019270111902717657, -0.1787899950787401604, 0.5659448818360001132 ) ) ;
#41218=CARTESIAN_POINT ( 'NONE',  ( 1.054774247047244540, -0.07405724077823318263, 1.948818897584033927 ) ) ;
#41219=CARTESIAN_POINT ( 'NONE',  ( -0.6971942568897637749, 2.189545951927499583E-17, 1.183562992072220599 ) ) ;
#41220=CARTESIAN_POINT ( 'NONE',  ( 0.7185039370078739607, 1.928577636452523993E-17, 1.555118110128692832 ) ) ;
#41223=CARTESIAN_POINT ( 'NONE',  ( 0.9500414927467377701, -0.1787899950787401604, 0.5314960629383620461 ) ) ;
#41224=CARTESIAN_POINT ( 'NONE',  ( -0.7495606340400177148, 0.1264236179284866091, 0.4306102361667086820 ) ) ;
#41227=VERTEX_POINT ( 'NONE', #19063 ) ;
#41228=CARTESIAN_POINT ( 'NONE',  ( 0.9500414927467378812, -0.1787899950787401604, 0.8858267715997791836 ) ) ;
#41229=CARTESIAN_POINT ( 'NONE',  ( -1.033464566929134687, 0.06523048226347956391, 0.1697834645669291653 ) ) ;
#41234=CARTESIAN_POINT ( 'NONE',  ( -0.9873396505805591694, -0.1113553986120547346, 1.304133858267716661 ) ) ;
#41239=EDGE_LOOP ( 'NONE', ( #26835, #1673, #7326, #13214 ) ) ;
#41244=CARTESIAN_POINT ( 'NONE',  ( 0.8759842519685039353, 0.1787899950787401882, 1.291830708607653477 ) ) ;
#41246=CARTESIAN_POINT ( 'NONE',  ( -0.7185039370078741827, 0.06523048226347841205, 0.8439960628845994961 ) ) ;
#41247=DIRECTION ( 'NONE',  ( 0.000000000000000000, 0.000000000000000000, -1.000000000000000000 ) ) ;
#41249=CARTESIAN_POINT ( 'NONE',  ( -0.8759842519685039353, 0.1574803149606299191, 1.437007874015747921 ) ) ;
#41250=CARTESIAN_POINT ( 'NONE',  ( 0.8759842519685039353, -0.1787899950787401882, 1.547736220418677089 ) ) ;
#41251=CARTESIAN_POINT ( 'NONE',  ( 1.002407869896990045, 0.1264236179284866091, 0.1058070865604098382 ) ) ;
#41255=CARTESIAN_POINT ( 'NONE',  ( -0.7185039370078739607, 1.928577636452523993E-17, 1.751968503829480106 ) ) ;
#41257=AXIS2_PLACEMENT_3D ( 'NONE', #30979, #27402, #9632 ) ;
#41258=CARTESIAN_POINT ( 'NONE',  ( -1.002407869896990045, 0.1264236179284866091, 0.6225393700249762796 ) ) ;
#41262=DIRECTION ( 'NONE',  ( 0.000000000000000000, 0.000000000000000000, -1.000000000000000000 ) ) ;
#41265=CARTESIAN_POINT ( 'NONE',  ( 0.8759842519685039353, 0.1787899950787401882, 1.336122047190330786 ) ) ;
#41266=AXIS2_PLACEMENT_3D ( 'NONE', #21218, #32513, #35847 ) ;
#41267=CARTESIAN_POINT ( 'NONE',  ( 0.9500414927467377701, 0.1787899950787401604, 1.919291338528913649 ) ) ;
#41268=FACE_OUTER_BOUND ( 'NONE', #31689, .T. ) ;
#41269=ORIENTED_EDGE ( 'NONE', *, *, #2578, .T. ) ;
#41271=DIRECTION ( 'NONE',  ( 1.000000000000000000, 0.000000000000000000, -1.822029033848725275E-16 ) ) ;
#41274=CARTESIAN_POINT ( 'NONE',  ( 0.8759842519685039353, 0.1787899950787401882, 0.3075787401037169411 ) ) ;
#41275=CARTESIAN_POINT ( 'NONE',  ( 0.8019270111902716547, 0.1787899950787401604, 1.294291338528913204 ) ) ;
#41276=CARTESIAN_POINT ( 'NONE',  ( 1.033464566929133799, 0.000000000000000000, 0.9055118109160944506 ) ) ;
#41278=CARTESIAN_POINT ( 'NONE',  ( -0.9412147342319837628, 0.1574803149606300301, 0.7652559055118115516 ) ) ;
#41279=CARTESIAN_POINT ( 'NONE',  ( -0.8759842519685039353, 0.1787899950787401882, 1.331200787347811110 ) ) ;
#41280=CARTESIAN_POINT ( 'NONE',  ( 0.7646288533564489232, 0.1113553986120547346, 0.8415354329633386588 ) ) ;
#41286=CARTESIAN_POINT ( 'NONE',  ( -0.7185039370078746268, -0.06523048226347956391, 1.213090551181103427 ) ) ;
#41287=CARTESIAN_POINT ( 'NONE',  ( 0.7495606340400177148, -0.1264236179284866091, 1.542814960576157413 ) ) ;
#41288=CARTESIAN_POINT ( 'NONE',  ( -1.033464566929133799, 0.000000000000000000, 1.230314960629921295 ) ) ;
#41290=CARTESIAN_POINT ( 'NONE',  ( -0.7185039370078746268, 0.06523048226347956391, 1.838090551181102317 ) ) ;
#41291=CARTESIAN_POINT ( 'NONE',  ( -0.8107537697050254399, -0.1574803149606297803, 0.4306102362204725642 ) ) ;
#41292=CARTESIAN_POINT ( 'NONE',  ( -1.033464566929133799, 0.000000000000000000, 0.8759842519685039353 ) ) ;
#41293=CARTESIAN_POINT ( 'NONE',  ( 0.8107537697050253289, -0.1574803149606297803, 1.326279527451528661 ) ) ;
#41296=CARTESIAN_POINT ( 'NONE',  ( 0.8759842519685039353, -0.1574803149606299191, 0.5905511811023621549 ) ) ;
#41298=CARTESIAN_POINT ( 'NONE',  ( 0.9500414927467378812, 0.1787899950787401604, 0.6643700786863929730 ) ) ;
#41299=CARTESIAN_POINT ( 'NONE',  ( 0.8019270111902716547, -0.1787899950787401604, 0.9596456692375763264 ) ) ;
#41301=CARTESIAN_POINT ( 'NONE',  ( -0.6971942568897648851, -0.07405724077823297447, 1.309055118056472899 ) ) ;
#41302=ORIENTED_EDGE ( 'NONE', *, *, #28773, .T. ) ;
#41304=CARTESIAN_POINT ( 'NONE',  ( -1.054774247047244540, -0.07405724077823318263, 0.3789370078202520253 ) ) ;
#41306=CARTESIAN_POINT ( 'NONE',  ( 0.7185039370078746268, 0.06523048226347956391, 0.8833661416247559073 ) ) ;
#41314=CARTESIAN_POINT ( 'NONE',  ( -1.033464566929133799, 0.000000000000000000, 0.2755905510735752184 ) ) ;
#41318=CARTESIAN_POINT ( 'NONE',  ( -0.8019270111902716547, -0.1787899950787401604, 0.2509842519147403861 ) ) ;
#41319=CARTESIAN_POINT ( 'NONE',  ( -1.033464566929133799, 0.000000000000000000, 0.8759842519685039353 ) ) ;
#41322=CARTESIAN_POINT ( 'NONE',  ( -0.7646288533564489232, 0.1113553986120547346, 1.943897637687747926 ) ) ;
#41323=CARTESIAN_POINT ( 'NONE',  ( 0.7495606340400177148, -0.1264236179284866091, 0.9965551180564724554 ) ) ;
#41324=CARTESIAN_POINT ( 'NONE',  ( 1.054774247047244540, 0.07405724077823318263, 1.402559055064346749 ) ) ;
#41326=CARTESIAN_POINT ( 'NONE',  ( 0.9873396505805591694, 0.1113553986120547346, 0.5167322833570401341 ) ) ;
#41327=CARTESIAN_POINT ( 'NONE',  ( 0.7185039370078739607, 1.928577636452523993E-17, 1.643700787401574992 ) ) ;
#41328=CARTESIAN_POINT ( 'NONE',  ( 0.7125420959524927378, -0.03489325537972703950, 1.983914969194383371 ) ) ;
#41329=CARTESIAN_POINT ( 'NONE',  ( 1.033464566929133799, 1.928577636452524610E-17, 4.498031496062992574 ) ) ;
#41330=FACE_OUTER_BOUND ( 'NONE', #39822, .T. ) ;
#41332=( BOUNDED_CURVE ( )  B_SPLINE_CURVE ( 2, ( #20190, #8946, #9429, #31476, #27897, #20432, #38649, #34841, #35066 ),
 .UNSPECIFIED., .F., .T. ) 
 B_SPLINE_CURVE_WITH_KNOTS ( ( 3, 2, 2, 2, 3 ),
 ( 0.02000000000000000042, 0.02249999999999999917, 0.02500000000000000139, 0.02750000000000000014, 0.02999999999999999889 ),
 .UNSPECIFIED. ) 
 CURVE ( )  GEOMETRIC_REPRESENTATION_ITEM ( )  RATIONAL_B_SPLINE_CURVE ( ( 1.000000000000000000, 0.9238795325112869605, 1.000000000000000000, 0.9238795325112869605, 1.000000000000000000, 0.9238795325112869605, 1.000000000000000000, 0.9238795325112869605, 1.000000000000000000 ) ) 
 REPRESENTATION_ITEM ( '' )  ) ;
#41334=CARTESIAN_POINT ( 'NONE',  ( 0.7495606340400177148, 0.1264236179284866091, 0.9817913385289134265 ) ) ;
#41335=CARTESIAN_POINT ( 'NONE',  ( -1.033464566929133799, 0.000000000000000000, 1.427165354330708569 ) ) ;
#41336=CARTESIAN_POINT ( 'NONE',  ( 0.9500414927467377701, 0.1787899950787401604, 1.806102362150961094 ) ) ;
#41338=EDGE_LOOP ( 'NONE', ( #40582, #40903, #36908, #44662 ) ) ;
#41339=CARTESIAN_POINT ( 'NONE',  ( -0.7185039370078746268, 0.06523048226347956391, 0.8538385826771661691 ) ) ;
#41341=CARTESIAN_POINT ( 'NONE',  ( -0.8759842519685039353, 0.1574803149606299191, 0.04921259831766984505 ) ) ;
#41342=CARTESIAN_POINT ( 'NONE',  ( 0.9500414927467378812, -0.1787899950787401604, 1.077755905458048113 ) ) ;
#41346=CARTESIAN_POINT ( 'NONE',  ( -1.033464566929134687, -0.06523048226347956391, 0.2829724409448821643 ) ) ;
#41347=CARTESIAN_POINT ( 'NONE',  ( -0.9500414927467378812, 0.1787899950787401604, 0.2263779527021421711 ) ) ;
#41350=CARTESIAN_POINT ( 'NONE',  ( -0.8019270111902717657, -0.1787899950787401604, 1.860236220418677089 ) ) ;
#41351=CARTESIAN_POINT ( 'NONE',  ( -0.8019270111902716547, -0.1787899950787401604, 0.9547244093950545407 ) ) ;
#41352=CARTESIAN_POINT ( 'NONE',  ( -0.7495606340400177148, 0.1264236179284866091, 0.5930118109698583329 ) ) ;
#41353=( BOUNDED_CURVE ( )  B_SPLINE_CURVE ( 2, ( #3469, #28663, #43229, #25034, #7057, #39629, #6810, #47319, #14494 ),
 .UNSPECIFIED., .F., .T. ) 
 B_SPLINE_CURVE_WITH_KNOTS ( ( 3, 2, 2, 2, 3 ),
 ( 0.2800000000000000266, 0.2824999999999999734, 0.2849999999999999756, 0.2874999999999999778, 0.2899999999999999800 ),
 .UNSPECIFIED. ) 
 CURVE ( )  GEOMETRIC_REPRESENTATION_ITEM ( )  RATIONAL_B_SPLINE_CURVE ( ( 1.000000000000000000, 0.9238795325112869605, 1.000000000000000000, 0.9238795325112869605, 1.000000000000000000, 0.9238795325112869605, 1.000000000000000000, 0.9238795325112869605, 1.000000000000000000 ) ) 
 REPRESENTATION_ITEM ( '' )  ) ;
#41357=CARTESIAN_POINT ( 'NONE',  ( -0.9873396505805591694, 0.1113553986120547346, 1.668307086614173373 ) ) ;
#41360=DIRECTION ( 'NONE',  ( -1.000000000000000000, 0.000000000000000000, 0.000000000000000000 ) ) ;
#41366=CARTESIAN_POINT ( 'NONE',  ( -0.8019270111902717657, -0.1787899950787401604, 0.4035433070328508509 ) ) ;
#41370=CARTESIAN_POINT ( 'NONE',  ( -0.6971942568897637749, 2.189545951927499583E-17, 1.582185039316315045 ) ) ;
#41373=( LENGTH_UNIT ( ) NAMED_UNIT ( * ) SI_UNIT ( $, .METRE. ) ) ;
#41374=CARTESIAN_POINT ( 'NONE',  ( 0.7185039370078739607, 0.000000000000000000, 4.498031496062992574 ) ) ;
#41375=CARTESIAN_POINT ( 'NONE',  ( 0.8107537697050253289, -0.1574803149606297803, 0.4699803149606304742 ) ) ;
#41377=CARTESIAN_POINT ( 'NONE',  ( -0.7185039370078746268, 0.06523048226347956391, 1.158956692805858113 ) ) ;
#41378=CARTESIAN_POINT ( 'NONE',  ( 0.7495606340400177148, -0.1264236179284866091, 0.6028543306548976854 ) ) ;
#41381=CARTESIAN_POINT ( 'NONE',  ( 0.7646288533564489232, 0.1113553986120547346, 1.943897637687747926 ) ) ;
#41384=CARTESIAN_POINT ( 'NONE',  ( -1.002407869896990045, 0.1264236179284866091, 1.134350393647023614 ) ) ;
#41385=CARTESIAN_POINT ( 'NONE',  ( 1.033464566929133799, 0.000000000000000000, 1.033464566929133799 ) ) ;
#41386=CARTESIAN_POINT ( 'NONE',  ( -1.033464566929133799, 0.000000000000000000, 0.7086614172153071767 ) ) ;
#41397=CARTESIAN_POINT ( 'NONE',  ( 0.8019270111902717657, 0.1787899950787401604, 0.7431102361667091261 ) ) ;
#41398=ORIENTED_EDGE ( 'NONE', *, *, #6559, .T. ) ;
#41399=CARTESIAN_POINT ( 'NONE',  ( -0.7185039370078739607, 1.928577636452523993E-17, 1.791338582569637738 ) ) ;
#41405=CARTESIAN_POINT ( 'NONE',  ( 0.8759842519685039353, 0.1574803149606299191, 1.190944881782236342 ) ) ;
#41409=CARTESIAN_POINT ( 'NONE',  ( -1.054774247047244096, 0.000000000000000000, 1.759350393647023614 ) ) ;
#41410=CARTESIAN_POINT ( 'NONE',  ( 0.6971942568897648851, -0.07405724077823297447, 1.781496062938362934 ) ) ;
#41414=CARTESIAN_POINT ( 'NONE',  ( 0.6971942568897637749, 2.189545951927499583E-17, 0.4404527558517480901 ) ) ;
#41415=CARTESIAN_POINT ( 'NONE',  ( -1.054774247047244540, -0.07405724077823318263, 1.358267716481669662 ) ) ;
#41417=CARTESIAN_POINT ( 'NONE',  ( -1.054774247047244540, 0.07405724077823318263, 1.284448818843874518 ) ) ;
#41418=CARTESIAN_POINT ( 'NONE',  ( -0.6971942568897637749, 2.189545951927499583E-17, 0.8686023621509606496 ) ) ;
#41419=CARTESIAN_POINT ( 'NONE',  ( -1.002407869896990045, -0.1264236179284866091, 0.1008858267178899676 ) ) ;
#41420=ADVANCED_FACE ( 'NONE', ( #45880 ), #2273, .T. ) ;
#41422=CARTESIAN_POINT ( 'NONE',  ( -0.9500414927467378812, -0.1787899950787401604, 1.791338582623401177 ) ) ;
#41423=CARTESIAN_POINT ( 'NONE',  ( -0.7495606340400177148, 0.1264236179284866091, 0.04183070860765386589 ) ) ;
#41425=CARTESIAN_POINT ( 'NONE',  ( -0.7185039370078746268, 0.06523048226347956391, 1.759350393700787940 ) ) ;
#41426=CARTESIAN_POINT ( 'NONE',  ( -1.033464566929133799, 0.000000000000000000, 0.2854330708661417804 ) ) ;
#41427=CARTESIAN_POINT ( 'NONE',  ( 0.8759842519685039353, 0.1787899950787401882, 1.651082677111590513 ) ) ;
#41430=ORIENTED_EDGE ( 'NONE', *, *, #43036, .T. ) ;
#41431=EDGE_CURVE ( 'NONE', #28079, #17196, #15077, .T. ) ;
#41433=ORIENTED_EDGE ( 'NONE', *, *, #4104, .F. ) ;
#41439=CARTESIAN_POINT ( 'NONE',  ( 0.8759842519685039353, 0.1787899950787401882, 1.843011810969858333 ) ) ;
#41443=CARTESIAN_POINT ( 'NONE',  ( 0.7185039370078746268, -0.06523048226347956391, 0.1008858266641264878 ) ) ;
#41445=CARTESIAN_POINT ( 'NONE',  ( 0.9412147342319837628, 0.1574803149606300301, 0.1747047244094488694 ) ) ;
#41451=CARTESIAN_POINT ( 'NONE',  ( 0.9500414927467378812, 0.1787899950787401604, 0.3100393700249766682 ) ) ;
#41452=DIRECTION ( 'NONE',  ( 1.000000000000000000, 0.000000000000000000, -1.822029033848725275E-16 ) ) ;
#41453=CARTESIAN_POINT ( 'NONE',  ( -1.054774247047244540, 0.07405724077823318263, 1.678149606245448622 ) ) ;
#41455=CARTESIAN_POINT ( 'NONE',  ( -0.7495606340400177148, 0.1264236179284866091, 1.262303149552535420 ) ) ;
#41457=CARTESIAN_POINT ( 'NONE',  ( 1.002407869896990045, 0.1264236179284866091, 1.449311023568283341 ) ) ;
#41461=CARTESIAN_POINT ( 'NONE',  ( -0.7495606340400177148, -0.1264236179284866091, 1.227854330654897685 ) ) ;
#41462=CARTESIAN_POINT ( 'NONE',  ( 0.9873396505805591694, -0.1113553986120547346, 0.6643700786326299790 ) ) ;
#41464=CARTESIAN_POINT ( 'NONE',  ( -0.7185039370078714072, 0.06523048226347728795, 1.355807086506647829 ) ) ;
#41465=CARTESIAN_POINT ( 'NONE',  ( 0.8759842519685039353, 0.1787899950787401882, 0.4306102361667086820 ) ) ;
#41466=CARTESIAN_POINT ( 'NONE',  ( -0.7495606340400177148, -0.1264236179284866091, 0.4010826771115905687 ) ) ;
#41467=CARTESIAN_POINT ( 'NONE',  ( 1.002407869896990045, -0.1264236179284866091, 0.9276574802611967652 ) ) ;
#41468=CARTESIAN_POINT ( 'NONE',  ( 0.8759842519685039353, -0.1787899950787401882, 1.158956692859621995 ) ) ;
#41470=CARTESIAN_POINT ( 'NONE',  ( 1.033464566929134687, 0.06523048226347956391, 1.301673228238930502 ) ) ;
#41471=ORIENTED_EDGE ( 'NONE', *, *, #35190, .F. ) ;
#41473=CARTESIAN_POINT ( 'NONE',  ( -1.054774247047244096, 0.000000000000000000, 0.9719488188438739629 ) ) ;
#41474=CARTESIAN_POINT ( 'NONE',  ( -1.054774247047244096, 0.000000000000000000, 0.02214566923757503927 ) ) ;
#41476=EDGE_LOOP ( 'NONE', ( #23612, #21575, #38134, #46378 ) ) ;
#41479=CARTESIAN_POINT ( 'NONE',  ( 0.7185039370078739607, 1.928577636452523993E-17, 0.6200787401574803237 ) ) ;
#41481=CARTESIAN_POINT ( 'NONE',  ( 1.002407869896990045, -0.1264236179284866091, 1.316437007820252081 ) ) ;
#41482=CARTESIAN_POINT ( 'NONE',  ( 0.9873396505805591694, 0.1113553986120547346, 1.461614173120818760 ) ) ;
#41483=CARTESIAN_POINT ( 'NONE',  ( -1.033464566929133799, 0.000000000000000000, 1.732283464459401623 ) ) ;
#41486=CARTESIAN_POINT ( 'NONE',  ( 0.6971942568897648851, -0.07405724077823297447, 1.619094488135213838 ) ) ;
#41492=CARTESIAN_POINT ( 'NONE',  ( -0.8019270111902716547, -0.1787899950787401604, 0.6053149605761580787 ) ) ;
#41493=CARTESIAN_POINT ( 'NONE',  ( -0.8107537697050254399, -0.1574803149606297803, 1.286909448711370585 ) ) ;
#41500=CARTESIAN_POINT ( 'NONE',  ( -0.7185039370078739607, 1.928577636452523993E-17, 1.515748031388535200 ) ) ;
#41501=CARTESIAN_POINT ( 'NONE',  ( 0.9500414927467378812, -0.1787899950787401604, 1.318897637741511364 ) ) ;
#41502=CARTESIAN_POINT ( 'NONE',  ( 0.8019270111902716547, 0.1787899950787401604, 1.806102362150961094 ) ) ;
#41504=CARTESIAN_POINT ( 'NONE',  ( -0.8107537697050234415, -0.1574803149606297803, 0.1451771652468037688 ) ) ;
#41506=DIRECTION ( 'NONE',  ( -1.000000000000000000, 0.000000000000000000, 0.000000000000000000 ) ) ;
#41507=DIRECTION ( 'NONE',  ( 0.000000000000000000, 0.000000000000000000, -1.000000000000000000 ) ) ;
#41509=CARTESIAN_POINT ( 'NONE',  ( 1.033464566929134687, -0.06523048226347956391, 0.5093503935932608417 ) ) ;
#41510=CARTESIAN_POINT ( 'NONE',  ( 0.6971942568897626646, 0.07405724077823318263, 0.4724409448281262636 ) ) ;
#41514=CARTESIAN_POINT ( 'NONE',  ( -0.9500414927467378812, -0.1787899950787401604, 1.353346456639149986 ) ) ;
#41515=CARTESIAN_POINT ( 'NONE',  ( 1.033464566929134687, -0.06523048226347956391, 0.7849409447743628254 ) ) ;
#41516=VERTEX_POINT ( 'NONE', #36059 ) ;
#41518=ADVANCED_FACE ( 'NONE', ( #32250 ), #23325, .F. ) ;
#41522=CARTESIAN_POINT ( 'NONE',  ( -0.8759842519685039353, -0.1574803149606299191, 0.6200787400499527813 ) ) ;
#41523=CARTESIAN_POINT ( 'NONE',  ( -0.9412147342319837628, -0.1574803149606297803, 1.222933070866141669 ) ) ;
#41524=CARTESIAN_POINT ( 'NONE',  ( -0.7646288533564489232, -0.1113553986120547346, 1.048228346349165507 ) ) ;
#41527=CARTESIAN_POINT ( 'NONE',  ( 0.8759842519685039353, -0.1787899950787401882, 0.05659448813521291560 ) ) ;
#41528=CARTESIAN_POINT ( 'NONE',  ( 0.7646288533564489232, -0.1113553986120547346, 1.481299212490897466 ) ) ;
#41530=ORIENTED_EDGE ( 'NONE', *, *, #4859, .T. ) ;
#41531=AXIS2_PLACEMENT_3D ( 'NONE', #4489, #27312, #27069 ) ;
#41532=CARTESIAN_POINT ( 'NONE',  ( 0.6971942568897637749, 2.189545951927499583E-17, 0.9522637794737952577 ) ) ;
#41533=CARTESIAN_POINT ( 'NONE',  ( -1.054774247047244540, -0.07405724077823318263, 1.594488188922615457 ) ) ;
#41535=CARTESIAN_POINT ( 'NONE',  ( -1.054774247047244540, 0.07405724077823318263, 1.328740157426552049 ) ) ;
#41540=CARTESIAN_POINT ( 'NONE',  ( -0.8759842519685039353, -0.1787899950787401882, 0.3715551180564728440 ) ) ;
#41542=FACE_OUTER_BOUND ( 'NONE', #36672, .T. ) ;
#41550=AXIS2_PLACEMENT_3D ( 'NONE', #207, #35942, #6937 ) ;
#41554=CARTESIAN_POINT ( 'NONE',  ( 1.054774247047244096, 0.000000000000000000, 0.8538385826234016207 ) ) ;
#41555=CARTESIAN_POINT ( 'NONE',  ( 0.9500414927467377701, -0.1787899950787401604, 1.432086614119464141 ) ) ;
#41556=CARTESIAN_POINT ( 'NONE',  ( 0.7495606340400177148, -0.1264236179284866091, 0.1254921259304885850 ) ) ;
#41558=DIRECTION ( 'NONE',  ( 1.822029033848725028E-16, 0.000000000000000000, 1.000000000000000000 ) ) ;
#41559=EDGE_CURVE ( 'NONE', #2953, #38075, #38011, .T. ) ;
#41560=CARTESIAN_POINT ( 'NONE',  ( 0.9873396505805591694, 0.1113553986120547346, 1.589566929133858331 ) ) ;
#41561=CARTESIAN_POINT ( 'NONE',  ( 0.7257667744041150781, -0.07649319432550391595, 1.984749488431225561 ) ) ;
#41563=FACE_OUTER_BOUND ( 'NONE', #30819, .T. ) ;
#41565=CARTESIAN_POINT ( 'NONE',  ( -1.033464566929134687, -0.06523048226347956391, 1.611712598317668999 ) ) ;
#41568=DIRECTION ( 'NONE',  ( 0.000000000000000000, 0.000000000000000000, -1.000000000000000000 ) ) ;
#41569=CARTESIAN_POINT ( 'NONE',  ( 1.054774247047244540, 0.07405724077823318263, 1.048228346402928723 ) ) ;
#41570=CARTESIAN_POINT ( 'NONE',  ( 0.8019270111902716547, 0.1787899950787401604, 1.889763779473794481 ) ) ;
#41571=CARTESIAN_POINT ( 'NONE',  ( 0.7646288533564489232, 0.1113553986120547346, 0.2903543306011346359 ) ) ;
#41578=CARTESIAN_POINT ( 'NONE',  ( -1.033464566929134687, 0.06523048226347956391, 0.2386811022546777294 ) ) ;
#41581=CARTESIAN_POINT ( 'NONE',  ( 1.054774247047244540, -0.07405724077823318263, 1.122047244040725644 ) ) ;
#41582=ADVANCED_FACE ( 'NONE', ( #37926 ), #15660, .T. ) ;
#41586=CARTESIAN_POINT ( 'NONE',  ( -1.002407869896990045, 0.1264236179284866091, 0.5782480314422993040 ) ) ;
#41587=DIRECTION ( 'NONE',  ( 1.822029033848725028E-16, 0.000000000000000000, 1.000000000000000000 ) ) ;
#41588=CARTESIAN_POINT ( 'NONE',  ( -1.054774247047244540, 0.07405724077823318263, 0.3001968503399373711 ) ) ;
#41590=CARTESIAN_POINT ( 'NONE',  ( -1.002407869896990045, 0.1264236179284866091, 0.4650590550643464716 ) ) ;
#41593=CARTESIAN_POINT ( 'NONE',  ( -0.7185039370078739607, 1.928577636452523993E-17, 0.9350393700787401619 ) ) ;
#41597=CARTESIAN_POINT ( 'NONE',  ( 0.8107537697050254399, -0.1574803149606297803, 0.4699803149606304742 ) ) ;
#41601=CARTESIAN_POINT ( 'NONE',  ( -0.9500414927467378812, -0.1787899950787401604, 0.4872047243556847929 ) ) ;
#41602=CARTESIAN_POINT ( 'NONE',  ( 0.8759842519685039353, 0.1574803149606299191, 1.190944881782236342 ) ) ;
#41603=EDGE_LOOP ( 'NONE', ( #30454, #45321, #14126, #46874 ) ) ;
#41606=CARTESIAN_POINT ( 'NONE',  ( -1.054774247047244540, 0.07405724077823318263, 1.486220472387181912 ) ) ;
#41610=( BOUNDED_CURVE ( )  B_SPLINE_CURVE ( 2, ( #8116, #14613, #18663, #36656, #22500, #11978, #3814, #18433, #22741 ),
 .UNSPECIFIED., .F., .T. ) 
 B_SPLINE_CURVE_WITH_KNOTS ( ( 3, 2, 2, 2, 3 ),
 ( 0.7700000000000000178, 0.7724999999999999645, 0.7750000000000000222, 0.7774999999999999689, 0.7800000000000000266 ),
 .UNSPECIFIED. ) 
 CURVE ( )  GEOMETRIC_REPRESENTATION_ITEM ( )  RATIONAL_B_SPLINE_CURVE ( ( 1.000000000000000000, 0.9238795325112869605, 1.000000000000000000, 0.9238795325112869605, 1.000000000000000000, 0.9238795325112869605, 1.000000000000000000, 0.9238795325112869605, 1.000000000000000000 ) ) 
 REPRESENTATION_ITEM ( '' )  ) ;
#41611=CARTESIAN_POINT ( 'NONE',  ( -0.7185039370078739607, 0.000000000000000000, -2.869337061179095023E-17 ) ) ;
#41612=CARTESIAN_POINT ( 'NONE',  ( 0.8759842519685039353, -0.1574803149606299191, 0.4724409448818898127 ) ) ;
#41614=CARTESIAN_POINT ( 'NONE',  ( -0.7185039370078739607, 1.928577636452523993E-17, 1.200787401467275695 ) ) ;
#41615=CARTESIAN_POINT ( 'NONE',  ( 1.002407869896990045, -0.1264236179284866091, 0.09596456687537027741 ) ) ;
#41618=CARTESIAN_POINT ( 'NONE',  ( -0.9873396505805591694, 0.1113553986120547346, 1.186023621939716666 ) ) ;
#41621=CARTESIAN_POINT ( 'NONE',  ( -0.8759842519685039353, 0.1787899950787401882, 1.060531496009228247 ) ) ;
#41622=CARTESIAN_POINT ( 'NONE',  ( 0.7185039370078746268, -0.06523048226347956391, 1.173720472440945573 ) ) ;
#41624=CARTESIAN_POINT ( 'NONE',  ( -0.8107537697050254399, 0.1574803149606300301, 0.7209645668216064784 ) ) ;
#41626=CARTESIAN_POINT ( 'NONE',  ( 0.8759842519685039353, -0.1574803149606299191, 0.5807086613097960370 ) ) ;
#41628=CARTESIAN_POINT ( 'NONE',  ( 0.9873396505805591694, 0.1113553986120547346, 0.5954724408373543998 ) ) ;
#41634=DIRECTION ( 'NONE',  ( 1.000000000000000000, 0.000000000000000000, -1.822029033848725275E-16 ) ) ;
#41635=CARTESIAN_POINT ( 'NONE',  ( 0.9500414927467378812, -0.1787899950787401604, 0.6840551180564720113 ) ) ;
#41637=ORIENTED_EDGE ( 'NONE', *, *, #21305, .T. ) ;
#41638=CARTESIAN_POINT ( 'NONE',  ( -0.7646288533564489232, 0.1113553986120547346, 1.786417322727117840 ) ) ;
#41643=CARTESIAN_POINT ( 'NONE',  ( 0.8759842519685039353, 0.1574803149606299191, 1.151574803042078710 ) ) ;
#41644=( BOUNDED_CURVE ( )  B_SPLINE_CURVE ( 2, ( #38005, #5166, #31077, #38475, #20256, #34904, #10915, #39393, #43467 ),
 .UNSPECIFIED., .F., .T. ) 
 B_SPLINE_CURVE_WITH_KNOTS ( ( 3, 2, 2, 2, 3 ),
 ( 0.2999999999999999889, 0.3024999999999999911, 0.3049999999999999933, 0.3074999999999999956, 0.3099999999999999978 ),
 .UNSPECIFIED. ) 
 CURVE ( )  GEOMETRIC_REPRESENTATION_ITEM ( )  RATIONAL_B_SPLINE_CURVE ( ( 1.000000000000000000, 0.9238795325112869605, 1.000000000000000000, 0.9238795325112869605, 1.000000000000000000, 0.9238795325112869605, 1.000000000000000000, 0.9238795325112869605, 1.000000000000000000 ) ) 
 REPRESENTATION_ITEM ( '' )  ) ;
#41645=CARTESIAN_POINT ( 'NONE',  ( -0.7646288533564489232, 0.1113553986120547346, 1.865157480207432883 ) ) ;
#41646=CARTESIAN_POINT ( 'NONE',  ( -0.9500414927467378812, 0.1787899950787401604, 0.4625984251430869665 ) ) ;
#41647=VERTEX_POINT ( 'NONE', #13690 ) ;
#41650=CARTESIAN_POINT ( 'NONE',  ( -1.002407869896990045, 0.1264236179284866091, 1.724901574749385880 ) ) ;
#41651=CARTESIAN_POINT ( 'NONE',  ( 0.6971942568897648851, -0.07405724077823297447, 1.899606299158834943 ) ) ;
#41654=CARTESIAN_POINT ( 'NONE',  ( 1.002407869896990045, 0.1264236179284866091, 0.4650590550643464716 ) ) ;
#41655=CARTESIAN_POINT ( 'NONE',  ( -0.9500414927467378812, -0.1787899950787401604, 1.432086614119464141 ) ) ;
#41657=CARTESIAN_POINT ( 'NONE',  ( -1.054774247047244540, -0.07405724077823318263, 0.1033464566391498751 ) ) ;
#41658=CARTESIAN_POINT ( 'NONE',  ( 0.7185039370078739607, 1.928577636452523993E-17, 1.564960629921259949 ) ) ;
#41659=CARTESIAN_POINT ( 'NONE',  ( -0.9500414927467378812, -0.1787899950787401604, 1.673228346402929834 ) ) ;
#41660=CARTESIAN_POINT ( 'NONE',  ( -1.033464566929134687, -0.06523048226347956391, 1.966043306979087246 ) ) ;
#41662=CARTESIAN_POINT ( 'NONE',  ( -0.7646288533564489232, -0.1113553986120547346, 1.727362204724409489 ) ) ;
#41664=CARTESIAN_POINT ( 'NONE',  ( 0.6971942568897648851, 0.07405724077823318263, 1.658464566875369472 ) ) ;
#41678=CARTESIAN_POINT ( 'NONE',  ( -0.7185039370078739607, 1.928577636452523993E-17, 0.8070866140657008136 ) ) ;
#41681=CARTESIAN_POINT ( 'NONE',  ( 1.054774247047244096, 0.000000000000000000, 0.9276574802611967652 ) ) ;
#41682=ADVANCED_FACE ( 'NONE', ( #27875 ), #42435, .T. ) ;
#41684=CARTESIAN_POINT ( 'NONE',  ( -1.033464566929133799, 0.000000000000000000, 1.574803149498771537 ) ) ;
#41686=CARTESIAN_POINT ( 'NONE',  ( 0.8107537697050254399, -0.1574803149606297803, 1.257381889763780736 ) ) ;
#41687=CARTESIAN_POINT ( 'NONE',  ( 0.8019270111902717657, -0.1787899950787401604, 1.943897637741510254 ) ) ;
#41688=ORIENTED_EDGE ( 'NONE', *, *, #29904, .F. ) ;
#41690=CARTESIAN_POINT ( 'NONE',  ( 0.9873396505805591694, 0.1113553986120547346, 0.2116141732283464416 ) ) ;
#41696=FACE_OUTER_BOUND ( 'NONE', #17243, .T. ) ;
#41697=CARTESIAN_POINT ( 'NONE',  ( -0.9500414927467378812, -0.1787899950787401604, 1.707677165300566235 ) ) ;
#41698=VERTEX_POINT ( 'NONE', #38854 ) ;
#41700=CARTESIAN_POINT ( 'NONE',  ( -0.8759842519685039353, -0.1787899950787401882, 1.237696850339937038 ) ) ;
#41701=CARTESIAN_POINT ( 'NONE',  ( 1.033464566929133799, 0.000000000000000000, 1.850393700679873854 ) ) ;
#41702=CARTESIAN_POINT ( 'NONE',  ( 1.002407869896990045, -0.1264236179284866091, 1.360728346402929168 ) ) ;
#41704=CARTESIAN_POINT ( 'NONE',  ( -0.9500414927467378812, -0.1787899950787401604, 0.5708661416785201226 ) ) ;
#41705=CARTESIAN_POINT ( 'NONE',  ( -0.6971942568897637749, 2.189545951927499583E-17, 1.222933070812378009 ) ) ;
#41706=CARTESIAN_POINT ( 'NONE',  ( 0.9412147342319837628, 0.1574803149606300301, 1.542814960522393308 ) ) ;
#41709=CARTESIAN_POINT ( 'NONE',  ( 0.8759842519685039353, 0.1787899950787401882, 0.5880905511273386566 ) ) ;
#41710=CARTESIAN_POINT ( 'NONE',  ( -1.002407869896990045, -0.1264236179284866091, 0.4502952755367874427 ) ) ;
#41714=CARTESIAN_POINT ( 'NONE',  ( -1.033464566929133799, 0.000000000000000000, 0.3641732283464567121 ) ) ;
#41715=CARTESIAN_POINT ( 'NONE',  ( 0.7495606340400177148, 0.1264236179284866091, 1.144192913332062966 ) ) ;
#41718=CARTESIAN_POINT ( 'NONE',  ( -0.7495606340400177148, -0.1264236179284866091, 0.9178149605761574126 ) ) ;
#41720=CARTESIAN_POINT ( 'NONE',  ( -0.7185039370078746268, -0.06523048226347956391, 0.3075787401574803792 ) ) ;
#41721=CARTESIAN_POINT ( 'NONE',  ( -1.054774247047244540, 0.07405724077823318263, 0.06397637789899228433 ) ) ;
#41727=CARTESIAN_POINT ( 'NONE',  ( 0.8759842519685039353, 0.1787899950787401882, 1.331200787347811110 ) ) ;
#41731=CARTESIAN_POINT ( 'NONE',  ( 0.9873396505805591694, 0.1113553986120547346, 1.865157480314960647 ) ) ;
#41732=ADVANCED_FACE ( 'NONE', ( #35286 ), #46511, .T. ) ;
#41733=AXIS2_PLACEMENT_3D ( 'NONE', #24503, #2212, #28345 ) ;
#41739=CARTESIAN_POINT ( 'NONE',  ( -0.9500414927467377701, -0.1787899950787401604, 0.6889763778989936860 ) ) ;
#41740=EDGE_CURVE ( 'NONE', #6896, #13064, #16603, .T. ) ;
#41742=DIRECTION ( 'NONE',  ( 0.000000000000000000, 0.000000000000000000, -1.000000000000000000 ) ) ;
#41744=DIRECTION ( 'NONE',  ( 1.000000000000000000, 0.000000000000000000, -1.822029033848725275E-16 ) ) ;
#41746=CARTESIAN_POINT ( 'NONE',  ( 1.002407869896990045, -0.1264236179284866091, 1.518208661363559031 ) ) ;
#41747=CARTESIAN_POINT ( 'NONE',  ( 1.002407869896990045, -0.1264236179284866091, 1.906988188922614125 ) ) ;
#41748=CARTESIAN_POINT ( 'NONE',  ( 0.7495606340400177148, 0.1264236179284866091, 0.3124999999462365619 ) ) ;
#41751=CYLINDRICAL_SURFACE ( 'NONE', #32775, 0.1574803149606299191 ) ;
#41754=CARTESIAN_POINT ( 'NONE',  ( 0.8759842519685039353, 0.1787899950787401882, 0.4650590550643464716 ) ) ;
#41755=CARTESIAN_POINT ( 'NONE',  ( -0.7646288533564489232, -0.1113553986120547346, 0.7431102362204724532 ) ) ;
#41757=CARTESIAN_POINT ( 'NONE',  ( -0.8107537697050254399, -0.1574803149606297803, 1.326279527451528661 ) ) ;
#41758=CARTESIAN_POINT ( 'NONE',  ( -0.7185039370078714072, 0.06523048226347728795, 1.592027558947592958 ) ) ;
#41759=CARTESIAN_POINT ( 'NONE',  ( -1.054774247047244540, -0.07405724077823318263, 1.318897637741511364 ) ) ;
#41760=CARTESIAN_POINT ( 'NONE',  ( 0.8107537697050253289, 0.1574803149606300301, 0.7997047243019228535 ) ) ;
#41762=CARTESIAN_POINT ( 'NONE',  ( 1.002407869896990045, 0.1264236179284866091, 0.9374999999462362288 ) ) ;
#41766=CARTESIAN_POINT ( 'NONE',  ( -0.9412147342319837628, 0.1574803149606300301, 0.5191929132782994172 ) ) ;
#41768=CARTESIAN_POINT ( 'NONE',  ( -0.8759842519685039353, -0.1574803149606299191, 1.181102362204724310 ) ) ;
#41770=DIRECTION ( 'NONE',  ( -1.000000000000000000, 0.000000000000000000, 0.000000000000000000 ) ) ;
#41773=CARTESIAN_POINT ( 'NONE',  ( 0.8759842519685039353, -0.1574803149606299191, 1.368110236112944911 ) ) ;
#41778=CARTESIAN_POINT ( 'NONE',  ( 0.8019270111902716547, 0.1787899950787401604, 0.9448818897100165204 ) ) ;
#41779=CARTESIAN_POINT ( 'NONE',  ( -1.054774247047244096, 0.000000000000000000, 1.596948818843874074 ) ) ;
#41781=CARTESIAN_POINT ( 'NONE',  ( -1.054774247047244540, 0.07405724077823318263, 1.486220472387181690 ) ) ;
#41784=VERTEX_POINT ( 'NONE', #32157 ) ;
#41789=ORIENTED_EDGE ( 'NONE', *, *, #15662, .F. ) ;
#41792=EDGE_LOOP ( 'NONE', ( #41471, #33616, #4572, #20108 ) ) ;
#41793=EDGE_CURVE ( 'NONE', #13799, #22426, #17850, .T. ) ;
#41795=DIRECTION ( 'NONE',  ( 1.822029033848725028E-16, 0.000000000000000000, 1.000000000000000000 ) ) ;
#41796=CARTESIAN_POINT ( 'NONE',  ( 0.9412147342319837628, -0.1574803149606297803, 1.813484251968503935 ) ) ;
#41799=CARTESIAN_POINT ( 'NONE',  ( -1.054774247047244540, -0.07405724077823318263, 0.1427165353793073133 ) ) ;
#41800=CARTESIAN_POINT ( 'NONE',  ( -0.8107537697050253289, -0.1574803149606297803, 1.099901574803150650 ) ) ;
#41803=CARTESIAN_POINT ( 'NONE',  ( 0.8759842519685039353, 0.1787899950787401882, 1.139271653489543290 ) ) ;
#41804=CARTESIAN_POINT ( 'NONE',  ( 1.002407869896990045, 0.1264236179284866091, 1.444389763725763665 ) ) ;
#41806=CARTESIAN_POINT ( 'NONE',  ( 0.8759842519685039353, -0.1574803149606299191, 1.614173228346456712 ) ) ;
#41809=CARTESIAN_POINT ( 'NONE',  ( 0.9873396505805591694, -0.1113553986120547346, 0.4675196849318432601 ) ) ;
#41810=CARTESIAN_POINT ( 'NONE',  ( -0.9412147342319837628, -0.1574803149606297803, 1.606791338475149766 ) ) ;
#41812=CARTESIAN_POINT ( 'NONE',  ( 0.7495606340400177148, -0.1264236179284866091, 0.9916338582139527791 ) ) ;
#41813=CARTESIAN_POINT ( 'NONE',  ( 0.6971942568897648851, -0.07405724077823297447, 1.820866141678520789 ) ) ;
#41814=CARTESIAN_POINT ( 'NONE',  ( 0.8759842519685039353, -0.1574803149606299191, 0.3444881888688507976 ) ) ;
#41816=CARTESIAN_POINT ( 'NONE',  ( 0.9873396505805591694, -0.1113553986120547346, 1.894685039370078927 ) ) ;
#41818=CARTESIAN_POINT ( 'NONE',  ( -0.9873396505805591694, -0.1113553986120547346, 0.2706692912310554866 ) ) ;
#41819=CYLINDRICAL_SURFACE ( 'NONE', #24446, 0.1574803149606299191 ) ;
#41820=CARTESIAN_POINT ( 'NONE',  ( 0.9500414927467378812, 0.1787899950787401604, 1.249999999946235896 ) ) ;
#41824=CARTESIAN_POINT ( 'NONE',  ( -0.9873396505805591694, -0.1113553986120547346, 1.018700787294047228 ) ) ;
#41825=CARTESIAN_POINT ( 'NONE',  ( -0.7495606340400177148, 0.1264236179284866091, 0.5880905511273386566 ) ) ;
#41826=CARTESIAN_POINT ( 'NONE',  ( 0.8759842519685039353, -0.1574803149606299191, 1.368110236112944911 ) ) ;
#41831=CARTESIAN_POINT ( 'NONE',  ( -1.002407869896990045, -0.1264236179284866091, 1.045767716481669440 ) ) ;
#41832=CARTESIAN_POINT ( 'NONE',  ( -0.9500414927467378812, 0.1787899950787401604, 1.761811023568284007 ) ) ;
#41834=CARTESIAN_POINT ( 'NONE',  ( -0.8019270111902717657, -0.1787899950787401604, 0.6053149605761579677 ) ) ;
#41844=CARTESIAN_POINT ( 'NONE',  ( -0.7495606340400177148, -0.1264236179284866091, 0.4010826771115905687 ) ) ;
#41845=CYLINDRICAL_SURFACE ( 'NONE', #18019, 0.1574803149606299191 ) ;
#41846=EDGE_CURVE ( 'NONE', #22349, #15853, #9530, .T. ) ;
#41848=CARTESIAN_POINT ( 'NONE',  ( -1.033464566929133799, 0.000000000000000000, 1.220472440837354400 ) ) ;
#41855=CARTESIAN_POINT ( 'NONE',  ( 0.9412147342319837628, 0.1574803149606300301, 0.4502952755905510474 ) ) ;
#41858=CARTESIAN_POINT ( 'NONE',  ( -1.033464566929134687, -0.06523048226347956391, 1.296751968396409049 ) ) ;
#41859=CARTESIAN_POINT ( 'NONE',  ( 1.054774247047244540, -0.07405724077823318263, 0.6151574802611974313 ) ) ;
#41860=CARTESIAN_POINT ( 'NONE',  ( 0.7495606340400177148, 0.1264236179284866091, 0.07627952750529173875 ) ) ;
#41862=CARTESIAN_POINT ( 'NONE',  ( 0.9873396505805591694, -0.1113553986120547346, 0.3592519685039369803 ) ) ;
#41866=CARTESIAN_POINT ( 'NONE',  ( -0.7495606340400177148, 0.1264236179284866091, 1.144192913332062966 ) ) ;
#41867=CARTESIAN_POINT ( 'NONE',  ( 0.7646288533564489232, 0.1113553986120547346, 1.048228346456692828 ) ) ;
#41868=CARTESIAN_POINT ( 'NONE',  ( -0.9972233763874301937, -0.1313180930730347140, 1.990531206743730630 ) ) ;
#41871=CARTESIAN_POINT ( 'NONE',  ( -0.7185039370078739607, 0.000000000000000000, -2.869337061179095023E-17 ) ) ;
#41875=CARTESIAN_POINT ( 'NONE',  ( 0.7185039370078739607, 1.928577636452523993E-17, 0.2657480314960630197 ) ) ;
#41876=CARTESIAN_POINT ( 'NONE',  ( 1.002407869896990045, -0.1264236179284866091, 0.8046259841982047467 ) ) ;
#41877=CYLINDRICAL_SURFACE ( 'NONE', #39450, 0.1574803149606299191 ) ;
#41878=CARTESIAN_POINT ( 'NONE',  ( 0.8759842519685039353, -0.1574803149606299191, 0.9055118110236221041 ) ) ;
#41884=ORIENTED_EDGE ( 'NONE', *, *, #22016, .F. ) ;
#41885=CARTESIAN_POINT ( 'NONE',  ( -0.6971942568897648851, -0.07405724077823297447, 1.938976377898990799 ) ) ;
#41886=CARTESIAN_POINT ( 'NONE',  ( 1.054774247047244540, -0.07405724077823318263, 1.914370078686394860 ) ) ;
#41889=CARTESIAN_POINT ( 'NONE',  ( 1.054774247047244540, -0.07405724077823318263, 0.4576771653005669016 ) ) ;
#41890=CARTESIAN_POINT ( 'NONE',  ( -0.9500414927467378812, -0.1787899950787401604, 1.353346456639149986 ) ) ;
#41891=CYLINDRICAL_SURFACE ( 'NONE', #602, 0.1574803149606299191 ) ;
#41892=CARTESIAN_POINT ( 'NONE',  ( -0.8019270111902717657, -0.1787899950787401604, 0.9940944881352130613 ) ) ;
#41894=CARTESIAN_POINT ( 'NONE',  ( -0.9500414927467378812, 0.1787899950787401604, 0.1525590550643468046 ) ) ;
#41895=CARTESIAN_POINT ( 'NONE',  ( 0.9873396505805591694, -0.1113553986120547346, 1.579724409448818978 ) ) ;
#41896=CARTESIAN_POINT ( 'NONE',  ( -0.9500414927467378812, 0.1787899950787401604, 1.806102362150961316 ) ) ;
#41897=CARTESIAN_POINT ( 'NONE',  ( -0.8759842519685039353, -0.1787899950787401882, 0.05659448813521291560 ) ) ;
#41899=CARTESIAN_POINT ( 'NONE',  ( -0.9873396505805591694, -0.1113553986120547346, 1.737204724409448842 ) ) ;
#41901=CARTESIAN_POINT ( 'NONE',  ( 0.8759842519685039353, 0.1787899950787401882, 1.729822834591905556 ) ) ;
#41903=( BOUNDED_CURVE ( )  B_SPLINE_CURVE ( 2, ( #26902, #12048, #27151, #41706, #26670, #23537, #8906, #25789, #41220 ),
 .UNSPECIFIED., .F., .F. ) 
 B_SPLINE_CURVE_WITH_KNOTS ( ( 3, 2, 2, 2, 3 ),
 ( 0.7600000000000000089, 0.7624999999999999556, 0.7650000000000000133, 0.7674999999999999600, 0.7700000000000000178 ),
 .UNSPECIFIED. ) 
 CURVE ( )  GEOMETRIC_REPRESENTATION_ITEM ( )  RATIONAL_B_SPLINE_CURVE ( ( 1.000000000000000000, 0.9238795325112869605, 1.000000000000000000, 0.9238795325112869605, 1.000000000000000000, 0.9238795325112869605, 1.000000000000000000, 0.9238795325112829637, 1.000000000000000000 ) ) 
 REPRESENTATION_ITEM ( '' )  ) ;
#41905=VERTEX_POINT ( 'NONE', #38044 ) ;
#41911=CARTESIAN_POINT ( 'NONE',  ( -1.033464566929134687, -0.06523048226347956391, 0.5979330708661413363 ) ) ;
#41914=CARTESIAN_POINT ( 'NONE',  ( -0.9412147342319837628, 0.1574803149606300301, 0.8735236219397174429 ) ) ;
#41916=CARTESIAN_POINT ( 'NONE',  ( 0.7495606340400177148, 0.1264236179284866091, 0.8636811023084409733 ) ) ;
#41917=AXIS2_PLACEMENT_3D ( 'NONE', #2141, #45503, #1909 ) ;
#41918=( BOUNDED_CURVE ( )  B_SPLINE_CURVE ( 2, ( #26147, #36460, #40717, #8145, #3617, #4533, #19170, #33828, #18234 ),
 .UNSPECIFIED., .F., .T. ) 
 B_SPLINE_CURVE_WITH_KNOTS ( ( 3, 2, 2, 2, 3 ),
 ( 0.4699999999999999734, 0.4724999999999999756, 0.4749999999999999778, 0.4774999999999999800, 0.4799999999999999822 ),
 .UNSPECIFIED. ) 
 CURVE ( )  GEOMETRIC_REPRESENTATION_ITEM ( )  RATIONAL_B_SPLINE_CURVE ( ( 1.000000000000000000, 0.9238795325112879597, 1.000000000000000000, 0.9238795325112869605, 1.000000000000000000, 0.9238795325112869605, 1.000000000000000000, 0.9238795325112869605, 1.000000000000000000 ) ) 
 REPRESENTATION_ITEM ( '' )  ) ;
#41921=CARTESIAN_POINT ( 'NONE',  ( 0.7646288533564489232, -0.1113553986120547346, 1.087598425089322918 ) ) ;
#41922=CARTESIAN_POINT ( 'NONE',  ( 0.6971942568897648851, 0.07405724077823318263, 1.934055118056471567 ) ) ;
#41923=CARTESIAN_POINT ( 'NONE',  ( 0.8107537697050234415, -0.1574803149606297803, 0.1943897637795276023 ) ) ;
#41924=CYLINDRICAL_SURFACE ( 'NONE', #10701, 0.1574803149606299191 ) ;
#41926=DIRECTION ( 'NONE',  ( 1.822029033848725028E-16, 0.000000000000000000, 1.000000000000000000 ) ) ;
#41927=EDGE_CURVE ( 'NONE', #34447, #815, #5686, .T. ) ;
#41929=CARTESIAN_POINT ( 'NONE',  ( 1.002407869896990045, 0.1264236179284866091, 0.3469488188438744070 ) ) ;
#41930=CARTESIAN_POINT ( 'NONE',  ( -0.7495606340400177148, -0.1264236179284866091, 1.857775590497417362 ) ) ;
#41931=EDGE_LOOP ( 'NONE', ( #19289, #10447, #20161, #298 ) ) ;
#41932=CARTESIAN_POINT ( 'NONE',  ( -1.002407869896990045, 0.1264236179284866091, 1.252460629867496067 ) ) ;
#41934=CARTESIAN_POINT ( 'NONE',  ( 0.7495606340400177148, 0.1264236179284866091, 1.419783464513165505 ) ) ;
#41935=LINE ( 'NONE', #16799, #45843 ) ;
#41936=CARTESIAN_POINT ( 'NONE',  ( 0.6971942568897626646, 0.07405724077823318263, 0.08366141726907129483 ) ) ;
#41937=CARTESIAN_POINT ( 'NONE',  ( -0.6971942568897648851, 0.07405724077823318263, 1.259842519631276359 ) ) ;
#41938=CARTESIAN_POINT ( 'NONE',  ( -0.7185039370078739607, 1.928577636452523993E-17, 0.5807086614173228023 ) ) ;
#41939=CARTESIAN_POINT ( 'NONE',  ( 0.8107537697050254399, 0.1574803149606300301, 1.203248031496062520 ) ) ;
#41940=CARTESIAN_POINT ( 'NONE',  ( 0.6971942568897648851, 0.07405724077823318263, 0.5954724408911187261 ) ) ;
#41941=CARTESIAN_POINT ( 'NONE',  ( -0.7495606340400177148, -0.1264236179284866091, 0.5585629920722204877 ) ) ;
#41944=VERTEX_POINT ( 'NONE', #1847 ) ;
#41947=CARTESIAN_POINT ( 'NONE',  ( -1.033464566929133799, 0.000000000000000000, 0.3248031496062992463 ) ) ;
#41948=CARTESIAN_POINT ( 'NONE',  ( 1.002407869896990045, -0.1264236179284866091, 1.203248031442299304 ) ) ;
#41950=CARTESIAN_POINT ( 'NONE',  ( 1.033464566929133799, 0.000000000000000000, 1.220472440837354400 ) ) ;
#41951=ORIENTED_EDGE ( 'NONE', *, *, #18881, .F. ) ;
#41953=CARTESIAN_POINT ( 'NONE',  ( -0.8759842519685039353, 0.1787899950787401882, 0.9030511810485984947 ) ) ;
#41955=CARTESIAN_POINT ( 'NONE',  ( -0.6971942568897626646, -0.07405724077823297447, 0.2017716534895435399 ) ) ;
#41956=ORIENTED_EDGE ( 'NONE', *, *, #13436, .T. ) ;
#41960=CARTESIAN_POINT ( 'NONE',  ( 0.9500414927467378812, 0.1787899950787401604, 1.328740157426552049 ) ) ;
#41963=DIRECTION ( 'NONE',  ( 0.000000000000000000, 0.000000000000000000, -1.000000000000000000 ) ) ;
#41965=CARTESIAN_POINT ( 'NONE',  ( 0.8107537697050254399, 0.1574803149606300301, 1.872539370078740495 ) ) ;
#41966=CARTESIAN_POINT ( 'NONE',  ( 0.8019270111902717657, 0.1787899950787401604, 1.569881889710015299 ) ) ;
#41969=CARTESIAN_POINT ( 'NONE',  ( -1.033464566929133799, 0.000000000000000000, 1.732283464459401623 ) ) ;
#41970=CARTESIAN_POINT ( 'NONE',  ( -0.9500414927467377701, 0.1787899950787401604, 0.8218503936470251681 ) ) ;
#41975=CARTESIAN_POINT ( 'NONE',  ( -0.7799827560997787401, -0.1420106181070925344, 1.986315487003310620 ) ) ;
#41976=CARTESIAN_POINT ( 'NONE',  ( -0.7185039370078739607, 1.928577636452523993E-17, 1.250000000000000000 ) ) ;
#41979=CARTESIAN_POINT ( 'NONE',  ( 0.7495606340400177148, -0.1264236179284866091, 1.468996062938362046 ) ) ;
#41980=CARTESIAN_POINT ( 'NONE',  ( 0.9500414927467377701, 0.1787899950787401604, 1.840551181048599938 ) ) ;
#41981=CARTESIAN_POINT ( 'NONE',  ( 0.8019270111902716547, -0.1787899950787401604, 0.3248031495525355861 ) ) ;
#41985=DIRECTION ( 'NONE',  ( 0.000000000000000000, 0.000000000000000000, -1.000000000000000000 ) ) ;
#41988=CARTESIAN_POINT ( 'NONE',  ( 0.9873396505805591694, -0.1113553986120547346, 0.5068897636720007815 ) ) ;
#41990=CARTESIAN_POINT ( 'NONE',  ( 0.7495606340400177148, -0.1264236179284866091, 0.4010826771115905687 ) ) ;
#41991=CARTESIAN_POINT ( 'NONE',  ( 0.7185039370078739607, 1.928577636452523993E-17, 0.2263779527559055260 ) ) ;
#41992=CARTESIAN_POINT ( 'NONE',  ( -0.7495606340400177148, -0.1264236179284866091, 1.345964566875370139 ) ) ;
#41993=CARTESIAN_POINT ( 'NONE',  ( 0.9873396505805591694, -0.1113553986120547346, 0.7824803148531023211 ) ) ;
#41996=CARTESIAN_POINT ( 'NONE',  ( 1.054774247047244540, -0.07405724077823318263, 1.008858267662772423 ) ) ;
#41999=ORIENTED_EDGE ( 'NONE', *, *, #11231, .T. ) ;
#42000=CARTESIAN_POINT ( 'NONE',  ( -1.033464566929134687, -0.06523048226347956391, 0.5880905510735753294 ) ) ;
#42001=CARTESIAN_POINT ( 'NONE',  ( 0.9873396505805591694, 0.1113553986120547346, 0.09350393700787401619 ) ) ;
#42002=CARTESIAN_POINT ( 'NONE',  ( -0.7185039370078746268, -0.06523048226347956391, 1.213090551181103427 ) ) ;
#42003=CARTESIAN_POINT ( 'NONE',  ( 0.7185039370078746268, 0.06523048226347956391, 0.5782480314960627421 ) ) ;
#42004=DIRECTION ( 'NONE',  ( 0.000000000000000000, 0.000000000000000000, -1.000000000000000000 ) ) ;
#42006=CARTESIAN_POINT ( 'NONE',  ( 0.8019270111902716547, 0.1787899950787401604, 0.1181102361667090567 ) ) ;
#42007=CARTESIAN_POINT ( 'NONE',  ( -0.8019270111902716547, -0.1787899950787401604, 0.1279527558517483676 ) ) ;
#42008=CARTESIAN_POINT ( 'NONE',  ( 0.9412147342319837628, -0.1574803149606297803, 1.370570866034205970 ) ) ;
#42010=ORIENTED_EDGE ( 'NONE', *, *, #11332, .T. ) ;
#42013=CARTESIAN_POINT ( 'NONE',  ( 0.8759842519685039353, 0.1787899950787401882, 0.7062007873478109987 ) ) ;
#42015=CARTESIAN_POINT ( 'NONE',  ( -0.9500414927467377701, -0.1787899950787401604, 1.747047244040724312 ) ) ;
#42020=AXIS2_PLACEMENT_3D ( 'NONE', #28074, #5772, #16564 ) ;
#42024=ORIENTED_EDGE ( 'NONE', *, *, #12957, .F. ) ;
#42032=EDGE_CURVE ( 'NONE', #6761, #24301, #8564, .T. ) ;
#42033=CARTESIAN_POINT ( 'NONE',  ( 0.7185039370078746268, -0.06523048226347956391, 1.803641732283465693 ) ) ;
#42037=( BOUNDED_CURVE ( )  B_SPLINE_CURVE ( 2, ( #20539, #10727, #7352, #14314, #600, #15257, #33250, #29209, #40613 ),
 .UNSPECIFIED., .F., .T. ) 
 B_SPLINE_CURVE_WITH_KNOTS ( ( 3, 2, 2, 2, 3 ),
 ( 0.2700000000000000178, 0.2725000000000000200, 0.2750000000000000222, 0.2775000000000000244, 0.2800000000000000266 ),
 .UNSPECIFIED. ) 
 CURVE ( )  GEOMETRIC_REPRESENTATION_ITEM ( )  RATIONAL_B_SPLINE_CURVE ( ( 1.000000000000000000, 0.9238795325112869605, 1.000000000000000000, 0.9238795325112869605, 1.000000000000000000, 0.9238795325112869605, 1.000000000000000000, 0.9238795325112869605, 1.000000000000000000 ) ) 
 REPRESENTATION_ITEM ( '' )  ) ;
#42038=CARTESIAN_POINT ( 'NONE',  ( -1.054774247047244540, 0.07405724077823318263, 0.3444881889226146243 ) ) ;
#42039=CARTESIAN_POINT ( 'NONE',  ( -0.9873396505805591694, -0.1113553986120547346, 1.028543307086614123 ) ) ;
#42041=CARTESIAN_POINT ( 'NONE',  ( 0.7646288533564489232, 0.1113553986120547346, 0.4183070866141732624 ) ) ;
#42042=CARTESIAN_POINT ( 'NONE',  ( 1.054774247047244540, 0.07405724077823318263, 0.2214566928596221063 ) ) ;
#42043=CARTESIAN_POINT ( 'NONE',  ( 0.9412147342319837628, -0.1574803149606297803, 0.2386811023622048278 ) ) ;
#42044=CARTESIAN_POINT ( 'NONE',  ( 0.7185039370078746268, 0.06523048226347956391, 1.523129921259841923 ) ) ;
#42045=CARTESIAN_POINT ( 'NONE',  ( 0.8107537697050254399, -0.1574803149606297803, 1.414862204724410377 ) ) ;
#42050=CARTESIAN_POINT ( 'NONE',  ( 0.9873396505805591694, -0.1113553986120547346, 1.658464566929134021 ) ) ;
#42051=CARTESIAN_POINT ( 'NONE',  ( 0.6971942568897648851, -0.07405724077823297447, 0.9104330708123777871 ) ) ;
#42053=CARTESIAN_POINT ( 'NONE',  ( 0.9500414927467377701, 0.1787899950787401604, 1.963582677111591401 ) ) ;
#42054=CARTESIAN_POINT ( 'NONE',  ( 0.7646288533564489232, 0.1113553986120547346, 0.3690944880814492901 ) ) ;
#42055=VERTEX_POINT ( 'NONE', #34236 ) ;
#42056=CARTESIAN_POINT ( 'NONE',  ( 1.000925231368313018, 0.1081788907238402098, 0.03936919960863846657 ) ) ;
#42057=CARTESIAN_POINT ( 'NONE',  ( -1.033464566929133799, 0.000000000000000000, 1.062992125876724314 ) ) ;
#42059=CARTESIAN_POINT ( 'NONE',  ( -0.8107537697050234415, -0.1574803149606297803, 0.2632874014672759722 ) ) ;
#42060=CARTESIAN_POINT ( 'NONE',  ( 1.054774247047244540, -0.07405724077823318263, 1.240157480261197431 ) ) ;
#42062=CARTESIAN_POINT ( 'NONE',  ( 0.8759842519685039353, 0.1574803149606299191, 1.230314960522393752 ) ) ;
#42066=CARTESIAN_POINT ( 'NONE',  ( -0.6971942568897626646, 0.07405724077823318263, 0.6299212597887560161 ) ) ;
#42067=CARTESIAN_POINT ( 'NONE',  ( -0.7185039370078746268, -0.06523048226347956391, 0.2682086614173227468 ) ) ;
#42069=VERTEX_POINT ( 'NONE', #32533 ) ;
#42070=EDGE_CURVE ( 'NONE', #19175, #43630, #28224, .T. ) ;
#42073=CARTESIAN_POINT ( 'NONE',  ( -0.8019270111902717657, 0.1787899950787401604, 1.023622047190330342 ) ) ;
#42074=CARTESIAN_POINT ( 'NONE',  ( -1.054774247047244540, -0.07405724077823318263, 1.988188976324187562 ) ) ;
#42076=CARTESIAN_POINT ( 'NONE',  ( -0.8759842519685039353, 0.1787899950787401882, 0.9768700786863937502 ) ) ;
#42077=CARTESIAN_POINT ( 'NONE',  ( -0.8759842519685039353, 0.1787899950787401882, 0.7455708660879684091 ) ) ;
#42083=CARTESIAN_POINT ( 'NONE',  ( 0.7185039370078746268, -0.06523048226347956391, 1.921751968503937480 ) ) ;
#42086=CARTESIAN_POINT ( 'NONE',  ( -0.6971942568897626646, 0.07405724077823318263, 0.4724409448281262636 ) ) ;
#42090=CARTESIAN_POINT ( 'NONE',  ( -0.7495606340400177148, 0.1264236179284866091, 1.695374015694267822 ) ) ;
#42091=VECTOR ( 'NONE', #26602, 39.37007874015748143 ) ;
#42097=CARTESIAN_POINT ( 'NONE',  ( -0.8759842519685039353, 0.1574803149606299191, 1.230314960522393752 ) ) ;
#42100=CARTESIAN_POINT ( 'NONE',  ( -0.7185039370078746268, 0.06523048226347956391, 1.198326771546015967 ) ) ;
#42102=DIRECTION ( 'NONE',  ( 0.000000000000000000, 0.000000000000000000, -1.000000000000000000 ) ) ;
#42103=CARTESIAN_POINT ( 'NONE',  ( -0.6971942568897648851, -0.07405724077823297447, 1.112204724355684959 ) ) ;
#42104=CARTESIAN_POINT ( 'NONE',  ( 0.8107537697050253289, -0.1574803149606297803, 1.060531496062992352 ) ) ;
#42106=CARTESIAN_POINT ( 'NONE',  ( -0.7185039370078739607, 0.000000000000000000, -2.869337061179095023E-17 ) ) ;
#42109=CARTESIAN_POINT ( 'NONE',  ( -0.9873396505805591694, -0.1113553986120547346, 1.963582677057826853 ) ) ;
#42110=CARTESIAN_POINT ( 'NONE',  ( 0.8759842519685039353, 0.1574803149606299191, 0.6003937006798740761 ) ) ;
#42113=CARTESIAN_POINT ( 'NONE',  ( 1.054774247047244540, 0.07405724077823318263, 0.7726377952218265177 ) ) ;
#42115=CARTESIAN_POINT ( 'NONE',  ( 0.7185039370078739607, 1.928577636452523993E-17, 1.446850393700787274 ) ) ;
#42116=CARTESIAN_POINT ( 'NONE',  ( -0.7185039370078746268, 0.06523048226347956391, 0.4502952754830242821 ) ) ;
#42121=CARTESIAN_POINT ( 'NONE',  ( 0.8107537697050254399, -0.1574803149606297803, 1.168799212490898576 ) ) ;
#42123=ORIENTED_EDGE ( 'NONE', *, *, #31033, .T. ) ;
#42125=CARTESIAN_POINT ( 'NONE',  ( -0.8019270111902717657, -0.1787899950787401604, 1.983267716481667886 ) ) ;
#42126=EDGE_CURVE ( 'NONE', #34753, #460, #5260, .T. ) ;
#42127=CARTESIAN_POINT ( 'NONE',  ( 0.7495606340400177148, -0.1264236179284866091, 1.823326771599779406 ) ) ;
#42129=CARTESIAN_POINT ( 'NONE',  ( 0.8107537697050254399, -0.1574803149606297803, 1.769192913385826404 ) ) ;
#42130=CARTESIAN_POINT ( 'NONE',  ( 0.9500414927467378812, 0.1787899950787401604, 0.3887795275052913224 ) ) ;
#42132=CARTESIAN_POINT ( 'NONE',  ( -0.6971942568897637749, 2.189545951927499583E-17, 1.301673228292692830 ) ) ;
#42133=EDGE_CURVE ( 'NONE', #8550, #32499, #32860, .T. ) ;
#42136=CARTESIAN_POINT ( 'NONE',  ( -1.054774247047244540, 0.07405724077823318263, 0.3051181101824569919 ) ) ;
#42137=CARTESIAN_POINT ( 'NONE',  ( -0.7185039370078739607, 1.928577636452523993E-17, 0.5807086614173228023 ) ) ;
#42138=CARTESIAN_POINT ( 'NONE',  ( -0.6971942568897648851, -0.07405724077823297447, 1.663385826717890925 ) ) ;
#42140=CARTESIAN_POINT ( 'NONE',  ( -0.9873396505805591694, 0.1113553986120547346, 1.786417322834645605 ) ) ;
#42141=CARTESIAN_POINT ( 'NONE',  ( -0.7646288533564489232, -0.1113553986120547346, 0.9399606299212598381 ) ) ;
#42144=CARTESIAN_POINT ( 'NONE',  ( 1.002407869896990045, -0.1264236179284866091, 1.715059055064346527 ) ) ;
#42146=CARTESIAN_POINT ( 'NONE',  ( -1.033464566929134687, -0.06523048226347956391, 0.7455708660342049710 ) ) ;
#42149=CARTESIAN_POINT ( 'NONE',  ( -0.8019270111902716547, 0.1787899950787401604, 1.259842519631276359 ) ) ;
#42153=VECTOR ( 'NONE', #31367, 39.37007874015748143 ) ;
#42154=CARTESIAN_POINT ( 'NONE',  ( -0.9412147342319837628, 0.1574803149606300301, 1.277066929133857442 ) ) ;
#42158=CARTESIAN_POINT ( 'NONE',  ( -0.7646288533564489232, 0.1113553986120547346, 0.7627952754830236159 ) ) ;
#42160=VECTOR ( 'NONE', #26755, 39.37007874015748143 ) ;
#42162=LINE ( 'NONE', #9606, #6192 ) ;
#42163=CARTESIAN_POINT ( 'NONE',  ( 0.7495606340400177148, 0.1264236179284866091, 0.9817913385289134265 ) ) ;
#42165=CARTESIAN_POINT ( 'NONE',  ( 0.7185039370078746268, 0.06523048226347956391, 0.6176181102362199304 ) ) ;
#42167=CARTESIAN_POINT ( 'NONE',  ( 0.8759842519685039353, 0.1574803149606299191, 0.04921259831766984505 ) ) ;
#42168=CARTESIAN_POINT ( 'NONE',  ( 0.7185039370078746268, -0.06523048226347956391, 0.2288385826771656140 ) ) ;
#42174=CARTESIAN_POINT ( 'NONE',  ( -0.7495606340400177148, 0.1264236179284866091, 1.887303149552535420 ) ) ;
#42175=ORIENTED_EDGE ( 'NONE', *, *, #28714, .F. ) ;
#42176=CARTESIAN_POINT ( 'NONE',  ( -0.8019270111902717657, -0.1787899950787401604, 1.392716535379308285 ) ) ;
#42179=CARTESIAN_POINT ( 'NONE',  ( 1.002407869896990045, -0.1264236179284866091, 1.478838582623401399 ) ) ;
#42180=CARTESIAN_POINT ( 'NONE',  ( -1.033464566929133799, 0.000000000000000000, 0.9153543307086614567 ) ) ;
#42182=CARTESIAN_POINT ( 'NONE',  ( -1.002407869896990045, -0.1264236179284866091, 0.6914370078202519698 ) ) ;
#42183=CARTESIAN_POINT ( 'NONE',  ( -0.8759842519685039353, -0.1787899950787401882, 1.232775590497417362 ) ) ;
#42184=EDGE_CURVE ( 'NONE', #18202, #6796, #35864, .T. ) ;
#42187=CARTESIAN_POINT ( 'NONE',  ( 1.054774247047244540, 0.07405724077823318263, 0.6200787401037166635 ) ) ;
#42188=CARTESIAN_POINT ( 'NONE',  ( -0.6971942568897648851, 0.07405724077823318263, 0.5511811023084406402 ) ) ;
#42190=( BOUNDED_CURVE ( )  B_SPLINE_CURVE ( 2, ( #32626, #2863, #29296, #7425, #21324, #33097, #3360, #218, #35955 ),
 .UNSPECIFIED., .F., .F. ) 
 B_SPLINE_CURVE_WITH_KNOTS ( ( 3, 2, 2, 2, 3 ),
 ( 0.2600000000000000089, 0.2625000000000000111, 0.2650000000000000133, 0.2675000000000000155, 0.2700000000000000178 ),
 .UNSPECIFIED. ) 
 CURVE ( )  GEOMETRIC_REPRESENTATION_ITEM ( )  RATIONAL_B_SPLINE_CURVE ( ( 1.000000000000000000, 0.9238795325112869605, 1.000000000000000000, 0.9238795325112869605, 1.000000000000000000, 0.9238795325112869605, 1.000000000000000000, 0.9238795325112869605, 1.000000000000000000 ) ) 
 REPRESENTATION_ITEM ( '' )  ) ;
#42193=VERTEX_POINT ( 'NONE', #32295 ) ;
#42195=CARTESIAN_POINT ( 'NONE',  ( -0.8759842519685039353, 0.1574803149606299191, 0.2559055118110236116 ) ) ;
#42196=CARTESIAN_POINT ( 'NONE',  ( 0.9500414927467377701, -0.1787899950787401604, 1.318897637741511364 ) ) ;
#42198=CARTESIAN_POINT ( 'NONE',  ( -0.7185039370078766252, -0.06523048226348168721, 1.833169291231055542 ) ) ;
#42201=AXIS2_PLACEMENT_3D ( 'NONE', #14273, #21691, #18089 ) ;
#42202=VECTOR ( 'NONE', #31545, 39.37007874015748143 ) ;
#42203=CARTESIAN_POINT ( 'NONE',  ( -1.054774247047244540, -0.07405724077823318263, 1.008858267662772423 ) ) ;
#42206=CARTESIAN_POINT ( 'NONE',  ( 0.9873396505805591694, 0.1113553986120547346, 0.9990157480314961758 ) ) ;
#42208=CARTESIAN_POINT ( 'NONE',  ( -0.8107537697050234415, -0.1574803149606297803, 0.07627952755905519078 ) ) ;
#42209=CARTESIAN_POINT ( 'NONE',  ( 0.7495606340400177148, -0.1264236179284866091, 1.464074803095842370 ) ) ;
#42212=( BOUNDED_CURVE ( )  B_SPLINE_CURVE ( 2, ( #11456, #40882, #4003, #25838, #29480, #11938, #3553, #18166, #7603 ),
 .UNSPECIFIED., .F., .F. ) 
 B_SPLINE_CURVE_WITH_KNOTS ( ( 3, 2, 2, 2, 3 ),
 ( 0.8800000000000000044, 0.8824999999999999512, 0.8850000000000000089, 0.8874999999999999556, 0.8900000000000000133 ),
 .UNSPECIFIED. ) 
 CURVE ( )  GEOMETRIC_REPRESENTATION_ITEM ( )  RATIONAL_B_SPLINE_CURVE ( ( 1.000000000000000000, 0.9238795325112869605, 1.000000000000000000, 0.9238795325112869605, 1.000000000000000000, 0.9238795325112869605, 1.000000000000000000, 0.9238795325112869605, 1.000000000000000000 ) ) 
 REPRESENTATION_ITEM ( '' )  ) ;
#42217=CARTESIAN_POINT ( 'NONE',  ( 0.7495606340400177148, -0.1264236179284866091, 1.621555118056472455 ) ) ;
#42223=CARTESIAN_POINT ( 'NONE',  ( 1.002407869896990045, 0.1264236179284866091, 0.4601377952218267953 ) ) ;
#42225=CARTESIAN_POINT ( 'NONE',  ( -0.9500414927467377701, 0.1787899950787401604, 0.7431102361667091261 ) ) ;
#42230=CARTESIAN_POINT ( 'NONE',  ( -0.8759842519685039353, 0.1574803149606299191, 1.033464566821606478 ) ) ;
#42231=CARTESIAN_POINT ( 'NONE',  ( 1.054774247047244540, -0.07405724077823318263, 1.441929133804504604 ) ) ;
#42233=CARTESIAN_POINT ( 'NONE',  ( 0.7495606340400177148, 0.1264236179284866091, 0.4306102361667086820 ) ) ;
#42237=CARTESIAN_POINT ( 'NONE',  ( -0.9873396505805591694, -0.1113553986120547346, 0.1525590550105832555 ) ) ;
#42242=CARTESIAN_POINT ( 'NONE',  ( 0.8759842519685039353, -0.1787899950787401882, 0.4060039369541102450 ) ) ;
#42244=EDGE_CURVE ( 'NONE', #40844, #42055, #46168, .T. ) ;
#42246=CARTESIAN_POINT ( 'NONE',  ( -1.054774247047244540, 0.07405724077823318263, 1.402559055064346971 ) ) ;
#42247=CARTESIAN_POINT ( 'NONE',  ( 0.8107537697050253289, -0.1574803149606297803, 0.8538385825696385156 ) ) ;
#42248=ORIENTED_EDGE ( 'NONE', *, *, #5419, .T. ) ;
#42249=CARTESIAN_POINT ( 'NONE',  ( -1.033464566929133799, 0.000000000000000000, 0.1181102361129454797 ) ) ;
#42250=CARTESIAN_POINT ( 'NONE',  ( 0.9500414927467378812, 0.1787899950787401604, 0.9399606298674970661 ) ) ;
#42255=CARTESIAN_POINT ( 'NONE',  ( -0.8759842519685039353, 0.1574803149606299191, 0.6397637794200314865 ) ) ;
#42257=CARTESIAN_POINT ( 'NONE',  ( -1.033464566929134687, 0.06523048226347956391, 1.429625984251968074 ) ) ;
#42259=CARTESIAN_POINT ( 'NONE',  ( -1.033464566929134687, 0.06523048226347956391, 0.5142716534357801850 ) ) ;
#42260=CARTESIAN_POINT ( 'NONE',  ( -1.033464566929134687, 0.06523048226347956391, 0.7209645669291341319 ) ) ;
#42262=CARTESIAN_POINT ( 'NONE',  ( 0.8759842519685039353, -0.1787899950787401882, 0.2140748030958428971 ) ) ;
#42263=CARTESIAN_POINT ( 'NONE',  ( 0.9873396505805591694, -0.1113553986120547346, 1.373031495955464587 ) ) ;
#42264=ORIENTED_EDGE ( 'NONE', *, *, #10963, .T. ) ;
#42265=EDGE_LOOP ( 'NONE', ( #46500, #42512, #32056, #26218 ) ) ;
#42268=CARTESIAN_POINT ( 'NONE',  ( -0.7495606340400177148, 0.1264236179284866091, 1.729822834591905556 ) ) ;
#42273=CARTESIAN_POINT ( 'NONE',  ( 0.7185039370078739607, 1.928577636452523993E-17, 1.594488188868850242 ) ) ;
#42280=CARTESIAN_POINT ( 'NONE',  ( 0.7646288533564489232, 0.1113553986120547346, 1.747047243986960652 ) ) ;
#42281=EDGE_CURVE ( 'NONE', #14529, #41944, #31314, .T. ) ;
#42282=CARTESIAN_POINT ( 'NONE',  ( -1.033464566929133799, 0.000000000000000000, 1.466535433070866201 ) ) ;
#42284=CARTESIAN_POINT ( 'NONE',  ( 0.8107537697050253289, 0.1574803149606300301, 1.872539370078740495 ) ) ;
#42286=CARTESIAN_POINT ( 'NONE',  ( -0.9500414927467377701, -0.1787899950787401604, 0.3346456692375752162 ) ) ;
#42287=CARTESIAN_POINT ( 'NONE',  ( -0.7185039370078739607, 1.928577636452523993E-17, 1.092519685039370136 ) ) ;
#42290=CARTESIAN_POINT ( 'NONE',  ( 1.054774247047244540, -0.07405724077823318263, 1.087598425143086578 ) ) ;
#42291=CARTESIAN_POINT ( 'NONE',  ( 1.054774247047244540, -0.07405724077823318263, 1.397637795221827517 ) ) ;
#42292=CARTESIAN_POINT ( 'NONE',  ( 0.9500414927467377701, -0.1787899950787401604, 0.2116141731745827814 ) ) ;
#42293=CARTESIAN_POINT ( 'NONE',  ( 0.9873396505805591694, -0.1113553986120547346, 0.2411417322834645827 ) ) ;
#42294=EDGE_CURVE ( 'NONE', #38421, #17885, #19943, .T. ) ;
#42295=CARTESIAN_POINT ( 'NONE',  ( 0.8759842519685039353, 0.1574803149606299191, 1.633858267716535639 ) ) ;
#42297=CARTESIAN_POINT ( 'NONE',  ( 0.7560775457342543415, 0.1089356967155813427, 1.980950116515386217 ) ) ;
#42298=CARTESIAN_POINT ( 'NONE',  ( 0.7185039370078739607, 1.928577636452523993E-17, 1.722440944881889813 ) ) ;
#42304=CARTESIAN_POINT ( 'NONE',  ( 0.8019270111902716547, 0.1787899950787401604, 0.9399606298674970661 ) ) ;
#42305=CARTESIAN_POINT ( 'NONE',  ( -1.002407869896990045, -0.1264236179284866091, 1.158956692859621995 ) ) ;
#42306=CARTESIAN_POINT ( 'NONE',  ( 0.9873396505805591694, 0.1113553986120547346, 0.3986220471365669038 ) ) ;
#42309=CARTESIAN_POINT ( 'NONE',  ( 1.032071497351902956, 0.03428311989231668661, 0.03936989784698766148 ) ) ;
#42310=CARTESIAN_POINT ( 'NONE',  ( -0.6971942568897637749, 2.189545951927499583E-17, 0.8341535432533228045 ) ) ;
#42312=CARTESIAN_POINT ( 'NONE',  ( -0.9873396505805591694, 0.1113553986120547346, 0.3198818896562523606 ) ) ;
#42313=CARTESIAN_POINT ( 'NONE',  ( 0.8019270111902717657, 0.1787899950787401604, 1.294291338528912982 ) ) ;
#42316=CARTESIAN_POINT ( 'NONE',  ( 0.8759842519685039353, 0.000000000000000000, 4.498031496062992574 ) ) ;
#42319=CARTESIAN_POINT ( 'NONE',  ( -0.9500414927467378812, 0.1787899950787401604, 0.6200787401037165525 ) ) ;
#42320=FACE_OUTER_BOUND ( 'NONE', #4501, .T. ) ;
#42324=CARTESIAN_POINT ( 'NONE',  ( -0.8019270111902717657, -0.1787899950787401604, 0.9596456692375764375 ) ) ;
#42325=CARTESIAN_POINT ( 'NONE',  ( -0.8107537697050253289, 0.1574803149606300301, 0.06151574803149607168 ) ) ;
#42326=CARTESIAN_POINT ( 'NONE',  ( -1.002407869896990045, 0.1264236179284866091, 0.9719488188438739629 ) ) ;
#42327=CARTESIAN_POINT ( 'NONE',  ( -1.002407869896990045, 0.1264236179284866091, 0.6619094487651338010 ) ) ;
#42329=CARTESIAN_POINT ( 'NONE',  ( -0.7185039370078739607, 1.928577636452523993E-17, 0.09842519674286673292 ) ) ;
#42336=CARTESIAN_POINT ( 'NONE',  ( 0.7185039370078739607, 1.928577636452523993E-17, 1.761811023622047223 ) ) ;
#42337=CARTESIAN_POINT ( 'NONE',  ( -0.8759842519685039353, 0.1787899950787401882, 0.5831692912848189803 ) ) ;
#42340=CARTESIAN_POINT ( 'NONE',  ( -0.8019270111902716547, -0.1787899950787401604, 1.628937007820252303 ) ) ;
#42343=CARTESIAN_POINT ( 'NONE',  ( -1.033464566929133799, 0.000000000000000000, 0.1968503935932602311 ) ) ;
#42344=CARTESIAN_POINT ( 'NONE',  ( 0.9412147342319837628, 0.1574803149606300301, 0.6471456692913394315 ) ) ;
#42345=CARTESIAN_POINT ( 'NONE',  ( 0.8107537697050253289, -0.1574803149606297803, 0.5487204724409447953 ) ) ;
#42348=CARTESIAN_POINT ( 'NONE',  ( -0.8107537697050253289, 0.1574803149606300301, 1.232775590443654812 ) ) ;
#42353=CARTESIAN_POINT ( 'NONE',  ( -1.033464566929133799, 0.000000000000000000, 1.742125984251968518 ) ) ;
#42354=ORIENTED_EDGE ( 'NONE', *, *, #25392, .F. ) ;
#42356=CARTESIAN_POINT ( 'NONE',  ( 1.033464566929134687, -0.06523048226347956391, 1.109744094488189115 ) ) ;
#42362=FACE_OUTER_BOUND ( 'NONE', #4476, .T. ) ;
#42364=CARTESIAN_POINT ( 'NONE',  ( 1.033464566929133799, 0.000000000000000000, 1.663385826771653697 ) ) ;
#42367=CARTESIAN_POINT ( 'NONE',  ( 0.8019270111902717657, -0.1787899950787401604, 0.8366141731745828647 ) ) ;
#42369=CARTESIAN_POINT ( 'NONE',  ( 0.8107537697050254399, -0.1574803149606297803, 1.296751968503936592 ) ) ;
#42370=CARTESIAN_POINT ( 'NONE',  ( -0.7185039370078746268, 0.06523048226347956391, 0.5388779527559055538 ) ) ;
#42374=CARTESIAN_POINT ( 'NONE',  ( 0.7185039370078739607, 1.928577636452523993E-17, 1.161417322727118284 ) ) ;
#42376=CARTESIAN_POINT ( 'NONE',  ( -0.8019270111902717657, 0.1787899950787401604, 1.929133858213952335 ) ) ;
#42377=CARTESIAN_POINT ( 'NONE',  ( 0.8759842519685039353, -0.1787899950787401882, 1.788877952702141672 ) ) ;
#42378=ORIENTED_EDGE ( 'NONE', *, *, #42184, .F. ) ;
#42380=CARTESIAN_POINT ( 'NONE',  ( 0.9412147342319837628, -0.1574803149606297803, 1.774114173228345859 ) ) ;
#42381=CARTESIAN_POINT ( 'NONE',  ( -1.054774247047244096, 0.000000000000000000, 1.478838582623401399 ) ) ;
#42383=CARTESIAN_POINT ( 'NONE',  ( -0.8019270111902717657, 0.1787899950787401604, 0.3149606298674962890 ) ) ;
#42385=CARTESIAN_POINT ( 'NONE',  ( -1.002407869896990045, 0.1264236179284866091, 1.685531496009228469 ) ) ;
#42386=CARTESIAN_POINT ( 'NONE',  ( -0.8107537697050253289, 0.1574803149606300301, 1.675688976377952777 ) ) ;
#42390=CARTESIAN_POINT ( 'NONE',  ( 0.6971942568897648851, 0.07405724077823318263, 1.697834645615527771 ) ) ;
#42393=CARTESIAN_POINT ( 'NONE',  ( -0.8107537697050254399, 0.1574803149606300301, 0.05167322823892971789 ) ) ;
#42396=CARTESIAN_POINT ( 'NONE',  ( -1.054774247047244096, 0.000000000000000000, 1.208169291284818980 ) ) ;
#42403=CARTESIAN_POINT ( 'NONE',  ( -1.033464566929134687, 0.06523048226347956391, 0.8686023620971983217 ) ) ;
#42404=CARTESIAN_POINT ( 'NONE',  ( -0.8759842519685039353, 0.1574803149606299191, 0.6889763779527560139 ) ) ;
#42407=CARTESIAN_POINT ( 'NONE',  ( 1.002407869896990045, -0.1264236179284866091, 1.001476377898992132 ) ) ;
#42411=CARTESIAN_POINT ( 'NONE',  ( 0.7646288533564489232, 0.1113553986120547346, 0.05413385816018952829 ) ) ;
#42414=CARTESIAN_POINT ( 'NONE',  ( -1.054774247047244540, 0.07405724077823318263, 1.953740157426552715 ) ) ;
#42417=CARTESIAN_POINT ( 'NONE',  ( -0.6971942568897637749, 2.189545951927499583E-17, 1.385334645615527549 ) ) ;
#42418=CARTESIAN_POINT ( 'NONE',  ( 1.002407869896990045, 0.1264236179284866091, 1.409940944828126153 ) ) ;
#42419=DIRECTION ( 'NONE',  ( 1.822029033848725028E-16, 0.000000000000000000, 1.000000000000000000 ) ) ;
#42420=CYLINDRICAL_SURFACE ( 'NONE', #4410, 0.1574803149606299191 ) ;
#42421=CARTESIAN_POINT ( 'NONE',  ( 0.8759842519685039353, -0.1787899950787401882, 0.6865157479777322935 ) ) ;
#42422=CARTESIAN_POINT ( 'NONE',  ( -1.054774247047244096, 0.000000000000000000, 0.4945866141194645849 ) ) ;
#42423=CARTESIAN_POINT ( 'NONE',  ( 0.7185039370078739607, 1.928577636452523993E-17, 0.6200787401574803237 ) ) ;
#42424=CARTESIAN_POINT ( 'NONE',  ( 1.033464566929133799, 0.000000000000000000, 1.653543306979086580 ) ) ;
#42426=ORIENTED_EDGE ( 'NONE', *, *, #17045, .T. ) ;
#42428=CARTESIAN_POINT ( 'NONE',  ( -0.7185039370078746268, -0.06523048226347956391, 0.3469488188976379561 ) ) ;
#42429=CARTESIAN_POINT ( 'NONE',  ( 0.8759842519685039353, 0.1787899950787401882, 1.336122047190330786 ) ) ;
#42434=VERTEX_POINT ( 'NONE', #41848 ) ;
#42435=CYLINDRICAL_SURFACE ( 'NONE', #36360, 0.1574803149606299191 ) ;
#42436=CARTESIAN_POINT ( 'NONE',  ( -1.054774247047244540, 0.07405724077823318263, 0.9350393700249758355 ) ) ;
#42438=EDGE_LOOP ( 'NONE', ( #22392, #10687, #12919, #17333 ) ) ;
#42446=CARTESIAN_POINT ( 'NONE',  ( 1.033464566929133799, 0.000000000000000000, 0.5118110235145204578 ) ) ;
#42448=CARTESIAN_POINT ( 'NONE',  ( 0.8019270111902717657, -0.1787899950787401604, 1.702755905458047003 ) ) ;
#42456=CARTESIAN_POINT ( 'NONE',  ( 0.6971942568897626646, -0.07405724077823297447, 0.5167322834108034613 ) ) ;
#42457=CARTESIAN_POINT ( 'NONE',  ( -0.6971942568897648851, -0.07405724077823297447, 0.8366141731745828647 ) ) ;
#42461=CARTESIAN_POINT ( 'NONE',  ( -0.7747212423720944985, -0.1378797577226987259, 1.986191570711806964 ) ) ;
#42464=CARTESIAN_POINT ( 'NONE',  ( 0.9500414927467378812, 0.1787899950787401604, 1.451771653489543290 ) ) ;
#42465=CARTESIAN_POINT ( 'NONE',  ( 0.8019270111902716547, -0.1787899950787401604, 1.978346456639149098 ) ) ;
#42467=CARTESIAN_POINT ( 'NONE',  ( 0.8019270111902716547, 0.1787899950787401604, 0.4281496062454490659 ) ) ;
#42470=CARTESIAN_POINT ( 'NONE',  ( 0.8759842519685039353, 0.000000000000000000, 4.498031496062992574 ) ) ;
#42473=CARTESIAN_POINT ( 'NONE',  ( 0.8019270111902717657, 0.1787899950787401604, 0.4675196849856070869 ) ) ;
#42475=CARTESIAN_POINT ( 'NONE',  ( 1.033464566929134687, -0.06523048226347956391, 0.08612204724409450174 ) ) ;
#42476=( BOUNDED_CURVE ( )  B_SPLINE_CURVE ( 2, ( #11914, #40167, #7367, #39938, #33268, #43776, #25595, #21979, #36602 ),
 .UNSPECIFIED., .F., .F. ) 
 B_SPLINE_CURVE_WITH_KNOTS ( ( 3, 2, 2, 2, 3 ),
 ( 0.7299999999999999822, 0.7325000000000000400, 0.7349999999999999867, 0.7375000000000000444, 0.7399999999999999911 ),
 .UNSPECIFIED. ) 
 CURVE ( )  GEOMETRIC_REPRESENTATION_ITEM ( )  RATIONAL_B_SPLINE_CURVE ( ( 1.000000000000000000, 0.9238795325112939549, 1.000000000000000000, 0.9238795325112869605, 1.000000000000000000, 0.9238795325112869605, 1.000000000000000000, 0.9238795325112869605, 1.000000000000000000 ) ) 
 REPRESENTATION_ITEM ( '' )  ) ;
#42477=CARTESIAN_POINT ( 'NONE',  ( -0.7185039370078739607, 1.928577636452523993E-17, 0.7381889763779527769 ) ) ;
#42478=CARTESIAN_POINT ( 'NONE',  ( -1.054774247047244540, -0.07405724077823318263, 1.437007873961985371 ) ) ;
#42480=CARTESIAN_POINT ( 'NONE',  ( -0.9500414927467378812, 0.1787899950787401604, 1.097440944828127041 ) ) ;
#42481=CARTESIAN_POINT ( 'NONE',  ( 0.6971942568897637749, 2.189545951927499583E-17, 0.9522637794737952577 ) ) ;
#42483=CARTESIAN_POINT ( 'NONE',  ( -1.033464566929134687, 0.06523048226347956391, 0.5142716534357801850 ) ) ;
#42484=CARTESIAN_POINT ( 'NONE',  ( 0.6971942568897648851, 0.07405724077823318263, 1.692913385773008539 ) ) ;
#42486=CARTESIAN_POINT ( 'NONE',  ( 0.6971942568897637749, 2.189545951927499583E-17, 0.1648622046706460786 ) ) ;
#42487=CARTESIAN_POINT ( 'NONE',  ( -0.8019270111902716547, -0.1787899950787401604, 0.08858267711159095725 ) ) ;
#42488=CARTESIAN_POINT ( 'NONE',  ( 1.033464566929134687, 0.06523048226347956391, 1.459153543199560144 ) ) ;
#42490=ORIENTED_EDGE ( 'NONE', *, *, #32872, .T. ) ;
#42491=CARTESIAN_POINT ( 'NONE',  ( 0.8759842519685039353, 0.1574803149606299191, 1.781496062884598164 ) ) ;
#42492=CARTESIAN_POINT ( 'NONE',  ( -1.002407869896990045, 0.1264236179284866091, 1.680610236166708793 ) ) ;
#42493=ORIENTED_EDGE ( 'NONE', *, *, #45099, .F. ) ;
#42495=( BOUNDED_CURVE ( )  B_SPLINE_CURVE ( 2, ( #46209, #28040, #42600, #9811, #38149, #27163, #1241, #3734, #1717 ),
 .UNSPECIFIED., .F., .T. ) 
 B_SPLINE_CURVE_WITH_KNOTS ( ( 3, 2, 2, 2, 3 ),
 ( 0.2200000000000000011, 0.2225000000000000033, 0.2250000000000000056, 0.2275000000000000078, 0.2300000000000000100 ),
 .UNSPECIFIED. ) 
 CURVE ( )  GEOMETRIC_REPRESENTATION_ITEM ( )  RATIONAL_B_SPLINE_CURVE ( ( 1.000000000000000000, 0.9238795325112869605, 1.000000000000000000, 0.9238795325112869605, 1.000000000000000000, 0.9238795325112869605, 1.000000000000000000, 0.9238795325112869605, 1.000000000000000000 ) ) 
 REPRESENTATION_ITEM ( '' )  ) ;
#42498=( BOUNDED_CURVE ( )  B_SPLINE_CURVE ( 2, ( #3295, #21267, #43063, #46904, #6885, #35892, #10756, #13607, #10510 ),
 .UNSPECIFIED., .F., .T. ) 
 B_SPLINE_CURVE_WITH_KNOTS ( ( 3, 2, 2, 2, 3 ),
 ( 0.3499999999999999778, 0.3524999999999999800, 0.3549999999999999822, 0.3574999999999999845, 0.3599999999999999867 ),
 .UNSPECIFIED. ) 
 CURVE ( )  GEOMETRIC_REPRESENTATION_ITEM ( )  RATIONAL_B_SPLINE_CURVE ( ( 1.000000000000000000, 0.9238795325112879597, 1.000000000000000000, 0.9238795325112869605, 1.000000000000000000, 0.9238795325112869605, 1.000000000000000000, 0.9238795325112869605, 1.000000000000000000 ) ) 
 REPRESENTATION_ITEM ( '' )  ) ;
#42505=VECTOR ( 'NONE', #5264, 39.37007874015748143 ) ;
#42508=CARTESIAN_POINT ( 'NONE',  ( -0.8107537697050254399, 0.1574803149606300301, 0.9178149605223947516 ) ) ;
#42509=EDGE_CURVE ( 'NONE', #5319, #36821, #10170, .T. ) ;
#42510=CARTESIAN_POINT ( 'NONE',  ( 0.9412147342319837628, 0.1574803149606300301, 1.828248031496063630 ) ) ;
#42512=ORIENTED_EDGE ( 'NONE', *, *, #11600, .T. ) ;
#42514=CARTESIAN_POINT ( 'NONE',  ( -0.8019270111902716547, 0.1787899950787401604, 0.3937007873478114983 ) ) ;
#42515=CARTESIAN_POINT ( 'NONE',  ( -0.7185039370078746268, 0.06523048226347956391, 0.9719488188976380671 ) ) ;
#42517=CARTESIAN_POINT ( 'NONE',  ( -0.8107537697050254399, 0.1574803149606300301, 0.2189960629921262614 ) ) ;
#42518=CARTESIAN_POINT ( 'NONE',  ( 0.9500414927467378812, 0.1787899950787401604, 1.136811023568283119 ) ) ;
#42519=CARTESIAN_POINT ( 'NONE',  ( 0.8759842519685039353, -0.1787899950787401882, 1.468996062938362046 ) ) ;
#42520=CARTESIAN_POINT ( 'NONE',  ( 0.8019270111902716547, -0.1787899950787401604, 0.1673228345919057503 ) ) ;
#42522=DIRECTION ( 'NONE',  ( 1.822029033848725028E-16, 0.000000000000000000, 1.000000000000000000 ) ) ;
#42523=CARTESIAN_POINT ( 'NONE',  ( 0.7959181182529732057, 0.1389122916488840231, 1.979994088609052127 ) ) ;
#42524=CARTESIAN_POINT ( 'NONE',  ( -1.033464566929133799, 0.000000000000000000, 1.151574803149606474 ) ) ;
#42525=CARTESIAN_POINT ( 'NONE',  ( 1.033464566929134687, -0.06523048226347956391, 0.7849409447743629364 ) ) ;
#42526=CARTESIAN_POINT ( 'NONE',  ( -0.8759842519685039353, 0.000000000000000000, 0.000000000000000000 ) ) ;
#42527=CARTESIAN_POINT ( 'NONE',  ( 0.6971942568897637749, 2.189545951927499583E-17, 1.144192913332062966 ) ) ;
#42528=CARTESIAN_POINT ( 'NONE',  ( 0.9500414927467377701, -0.1787899950787401604, 1.988188976324191781 ) ) ;
#42529=CARTESIAN_POINT ( 'NONE',  ( 0.9412147342319837628, 0.1574803149606300301, 0.4010826770578274081 ) ) ;
#42532=CARTESIAN_POINT ( 'NONE',  ( -0.7185039370078746268, 0.06523048226347956391, 0.1747047243019218821 ) ) ;
#42534=CARTESIAN_POINT ( 'NONE',  ( 0.7495606340400177148, -0.1264236179284866091, 1.227854330654897685 ) ) ;
#42539=CARTESIAN_POINT ( 'NONE',  ( -0.9873396505805591694, 0.1113553986120547346, 1.865157480314960647 ) ) ;
#42541=FACE_OUTER_BOUND ( 'NONE', #13409, .T. ) ;
#42542=DIRECTION ( 'NONE',  ( 0.000000000000000000, 0.000000000000000000, 1.000000000000000000 ) ) ;
#42543=ORIENTED_EDGE ( 'NONE', *, *, #21771, .F. ) ;
#42545=CARTESIAN_POINT ( 'NONE',  ( -0.7495606340400177148, 0.1264236179284866091, 1.375492125930488196 ) ) ;
#42548=CARTESIAN_POINT ( 'NONE',  ( -0.9500414927467378812, -0.1787899950787401604, 0.9251968503399374821 ) ) ;
#42549=CARTESIAN_POINT ( 'NONE',  ( -0.8019270111902717657, -0.1787899950787401604, 1.978346456639149320 ) ) ;
#42551=CARTESIAN_POINT ( 'NONE',  ( -0.8019270111902716547, 0.1787899950787401604, 0.9793307086076531442 ) ) ;
#42552=CARTESIAN_POINT ( 'NONE',  ( -0.8759842519685039353, -0.1787899950787401882, 0.7258858267178898149 ) ) ;
#42555=VERTEX_POINT ( 'NONE', #1255 ) ;
#42558=CARTESIAN_POINT ( 'NONE',  ( -0.8759842519685039353, -0.1787899950787401882, 0.6815944881352126172 ) ) ;
#42562=CARTESIAN_POINT ( 'NONE',  ( -0.9500414927467377701, -0.1787899950787401604, 1.712598425143087466 ) ) ;
#42567=CARTESIAN_POINT ( 'NONE',  ( 0.8759842519685039353, 0.1574803149606299191, 0.5314960629921260393 ) ) ;
#42570=CARTESIAN_POINT ( 'NONE',  ( -0.7185039370078739607, 1.928577636452523993E-17, 1.240157480207432883 ) ) ;
#42572=CARTESIAN_POINT ( 'NONE',  ( -0.8107537697050254399, 0.1574803149606300301, 0.6815944880814486240 ) ) ;
#42573=CARTESIAN_POINT ( 'NONE',  ( 1.033464566929133799, 0.000000000000000000, 1.377952755797984263 ) ) ;
#42576=CARTESIAN_POINT ( 'NONE',  ( 0.9873396505805591694, 0.1113553986120547346, 1.274606299212598604 ) ) ;
#42578=CARTESIAN_POINT ( 'NONE',  ( 0.7185039370078739607, 1.928577636452523993E-17, 1.840551181102362266 ) ) ;
#42583=VERTEX_POINT ( 'NONE', #30310 ) ;
#42585=CARTESIAN_POINT ( 'NONE',  ( 1.054774247047244096, 0.000000000000000000, 0.7701771653005669016 ) ) ;
#42586=ORIENTED_EDGE ( 'NONE', *, *, #38758, .F. ) ;
#42592=CARTESIAN_POINT ( 'NONE',  ( 0.7185039370078746268, -0.06523048226347956391, 1.242618110128693276 ) ) ;
#42593=ADVANCED_FACE ( 'NONE', ( #5091 ), #13480, .T. ) ;
#42595=CARTESIAN_POINT ( 'NONE',  ( -0.7495606340400177148, 0.1264236179284866091, 1.852854330654897685 ) ) ;
#42596=ORIENTED_EDGE ( 'NONE', *, *, #34387, .T. ) ;
#42597=CARTESIAN_POINT ( 'NONE',  ( -0.7185039370078739607, 1.928577636452523993E-17, 0.8070866140657008136 ) ) ;
#42598=ORIENTED_EDGE ( 'NONE', *, *, #20710, .F. ) ;
#42600=CARTESIAN_POINT ( 'NONE',  ( -0.9873396505805591694, 0.1113553986120547346, 0.4773622046168818911 ) ) ;
#42601=CARTESIAN_POINT ( 'NONE',  ( -0.8019270111902717657, 0.1787899950787401604, 1.491141732229701367 ) ) ;
#42602=CARTESIAN_POINT ( 'NONE',  ( 0.7185039370078739607, 1.928577636452523993E-17, 1.446850393700787274 ) ) ;
#42603=CARTESIAN_POINT ( 'NONE',  ( -0.8019270111902717657, 0.1787899950787401604, 0.9793307086076531442 ) ) ;
#42604=CARTESIAN_POINT ( 'NONE',  ( -0.6971942568897626646, 0.07405724077823318263, 0.2805118109698587214 ) ) ;
#42605=( BOUNDED_CURVE ( )  B_SPLINE_CURVE ( 2, ( #41969, #16383, #34836, #30539, #45102, #26937, #20187, #1023, #41255 ),
 .UNSPECIFIED., .F., .F. ) 
 B_SPLINE_CURVE_WITH_KNOTS ( ( 3, 2, 2, 2, 3 ),
 ( 0.8599999999999999867, 0.8625000000000000444, 0.8649999999999999911, 0.8675000000000000488, 0.8699999999999999956 ),
 .UNSPECIFIED. ) 
 CURVE ( )  GEOMETRIC_REPRESENTATION_ITEM ( )  RATIONAL_B_SPLINE_CURVE ( ( 1.000000000000000000, 0.9238795325112869605, 1.000000000000000000, 0.9238795325112869605, 1.000000000000000000, 0.9238795325112869605, 1.000000000000000000, 0.9238795325112829637, 1.000000000000000000 ) ) 
 REPRESENTATION_ITEM ( '' )  ) ;
#42607=CARTESIAN_POINT ( 'NONE',  ( -0.8019270111902717657, -0.1787899950787401604, 1.943897637741510254 ) ) ;
#42611=ADVANCED_FACE ( 'NONE', ( #6264 ), #8936, .T. ) ;
#42613=CYLINDRICAL_SURFACE ( 'NONE', #24912, 0.1574803149606299191 ) ;
#42618=CARTESIAN_POINT ( 'NONE',  ( -0.7495606340400177148, -0.1264236179284866091, 1.193405511757259951 ) ) ;
#42622=ADVANCED_FACE ( 'NONE', ( #39091 ), #1975, .T. ) ;
#42623=CARTESIAN_POINT ( 'NONE',  ( -0.9412147342319837628, 0.1574803149606300301, 1.542814960522393308 ) ) ;
#42626=LINE ( 'NONE', #3342, #43853 ) ;
#42627=CARTESIAN_POINT ( 'NONE',  ( -0.8759842519685039353, 0.1574803149606299191, 0.8366141731208189825 ) ) ;
#42628=CARTESIAN_POINT ( 'NONE',  ( -0.7646288533564489232, -0.1113553986120547346, 0.7824803149606299746 ) ) ;
#42631=CARTESIAN_POINT ( 'NONE',  ( 0.9500414927467378812, 0.1787899950787401604, 0.8562992125446617919 ) ) ;
#42633=CARTESIAN_POINT ( 'NONE',  ( 0.7185039370078746268, 0.06523048226347956391, 0.1747047243019218821 ) ) ;
#42634=CARTESIAN_POINT ( 'NONE',  ( -1.033464566929133799, 0.000000000000000000, 0.7874015746956221085 ) ) ;
#42635=CARTESIAN_POINT ( 'NONE',  ( -0.7185039370078739607, 1.928577636452523993E-17, 1.437007873908220601 ) ) ;
#42639=CARTESIAN_POINT ( 'NONE',  ( 0.8019270111902717657, -0.1787899950787401604, 0.3690944881352128393 ) ) ;
#42640=CARTESIAN_POINT ( 'NONE',  ( -0.8019270111902717657, -0.1787899950787401604, 1.978346456639149320 ) ) ;
#42641=ORIENTED_EDGE ( 'NONE', *, *, #28580, .F. ) ;
#42643=CARTESIAN_POINT ( 'NONE',  ( -0.8019270111902717657, -0.1787899950787401604, 1.510826771599780294 ) ) ;
#42644=CARTESIAN_POINT ( 'NONE',  ( 0.8019270111902717657, -0.1787899950787401604, 1.589566929080094448 ) ) ;
#42646=CARTESIAN_POINT ( 'NONE',  ( -0.9500414927467378812, -0.1787899950787401604, 0.6496062991588353874 ) ) ;
#42649=CARTESIAN_POINT ( 'NONE',  ( 0.7495606340400177148, 0.1264236179284866091, 0.5536417322297008115 ) ) ;
#42650=CARTESIAN_POINT ( 'NONE',  ( -1.002407869896990045, 0.1264236179284866091, 0.5782480314422993040 ) ) ;
#42654=CARTESIAN_POINT ( 'NONE',  ( -0.8019270111902717657, 0.1787899950787401604, 1.377952755851748146 ) ) ;
#42655=CARTESIAN_POINT ( 'NONE',  ( -0.8759842519685039353, 0.000000000000000000, 0.000000000000000000 ) ) ;
#42656=CARTESIAN_POINT ( 'NONE',  ( -0.7646288533564489232, 0.1113553986120547346, 0.3789370078740157410 ) ) ;
#42657=EDGE_CURVE ( 'NONE', #24301, #19795, #22752, .T. ) ;
#42664=CARTESIAN_POINT ( 'NONE',  ( 0.9412147342319837628, 0.1574803149606300301, 0.8046259842519695171 ) ) ;
#42666=ORIENTED_EDGE ( 'NONE', *, *, #34815, .T. ) ;
#42667=CARTESIAN_POINT ( 'NONE',  ( 1.002407869896990045, -0.1264236179284866091, 1.395177165300567124 ) ) ;
#42672=CARTESIAN_POINT ( 'NONE',  ( 0.7185039370078739607, 1.928577636452523993E-17, 0.1771653542231816925 ) ) ;
#42674=CARTESIAN_POINT ( 'NONE',  ( 0.8759842519685039353, -0.1787899950787401882, 1.665846456639149764 ) ) ;
#42678=CYLINDRICAL_SURFACE ( 'NONE', #41733, 0.1574803149606299191 ) ;
#42679=CARTESIAN_POINT ( 'NONE',  ( -0.6971942568897648851, 0.07405724077823318263, 0.7923228345919055560 ) ) ;
#42683=CARTESIAN_POINT ( 'NONE',  ( 0.6971942568897637749, 2.189545951927499583E-17, 1.464074803095842370 ) ) ;
#42686=CARTESIAN_POINT ( 'NONE',  ( 1.002407869896990045, 0.1264236179284866091, 0.3813976377415121966 ) ) ;
#42691=CARTESIAN_POINT ( 'NONE',  ( 1.054774247047244096, 0.000000000000000000, 0.5733267715997795166 ) ) ;
#42693=CARTESIAN_POINT ( 'NONE',  ( 0.7870214370185560915, -0.1374925161510997529, 0.03936976900452263811 ) ) ;
#42696=CARTESIAN_POINT ( 'NONE',  ( -0.9500414927467378812, -0.1787899950787401604, 1.471456692859622217 ) ) ;
#42698=CARTESIAN_POINT ( 'NONE',  ( 0.7185039370078746268, -0.06523048226347956391, 0.4256889763779528879 ) ) ;
#42699=CARTESIAN_POINT ( 'NONE',  ( 0.9500414927467378812, -0.1787899950787401604, 1.043307086560409269 ) ) ;
#42700=CARTESIAN_POINT ( 'NONE',  ( -0.8759842519685039353, -0.1574803149606299191, 0.6594488187901103027 ) ) ;
#42702=CARTESIAN_POINT ( 'NONE',  ( 1.054774247047244540, -0.07405724077823318263, 1.830708661363559253 ) ) ;
#42703=CARTESIAN_POINT ( 'NONE',  ( -0.8107537697050253289, -0.1574803149606297803, 1.454232283464566677 ) ) ;
#42704=CARTESIAN_POINT ( 'NONE',  ( -0.8759842519685039353, -0.1787899950787401882, 0.9178149605761574126 ) ) ;
#42706=CARTESIAN_POINT ( 'NONE',  ( 0.9873396505805591694, -0.1113553986120547346, 1.806102362097196767 ) ) ;
#42707=CARTESIAN_POINT ( 'NONE',  ( -0.7716059914281355736, -0.1284597044140924071, 0.03937007874015843040 ) ) ;
#42708=CARTESIAN_POINT ( 'NONE',  ( 0.6971942568897626646, -0.07405724077823297447, 0.08858267711159095725 ) ) ;
#42709=CARTESIAN_POINT ( 'NONE',  ( -0.6971942568897626646, -0.07405724077823297447, 0.1230314960092287191 ) ) ;
#42711=CARTESIAN_POINT ( 'NONE',  ( 1.033464566929134687, 0.06523048226347956391, 1.537893700679874298 ) ) ;
#42713=AXIS2_PLACEMENT_3D ( 'NONE', #22291, #40955, #22062 ) ;
#42714=EDGE_CURVE ( 'NONE', #3332, #32743, #18415, .T. ) ;
#42717=CARTESIAN_POINT ( 'NONE',  ( -0.8019270111902716547, 0.1787899950787401604, 1.648622047190331230 ) ) ;
#42718=ADVANCED_FACE ( 'NONE', ( #5573 ), #45566, .T. ) ;
#42720=CYLINDRICAL_SURFACE ( 'NONE', #12204, 0.1574803149606299191 ) ;
#42724=CARTESIAN_POINT ( 'NONE',  ( 0.7495606340400177148, -0.1264236179284866091, 1.070374015694267600 ) ) ;
#42729=CARTESIAN_POINT ( 'NONE',  ( 0.8759842519685039353, 0.1574803149606299191, 1.791338582677165281 ) ) ;
#42732=CARTESIAN_POINT ( 'NONE',  ( -0.6971942568897626646, -0.07405724077823297447, 0.2854330708123783977 ) ) ;
#42735=CARTESIAN_POINT ( 'NONE',  ( 0.9500414927467378812, -0.1787899950787401604, 1.082677165300567346 ) ) ;
#42736=CARTESIAN_POINT ( 'NONE',  ( 0.8019270111902716547, -0.1787899950787401604, 1.584645669237574994 ) ) ;
#42737=CARTESIAN_POINT ( 'NONE',  ( 0.8759842519685039353, -0.1787899950787401882, 0.2091535432533232486 ) ) ;
#42738=CARTESIAN_POINT ( 'NONE',  ( 0.8759842519685039353, -0.1574803149606299191, 1.692913385826771533 ) ) ;
#42739=DIRECTION ( 'NONE',  ( 0.000000000000000000, 0.000000000000000000, -1.000000000000000000 ) ) ;
#42740=CARTESIAN_POINT ( 'NONE',  ( -1.033464566929134687, -0.06523048226347956391, 1.109744094488189115 ) ) ;
#42741=CARTESIAN_POINT ( 'NONE',  ( 0.8759842519685039353, 0.1574803149606299191, 0.6791338581601890079 ) ) ;
#42743=CARTESIAN_POINT ( 'NONE',  ( -0.8759842519685039353, -0.1574803149606299191, 1.683070866034204638 ) ) ;
#42744=CARTESIAN_POINT ( 'NONE',  ( 1.054774247047244540, 0.07405724077823318263, 0.2214566928596220785 ) ) ;
#42745=CARTESIAN_POINT ( 'NONE',  ( -0.7185039370078739607, 1.928577636452523993E-17, 1.564960629921259949 ) ) ;
#42746=CARTESIAN_POINT ( 'NONE',  ( 1.002407869896990045, 0.1264236179284866091, 1.090059055064346527 ) ) ;
#42747=CARTESIAN_POINT ( 'NONE',  ( 0.7495606340400177148, 0.1264236179284866091, 1.931594488135212728 ) ) ;
#42748=CARTESIAN_POINT ( 'NONE',  ( 0.9873396505805591694, 0.1113553986120547346, 0.5561023620971968784 ) ) ;
#42751=CARTESIAN_POINT ( 'NONE',  ( -0.9873396505805591694, -0.1113553986120547346, 0.3494094487113705294 ) ) ;
#42753=CARTESIAN_POINT ( 'NONE',  ( 0.7495606340400177148, -0.1264236179284866091, 1.306594488135212728 ) ) ;
#42754=CARTESIAN_POINT ( 'NONE',  ( -0.8759842519685039353, -0.1574803149606299191, 1.771653543307086576 ) ) ;
#42757=( BOUNDED_CURVE ( )  B_SPLINE_CURVE ( 2, ( #6030, #13703, #42910, #20653, #6265, #13945, #6985, #2437, #17772 ),
 .UNSPECIFIED., .F., .T. ) 
 B_SPLINE_CURVE_WITH_KNOTS ( ( 3, 2, 2, 2, 3 ),
 ( 0.4699999999999999734, 0.4724999999999999756, 0.4749999999999999778, 0.4774999999999999800, 0.4799999999999999822 ),
 .UNSPECIFIED. ) 
 CURVE ( )  GEOMETRIC_REPRESENTATION_ITEM ( )  RATIONAL_B_SPLINE_CURVE ( ( 1.000000000000000000, 0.9238795325112879597, 1.000000000000000000, 0.9238795325112869605, 1.000000000000000000, 0.9238795325112869605, 1.000000000000000000, 0.9238795325112869605, 1.000000000000000000 ) ) 
 REPRESENTATION_ITEM ( '' )  ) ;
#42763=( BOUNDED_CURVE ( )  B_SPLINE_CURVE ( 2, ( #38018, #19798, #30620, #45897, #8779, #13112, #41816, #45184, #41106 ),
 .UNSPECIFIED., .F., .F. ) 
 B_SPLINE_CURVE_WITH_KNOTS ( ( 3, 2, 2, 2, 3 ),
 ( 0.9499999999999999556, 0.9525000000000000133, 0.9549999999999999600, 0.9575000000000000178, 0.9599999999999999645 ),
 .UNSPECIFIED. ) 
 CURVE ( )  GEOMETRIC_REPRESENTATION_ITEM ( )  RATIONAL_B_SPLINE_CURVE ( ( 1.000000000000000000, 0.9238795325112899581, 1.000000000000000000, 0.9238795325112869605, 1.000000000000000000, 0.9238795325112869605, 1.000000000000000000, 0.9238795325112869605, 1.000000000000000000 ) ) 
 REPRESENTATION_ITEM ( '' )  ) ;
#42764=VERTEX_POINT ( 'NONE', #42446 ) ;
#42765=CARTESIAN_POINT ( 'NONE',  ( -0.6971942568897648851, 0.07405724077823318263, 1.417322834591906444 ) ) ;
#42768=CARTESIAN_POINT ( 'NONE',  ( -0.8759842519685039353, -0.1787899950787401882, 1.001476377898992132 ) ) ;
#42769=CARTESIAN_POINT ( 'NONE',  ( -1.054774247047244540, 0.07405724077823318263, 1.953740157426552715 ) ) ;
#42771=CARTESIAN_POINT ( 'NONE',  ( -1.054774247047244540, 0.07405724077823318263, 1.126968503883244654 ) ) ;
#42773=CARTESIAN_POINT ( 'NONE',  ( -0.8019270111902717657, -0.1787899950787401604, 0.7234251967966300878 ) ) ;
#42776=ORIENTED_EDGE ( 'NONE', *, *, #27597, .F. ) ;
#42781=CARTESIAN_POINT ( 'NONE',  ( 0.7185039370078746268, 0.06523048226347956391, 0.7750984251968497940 ) ) ;
#42782=CARTESIAN_POINT ( 'NONE',  ( -0.9500414927467378812, 0.1787899950787401604, 0.6200787401037165525 ) ) ;
#42785=CARTESIAN_POINT ( 'NONE',  ( -0.7495606340400177148, 0.1264236179284866091, 1.616633858213952779 ) ) ;
#42788=CARTESIAN_POINT ( 'NONE',  ( -0.7646288533564489232, 0.1113553986120547346, 0.1328740156405045225 ) ) ;
#42789=CARTESIAN_POINT ( 'NONE',  ( 0.8107537697050254399, 0.1574803149606300301, 0.6520669291338587747 ) ) ;
#42790=CARTESIAN_POINT ( 'NONE',  ( 0.7646288533564489232, 0.1113553986120547346, 0.5364173228346457156 ) ) ;
#42792=CARTESIAN_POINT ( 'NONE',  ( -0.9412147342319837628, -0.1574803149606297803, 1.331200787294047672 ) ) ;
#42793=CARTESIAN_POINT ( 'NONE',  ( 0.8759842519685039353, 0.1787899950787401882, 0.6668307086076534773 ) ) ;
#42796=ORIENTED_EDGE ( 'NONE', *, *, #1017, .T. ) ;
#42798=CARTESIAN_POINT ( 'NONE',  ( 1.033464566929133799, 0.000000000000000000, 1.190944881889763884 ) ) ;
#42800=CARTESIAN_POINT ( 'NONE',  ( -1.033464566929134687, -0.06523048226347956391, 1.345964566929133133 ) ) ;
#42802=CARTESIAN_POINT ( 'NONE',  ( 0.7185039370078739607, 1.928577636452523993E-17, 0.4625984251968504046 ) ) ;
#42803=CARTESIAN_POINT ( 'NONE',  ( 0.6971942568897648851, 0.07405724077823318263, 0.7086614172690703928 ) ) ;
#42804=CARTESIAN_POINT ( 'NONE',  ( -1.054774247047244540, -0.07405724077823318263, 1.988188976324187562 ) ) ;
#42805=CARTESIAN_POINT ( 'NONE',  ( -0.8107537697050254399, 0.1574803149606300301, 0.6914370078740148529 ) ) ;
#42809=ORIENTED_EDGE ( 'NONE', *, *, #18969, .F. ) ;
#42812=CARTESIAN_POINT ( 'NONE',  ( 0.7495606340400177148, -0.1264236179284866091, 0.8341535432533228045 ) ) ;
#42813=CARTESIAN_POINT ( 'NONE',  ( 1.033464566929133799, 0.000000000000000000, 1.309055118110236338 ) ) ;
#42814=CARTESIAN_POINT ( 'NONE',  ( 0.8759842519685039353, 0.000000000000000000, 4.498031496062992574 ) ) ;
#42820=ORIENTED_EDGE ( 'NONE', *, *, #38948, .T. ) ;
#42821=CARTESIAN_POINT ( 'NONE',  ( -0.7495606340400177148, -0.1264236179284866091, 1.902066929080094448 ) ) ;
#42822=CARTESIAN_POINT ( 'NONE',  ( 0.8019270111902717657, 0.1787899950787401604, 1.968503936954110189 ) ) ;
#42825=CARTESIAN_POINT ( 'NONE',  ( -0.7495606340400177148, -0.1264236179284866091, 1.902066929080094448 ) ) ;
#42826=CARTESIAN_POINT ( 'NONE',  ( -1.002407869896990045, 0.1264236179284866091, 1.483759842465921075 ) ) ;
#42828=ADVANCED_FACE ( 'NONE', ( #36472 ), #28836, .T. ) ;
#42829=CARTESIAN_POINT ( 'NONE',  ( -0.9500414927467378812, -0.1787899950787401604, 0.9596456692375764375 ) ) ;
#42830=CARTESIAN_POINT ( 'NONE',  ( -1.054774247047244540, 0.07405724077823318263, 0.1870078739619845387 ) ) ;
#42833=CARTESIAN_POINT ( 'NONE',  ( -0.6971942568897637749, 2.189545951927499583E-17, 1.857775590497417362 ) ) ;
#42834=CARTESIAN_POINT ( 'NONE',  ( -0.9500414927467378812, -0.1787899950787401604, 0.1377952755367876370 ) ) ;
#42836=CARTESIAN_POINT ( 'NONE',  ( -0.8759842519685039353, 0.1574803149606299191, 1.948818897637795367 ) ) ;
#42839=CARTESIAN_POINT ( 'NONE',  ( -0.9873396505805591694, -0.1113553986120547346, 1.500984251968503935 ) ) ;
#42842=CARTESIAN_POINT ( 'NONE',  ( -0.8019270111902717657, -0.1787899950787401604, 0.1673228345919057225 ) ) ;
#42843=ORIENTED_EDGE ( 'NONE', *, *, #1082, .F. ) ;
#42844=CARTESIAN_POINT ( 'NONE',  ( -0.8759842519685039353, -0.1787899950787401882, 1.198326771599779628 ) ) ;
#42851=SHAPE_REPRESENTATION_RELATIONSHIP ( 'NONE' , 'NONE' ,  #7769, #27304 ) ;
#42852=CARTESIAN_POINT ( 'NONE',  ( -0.8759842519685039353, 0.1574803149606299191, 0.9547244093412913246 ) ) ;
#42853=CARTESIAN_POINT ( 'NONE',  ( -0.7185039370078746268, -0.06523048226347956391, 0.6619094488188971281 ) ) ;
#42855=CARTESIAN_POINT ( 'NONE',  ( 0.7185039370078746268, 0.06523048226347956391, 1.867618110128693720 ) ) ;
#42856=CARTESIAN_POINT ( 'NONE',  ( 0.7185039370078746268, -0.06523048226347956391, 0.7406496062992133922 ) ) ;
#42859=CARTESIAN_POINT ( 'NONE',  ( 0.9873396505805591694, 0.1113553986120547346, 0.6053149606299212948 ) ) ;
#42860=CARTESIAN_POINT ( 'NONE',  ( 1.033464566929133799, 1.928577636452524610E-17, 4.498031496062992574 ) ) ;
#42861=CARTESIAN_POINT ( 'NONE',  ( 0.9412147342319837628, 0.1574803149606300301, 0.2042322833570398011 ) ) ;
#42863=ORIENTED_EDGE ( 'NONE', *, *, #8070, .F. ) ;
#42865=CARTESIAN_POINT ( 'NONE',  ( 0.7185039370078739607, 1.928577636452523993E-17, 0.7283464565853858819 ) ) ;
#42870=( BOUNDED_CURVE ( )  B_SPLINE_CURVE ( 2, ( #5115, #38432, #23813, #45125, #24690, #39290, #16629, #41758, #30562 ),
 .UNSPECIFIED., .F., .F. ) 
 B_SPLINE_CURVE_WITH_KNOTS ( ( 3, 2, 2, 2, 3 ),
 ( 0.7800000000000000266, 0.7824999999999999734, 0.7850000000000000311, 0.7874999999999999778, 0.7900000000000000355 ),
 .UNSPECIFIED. ) 
 CURVE ( )  GEOMETRIC_REPRESENTATION_ITEM ( )  RATIONAL_B_SPLINE_CURVE ( ( 1.000000000000000000, 0.9238795325112869605, 1.000000000000000000, 0.9238795325112869605, 1.000000000000000000, 0.9238795325112869605, 1.000000000000000000, 0.9238795325112829637, 1.000000000000000000 ) ) 
 REPRESENTATION_ITEM ( '' )  ) ;
#42872=CARTESIAN_POINT ( 'NONE',  ( -1.054774247047244540, 0.07405724077823318263, 1.914370078686394860 ) ) ;
#42874=CARTESIAN_POINT ( 'NONE',  ( -0.7495606340400177148, -0.1264236179284866091, 1.390255905458047447 ) ) ;
#42875=CARTESIAN_POINT ( 'NONE',  ( 1.002407869896990045, 0.1264236179284866091, 1.488681102308440751 ) ) ;
#42877=CARTESIAN_POINT ( 'NONE',  ( 0.8075642843603819676, 0.1651804176431314886, 0.03937007863263043694 ) ) ;
#42878=CARTESIAN_POINT ( 'NONE',  ( -1.054774247047244540, 0.07405724077823318263, 0.5807086613635594752 ) ) ;
#42879=CARTESIAN_POINT ( 'NONE',  ( 0.8759842519685039353, 0.1787899950787401882, 0.1943897637257641919 ) ) ;
#42881=CARTESIAN_POINT ( 'NONE',  ( 0.6971942568897648851, 0.07405724077823318263, 0.7529527558517473684 ) ) ;
#42882=CARTESIAN_POINT ( 'NONE',  ( -0.6971942568897648851, -0.07405724077823297447, 0.5561023621509617598 ) ) ;
#42884=CARTESIAN_POINT ( 'NONE',  ( 0.7185039370078746268, -0.06523048226347956391, 0.6225393700787400508 ) ) ;
#42885=CARTESIAN_POINT ( 'NONE',  ( 0.8759842519685039353, -0.1574803149606299191, 1.141732283464567121 ) ) ;
#42888=CARTESIAN_POINT ( 'NONE',  ( -1.054774247047244540, -0.07405724077823318263, 1.481299212544662680 ) ) ;
#42889=CYLINDRICAL_SURFACE ( 'NONE', #29513, 0.1574803149606299191 ) ;
#42890=CARTESIAN_POINT ( 'NONE',  ( -1.033464566929134687, -0.06523048226347956391, 1.503444881889762774 ) ) ;
#42891=CARTESIAN_POINT ( 'NONE',  ( -0.9412147342319837628, -0.1574803149606297803, 0.4749015748031497064 ) ) ;
#42892=CARTESIAN_POINT ( 'NONE',  ( 1.054774247047244096, 0.000000000000000000, 1.326279527505291433 ) ) ;
#42895=CARTESIAN_POINT ( 'NONE',  ( -1.033464566929133799, 0.000000000000000000, 0.5610236220472440971 ) ) ;
#42896=EDGE_LOOP ( 'NONE', ( #9212, #22689, #43550, #21173 ) ) ;
#42897=( BOUNDED_CURVE ( )  B_SPLINE_CURVE ( 2, ( #25047, #21934, #9968, #46607, #20966, #28917, #25295, #18337, #14031 ),
 .UNSPECIFIED., .F., .F. ) 
 B_SPLINE_CURVE_WITH_KNOTS ( ( 3, 2, 2, 2, 3 ),
 ( 0.5600000000000000533, 0.5625000000000000000, 0.5649999999999999467, 0.5675000000000000044, 0.5699999999999999512 ),
 .UNSPECIFIED. ) 
 CURVE ( )  GEOMETRIC_REPRESENTATION_ITEM ( )  RATIONAL_B_SPLINE_CURVE ( ( 1.000000000000000000, 0.9238795325112869605, 1.000000000000000000, 0.9238795325112869605, 1.000000000000000000, 0.9238795325112869605, 1.000000000000000000, 0.9238795325112829637, 1.000000000000000000 ) ) 
 REPRESENTATION_ITEM ( '' )  ) ;
#42900=ORIENTED_EDGE ( 'NONE', *, *, #16889, .F. ) ;
#42902=CARTESIAN_POINT ( 'NONE',  ( 0.8759842519685039353, 0.1574803149606299191, 0.4921259842519685179 ) ) ;
#42904=VECTOR ( 'NONE', #1576, 39.37007874015748143 ) ;
#42906=FACE_OUTER_BOUND ( 'NONE', #40963, .T. ) ;
#42910=CARTESIAN_POINT ( 'NONE',  ( -0.7646288533564489232, -0.1113553986120547346, 0.9694881888688504645 ) ) ;
#42911=CARTESIAN_POINT ( 'NONE',  ( 0.8019270111902717657, 0.1787899950787401604, 1.687992125930489307 ) ) ;
#42912=CARTESIAN_POINT ( 'NONE',  ( 0.8019270111902717657, 0.1787899950787401604, 0.3100393700249766682 ) ) ;
#42915=DIRECTION ( 'NONE',  ( 0.000000000000000000, 0.000000000000000000, -1.000000000000000000 ) ) ;
#42916=CARTESIAN_POINT ( 'NONE',  ( 0.8759842519685039353, 0.000000000000000000, 4.498031496062992574 ) ) ;
#42917=CARTESIAN_POINT ( 'NONE',  ( 0.9500414927467378812, 0.1787899950787401604, 0.6200787401037165525 ) ) ;
#42918=CARTESIAN_POINT ( 'NONE',  ( -0.7495606340400177148, 0.1264236179284866091, 0.7504921259304880854 ) ) ;
#42922=CARTESIAN_POINT ( 'NONE',  ( -0.8080376074351401927, -0.1583691422869495102, 1.986918182731025384 ) ) ;
#42923=DIRECTION ( 'NONE',  ( -1.000000000000000000, 0.000000000000000000, 0.000000000000000000 ) ) ;
#42924=CARTESIAN_POINT ( 'NONE',  ( 0.8759842519685039353, 0.1787899950787401882, 1.690452755851748146 ) ) ;
#42925=CARTESIAN_POINT ( 'NONE',  ( 0.6971942568897648851, 0.07405724077823318263, 1.968503936954110412 ) ) ;
#42927=CARTESIAN_POINT ( 'NONE',  ( 1.002407869896990045, -0.1264236179284866091, 0.3715551180564728440 ) ) ;
#42934=CARTESIAN_POINT ( 'NONE',  ( 1.002407869896990045, -0.1264236179284866091, 0.5684055117572598403 ) ) ;
#42936=CARTESIAN_POINT ( 'NONE',  ( 1.054774247047244540, 0.07405724077823318263, 0.1082677164816695514 ) ) ;
#42938=CARTESIAN_POINT ( 'NONE',  ( 0.9500414927467377701, 0.1787899950787401604, 0.5413385826234012876 ) ) ;
#42941=CARTESIAN_POINT ( 'NONE',  ( -0.7495606340400177148, 0.1264236179284866091, 1.454232283410803017 ) ) ;
#42942=VERTEX_POINT ( 'NONE', #25459 ) ;
#42944=CARTESIAN_POINT ( 'NONE',  ( 0.8019270111902717657, 0.1787899950787401604, 1.220472440891118504 ) ) ;
#42945=CARTESIAN_POINT ( 'NONE',  ( -0.8107537697050253289, -0.1574803149606297803, 0.7357283463491665065 ) ) ;
#42946=AXIS2_PLACEMENT_3D ( 'NONE', #17281, #31917, #2875 ) ;
#42947=CARTESIAN_POINT ( 'NONE',  ( 0.8107537697050254399, 0.1574803149606300301, 0.1008858267716536417 ) ) ;
#42948=CARTESIAN_POINT ( 'NONE',  ( 1.002407869896990045, 0.1264236179284866091, 1.798720472387181024 ) ) ;
#42949=CARTESIAN_POINT ( 'NONE',  ( -0.7185039370078739607, 1.928577636452523993E-17, 1.328740157480315043 ) ) ;
#42950=CARTESIAN_POINT ( 'NONE',  ( -1.002407869896990045, 0.1264236179284866091, 0.8932086613635591421 ) ) ;
#42952=CARTESIAN_POINT ( 'NONE',  ( -0.7010411943706328364, 0.01421195604105837673, 0.03937007874015843734 ) ) ;
#42953=CARTESIAN_POINT ( 'NONE',  ( 0.7495606340400177148, -0.1264236179284866091, 0.1304133857730082613 ) ) ;
#42954=ADVANCED_FACE ( 'NONE', ( #43393 ), #39564, .T. ) ;
#42955=CARTESIAN_POINT ( 'NONE',  ( 0.8759842519685039353, 0.1574803149606299191, 1.505905511703495847 ) ) ;
#42957=EDGE_CURVE ( 'NONE', #18156, #10815, #33138, .T. ) ;
#42959=CARTESIAN_POINT ( 'NONE',  ( 0.7495606340400177148, 0.1264236179284866091, 0.8292322834108031282 ) ) ;
#42960=CARTESIAN_POINT ( 'NONE',  ( -0.8019270111902716547, 0.1787899950787401604, 1.687992125930489307 ) ) ;
#42961=EDGE_LOOP ( 'NONE', ( #44160, #26404, #11862, #45926 ) ) ;
#42967=VERTEX_POINT ( 'NONE', #17299 ) ;
#42968=CARTESIAN_POINT ( 'NONE',  ( 0.6971942568897648851, 0.07405724077823318263, 1.102362204670646495 ) ) ;
#42970=CARTESIAN_POINT ( 'NONE',  ( 0.7185039370078739607, 1.928577636452523993E-17, 0.8070866140657008136 ) ) ;
#42972=CARTESIAN_POINT ( 'NONE',  ( 0.9873396505805591694, 0.1113553986120547346, 1.943897637795275690 ) ) ;
#42978=CARTESIAN_POINT ( 'NONE',  ( -0.8019270111902716547, 0.1787899950787401604, 0.3543307086076538659 ) ) ;
#42980=CARTESIAN_POINT ( 'NONE',  ( -0.7287072466478243804, 0.07236760742655255763, 1.981831751466828884 ) ) ;
#42981=CARTESIAN_POINT ( 'NONE',  ( -0.9412147342319837628, 0.1574803149606300301, 0.2140748031496061965 ) ) ;
#42982=CARTESIAN_POINT ( 'NONE',  ( 1.054774247047244096, 0.000000000000000000, 1.208169291284818980 ) ) ;
#42983=CARTESIAN_POINT ( 'NONE',  ( 0.6971942568897637749, 2.189545951927499583E-17, 1.459153543253322693 ) ) ;
#42985=CARTESIAN_POINT ( 'NONE',  ( 0.8759842519685039353, -0.1574803149606299191, 1.653543307086614345 ) ) ;
#42987=CARTESIAN_POINT ( 'NONE',  ( -0.7185039370078739607, 1.928577636452523993E-17, 1.092519685039370136 ) ) ;
#42988=CYLINDRICAL_SURFACE ( 'NONE', #33596, 0.1574803149606299191 ) ;
#42989=CARTESIAN_POINT ( 'NONE',  ( -0.9873396505805591694, 0.1113553986120547346, 1.776574803042078488 ) ) ;
#42990=CARTESIAN_POINT ( 'NONE',  ( 1.054774247047244540, -0.07405724077823318263, 0.1771653542769450751 ) ) ;
#42992=CARTESIAN_POINT ( 'NONE',  ( 1.054774247047244096, 0.000000000000000000, 1.085137795221826629 ) ) ;
#42993=CARTESIAN_POINT ( 'NONE',  ( -0.9873396505805591694, 0.1113553986120547346, 1.943897637795275690 ) ) ;
#42994=CARTESIAN_POINT ( 'NONE',  ( 0.8019270111902716547, -0.1787899950787401604, 1.983267716481668108 ) ) ;
#42995=CARTESIAN_POINT ( 'NONE',  ( 0.7646288533564489232, 0.1113553986120547346, 0.5659448817822370081 ) ) ;
#42996=ORIENTED_EDGE ( 'NONE', *, *, #29905, .F. ) ;
#42998=CARTESIAN_POINT ( 'NONE',  ( 0.9697133612655820523, 0.1395208940671603115, 0.03936960452481068351 ) ) ;
#42999=CARTESIAN_POINT ( 'NONE',  ( -0.9873396505805591694, -0.1113553986120547346, 0.4281496061916850726 ) ) ;
#43001=CARTESIAN_POINT ( 'NONE',  ( 0.8759842519685039353, -0.1787899950787401882, 1.508366141678519678 ) ) ;
#43003=CARTESIAN_POINT ( 'NONE',  ( -0.7185039370078739607, 1.928577636452523993E-17, 1.643700787401574992 ) ) ;
#43006=ORIENTED_EDGE ( 'NONE', *, *, #25746, .F. ) ;
#43012=CARTESIAN_POINT ( 'NONE',  ( 0.7495606340400177148, -0.1264236179284866091, 0.4453740156942677664 ) ) ;
#43014=CARTESIAN_POINT ( 'NONE',  ( -0.9500414927467377701, -0.1787899950787401604, 1.432086614119464141 ) ) ;
#43017=CARTESIAN_POINT ( 'NONE',  ( -1.054774247047244540, 0.07405724077823318263, 1.131889763725763665 ) ) ;
#43019=CARTESIAN_POINT ( 'NONE',  ( -1.054774247047244096, 0.000000000000000000, 1.951279527505291433 ) ) ;
#43021=CARTESIAN_POINT ( 'NONE',  ( -0.7495606340400177148, -0.1264236179284866091, 1.109744094434425232 ) ) ;
#43022=CARTESIAN_POINT ( 'NONE',  ( -0.8759842519685039353, -0.1787899950787401882, 0.7652559054580472253 ) ) ;
#43024=CARTESIAN_POINT ( 'NONE',  ( 1.033464566929133799, 0.000000000000000000, 0.8366141732283465249 ) ) ;
#43027=VERTEX_POINT ( 'NONE', #30248 ) ;
#43032=CARTESIAN_POINT ( 'NONE',  ( -0.9873396505805591694, -0.1113553986120547346, 1.737204724409448842 ) ) ;
#43033=CARTESIAN_POINT ( 'NONE',  ( -1.054774247047244096, 0.000000000000000000, 0.6520669290800944484 ) ) ;
#43035=CARTESIAN_POINT ( 'NONE',  ( -0.7495606340400177148, -0.1264236179284866091, 1.626476377898992132 ) ) ;
#43036=EDGE_CURVE ( 'NONE', #5382, #17227, #24852, .T. ) ;
#43038=EDGE_CURVE ( 'NONE', #44478, #25373, #13254, .T. ) ;
#43040=CARTESIAN_POINT ( 'NONE',  ( 0.7646288533564489232, 0.1113553986120547346, 1.038385826664126155 ) ) ;
#43042=CARTESIAN_POINT ( 'NONE',  ( 1.033464566929134687, 0.06523048226347956391, 0.6028543307086614567 ) ) ;
#43045=CARTESIAN_POINT ( 'NONE',  ( 0.8019270111902717657, 0.1787899950787401604, 0.7480314960092282472 ) ) ;
#43049=ORIENTED_EDGE ( 'NONE', *, *, #22188, .T. ) ;
#43051=FACE_OUTER_BOUND ( 'NONE', #482, .T. ) ;
#43052=CARTESIAN_POINT ( 'NONE',  ( 0.9412147342319837628, 0.1574803149606300301, 1.237696850393701586 ) ) ;
#43053=CARTESIAN_POINT ( 'NONE',  ( 0.7550969956560203977, -0.1199135176416183252, 1.985721262792661257 ) ) ;
#43055=CARTESIAN_POINT ( 'NONE',  ( 1.033464566929133799, 0.000000000000000000, 1.860236220472440971 ) ) ;
#43056=CARTESIAN_POINT ( 'NONE',  ( 1.054774247047244540, 0.07405724077823318263, 0.7332677164816705506 ) ) ;
#43062=CARTESIAN_POINT ( 'NONE',  ( 0.9873396505805591694, 0.1113553986120547346, 1.747047244094488194 ) ) ;
#43063=CARTESIAN_POINT ( 'NONE',  ( 0.7646288533564489232, -0.1113553986120547346, 0.7037401574803149318 ) ) ;
#43064=CARTESIAN_POINT ( 'NONE',  ( 1.002407869896990045, 0.1264236179284866091, 0.9325787401037164415 ) ) ;
#43066=CARTESIAN_POINT ( 'NONE',  ( 0.8107537697050254399, -0.1574803149606297803, 0.6963582676090083190 ) ) ;
#43071=CARTESIAN_POINT ( 'NONE',  ( -0.7495606340400177148, -0.1264236179284866091, 0.1254921259304885850 ) ) ;
#43072=EDGE_LOOP ( 'NONE', ( #4282, #29202, #9732, #43497 ) ) ;
#43073=VERTEX_POINT ( 'NONE', #16493 ) ;
#43074=DIRECTION ( 'NONE',  ( 1.000000000000000000, 0.000000000000000000, -1.822029033848725275E-16 ) ) ;
#43077=CARTESIAN_POINT ( 'NONE',  ( -1.002407869896990045, -0.1264236179284866091, 1.990649606245448844 ) ) ;
#43078=CARTESIAN_POINT ( 'NONE',  ( -0.9500414927467378812, 0.1787899950787401604, 1.486220472387181690 ) ) ;
#43079=CARTESIAN_POINT ( 'NONE',  ( 1.002407869896990045, 0.1264236179284866091, 0.8587598424659212970 ) ) ;
#43080=CARTESIAN_POINT ( 'NONE',  ( -0.8759842519685039353, 0.1787899950787401882, 0.8193897637257637756 ) ) ;
#43082=CARTESIAN_POINT ( 'NONE',  ( -0.8019270111902717657, -0.1787899950787401604, 1.072834645615528659 ) ) ;
#43083=CARTESIAN_POINT ( 'NONE',  ( -1.054774247047244540, -0.07405724077823318263, 0.1820866141194649179 ) ) ;
#43085=DIRECTION ( 'NONE',  ( -1.000000000000000000, 0.000000000000000000, 0.000000000000000000 ) ) ;
#43086=CARTESIAN_POINT ( 'NONE',  ( -0.6971942568897648851, 0.07405724077823318263, 1.973425196796630088 ) ) ;
#43087=CARTESIAN_POINT ( 'NONE',  ( -0.7185039370078746268, -0.06523048226347956391, 1.843011811023621327 ) ) ;
#43088=DIRECTION ( 'NONE',  ( 1.000000000000000000, 0.000000000000000000, -1.822029033848725275E-16 ) ) ;
#43092=AXIS2_PLACEMENT_3D ( 'NONE', #36773, #3932, #26241 ) ;
#43093=CARTESIAN_POINT ( 'NONE',  ( -0.7495606340400177148, 0.1264236179284866091, 0.2337598424659216578 ) ) ;
#43094=ORIENTED_EDGE ( 'NONE', *, *, #12298, .T. ) ;
#43095=CARTESIAN_POINT ( 'NONE',  ( -0.7495606340400177148, -0.1264236179284866091, 1.232775590497417362 ) ) ;
#43100=CARTESIAN_POINT ( 'NONE',  ( -0.9873396505805591694, -0.1113553986120547346, 1.373031495955464587 ) ) ;
#43101=CARTESIAN_POINT ( 'NONE',  ( -0.7646288533564489232, -0.1113553986120547346, 0.2312992125984252023 ) ) ;
#43102=CARTESIAN_POINT ( 'NONE',  ( -0.9412147342319837628, 0.1574803149606300301, 0.6865157480314957317 ) ) ;
#43104=CARTESIAN_POINT ( 'NONE',  ( 0.8107537697050253289, 0.1574803149606300301, 1.783956692805858779 ) ) ;
#43107=CARTESIAN_POINT ( 'NONE',  ( -0.9873396505805591694, 0.1113553986120547346, 1.422244094380661572 ) ) ;
#43108=CARTESIAN_POINT ( 'NONE',  ( 0.7185039370078746268, 0.06523048226347956391, 0.7750984251968497940 ) ) ;
#43110=CARTESIAN_POINT ( 'NONE',  ( -0.8107537697050254399, 0.1574803149606300301, 1.242618110236220819 ) ) ;
#43112=CARTESIAN_POINT ( 'NONE',  ( 0.9873396505805591694, 0.1113553986120547346, 1.510826771653543288 ) ) ;
#43113=CARTESIAN_POINT ( 'NONE',  ( 0.8107537697050234415, -0.1574803149606297803, 0.2239173227271187561 ) ) ;
#43114=VECTOR ( 'NONE', #34246, 39.37007874015748143 ) ;
#43117=CARTESIAN_POINT ( 'NONE',  ( -1.033464566929134687, -0.06523048226347956391, 0.6274606298137325178 ) ) ;
#43118=CARTESIAN_POINT ( 'NONE',  ( 0.7185039370078739607, 1.928577636452523993E-17, 1.407480314960629864 ) ) ;
#43122=CARTESIAN_POINT ( 'NONE',  ( 1.033464566929134687, 0.06523048226347956391, 0.9473425195775121432 ) ) ;
#43124=CARTESIAN_POINT ( 'NONE',  ( -1.002407869896990045, 0.1264236179284866091, 0.4207677164816693294 ) ) ;
#43125=ORIENTED_EDGE ( 'NONE', *, *, #30773, .F. ) ;
#43127=CARTESIAN_POINT ( 'NONE',  ( -0.7495606340400177148, 0.1264236179284866091, 1.498523621993480326 ) ) ;
#43128=CARTESIAN_POINT ( 'NONE',  ( 0.6971942568897648851, 0.07405724077823318263, 1.540354330654897685 ) ) ;
#43131=CARTESIAN_POINT ( 'NONE',  ( -0.6971942568897626646, -0.07405724077823297447, 0.6003937007336389575 ) ) ;
#43132=CARTESIAN_POINT ( 'NONE',  ( 0.6971942568897626646, -0.07405724077823297447, 0.2066929133320631329 ) ) ;
#43134=CARTESIAN_POINT ( 'NONE',  ( 1.002407869896990045, 0.1264236179284866091, 0.7406496062454487328 ) ) ;
#43135=CARTESIAN_POINT ( 'NONE',  ( -0.7495606340400177148, 0.1264236179284866091, 0.7062007873478109987 ) ) ;
#43138=CARTESIAN_POINT ( 'NONE',  ( -1.002407869896990045, -0.1264236179284866091, 1.400098425143086800 ) ) ;
#43139=DIRECTION ( 'NONE',  ( 1.822029033848725028E-16, 0.000000000000000000, 1.000000000000000000 ) ) ;
#43140=CARTESIAN_POINT ( 'NONE',  ( -1.033464566929134687, -0.06523048226347956391, 0.4798228346456688831 ) ) ;
#43141=CARTESIAN_POINT ( 'NONE',  ( 1.054774247047244540, -0.07405724077823318263, 1.284448818843874518 ) ) ;
#43143=EDGE_LOOP ( 'NONE', ( #18364, #3259, #8260 ) ) ;
#43144=CARTESIAN_POINT ( 'NONE',  ( -0.7646288533564489232, -0.1113553986120547346, 0.6250000000000000000 ) ) ;
#43148=CARTESIAN_POINT ( 'NONE',  ( 1.054774247047244540, -0.07405724077823318263, 1.397637795221827295 ) ) ;
#43149=EDGE_CURVE ( 'NONE', #42942, #39852, #46407, .T. ) ;
#43150=CARTESIAN_POINT ( 'NONE',  ( -0.8759842519685039353, -0.1574803149606299191, 0.03937007874015843040 ) ) ;
#43156=CARTESIAN_POINT ( 'NONE',  ( 1.002407869896990045, -0.1264236179284866091, 0.2534448818360003908 ) ) ;
#43164=CARTESIAN_POINT ( 'NONE',  ( 1.002407869896990045, 0.1264236179284866091, 0.6176181101824566033 ) ) ;
#43165=( BOUNDED_CURVE ( )  B_SPLINE_CURVE ( 2, ( #46913, #46671, #14103, #43792, #40181, #28504, #10517, #47398, #7382 ),
 .UNSPECIFIED., .F., .F. ) 
 B_SPLINE_CURVE_WITH_KNOTS ( ( 3, 2, 2, 2, 3 ),
 ( 0.6199999999999999956, 0.6225000000000000533, 0.6250000000000000000, 0.6274999999999999467, 0.6300000000000000044 ),
 .UNSPECIFIED. ) 
 CURVE ( )  GEOMETRIC_REPRESENTATION_ITEM ( )  RATIONAL_B_SPLINE_CURVE ( ( 1.000000000000000000, 0.9238795325112869605, 1.000000000000000000, 0.9238795325112869605, 1.000000000000000000, 0.9238795325112869605, 1.000000000000000000, 0.9238795325112869605, 1.000000000000000000 ) ) 
 REPRESENTATION_ITEM ( '' )  ) ;
#43166=CARTESIAN_POINT ( 'NONE',  ( -0.8759842519685039353, -0.1787899950787401882, 0.9227362204186770889 ) ) ;
#43168=CARTESIAN_POINT ( 'NONE',  ( 1.033464566929134687, 0.06523048226347956391, 1.695374015640504828 ) ) ;
#43171=CARTESIAN_POINT ( 'NONE',  ( 1.054774247047244540, 0.07405724077823318263, 1.604330708607653921 ) ) ;
#43172=CARTESIAN_POINT ( 'NONE',  ( 1.054774247047244540, -0.07405724077823318263, 1.988188976324191781 ) ) ;
#43174=CARTESIAN_POINT ( 'NONE',  ( 0.8759842519685039353, -0.1787899950787401882, 0.5241141731745827537 ) ) ;
#43175=VERTEX_POINT ( 'NONE', #30897 ) ;
#43178=CARTESIAN_POINT ( 'NONE',  ( 0.8019270111902717657, 0.1787899950787401604, 0.6643700786863951935 ) ) ;
#43180=CARTESIAN_POINT ( 'NONE',  ( 0.6971942568897637749, 2.189545951927499583E-17, 0.1254921259304885850 ) ) ;
#43182=CARTESIAN_POINT ( 'NONE',  ( -1.002407869896990045, 0.1264236179284866091, 1.523129921206078707 ) ) ;
#43184=CARTESIAN_POINT ( 'NONE',  ( 0.8107537697050234415, -0.1574803149606297803, 0.1550196850393702197 ) ) ;
#43185=CARTESIAN_POINT ( 'NONE',  ( 0.8759842519685039353, 0.1787899950787401882, 1.218011810969858111 ) ) ;
#43187=CARTESIAN_POINT ( 'NONE',  ( 0.9500414927467378812, -0.1787899950787401604, 1.786417322780882388 ) ) ;
#43188=CARTESIAN_POINT ( 'NONE',  ( -0.9873396505805591694, 0.1113553986120547346, 0.5659448818897637734 ) ) ;
#43189=CARTESIAN_POINT ( 'NONE',  ( -0.9500414927467378812, 0.1787899950787401604, 0.9744094487651340231 ) ) ;
#43190=CARTESIAN_POINT ( 'NONE',  ( -0.9412147342319837628, 0.1574803149606300301, 0.5191929132782994172 ) ) ;
#43191=CARTESIAN_POINT ( 'NONE',  ( -0.7081935964228096569, -0.04031566679114802210, 0.03937007874015843040 ) ) ;
#43192=CARTESIAN_POINT ( 'NONE',  ( 0.6971942568897626646, -0.07405724077823297447, 0.2460629920722207653 ) ) ;
#43193=CARTESIAN_POINT ( 'NONE',  ( -0.8019270111902716547, -0.1787899950787401604, 0.2066929133320631329 ) ) ;
#43195=CARTESIAN_POINT ( 'NONE',  ( -0.6971942568897637749, 2.189545951927499583E-17, 0.5930118109698583329 ) ) ;
#43196=CARTESIAN_POINT ( 'NONE',  ( 0.7646288533564489232, 0.1113553986120547346, 1.589566929026330566 ) ) ;
#43198=( BOUNDED_CURVE ( )  B_SPLINE_CURVE ( 2, ( #26077, #40425, #29712, #1124, #14820, #7608, #40890, #8083, #174 ),
 .UNSPECIFIED., .F., .T. ) 
 B_SPLINE_CURVE_WITH_KNOTS ( ( 3, 2, 2, 2, 3 ),
 ( 0.02999999999999999889, 0.03250000000000000111, 0.03500000000000000333, 0.03749999999999999861, 0.04000000000000000083 ),
 .UNSPECIFIED. ) 
 CURVE ( )  GEOMETRIC_REPRESENTATION_ITEM ( )  RATIONAL_B_SPLINE_CURVE ( ( 1.000000000000000000, 0.9238795325112869605, 1.000000000000000000, 0.9238795325112869605, 1.000000000000000000, 0.9238795325112869605, 1.000000000000000000, 0.9238795325112869605, 1.000000000000000000 ) ) 
 REPRESENTATION_ITEM ( '' )  ) ;
#43200=CARTESIAN_POINT ( 'NONE',  ( 1.002407869896990045, 0.1264236179284866091, 0.8193897637257637756 ) ) ;
#43201=CARTESIAN_POINT ( 'NONE',  ( -0.6971942568897648851, -0.07405724077823297447, 1.815944881835999780 ) ) ;
#43205=VERTEX_POINT ( 'NONE', #31124 ) ;
#43212=CARTESIAN_POINT ( 'NONE',  ( 0.8019270111902717657, 0.1787899950787401604, 1.058070866087969186 ) ) ;
#43216=CARTESIAN_POINT ( 'NONE',  ( 0.8759842519685039353, 0.1574803149606299191, 1.909448818897637956 ) ) ;
#43222=B_SPLINE_CURVE_WITH_KNOTS ( 'NONE', 3,
 ( #17606, #16683, #31310, #46364, #13544, #45888, #13100, #28180, #31548, #20497, #46126, #4162, #11379, #25990, #40571, #18785, #3702, #44404, #32729, #43469, #21685, #36316, #47321, #12092, #37720, #26239, #37959, #19732, #18137, #35594, #34900, #42980, #24796, #23861, #6574, #31302, #16900, #31540, #14490, #7518, #6806, #3696, #40102, #22139, #3925, #18319, #7756, #10668, #14975, #29149, #11372, #25983, #32957, #22374, #21426, #17600, #14260, #7296, #32243, #28902, #25276, #21916, #43463, #39864, #21679, #79, #38877, #35310, #28352, #38651, #5826, #2447, #31009, #46062, #31245, #17075, #9896, #6277, #46301, #13492, #42461, #20192, #27434, #34595, #41975, #28123, #1745, #39104, #9431, #27668, #45822, #42922, #9183, #20434, #5335, #9666, #23798, #24509, #31949, #19955, #46535, #10134, #38415, #5586, #35068, #24282, #13032, #32904, #29091, #11088, #35770, #2911, #28607, #17785, #6754, #21376, #14203, #5470, #27319, #16509, #15153, #30671, #38542, #25931, #33378, #45231, #16279, #12455, #1871, #34963, #16737, #45468, #5706, #7939, #41868, #1631 ),
 .UNSPECIFIED., .F., .F.,
 ( 4, 2, 2, 1, 1, 2, 2, 2, 2, 2, 1, 2, 2, 2, 2, 1, 2, 2, 2, 2, 2, 1, 1, 1, 2, 2, 2, 2, 2, 1, 1, 2, 2, 2, 2, 2, 1, 1, 1, 2, 2, 2, 2, 2, 1, 1, 1, 1, 2, 2, 2, 2, 2, 1, 1, 1, 2, 2, 2, 2, 1, 1, 1, 2, 2, 2, 2, 1, 1, 1, 1, 2, 2, 2, 2, 2, 2, 2, 2, 2, 4 ),
 ( 0.000000000000000000, 0.03125000000001836725, 0.04687500000002754741, 0.05468750000003212708, 0.05859375000003467365, 0.06054687500003567979, 0.06250000000003667899, 0.1250000000000644484, 0.1562500000000783540, 0.1718750000000852929, 0.1796875000000887623, 0.1835937500000907330, 0.1875000000000926759, 0.2187500000001105782, 0.2343750000001197653, 0.2421875000001245670, 0.2460937500001267597, 0.2500000000001290079, 0.3125000000001651457, 0.3437500000001831868, 0.3593750000001922351, 0.3671875000001968425, 0.3710937500001991185, 0.3730468750002002842, 0.3740234375002007838, 0.3750000000002012834, 0.4062500000002193801, 0.4218750000002284839, 0.4296875000002330913, 0.4335937500002354228, 0.4355468750002366995, 0.4365234375002373657, 0.4375000000002380318, 0.4687500000002480238, 0.4843750000002531308, 0.4921875000002556844, 0.4960937500002569611, 0.4980468750002575162, 0.4990234375002578493, 0.4995117187502580158, 0.5000000000002581269, 0.5625000000002646772, 0.5937500000002678968, 0.6093750000002693401, 0.6171875000002700062, 0.6210937500002703393, 0.6230468750002706724, 0.6240234375002710054, 0.6245117187502710054, 0.6250000000002711165, 0.6562500000002340350, 0.6718750000002152722, 0.6796875000002060574, 0.6835937500002017275, 0.6855468750001995071, 0.6865234375001983969, 0.6870117187501978417, 0.6875000000001972866, 0.7187500000001568745, 0.7343750000001364464, 0.7421875000001262324, 0.7460937500001215694, 0.7480468750001187939, 0.7490234375001173506, 0.7500000000001159073, 0.7812500000000520695, 0.7968750000000202061, 0.8046875000000038858, 0.8085937499999957812, 0.8105468749999913403, 0.8115234374999894529, 0.8120117187499882316, 0.8124999999999868994, 0.8437499999999894529, 0.8593749999999904521, 0.8671874999999908962, 0.8710937499999911182, 0.8749999999999912292, 0.9062499999999934497, 0.9374999999999955591, 1.000000000000000000 ),
 .UNSPECIFIED. ) ;
#43224=CARTESIAN_POINT ( 'NONE',  ( -0.6971942568897648851, -0.07405724077823297447, 0.4822834645131655606 ) ) ;
#43227=CARTESIAN_POINT ( 'NONE',  ( 1.054774247047244096, 0.000000000000000000, 1.168799212544661348 ) ) ;
#43228=CARTESIAN_POINT ( 'NONE',  ( 0.6971942568897637749, 2.189545951927499583E-17, 1.498523621993480326 ) ) ;
#43229=CARTESIAN_POINT ( 'NONE',  ( -0.9873396505805591694, 0.1113553986120547346, 0.5954724408373543998 ) ) ;
#43230=CARTESIAN_POINT ( 'NONE',  ( 0.8759842519685039353, 0.1574803149606299191, 1.712598425196850238 ) ) ;
#43234=CARTESIAN_POINT ( 'NONE',  ( 0.9412147342319837628, -0.1574803149606297803, 1.449311023514519681 ) ) ;
#43236=CARTESIAN_POINT ( 'NONE',  ( -0.8107537697050253289, 0.1574803149606300301, 1.744586614065703145 ) ) ;
#43238=CARTESIAN_POINT ( 'NONE',  ( 0.6971942568897626646, 0.07405724077823318263, 0.1181102361667090567 ) ) ;
#43239=CARTESIAN_POINT ( 'NONE',  ( 0.7117210317037124812, -0.04900334798748854498, 0.03937011140070836857 ) ) ;
#43240=CARTESIAN_POINT ( 'NONE',  ( 0.8019270111902716547, -0.1787899950787401604, 1.112204724355684959 ) ) ;
#43241=CARTESIAN_POINT ( 'NONE',  ( -0.8107537697050254399, 0.1574803149606300301, 1.823326771546017078 ) ) ;
#43243=CARTESIAN_POINT ( 'NONE',  ( -0.8019270111902717657, 0.1787899950787401604, 1.136811023568283119 ) ) ;
#43244=CARTESIAN_POINT ( 'NONE',  ( 0.8759842519685039353, 0.1574803149606299191, 0.4822834644594015674 ) ) ;
#43247=CARTESIAN_POINT ( 'NONE',  ( 0.9873396505805591694, -0.1113553986120547346, 0.2805118110236220486 ) ) ;
#43249=CARTESIAN_POINT ( 'NONE',  ( -0.9412147342319837628, -0.1574803149606297803, 0.3863188975302684902 ) ) ;
#43250=VERTEX_POINT ( 'NONE', #27540 ) ;
#43251=CARTESIAN_POINT ( 'NONE',  ( 0.7495606340400177148, 0.1264236179284866091, 1.454232283410803017 ) ) ;
#43254=CARTESIAN_POINT ( 'NONE',  ( -0.6971942568897626646, -0.07405724077823297447, 0.04429133852891373180 ) ) ;
#43257=DIRECTION ( 'NONE',  ( 1.000000000000000000, 0.000000000000000000, -1.822029033848725275E-16 ) ) ;
#43259=CARTESIAN_POINT ( 'NONE',  ( 1.033464566929133799, 0.000000000000000000, 1.299212598317669221 ) ) ;
#43261=CARTESIAN_POINT ( 'NONE',  ( 1.054774247047244540, 0.07405724077823318263, 0.6200787401037165525 ) ) ;
#43264=CARTESIAN_POINT ( 'NONE',  ( -1.054774247047244540, -0.07405724077823318263, 1.087598425143086578 ) ) ;
#43267=CARTESIAN_POINT ( 'NONE',  ( -0.7646288533564489232, 0.1113553986120547346, 0.1820866141732283561 ) ) ;
#43269=EDGE_CURVE ( 'NONE', #20097, #25251, #5696, .T. ) ;
#43270=CARTESIAN_POINT ( 'NONE',  ( -1.002407869896990045, -0.1264236179284866091, 1.080216535379306952 ) ) ;
#43271=CARTESIAN_POINT ( 'NONE',  ( -0.7495606340400177148, -0.1264236179284866091, 0.8390748030958424808 ) ) ;
#43272=CARTESIAN_POINT ( 'NONE',  ( -1.054774247047244540, 0.07405724077823318263, 0.2263779527021421711 ) ) ;
#43274=FACE_OUTER_BOUND ( 'NONE', #44660, .T. ) ;
#43276=ORIENTED_EDGE ( 'NONE', *, *, #33416, .T. ) ;
#43280=EDGE_CURVE ( 'NONE', #8074, #26592, #2093, .T. ) ;
#43281=ORIENTED_EDGE ( 'NONE', *, *, #10473, .T. ) ;
#43282=CARTESIAN_POINT ( 'NONE',  ( -1.033464566929134687, -0.06523048226347956391, 1.739665354330709235 ) ) ;
#43283=CARTESIAN_POINT ( 'NONE',  ( 0.8759842519685039353, 0.000000000000000000, 4.498031496062992574 ) ) ;
#43284=CARTESIAN_POINT ( 'NONE',  ( -0.8759842519685039353, -0.1787899950787401882, 0.6422244093950550958 ) ) ;
#43287=CARTESIAN_POINT ( 'NONE',  ( -1.054774247047244540, -0.07405724077823318263, 1.756889763725764553 ) ) ;
#43290=CARTESIAN_POINT ( 'NONE',  ( 0.7646288533564489232, 0.1113553986120547346, 0.6545275590551181688 ) ) ;
#43293=CARTESIAN_POINT ( 'NONE',  ( -0.8759842519685039353, -0.1574803149606299191, 1.368110236112944911 ) ) ;
#43294=CARTESIAN_POINT ( 'NONE',  ( 1.002407869896990045, 0.1264236179284866091, 0.7406496062454487328 ) ) ;
#43297=ORIENTED_EDGE ( 'NONE', *, *, #26538, .F. ) ;
#43299=CARTESIAN_POINT ( 'NONE',  ( 0.9873396505805591694, 0.1113553986120547346, 1.313976377952756014 ) ) ;
#43300=CARTESIAN_POINT ( 'NONE',  ( 0.8296574145072385109, -0.1668241634633925718, 1.987349479867523749 ) ) ;
#43301=CARTESIAN_POINT ( 'NONE',  ( 0.8107537697050254399, -0.1574803149606297803, 1.729822834645670548 ) ) ;
#43302=CARTESIAN_POINT ( 'NONE',  ( 0.8759842519685039353, -0.1787899950787401882, 0.6422244093950550958 ) ) ;
#43307=CARTESIAN_POINT ( 'NONE',  ( 0.8019270111902717657, -0.1787899950787401604, 0.9940944881352130613 ) ) ;
#43314=ORIENTED_EDGE ( 'NONE', *, *, #33957, .F. ) ;
#43315=CARTESIAN_POINT ( 'NONE',  ( -1.002407869896990045, 0.1264236179284866091, 0.1451771653005673179 ) ) ;
#43318=ORIENTED_EDGE ( 'NONE', *, *, #19902, .T. ) ;
#43321=CARTESIAN_POINT ( 'NONE',  ( -0.8759842519685039353, 0.1787899950787401882, 1.488681102308440751 ) ) ;
#43323=CARTESIAN_POINT ( 'NONE',  ( 1.054774247047244096, 0.000000000000000000, 0.8144685038832440993 ) ) ;
#43325=CARTESIAN_POINT ( 'NONE',  ( -1.054774247047244540, 0.07405724077823318263, 0.8120078739619844832 ) ) ;
#43326=CARTESIAN_POINT ( 'NONE',  ( -0.6971942568897626646, 0.07405724077823318263, 0.3986220471903312301 ) ) ;
#43329=CARTESIAN_POINT ( 'NONE',  ( -0.6971942568897648851, -0.07405724077823297447, 1.820866141678520789 ) ) ;
#43330=CARTESIAN_POINT ( 'NONE',  ( -0.7646288533564489232, -0.1113553986120547346, 1.963582677165354395 ) ) ;
#43334=DIRECTION ( 'NONE',  ( -1.000000000000000000, 0.000000000000000000, 0.000000000000000000 ) ) ;
#43338=CARTESIAN_POINT ( 'NONE',  ( -0.7495606340400177148, 0.1264236179284866091, 0.1156496062454492185 ) ) ;
#43339=ORIENTED_EDGE ( 'NONE', *, *, #18645, .T. ) ;
#43340=CARTESIAN_POINT ( 'NONE',  ( -0.9500414927467377701, 0.1787899950787401604, 1.373031496009229357 ) ) ;
#43341=ORIENTED_EDGE ( 'NONE', *, *, #1611, .F. ) ;
#43344=CARTESIAN_POINT ( 'NONE',  ( -0.7646288533564489232, 0.1113553986120547346, 1.550196850286173156 ) ) ;
#43345=CARTESIAN_POINT ( 'NONE',  ( -1.033464566929133799, 0.000000000000000000, 1.387795275590551158 ) ) ;
#43346=CARTESIAN_POINT ( 'NONE',  ( -1.033464566929133799, 0.000000000000000000, 0.9448818896562519720 ) ) ;
#43347=CARTESIAN_POINT ( 'NONE',  ( -0.8107537697050253289, 0.1574803149606300301, 0.7701771653543306728 ) ) ;
#43349=CARTESIAN_POINT ( 'NONE',  ( 0.7185039370078739607, 1.928577636452523993E-17, 1.870078740049952559 ) ) ;
#43352=CARTESIAN_POINT ( 'NONE',  ( 0.9412147342319837628, 0.1574803149606300301, 0.8439960629921254842 ) ) ;
#43354=CARTESIAN_POINT ( 'NONE',  ( -0.9412147342319837628, -0.1574803149606297803, 0.4749015748031497064 ) ) ;
#43355=LINE ( 'NONE', #42860, #39934 ) ;
#43356=CARTESIAN_POINT ( 'NONE',  ( 0.7185039370078746268, -0.06523048226347956391, 0.2583661416247562959 ) ) ;
#43358=ORIENTED_EDGE ( 'NONE', *, *, #21423, .T. ) ;
#43359=FACE_OUTER_BOUND ( 'NONE', #7900, .T. ) ;
#43363=CARTESIAN_POINT ( 'NONE',  ( 0.9412147342319837628, 0.1574803149606300301, 0.9128937006798734100 ) ) ;
#43365=CARTESIAN_POINT ( 'NONE',  ( -0.9500414927467378812, -0.1787899950787401604, 0.4478346456155276045 ) ) ;
#43367=CARTESIAN_POINT ( 'NONE',  ( -1.054774247047244096, 0.000000000000000000, 1.601870078686393750 ) ) ;
#43369=CARTESIAN_POINT ( 'NONE',  ( 0.8759842519685039353, 0.1787899950787401882, 1.611712598371433103 ) ) ;
#43370=ORIENTED_EDGE ( 'NONE', *, *, #14669, .F. ) ;
#43371=CARTESIAN_POINT ( 'NONE',  ( -0.6971942568897626646, 0.07405724077823318263, 0.7529527558517473684 ) ) ;
#43372=CARTESIAN_POINT ( 'NONE',  ( 1.054774247047244540, 0.07405724077823318263, 0.2263779527021421711 ) ) ;
#43374=CARTESIAN_POINT ( 'NONE',  ( 1.054774247047244096, 0.000000000000000000, 0.7750984251430865779 ) ) ;
#43375=CARTESIAN_POINT ( 'NONE',  ( -1.054774247047244540, -0.07405724077823318263, 0.6496062991588353874 ) ) ;
#43379=DIRECTION ( 'NONE',  ( 1.822029033848725028E-16, 0.000000000000000000, 1.000000000000000000 ) ) ;
#43381=CARTESIAN_POINT ( 'NONE',  ( -0.8759842519685039353, 0.1787899950787401882, 1.454232283410803017 ) ) ;
#43382=CARTESIAN_POINT ( 'NONE',  ( -0.8759842519685039353, 0.1574803149606299191, 0.4527559055118110520 ) ) ;
#43383=CARTESIAN_POINT ( 'NONE',  ( 0.7495606340400177148, -0.1264236179284866091, 1.390255905458047447 ) ) ;
#43385=ORIENTED_EDGE ( 'NONE', *, *, #38508, .T. ) ;
#43389=DIRECTION ( 'NONE',  ( 0.000000000000000000, 0.000000000000000000, -1.000000000000000000 ) ) ;
#43390=ORIENTED_EDGE ( 'NONE', *, *, #2894, .T. ) ;
#43393=FACE_OUTER_BOUND ( 'NONE', #24029, .T. ) ;
#43395=CARTESIAN_POINT ( 'NONE',  ( 0.6971942568897626646, 0.07405724077823318263, 0.3149606298674962890 ) ) ;
#43401=CARTESIAN_POINT ( 'NONE',  ( 1.002407869896990045, 0.1264236179284866091, 0.6569881889226141247 ) ) ;
#43402=EDGE_CURVE ( 'NONE', #10631, #16808, #33431, .T. ) ;
#43404=CARTESIAN_POINT ( 'NONE',  ( -0.9500414927467377701, 0.1787899950787401604, 0.9399606298674970661 ) ) ;
#43408=CARTESIAN_POINT ( 'NONE',  ( 0.6971942568897648851, 0.07405724077823318263, 1.658464566875369472 ) ) ;
#43409=CARTESIAN_POINT ( 'NONE',  ( 0.7185039370078739607, 0.000000000000000000, 4.498031496062992574 ) ) ;
#43410=CARTESIAN_POINT ( 'NONE',  ( -0.7185039370078739607, 0.000000000000000000, -2.869337061179095023E-17 ) ) ;
#43412=CARTESIAN_POINT ( 'NONE',  ( 0.8759842519685039353, 0.1574803149606299191, 0.01968503937007873988 ) ) ;
#43414=CARTESIAN_POINT ( 'NONE',  ( 0.7185039370078766252, -0.06523048226348168721, 1.321358267609009207 ) ) ;
#43416=CARTESIAN_POINT ( 'NONE',  ( -1.002407869896990045, 0.1264236179284866091, 0.4256889763241890057 ) ) ;
#43417=CARTESIAN_POINT ( 'NONE',  ( 0.7495606340400177148, -0.1264236179284866091, 0.6766732282926929409 ) ) ;
#43419=CARTESIAN_POINT ( 'NONE',  ( 1.054774247047244540, -0.07405724077823318263, 0.1427165353793072855 ) ) ;
#43421=CARTESIAN_POINT ( 'NONE',  ( -0.8759842519685039353, 0.1787899950787401882, 1.646161417269070837 ) ) ;
#43423=CARTESIAN_POINT ( 'NONE',  ( 0.7646288533564489232, -0.1113553986120547346, 0.4281496062992125595 ) ) ;
#43424=CARTESIAN_POINT ( 'NONE',  ( 0.7495606340400177148, 0.1264236179284866091, 1.222933070812378009 ) ) ;
#43425=CARTESIAN_POINT ( 'NONE',  ( -0.8759842519685039353, -0.1574803149606299191, 0.6988188975302678241 ) ) ;
#43426=CARTESIAN_POINT ( 'NONE',  ( -1.033464566929133799, 0.000000000000000000, 1.496062992018456494 ) ) ;
#43427=CARTESIAN_POINT ( 'NONE',  ( 1.054774247047244540, 0.07405724077823318263, 1.796259842465923073 ) ) ;
#43428=CARTESIAN_POINT ( 'NONE',  ( -0.8759842519685039353, 0.1574803149606299191, 0.5708661417322835607 ) ) ;
#43429=CARTESIAN_POINT ( 'NONE',  ( -1.054774247047244096, 0.000000000000000000, 0.8489173227808819444 ) ) ;
#43432=CARTESIAN_POINT ( 'NONE',  ( 1.054774247047244540, -0.07405724077823318263, 0.2608267715997797387 ) ) ;
#43433=CARTESIAN_POINT ( 'NONE',  ( -0.6971942568897626646, -0.07405724077823297447, 0.2805118109698587214 ) ) ;
#43434=CARTESIAN_POINT ( 'NONE',  ( -0.8759842519685039353, 0.1787899950787401882, 0.7012795275052913224 ) ) ;
#43435=CARTESIAN_POINT ( 'NONE',  ( 0.7185039370078746268, -0.06523048226347956391, 1.636318897530269156 ) ) ;
#43437=EDGE_CURVE ( 'NONE', #43073, #33230, #3446, .T. ) ;
#43441=ORIENTED_EDGE ( 'NONE', *, *, #23762, .F. ) ;
#43442=CARTESIAN_POINT ( 'NONE',  ( 0.8759842519685039353, -0.1787899950787401882, 0.7652559054580472253 ) ) ;
#43443=CARTESIAN_POINT ( 'NONE',  ( 1.002407869896990045, -0.1264236179284866091, 1.045767716481669440 ) ) ;
#43444=CARTESIAN_POINT ( 'NONE',  ( -0.9500414927467377701, 0.1787899950787401604, 1.879921259788756016 ) ) ;
#43445=EDGE_CURVE ( 'NONE', #14468, #44045, #37743, .T. ) ;
#43446=CARTESIAN_POINT ( 'NONE',  ( 0.6971942568897637749, 2.189545951927499583E-17, 1.970964566875370139 ) ) ;
#43448=CARTESIAN_POINT ( 'NONE',  ( 1.033464566929133799, 0.000000000000000000, 1.614173228238929170 ) ) ;
#43450=VERTEX_POINT ( 'NONE', #36115 ) ;
#43454=CARTESIAN_POINT ( 'NONE',  ( 0.7185039370078739607, 1.928577636452523993E-17, 1.397637795168062969 ) ) ;
#43455=( BOUNDED_CURVE ( )  B_SPLINE_CURVE ( 2, ( #45890, #35605, #16912, #9728, #27959, #9961, #1815, #38483, #28186 ),
 .UNSPECIFIED., .F., .T. ) 
 B_SPLINE_CURVE_WITH_KNOTS ( ( 3, 2, 2, 2, 3 ),
 ( 0.3300000000000000155, 0.3325000000000000178, 0.3350000000000000200, 0.3375000000000000222, 0.3400000000000000244 ),
 .UNSPECIFIED. ) 
 CURVE ( )  GEOMETRIC_REPRESENTATION_ITEM ( )  RATIONAL_B_SPLINE_CURVE ( ( 1.000000000000000000, 0.9238795325112869605, 1.000000000000000000, 0.9238795325112869605, 1.000000000000000000, 0.9238795325112869605, 1.000000000000000000, 0.9238795325112869605, 1.000000000000000000 ) ) 
 REPRESENTATION_ITEM ( '' )  ) ;
#43456=CARTESIAN_POINT ( 'NONE',  ( 0.6971942568897637749, 2.189545951927499583E-17, 0.08120078734781142893 ) ) ;
#43459=CARTESIAN_POINT ( 'NONE',  ( -1.054774247047244540, 0.07405724077823318263, 0.4232283464029293896 ) ) ;
#43463=CARTESIAN_POINT ( 'NONE',  ( -0.7219032811190957410, -0.06759513565020623671, 1.984564416229634309 ) ) ;
#43465=CARTESIAN_POINT ( 'NONE',  ( 0.8019270111902717657, 0.1787899950787401604, 1.181102362150960428 ) ) ;
#43466=CARTESIAN_POINT ( 'NONE',  ( 1.002407869896990045, 0.1264236179284866091, 1.483759842465921075 ) ) ;
#43467=CARTESIAN_POINT ( 'NONE',  ( -0.7185039370078739607, 1.928577636452523993E-17, 0.6496062991050708391 ) ) ;
#43469=CARTESIAN_POINT ( 'NONE',  ( -0.7653144731331090744, 0.1177361346232950190, 1.980714588250390706 ) ) ;
#43471=CARTESIAN_POINT ( 'NONE',  ( -0.7185039370078746268, -0.06523048226347956391, 1.675688976270425679 ) ) ;
#43473=CARTESIAN_POINT ( 'NONE',  ( 0.8759842519685039353, -0.1787899950787401882, 0.09104330703285078152 ) ) ;
#43474=( BOUNDED_CURVE ( )  B_SPLINE_CURVE ( 2, ( #45851, #20218, #13058, #6546, #24076, #17100, #42706, #28383, #38685 ),
 .UNSPECIFIED., .F., .F. ) 
 B_SPLINE_CURVE_WITH_KNOTS ( ( 3, 2, 2, 2, 3 ),
 ( 0.8900000000000000133, 0.8924999999999999600, 0.8950000000000000178, 0.8974999999999999645, 0.9000000000000000222 ),
 .UNSPECIFIED. ) 
 CURVE ( )  GEOMETRIC_REPRESENTATION_ITEM ( )  RATIONAL_B_SPLINE_CURVE ( ( 1.000000000000000000, 0.9238795325112899581, 1.000000000000000000, 0.9238795325112869605, 1.000000000000000000, 0.9238795325112869605, 1.000000000000000000, 0.9238795325112869605, 1.000000000000000000 ) ) 
 REPRESENTATION_ITEM ( '' )  ) ;
#43475=CARTESIAN_POINT ( 'NONE',  ( 0.6971942568897648851, 0.07405724077823318263, 1.102362204670646495 ) ) ;
#43477=CARTESIAN_POINT ( 'NONE',  ( -0.7495606340400177148, -0.1264236179284866091, 1.227854330654897685 ) ) ;
#43478=CARTESIAN_POINT ( 'NONE',  ( 0.9412147342319837628, 0.1574803149606300301, 0.4798228345381422844 ) ) ;
#43481=CARTESIAN_POINT ( 'NONE',  ( -1.033464566929133799, 1.928577636452533546E-17, 4.498031496062992574 ) ) ;
#43482=CARTESIAN_POINT ( 'NONE',  ( 0.9716762863782174575, 0.1379795071755416380, 0.03936908659436527680 ) ) ;
#43483=CARTESIAN_POINT ( 'NONE',  ( 0.8759842519685039353, 0.1574803149606299191, 0.2559055118110236116 ) ) ;
#43484=CARTESIAN_POINT ( 'NONE',  ( -0.9873396505805591694, 0.1113553986120547346, 0.4773622046168818911 ) ) ;
#43486=CARTESIAN_POINT ( 'NONE',  ( 0.7495606340400177148, -0.1264236179284866091, 1.385334645615527549 ) ) ;
#43487=CARTESIAN_POINT ( 'NONE',  ( -1.033464566929134687, -0.06523048226347956391, 1.149114173228346969 ) ) ;
#43491=ORIENTED_EDGE ( 'NONE', *, *, #39049, .T. ) ;
#43492=CARTESIAN_POINT ( 'NONE',  ( 0.7185039370078739607, 1.928577636452523993E-17, 0.4527559054042842868 ) ) ;
#43497=ORIENTED_EDGE ( 'NONE', *, *, #23617, .T. ) ;
#43500=CARTESIAN_POINT ( 'NONE',  ( -1.054774247047244540, 0.07405724077823318263, 1.092519684985605810 ) ) ;
#43501=CARTESIAN_POINT ( 'NONE',  ( -0.9873396505805591694, 0.1113553986120547346, 0.2116141732283464416 ) ) ;
#43502=CARTESIAN_POINT ( 'NONE',  ( -0.7495606340400177148, 0.1264236179284866091, 1.099901574749385880 ) ) ;
#43503=CARTESIAN_POINT ( 'NONE',  ( -0.8759842519685039353, -0.1787899950787401882, 0.8046259841982047467 ) ) ;
#43505=AXIS2_PLACEMENT_3D ( 'NONE', #34665, #34908, #31082 ) ;
#43506=CARTESIAN_POINT ( 'NONE',  ( -0.8019270111902717657, 0.1787899950787401604, 0.2362204723871814960 ) ) ;
#43511=CARTESIAN_POINT ( 'NONE',  ( -0.7646288533564489232, -0.1113553986120547346, 0.8513779526483780113 ) ) ;
#43513=EDGE_LOOP ( 'NONE', ( #26204, #2730, #43491, #8931 ) ) ;
#43517=CARTESIAN_POINT ( 'NONE',  ( -0.8019270111902717657, -0.1787899950787401604, 0.7972440944344250102 ) ) ;
#43519=CARTESIAN_POINT ( 'NONE',  ( -0.8107537697050254399, -0.1574803149606297803, 1.129429133750740277 ) ) ;
#43520=CARTESIAN_POINT ( 'NONE',  ( -1.002407869896990045, 0.1264236179284866091, 0.1107283464029293202 ) ) ;
#43523=CARTESIAN_POINT ( 'NONE',  ( -0.7185039370078746268, -0.06523048226347956391, 1.439468503829481216 ) ) ;
#43524=CARTESIAN_POINT ( 'NONE',  ( 0.6971942568897637749, 2.189545951927499583E-17, 0.7554133857730077617 ) ) ;
#43529=CARTESIAN_POINT ( 'NONE',  ( 0.8107537697050253289, 0.1574803149606300301, 1.242618110236220819 ) ) ;
#43530=CARTESIAN_POINT ( 'NONE',  ( 0.8777546437831791337, -0.1746983550445412314, 1.988227210017399882 ) ) ;
#43533=CARTESIAN_POINT ( 'NONE',  ( 0.7495606340400177148, -0.1264236179284866091, 0.7160433070328504623 ) ) ;
#43535=VECTOR ( 'NONE', #13500, 39.37007874015748143 ) ;
#43541=CARTESIAN_POINT ( 'NONE',  ( 1.033464566929133799, 0.000000000000000000, 0.6299212597349921339 ) ) ;
#43543=CARTESIAN_POINT ( 'NONE',  ( 0.9500414927467378812, 0.1787899950787401604, 0.9350393700249758355 ) ) ;
#43549=CARTESIAN_POINT ( 'NONE',  ( -1.054774247047244540, 0.07405724077823318263, 0.1033464566391498751 ) ) ;
#43550=ORIENTED_EDGE ( 'NONE', *, *, #31519, .T. ) ;
#43551=VECTOR ( 'NONE', #17001, 39.37007874015748143 ) ;
#43552=CARTESIAN_POINT ( 'NONE',  ( 0.9500414927467378812, 0.1787899950787401604, 1.963582677111591401 ) ) ;
#43553=ORIENTED_EDGE ( 'NONE', *, *, #10849, .F. ) ;
#43555=CARTESIAN_POINT ( 'NONE',  ( -0.8759842519685039353, 0.1787899950787401882, 1.966043307032850462 ) ) ;
#43556=CARTESIAN_POINT ( 'NONE',  ( -0.7495606340400177148, 0.1264236179284866091, 1.690452755851748146 ) ) ;
#43558=CARTESIAN_POINT ( 'NONE',  ( -0.9500414927467378812, 0.1787899950787401604, 0.3887795275052913224 ) ) ;
#43560=CARTESIAN_POINT ( 'NONE',  ( -1.054774247047244540, -0.07405724077823318263, 1.993110236166711013 ) ) ;
#43561=FACE_OUTER_BOUND ( 'NONE', #41338, .T. ) ;
#43562=CARTESIAN_POINT ( 'NONE',  ( -0.8107537697050253289, -0.1574803149606297803, 1.847933070866143002 ) ) ;
#43567=CARTESIAN_POINT ( 'NONE',  ( -1.054774247047244096, 0.000000000000000000, 0.1796259841982051075 ) ) ;
#43568=VECTOR ( 'NONE', #22798, 39.37007874015748143 ) ;
#43570=CARTESIAN_POINT ( 'NONE',  ( -1.002407869896990045, -0.1264236179284866091, 1.400098425143086800 ) ) ;
#43571=ORIENTED_EDGE ( 'NONE', *, *, #37940, .T. ) ;
#43579=CARTESIAN_POINT ( 'NONE',  ( -0.8107537697050253289, 0.1574803149606300301, 0.8784448817822366751 ) ) ;
#43582=CARTESIAN_POINT ( 'NONE',  ( 0.8107537697050253289, 0.1574803149606300301, 1.744586614065703145 ) ) ;
#43583=VERTEX_POINT ( 'NONE', #8457 ) ;
#43584=EDGE_CURVE ( 'NONE', #14779, #34930, #2723, .T. ) ;
#43586=CARTESIAN_POINT ( 'NONE',  ( 0.8107537697050253289, 0.1574803149606300301, 0.7701771653543306728 ) ) ;
#43588=CARTESIAN_POINT ( 'NONE',  ( -0.8759842519685039353, -0.1574803149606299191, 1.604330708553889595 ) ) ;
#43593=CARTESIAN_POINT ( 'NONE',  ( 1.033464566929133799, 0.000000000000000000, 0.1181102361129454797 ) ) ;
#43595=EDGE_CURVE ( 'NONE', #46242, #26440, #42605, .T. ) ;
#43596=DIRECTION ( 'NONE',  ( 0.000000000000000000, 0.000000000000000000, -1.000000000000000000 ) ) ;
#43601=CARTESIAN_POINT ( 'NONE',  ( 0.8107537697050253289, -0.1574803149606297803, 0.8932086613097963701 ) ) ;
#43604=CARTESIAN_POINT ( 'NONE',  ( -0.8759842519685039353, 0.1787899950787401882, 0.4256889763241890057 ) ) ;
#43607=CARTESIAN_POINT ( 'NONE',  ( -0.6971942568897648851, -0.07405724077823297447, 1.584645669237574994 ) ) ;
#43608=CARTESIAN_POINT ( 'NONE',  ( 0.8019270111902717657, 0.1787899950787401604, 1.496062992072220821 ) ) ;
#43610=CARTESIAN_POINT ( 'NONE',  ( -1.002407869896990045, -0.1264236179284866091, 0.8489173227808819444 ) ) ;
#43612=CARTESIAN_POINT ( 'NONE',  ( 0.6971942568897648851, -0.07405724077823297447, 0.7185039369541108556 ) ) ;
#43613=CARTESIAN_POINT ( 'NONE',  ( -0.7495606340400177148, -0.1264236179284866091, 0.7554133857730077617 ) ) ;
#43618=CARTESIAN_POINT ( 'NONE',  ( -0.8759842519685039353, 0.1574803149606299191, 1.899606299105070839 ) ) ;
#43619=ORIENTED_EDGE ( 'NONE', *, *, #44664, .F. ) ;
#43621=CARTESIAN_POINT ( 'NONE',  ( -0.7185039370078746268, 0.06523048226347956391, 1.483759842519686067 ) ) ;
#43622=CARTESIAN_POINT ( 'NONE',  ( -0.7646288533564489232, 0.1113553986120547346, 0.4183070866141732624 ) ) ;
#43623=CARTESIAN_POINT ( 'NONE',  ( 1.054774247047244096, 0.000000000000000000, 1.483759842465921075 ) ) ;
#43625=CARTESIAN_POINT ( 'NONE',  ( -0.8759842519685039353, 0.000000000000000000, 0.000000000000000000 ) ) ;
#43626=ORIENTED_EDGE ( 'NONE', *, *, #38750, .T. ) ;
#43628=EDGE_LOOP ( 'NONE', ( #23595, #11686, #3831, #39617 ) ) ;
#43630=VERTEX_POINT ( 'NONE', #8697 ) ;
#43631=CARTESIAN_POINT ( 'NONE',  ( -0.8759842519685039353, 0.000000000000000000, 0.000000000000000000 ) ) ;
#43635=CARTESIAN_POINT ( 'NONE',  ( 0.7185039370078746268, 0.06523048226347956391, 1.050688976377951889 ) ) ;
#43636=CARTESIAN_POINT ( 'NONE',  ( 0.8759842519685039353, -0.1787899950787401882, 1.744586614119464807 ) ) ;
#43637=CARTESIAN_POINT ( 'NONE',  ( 0.8759842519685039353, 0.1787899950787401882, 0.3469488188438744070 ) ) ;
#43645=CARTESIAN_POINT ( 'NONE',  ( 0.8019270111902717657, -0.1787899950787401604, 0.6003937007336380693 ) ) ;
#43647=ADVANCED_FACE ( 'NONE', ( #33904 ), #16148, .T. ) ;
#43648=DIRECTION ( 'NONE',  ( 1.000000000000000000, 0.000000000000000000, -1.822029033848725275E-16 ) ) ;
#43651=CARTESIAN_POINT ( 'NONE',  ( 0.7495606340400177148, -0.1264236179284866091, 1.705216535379307174 ) ) ;
#43652=LINE ( 'NONE', #43409, #38317 ) ;
#43654=ADVANCED_FACE ( 'NONE', ( #15680 ), #23086, .T. ) ;
#43658=CARTESIAN_POINT ( 'NONE',  ( 0.7185039370078737386, 0.06523048226348011902, 0.4896653542231809153 ) ) ;
#43660=CARTESIAN_POINT ( 'NONE',  ( 1.002407869896990045, -0.1264236179284866091, 0.06151574797773248782 ) ) ;
#43662=CARTESIAN_POINT ( 'NONE',  ( -0.6971942568897648851, 0.07405724077823318263, 1.614173228292692386 ) ) ;
#43663=EDGE_LOOP ( 'NONE', ( #29760, #249, #15580, #13200 ) ) ;
#43664=CARTESIAN_POINT ( 'NONE',  ( -1.054774247047244540, 0.07405724077823318263, 1.131889763725763665 ) ) ;
#43666=CARTESIAN_POINT ( 'NONE',  ( 1.054774247047244540, 0.07405724077823318263, 1.835629921206078485 ) ) ;
#43667=CARTESIAN_POINT ( 'NONE',  ( -1.033464566929133799, 0.000000000000000000, 0.6003937007874016185 ) ) ;
#43668=CARTESIAN_POINT ( 'NONE',  ( -0.7495606340400177148, -0.1264236179284866091, 1.031003936954110189 ) ) ;
#43671=CARTESIAN_POINT ( 'NONE',  ( 1.054774247047244540, -0.07405724077823318263, 0.3789370078202520253 ) ) ;
#43672=CARTESIAN_POINT ( 'NONE',  ( -0.6971942568897626646, -0.07405724077823297447, 0.1624015747493861017 ) ) ;
#43674=CARTESIAN_POINT ( 'NONE',  ( -1.002407869896990045, 0.1264236179284866091, 0.6963582676627716461 ) ) ;
#43675=CARTESIAN_POINT ( 'NONE',  ( 0.9873396505805591694, 0.1113553986120547346, 1.579724409341291214 ) ) ;
#43679=ORIENTED_EDGE ( 'NONE', *, *, #35575, .F. ) ;
#43680=CARTESIAN_POINT ( 'NONE',  ( 0.8019270111902717657, 0.1787899950787401604, 0.8661417322297003674 ) ) ;
#43681=CARTESIAN_POINT ( 'NONE',  ( 0.7495606340400177148, -0.1264236179284866091, 1.114665354276944909 ) ) ;
#43682=CARTESIAN_POINT ( 'NONE',  ( -1.054774247047244540, 0.07405724077823318263, 1.914370078686394860 ) ) ;
#43684=CARTESIAN_POINT ( 'NONE',  ( 0.7495606340400177148, 0.1264236179284866091, 1.887303149552535420 ) ) ;
#43691=CARTESIAN_POINT ( 'NONE',  ( -0.8107537697050254399, 0.1574803149606300301, 1.705216535325545069 ) ) ;
#43693=CARTESIAN_POINT ( 'NONE',  ( 1.054774247047244540, 0.07405724077823318263, 1.166338582623402509 ) ) ;
#43695=CARTESIAN_POINT ( 'NONE',  ( 0.7495606340400177148, 0.1264236179284866091, 1.493602362150960650 ) ) ;
#43696=CARTESIAN_POINT ( 'NONE',  ( 1.054774247047244540, -0.07405724077823318263, 0.05905511805647267048 ) ) ;
#43702=CARTESIAN_POINT ( 'NONE',  ( -0.9500414927467377701, 0.1787899950787401604, 0.5462598424659214080 ) ) ;
#43703=CARTESIAN_POINT ( 'NONE',  ( -0.9412147342319837628, 0.1574803149606300301, 0.6766732282389295028 ) ) ;
#43707=CARTESIAN_POINT ( 'NONE',  ( 0.9500414927467378812, 0.1787899950787401604, 1.254921259788757348 ) ) ;
#43708=CARTESIAN_POINT ( 'NONE',  ( 0.6971942568897637749, 2.189545951927499583E-17, 1.656003936954110412 ) ) ;
#43711=CARTESIAN_POINT ( 'NONE',  ( -0.7185039370078746268, 0.06523048226347956391, 1.916830708661418026 ) ) ;
#43715=CARTESIAN_POINT ( 'NONE',  ( -1.033464566929133799, 0.000000000000000000, 1.771653543199558811 ) ) ;
#43716=CARTESIAN_POINT ( 'NONE',  ( 0.8759842519685039353, 0.1787899950787401882, 0.1107283464029295283 ) ) ;
#43717=CARTESIAN_POINT ( 'NONE',  ( 0.7092216557579411607, -0.04177231851234675108, 0.03937054267072845337 ) ) ;
#43718=CARTESIAN_POINT ( 'NONE',  ( -0.7646288533564489232, 0.1113553986120547346, 1.953740157480315043 ) ) ;
#43719=CARTESIAN_POINT ( 'NONE',  ( -0.7495606340400177148, 0.1264236179284866091, 1.178641732229700922 ) ) ;
#43720=CARTESIAN_POINT ( 'NONE',  ( 0.9412147342319837628, 0.1574803149606300301, 0.5585629920184573827 ) ) ;
#43723=CARTESIAN_POINT ( 'NONE',  ( 0.8687400033924506104, 0.1748083731305843380, 0.03936971248799488177 ) ) ;
#43724=CARTESIAN_POINT ( 'NONE',  ( 0.8759842519685039353, 0.1574803149606299191, 0.8366141731208189825 ) ) ;
#43726=CARTESIAN_POINT ( 'NONE',  ( -0.9412147342319837628, 0.1574803149606300301, 0.4404527557979849850 ) ) ;
#43728=CARTESIAN_POINT ( 'NONE',  ( 1.054774247047244540, -0.07405724077823318263, 1.397637795221827295 ) ) ;
#43729=CARTESIAN_POINT ( 'NONE',  ( -0.8759842519685039353, -0.1574803149606299191, 1.092519684931842594 ) ) ;
#43730=CARTESIAN_POINT ( 'NONE',  ( -0.9412147342319837628, 0.1574803149606300301, 0.09596456692913379882 ) ) ;
#43731=CARTESIAN_POINT ( 'NONE',  ( -0.7185039370078766252, -0.06523048226348168721, 1.370570866141733068 ) ) ;
#43735=ORIENTED_EDGE ( 'NONE', *, *, #966, .T. ) ;
#43736=CARTESIAN_POINT ( 'NONE',  ( -0.8759842519685039353, 0.1574803149606299191, 0.3740157480314960647 ) ) ;
#43738=CARTESIAN_POINT ( 'NONE',  ( 0.8019270111902717657, -0.1787899950787401604, 0.6446850393163160442 ) ) ;
#43741=CARTESIAN_POINT ( 'NONE',  ( -0.8019270111902717657, 0.1787899950787401604, 1.141732283410804349 ) ) ;
#43743=CARTESIAN_POINT ( 'NONE',  ( -0.9500414927467377701, -0.1787899950787401604, 1.117125984198203970 ) ) ;
#43744=CARTESIAN_POINT ( 'NONE',  ( -1.002407869896990045, 0.1264236179284866091, 0.8587598424659212970 ) ) ;
#43746=( BOUNDED_CURVE ( )  B_SPLINE_CURVE ( 2, ( #4766, #15588, #22994, #16061, #29993, #44537, #22753, #19147, #33814 ),
 .UNSPECIFIED., .F., .T. ) 
 B_SPLINE_CURVE_WITH_KNOTS ( ( 3, 2, 2, 2, 3 ),
 ( 0.8299999999999999600, 0.8325000000000000178, 0.8349999999999999645, 0.8375000000000000222, 0.8399999999999999689 ),
 .UNSPECIFIED. ) 
 CURVE ( )  GEOMETRIC_REPRESENTATION_ITEM ( )  RATIONAL_B_SPLINE_CURVE ( ( 1.000000000000000000, 0.9238795325112899581, 1.000000000000000000, 0.9238795325112869605, 1.000000000000000000, 0.9238795325112869605, 1.000000000000000000, 0.9238795325112869605, 1.000000000000000000 ) ) 
 REPRESENTATION_ITEM ( '' )  ) ;
#43748=CARTESIAN_POINT ( 'NONE',  ( -0.7495606340400177148, -0.1264236179284866091, 0.2485236219934806867 ) ) ;
#43749=DIRECTION ( 'NONE',  ( 1.000000000000000000, 0.000000000000000000, -1.822029033848725275E-16 ) ) ;
#43752=EDGE_LOOP ( 'NONE', ( #4130, #344, #1076, #27454 ) ) ;
#43754=CARTESIAN_POINT ( 'NONE',  ( 0.7813541305413828075, 0.1521468885085573985, 0.03937552627153136087 ) ) ;
#43756=CARTESIAN_POINT ( 'NONE',  ( -0.7646288533564489232, 0.1113553986120547346, 0.5659448817822370081 ) ) ;
#43757=CARTESIAN_POINT ( 'NONE',  ( -0.8759842519685039353, 0.1787899950787401882, 0.7800196849856062542 ) ) ;
#43760=CARTESIAN_POINT ( 'NONE',  ( -0.6971942568897648851, 0.07405724077823318263, 1.855314960576157635 ) ) ;
#43761=( BOUNDED_CURVE ( )  B_SPLINE_CURVE ( 2, ( #20760, #10233, #15663, #12300, #21959, #44851, #23314, #23550, #34344 ),
 .UNSPECIFIED., .F., .T. ) 
 B_SPLINE_CURVE_WITH_KNOTS ( ( 3, 2, 2, 2, 3 ),
 ( 0.7199999999999999734, 0.7225000000000000311, 0.7249999999999999778, 0.7275000000000000355, 0.7299999999999999822 ),
 .UNSPECIFIED. ) 
 CURVE ( )  GEOMETRIC_REPRESENTATION_ITEM ( )  RATIONAL_B_SPLINE_CURVE ( ( 1.000000000000000000, 0.9238795325112869605, 1.000000000000000000, 0.9238795325112869605, 1.000000000000000000, 0.9238795325112869605, 1.000000000000000000, 0.9238795325112799661, 1.000000000000000000 ) ) 
 REPRESENTATION_ITEM ( '' )  ) ;
#43763=CARTESIAN_POINT ( 'NONE',  ( -0.8075642815980649258, 0.1651804164989427171, 0.03937007874015843040 ) ) ;
#43764=CARTESIAN_POINT ( 'NONE',  ( 0.9412147342319837628, -0.1574803149606297803, 0.6717519685039377020 ) ) ;
#43767=CARTESIAN_POINT ( 'NONE',  ( 0.7495606340400177148, 0.1264236179284866091, 0.7898622046706456068 ) ) ;
#43768=CARTESIAN_POINT ( 'NONE',  ( 0.6971942568897648851, 0.07405724077823318263, 1.377952755851748368 ) ) ;
#43773=CARTESIAN_POINT ( 'NONE',  ( 1.033464566929133799, 0.000000000000000000, 1.466535433070866201 ) ) ;
#43774=CARTESIAN_POINT ( 'NONE',  ( 0.8513189030870298435, -0.1720149802712487852, 1.987756617428876327 ) ) ;
#43776=CARTESIAN_POINT ( 'NONE',  ( 0.9412147342319837628, -0.1574803149606297803, 1.488681102254677535 ) ) ;
#43779=CARTESIAN_POINT ( 'NONE',  ( 0.9500414927467377701, 0.1787899950787401604, 0.6988188975840318173 ) ) ;
#43780=CARTESIAN_POINT ( 'NONE',  ( 0.8759842519685039353, -0.1574803149606299191, 0.2657480313885358103 ) ) ;
#43782=CARTESIAN_POINT ( 'NONE',  ( 0.7646288533564489232, 0.1113553986120547346, 1.560039370078740273 ) ) ;
#43784=CARTESIAN_POINT ( 'NONE',  ( -1.033464566929134687, 0.06523048226347956391, 1.154035433070866423 ) ) ;
#43788=CARTESIAN_POINT ( 'NONE',  ( 0.7495606340400177148, 0.1264236179284866091, 1.060531496009228247 ) ) ;
#43790=LINE ( 'NONE', #6888, #16536 ) ;
#43792=CARTESIAN_POINT ( 'NONE',  ( 0.9412147342319837628, 0.1574803149606300301, 1.237696850393701586 ) ) ;
#43794=CARTESIAN_POINT ( 'NONE',  ( -1.054774247047244540, -0.07405724077823318263, 0.05905511805647267048 ) ) ;
#43797=CARTESIAN_POINT ( 'NONE',  ( -0.8107537697050254399, -0.1574803149606297803, 1.847933070866142780 ) ) ;
#43798=CARTESIAN_POINT ( 'NONE',  ( -0.6971942568897648851, -0.07405724077823297447, 1.697834645615527771 ) ) ;
#43799=CARTESIAN_POINT ( 'NONE',  ( 0.7185039370078739607, 0.000000000000000000, 4.498031496062992574 ) ) ;
#43800=CARTESIAN_POINT ( 'NONE',  ( -0.8019270111902717657, -0.1787899950787401604, 1.983267716481667886 ) ) ;
#43801=CARTESIAN_POINT ( 'NONE',  ( 0.8759842519685039353, 0.1574803149606299191, 0.2952755905511810774 ) ) ;
#43802=CARTESIAN_POINT ( 'NONE',  ( 0.9500414927467378812, -0.1787899950787401604, 0.05413385821395302888 ) ) ;
#43805=CYLINDRICAL_SURFACE ( 'NONE', #5778, 0.1574803149606299191 ) ;
#43807=CARTESIAN_POINT ( 'NONE',  ( -0.6971942568897637749, 2.189545951927499583E-17, 0.2386811023084413619 ) ) ;
#43811=CARTESIAN_POINT ( 'NONE',  ( -0.7495606340400177148, 0.1264236179284866091, 1.380413385773007873 ) ) ;
#43817=ADVANCED_FACE ( 'NONE', ( #45814 ), #42678, .T. ) ;
#43820=CARTESIAN_POINT ( 'NONE',  ( -0.9873396505805591694, 0.1113553986120547346, 0.9104330707586141269 ) ) ;
#43822=CARTESIAN_POINT ( 'NONE',  ( 1.054774247047244540, -0.07405724077823318263, 0.4576771653005669016 ) ) ;
#43824=CARTESIAN_POINT ( 'NONE',  ( 1.033464566929134687, 0.06523048226347956391, 1.774114173120818316 ) ) ;
#43826=CARTESIAN_POINT ( 'NONE',  ( -1.033464566929131356, 0.06523048226348168721, 1.419783464459401845 ) ) ;
#43827=CARTESIAN_POINT ( 'NONE',  ( 0.8759842519685039353, 0.1574803149606299191, 0.7283464566929134243 ) ) ;
#43829=ADVANCED_FACE ( 'NONE', ( #27892 ), #31940, .T. ) ;
#43832=CARTESIAN_POINT ( 'NONE',  ( 1.033464566929133799, 1.928577636452524610E-17, 4.498031496062992574 ) ) ;
#43833=VERTEX_POINT ( 'NONE', #24043 ) ;
#43835=VERTEX_POINT ( 'NONE', #21128 ) ;
#43837=CARTESIAN_POINT ( 'NONE',  ( 0.8107537697050254399, -0.1574803149606297803, 1.375492125984252745 ) ) ;
#43841=CARTESIAN_POINT ( 'NONE',  ( -1.033464566929133799, 0.000000000000000000, 0.1574803148531029595 ) ) ;
#43843=CARTESIAN_POINT ( 'NONE',  ( 1.033464566929134687, -0.06523048226347956391, 1.021161417215306955 ) ) ;
#43845=CARTESIAN_POINT ( 'NONE',  ( -0.6971942568897637749, 2.189545951927499583E-17, 0.3961614172690708924 ) ) ;
#43846=ORIENTED_EDGE ( 'NONE', *, *, #18066, .T. ) ;
#43848=CARTESIAN_POINT ( 'NONE',  ( -1.054774247047244096, 0.000000000000000000, 1.680610236166708793 ) ) ;
#43850=CARTESIAN_POINT ( 'NONE',  ( 0.6971942568897648851, -0.07405724077823297447, 1.624015747977732849 ) ) ;
#43851=CARTESIAN_POINT ( 'NONE',  ( -0.9500414927467378812, 0.1787899950787401604, 0.7431102361667091261 ) ) ;
#43852=CARTESIAN_POINT ( 'NONE',  ( 0.8019270111902717657, -0.1787899950787401604, 1.550196850339937926 ) ) ;
#43853=VECTOR ( 'NONE', #28532, 39.37007874015748143 ) ;
#43854=CARTESIAN_POINT ( 'NONE',  ( -1.033464566929133799, 0.000000000000000000, 0.4724409447743622148 ) ) ;
#43855=CARTESIAN_POINT ( 'NONE',  ( -0.9500414927467377701, 0.1787899950787401604, 0.6988188975840318173 ) ) ;
#43858=CARTESIAN_POINT ( 'NONE',  ( 0.7185039370078766252, -0.06523048226348168721, 1.134350393700787940 ) ) ;
#43859=CARTESIAN_POINT ( 'NONE',  ( -0.8019270111902717657, 0.1787899950787401604, 1.574803149552536530 ) ) ;
#43860=CARTESIAN_POINT ( 'NONE',  ( -0.9873396505805591694, -0.1113553986120547346, 1.963582677057826853 ) ) ;
#43861=ORIENTED_EDGE ( 'NONE', *, *, #24269, .F. ) ;
#43862=CARTESIAN_POINT ( 'NONE',  ( -0.7185039370078746268, -0.06523048226347956391, 1.528051181102361600 ) ) ;
#43864=CARTESIAN_POINT ( 'NONE',  ( 1.002407869896990045, 0.1264236179284866091, 1.488681102308440751 ) ) ;
#43866=CYLINDRICAL_SURFACE ( 'NONE', #32563, 0.1574803149606299191 ) ;
#43867=VERTEX_POINT ( 'NONE', #32176 ) ;
#43869=ORIENTED_EDGE ( 'NONE', *, *, #16997, .T. ) ;
#43870=ADVANCED_FACE ( 'NONE', ( #9890 ), #35762, .T. ) ;
#43874=CARTESIAN_POINT ( 'NONE',  ( -0.8759842519685039353, 0.000000000000000000, 0.000000000000000000 ) ) ;
#43877=CARTESIAN_POINT ( 'NONE',  ( 0.6971942568897648851, -0.07405724077823297447, 1.776574803095843924 ) ) ;
#43884=CARTESIAN_POINT ( 'NONE',  ( 1.002407869896990045, -0.1264236179284866091, 0.6865157479777322935 ) ) ;
#43886=CARTESIAN_POINT ( 'NONE',  ( 0.7185039370078739607, 1.928577636452523993E-17, 1.131889763779527547 ) ) ;
#43890=CARTESIAN_POINT ( 'NONE',  ( 0.8759842519685039353, -0.1787899950787401882, 1.828248031442299082 ) ) ;
#43892=CYLINDRICAL_SURFACE ( 'NONE', #19329, 0.1574803149606299191 ) ;
#43893=CARTESIAN_POINT ( 'NONE',  ( 1.054774247047244540, 0.07405724077823318263, 0.4970472440407249226 ) ) ;
#43897=CARTESIAN_POINT ( 'NONE',  ( -0.8019270111902717657, 0.1787899950787401604, 0.4724409448281262636 ) ) ;
#43899=DIRECTION ( 'NONE',  ( -1.000000000000000000, 0.000000000000000000, 0.000000000000000000 ) ) ;
#43901=CARTESIAN_POINT ( 'NONE',  ( -0.7495606340400177148, -0.1264236179284866091, 1.542814960576157413 ) ) ;
#43903=CARTESIAN_POINT ( 'NONE',  ( -1.002407869896990045, -0.1264236179284866091, 1.163877952702141672 ) ) ;
#43906=CARTESIAN_POINT ( 'NONE',  ( 1.002407869896990045, -0.1264236179284866091, 1.946358267662771757 ) ) ;
#43907=CARTESIAN_POINT ( 'NONE',  ( -0.9873396505805591694, 0.1113553986120547346, 0.6053149606299212948 ) ) ;
#43908=CARTESIAN_POINT ( 'NONE',  ( -0.9500414927467378812, 0.1787899950787401604, 1.053149606245450176 ) ) ;
#43911=CARTESIAN_POINT ( 'NONE',  ( 0.9500414927467377701, 0.1787899950787401604, 0.3100393700249766682 ) ) ;
#43912=CARTESIAN_POINT ( 'NONE',  ( -0.8019270111902716547, 0.1787899950787401604, 0.2706692912848194243 ) ) ;
#43913=CARTESIAN_POINT ( 'NONE',  ( -0.8019270111902717657, -0.1787899950787401604, 0.7578740156942689321 ) ) ;
#43914=CARTESIAN_POINT ( 'NONE',  ( 1.033464566929133799, 0.000000000000000000, 1.653543306979086580 ) ) ;
#43917=CARTESIAN_POINT ( 'NONE',  ( 1.054774247047244540, 0.07405724077823318263, 0.7381889763241898939 ) ) ;
#43918=CARTESIAN_POINT ( 'NONE',  ( 0.9500414927467377701, -0.1787899950787401604, 1.043307086560409269 ) ) ;
#43919=CARTESIAN_POINT ( 'NONE',  ( -1.054774247047244540, -0.07405724077823318263, 1.870078740103715331 ) ) ;
#43924=CARTESIAN_POINT ( 'NONE',  ( 1.054774247047244540, -0.07405724077823318263, 1.909448818843873186 ) ) ;
#43931=ADVANCED_FACE ( 'NONE', ( #20656 ), #35535, .T. ) ;
#43933=ORIENTED_EDGE ( 'NONE', *, *, #47352, .T. ) ;
#43934=CARTESIAN_POINT ( 'NONE',  ( 1.054774247047244096, 0.000000000000000000, 1.242618110182456714 ) ) ;
#43937=LINE ( 'NONE', #32951, #128 ) ;
#43938=CARTESIAN_POINT ( 'NONE',  ( 0.7495606340400177148, 0.1264236179284866091, 0.07627952750529173875 ) ) ;
#43941=CARTESIAN_POINT ( 'NONE',  ( -0.8759842519685039353, -0.1787899950787401882, 0.5684055117572598403 ) ) ;
#43945=VECTOR ( 'NONE', #16200, 39.37007874015748143 ) ;
#43946=CARTESIAN_POINT ( 'NONE',  ( 0.9500414927467378812, -0.1787899950787401604, 1.279527559001355286 ) ) ;
#43947=CARTESIAN_POINT ( 'NONE',  ( 1.054774247047244096, 0.000000000000000000, 1.636318897584031484 ) ) ;
#43949=CARTESIAN_POINT ( 'NONE',  ( -0.7185039370078766252, -0.06523048226348168721, 1.636318897530268490 ) ) ;
#43951=CARTESIAN_POINT ( 'NONE',  ( -0.7646288533564489232, -0.1113553986120547346, 1.924212598425196985 ) ) ;
#43952=DIRECTION ( 'NONE',  ( 1.822029033848725028E-16, 0.000000000000000000, 1.000000000000000000 ) ) ;
#43953=CARTESIAN_POINT ( 'NONE',  ( 0.7495606340400177148, -0.1264236179284866091, 0.2829724408911185041 ) ) ;
#43954=CARTESIAN_POINT ( 'NONE',  ( 0.7326906711842074982, -0.08861378245919243613, 0.03937031356849532426 ) ) ;
#43958=CARTESIAN_POINT ( 'NONE',  ( -0.6971942568897648851, 0.07405724077823318263, 1.220472440891118504 ) ) ;
#43959=CARTESIAN_POINT ( 'NONE',  ( 0.7646288533564489232, -0.1113553986120547346, 0.6151574802074331050 ) ) ;
#43963=CARTESIAN_POINT ( 'NONE',  ( 0.9651124939922542945, 0.1429248741482666007, 0.03937007863209032038 ) ) ;
#43964=CARTESIAN_POINT ( 'NONE',  ( 1.033464566929133799, 0.000000000000000000, 0.8267716534357796299 ) ) ;
#43965=CARTESIAN_POINT ( 'NONE',  ( -0.9412147342319837628, 0.1574803149606300301, 1.109744094380661350 ) ) ;
#43966=CARTESIAN_POINT ( 'NONE',  ( 0.7495606340400177148, 0.1264236179284866091, 1.493602362150960650 ) ) ;
#43967=CARTESIAN_POINT ( 'NONE',  ( -0.8107537697050254399, 0.1574803149606300301, 0.9276574803149607584 ) ) ;
#43972=CARTESIAN_POINT ( 'NONE',  ( -1.033464566929134687, 0.06523048226347956391, 0.3666338582677165503 ) ) ;
#43975=CARTESIAN_POINT ( 'NONE',  ( 0.8019270111902717657, 0.1787899950787401604, 0.5511811023084406402 ) ) ;
#43978=CARTESIAN_POINT ( 'NONE',  ( -0.6971942568897648851, 0.07405724077823318263, 1.107283464513165949 ) ) ;
#43979=CARTESIAN_POINT ( 'NONE',  ( -1.033464566929134687, -0.06523048226347956391, 1.975885826771653475 ) ) ;
#43980=CARTESIAN_POINT ( 'NONE',  ( -0.9500414927467378812, -0.1787899950787401604, 0.8070866141194653620 ) ) ;
#43981=EDGE_CURVE ( 'NONE', #34250, #40379, #10853, .T. ) ;
#43983=CARTESIAN_POINT ( 'NONE',  ( -0.8759842519685039353, -0.1787899950787401882, 0.2534448818360003908 ) ) ;
#43984=CARTESIAN_POINT ( 'NONE',  ( 0.9412147342319837628, -0.1574803149606297803, 0.6717519685039375910 ) ) ;
#43988=ORIENTED_EDGE ( 'NONE', *, *, #26374, .F. ) ;
#43996=CARTESIAN_POINT ( 'NONE',  ( -1.054774247047244096, 0.000000000000000000, 0.8095472440407244230 ) ) ;
#43997=CARTESIAN_POINT ( 'NONE',  ( -0.9500414927467377701, 0.1787899950787401604, 1.806102362150961094 ) ) ;
#43998=CARTESIAN_POINT ( 'NONE',  ( -1.054774247047244096, 0.000000000000000000, 0.06643700782025216411 ) ) ;
#44000=CYLINDRICAL_SURFACE ( 'NONE', #21768, 0.1574803149606299191 ) ;
#44001=CARTESIAN_POINT ( 'NONE',  ( -1.033464566929134687, -0.06523048226347956391, 1.493602362097197211 ) ) ;
#44002=CARTESIAN_POINT ( 'NONE',  ( 1.054774247047244096, 0.000000000000000000, 0.8144685038832440993 ) ) ;
#44004=CARTESIAN_POINT ( 'NONE',  ( 0.9412147342319837628, -0.1574803149606297803, 1.380413385826771977 ) ) ;
#44005=CARTESIAN_POINT ( 'NONE',  ( 0.8673732830012496064, -0.1740754669566842439, 1.988051277661635474 ) ) ;
#44008=CARTESIAN_POINT ( 'NONE',  ( 1.054774247047244540, 0.07405724077823318263, 0.8513779527021426707 ) ) ;
#44012=ORIENTED_EDGE ( 'NONE', *, *, #5186, .T. ) ;
#44015=CARTESIAN_POINT ( 'NONE',  ( 0.7495606340400177148, 0.1264236179284866091, 0.9424212597887559051 ) ) ;
#44020=VERTEX_POINT ( 'NONE', #21615 ) ;
#44022=CARTESIAN_POINT ( 'NONE',  ( -0.9500414927467378812, 0.1787899950787401604, 0.02952755900135462311 ) ) ;
#44023=CARTESIAN_POINT ( 'NONE',  ( -0.7185039370078760701, -0.06523048226348075740, 0.7012795275590564259 ) ) ;
#44025=CARTESIAN_POINT ( 'NONE',  ( -0.6971942568897648851, 0.07405724077823318263, 1.732283464513166615 ) ) ;
#44026=VERTEX_POINT ( 'NONE', #29085 ) ;
#44027=CARTESIAN_POINT ( 'NONE',  ( -0.7495606340400177148, -0.1264236179284866091, 0.8735236219934803259 ) ) ;
#44028=CARTESIAN_POINT ( 'NONE',  ( -1.054774247047244540, -0.07405724077823318263, 1.043307086560409269 ) ) ;
#44029=CARTESIAN_POINT ( 'NONE',  ( -0.8759842519685039353, 0.1787899950787401882, 0.3518700786863940833 ) ) ;
#44031=CARTESIAN_POINT ( 'NONE',  ( -0.7185039370078739607, 1.928577636452523993E-17, 0.1476377952755905387 ) ) ;
#44033=CARTESIAN_POINT ( 'NONE',  ( -0.9412147342319837628, 0.1574803149606300301, 0.3223425195775121432 ) ) ;
#44034=CARTESIAN_POINT ( 'NONE',  ( 0.6971942568897626646, 0.07405724077823318263, 0.07874015742655145200 ) ) ;
#44042=( BOUNDED_CURVE ( )  B_SPLINE_CURVE ( 2, ( #30351, #9207, #30119, #19515, #4404, #30574, #11871, #23591, #12595 ),
 .UNSPECIFIED., .F., .F. ) 
 B_SPLINE_CURVE_WITH_KNOTS ( ( 3, 2, 2, 2, 3 ),
 ( 0.1000000000000000056, 0.1024999999999999939, 0.1049999999999999961, 0.1074999999999999983, 0.1100000000000000006 ),
 .UNSPECIFIED. ) 
 CURVE ( )  GEOMETRIC_REPRESENTATION_ITEM ( )  RATIONAL_B_SPLINE_CURVE ( ( 1.000000000000000000, 0.9238795325112869605, 1.000000000000000000, 0.9238795325112869605, 1.000000000000000000, 0.9238795325112869605, 1.000000000000000000, 0.9238795325112869605, 1.000000000000000000 ) ) 
 REPRESENTATION_ITEM ( '' )  ) ;
#44043=CARTESIAN_POINT ( 'NONE',  ( -1.002407869896990045, 0.1264236179284866091, 0.3813976377415121966 ) ) ;
#44045=VERTEX_POINT ( 'NONE', #4091 ) ;
#44046=CARTESIAN_POINT ( 'NONE',  ( -0.8759842519685039353, 0.1787899950787401882, 1.454232283410803017 ) ) ;
#44053=CARTESIAN_POINT ( 'NONE',  ( 1.033464566929134687, -0.06523048226347956391, 0.4010826771653545619 ) ) ;
#44055=CARTESIAN_POINT ( 'NONE',  ( -0.7185039370078739607, 1.928577636452523993E-17, 1.043307086506645831 ) ) ;
#44056=CARTESIAN_POINT ( 'NONE',  ( 1.054774247047244096, 0.000000000000000000, 0.4207677164816693294 ) ) ;
#44057=CARTESIAN_POINT ( 'NONE',  ( -0.9412147342319837628, -0.1574803149606297803, 1.488681102254677535 ) ) ;
#44063=CARTESIAN_POINT ( 'NONE',  ( 1.033464566929134687, -0.06523048226347956391, 0.8735236220472449853 ) ) ;
#44066=EDGE_CURVE ( 'NONE', #19512, #24526, #62, .T. ) ;
#44071=CARTESIAN_POINT ( 'NONE',  ( 1.033464566929133355, 0.06523048226348168721, 1.892224409341292546 ) ) ;
#44077=CARTESIAN_POINT ( 'NONE',  ( 0.7646288533564489232, 0.1113553986120547346, 0.9990157479239685223 ) ) ;
#44079=CARTESIAN_POINT ( 'NONE',  ( -0.6971942568897626646, -0.07405724077823297447, 0.3592519684501735977 ) ) ;
#44083=CARTESIAN_POINT ( 'NONE',  ( -0.8019270111902717657, 0.1787899950787401604, 1.574803149552536530 ) ) ;
#44085=CARTESIAN_POINT ( 'NONE',  ( 0.8019270111902717657, 0.1787899950787401604, 1.771653543253322249 ) ) ;
#44086=CARTESIAN_POINT ( 'NONE',  ( -0.7495606340400177148, 0.1264236179284866091, 0.8292322834108031282 ) ) ;
#44088=CARTESIAN_POINT ( 'NONE',  ( 1.054774247047244540, -0.07405724077823318263, 0.3001968503399373711 ) ) ;
#44089=CARTESIAN_POINT ( 'NONE',  ( -1.033464566929134687, 0.06523048226347956391, 0.2485236220472441526 ) ) ;
#44090=CARTESIAN_POINT ( 'NONE',  ( -0.7495606340400177148, -0.1264236179284866091, 1.267224409395055096 ) ) ;
#44091=CARTESIAN_POINT ( 'NONE',  ( -1.054774247047244096, 0.000000000000000000, 0.7701771653005669016 ) ) ;
#44092=DIRECTION ( 'NONE',  ( 1.822029033848725028E-16, 0.000000000000000000, 1.000000000000000000 ) ) ;
#44093=EDGE_CURVE ( 'NONE', #41784, #35698, #4970, .T. ) ;
#44094=CARTESIAN_POINT ( 'NONE',  ( 0.8759842519685039353, 0.000000000000000000, 4.498031496062992574 ) ) ;
#44095=CARTESIAN_POINT ( 'NONE',  ( -0.6971942568897648851, 0.07405724077823318263, 1.579724409395055318 ) ) ;
#44096=CARTESIAN_POINT ( 'NONE',  ( -1.033464566929133799, 0.000000000000000000, 1.929133858160188897 ) ) ;
#44097=ORIENTED_EDGE ( 'NONE', *, *, #31884, .F. ) ;
#44099=CARTESIAN_POINT ( 'NONE',  ( -1.033464566929133799, 0.000000000000000000, 1.584645669291338654 ) ) ;
#44101=CARTESIAN_POINT ( 'NONE',  ( 1.002407869896990045, 0.1264236179284866091, 1.449311023568283341 ) ) ;
#44103=CARTESIAN_POINT ( 'NONE',  ( -0.7185039370078746268, -0.06523048226347956391, 1.567421259842519454 ) ) ;
#44104=VERTEX_POINT ( 'NONE', #46222 ) ;
#44105=EDGE_CURVE ( 'NONE', #35698, #29740, #17240, .T. ) ;
#44107=EDGE_CURVE ( 'NONE', #34169, #8469, #22185, .T. ) ;
#44117=CARTESIAN_POINT ( 'NONE',  ( 0.6971942568897626646, 0.07405724077823318263, 0.7480314960092282472 ) ) ;
#44121=CARTESIAN_POINT ( 'NONE',  ( 0.6971942568897648851, 0.07405724077823318263, 1.894685039316315489 ) ) ;
#44123=DIRECTION ( 'NONE',  ( 1.822029033848725028E-16, 0.000000000000000000, 1.000000000000000000 ) ) ;
#44125=CARTESIAN_POINT ( 'NONE',  ( 0.9873396505805591694, 0.1113553986120547346, 0.1328740157480315098 ) ) ;
#44128=CARTESIAN_POINT ( 'NONE',  ( -0.8759842519685039353, -0.1787899950787401882, 0.4896653542769449086 ) ) ;
#44131=CARTESIAN_POINT ( 'NONE',  ( 0.8019270111902717657, 0.1787899950787401604, 0.3149606298674962890 ) ) ;
#44133=CARTESIAN_POINT ( 'NONE',  ( 0.8019270111902716547, -0.1787899950787401604, 0.5610236219934807700 ) ) ;
#44134=ADVANCED_FACE ( 'NONE', ( #6674 ), #13197, .T. ) ;
#44135=CARTESIAN_POINT ( 'NONE',  ( -0.9500414927467378812, 0.1787899950787401604, 1.604330708607653921 ) ) ;
#44138=CARTESIAN_POINT ( 'NONE',  ( 0.7495606340400177148, 0.1264236179284866091, 1.262303149552535420 ) ) ;
#44140=CARTESIAN_POINT ( 'NONE',  ( -0.8759842519685039353, -0.1787899950787401882, 1.035925196796629866 ) ) ;
#44143=CARTESIAN_POINT ( 'NONE',  ( -0.7495606340400177148, 0.1264236179284866091, 0.1943897637257641919 ) ) ;
#44144=PRODUCT_DEFINITION_CONTEXT ( 'detailed design', #20485, 'design' ) ;
#44145=CARTESIAN_POINT ( 'NONE',  ( -1.054774247047244540, 0.07405724077823318263, 0.7332677164816707727 ) ) ;
#44146=CARTESIAN_POINT ( 'NONE',  ( 0.7185039370078739607, 1.928577636452523993E-17, 1.673228346349165285 ) ) ;
#44150=CARTESIAN_POINT ( 'NONE',  ( 1.054774247047244540, -0.07405724077823318263, 1.126968503883244654 ) ) ;
#44151=CARTESIAN_POINT ( 'NONE',  ( -0.8759842519685039353, 0.1787899950787401882, 1.803641732229700700 ) ) ;
#44153=CARTESIAN_POINT ( 'NONE',  ( 0.8019270111902717657, 0.1787899950787401604, 1.963582677111591401 ) ) ;
#44154=( BOUNDED_CURVE ( )  B_SPLINE_CURVE ( 2, ( #17382, #577, #26735, #1057, #353, #43967, #33701, #7782, #8017 ),
 .UNSPECIFIED., .F., .T. ) 
 B_SPLINE_CURVE_WITH_KNOTS ( ( 3, 2, 2, 2, 3 ),
 ( 0.4600000000000000200, 0.4625000000000000222, 0.4650000000000000244, 0.4675000000000000266, 0.4699999999999999734 ),
 .UNSPECIFIED. ) 
 CURVE ( )  GEOMETRIC_REPRESENTATION_ITEM ( )  RATIONAL_B_SPLINE_CURVE ( ( 1.000000000000000000, 0.9238795325112869605, 1.000000000000000000, 0.9238795325112869605, 1.000000000000000000, 0.9238795325112869605, 1.000000000000000000, 0.9238795325112849621, 1.000000000000000000 ) ) 
 REPRESENTATION_ITEM ( '' )  ) ;
#44155=CARTESIAN_POINT ( 'NONE',  ( 0.7185039370078739607, 1.928577636452523993E-17, 0.7381889763779527769 ) ) ;
#44157=ORIENTED_EDGE ( 'NONE', *, *, #13985, .F. ) ;
#44160=ORIENTED_EDGE ( 'NONE', *, *, #37703, .F. ) ;
#44161=CARTESIAN_POINT ( 'NONE',  ( 1.054774247047244540, -0.07405724077823318263, 1.200787401521039355 ) ) ;
#44164=CARTESIAN_POINT ( 'NONE',  ( 0.9500414927467378812, 0.1787899950787401604, 0.1476377952218271561 ) ) ;
#44166=CARTESIAN_POINT ( 'NONE',  ( -0.8019270111902716547, -0.1787899950787401604, 0.4478346456155276045 ) ) ;
#44168=CARTESIAN_POINT ( 'NONE',  ( 0.7185039370078746268, 0.06523048226347956391, 0.3813976377952755237 ) ) ;
#44170=CARTESIAN_POINT ( 'NONE',  ( 1.033464566929133799, 0.000000000000000000, 0.7480314959554645871 ) ) ;
#44171=CARTESIAN_POINT ( 'NONE',  ( 0.6971942568897648851, -0.07405724077823297447, 1.387795275536786610 ) ) ;
#44172=CARTESIAN_POINT ( 'NONE',  ( 0.8759842519685039353, -0.1787899950787401882, 1.744586614119464807 ) ) ;
#44173=CARTESIAN_POINT ( 'NONE',  ( -0.7185039370078739607, 0.000000000000000000, -2.869337061179095023E-17 ) ) ;
#44176=CARTESIAN_POINT ( 'NONE',  ( -0.8759842519685039353, 0.000000000000000000, 0.000000000000000000 ) ) ;
#44177=CARTESIAN_POINT ( 'NONE',  ( -0.8107537697050254399, -0.1574803149606297803, 1.021161417322834497 ) ) ;
#44178=CARTESIAN_POINT ( 'NONE',  ( 1.033464566929134687, 0.06523048226347956391, 0.7504921258767240921 ) ) ;
#44179=CARTESIAN_POINT ( 'NONE',  ( 1.002407869896990045, -0.1264236179284866091, 0.2534448818360003908 ) ) ;
#44181=CARTESIAN_POINT ( 'NONE',  ( 0.7020369131201283919, 0.02831345972461313948, 0.03937007867491748581 ) ) ;
#44184=CARTESIAN_POINT ( 'NONE',  ( -0.9500414927467378812, -0.1787899950787401604, 1.274606299158834277 ) ) ;
#44185=CARTESIAN_POINT ( 'NONE',  ( 0.7185039370078746268, -0.06523048226347956391, 0.6914370077664893088 ) ) ;
#44193=CARTESIAN_POINT ( 'NONE',  ( -1.033464566929133799, 0.000000000000000000, 0.03937007874015843040 ) ) ;
#44194=CARTESIAN_POINT ( 'NONE',  ( 0.8759842519685039353, 0.1787899950787401882, 1.646161417269070837 ) ) ;
#44200=AXIS2_PLACEMENT_3D ( 'NONE', #13552, #28188, #17375 ) ;
#44201=CYLINDRICAL_SURFACE ( 'NONE', #47433, 0.1574803149606299191 ) ;
#44204=VERTEX_POINT ( 'NONE', #17936 ) ;
#44205=CARTESIAN_POINT ( 'NONE',  ( -1.054774247047244540, -0.07405724077823318263, 1.476377952702141449 ) ) ;
#44207=CARTESIAN_POINT ( 'NONE',  ( -1.054774247047244540, -0.07405724077823318263, 1.284448818843874740 ) ) ;
#44209=DIRECTION ( 'NONE',  ( 0.000000000000000000, 0.000000000000000000, -1.000000000000000000 ) ) ;
#44210=CARTESIAN_POINT ( 'NONE',  ( -1.054774247047244540, 0.07405724077823318263, 0.2657480314422993595 ) ) ;
#44214=ORIENTED_EDGE ( 'NONE', *, *, #4698, .T. ) ;
#44215=CARTESIAN_POINT ( 'NONE',  ( 0.9873396505805591694, -0.1113553986120547346, 1.067913385826771755 ) ) ;
#44216=ORIENTED_EDGE ( 'NONE', *, *, #27476, .T. ) ;
#44217=CARTESIAN_POINT ( 'NONE',  ( 0.9500414927467378812, 0.1787899950787401604, 1.013779527505291878 ) ) ;
#44219=CARTESIAN_POINT ( 'NONE',  ( -0.8759842519685039353, -0.1787899950787401882, 0.7997047243556849594 ) ) ;
#44220=AXIS2_PLACEMENT_3D ( 'NONE', #5471, #9314, #4997 ) ;
#44221=CARTESIAN_POINT ( 'NONE',  ( -0.8759842519685039353, -0.1787899950787401882, 1.828248031442299082 ) ) ;
#44224=CARTESIAN_POINT ( 'NONE',  ( -0.7646288533564489232, -0.1113553986120547346, 0.8612204724409449064 ) ) ;
#44227=LINE ( 'NONE', #26049, #6454 ) ;
#44228=CARTESIAN_POINT ( 'NONE',  ( -0.7185039370078739607, 1.928577636452523993E-17, 1.476377952648377789 ) ) ;
#44229=CARTESIAN_POINT ( 'NONE',  ( 1.054774247047244540, -0.07405724077823318263, 0.8513779527021426707 ) ) ;
#44231=CARTESIAN_POINT ( 'NONE',  ( 0.7185039370078746268, -0.06523048226347956391, 1.370570866141733291 ) ) ;
#44232=CARTESIAN_POINT ( 'NONE',  ( 0.7316628141368787253, 0.07653111172288938613, 1.981731121241584015 ) ) ;
#44233=CARTESIAN_POINT ( 'NONE',  ( 0.7185039370078739607, 1.928577636452523993E-17, 1.555118110128692832 ) ) ;
#44235=ADVANCED_FACE ( 'NONE', ( #22713 ), #3793, .T. ) ;
#44236=CARTESIAN_POINT ( 'NONE',  ( 1.054774247047244540, 0.07405724077823318263, 0.8907480314422985268 ) ) ;
#44240=ORIENTED_EDGE ( 'NONE', *, *, #36817, .T. ) ;
#44241=CARTESIAN_POINT ( 'NONE',  ( 0.8759842519685039353, 0.1574803149606299191, 1.082677165354330784 ) ) ;
#44243=CARTESIAN_POINT ( 'NONE',  ( 1.054774247047244540, -0.07405724077823318263, 1.200787401521039355 ) ) ;
#44245=CARTESIAN_POINT ( 'NONE',  ( -0.9412147342319837628, 0.1574803149606300301, 1.040846456692913424 ) ) ;
#44250=CARTESIAN_POINT ( 'NONE',  ( 0.8759842519685039353, 0.000000000000000000, 4.498031496062992574 ) ) ;
#44251=CARTESIAN_POINT ( 'NONE',  ( -1.054774247047244540, -0.07405724077823318263, 0.1771653542769450751 ) ) ;
#44253=CARTESIAN_POINT ( 'NONE',  ( 0.8759842519685039353, 0.1574803149606299191, 0.3346456692913385988 ) ) ;
#44255=CARTESIAN_POINT ( 'NONE',  ( -0.8759842519685039353, -0.1787899950787401882, 1.665846456639149764 ) ) ;
#44256=CARTESIAN_POINT ( 'NONE',  ( -1.054774247047244540, -0.07405724077823318263, 0.9251968503399373711 ) ) ;
#44258=CARTESIAN_POINT ( 'NONE',  ( -1.002407869896990045, -0.1264236179284866091, 0.3371062991588349989 ) ) ;
#44259=DIRECTION ( 'NONE',  ( 0.000000000000000000, 0.000000000000000000, -1.000000000000000000 ) ) ;
#44267=CARTESIAN_POINT ( 'NONE',  ( -1.002407869896990045, 0.1264236179284866091, 0.2632874015210397434 ) ) ;
#44268=ORIENTED_EDGE ( 'NONE', *, *, #34263, .T. ) ;
#44269=CARTESIAN_POINT ( 'NONE',  ( -1.054774247047244096, 0.000000000000000000, 1.326279527505291433 ) ) ;
#44273=DIRECTION ( 'NONE',  ( -1.000000000000000000, 0.000000000000000000, 0.000000000000000000 ) ) ;
#44274=CARTESIAN_POINT ( 'NONE',  ( 0.7185039370078746268, -0.06523048226347956391, 0.4256889763779528324 ) ) ;
#44276=CARTESIAN_POINT ( 'NONE',  ( -1.033464566929134687, 0.06523048226347956391, 1.065452755797984041 ) ) ;
#44278=CARTESIAN_POINT ( 'NONE',  ( 0.9500414927467378812, -0.1787899950787401604, 0.4527559054580477249 ) ) ;
#44279=CARTESIAN_POINT ( 'NONE',  ( 0.7185039370078746268, 0.06523048226347956391, 0.5684055117034967353 ) ) ;
#44281=CARTESIAN_POINT ( 'NONE',  ( 0.9873396505805591694, -0.1113553986120547346, 1.924212598317669221 ) ) ;
#44283=FACE_OUTER_BOUND ( 'NONE', #13065, .T. ) ;
#44284=CARTESIAN_POINT ( 'NONE',  ( -0.9500414927467377701, 0.1787899950787401604, 0.9005905511273391006 ) ) ;
#44285=CARTESIAN_POINT ( 'NONE',  ( 0.8107537697050253289, 0.1574803149606300301, 0.9276574803149607584 ) ) ;
#44290=CARTESIAN_POINT ( 'NONE',  ( -0.7185039370078760701, -0.06523048226348075740, 0.8193897637795283240 ) ) ;
#44294=CARTESIAN_POINT ( 'NONE',  ( 0.8759842519685039353, 0.1787899950787401882, 0.6619094487651338010 ) ) ;
#44296=ORIENTED_EDGE ( 'NONE', *, *, #14723, .F. ) ;
#44297=CARTESIAN_POINT ( 'NONE',  ( -0.8759842519685039353, 0.1574803149606299191, 1.781496062884598164 ) ) ;
#44302=CARTESIAN_POINT ( 'NONE',  ( 0.7185039370078746268, 0.06523048226347956391, 1.080216535325543958 ) ) ;
#44304=CARTESIAN_POINT ( 'NONE',  ( -0.6971942568897626646, -0.07405724077823297447, 0.4773622046706456068 ) ) ;
#44307=ORIENTED_EDGE ( 'NONE', *, *, #24160, .F. ) ;
#44308=CARTESIAN_POINT ( 'NONE',  ( -1.054774247047244540, -0.07405724077823318263, 1.717519684985606476 ) ) ;
#44309=CARTESIAN_POINT ( 'NONE',  ( 1.054774247047244096, 0.000000000000000000, 1.680610236166708793 ) ) ;
#44311=CARTESIAN_POINT ( 'NONE',  ( -0.8759842519685039353, -0.1787899950787401882, 0.7258858267178898149 ) ) ;
#44313=CARTESIAN_POINT ( 'NONE',  ( 0.7495606340400177148, -0.1264236179284866091, 0.2485236219934806867 ) ) ;
#44314=CARTESIAN_POINT ( 'NONE',  ( -0.9500414927467377701, -0.1787899950787401604, 1.195866141678520345 ) ) ;
#44315=CARTESIAN_POINT ( 'NONE',  ( -0.9500414927467377701, -0.1787899950787401604, 0.8021653542769462408 ) ) ;
#44317=( BOUNDED_CURVE ( )  B_SPLINE_CURVE ( 2, ( #29894, #33001, #44913, #123, #33242, #43984, #44672, #25800, #29673 ),
 .UNSPECIFIED., .F., .T. ) 
 B_SPLINE_CURVE_WITH_KNOTS ( ( 3, 2, 2, 2, 3 ),
 ( 0.3300000000000000155, 0.3325000000000000178, 0.3350000000000000200, 0.3375000000000000222, 0.3400000000000000244 ),
 .UNSPECIFIED. ) 
 CURVE ( )  GEOMETRIC_REPRESENTATION_ITEM ( )  RATIONAL_B_SPLINE_CURVE ( ( 1.000000000000000000, 0.9238795325112869605, 1.000000000000000000, 0.9238795325112869605, 1.000000000000000000, 0.9238795325112869605, 1.000000000000000000, 0.9238795325112869605, 1.000000000000000000 ) ) 
 REPRESENTATION_ITEM ( '' )  ) ;
#44320=CARTESIAN_POINT ( 'NONE',  ( -0.8019270111902717657, -0.1787899950787401604, 1.628937007820252303 ) ) ;
#44321=CARTESIAN_POINT ( 'NONE',  ( -0.9873396505805591694, 0.1113553986120547346, 1.815944881782236120 ) ) ;
#44323=CARTESIAN_POINT ( 'NONE',  ( -0.8759842519685039353, 0.1574803149606299191, 1.555118110236220597 ) ) ;
#44325=CARTESIAN_POINT ( 'NONE',  ( 0.7495606340400177148, 0.1264236179284866091, 1.459153543253322693 ) ) ;
#44336=CARTESIAN_POINT ( 'NONE',  ( 1.002407869896990045, 0.1264236179284866091, 1.759350393647023614 ) ) ;
#44339=CARTESIAN_POINT ( 'NONE',  ( -0.7646288533564489232, 0.1113553986120547346, 1.077755905404283565 ) ) ;
#44340=CARTESIAN_POINT ( 'NONE',  ( 0.8759842519685039353, -0.1787899950787401882, 0.7209645668753701386 ) ) ;
#44345=CARTESIAN_POINT ( 'NONE',  ( 1.033464566929134687, 0.06523048226347956391, 0.4453740157480309270 ) ) ;
#44349=CARTESIAN_POINT ( 'NONE',  ( 0.8107537697050253289, 0.1574803149606300301, 0.1008858267716536417 ) ) ;
#44352=CARTESIAN_POINT ( 'NONE',  ( -0.7646288533564489232, 0.1113553986120547346, 0.1820866141732283561 ) ) ;
#44354=CARTESIAN_POINT ( 'NONE',  ( 1.054774247047244096, 0.000000000000000000, 0.1845472440407248116 ) ) ;
#44355=CARTESIAN_POINT ( 'NONE',  ( 0.7185039370078739607, 1.928577636452523993E-17, 0.06889763779527559306 ) ) ;
#44356=CARTESIAN_POINT ( 'NONE',  ( -1.002407869896990045, 0.1264236179284866091, 1.798720472387181024 ) ) ;
#44358=CARTESIAN_POINT ( 'NONE',  ( -0.7495606340400177148, 0.1264236179284866091, 1.183562992072220599 ) ) ;
#44359=DIRECTION ( 'NONE',  ( 1.822029033848725028E-16, 0.000000000000000000, 1.000000000000000000 ) ) ;
#44360=CARTESIAN_POINT ( 'NONE',  ( 0.6971942568897648851, -0.07405724077823297447, 1.269685039316314601 ) ) ;
#44362=CARTESIAN_POINT ( 'NONE',  ( 0.9500414927467378812, -0.1787899950787401604, 1.983267716481667886 ) ) ;
#44363=CARTESIAN_POINT ( 'NONE',  ( -0.8759842519685039353, 0.1787899950787401882, 1.134350393647023614 ) ) ;
#44365=DIRECTION ( 'NONE',  ( 0.000000000000000000, 0.000000000000000000, -1.000000000000000000 ) ) ;
#44366=CARTESIAN_POINT ( 'NONE',  ( 0.6971942568897637749, 2.189545951927499583E-17, 0.4798228345919055560 ) ) ;
#44367=CARTESIAN_POINT ( 'NONE',  ( -0.8759842519685039353, -0.1787899950787401882, 0.3666338582139531677 ) ) ;
#44368=CARTESIAN_POINT ( 'NONE',  ( -0.9500414927467378812, 0.1787899950787401604, 0.7775590550643479704 ) ) ;
#44370=CARTESIAN_POINT ( 'NONE',  ( -0.7185039370078739607, 1.928577636452523993E-17, 0.8858267715460158565 ) ) ;
#44371=ORIENTED_EDGE ( 'NONE', *, *, #16889, .T. ) ;
#44372=CARTESIAN_POINT ( 'NONE',  ( -1.033464566929133799, 0.000000000000000000, 0.2066929133858267931 ) ) ;
#44373=CARTESIAN_POINT ( 'NONE',  ( 0.6971942568897637749, 2.189545951927499583E-17, 1.070374015694267600 ) ) ;
#44374=CARTESIAN_POINT ( 'NONE',  ( -0.8019270111902716547, -0.1787899950787401604, 1.938976377898990799 ) ) ;
#44376=CARTESIAN_POINT ( 'NONE',  ( 0.6971942568897637749, 2.189545951927499583E-17, 1.931594488135212728 ) ) ;
#44380=ORIENTED_EDGE ( 'NONE', *, *, #31241, .T. ) ;
#44384=CARTESIAN_POINT ( 'NONE',  ( 1.054774247047244096, 0.000000000000000000, 1.203248031442299304 ) ) ;
#44387=CARTESIAN_POINT ( 'NONE',  ( 1.054774247047244096, 0.000000000000000000, 1.478838582623401399 ) ) ;
#44388=CARTESIAN_POINT ( 'NONE',  ( 1.054774247047244096, 0.000000000000000000, 0.1402559054580474474 ) ) ;
#44389=EDGE_CURVE ( 'NONE', #20413, #33274, #2754, .T. ) ;
#44393=CARTESIAN_POINT ( 'NONE',  ( -1.002407869896990045, 0.1264236179284866091, 0.5831692912848189803 ) ) ;
#44397=CARTESIAN_POINT ( 'NONE',  ( -0.8759842519685039353, 0.1574803149606299191, 1.200787401574803237 ) ) ;
#44398=CARTESIAN_POINT ( 'NONE',  ( 0.8019270111902717657, 0.1787899950787401604, 1.417322834591906222 ) ) ;
#44399=CARTESIAN_POINT ( 'NONE',  ( 0.8019270111902716547, -0.1787899950787401604, 1.702755905458047003 ) ) ;
#44400=CARTESIAN_POINT ( 'NONE',  ( 1.002407869896990045, -0.1264236179284866091, 0.2928149605761578567 ) ) ;
#44401=CARTESIAN_POINT ( 'NONE',  ( 0.9873396505805591694, 0.1113553986120547346, 0.1328740157480315098 ) ) ;
#44403=CARTESIAN_POINT ( 'NONE',  ( -0.7185039370078778465, -0.06523048226348396317, 1.439468503829480772 ) ) ;
#44404=CARTESIAN_POINT ( 'NONE',  ( -0.7692685849603985160, 0.1211171519384340173, 1.980616872294691522 ) ) ;
#44410=CARTESIAN_POINT ( 'NONE',  ( -0.8759842519685039353, -0.1787899950787401882, 1.232775590497417362 ) ) ;
#44411=CARTESIAN_POINT ( 'NONE',  ( 0.7646288533564489232, 0.1113553986120547346, 0.6446850392625511628 ) ) ;
#44414=CARTESIAN_POINT ( 'NONE',  ( 0.8075642843603819676, 0.1651804176431314886, 0.03937007863263043694 ) ) ;
#44415=ORIENTED_EDGE ( 'NONE', *, *, #321, .F. ) ;
#44417=CARTESIAN_POINT ( 'NONE',  ( -0.7646288533564489232, -0.1113553986120547346, 0.3001968502861740440 ) ) ;
#44419=ORIENTED_EDGE ( 'NONE', *, *, #10130, .F. ) ;
#44420=FACE_OUTER_BOUND ( 'NONE', #13825, .T. ) ;
#44421=CARTESIAN_POINT ( 'NONE',  ( 0.9500414927467378812, 0.1787899950787401604, 1.564960629867495845 ) ) ;
#44424=CARTESIAN_POINT ( 'NONE',  ( -0.7646288533564489232, -0.1113553986120547346, 0.1131889763779527630 ) ) ;
#44425=CARTESIAN_POINT ( 'NONE',  ( 0.7646288533564489232, 0.1113553986120547346, 0.3690944880814492901 ) ) ;
#44426=CARTESIAN_POINT ( 'NONE',  ( -0.8759842519685039353, -0.1787899950787401882, 0.05167322829269314910 ) ) ;
#44429=( BOUNDED_CURVE ( )  B_SPLINE_CURVE ( 2, ( #25880, #36899, #4053, #3591, #32381, #10322, #47447, #43117, #24934 ),
 .UNSPECIFIED., .F., .T. ) 
 B_SPLINE_CURVE_WITH_KNOTS ( ( 3, 2, 2, 2, 3 ),
 ( 0.2899999999999999800, 0.2924999999999999822, 0.2949999999999999845, 0.2974999999999999867, 0.2999999999999999889 ),
 .UNSPECIFIED. ) 
 CURVE ( )  GEOMETRIC_REPRESENTATION_ITEM ( )  RATIONAL_B_SPLINE_CURVE ( ( 1.000000000000000000, 0.9238795325112869605, 1.000000000000000000, 0.9238795325112869605, 1.000000000000000000, 0.9238795325112869605, 1.000000000000000000, 0.9238795325112869605, 1.000000000000000000 ) ) 
 REPRESENTATION_ITEM ( '' )  ) ;
#44432=CARTESIAN_POINT ( 'NONE',  ( 0.6971942568897637749, 2.189545951927499583E-17, 0.8341535432533228045 ) ) ;
#44433=CARTESIAN_POINT ( 'NONE',  ( -0.7495606340400177148, 0.1264236179284866091, 1.493602362150960650 ) ) ;
#44435=CARTESIAN_POINT ( 'NONE',  ( -0.7495606340400177148, 0.1264236179284866091, 1.341043307032850462 ) ) ;
#44437=CARTESIAN_POINT ( 'NONE',  ( -0.8759842519685039353, 0.1787899950787401882, 0.3124999999462365619 ) ) ;
#44442=CARTESIAN_POINT ( 'NONE',  ( -1.033464566929133799, 0.000000000000000000, 0.8661417321759370402 ) ) ;
#44445=CARTESIAN_POINT ( 'NONE',  ( 0.7495606340400177148, -0.1264236179284866091, 1.031003936954110189 ) ) ;
#44452=AXIS2_PLACEMENT_3D ( 'NONE', #3840, #469, #21583 ) ;
#44455=CARTESIAN_POINT ( 'NONE',  ( -0.6971942568897626646, -0.07405724077823297447, 0.1673228345919059168 ) ) ;
#44456=CARTESIAN_POINT ( 'NONE',  ( -0.9873396505805591694, 0.1113553986120547346, 0.8415354330708662012 ) ) ;
#44458=DIRECTION ( 'NONE',  ( 0.000000000000000000, 0.000000000000000000, 1.000000000000000000 ) ) ;
#44460=CARTESIAN_POINT ( 'NONE',  ( 0.8759842519685039353, -0.1787899950787401882, 0.9621062991588346103 ) ) ;
#44461=CARTESIAN_POINT ( 'NONE',  ( 0.6971942568897648851, -0.07405724077823297447, 1.382874015694267822 ) ) ;
#44462=CARTESIAN_POINT ( 'NONE',  ( 0.9500414927467377701, 0.1787899950787401604, 0.1082677164816695514 ) ) ;
#44464=CARTESIAN_POINT ( 'NONE',  ( 1.033464566929134687, 0.06523048226347956391, 1.468996062992126150 ) ) ;
#44465=CARTESIAN_POINT ( 'NONE',  ( 0.7132418682741867855, -0.03858023259734958549, 1.983985632872960592 ) ) ;
#44468=CARTESIAN_POINT ( 'NONE',  ( 0.7495606340400177148, 0.1264236179284866091, 0.8243110235682834519 ) ) ;
#44472=CARTESIAN_POINT ( 'NONE',  ( 0.8107537697050254399, -0.1574803149606297803, 0.4207677164279060578 ) ) ;
#44474=CARTESIAN_POINT ( 'NONE',  ( 0.6971942568897648851, -0.07405724077823297447, 1.186023621993481658 ) ) ;
#44475=CARTESIAN_POINT ( 'NONE',  ( -0.8107537697050254399, 0.1574803149606300301, 1.045767716535432879 ) ) ;
#44478=VERTEX_POINT ( 'NONE', #644 ) ;
#44480=CARTESIAN_POINT ( 'NONE',  ( -0.7495606340400177148, -0.1264236179284866091, 0.2436023621509610382 ) ) ;
#44483=VECTOR ( 'NONE', #13801, 39.37007874015748143 ) ;
#44484=CARTESIAN_POINT ( 'NONE',  ( -0.6971942568897637749, 2.189545951927499583E-17, 1.852854330654897685 ) ) ;
#44485=CARTESIAN_POINT ( 'NONE',  ( -0.8019270111902716547, 0.1787899950787401604, 0.9005905511273391006 ) ) ;
#44487=CARTESIAN_POINT ( 'NONE',  ( -1.002407869896990045, -0.1264236179284866091, 0.4945866141194645849 ) ) ;
#44497=CARTESIAN_POINT ( 'NONE',  ( -0.7495606340400177148, -0.1264236179284866091, 0.2436023621509610382 ) ) ;
#44499=EDGE_CURVE ( 'NONE', #7899, #398, #9038, .T. ) ;
#44503=ADVANCED_FACE ( 'NONE', ( #16484 ), #886, .T. ) ;
#44504=ORIENTED_EDGE ( 'NONE', *, *, #23109, .T. ) ;
#44512=CARTESIAN_POINT ( 'NONE',  ( 0.9873396505805591694, -0.1113553986120547346, 0.4773622047244094890 ) ) ;
#44514=CARTESIAN_POINT ( 'NONE',  ( -0.7646288533564489232, -0.1113553986120547346, 1.087598425089322918 ) ) ;
#44515=CARTESIAN_POINT ( 'NONE',  ( 1.002407869896990045, 0.1264236179284866091, 0.6225393700249762796 ) ) ;
#44523=CARTESIAN_POINT ( 'NONE',  ( -1.054774247047244540, 0.07405724077823318263, 0.9350393700249758355 ) ) ;
#44524=CARTESIAN_POINT ( 'NONE',  ( 0.9873396505805591694, -0.1113553986120547346, 0.9104330708661417804 ) ) ;
#44529=CARTESIAN_POINT ( 'NONE',  ( 1.033464566929133799, 0.000000000000000000, 1.466535433070866201 ) ) ;
#44531=CARTESIAN_POINT ( 'NONE',  ( 0.8107537697050254399, 0.1574803149606300301, 1.281988188976378895 ) ) ;
#44536=CARTESIAN_POINT ( 'NONE',  ( 0.8107537697050253289, 0.1574803149606300301, 1.154035432963338659 ) ) ;
#44537=CARTESIAN_POINT ( 'NONE',  ( -0.9412147342319837628, -0.1574803149606297803, 1.656003937007873628 ) ) ;
#44538=ORIENTED_EDGE ( 'NONE', *, *, #17593, .F. ) ;
#44540=CARTESIAN_POINT ( 'NONE',  ( -0.8019270111902717657, -0.1787899950787401604, 1.707677165300566235 ) ) ;
#44541=CARTESIAN_POINT ( 'NONE',  ( 0.9500414927467378812, 0.1787899950787401604, 1.766732283410803461 ) ) ;
#44542=ORIENTED_EDGE ( 'NONE', *, *, #15497, .T. ) ;
#44543=CARTESIAN_POINT ( 'NONE',  ( -0.7495606340400177148, 0.1264236179284866091, 0.9079724408911180600 ) ) ;
#44546=CARTESIAN_POINT ( 'NONE',  ( -0.9500414927467377701, 0.1787899950787401604, 1.210629921206079818 ) ) ;
#44547=CARTESIAN_POINT ( 'NONE',  ( -0.7495606340400177148, -0.1264236179284866091, 0.8735236219934803259 ) ) ;
#44548=CARTESIAN_POINT ( 'NONE',  ( -0.7495606340400177148, 0.1264236179284866091, 0.1599409448281264023 ) ) ;
#44551=CARTESIAN_POINT ( 'NONE',  ( -0.7495606340400177148, 0.1264236179284866091, 1.616633858213952779 ) ) ;
#44552=CARTESIAN_POINT ( 'NONE',  ( -0.9412147342319837628, 0.1574803149606300301, 1.857775590443653257 ) ) ;
#44555=CARTESIAN_POINT ( 'NONE',  ( -0.9873396505805591694, -0.1113553986120547346, 1.579724409448818978 ) ) ;
#44556=CARTESIAN_POINT ( 'NONE',  ( 0.9873396505805591694, 0.1113553986120547346, 1.628937007874015963 ) ) ;
#44557=CARTESIAN_POINT ( 'NONE',  ( 0.7495606340400177148, -0.1264236179284866091, 1.626476377898992132 ) ) ;
#44559=CARTESIAN_POINT ( 'NONE',  ( -1.033464566929133799, 0.000000000000000000, 0.7972440944881890035 ) ) ;
#44561=VERTEX_POINT ( 'NONE', #12179 ) ;
#44573=CARTESIAN_POINT ( 'NONE',  ( 0.9500414927467378812, -0.1787899950787401604, 0.7234251967966300878 ) ) ;
#44577=LINE ( 'NONE', #726, #16970 ) ;
#44578=CARTESIAN_POINT ( 'NONE',  ( 0.8759842519685039353, 0.1787899950787401882, 1.847933070812378009 ) ) ;
#44580=CARTESIAN_POINT ( 'NONE',  ( 0.7646288533564489232, 0.1113553986120547346, 0.06397637795275590289 ) ) ;
#44584=ADVANCED_FACE ( 'NONE', ( #30418 ), #20059, .T. ) ;
#44586=( BOUNDED_CURVE ( )  B_SPLINE_CURVE ( 2, ( #13162, #17203, #45950, #35664, #46422, #31838, #38997, #42800, #46655 ),
 .UNSPECIFIED., .F., .F. ) 
 B_SPLINE_CURVE_WITH_KNOTS ( ( 3, 2, 2, 2, 3 ),
 ( 0.6700000000000000400, 0.6724999999999999867, 0.6750000000000000444, 0.6774999999999999911, 0.6800000000000000488 ),
 .UNSPECIFIED. ) 
 CURVE ( )  GEOMETRIC_REPRESENTATION_ITEM ( )  RATIONAL_B_SPLINE_CURVE ( ( 1.000000000000000000, 0.9238795325112869605, 1.000000000000000000, 0.9238795325112869605, 1.000000000000000000, 0.9238795325112869605, 1.000000000000000000, 0.9238795325112869605, 1.000000000000000000 ) ) 
 REPRESENTATION_ITEM ( '' )  ) ;
#44587=CARTESIAN_POINT ( 'NONE',  ( 0.6971942568897626646, 0.07405724077823318263, 0.2411417322297011168 ) ) ;
#44588=CARTESIAN_POINT ( 'NONE',  ( 1.033464566929133799, 0.000000000000000000, 1.742125984251968518 ) ) ;
#44589=CARTESIAN_POINT ( 'NONE',  ( -1.054774247047244096, 0.000000000000000000, 1.793799212544661348 ) ) ;
#44592=CARTESIAN_POINT ( 'NONE',  ( -0.7495606340400177148, 0.1264236179284866091, 1.301673228292692830 ) ) ;
#44594=CARTESIAN_POINT ( 'NONE',  ( 0.8759842519685039353, 0.1787899950787401882, 1.961122047190330786 ) ) ;
#44595=CARTESIAN_POINT ( 'NONE',  ( -0.9500414927467378812, 0.1787899950787401604, 1.013779527505291878 ) ) ;
#44598=CARTESIAN_POINT ( 'NONE',  ( 0.6971942568897648851, 0.07405724077823318263, 0.5167322834108035723 ) ) ;
#44599=CARTESIAN_POINT ( 'NONE',  ( -1.002407869896990045, -0.1264236179284866091, 0.4109251967966299213 ) ) ;
#44600=CARTESIAN_POINT ( 'NONE',  ( 0.7646288533564489232, 0.1113553986120547346, 1.668307086506645609 ) ) ;
#44601=CARTESIAN_POINT ( 'NONE',  ( -1.033464566929133799, 0.000000000000000000, 1.348425196850393748 ) ) ;
#44602=CARTESIAN_POINT ( 'NONE',  ( 0.6971942568897626646, -0.07405724077823297447, 0.8759842519147408302 ) ) ;
#44603=CARTESIAN_POINT ( 'NONE',  ( -0.9412147342319837628, -0.1574803149606297803, 0.08120078740157485320 ) ) ;
#44606=VECTOR ( 'NONE', #26941, 39.37007874015748143 ) ;
#44609=CARTESIAN_POINT ( 'NONE',  ( -0.8759842519685039353, 0.1787899950787401882, 0.03198818892261445085 ) ) ;
#44615=CARTESIAN_POINT ( 'NONE',  ( 0.8759842519685039353, -0.1787899950787401882, 1.154035433017102319 ) ) ;
#44616=EDGE_CURVE ( 'NONE', #1642, #12322, #35292, .T. ) ;
#44618=EDGE_CURVE ( 'NONE', #23610, #12346, #22955, .T. ) ;
#44620=DIRECTION ( 'NONE',  ( 1.822029033848725028E-16, 0.000000000000000000, 1.000000000000000000 ) ) ;
#44621=CARTESIAN_POINT ( 'NONE',  ( 0.8759842519685039353, 0.1787899950787401882, 1.528051181048598384 ) ) ;
#44622=CARTESIAN_POINT ( 'NONE',  ( 0.8019270111902717657, -0.1787899950787401604, 0.2066929133320631329 ) ) ;
#44626=CARTESIAN_POINT ( 'NONE',  ( -0.8759842519685039353, -0.1787899950787401882, 0.7258858267178898149 ) ) ;
#44628=CARTESIAN_POINT ( 'NONE',  ( 0.7646288533564489232, -0.1113553986120547346, 0.3001968502861740440 ) ) ;
#44632=CARTESIAN_POINT ( 'NONE',  ( 0.8019270111902717657, 0.1787899950787401604, 1.299212598371432215 ) ) ;
#44633=CARTESIAN_POINT ( 'NONE',  ( 0.8759842519685039353, 0.1787899950787401882, 1.764271653489543290 ) ) ;
#44634=CARTESIAN_POINT ( 'NONE',  ( 1.002407869896990045, -0.1264236179284866091, 0.2534448818360003908 ) ) ;
#44636=CARTESIAN_POINT ( 'NONE',  ( 0.7185039370078739607, 1.928577636452523993E-17, 1.161417322727118284 ) ) ;
#44637=CARTESIAN_POINT ( 'NONE',  ( 1.033464566929133799, 0.000000000000000000, 1.899606299212598604 ) ) ;
#44640=CARTESIAN_POINT ( 'NONE',  ( 0.8107537697050254399, -0.1574803149606297803, 0.5388779526483779003 ) ) ;
#44641=CARTESIAN_POINT ( 'NONE',  ( 1.054774247047244096, 0.000000000000000000, 1.242618110182456714 ) ) ;
#44644=CARTESIAN_POINT ( 'NONE',  ( 0.9873396505805591694, -0.1113553986120547346, 0.6249999998924724576 ) ) ;
#44645=ORIENTED_EDGE ( 'NONE', *, *, #220, .T. ) ;
#44646=CARTESIAN_POINT ( 'NONE',  ( -1.033464566929134687, 0.06523048226347956391, 1.744586614173228245 ) ) ;
#44652=CARTESIAN_POINT ( 'NONE',  ( 1.054774247047244540, 0.07405724077823318263, 1.560039370024977057 ) ) ;
#44653=CARTESIAN_POINT ( 'NONE',  ( -0.7185039370078746268, 0.06523048226347956391, 1.286909448818898127 ) ) ;
#44654=CARTESIAN_POINT ( 'NONE',  ( 1.033464566929133799, 0.000000000000000000, 0.5610236220472440971 ) ) ;
#44660=EDGE_LOOP ( 'NONE', ( #2353, #26004, #15939, #1286 ) ) ;
#44662=ORIENTED_EDGE ( 'NONE', *, *, #911, .F. ) ;
#44663=CARTESIAN_POINT ( 'NONE',  ( 0.7495606340400177148, 0.1264236179284866091, 0.6717519684501732646 ) ) ;
#44664=EDGE_CURVE ( 'NONE', #27388, #2356, #17577, .T. ) ;
#44665=CARTESIAN_POINT ( 'NONE',  ( -1.002407869896990045, -0.1264236179284866091, 1.552657480261196765 ) ) ;
#44667=CARTESIAN_POINT ( 'NONE',  ( -0.9500414927467378812, -0.1787899950787401604, 1.240157480261197431 ) ) ;
#44668=EDGE_CURVE ( 'NONE', #46488, #8568, #22464, .T. ) ;
#44671=CARTESIAN_POINT ( 'NONE',  ( -1.002407869896990045, -0.1264236179284866091, 0.3371062991588349989 ) ) ;
#44672=CARTESIAN_POINT ( 'NONE',  ( 0.9873396505805591694, -0.1113553986120547346, 0.6742125984251968740 ) ) ;
#44673=CARTESIAN_POINT ( 'NONE',  ( -0.8759842519685039353, -0.1574803149606299191, 1.879921259734992134 ) ) ;
#44678=CARTESIAN_POINT ( 'NONE',  ( 0.8759842519685039353, -0.1787899950787401882, 1.035925196796629866 ) ) ;
#44682=CARTESIAN_POINT ( 'NONE',  ( 0.8759842519685039353, 0.1574803149606299191, 1.427165354223181248 ) ) ;
#44683=CARTESIAN_POINT ( 'NONE',  ( -0.8019270111902716547, 0.1787899950787401604, 0.1574803149068664809 ) ) ;
#44684=CARTESIAN_POINT ( 'NONE',  ( -0.7185039370078746268, -0.06523048226347956391, 0.8981299212598431447 ) ) ;
#44688=CARTESIAN_POINT ( 'NONE',  ( 0.8759842519685039353, 0.000000000000000000, 4.498031496062992574 ) ) ;
#44689=CARTESIAN_POINT ( 'NONE',  ( -1.033464566929134687, 0.06523048226347956391, 1.498523621939716444 ) ) ;
#44691=CARTESIAN_POINT ( 'NONE',  ( 1.002407869896990045, -0.1264236179284866091, 0.8882874015210394658 ) ) ;
#44692=CARTESIAN_POINT ( 'NONE',  ( 1.033464566929134687, 0.06523048226347956391, 0.5142716534357801850 ) ) ;
#44693=CARTESIAN_POINT ( 'NONE',  ( 0.8107537697050253289, -0.1574803149606297803, 1.414862204724410377 ) ) ;
#44694=CARTESIAN_POINT ( 'NONE',  ( 0.7114281668690185523, 0.01826851868682138544, 1.982933749348845032 ) ) ;
#44696=CARTESIAN_POINT ( 'NONE',  ( 0.9412147342319837628, -0.1574803149606297803, 1.724901574695621775 ) ) ;
#44697=( BOUNDED_CURVE ( )  B_SPLINE_CURVE ( 2, ( #41103, #208, #37346, #4047, #11494, #29745, #11741, #3588, #40223 ),
 .UNSPECIFIED., .F., .T. ) 
 B_SPLINE_CURVE_WITH_KNOTS ( ( 3, 2, 2, 2, 3 ),
 ( 0.3699999999999999956, 0.3724999999999999978, 0.3750000000000000000, 0.3775000000000000022, 0.3800000000000000044 ),
 .UNSPECIFIED. ) 
 CURVE ( )  GEOMETRIC_REPRESENTATION_ITEM ( )  RATIONAL_B_SPLINE_CURVE ( ( 1.000000000000000000, 0.9238795325112869605, 1.000000000000000000, 0.9238795325112869605, 1.000000000000000000, 0.9238795325112869605, 1.000000000000000000, 0.9238795325112869605, 1.000000000000000000 ) ) 
 REPRESENTATION_ITEM ( '' )  ) ;
#44699=CARTESIAN_POINT ( 'NONE',  ( 0.8019270111902716547, -0.1787899950787401604, 0.7972440944344248992 ) ) ;
#44700=CARTESIAN_POINT ( 'NONE',  ( 0.8759842519685039353, 0.1787899950787401882, 1.808562992072220377 ) ) ;
#44702=ORIENTED_EDGE ( 'NONE', *, *, #37998, .F. ) ;
#44703=CARTESIAN_POINT ( 'NONE',  ( -0.7646288533564489232, 0.1113553986120547346, 0.8513779527559054427 ) ) ;
#44705=FACE_OUTER_BOUND ( 'NONE', #8605, .T. ) ;
#44706=CARTESIAN_POINT ( 'NONE',  ( 0.9500414927467378812, -0.1787899950787401604, 1.117125984198206412 ) ) ;
#44708=CARTESIAN_POINT ( 'NONE',  ( -1.033464566929133799, 0.000000000000000000, 1.033464566929133799 ) ) ;
#44711=CARTESIAN_POINT ( 'NONE',  ( -0.6971942568897626646, 0.07405724077823318263, 0.5118110235682844511 ) ) ;
#44712=ORIENTED_EDGE ( 'NONE', *, *, #15948, .T. ) ;
#44715=CARTESIAN_POINT ( 'NONE',  ( -1.054774247047244540, 0.07405724077823318263, 0.2214566928596220785 ) ) ;
#44718=FACE_OUTER_BOUND ( 'NONE', #6115, .T. ) ;
#44721=AXIS2_PLACEMENT_3D ( 'NONE', #12386, #30147, #4431 ) ;
#44723=CARTESIAN_POINT ( 'NONE',  ( 0.7646288533564489232, -0.1113553986120547346, 0.3395669290263311213 ) ) ;
#44724=CARTESIAN_POINT ( 'NONE',  ( -0.8019270111902716547, -0.1787899950787401604, 0.9153543306548987957 ) ) ;
#44725=CARTESIAN_POINT ( 'NONE',  ( -1.054774247047244540, -0.07405724077823318263, 1.122047244040725644 ) ) ;
#44726=CARTESIAN_POINT ( 'NONE',  ( -0.8019270111902717657, 0.1787899950787401604, 0.4724409448281262636 ) ) ;
#44728=CARTESIAN_POINT ( 'NONE',  ( -0.9412147342319837628, -0.1574803149606297803, 0.1599409448818898405 ) ) ;
#44734=DIRECTION ( 'NONE',  ( 0.000000000000000000, 0.000000000000000000, -1.000000000000000000 ) ) ;
#44736=CARTESIAN_POINT ( 'NONE',  ( -0.6971942568897626646, 0.07405724077823318263, 0.2755905511273391006 ) ) ;
#44738=ORIENTED_EDGE ( 'NONE', *, *, #23162, .F. ) ;
#44741=CARTESIAN_POINT ( 'NONE',  ( -1.054774247047244096, 0.000000000000000000, 1.483759842465921075 ) ) ;
#44742=ORIENTED_EDGE ( 'NONE', *, *, #11017, .T. ) ;
#44746=DIRECTION ( 'NONE',  ( 0.000000000000000000, 0.000000000000000000, -1.000000000000000000 ) ) ;
#44750=CARTESIAN_POINT ( 'NONE',  ( -0.9412147342319837628, -0.1574803149606297803, 1.016240157372787722 ) ) ;
#44751=CARTESIAN_POINT ( 'NONE',  ( 0.8759842519685039353, -0.1787899950787401882, 0.05167322829269314910 ) ) ;
#44753=CARTESIAN_POINT ( 'NONE',  ( 1.033464566929133799, 0.000000000000000000, 1.771653543199558811 ) ) ;
#44755=CARTESIAN_POINT ( 'NONE',  ( 0.8107537697050253289, -0.1574803149606297803, 1.956200787294048338 ) ) ;
#44756=ORIENTED_EDGE ( 'NONE', *, *, #15494, .F. ) ;
#44758=CARTESIAN_POINT ( 'NONE',  ( -0.7495606340400177148, -0.1264236179284866091, 0.9178149605761574126 ) ) ;
#44759=CARTESIAN_POINT ( 'NONE',  ( 0.9412147342319837628, 0.1574803149606300301, 1.001476377952755348 ) ) ;
#44763=VERTEX_POINT ( 'NONE', #38973 ) ;
#44766=ORIENTED_EDGE ( 'NONE', *, *, #42126, .F. ) ;
#44767=CARTESIAN_POINT ( 'NONE',  ( -1.033464566929133799, 0.000000000000000000, 1.938976377952756014 ) ) ;
#44772=CARTESIAN_POINT ( 'NONE',  ( 1.033464566929133799, 0.000000000000000000, 1.102362204616881947 ) ) ;
#44774=CYLINDRICAL_SURFACE ( 'NONE', #28337, 0.1574803149606299191 ) ;
#44776=ORIENTED_EDGE ( 'NONE', *, *, #44920, .T. ) ;
#44777=CARTESIAN_POINT ( 'NONE',  ( -1.002407869896990045, 0.1264236179284866091, 1.764271653489543290 ) ) ;
#44778=CARTESIAN_POINT ( 'NONE',  ( -0.7646288533564489232, 0.1113553986120547346, 0.5364173228346457156 ) ) ;
#44780=CARTESIAN_POINT ( 'NONE',  ( 0.6971942568897648851, -0.07405724077823297447, 1.742125984198204858 ) ) ;
#44782=CARTESIAN_POINT ( 'NONE',  ( 0.7185039370078692977, 0.06523048226347515077, 1.473917322727118506 ) ) ;
#44783=CARTESIAN_POINT ( 'NONE',  ( 0.8759842519685039353, -0.1787899950787401882, 0.2928149605761578567 ) ) ;
#44784=CARTESIAN_POINT ( 'NONE',  ( -1.002407869896990045, -0.1264236179284866091, 1.355807086560409491 ) ) ;
#44785=EDGE_CURVE ( 'NONE', #24545, #26852, #27410, .T. ) ;
#44787=CARTESIAN_POINT ( 'NONE',  ( -0.6971942568897637749, 2.189545951927499583E-17, 1.183562992072220599 ) ) ;
#44788=CARTESIAN_POINT ( 'NONE',  ( -1.002407869896990045, 0.1264236179284866091, 0.8932086613635591421 ) ) ;
#44789=DIRECTION ( 'NONE',  ( 0.000000000000000000, 0.000000000000000000, -1.000000000000000000 ) ) ;
#44790=CARTESIAN_POINT ( 'NONE',  ( -1.054774247047244096, 0.000000000000000000, 1.641240157426551161 ) ) ;
#44791=CARTESIAN_POINT ( 'NONE',  ( -0.8759842519685039353, 0.1787899950787401882, 0.03690944876513417572 ) ) ;
#44794=CARTESIAN_POINT ( 'NONE',  ( -1.033464566929133799, 0.000000000000000000, 1.545275590551181244 ) ) ;
#44795=CARTESIAN_POINT ( 'NONE',  ( 0.7185039370078714072, 0.06523048226347728795, 1.641240157480314377 ) ) ;
#44796=CARTESIAN_POINT ( 'NONE',  ( 0.6971942568897637749, 2.189545951927499583E-17, 1.621555118056472455 ) ) ;
#44798=CARTESIAN_POINT ( 'NONE',  ( 1.033464566929134687, 0.06523048226347956391, 0.1993110235145201248 ) ) ;
#44799=CARTESIAN_POINT ( 'NONE',  ( -1.033464566929133799, 0.000000000000000000, 1.781496062992125928 ) ) ;
#44802=ORIENTED_EDGE ( 'NONE', *, *, #5293, .T. ) ;
#44814=CARTESIAN_POINT ( 'NONE',  ( -1.033464566929133799, 0.000000000000000000, 0.1279527559055118058 ) ) ;
#44815=CARTESIAN_POINT ( 'NONE',  ( 1.002407869896990045, -0.1264236179284866091, 0.7258858267178898149 ) ) ;
#44818=CARTESIAN_POINT ( 'NONE',  ( -0.7185039370078714072, 0.06523048226347728795, 1.316437007766489531 ) ) ;
#44819=CARTESIAN_POINT ( 'NONE',  ( 0.8759842519685039353, -0.1787899950787401882, 1.788877952702141672 ) ) ;
#44822=CARTESIAN_POINT ( 'NONE',  ( 0.9873396505805591694, -0.1113553986120547346, 0.1230314960629921295 ) ) ;
#44823=DIRECTION ( 'NONE',  ( -1.000000000000000000, 0.000000000000000000, 0.000000000000000000 ) ) ;
#44827=CARTESIAN_POINT ( 'NONE',  ( 0.6971942568897637749, 2.189545951927499583E-17, 0.2436023621509610382 ) ) ;
#44829=DIRECTION ( 'NONE',  ( 1.822029033848725028E-16, 0.000000000000000000, 1.000000000000000000 ) ) ;
#44830=CARTESIAN_POINT ( 'NONE',  ( -1.054774247047244096, 0.000000000000000000, 1.715059055064346527 ) ) ;
#44832=CARTESIAN_POINT ( 'NONE',  ( -0.6971942568897648851, 0.07405724077823318263, 1.304133858213953667 ) ) ;
#44833=CARTESIAN_POINT ( 'NONE',  ( 0.8759842519685039353, -0.1787899950787401882, 1.237696850339937038 ) ) ;
#44834=CARTESIAN_POINT ( 'NONE',  ( -0.8019270111902717657, 0.1787899950787401604, 0.5511811023084406402 ) ) ;
#44835=CARTESIAN_POINT ( 'NONE',  ( 1.054774247047244096, 0.000000000000000000, 1.911909448765133801 ) ) ;
#44836=CARTESIAN_POINT ( 'NONE',  ( -0.9500414927467378812, -0.1787899950787401604, 1.156496062938362046 ) ) ;
#44837=CARTESIAN_POINT ( 'NONE',  ( -0.8759842519685039353, 0.000000000000000000, 0.000000000000000000 ) ) ;
#44840=CARTESIAN_POINT ( 'NONE',  ( 0.7185039370078746268, 0.06523048226347956391, 1.208169291338584417 ) ) ;
#44841=CARTESIAN_POINT ( 'NONE',  ( 0.8019270111902716547, -0.1787899950787401604, 0.5265748030958428139 ) ) ;
#44842=CARTESIAN_POINT ( 'NONE',  ( -0.8019270111902716547, 0.1787899950787401604, 0.4281496062454490659 ) ) ;
#44843=CARTESIAN_POINT ( 'NONE',  ( -0.8759842519685039353, 0.1787899950787401882, 0.8587598424659212970 ) ) ;
#44844=ORIENTED_EDGE ( 'NONE', *, *, #8070, .T. ) ;
#44847=CARTESIAN_POINT ( 'NONE',  ( -1.033464566929134687, -0.06523048226347956391, 0.1254921259842518844 ) ) ;
#44849=ORIENTED_EDGE ( 'NONE', *, *, #35453, .T. ) ;
#44850=CARTESIAN_POINT ( 'NONE',  ( -0.8759842519685039353, 0.000000000000000000, 1.978346456692913646 ) ) ;
#44851=CARTESIAN_POINT ( 'NONE',  ( -0.8107537697050254399, 0.1574803149606300301, 1.468996062884598830 ) ) ;
#44852=CARTESIAN_POINT ( 'NONE',  ( -0.9500414927467378812, 0.1787899950787401604, 0.06889763774151215492 ) ) ;
#44858=CARTESIAN_POINT ( 'NONE',  ( 0.6971942568897648851, -0.07405724077823297447, 1.343503936954111744 ) ) ;
#44860=EDGE_CURVE ( 'NONE', #26440, #43205, #28950, .T. ) ;
#44862=CARTESIAN_POINT ( 'NONE',  ( 0.6971942568897637749, 2.189545951927499583E-17, 1.656003936954110412 ) ) ;
#44863=CARTESIAN_POINT ( 'NONE',  ( 0.7495606340400177148, 0.1264236179284866091, 0.2337598424659216578 ) ) ;
#44867=CARTESIAN_POINT ( 'NONE',  ( -0.9500414927467377701, 0.1787899950787401604, 0.7037401574265510495 ) ) ;
#44868=DIRECTION ( 'NONE',  ( 0.000000000000000000, 0.000000000000000000, -1.000000000000000000 ) ) ;
#44873=CARTESIAN_POINT ( 'NONE',  ( 0.9500414927467378812, -0.1787899950787401604, 1.358267716481669662 ) ) ;
#44874=CARTESIAN_POINT ( 'NONE',  ( 1.054774247047244096, 0.000000000000000000, 1.911909448765133801 ) ) ;
#44876=CYLINDRICAL_SURFACE ( 'NONE', #769, 0.1574803149606299191 ) ;
#44878=CARTESIAN_POINT ( 'NONE',  ( -0.8759842519685039353, 0.1574803149606299191, 1.515748031496062964 ) ) ;
#44881=CYLINDRICAL_SURFACE ( 'NONE', #43092, 0.1574803149606299191 ) ;
#44883=CARTESIAN_POINT ( 'NONE',  ( 0.8019270111902717657, 0.1787899950787401604, 0.2706692912848194243 ) ) ;
#44884=EDGE_CURVE ( 'NONE', #10815, #19533, #7491, .T. ) ;
#44887=CARTESIAN_POINT ( 'NONE',  ( -1.033464566929134687, 0.06523048226347956391, 0.9473425195775121432 ) ) ;
#44888=CARTESIAN_POINT ( 'NONE',  ( 0.7646288533564489232, 0.1113553986120547346, 0.6840551180027086842 ) ) ;
#44891=CARTESIAN_POINT ( 'NONE',  ( 0.8498898284424959426, 0.1741572742611180169, 0.03937012805171165308 ) ) ;
#44895=CARTESIAN_POINT ( 'NONE',  ( -0.7185039370078739607, 1.928577636452523993E-17, 1.210629921259842590 ) ) ;
#44896=CARTESIAN_POINT ( 'NONE',  ( 0.6971942568897648851, 0.07405724077823318263, 1.535433070812378675 ) ) ;
#44897=CARTESIAN_POINT ( 'NONE',  ( -0.7646288533564489232, 0.1113553986120547346, 1.245078740157480324 ) ) ;
#44899=CARTESIAN_POINT ( 'NONE',  ( -0.7185039370078714072, 0.06523048226347728795, 1.158956692805858779 ) ) ;
#44906=CARTESIAN_POINT ( 'NONE',  ( -0.7495606340400177148, -0.1264236179284866091, 1.542814960576157413 ) ) ;
#44908=CARTESIAN_POINT ( 'NONE',  ( -0.6971942568897648851, -0.07405724077823297447, 1.348425196796630976 ) ) ;
#44911=DIRECTION ( 'NONE',  ( 0.000000000000000000, 0.000000000000000000, -1.000000000000000000 ) ) ;
#44912=CARTESIAN_POINT ( 'NONE',  ( -0.8019270111902717657, -0.1787899950787401604, 0.2903543306548980185 ) ) ;
#44913=CARTESIAN_POINT ( 'NONE',  ( 0.7646288533564489232, -0.1113553986120547346, 0.6643700787401575214 ) ) ;
#44914=CARTESIAN_POINT ( 'NONE',  ( 0.7185039370078739607, 1.928577636452523993E-17, 0.5807086614173228023 ) ) ;
#44916=ORIENTED_EDGE ( 'NONE', *, *, #24552, .F. ) ;
#44919=CARTESIAN_POINT ( 'NONE',  ( -0.8759842519685039353, -0.1574803149606299191, 0.2657480313885358103 ) ) ;
#44920=EDGE_CURVE ( 'NONE', #1283, #42583, #25413, .T. ) ;
#44922=CARTESIAN_POINT ( 'NONE',  ( 0.9412147342319837628, 0.1574803149606300301, 1.818405511703497845 ) ) ;
#44923=CARTESIAN_POINT ( 'NONE',  ( -1.002407869896990045, 0.1264236179284866091, 0.2288385826234019815 ) ) ;
#44924=CARTESIAN_POINT ( 'NONE',  ( -0.8107537697050253289, -0.1574803149606297803, 0.9030511811023627100 ) ) ;
#44927=EDGE_CURVE ( 'NONE', #43250, #44104, #45122, .T. ) ;
#44928=CARTESIAN_POINT ( 'NONE',  ( 1.054774247047244096, 0.000000000000000000, 0.9325787401037164415 ) ) ;
#44929=CARTESIAN_POINT ( 'NONE',  ( 0.8019270111902716547, -0.1787899950787401604, 1.427165354276944687 ) ) ;
#44930=CARTESIAN_POINT ( 'NONE',  ( -0.8107537697050254399, 0.1574803149606300301, 0.4552165354330711677 ) ) ;
#44931=CARTESIAN_POINT ( 'NONE',  ( 0.7185039370078746268, 0.06523048226347956391, 1.641240157480315931 ) ) ;
#44932=CARTESIAN_POINT ( 'NONE',  ( 0.7108616290341307486, -0.02448449591372561102, 1.983713913184816713 ) ) ;
#44939=CARTESIAN_POINT ( 'NONE',  ( 0.7495606340400177148, -0.1264236179284866091, 0.7554133857730077617 ) ) ;
#44941=CARTESIAN_POINT ( 'NONE',  ( 0.6971942568897637749, 2.189545951927499583E-17, 1.857775590497417362 ) ) ;
#44944=CARTESIAN_POINT ( 'NONE',  ( 0.9412147342319837628, 0.1574803149606300301, 0.9227362204724415262 ) ) ;
#44948=CARTESIAN_POINT ( 'NONE',  ( 0.7495606340400177148, 0.1264236179284866091, 1.099901574749385880 ) ) ;
#44950=CYLINDRICAL_SURFACE ( 'NONE', #28792, 0.1574803149606299191 ) ;
#44954=CARTESIAN_POINT ( 'NONE',  ( -0.6971942568897637749, 2.189545951927499583E-17, 0.3174212597887562382 ) ) ;
#44957=CARTESIAN_POINT ( 'NONE',  ( -1.054774247047244096, 0.000000000000000000, 1.833169291284818758 ) ) ;
#44958=CARTESIAN_POINT ( 'NONE',  ( -0.7495606340400177148, -0.1264236179284866091, 0.9128937007336377363 ) ) ;
#44959=CARTESIAN_POINT ( 'NONE',  ( -1.054774247047244540, 0.07405724077823318263, 0.5413385826234012876 ) ) ;
#44962=CARTESIAN_POINT ( 'NONE',  ( -0.7185039370078739607, 1.928577636452523993E-17, 1.919291338582677309 ) ) ;
#44969=CARTESIAN_POINT ( 'NONE',  ( -1.054774247047244540, -0.07405724077823318263, 0.4133858267178901480 ) ) ;
#44970=CARTESIAN_POINT ( 'NONE',  ( -0.8759842519685039353, -0.1574803149606299191, 0.3937007874015748254 ) ) ;
#44971=ORIENTED_EDGE ( 'NONE', *, *, #25577, .F. ) ;
#44973=CARTESIAN_POINT ( 'NONE',  ( -1.002407869896990045, -0.1264236179284866091, 1.518208661363559031 ) ) ;
#44976=( BOUNDED_CURVE ( )  B_SPLINE_CURVE ( 2, ( #15685, #40564, #7754, #8226, #22372, #25981, #22617, #44168, #30545 ),
 .UNSPECIFIED., .F., .F. ) 
 B_SPLINE_CURVE_WITH_KNOTS ( ( 3, 2, 2, 2, 3 ),
 ( 0.1799999999999999933, 0.1824999999999999956, 0.1849999999999999978, 0.1875000000000000000, 0.1900000000000000022 ),
 .UNSPECIFIED. ) 
 CURVE ( )  GEOMETRIC_REPRESENTATION_ITEM ( )  RATIONAL_B_SPLINE_CURVE ( ( 1.000000000000000000, 0.9238795325112869605, 1.000000000000000000, 0.9238795325112869605, 1.000000000000000000, 0.9238795325112869605, 1.000000000000000000, 0.9238795325112869605, 1.000000000000000000 ) ) 
 REPRESENTATION_ITEM ( '' )  ) ;
#44977=( NAMED_UNIT ( * ) SI_UNIT ( $, .STERADIAN. ) SOLID_ANGLE_UNIT ( ) ) ;
#44980=CARTESIAN_POINT ( 'NONE',  ( 1.033464566929133799, 0.000000000000000000, 0.4822834645669291653 ) ) ;
#44982=CARTESIAN_POINT ( 'NONE',  ( -0.8759842519685039353, -0.1574803149606299191, 1.131889763672000004 ) ) ;
#44983=EDGE_CURVE ( 'NONE', #36086, #11894, #8330, .T. ) ;
#44984=CARTESIAN_POINT ( 'NONE',  ( 0.6971942568897626646, -0.07405724077823297447, 0.6003937007336389575 ) ) ;
#44985=CARTESIAN_POINT ( 'NONE',  ( 0.8759842519685039353, -0.1787899950787401882, 0.09104330703285078152 ) ) ;
#44988=CARTESIAN_POINT ( 'NONE',  ( 0.7185039370078746268, -0.06523048226347956391, 1.911909448711371917 ) ) ;
#44991=CARTESIAN_POINT ( 'NONE',  ( 0.8107537697050253289, -0.1574803149606297803, 0.9817913385826764205 ) ) ;
#44992=CARTESIAN_POINT ( 'NONE',  ( -0.8759842519685039353, 0.000000000000000000, 0.000000000000000000 ) ) ;
#44994=VECTOR ( 'NONE', #12205, 39.37007874015748143 ) ;
#44995=CARTESIAN_POINT ( 'NONE',  ( 0.7185039370078739607, 1.928577636452523993E-17, 0.6102362203649134287 ) ) ;
#45001=CARTESIAN_POINT ( 'NONE',  ( 0.8759842519685039353, 0.1787899950787401882, 0.7406496062454487328 ) ) ;
#45004=DIRECTION ( 'NONE',  ( 1.822029033848725028E-16, 0.000000000000000000, 1.000000000000000000 ) ) ;
#45008=CARTESIAN_POINT ( 'NONE',  ( 0.9873396505805591694, -0.1113553986120547346, 1.176181102254677313 ) ) ;
#45009=( BOUNDED_CURVE ( )  B_SPLINE_CURVE ( 2, ( #26250, #34156, #24361, #2535, #20520, #13347, #38959, #17163, #5906 ),
 .UNSPECIFIED., .F., .T. ) 
 B_SPLINE_CURVE_WITH_KNOTS ( ( 3, 2, 2, 2, 3 ),
 ( 0.08000000000000000167, 0.08250000000000000389, 0.08500000000000000611, 0.08749999999999999445, 0.08999999999999999667 ),
 .UNSPECIFIED. ) 
 CURVE ( )  GEOMETRIC_REPRESENTATION_ITEM ( )  RATIONAL_B_SPLINE_CURVE ( ( 1.000000000000000000, 0.9238795325112869605, 1.000000000000000000, 0.9238795325112869605, 1.000000000000000000, 0.9238795325112869605, 1.000000000000000000, 0.9238795325112869605, 1.000000000000000000 ) ) 
 REPRESENTATION_ITEM ( '' )  ) ;
#45010=CARTESIAN_POINT ( 'NONE',  ( 0.7646288533564489232, 0.1113553986120547346, 1.835629921259842590 ) ) ;
#45011=VERTEX_POINT ( 'NONE', #27296 ) ;
#45013=CARTESIAN_POINT ( 'NONE',  ( -1.054774247047244540, -0.07405724077823318263, 1.756889763725764553 ) ) ;
#45014=CARTESIAN_POINT ( 'NONE',  ( 0.8019270111902717657, 0.1787899950787401604, 1.889763779473794258 ) ) ;
#45016=CARTESIAN_POINT ( 'NONE',  ( -0.6971942568897637749, 2.189545951927499583E-17, 0.9128937007336377363 ) ) ;
#45018=CARTESIAN_POINT ( 'NONE',  ( 0.8759842519685039353, -0.1787899950787401882, 0.4896653542769449086 ) ) ;
#45019=CARTESIAN_POINT ( 'NONE',  ( -0.8019270111902717657, -0.1787899950787401604, 1.348425196796630976 ) ) ;
#45020=CARTESIAN_POINT ( 'NONE',  ( -0.7185039370078714072, 0.06523048226347728795, 1.513287401467276583 ) ) ;
#45021=CARTESIAN_POINT ( 'NONE',  ( -1.054774247047244540, -0.07405724077823318263, 1.240157480261197875 ) ) ;
#45022=CARTESIAN_POINT ( 'NONE',  ( -0.7185039370078739607, 0.000000000000000000, -2.869337061179095023E-17 ) ) ;
#45023=CARTESIAN_POINT ( 'NONE',  ( -1.002407869896990045, 0.1264236179284866091, 1.724901574749385880 ) ) ;
#45024=CARTESIAN_POINT ( 'NONE',  ( -1.002407869896990045, 0.1264236179284866091, 0.07135826766277185429 ) ) ;
#45026=CARTESIAN_POINT ( 'NONE',  ( -0.7646288533564489232, 0.1113553986120547346, 1.717519685039369914 ) ) ;
#45028=CARTESIAN_POINT ( 'NONE',  ( 0.7495606340400177148, 0.1264236179284866091, 1.656003936954110412 ) ) ;
#45030=DIRECTION ( 'NONE',  ( 1.822029033848725028E-16, 0.000000000000000000, 1.000000000000000000 ) ) ;
#45032=ORIENTED_EDGE ( 'NONE', *, *, #15224, .F. ) ;
#45035=ADVANCED_FACE ( 'NONE', ( #37324 ), #41845, .T. ) ;
#45038=EDGE_CURVE ( 'NONE', #11471, #22426, #23672, .T. ) ;
#45040=CARTESIAN_POINT ( 'NONE',  ( -0.7185039370078739607, 1.928577636452523993E-17, 1.289370078740157632 ) ) ;
#45041=CARTESIAN_POINT ( 'NONE',  ( 1.054774247047244540, 0.07405724077823318263, 1.835629921206078485 ) ) ;
#45045=CARTESIAN_POINT ( 'NONE',  ( -0.7185039370078739607, 1.928577636452523993E-17, 0.1476377952755905387 ) ) ;
#45046=CARTESIAN_POINT ( 'NONE',  ( 1.002407869896990045, 0.1264236179284866091, 0.8144685038832440993 ) ) ;
#45050=CARTESIAN_POINT ( 'NONE',  ( -0.7646288533564489232, -0.1113553986120547346, 0.06397637784522892945 ) ) ;
#45051=CARTESIAN_POINT ( 'NONE',  ( 0.8759842519685039353, 0.1574803149606299191, 0.08858267705782735257 ) ) ;
#45053=CARTESIAN_POINT ( 'NONE',  ( 1.033464566929133799, 0.000000000000000000, 0.1673228346456692994 ) ) ;
#45059=CARTESIAN_POINT ( 'NONE',  ( 0.9500414927467378812, -0.1787899950787401604, 0.2952755904974176393 ) ) ;
#45060=FACE_OUTER_BOUND ( 'NONE', #17105, .T. ) ;
#45062=CARTESIAN_POINT ( 'NONE',  ( -0.8759842519685039353, -0.1787899950787401882, 1.823326771599779406 ) ) ;
#45063=ORIENTED_EDGE ( 'NONE', *, *, #41927, .T. ) ;
#45064=CARTESIAN_POINT ( 'NONE',  ( -0.8759842519685039353, -0.1787899950787401882, 1.355807086560409491 ) ) ;
#45065=CARTESIAN_POINT ( 'NONE',  ( 0.8759842519685039353, -0.1787899950787401882, 1.316437007820252081 ) ) ;
#45066=CARTESIAN_POINT ( 'NONE',  ( 0.9500414927467378812, -0.1787899950787401604, 0.09842519679663024046 ) ) ;
#45067=CARTESIAN_POINT ( 'NONE',  ( -1.002407869896990045, 0.1264236179284866091, 1.247539370024976391 ) ) ;
#45070=LINE ( 'NONE', #23539, #17034 ) ;
#45071=CARTESIAN_POINT ( 'NONE',  ( 1.054774247047244096, 0.000000000000000000, 0.4207677164816693294 ) ) ;
#45072=CARTESIAN_POINT ( 'NONE',  ( -0.8759842519685039353, -0.1787899950787401882, 0.3272637794737956463 ) ) ;
#45073=CARTESIAN_POINT ( 'NONE',  ( -0.8019270111902717657, 0.1787899950787401604, 0.8612204723871809131 ) ) ;
#45075=DIRECTION ( 'NONE',  ( 1.000000000000000000, 0.000000000000000000, -1.822029033848725275E-16 ) ) ;
#45077=CARTESIAN_POINT ( 'NONE',  ( 0.6971942568897637749, 2.189545951927499583E-17, 0.9128937007336377363 ) ) ;
#45078=CARTESIAN_POINT ( 'NONE',  ( -1.033464566929133799, 0.000000000000000000, 0.2854330708661417804 ) ) ;
#45080=CARTESIAN_POINT ( 'NONE',  ( 0.6971942568897648851, -0.07405724077823297447, 1.230314960576158967 ) ) ;
#45081=CARTESIAN_POINT ( 'NONE',  ( -0.7495606340400177148, 0.1264236179284866091, 1.966043307032850462 ) ) ;
#45084=CARTESIAN_POINT ( 'NONE',  ( 1.033464566929133799, 1.928577636452524610E-17, 4.498031496062992574 ) ) ;
#45086=ORIENTED_EDGE ( 'NONE', *, *, #21480, .T. ) ;
#45089=CARTESIAN_POINT ( 'NONE',  ( -0.7185039370078739607, 0.000000000000000000, -2.869337061179095023E-17 ) ) ;
#45090=ORIENTED_EDGE ( 'NONE', *, *, #10794, .T. ) ;
#45091=EDGE_CURVE ( 'NONE', #35775, #37979, #35645, .T. ) ;
#45094=EDGE_CURVE ( 'NONE', #38209, #13767, #30648, .T. ) ;
#45096=CARTESIAN_POINT ( 'NONE',  ( -0.7185039370078739607, 1.928577636452523993E-17, 1.446850393700787274 ) ) ;
#45097=CARTESIAN_POINT ( 'NONE',  ( 1.002407869896990045, -0.1264236179284866091, 1.552657480261196765 ) ) ;
#45098=CARTESIAN_POINT ( 'NONE',  ( 0.6971942568897626646, 0.07405724077823318263, 0.1968503936470238913 ) ) ;
#45099=EDGE_CURVE ( 'NONE', #13693, #12042, #24023, .T. ) ;
#45102=CARTESIAN_POINT ( 'NONE',  ( -0.8759842519685039353, 0.1574803149606299191, 1.742125984144440975 ) ) ;
#45105=CARTESIAN_POINT ( 'NONE',  ( -1.054774247047244096, 0.000000000000000000, 0.5782480314422993040 ) ) ;
#45110=DIRECTION ( 'NONE',  ( 1.822029033848725028E-16, 0.000000000000000000, 1.000000000000000000 ) ) ;
#45111=CARTESIAN_POINT ( 'NONE',  ( 1.054774247047244540, -0.07405724077823318263, 1.402559055064346971 ) ) ;
#45112=VECTOR ( 'NONE', #112, 39.37007874015748143 ) ;
#45113=CARTESIAN_POINT ( 'NONE',  ( 0.6971942568897637749, 2.189545951927499583E-17, 1.852854330654897685 ) ) ;
#45114=CARTESIAN_POINT ( 'NONE',  ( 1.002407869896990045, 0.1264236179284866091, 0.3026574802611972648 ) ) ;
#45115=ORIENTED_EDGE ( 'NONE', *, *, #20502, .T. ) ;
#45121=CARTESIAN_POINT ( 'NONE',  ( 0.8019270111902717657, 0.1787899950787401604, 0.5068897637257642197 ) ) ;
#45122=( BOUNDED_CURVE ( )  B_SPLINE_CURVE ( 2, ( #37043, #14307, #43511, #29677, #32769, #25326, #7565, #18363, #44442 ),
 .UNSPECIFIED., .F., .T. ) 
 B_SPLINE_CURVE_WITH_KNOTS ( ( 3, 2, 2, 2, 3 ),
 ( 0.4099999999999999756, 0.4124999999999999778, 0.4149999999999999800, 0.4174999999999999822, 0.4199999999999999845 ),
 .UNSPECIFIED. ) 
 CURVE ( )  GEOMETRIC_REPRESENTATION_ITEM ( )  RATIONAL_B_SPLINE_CURVE ( ( 1.000000000000000000, 0.9238795325112879597, 1.000000000000000000, 0.9238795325112869605, 1.000000000000000000, 0.9238795325112869605, 1.000000000000000000, 0.9238795325112869605, 1.000000000000000000 ) ) 
 REPRESENTATION_ITEM ( '' )  ) ;
#45123=CARTESIAN_POINT ( 'NONE',  ( 0.7330905279855389756, -0.08917163514578783923, 0.03937008531791959948 ) ) ;
#45124=CARTESIAN_POINT ( 'NONE',  ( 1.033464566929133799, 0.000000000000000000, 1.968503936900346529 ) ) ;
#45125=CARTESIAN_POINT ( 'NONE',  ( -0.9412147342319837628, 0.1574803149606300301, 1.582185039262551607 ) ) ;
#45126=CARTESIAN_POINT ( 'NONE',  ( 0.9412147342319837628, 0.1574803149606300301, 0.7947834644594014009 ) ) ;
#45127=ORIENTED_EDGE ( 'NONE', *, *, #4623, .F. ) ;
#45131=CARTESIAN_POINT ( 'NONE',  ( -0.8759842519685039353, 0.1574803149606299191, 0.6003937006798740761 ) ) ;
#45132=CARTESIAN_POINT ( 'NONE',  ( -1.033464566929133799, 0.000000000000000000, 1.230314960629921295 ) ) ;
#45133=CARTESIAN_POINT ( 'NONE',  ( 1.002407869896990045, -0.1264236179284866091, 1.631397637741511808 ) ) ;
#45134=CARTESIAN_POINT ( 'NONE',  ( -0.7185039370078739607, 1.928577636452523993E-17, 1.289370078740157632 ) ) ;
#45136=CARTESIAN_POINT ( 'NONE',  ( -1.033464566929133799, 0.000000000000000000, 0.7185039370078739607 ) ) ;
#45137=CARTESIAN_POINT ( 'NONE',  ( -0.9873396505805591694, -0.1113553986120547346, 0.4379921259842519676 ) ) ;
#45138=CARTESIAN_POINT ( 'NONE',  ( 1.033464566929134687, 0.06523048226347956391, 0.3567913384751500994 ) ) ;
#45139=CARTESIAN_POINT ( 'NONE',  ( 1.033464566929134687, -0.06523048226347956391, 1.375492125876724980 ) ) ;
#45144=CARTESIAN_POINT ( 'NONE',  ( -0.8019270111902716547, -0.1787899950787401604, 1.584645669237574994 ) ) ;
#45146=CARTESIAN_POINT ( 'NONE',  ( -1.002407869896990045, 0.1264236179284866091, 1.213090551127338435 ) ) ;
#45149=CARTESIAN_POINT ( 'NONE',  ( 0.8759842519685039353, 0.000000000000000000, 4.498031496062992574 ) ) ;
#45150=CARTESIAN_POINT ( 'NONE',  ( -0.8019270111902717657, 0.1787899950787401604, 0.2755905511273391006 ) ) ;
#45154=VERTEX_POINT ( 'NONE', #35174 ) ;
#45157=CARTESIAN_POINT ( 'NONE',  ( -0.7185039370078739607, 1.928577636452523993E-17, 1.397637795168062969 ) ) ;
#45159=EDGE_CURVE ( 'NONE', #36569, #8914, #25580, .T. ) ;
#45162=CARTESIAN_POINT ( 'NONE',  ( -0.8759842519685039353, -0.1787899950787401882, 0.1353346456155279653 ) ) ;
#45163=CARTESIAN_POINT ( 'NONE',  ( -0.7185039370078746268, -0.06523048226347956391, 0.9374999999999991118 ) ) ;
#45166=CARTESIAN_POINT ( 'NONE',  ( 1.033464566929133799, 0.000000000000000000, 1.112204724409448842 ) ) ;
#45167=CARTESIAN_POINT ( 'NONE',  ( 0.9500414927467378812, -0.1787899950787401604, 0.9251968503399374821 ) ) ;
#45168=CARTESIAN_POINT ( 'NONE',  ( 0.9500414927467377701, 0.1787899950787401604, 1.407480314906865981 ) ) ;
#45170=FACE_OUTER_BOUND ( 'NONE', #3353, .T. ) ;
#45171=CARTESIAN_POINT ( 'NONE',  ( 0.8759842519685039353, -0.1574803149606299191, 1.496062992125984259 ) ) ;
#45172=CARTESIAN_POINT ( 'NONE',  ( 0.7199145177299522969, -0.06352406682034270058, 1.984478708794018775 ) ) ;
#45174=AXIS2_PLACEMENT_3D ( 'NONE', #7559, #44209, #11410 ) ;
#45176=CARTESIAN_POINT ( 'NONE',  ( -0.8759842519685039353, 0.1574803149606299191, 1.624015747923968522 ) ) ;
#45178=CARTESIAN_POINT ( 'NONE',  ( 0.8759842519685039353, -0.1787899950787401882, 1.035925196796629866 ) ) ;
#45179=CARTESIAN_POINT ( 'NONE',  ( 1.054774247047244540, 0.07405724077823318263, 1.879921259788756016 ) ) ;
#45181=CARTESIAN_POINT ( 'NONE',  ( 0.7185039370078746268, 0.06523048226347956391, 0.4109251967428667052 ) ) ;
#45183=CARTESIAN_POINT ( 'NONE',  ( -0.7185039370078739607, 1.928577636452523993E-17, 0.8070866140657008136 ) ) ;
#45184=CARTESIAN_POINT ( 'NONE',  ( 1.033464566929134687, -0.06523048226347956391, 1.897145669291339543 ) ) ;
#45186=CARTESIAN_POINT ( 'NONE',  ( -0.8107537697050253289, 0.1574803149606300301, 0.1304133857192446289 ) ) ;
#45188=CARTESIAN_POINT ( 'NONE',  ( 1.002407869896990045, -0.1264236179284866091, 1.119586614119464585 ) ) ;
#45192=CARTESIAN_POINT ( 'NONE',  ( -1.054774247047244540, -0.07405724077823318263, 0.5314960629383620461 ) ) ;
#45193=CARTESIAN_POINT ( 'NONE',  ( -0.7646288533564489232, -0.1113553986120547346, 0.2706692913385826960 ) ) ;
#45194=CARTESIAN_POINT ( 'NONE',  ( -0.8019270111902717657, -0.1787899950787401604, 0.2854330708123783422 ) ) ;
#45198=CARTESIAN_POINT ( 'NONE',  ( -0.7495606340400177148, 0.1264236179284866091, 1.769192913332062966 ) ) ;
#45199=CARTESIAN_POINT ( 'NONE',  ( -1.002407869896990045, 0.1264236179284866091, 1.011318897584031484 ) ) ;
#45200=CARTESIAN_POINT ( 'NONE',  ( -0.6971942568897637749, 2.189545951927499583E-17, 0.5191929133320630774 ) ) ;
#45201=CARTESIAN_POINT ( 'NONE',  ( -0.7185039370078746268, 0.06523048226347956391, 1.680610236220472009 ) ) ;
#45205=DIRECTION ( 'NONE',  ( -0.8660254037844389297, 0.000000000000000000, -0.4999999999999994449 ) ) ;
#45209=CARTESIAN_POINT ( 'NONE',  ( -0.7646288533564489232, -0.1113553986120547346, 1.166338582569637961 ) ) ;
#45210=CARTESIAN_POINT ( 'NONE',  ( -0.8759842519685039353, -0.1787899950787401882, 0.4847440944344252323 ) ) ;
#45211=CARTESIAN_POINT ( 'NONE',  ( -0.7185039370078739607, 1.928577636452523993E-17, 0.3838582677165354173 ) ) ;
#45217=CARTESIAN_POINT ( 'NONE',  ( 0.9873396505805591694, -0.1113553986120547346, 0.2017716535433070890 ) ) ;
#45218=CARTESIAN_POINT ( 'NONE',  ( 0.9412147342319837628, 0.1574803149606300301, 0.9621062992125994917 ) ) ;
#45219=CARTESIAN_POINT ( 'NONE',  ( 0.9412147342319837628, -0.1574803149606297803, 0.5142716535433068392 ) ) ;
#45221=CARTESIAN_POINT ( 'NONE',  ( -0.9873396505805591694, -0.1113553986120547346, 1.294291338475149544 ) ) ;
#45222=CARTESIAN_POINT ( 'NONE',  ( 1.002407869896990045, 0.1264236179284866091, 0.5044291338045039375 ) ) ;
#45223=CARTESIAN_POINT ( 'NONE',  ( 1.054774247047244540, 0.07405724077823318263, 0.06397637789899228433 ) ) ;
#45225=CYLINDRICAL_SURFACE ( 'NONE', #41531, 0.1574803149606299191 ) ;
#45229=CARTESIAN_POINT ( 'NONE',  ( -0.7495606340400177148, -0.1264236179284866091, 1.075295275536787276 ) ) ;
#45230=CARTESIAN_POINT ( 'NONE',  ( 0.8759842519685039353, 0.1574803149606299191, 1.082677165354330784 ) ) ;
#45231=CARTESIAN_POINT ( 'NONE',  ( -0.9251144371765599450, -0.1690582487949516266, 1.989066791630040187 ) ) ;
#45234=CARTESIAN_POINT ( 'NONE',  ( 0.7185039370078739607, 1.928577636452523993E-17, 0.5708661416247566844 ) ) ;
#45235=CARTESIAN_POINT ( 'NONE',  ( -0.8759842519685039353, 0.000000000000000000, 0.000000000000000000 ) ) ;
#45236=CARTESIAN_POINT ( 'NONE',  ( 1.033464566929134909, 0.06523048226347841205, 0.5930118109160948947 ) ) ;
#45239=ORIENTED_EDGE ( 'NONE', *, *, #3841, .F. ) ;
#45243=CARTESIAN_POINT ( 'NONE',  ( -0.9412147342319837628, 0.1574803149606300301, 1.119586614173229577 ) ) ;
#45244=ORIENTED_EDGE ( 'NONE', *, *, #17416, .T. ) ;
#45251=CARTESIAN_POINT ( 'NONE',  ( 0.7185039370078746268, 0.06523048226347956391, 1.119586614065702035 ) ) ;
#45254=ORIENTED_EDGE ( 'NONE', *, *, #1719, .F. ) ;
#45255=CARTESIAN_POINT ( 'NONE',  ( -0.9500414927467378812, 0.1787899950787401604, 1.727362204670645385 ) ) ;
#45256=CARTESIAN_POINT ( 'NONE',  ( 0.6971942568897648851, 0.07405724077823318263, 1.815944881835999558 ) ) ;
#45258=DIRECTION ( 'NONE',  ( -1.000000000000000000, 0.000000000000000000, 0.000000000000000000 ) ) ;
#45259=CARTESIAN_POINT ( 'NONE',  ( 0.8759842519685039353, 0.1787899950787401882, 0.4699803149068661479 ) ) ;
#45260=CARTESIAN_POINT ( 'NONE',  ( -0.8019270111902717657, -0.1787899950787401604, 1.427165354276944687 ) ) ;
#45262=CARTESIAN_POINT ( 'NONE',  ( -0.6971942568897648851, -0.07405724077823297447, 1.343503936954111966 ) ) ;
#45263=CARTESIAN_POINT ( 'NONE',  ( -0.7495606340400177148, -0.1264236179284866091, 0.7947834645131652831 ) ) ;
#45264=CARTESIAN_POINT ( 'NONE',  ( -0.6971942568897626646, -0.07405724077823297447, 0.08858267711159097113 ) ) ;
#45266=CARTESIAN_POINT ( 'NONE',  ( -0.9500414927467378812, 0.1787899950787401604, 1.727362204670645385 ) ) ;
#45267=CARTESIAN_POINT ( 'NONE',  ( -0.7185039370078746268, 0.06523048226347956391, 1.985728346349167950 ) ) ;
#45268=CARTESIAN_POINT ( 'NONE',  ( -0.7185039370078746268, -0.06523048226347956391, 1.685531496062990797 ) ) ;
#45269=CYLINDRICAL_SURFACE ( 'NONE', #41917, 0.1574803149606299191 ) ;
#45271=CARTESIAN_POINT ( 'NONE',  ( 0.7495606340400177148, 0.1264236179284866091, 1.616633858213952779 ) ) ;
#45274=( BOUNDED_CURVE ( )  B_SPLINE_CURVE ( 2, ( #41207, #23041, #23287, #37659, #45301, #5291, #23527, #37900, #34317 ),
 .UNSPECIFIED., .F., .T. ) 
 B_SPLINE_CURVE_WITH_KNOTS ( ( 3, 2, 2, 2, 3 ),
 ( 0.05000000000000000278, 0.05249999999999999806, 0.05500000000000000028, 0.05750000000000000250, 0.05999999999999999778 ),
 .UNSPECIFIED. ) 
 CURVE ( )  GEOMETRIC_REPRESENTATION_ITEM ( )  RATIONAL_B_SPLINE_CURVE ( ( 1.000000000000000000, 0.9238795325112859613, 1.000000000000000000, 0.9238795325112869605, 1.000000000000000000, 0.9238795325112869605, 1.000000000000000000, 0.9238795325112869605, 1.000000000000000000 ) ) 
 REPRESENTATION_ITEM ( '' )  ) ;
#45278=ORIENTED_EDGE ( 'NONE', *, *, #25337, .F. ) ;
#45281=EDGE_CURVE ( 'NONE', #4590, #11117, #2785, .T. ) ;
#45284=EDGE_CURVE ( 'NONE', #22900, #110, #17411, .T. ) ;
#45287=CARTESIAN_POINT ( 'NONE',  ( 0.8759842519685039353, -0.1787899950787401882, 1.823326771599779406 ) ) ;
#45289=CARTESIAN_POINT ( 'NONE',  ( -0.8107537697050253289, 0.1574803149606300301, 0.7997047243019228535 ) ) ;
#45292=CARTESIAN_POINT ( 'NONE',  ( 0.8759842519685039353, 0.1787899950787401882, 0.9374999999462362288 ) ) ;
#45293=( BOUNDED_CURVE ( )  B_SPLINE_CURVE ( 2, ( #11641, #12355, #578, #5129, #8259, #41061, #30122, #4178, #29881 ),
 .UNSPECIFIED., .F., .F. ) 
 B_SPLINE_CURVE_WITH_KNOTS ( ( 3, 2, 2, 2, 3 ),
 ( 0.9499999999999999556, 0.9525000000000000133, 0.9549999999999999600, 0.9575000000000000178, 0.9599999999999999645 ),
 .UNSPECIFIED. ) 
 CURVE ( )  GEOMETRIC_REPRESENTATION_ITEM ( )  RATIONAL_B_SPLINE_CURVE ( ( 1.000000000000000000, 0.9238795325112939549, 1.000000000000000000, 0.9238795325112869605, 1.000000000000000000, 0.9238795325112869605, 1.000000000000000000, 0.9238795325112869605, 1.000000000000000000 ) ) 
 REPRESENTATION_ITEM ( '' )  ) ;
#45294=CARTESIAN_POINT ( 'NONE',  ( -1.002407869896990045, -0.1264236179284866091, 1.990649606245448844 ) ) ;
#45296=CARTESIAN_POINT ( 'NONE',  ( 0.8759842519685039353, -0.1787899950787401882, 1.906988188922614125 ) ) ;
#45298=CARTESIAN_POINT ( 'NONE',  ( 0.7646288533564489232, 0.1113553986120547346, 0.1820866141732283561 ) ) ;
#45299=CARTESIAN_POINT ( 'NONE',  ( 0.7185039370078739607, 0.000000000000000000, 4.498031496062992574 ) ) ;
#45301=CARTESIAN_POINT ( 'NONE',  ( 0.8759842519685039353, -0.1574803149606299191, 0.1181102362204724532 ) ) ;
#45304=CARTESIAN_POINT ( 'NONE',  ( -1.054774247047244096, 0.000000000000000000, 1.754429133804503715 ) ) ;
#45306=CARTESIAN_POINT ( 'NONE',  ( -0.8019270111902717657, -0.1787899950787401604, 1.274606299158834277 ) ) ;
#45308=CARTESIAN_POINT ( 'NONE',  ( -0.6971942568897626646, -0.07405724077823297447, 0.5610236219934807700 ) ) ;
#45311=CARTESIAN_POINT ( 'NONE',  ( -1.054774247047244096, 0.000000000000000000, 1.203248031442299304 ) ) ;
#45313=DIRECTION ( 'NONE',  ( 1.822029033848725028E-16, 0.000000000000000000, 1.000000000000000000 ) ) ;
#45316=CARTESIAN_POINT ( 'NONE',  ( 1.054774247047244540, -0.07405724077823318263, 0.5757874015210393548 ) ) ;
#45317=CARTESIAN_POINT ( 'NONE',  ( -0.9500414927467377701, -0.1787899950787401604, 0.4478346456155276045 ) ) ;
#45320=EDGE_CURVE ( 'NONE', #19846, #41516, #42037, .T. ) ;
#45321=ORIENTED_EDGE ( 'NONE', *, *, #5759, .T. ) ;
#45322=CARTESIAN_POINT ( 'NONE',  ( -1.033464566929134687, -0.06523048226347956391, 0.2436023622047244763 ) ) ;
#45324=CARTESIAN_POINT ( 'NONE',  ( 1.002407869896990045, 0.1264236179284866091, 1.134350393647023614 ) ) ;
#45325=CARTESIAN_POINT ( 'NONE',  ( 0.8759842519685039353, 0.1574803149606299191, 1.309055118002708573 ) ) ;
#45327=CARTESIAN_POINT ( 'NONE',  ( -1.002407869896990045, 0.1264236179284866091, 0.9374999999462362288 ) ) ;
#45329=CARTESIAN_POINT ( 'NONE',  ( -0.9873396505805591694, -0.1113553986120547346, 0.2017716535433070890 ) ) ;
#45331=ORIENTED_EDGE ( 'NONE', *, *, #39963, .F. ) ;
#45336=PRODUCT_DEFINITION ( 'UNKNOWN', '', #35466, #44144 ) ;
#45338=CARTESIAN_POINT ( 'NONE',  ( -0.8759842519685039353, 0.000000000000000000, 0.000000000000000000 ) ) ;
#45342=CARTESIAN_POINT ( 'NONE',  ( 0.7495606340400177148, -0.1264236179284866091, 1.582185039316315045 ) ) ;
#45347=CARTESIAN_POINT ( 'NONE',  ( 1.054774247047244096, 0.000000000000000000, 0.5339566928596221063 ) ) ;
#45348=CARTESIAN_POINT ( 'NONE',  ( -0.6971942568897637749, 2.189545951927499583E-17, 0.6373031495525354195 ) ) ;
#45350=CARTESIAN_POINT ( 'NONE',  ( -1.033464566929133799, 1.928577636452524610E-17, 2.869337061179095023E-17 ) ) ;
#45355=CARTESIAN_POINT ( 'NONE',  ( 0.9500414927467378812, 0.1787899950787401604, 1.530511810969859443 ) ) ;
#45356=CARTESIAN_POINT ( 'NONE',  ( 0.6971942568897648851, -0.07405724077823297447, 1.815944881835999780 ) ) ;
#45357=CYLINDRICAL_SURFACE ( 'NONE', #11516, 0.1574803149606299191 ) ;
#45360=CARTESIAN_POINT ( 'NONE',  ( 0.8759842519685039353, 0.000000000000000000, 4.498031496062992574 ) ) ;
#45363=CARTESIAN_POINT ( 'NONE',  ( -1.033464566929134687, 0.06523048226347956391, 0.1697834645669291653 ) ) ;
#45364=CARTESIAN_POINT ( 'NONE',  ( 0.9500414927467378812, 0.1787899950787401604, 0.4232283464029293896 ) ) ;
#45365=CARTESIAN_POINT ( 'NONE',  ( 0.8215752181199765802, -0.1517888380884206134, 0.03937426606394420214 ) ) ;
#45366=CARTESIAN_POINT ( 'NONE',  ( 0.7185039370078778465, -0.06523048226348396317, 1.951279527451527329 ) ) ;
#45368=CARTESIAN_POINT ( 'NONE',  ( -1.054774247047244540, -0.07405724077823318263, 1.358267716481669662 ) ) ;
#45369=CARTESIAN_POINT ( 'NONE',  ( 1.033464566929133799, 0.000000000000000000, 0.8267716534357796299 ) ) ;
#45371=CARTESIAN_POINT ( 'NONE',  ( -0.9500414927467378812, -0.1787899950787401604, 1.082677165300567346 ) ) ;
#45372=DIRECTION ( 'NONE',  ( 1.822029033848725028E-16, 0.000000000000000000, 1.000000000000000000 ) ) ;
#45373=CARTESIAN_POINT ( 'NONE',  ( 1.002407869896990045, 0.1264236179284866091, 1.055610236166708793 ) ) ;
#45376=CARTESIAN_POINT ( 'NONE',  ( -1.033464566929134687, -0.06523048226347956391, 0.5487204723334181411 ) ) ;
#45377=CARTESIAN_POINT ( 'NONE',  ( -0.7646288533564489232, -0.1113553986120547346, 1.215551181102362266 ) ) ;
#45378=CARTESIAN_POINT ( 'NONE',  ( 0.7495606340400177148, 0.1264236179284866091, 1.729822834591905556 ) ) ;
#45379=CARTESIAN_POINT ( 'NONE',  ( -0.9873396505805591694, 0.1113553986120547346, 1.313976377952756014 ) ) ;
#45381=CARTESIAN_POINT ( 'NONE',  ( 1.033464566929134687, 0.06523048226347956391, 0.5634842519685042683 ) ) ;
#45383=CARTESIAN_POINT ( 'NONE',  ( 1.054774247047244540, -0.07405724077823318263, 0.06397637789899228433 ) ) ;
#45384=CARTESIAN_POINT ( 'NONE',  ( 0.7185039370078746268, -0.06523048226347956391, 1.439468503829481216 ) ) ;
#45388=VERTEX_POINT ( 'NONE', #21731 ) ;
#45390=CARTESIAN_POINT ( 'NONE',  ( -1.002407869896990045, -0.1264236179284866091, 1.513287401521039355 ) ) ;
#45392=CARTESIAN_POINT ( 'NONE',  ( -0.9500414927467378812, -0.1787899950787401604, 1.476377952702141449 ) ) ;
#45402=EDGE_LOOP ( 'NONE', ( #44702, #30018, #37862, #38950 ) ) ;
#45404=CARTESIAN_POINT ( 'NONE',  ( -0.7185039370078746268, -0.06523048226347956391, 1.203248031388535200 ) ) ;
#45406=CARTESIAN_POINT ( 'NONE',  ( 0.8107537697050253289, -0.1574803149606297803, 1.769192913385826404 ) ) ;
#45409=CARTESIAN_POINT ( 'NONE',  ( -1.054774247047244540, 0.07405724077823318263, 0.1870078739619845110 ) ) ;
#45410=CARTESIAN_POINT ( 'NONE',  ( -1.033464566929134687, -0.06523048226347956391, 1.031003937007875182 ) ) ;
#45413=CARTESIAN_POINT ( 'NONE',  ( 0.6971942568897637749, 2.189545951927499583E-17, 1.031003936954110189 ) ) ;
#45414=FACE_OUTER_BOUND ( 'NONE', #29899, .T. ) ;
#45415=CARTESIAN_POINT ( 'NONE',  ( 0.8107537697050253289, 0.1574803149606300301, 1.518208661417322469 ) ) ;
#45416=CARTESIAN_POINT ( 'NONE',  ( 0.9873396505805591694, -0.1113553986120547346, 1.422244094488188892 ) ) ;
#45417=DIRECTION ( 'NONE',  ( 0.000000000000000000, 0.000000000000000000, -1.000000000000000000 ) ) ;
#45419=CARTESIAN_POINT ( 'NONE',  ( 1.054774247047244096, 0.000000000000000000, 1.006397637741511808 ) ) ;
#45420=CARTESIAN_POINT ( 'NONE',  ( 0.8759842519685039353, 0.1787899950787401882, 1.887303149552535420 ) ) ;
#45421=CARTESIAN_POINT ( 'NONE',  ( 0.8107537697050234415, -0.1574803149606297803, 0.3420275589475912925 ) ) ;
#45422=EDGE_LOOP ( 'NONE', ( #24122, #8851, #19353, #12334 ) ) ;
#45423=CARTESIAN_POINT ( 'NONE',  ( 0.8759842519685039353, -0.1574803149606299191, 1.249999999892472236 ) ) ;
#45426=CARTESIAN_POINT ( 'NONE',  ( -0.7646288533564489232, 0.1113553986120547346, 0.2509842518609771700 ) ) ;
#45427=CARTESIAN_POINT ( 'NONE',  ( 1.002407869896990045, 0.1264236179284866091, 1.326279527505291433 ) ) ;
#45428=CARTESIAN_POINT ( 'NONE',  ( 1.033464566929133799, 0.000000000000000000, 1.417322834538141674 ) ) ;
#45430=DIRECTION ( 'NONE',  ( 1.822029033848725028E-16, 0.000000000000000000, 1.000000000000000000 ) ) ;
#45431=EDGE_CURVE ( 'NONE', #35669, #1467, #6857, .T. ) ;
#45432=CARTESIAN_POINT ( 'NONE',  ( -1.002407869896990045, 0.1264236179284866091, 0.6176181101824566033 ) ) ;
#45435=ORIENTED_EDGE ( 'NONE', *, *, #26379, .T. ) ;
#45439=CARTESIAN_POINT ( 'NONE',  ( -0.9500414927467378812, -0.1787899950787401604, 0.5314960629383620461 ) ) ;
#45440=ORIENTED_EDGE ( 'NONE', *, *, #23441, .F. ) ;
#45445=CARTESIAN_POINT ( 'NONE',  ( 0.8759842519685039353, -0.1574803149606299191, 0.4724409448818898127 ) ) ;
#45448=CARTESIAN_POINT ( 'NONE',  ( -0.7495606340400177148, -0.1264236179284866091, 0.4798228345919055560 ) ) ;
#45449=DIRECTION ( 'NONE',  ( 1.822029033848725028E-16, 0.000000000000000000, 1.000000000000000000 ) ) ;
#45454=CARTESIAN_POINT ( 'NONE',  ( 0.9412147342319837628, 0.1574803149606300301, 1.031003936900347639 ) ) ;
#45457=CARTESIAN_POINT ( 'NONE',  ( 0.8759842519685039353, -0.1574803149606299191, 0.9448818897637796255 ) ) ;
#45458=CARTESIAN_POINT ( 'NONE',  ( -0.8107537697050253289, -0.1574803149606297803, 1.286909448711370585 ) ) ;
#45459=CARTESIAN_POINT ( 'NONE',  ( 0.6971942568897637749, 2.189545951927499583E-17, 0.5979330708123780092 ) ) ;
#45460=CARTESIAN_POINT ( 'NONE',  ( 0.8019270111902716547, -0.1787899950787401604, 0.04921259837143338728 ) ) ;
#45462=FACE_OUTER_BOUND ( 'NONE', #1795, .T. ) ;
#45465=CARTESIAN_POINT ( 'NONE',  ( 0.7185039370078739607, 1.928577636452523993E-17, 1.594488188868850242 ) ) ;
#45466=CARTESIAN_POINT ( 'NONE',  ( -0.8019270111902716547, 0.1787899950787401604, 1.141732283410804349 ) ) ;
#45467=CARTESIAN_POINT ( 'NONE',  ( 0.7185039370078739607, 1.928577636452523993E-17, 1.053149606299212504 ) ) ;
#45468=CARTESIAN_POINT ( 'NONE',  ( -0.9653136480190166457, -0.1535042515562757837, 1.989856082496901601 ) ) ;
#45471=CARTESIAN_POINT ( 'NONE',  ( -0.7185039370078739607, 1.928577636452523993E-17, 1.948818897530267602 ) ) ;
#45475=ORIENTED_EDGE ( 'NONE', *, *, #28240, .T. ) ;
#45476=AXIS2_PLACEMENT_3D ( 'NONE', #44850, #18984, #5080 ) ;
#45477=CARTESIAN_POINT ( 'NONE',  ( 1.054774247047244540, 0.07405724077823318263, 0.6938976377415123631 ) ) ;
#45479=CARTESIAN_POINT ( 'NONE',  ( -0.7185039370078739607, 1.928577636452523993E-17, 1.200787401467275695 ) ) ;
#45487=ORIENTED_EDGE ( 'NONE', *, *, #47008, .F. ) ;
#45488=CARTESIAN_POINT ( 'NONE',  ( -1.002407869896990045, -0.1264236179284866091, 1.951279527505291433 ) ) ;
#45489=CARTESIAN_POINT ( 'NONE',  ( 1.054774247047244540, -0.07405724077823318263, 1.874999999946236784 ) ) ;
#45492=CARTESIAN_POINT ( 'NONE',  ( 0.6971942568897626646, -0.07405724077823297447, 0.4822834645131655606 ) ) ;
#45493=CARTESIAN_POINT ( 'NONE',  ( -0.9500414927467378812, 0.1787899950787401604, 1.368110236166710125 ) ) ;
#45495=EDGE_CURVE ( 'NONE', #39969, #27120, #23391, .T. ) ;
#45496=CARTESIAN_POINT ( 'NONE',  ( -0.9500414927467378812, -0.1787899950787401604, 0.1377952755367876370 ) ) ;
#45499=CARTESIAN_POINT ( 'NONE',  ( -0.8759842519685039353, 0.1787899950787401882, 1.729822834591905556 ) ) ;
#45500=CARTESIAN_POINT ( 'NONE',  ( -1.033464566929134687, -0.06523048226347956391, 2.005413385719245323 ) ) ;
#45501=CARTESIAN_POINT ( 'NONE',  ( 0.7646288533564489232, -0.1113553986120547346, 1.402559055010582645 ) ) ;
#45502=CARTESIAN_POINT ( 'NONE',  ( -0.9412147342319837628, 0.1574803149606300301, 1.749507874015747699 ) ) ;
#45503=DIRECTION ( 'NONE',  ( 1.822029033848725028E-16, 0.000000000000000000, 1.000000000000000000 ) ) ;
#45504=CARTESIAN_POINT ( 'NONE',  ( 1.054774247047244096, 0.000000000000000000, 1.601870078686393750 ) ) ;
#45507=ORIENTED_EDGE ( 'NONE', *, *, #2894, .F. ) ;
#45508=CARTESIAN_POINT ( 'NONE',  ( -0.8759842519685039353, 0.1574803149606299191, 1.791338582677165281 ) ) ;
#45509=EDGE_LOOP ( 'NONE', ( #22160, #4051, #39235, #24959 ) ) ;
#45513=AXIS2_PLACEMENT_3D ( 'NONE', #1962, #39317, #31695 ) ;
#45519=CARTESIAN_POINT ( 'NONE',  ( -0.9412147342319837628, 0.1574803149606300301, 0.8341535431995593664 ) ) ;
#45522=CARTESIAN_POINT ( 'NONE',  ( 0.8759842519685039353, 0.1787899950787401882, 0.8587598424659212970 ) ) ;
#45525=CARTESIAN_POINT ( 'NONE',  ( 1.054774247047244540, 0.07405724077823318263, 1.958661417269071947 ) ) ;
#45527=CARTESIAN_POINT ( 'NONE',  ( 0.9412147342319837628, 0.1574803149606300301, 0.2140748031496061687 ) ) ;
#45532=EDGE_CURVE ( 'NONE', #2118, #22349, #20006, .T. ) ;
#45533=CARTESIAN_POINT ( 'NONE',  ( -1.054774247047244540, -0.07405724077823318263, 1.909448818843873186 ) ) ;
#45535=CARTESIAN_POINT ( 'NONE',  ( -0.7495606340400177148, -0.1264236179284866091, 1.311515747977732405 ) ) ;
#45537=CARTESIAN_POINT ( 'NONE',  ( 0.6971942568897648851, -0.07405724077823297447, 1.466535433017102763 ) ) ;
#45540=CARTESIAN_POINT ( 'NONE',  ( -1.002407869896990045, 0.1264236179284866091, 1.286909448765133801 ) ) ;
#45542=CARTESIAN_POINT ( 'NONE',  ( 0.6971942568897648851, -0.07405724077823297447, 0.6397637794737947026 ) ) ;
#45543=CARTESIAN_POINT ( 'NONE',  ( -0.7495606340400177148, 0.1264236179284866091, 0.4699803149068661479 ) ) ;
#45545=( BOUNDED_CURVE ( )  B_SPLINE_CURVE ( 2, ( #38186, #34609, #15930, #13042, #26957, #35081, #41988, #41509, #1510 ),
 .UNSPECIFIED., .F., .T. ) 
 B_SPLINE_CURVE_WITH_KNOTS ( ( 3, 2, 2, 2, 3 ),
 ( 0.2300000000000000100, 0.2325000000000000122, 0.2349999999999999867, 0.2374999999999999889, 0.2399999999999999911 ),
 .UNSPECIFIED. ) 
 CURVE ( )  GEOMETRIC_REPRESENTATION_ITEM ( )  RATIONAL_B_SPLINE_CURVE ( ( 1.000000000000000000, 0.9238795325112859613, 1.000000000000000000, 0.9238795325112869605, 1.000000000000000000, 0.9238795325112869605, 1.000000000000000000, 0.9238795325112869605, 1.000000000000000000 ) ) 
 REPRESENTATION_ITEM ( '' )  ) ;
#45547=ORIENTED_EDGE ( 'NONE', *, *, #19179, .F. ) ;
#45548=ORIENTED_EDGE ( 'NONE', *, *, #44664, .T. ) ;
#45549=CARTESIAN_POINT ( 'NONE',  ( -0.7185039370078746268, 0.06523048226347956391, 0.2239173228346459099 ) ) ;
#45550=CARTESIAN_POINT ( 'NONE',  ( 1.002407869896990045, -0.1264236179284866091, 1.163877952702141672 ) ) ;
#45553=CARTESIAN_POINT ( 'NONE',  ( -0.8759842519685039353, -0.1574803149606299191, 1.299212598425196985 ) ) ;
#45554=CARTESIAN_POINT ( 'NONE',  ( -0.8019270111902717657, 0.1787899950787401604, 0.1919291338045042428 ) ) ;
#45556=ORIENTED_EDGE ( 'NONE', *, *, #27597, .T. ) ;
#45557=CARTESIAN_POINT ( 'NONE',  ( -0.9873396505805591694, 0.1113553986120547346, 1.382874015640503940 ) ) ;
#45561=CARTESIAN_POINT ( 'NONE',  ( 0.7495606340400177148, 0.1264236179284866091, 1.296751968450173154 ) ) ;
#45564=( BOUNDED_CURVE ( )  B_SPLINE_CURVE ( 2, ( #42273, #35112, #2257, #18059, #36748, #14246, #28888, #29382, #43448 ),
 .UNSPECIFIED., .F., .F. ) 
 B_SPLINE_CURVE_WITH_KNOTS ( ( 3, 2, 2, 2, 3 ),
 ( 0.7900000000000000355, 0.7924999999999999822, 0.7950000000000000400, 0.7974999999999999867, 0.8000000000000000444 ),
 .UNSPECIFIED. ) 
 CURVE ( )  GEOMETRIC_REPRESENTATION_ITEM ( )  RATIONAL_B_SPLINE_CURVE ( ( 1.000000000000000000, 0.9238795325112899581, 1.000000000000000000, 0.9238795325112869605, 1.000000000000000000, 0.9238795325112869605, 1.000000000000000000, 0.9238795325112869605, 1.000000000000000000 ) ) 
 REPRESENTATION_ITEM ( '' )  ) ;
#45566=CYLINDRICAL_SURFACE ( 'NONE', #9623, 0.1574803149606299191 ) ;
#45574=CARTESIAN_POINT ( 'NONE',  ( -1.054774247047244540, -0.07405724077823318263, 0.7332677164816705506 ) ) ;
#45576=LINE ( 'NONE', #45350, #22320 ) ;
#45581=CARTESIAN_POINT ( 'NONE',  ( 0.8759842519685039353, 0.1787899950787401882, 1.493602362150960650 ) ) ;
#45582=CARTESIAN_POINT ( 'NONE',  ( 0.8019270111902716547, -0.1787899950787401604, 1.820866141678520789 ) ) ;
#45583=CARTESIAN_POINT ( 'NONE',  ( 0.8019270111902716547, 0.1787899950787401604, 0.4675196849856070314 ) ) ;
#45589=CYLINDRICAL_SURFACE ( 'NONE', #19053, 0.1574803149606299191 ) ;
#45593=CARTESIAN_POINT ( 'NONE',  ( 1.054774247047244096, 0.000000000000000000, 0.4945866141194645849 ) ) ;
#45595=CARTESIAN_POINT ( 'NONE',  ( -0.8107537697050254399, -0.1574803149606297803, 0.7455708661417325134 ) ) ;
#45597=CARTESIAN_POINT ( 'NONE',  ( -1.054774247047244540, 0.07405724077823318263, 1.284448818843874740 ) ) ;
#45598=CARTESIAN_POINT ( 'NONE',  ( 0.7185039370078746268, -0.06523048226347956391, 0.8489173227271192834 ) ) ;
#45600=DIRECTION ( 'NONE',  ( 1.822029033848725028E-16, 0.000000000000000000, 1.000000000000000000 ) ) ;
#45601=CARTESIAN_POINT ( 'NONE',  ( 0.7495606340400177148, -0.1264236179284866091, 1.075295275536787276 ) ) ;
#45604=CARTESIAN_POINT ( 'NONE',  ( -0.7646288533564489232, -0.1113553986120547346, 0.6151574802074331050 ) ) ;
#45605=CARTESIAN_POINT ( 'NONE',  ( 1.033464566929134687, 0.06523048226347956391, 0.09104330708661413640 ) ) ;
#45606=CARTESIAN_POINT ( 'NONE',  ( -0.8107537697050253289, 0.1574803149606300301, 1.321358267716534751 ) ) ;
#45608=CARTESIAN_POINT ( 'NONE',  ( -0.9873396505805591694, -0.1113553986120547346, 1.058070866034204860 ) ) ;
#45609=FACE_OUTER_BOUND ( 'NONE', #22700, .T. ) ;
#45611=CARTESIAN_POINT ( 'NONE',  ( 0.7495606340400177148, -0.1264236179284866091, 0.1697834645131657827 ) ) ;
#45612=CARTESIAN_POINT ( 'NONE',  ( 0.7185039370078739607, 1.928577636452523993E-17, 1.437007873908220601 ) ) ;
#45613=EDGE_LOOP ( 'NONE', ( #6421, #33174, #45063, #33865 ) ) ;
#45615=DIRECTION ( 'NONE',  ( 1.822029033848725028E-16, 0.000000000000000000, 1.000000000000000000 ) ) ;
#45617=CARTESIAN_POINT ( 'NONE',  ( 1.054774247047244540, 0.07405724077823318263, 0.6988188975840318173 ) ) ;
#45619=ORIENTED_EDGE ( 'NONE', *, *, #8435, .F. ) ;
#45621=CARTESIAN_POINT ( 'NONE',  ( -0.7185039370078746268, 0.06523048226347956391, 0.2534448817822371192 ) ) ;
#45622=CARTESIAN_POINT ( 'NONE',  ( 0.7185039370078714072, 0.06523048226347728795, 1.867618110128693720 ) ) ;
#45623=CARTESIAN_POINT ( 'NONE',  ( -0.9873396505805591694, -0.1113553986120547346, 1.884842519577511810 ) ) ;
#45631=CARTESIAN_POINT ( 'NONE',  ( 0.9873396505805591694, -0.1113553986120547346, 1.894685039370078927 ) ) ;
#45633=EDGE_CURVE ( 'NONE', #47216, #40379, #1319, .T. ) ;
#45635=CARTESIAN_POINT ( 'NONE',  ( -0.8019270111902716547, 0.1787899950787401604, 0.2755905511273391006 ) ) ;
#45636=CARTESIAN_POINT ( 'NONE',  ( -0.8107537697050253289, 0.1574803149606300301, 1.006397637795276800 ) ) ;
#45638=CARTESIAN_POINT ( 'NONE',  ( 0.9873396505805591694, -0.1113553986120547346, 1.107283464566929165 ) ) ;
#45639=CARTESIAN_POINT ( 'NONE',  ( 0.9500414927467378812, 0.1787899950787401604, 1.097440944828127041 ) ) ;
#45640=CARTESIAN_POINT ( 'NONE',  ( 1.054774247047244096, 0.000000000000000000, 0.2189960629383626012 ) ) ;
#45643=CARTESIAN_POINT ( 'NONE',  ( 1.033464566929133799, 0.000000000000000000, 1.624015748031496287 ) ) ;
#45644=CARTESIAN_POINT ( 'NONE',  ( 0.7617962702031515487, 0.1145390712115343795, 1.980802457175323328 ) ) ;
#45650=CARTESIAN_POINT ( 'NONE',  ( 1.054774247047244540, -0.07405724077823318263, 1.043307086560409269 ) ) ;
#45651=CARTESIAN_POINT ( 'NONE',  ( 0.6971942568897648851, -0.07405724077823297447, 1.899606299158834943 ) ) ;
#45652=CARTESIAN_POINT ( 'NONE',  ( 0.7185039370078746268, 0.06523048226347956391, 0.3321850392625518844 ) ) ;
#45653=ORIENTED_EDGE ( 'NONE', *, *, #11713, .T. ) ;
#45656=CARTESIAN_POINT ( 'NONE',  ( -0.7185039370078739607, 1.928577636452523993E-17, 0.1771653542231816925 ) ) ;
#45657=CARTESIAN_POINT ( 'NONE',  ( 0.8759842519685039353, -0.1787899950787401882, 1.311515747977732405 ) ) ;
#45661=CARTESIAN_POINT ( 'NONE',  ( -0.7646288533564489232, 0.1113553986120547346, 1.875000000000000000 ) ) ;
#45662=CARTESIAN_POINT ( 'NONE',  ( -0.8759842519685039353, -0.1787899950787401882, 0.5634842519147401640 ) ) ;
#45664=FACE_OUTER_BOUND ( 'NONE', #11266, .T. ) ;
#45665=ORIENTED_EDGE ( 'NONE', *, *, #9973, .T. ) ;
#45668=CARTESIAN_POINT ( 'NONE',  ( -0.6971942568897626646, -0.07405724077823297447, 0.9547244093950547628 ) ) ;
#45669=CARTESIAN_POINT ( 'NONE',  ( -0.8759842519685039353, 0.1574803149606299191, 0.01968503937007873988 ) ) ;
#45671=CARTESIAN_POINT ( 'NONE',  ( -0.6971942568897626646, -0.07405724077823297447, 0.6791338582139527791 ) ) ;
#45677=ORIENTED_EDGE ( 'NONE', *, *, #15662, .T. ) ;
#45681=CARTESIAN_POINT ( 'NONE',  ( -0.9500414927467378812, -0.1787899950787401604, 0.4084645668753704717 ) ) ;
#45682=( BOUNDED_CURVE ( )  B_SPLINE_CURVE ( 2, ( #40462, #44071, #18668, #25419, #25168, #39994, #33328, #7186, #21811 ),
 .UNSPECIFIED., .F., .T. ) 
 B_SPLINE_CURVE_WITH_KNOTS ( ( 3, 2, 2, 2, 3 ),
 ( 0.9399999999999999467, 0.9425000000000000044, 0.9449999999999999512, 0.9475000000000000089, 0.9499999999999999556 ),
 .UNSPECIFIED. ) 
 CURVE ( )  GEOMETRIC_REPRESENTATION_ITEM ( )  RATIONAL_B_SPLINE_CURVE ( ( 1.000000000000000000, 0.9238795325112899581, 1.000000000000000000, 0.9238795325112869605, 1.000000000000000000, 0.9238795325112869605, 1.000000000000000000, 0.9238795325112799661, 1.000000000000000000 ) ) 
 REPRESENTATION_ITEM ( '' )  ) ;
#45683=CARTESIAN_POINT ( 'NONE',  ( -0.8107537697050254399, -0.1574803149606297803, 0.3912401574803148208 ) ) ;
#45684=ORIENTED_EDGE ( 'NONE', *, *, #16538, .F. ) ;
#45685=CARTESIAN_POINT ( 'NONE',  ( -1.002407869896990045, -0.1264236179284866091, 1.636318897584031484 ) ) ;
#45689=ADVANCED_FACE ( 'NONE', ( #40847 ), #27240, .T. ) ;
#45691=CARTESIAN_POINT ( 'NONE',  ( 1.033464566929133799, 0.000000000000000000, 0.9547244094488189781 ) ) ;
#45692=CARTESIAN_POINT ( 'NONE',  ( 1.033464566929134687, -0.06523048226347956391, 0.5585629921259840369 ) ) ;
#45694=LINE ( 'NONE', #12914, #43114 ) ;
#45695=CARTESIAN_POINT ( 'NONE',  ( -1.033464566929134687, 0.06523048226347956391, 1.222933070758614127 ) ) ;
#45699=CARTESIAN_POINT ( 'NONE',  ( -1.033464566929134687, 0.06523048226347956391, 1.183562992018456272 ) ) ;
#45703=CARTESIAN_POINT ( 'NONE',  ( -0.6971942568897637749, 2.189545951927499583E-17, 1.070374015694267600 ) ) ;
#45704=CARTESIAN_POINT ( 'NONE',  ( 0.7185039370078746268, 0.06523048226347956391, 1.050688976377951889 ) ) ;
#45710=CARTESIAN_POINT ( 'NONE',  ( -0.8759842519685039353, -0.1574803149606299191, 1.958661417215307177 ) ) ;
#45712=PRODUCT_DEFINITION_SHAPE ( 'NONE', 'NONE',  #45336 ) ;
#45716=CARTESIAN_POINT ( 'NONE',  ( 0.8019270111902717657, 0.1787899950787401604, 0.7824803149068669805 ) ) ;
#45719=FACE_OUTER_BOUND ( 'NONE', #2546, .T. ) ;
#45723=CARTESIAN_POINT ( 'NONE',  ( 0.9873396505805591694, -0.1113553986120547346, 1.254921259734991912 ) ) ;
#45724=CARTESIAN_POINT ( 'NONE',  ( -1.033464566929133799, 0.000000000000000000, 1.387795275590551158 ) ) ;
#45726=ORIENTED_EDGE ( 'NONE', *, *, #8004, .T. ) ;
#45727=CARTESIAN_POINT ( 'NONE',  ( -0.8019270111902717657, 0.1787899950787401604, 1.968503936954110189 ) ) ;
#45728=ORIENTED_EDGE ( 'NONE', *, *, #13640, .F. ) ;
#45729=CARTESIAN_POINT ( 'NONE',  ( 0.9500414927467378812, 0.1787899950787401604, 1.806102362150961316 ) ) ;
#45732=DIRECTION ( 'NONE',  ( 0.000000000000000000, 0.000000000000000000, -1.000000000000000000 ) ) ;
#45733=CARTESIAN_POINT ( 'NONE',  ( 1.054774247047244096, 0.000000000000000000, 0.3813976377415121966 ) ) ;
#45734=CARTESIAN_POINT ( 'NONE',  ( -0.8759842519685039353, 0.1787899950787401882, 1.409940944828126153 ) ) ;
#45735=CARTESIAN_POINT ( 'NONE',  ( -0.8759842519685039353, 0.000000000000000000, 0.000000000000000000 ) ) ;
#45737=CARTESIAN_POINT ( 'NONE',  ( -0.9500414927467378812, 0.1787899950787401604, 0.9744094487651340231 ) ) ;
#45739=CARTESIAN_POINT ( 'NONE',  ( -0.8759842519685039353, -0.1787899950787401882, 0.2928149605761578567 ) ) ;
#45741=CARTESIAN_POINT ( 'NONE',  ( -0.8759842519685039353, -0.1787899950787401882, 1.710137795221826851 ) ) ;
#45742=CARTESIAN_POINT ( 'NONE',  ( -0.7185039370078746268, -0.06523048226347956391, 1.990649606191687404 ) ) ;
#45744=CARTESIAN_POINT ( 'NONE',  ( -0.7185039370078739607, 1.928577636452523993E-17, 1.683070866141732402 ) ) ;
#45745=CARTESIAN_POINT ( 'NONE',  ( -0.7185039370078760701, -0.06523048226348075740, 0.9375000000000002220 ) ) ;
#45746=CARTESIAN_POINT ( 'NONE',  ( 0.8019270111902716547, -0.1787899950787401604, 1.707677165300568456 ) ) ;
#45748=FACE_OUTER_BOUND ( 'NONE', #42438, .T. ) ;
#45758=CARTESIAN_POINT ( 'NONE',  ( -0.8107537697050253289, 0.1574803149606300301, 0.7603346455617647770 ) ) ;
#45760=EDGE_CURVE ( 'NONE', #36821, #46851, #2584, .T. ) ;
#45761=CARTESIAN_POINT ( 'NONE',  ( 1.054774247047244540, -0.07405724077823318263, 0.9645669290800953366 ) ) ;
#45764=CARTESIAN_POINT ( 'NONE',  ( 0.9412147342319837628, 0.1574803149606300301, 0.08612204713656734789 ) ) ;
#45765=VERTEX_POINT ( 'NONE', #31763 ) ;
#45766=CARTESIAN_POINT ( 'NONE',  ( 0.9873396505805591694, -0.1113553986120547346, 0.2017716535433070890 ) ) ;
#45771=CARTESIAN_POINT ( 'NONE',  ( 1.054774247047244540, -0.07405724077823318263, 0.3789370078202520253 ) ) ;
#45773=CARTESIAN_POINT ( 'NONE',  ( -0.9500414927467378812, -0.1787899950787401604, 1.865157480261195877 ) ) ;
#45774=ORIENTED_EDGE ( 'NONE', *, *, #38508, .F. ) ;
#45775=CARTESIAN_POINT ( 'NONE',  ( -1.054774247047244540, -0.07405724077823318263, 1.520669291284818758 ) ) ;
#45776=DIRECTION ( 'NONE',  ( 0.000000000000000000, 0.000000000000000000, -1.000000000000000000 ) ) ;
#45777=CARTESIAN_POINT ( 'NONE',  ( 0.7495606340400177148, 0.1264236179284866091, 1.341043307032850462 ) ) ;
#45780=CARTESIAN_POINT ( 'NONE',  ( -0.6971942568897626646, 0.07405724077823318263, 0.6742125983714335469 ) ) ;
#45781=CARTESIAN_POINT ( 'NONE',  ( 0.7495606340400177148, 0.1264236179284866091, 0.1205708660879689087 ) ) ;
#45782=CARTESIAN_POINT ( 'NONE',  ( -0.9500414927467378812, 0.1787899950787401604, 1.210629921206079818 ) ) ;
#45783=DIRECTION ( 'NONE',  ( 1.822029033848725028E-16, 0.000000000000000000, 1.000000000000000000 ) ) ;
#45784=CARTESIAN_POINT ( 'NONE',  ( 0.7495606340400177148, -0.1264236179284866091, 0.6028543306548976854 ) ) ;
#45785=CARTESIAN_POINT ( 'NONE',  ( -0.6971942568897648851, -0.07405724077823297447, 0.5167322834108035723 ) ) ;
#45790=ORIENTED_EDGE ( 'NONE', *, *, #32933, .T. ) ;
#45791=CARTESIAN_POINT ( 'NONE',  ( -0.7646288533564489232, -0.1113553986120547346, 0.2312992125984252023 ) ) ;
#45793=CARTESIAN_POINT ( 'NONE',  ( 0.9500414927467377701, -0.1787899950787401604, 1.240157480261197875 ) ) ;
#45795=ORIENTED_EDGE ( 'NONE', *, *, #3786, .F. ) ;
#45796=CARTESIAN_POINT ( 'NONE',  ( -0.9873396505805591694, -0.1113553986120547346, 0.6348425196850393526 ) ) ;
#45797=CARTESIAN_POINT ( 'NONE',  ( -0.8759842519685039353, 0.1787899950787401882, 0.9424212597887559051 ) ) ;
#45800=CARTESIAN_POINT ( 'NONE',  ( -0.7185039370078739607, 1.928577636452523993E-17, 0.1771653542231816925 ) ) ;
#45804=CARTESIAN_POINT ( 'NONE',  ( 0.8019270111902717657, -0.1787899950787401604, 1.309055118056472899 ) ) ;
#45806=EDGE_CURVE ( 'NONE', #6785, #13130, #2266, .T. ) ;
#45808=EDGE_CURVE ( 'NONE', #27525, #41698, #15782, .T. ) ;
#45810=CARTESIAN_POINT ( 'NONE',  ( 0.9873396505805591694, 0.1113553986120547346, 1.815944881782236120 ) ) ;
#45811=CARTESIAN_POINT ( 'NONE',  ( 0.9500414927467378812, 0.1787899950787401604, 1.604330708607653921 ) ) ;
#45814=FACE_OUTER_BOUND ( 'NONE', #39436, .T. ) ;
#45815=EDGE_CURVE ( 'NONE', #43027, #38897, #28954, .T. ) ;
#45816=CARTESIAN_POINT ( 'NONE',  ( 1.002407869896990045, 0.1264236179284866091, 0.4995078739619842612 ) ) ;
#45817=CARTESIAN_POINT ( 'NONE',  ( -0.7495606340400177148, -0.1264236179284866091, 0.8784448818360000022 ) ) ;
#45822=CARTESIAN_POINT ( 'NONE',  ( -0.8057660207509481642, -0.1572945814199120107, 1.986871297128391056 ) ) ;
#45824=CARTESIAN_POINT ( 'NONE',  ( 0.8759842519685039353, 0.1787899950787401882, 1.572342519631275692 ) ) ;
#45826=CARTESIAN_POINT ( 'NONE',  ( 0.6971942568897648851, 0.07405724077823318263, 0.3937007873478114983 ) ) ;
#45827=VECTOR ( 'NONE', #6813, 39.37007874015748143 ) ;
#45828=VERTEX_POINT ( 'NONE', #39154 ) ;
#45829=CARTESIAN_POINT ( 'NONE',  ( -0.8759842519685039353, -0.1574803149606299191, 0.1476377951680635792 ) ) ;
#45830=CARTESIAN_POINT ( 'NONE',  ( 0.7646288533564489232, -0.1113553986120547346, 0.8513779526483780113 ) ) ;
#45834=CARTESIAN_POINT ( 'NONE',  ( 0.9500414927467378812, 0.1787899950787401604, 0.3838582676627718127 ) ) ;
#45836=CARTESIAN_POINT ( 'NONE',  ( 1.002407869896990045, -0.1264236179284866091, 1.316437007820252081 ) ) ;
#45837=CARTESIAN_POINT ( 'NONE',  ( -0.8107537697050254399, 0.1574803149606300301, 1.715059055118110631 ) ) ;
#45839=CARTESIAN_POINT ( 'NONE',  ( -1.054774247047244540, -0.07405724077823318263, 1.476377952702141449 ) ) ;
#45840=CARTESIAN_POINT ( 'NONE',  ( 1.033464566929134687, 0.06523048226347956391, 0.7898622046168821687 ) ) ;
#45841=ORIENTED_EDGE ( 'NONE', *, *, #5516, .T. ) ;
#45842=CARTESIAN_POINT ( 'NONE',  ( -1.033464566929134687, 0.06523048226347956391, 0.7898622046168821687 ) ) ;
#45843=VECTOR ( 'NONE', #42419, 39.37007874015748143 ) ;
#45844=CARTESIAN_POINT ( 'NONE',  ( 0.8759842519685039353, 0.1787899950787401882, 0.9817913385289134265 ) ) ;
#45845=ORIENTED_EDGE ( 'NONE', *, *, #8215, .F. ) ;
#45847=CARTESIAN_POINT ( 'NONE',  ( -1.033464566929133799, 0.000000000000000000, 0.5511811022546778682 ) ) ;
#45848=CARTESIAN_POINT ( 'NONE',  ( -0.8759842519685039353, 0.000000000000000000, 0.000000000000000000 ) ) ;
#45849=CARTESIAN_POINT ( 'NONE',  ( 0.9500414927467378812, -0.1787899950787401604, 1.668307086560410157 ) ) ;
#45850=CARTESIAN_POINT ( 'NONE',  ( -0.7646288533564489232, -0.1113553986120547346, 1.412401574803149540 ) ) ;
#45851=CARTESIAN_POINT ( 'NONE',  ( 0.7185039370078739607, 1.928577636452523993E-17, 1.791338582569637738 ) ) ;
#45853=CARTESIAN_POINT ( 'NONE',  ( 1.002407869896990045, -0.1264236179284866091, 0.1008858267178899676 ) ) ;
#45854=CARTESIAN_POINT ( 'NONE',  ( 0.8759842519685039353, -0.1574803149606299191, 1.486220472333417142 ) ) ;
#45858=CARTESIAN_POINT ( 'NONE',  ( -0.6971942568897648851, 0.07405724077823318263, 1.692913385773008539 ) ) ;
#45860=( BOUNDED_CURVE ( )  B_SPLINE_CURVE ( 2, ( #10238, #29444, #9996, #14541, #21473, #36583, #43756, #39445, #39206 ),
 .UNSPECIFIED., .F., .F. ) 
 B_SPLINE_CURVE_WITH_KNOTS ( ( 3, 2, 2, 2, 3 ),
 ( 0.2600000000000000089, 0.2625000000000000111, 0.2650000000000000133, 0.2675000000000000155, 0.2700000000000000178 ),
 .UNSPECIFIED. ) 
 CURVE ( )  GEOMETRIC_REPRESENTATION_ITEM ( )  RATIONAL_B_SPLINE_CURVE ( ( 1.000000000000000000, 0.9238795325112869605, 1.000000000000000000, 0.9238795325112869605, 1.000000000000000000, 0.9238795325112869605, 1.000000000000000000, 0.9238795325112869605, 1.000000000000000000 ) ) 
 REPRESENTATION_ITEM ( '' )  ) ;
#45863=( BOUNDED_CURVE ( )  B_SPLINE_CURVE ( 2, ( #33685, #18792, #4635, #41278, #23113, #796, #26723, #14990, #19266 ),
 .UNSPECIFIED., .F., .T. ) 
 B_SPLINE_CURVE_WITH_KNOTS ( ( 3, 2, 2, 2, 3 ),
 ( 0.3800000000000000044, 0.3825000000000000067, 0.3850000000000000089, 0.3875000000000000111, 0.3900000000000000133 ),
 .UNSPECIFIED. ) 
 CURVE ( )  GEOMETRIC_REPRESENTATION_ITEM ( )  RATIONAL_B_SPLINE_CURVE ( ( 1.000000000000000000, 0.9238795325112869605, 1.000000000000000000, 0.9238795325112869605, 1.000000000000000000, 0.9238795325112869605, 1.000000000000000000, 0.9238795325112869605, 1.000000000000000000 ) ) 
 REPRESENTATION_ITEM ( '' )  ) ;
#45864=FACE_OUTER_BOUND ( 'NONE', #5236, .T. ) ;
#45876=CARTESIAN_POINT ( 'NONE',  ( 0.8759842519685039353, -0.1574803149606299191, 1.771653543307086576 ) ) ;
#45879=EDGE_CURVE ( 'NONE', #9079, #2757, #10887, .T. ) ;
#45880=FACE_OUTER_BOUND ( 'NONE', #40132, .T. ) ;
#45882=CARTESIAN_POINT ( 'NONE',  ( -0.8759842519685039353, 0.1574803149606299191, 0.2165354330708661457 ) ) ;
#45883=CARTESIAN_POINT ( 'NONE',  ( 0.9500414927467378812, 0.1787899950787401604, 1.058070866087969186 ) ) ;
#45884=CARTESIAN_POINT ( 'NONE',  ( 0.8019270111902716547, -0.1787899950787401604, 0.2460629920722207653 ) ) ;
#45885=CARTESIAN_POINT ( 'NONE',  ( 0.8759842519685039353, -0.1574803149606299191, 0.2362204724409449064 ) ) ;
#45886=CARTESIAN_POINT ( 'NONE',  ( 1.033464566929133799, 0.000000000000000000, 1.545275590551181244 ) ) ;
#45888=CARTESIAN_POINT ( 'NONE',  ( -0.8446276132374470613, 0.1554194282501662749, 1.978957984283404414 ) ) ;
#45890=CARTESIAN_POINT ( 'NONE',  ( -0.7185039370078739607, 1.928577636452523993E-17, 0.6889763778452283605 ) ) ;
#45891=CARTESIAN_POINT ( 'NONE',  ( 0.8759842519685039353, 0.1787899950787401882, 0.9374999999462362288 ) ) ;
#45892=CARTESIAN_POINT ( 'NONE',  ( 1.033464566929133799, 0.000000000000000000, 0.3937007872940480047 ) ) ;
#45893=EDGE_LOOP ( 'NONE', ( #10166, #46632, #45086, #45278 ) ) ;
#45894=CARTESIAN_POINT ( 'NONE',  ( 1.033464566929133799, 0.000000000000000000, 1.259842519577511810 ) ) ;
#45895=CARTESIAN_POINT ( 'NONE',  ( 0.9966270878031755487, 0.1135902891731694064, 0.03937007931061534821 ) ) ;
#45896=CARTESIAN_POINT ( 'NONE',  ( 1.033464566929134687, -0.06523048226347956391, 0.2436023622047244763 ) ) ;
#45897=CARTESIAN_POINT ( 'NONE',  ( 0.8107537697050254399, -0.1574803149606297803, 1.887303149606298414 ) ) ;
#45899=CARTESIAN_POINT ( 'NONE',  ( -0.9412147342319837628, -0.1574803149606297803, 0.3075787400499532809 ) ) ;
#45901=CARTESIAN_POINT ( 'NONE',  ( 1.054774247047244096, 0.000000000000000000, 1.321358267662771757 ) ) ;
#45906=CARTESIAN_POINT ( 'NONE',  ( -0.8019270111902717657, 0.1787899950787401604, 0.6643700786863951935 ) ) ;
#45907=CARTESIAN_POINT ( 'NONE',  ( -0.7185039370078739607, 1.928577636452523993E-17, 0.3444881889763780070 ) ) ;
#45913=CARTESIAN_POINT ( 'NONE',  ( -0.9500414927467378812, 0.1787899950787401604, 0.9399606298674970661 ) ) ;
#45914=CARTESIAN_POINT ( 'NONE',  ( -0.9412147342319837628, 0.1574803149606300301, 0.05659448818897635375 ) ) ;
#45915=ORIENTED_EDGE ( 'NONE', *, *, #16944, .F. ) ;
#45917=CARTESIAN_POINT ( 'NONE',  ( -1.054774247047244540, 0.07405724077823318263, 0.6200787401037165525 ) ) ;
#45926=ORIENTED_EDGE ( 'NONE', *, *, #3304, .F. ) ;
#45929=CARTESIAN_POINT ( 'NONE',  ( -1.054774247047244540, 0.07405724077823318263, 0.4183070865604097133 ) ) ;
#45933=CARTESIAN_POINT ( 'NONE',  ( -0.8759842519685039353, 0.1787899950787401882, 1.651082677111590513 ) ) ;
#45934=AXIS2_PLACEMENT_3D ( 'NONE', #36138, #32074, #3294 ) ;
#45936=DIRECTION ( 'NONE',  ( 0.000000000000000000, 0.000000000000000000, -1.000000000000000000 ) ) ;
#45938=DIRECTION ( 'NONE',  ( 0.000000000000000000, 0.000000000000000000, -1.000000000000000000 ) ) ;
#45940=CARTESIAN_POINT ( 'NONE',  ( 0.7646288533564489232, -0.1113553986120547346, 0.5856299212598424786 ) ) ;
#45943=CARTESIAN_POINT ( 'NONE',  ( -0.8759842519685039353, -0.1574803149606299191, 1.210629921152315047 ) ) ;
#45945=CARTESIAN_POINT ( 'NONE',  ( 1.033464566929133799, 0.000000000000000000, 1.181102362097196989 ) ) ;
#45948=CARTESIAN_POINT ( 'NONE',  ( 0.7185039370078746268, 0.06523048226347956391, 1.090059055118109965 ) ) ;
#45949=DIRECTION ( 'NONE',  ( 1.822029033848725028E-16, 0.000000000000000000, 1.000000000000000000 ) ) ;
#45950=CARTESIAN_POINT ( 'NONE',  ( -0.7646288533564489232, -0.1113553986120547346, 1.333661417322834719 ) ) ;
#45952=DIRECTION ( 'NONE',  ( 1.822029033848725028E-16, 0.000000000000000000, 1.000000000000000000 ) ) ;
#45953=CARTESIAN_POINT ( 'NONE',  ( 0.9873396505805591694, -0.1113553986120547346, 1.687992125876724536 ) ) ;
#45957=CARTESIAN_POINT ( 'NONE',  ( 1.054774247047244540, 0.07405724077823318263, 0.8513779527021426707 ) ) ;
#45958=CARTESIAN_POINT ( 'NONE',  ( -0.8759842519685039353, 0.000000000000000000, 0.000000000000000000 ) ) ;
#45966=CARTESIAN_POINT ( 'NONE',  ( -1.054774247047244540, 0.07405724077823318263, 1.879921259788756016 ) ) ;
#45967=CARTESIAN_POINT ( 'NONE',  ( 0.8019270111902717657, -0.1787899950787401604, 1.825787401521040243 ) ) ;
#45968=ORIENTED_EDGE ( 'NONE', *, *, #26158, .T. ) ;
#45970=CARTESIAN_POINT ( 'NONE',  ( 1.033464566929133799, 0.000000000000000000, 1.781496062992125928 ) ) ;
#45971=VECTOR ( 'NONE', #99, 39.37007874015748143 ) ;
#45972=CARTESIAN_POINT ( 'NONE',  ( -0.8019270111902717657, 0.1787899950787401604, 1.569881889710015299 ) ) ;
#45976=CARTESIAN_POINT ( 'NONE',  ( -1.054774247047244096, 0.000000000000000000, 0.1845472440407248116 ) ) ;
#45977=( BOUNDED_CURVE ( )  B_SPLINE_CURVE ( 2, ( #39891, #14514, #2759, #46848, #42754, #32507, #25053, #7075, #29180 ),
 .UNSPECIFIED., .F., .T. ) 
 B_SPLINE_CURVE_WITH_KNOTS ( ( 3, 2, 2, 2, 3 ),
 ( 0.8900000000000000133, 0.8924999999999999600, 0.8950000000000000178, 0.8974999999999999645, 0.9000000000000000222 ),
 .UNSPECIFIED. ) 
 CURVE ( )  GEOMETRIC_REPRESENTATION_ITEM ( )  RATIONAL_B_SPLINE_CURVE ( ( 1.000000000000000000, 0.9238795325112869605, 1.000000000000000000, 0.9238795325112869605, 1.000000000000000000, 0.9238795325112869605, 1.000000000000000000, 0.9238795325112869605, 1.000000000000000000 ) ) 
 REPRESENTATION_ITEM ( '' )  ) ;
#45978=EDGE_CURVE ( 'NONE', #32474, #426, #37160, .T. ) ;
#45980=CARTESIAN_POINT ( 'NONE',  ( -0.8019270111902717657, 0.1787899950787401604, 1.732283464513166615 ) ) ;
#45982=CARTESIAN_POINT ( 'NONE',  ( -0.9873396505805591694, 0.1113553986120547346, 1.747047244094488194 ) ) ;
#45986=CARTESIAN_POINT ( 'NONE',  ( 0.6971942568897648851, -0.07405724077823297447, 1.702755905458047003 ) ) ;
#45988=CARTESIAN_POINT ( 'NONE',  ( -0.9412147342319837628, -0.1574803149606297803, 0.7406496061916858498 ) ) ;
#45990=EDGE_CURVE ( 'NONE', #34176, #33274, #43937, .T. ) ;
#45993=CARTESIAN_POINT ( 'NONE',  ( -0.9500414927467377701, 0.1787899950787401604, 1.215551181048599272 ) ) ;
#45996=AXIS2_PLACEMENT_3D ( 'NONE', #37953, #1268, #8704 ) ;
#45999=CARTESIAN_POINT ( 'NONE',  ( 0.6971942568897626646, 0.07405724077823318263, 0.3937007873478115538 ) ) ;
#46000=CARTESIAN_POINT ( 'NONE',  ( -0.8107537697050253289, -0.1574803149606297803, 0.8538385825696385156 ) ) ;
#46001=CARTESIAN_POINT ( 'NONE',  ( -0.7646288533564489232, -0.1113553986120547346, 0.7037401574803149318 ) ) ;
#46004=AXIS2_PLACEMENT_3D ( 'NONE', #28445, #7085, #32753 ) ;
#46005=CARTESIAN_POINT ( 'NONE',  ( 0.6971942568897626646, -0.07405724077823297447, 0.9104330708123776761 ) ) ;
#46010=CARTESIAN_POINT ( 'NONE',  ( 1.054774247047244540, -0.07405724077823318263, 1.914370078686394860 ) ) ;
#46012=DIRECTION ( 'NONE',  ( -1.000000000000000000, 0.000000000000000000, 0.000000000000000000 ) ) ;
#46015=CARTESIAN_POINT ( 'NONE',  ( -0.6971942568897648851, -0.07405724077823297447, 1.894685039316315489 ) ) ;
#46017=CARTESIAN_POINT ( 'NONE',  ( -1.054774247047244540, -0.07405724077823318263, 1.402559055064346971 ) ) ;
#46018=CARTESIAN_POINT ( 'NONE',  ( 1.054774247047244096, 0.000000000000000000, 1.365649606245448844 ) ) ;
#46021=CARTESIAN_POINT ( 'NONE',  ( -0.8019270111902717657, -0.1787899950787401604, 0.6446850393163160442 ) ) ;
#46022=LINE ( 'NONE', #35736, #2892 ) ;
#46024=CARTESIAN_POINT ( 'NONE',  ( 0.6971942568897648851, -0.07405724077823297447, 0.6791338582139527791 ) ) ;
#46025=CARTESIAN_POINT ( 'NONE',  ( -0.8019270111902716547, -0.1787899950787401604, 0.5216535432533228045 ) ) ;
#46029=CARTESIAN_POINT ( 'NONE',  ( 0.8759842519685039353, 0.1574803149606299191, 1.663385826664125933 ) ) ;
#46032=CARTESIAN_POINT ( 'NONE',  ( -0.9873396505805591694, 0.1113553986120547346, 0.3297244094488189226 ) ) ;
#46033=CARTESIAN_POINT ( 'NONE',  ( 0.6971942568897648851, 0.07405724077823318263, 1.382874015694267822 ) ) ;
#46035=CARTESIAN_POINT ( 'NONE',  ( -0.8759842519685039353, -0.1574803149606299191, 1.840551180994834501 ) ) ;
#46037=EDGE_LOOP ( 'NONE', ( #3678, #38920, #40293, #29467 ) ) ;
#46042=CARTESIAN_POINT ( 'NONE',  ( 0.8107537697050254399, 0.1574803149606300301, 1.006397637795276800 ) ) ;
#46045=ORIENTED_EDGE ( 'NONE', *, *, #35455, .T. ) ;
#46050=CARTESIAN_POINT ( 'NONE',  ( 0.9873396505805591694, 0.1113553986120547346, 1.422244094380661572 ) ) ;
#46051=CARTESIAN_POINT ( 'NONE',  ( 1.002407869896990045, 0.1264236179284866091, 1.680610236166708793 ) ) ;
#46056=CARTESIAN_POINT ( 'NONE',  ( 1.054774247047244540, 0.07405724077823318263, 0.4970472440407249226 ) ) ;
#46057=AXIS2_PLACEMENT_3D ( 'NONE', #36336, #3488, #12113 ) ;
#46058=CARTESIAN_POINT ( 'NONE',  ( -0.7495606340400177148, 0.1264236179284866091, 0.8686023621509606496 ) ) ;
#46060=CARTESIAN_POINT ( 'NONE',  ( -0.7185039370078739607, 0.000000000000000000, -2.869337061179095023E-17 ) ) ;
#46062=CARTESIAN_POINT ( 'NONE',  ( -0.7614880836181143753, -0.1264398804583182212, 1.985866350195779395 ) ) ;
#46066=CARTESIAN_POINT ( 'NONE',  ( 0.6971942568897648851, 0.07405724077823318263, 1.540354330654897685 ) ) ;
#46069=CARTESIAN_POINT ( 'NONE',  ( 0.9500414927467377701, 0.1787899950787401604, 0.3444881889226146243 ) ) ;
#46071=DIRECTION ( 'NONE',  ( 0.000000000000000000, 0.000000000000000000, -1.000000000000000000 ) ) ;
#46072=CARTESIAN_POINT ( 'NONE',  ( -0.7185039370078739607, 1.928577636452523993E-17, 0.1377952754830242266 ) ) ;
#46073=CYLINDRICAL_SURFACE ( 'NONE', #655, 0.1574803149606299191 ) ;
#46076=CARTESIAN_POINT ( 'NONE',  ( 1.054774247047244540, -0.07405724077823318263, 0.4133858267178901480 ) ) ;
#46078=CARTESIAN_POINT ( 'NONE',  ( 0.9873396505805591694, -0.1113553986120547346, 0.08366141732283464971 ) ) ;
#46080=CARTESIAN_POINT ( 'NONE',  ( -1.002407869896990045, -0.1264236179284866091, 1.473917322780881722 ) ) ;
#46081=ORIENTED_EDGE ( 'NONE', *, *, #36171, .T. ) ;
#46082=CARTESIAN_POINT ( 'NONE',  ( 1.054774247047244540, -0.07405724077823318263, 1.087598425143086578 ) ) ;
#46084=CARTESIAN_POINT ( 'NONE',  ( -0.7185039370078746268, 0.06523048226347956391, 0.5290354329633386588 ) ) ;
#46085=CARTESIAN_POINT ( 'NONE',  ( 0.8759842519685039353, 0.1574803149606299191, 0.09842519685039370636 ) ) ;
#46086=CARTESIAN_POINT ( 'NONE',  ( 0.8019270111902717657, -0.1787899950787401604, 1.702755905458047003 ) ) ;
#46087=CARTESIAN_POINT ( 'NONE',  ( -0.7185039370078746268, 0.06523048226347956391, 1.405019685039369914 ) ) ;
#46090=CARTESIAN_POINT ( 'NONE',  ( 1.054774247047244540, -0.07405724077823318263, 0.2214566928596221063 ) ) ;
#46092=CARTESIAN_POINT ( 'NONE',  ( 0.8107537697050253289, -0.1574803149606297803, 1.444389763672000671 ) ) ;
#46095=ADVANCED_FACE ( 'NONE', ( #8212 ), #15195, .T. ) ;
#46097=CARTESIAN_POINT ( 'NONE',  ( 1.033464566929133799, 0.000000000000000000, 1.771653543199558811 ) ) ;
#46100=CARTESIAN_POINT ( 'NONE',  ( -1.054774247047244540, -0.07405724077823318263, 1.673228346402929834 ) ) ;
#46102=CARTESIAN_POINT ( 'NONE',  ( 1.033464566929133799, 0.000000000000000000, 0.03937007863263043694 ) ) ;
#46108=ORIENTED_EDGE ( 'NONE', *, *, #4104, .T. ) ;
#46109=ORIENTED_EDGE ( 'NONE', *, *, #34779, .T. ) ;
#46113=CARTESIAN_POINT ( 'NONE',  ( -0.7185039370078739607, 1.928577636452523993E-17, 1.446850393700787274 ) ) ;
#46115=CARTESIAN_POINT ( 'NONE',  ( 0.8107537697050253289, 0.1574803149606300301, 1.833169291338582418 ) ) ;
#46118=CARTESIAN_POINT ( 'NONE',  ( -0.8759842519685039353, 0.1787899950787401882, 0.3912401574265515491 ) ) ;
#46119=CARTESIAN_POINT ( 'NONE',  ( -0.7646288533564489232, -0.1113553986120547346, 1.058070866141732402 ) ) ;
#46121=CARTESIAN_POINT ( 'NONE',  ( -1.033464566929134687, 0.06523048226347956391, 0.2091535433070865757 ) ) ;
#46122=CARTESIAN_POINT ( 'NONE',  ( 0.8759842519685039353, 0.1787899950787401882, 1.060531496009228247 ) ) ;
#46123=CARTESIAN_POINT ( 'NONE',  ( 0.9500414927467377701, 0.1787899950787401604, 1.604330708607653921 ) ) ;
#46124=CYLINDRICAL_SURFACE ( 'NONE', #10068, 0.1574803149606299191 ) ;
#46126=CARTESIAN_POINT ( 'NONE',  ( -0.8354712756307374200, 0.1536107227041229595, 1.979144599375029623 ) ) ;
#46127=CARTESIAN_POINT ( 'NONE',  ( 0.7185039370078739607, 0.000000000000000000, 4.498031496062992574 ) ) ;
#46130=CARTESIAN_POINT ( 'NONE',  ( 0.7185039370078739607, 1.928577636452523993E-17, 1.643700787401574992 ) ) ;
#46131=CARTESIAN_POINT ( 'NONE',  ( 0.9500414927467377701, 0.1787899950787401604, 0.9744094487651340231 ) ) ;
#46132=CARTESIAN_POINT ( 'NONE',  ( 0.8759842519685039353, -0.1787899950787401882, 1.985728346402929168 ) ) ;
#46133=CARTESIAN_POINT ( 'NONE',  ( 0.9412147342319837628, 0.1574803149606300301, 0.3617125983176697201 ) ) ;
#46137=CARTESIAN_POINT ( 'NONE',  ( 1.019390624703269133, 0.07727918952924982265, 0.03937226948580224706 ) ) ;
#46141=CARTESIAN_POINT ( 'NONE',  ( -0.9873396505805591694, -0.1113553986120547346, 0.3100393699712130080 ) ) ;
#46143=CARTESIAN_POINT ( 'NONE',  ( 1.054774247047244540, 0.07405724077823318263, 1.245078740103716886 ) ) ;
#46144=CARTESIAN_POINT ( 'NONE',  ( 1.033464566929133799, 0.000000000000000000, 1.220472440837354400 ) ) ;
#46147=CARTESIAN_POINT ( 'NONE',  ( -0.7185039370078746268, -0.06523048226347956391, 1.006397637687749258 ) ) ;
#46148=( BOUNDED_CURVE ( )  B_SPLINE_CURVE ( 2, ( #46454, #20123, #27596, #12730, #16771, #45988, #9112, #42146, #17006 ),
 .UNSPECIFIED., .F., .T. ) 
 B_SPLINE_CURVE_WITH_KNOTS ( ( 3, 2, 2, 2, 3 ),
 ( 0.3499999999999999778, 0.3524999999999999800, 0.3549999999999999822, 0.3574999999999999845, 0.3599999999999999867 ),
 .UNSPECIFIED. ) 
 CURVE ( )  GEOMETRIC_REPRESENTATION_ITEM ( )  RATIONAL_B_SPLINE_CURVE ( ( 1.000000000000000000, 0.9238795325112879597, 1.000000000000000000, 0.9238795325112869605, 1.000000000000000000, 0.9238795325112869605, 1.000000000000000000, 0.9238795325112869605, 1.000000000000000000 ) ) 
 REPRESENTATION_ITEM ( '' )  ) ;
#46151=ORIENTED_EDGE ( 'NONE', *, *, #37703, .T. ) ;
#46152=CARTESIAN_POINT ( 'NONE',  ( 0.9412147342319837628, -0.1574803149606297803, 0.5142716535433068392 ) ) ;
#46156=CARTESIAN_POINT ( 'NONE',  ( -0.9500414927467378812, -0.1787899950787401604, 0.9645669290800953366 ) ) ;
#46157=CARTESIAN_POINT ( 'NONE',  ( -0.6971942568897648851, 0.07405724077823318263, 1.929133858213952335 ) ) ;
#46159=EDGE_CURVE ( 'NONE', #29926, #26131, #46955, .T. ) ;
#46160=CARTESIAN_POINT ( 'NONE',  ( -1.054774247047244540, -0.07405724077823318263, 0.6545275590013545086 ) ) ;
#46164=ORIENTED_EDGE ( 'NONE', *, *, #42509, .F. ) ;
#46168=LINE ( 'NONE', #21729, #2658 ) ;
#46169=CARTESIAN_POINT ( 'NONE',  ( -0.8759842519685039353, -0.1574803149606299191, 1.761811023514519459 ) ) ;
#46170=CARTESIAN_POINT ( 'NONE',  ( -0.7495606340400177148, 0.1264236179284866091, 0.5880905511273386566 ) ) ;
#46171=CARTESIAN_POINT ( 'NONE',  ( 1.033464566929133799, 1.928577636452524610E-17, 4.498031496062992574 ) ) ;
#46172=CARTESIAN_POINT ( 'NONE',  ( -0.8759842519685039353, -0.1787899950787401882, 1.710137795221826851 ) ) ;
#46177=CARTESIAN_POINT ( 'NONE',  ( 0.9412147342319837628, -0.1574803149606297803, 0.5536417322834641386 ) ) ;
#46178=CARTESIAN_POINT ( 'NONE',  ( 0.7185039370078746268, 0.06523048226347956391, 0.6471456691838118891 ) ) ;
#46179=CARTESIAN_POINT ( 'NONE',  ( -0.7185039370078739607, 1.928577636452523993E-17, 1.279527558947590515 ) ) ;
#46182=CARTESIAN_POINT ( 'NONE',  ( -0.9412147342319837628, 0.1574803149606300301, 1.188484251860977503 ) ) ;
#46183=ORIENTED_EDGE ( 'NONE', *, *, #4640, .F. ) ;
#46186=CARTESIAN_POINT ( 'NONE',  ( 0.9412147342319837628, -0.1574803149606297803, 1.262303149606299746 ) ) ;
#46192=DIRECTION ( 'NONE',  ( 1.822029033848725028E-16, 0.000000000000000000, 1.000000000000000000 ) ) ;
#46193=CARTESIAN_POINT ( 'NONE',  ( -1.033464566929133799, 0.000000000000000000, 0.6791338582677166613 ) ) ;
#46198=CARTESIAN_POINT ( 'NONE',  ( 1.054774247047244096, 0.000000000000000000, 0.8489173227808819444 ) ) ;
#46204=CARTESIAN_POINT ( 'NONE',  ( 0.7185039370078746268, -0.06523048226347956391, 1.281988188868851575 ) ) ;
#46206=CARTESIAN_POINT ( 'NONE',  ( -1.054774247047244540, -0.07405724077823318263, 1.914370078686394860 ) ) ;
#46207=CARTESIAN_POINT ( 'NONE',  ( 0.8019270111902717657, -0.1787899950787401604, 1.983267716481667886 ) ) ;
#46209=CARTESIAN_POINT ( 'NONE',  ( -1.033464566929133799, 0.000000000000000000, 0.4724409447743622148 ) ) ;
#46210=CARTESIAN_POINT ( 'NONE',  ( -0.6971942568897637749, 2.189545951927499583E-17, 1.537893700733637736 ) ) ;
#46212=CARTESIAN_POINT ( 'NONE',  ( -0.6971942568897648851, 0.07405724077823318263, 1.023622047190330342 ) ) ;
#46213=CARTESIAN_POINT ( 'NONE',  ( -0.8019270111902717657, -0.1787899950787401604, 0.2903543306548980185 ) ) ;
#46215=CARTESIAN_POINT ( 'NONE',  ( -0.6971942568897648851, -0.07405724077823297447, 1.938976377898990799 ) ) ;
#46216=CARTESIAN_POINT ( 'NONE',  ( -0.7646288533564489232, -0.1113553986120547346, 1.845472440944881942 ) ) ;
#46218=DIRECTION ( 'NONE',  ( 0.000000000000000000, 0.000000000000000000, -1.000000000000000000 ) ) ;
#46221=CARTESIAN_POINT ( 'NONE',  ( -0.9412147342319837628, -0.1574803149606297803, 1.498523622047243764 ) ) ;
#46222=CARTESIAN_POINT ( 'NONE',  ( -1.033464566929133799, 0.000000000000000000, 0.8661417321759370402 ) ) ;
#46227=CARTESIAN_POINT ( 'NONE',  ( -0.8759842519685039353, -0.1574803149606299191, 1.368110236112944911 ) ) ;
#46230=CARTESIAN_POINT ( 'NONE',  ( -1.033464566929133799, 0.000000000000000000, 0.7874015746956221085 ) ) ;
#46231=CARTESIAN_POINT ( 'NONE',  ( -0.7185039370078746268, 0.06523048226347956391, 0.7750984251968497940 ) ) ;
#46235=CARTESIAN_POINT ( 'NONE',  ( 1.002407869896990045, -0.1264236179284866091, 0.9621062991588346103 ) ) ;
#46237=ADVANCED_FACE ( 'NONE', ( #15430 ), #19474, .T. ) ;
#46239=CYLINDRICAL_SURFACE ( 'NONE', #3204, 0.1574803149606299191 ) ;
#46240=CARTESIAN_POINT ( 'NONE',  ( 0.8759842519685039353, -0.1574803149606299191, 0.2263779526483783444 ) ) ;
#46242=VERTEX_POINT ( 'NONE', #41483 ) ;
#46243=ADVANCED_FACE ( 'NONE', ( #18997 ), #36988, .T. ) ;
#46245=CARTESIAN_POINT ( 'NONE',  ( -0.9412147342319837628, -0.1574803149606297803, 0.7800196849318437042 ) ) ;
#46246=CARTESIAN_POINT ( 'NONE',  ( -0.9873396505805591694, -0.1113553986120547346, 1.186023622047243986 ) ) ;
#46249=CARTESIAN_POINT ( 'NONE',  ( 0.6971942568897637749, 2.189545951927499583E-17, 0.3223425196312759144 ) ) ;
#46250=( BOUNDED_CURVE ( )  B_SPLINE_CURVE ( 2, ( #15648, #111, #11173, #8424, #36565, #8660, #41462, #40360, #5068 ),
 .UNSPECIFIED., .F., .T. ) 
 B_SPLINE_CURVE_WITH_KNOTS ( ( 3, 2, 2, 2, 3 ),
 ( 0.3099999999999999978, 0.3125000000000000000, 0.3150000000000000022, 0.3175000000000000044, 0.3200000000000000067 ),
 .UNSPECIFIED. ) 
 CURVE ( )  GEOMETRIC_REPRESENTATION_ITEM ( )  RATIONAL_B_SPLINE_CURVE ( ( 1.000000000000000000, 0.9238795325112869605, 1.000000000000000000, 0.9238795325112869605, 1.000000000000000000, 0.9238795325112869605, 1.000000000000000000, 0.9238795325112869605, 1.000000000000000000 ) ) 
 REPRESENTATION_ITEM ( '' )  ) ;
#46251=CARTESIAN_POINT ( 'NONE',  ( -0.7495606340400177148, -0.1264236179284866091, 1.975885826717889815 ) ) ;
#46254=CARTESIAN_POINT ( 'NONE',  ( -0.8759842519685039353, 0.1787899950787401882, 1.454232283410803017 ) ) ;
#46255=CARTESIAN_POINT ( 'NONE',  ( 0.9500414927467378812, 0.1787899950787401604, 1.412401574749386990 ) ) ;
#46259=CARTESIAN_POINT ( 'NONE',  ( -0.7495606340400177148, -0.1264236179284866091, 0.6028543306548976854 ) ) ;
#46260=CARTESIAN_POINT ( 'NONE',  ( -0.7495606340400177148, 0.1264236179284866091, 1.296751968450173154 ) ) ;
#46262=CARTESIAN_POINT ( 'NONE',  ( -1.033464566929133799, 0.000000000000000000, 1.614173228238929170 ) ) ;
#46263=CARTESIAN_POINT ( 'NONE',  ( 1.054774247047244540, -0.07405724077823318263, 0.6938976377415124741 ) ) ;
#46264=CARTESIAN_POINT ( 'NONE',  ( -0.6971942568897648851, 0.07405724077823318263, 0.4724409448281262636 ) ) ;
#46266=DIRECTION ( 'NONE',  ( 1.822029033848725028E-16, 0.000000000000000000, 1.000000000000000000 ) ) ;
#46268=CARTESIAN_POINT ( 'NONE',  ( -0.6971942568897637749, 2.189545951927499583E-17, 1.503444881836000002 ) ) ;
#46270=FACE_OUTER_BOUND ( 'NONE', #28648, .T. ) ;
#46271=CARTESIAN_POINT ( 'NONE',  ( -0.8759842519685039353, -0.1574803149606299191, 0.4724409448818898127 ) ) ;
#46272=CARTESIAN_POINT ( 'NONE',  ( 0.7495606340400177148, -0.1264236179284866091, 1.350885826717889815 ) ) ;
#46274=CARTESIAN_POINT ( 'NONE',  ( -0.7646288533564489232, -0.1113553986120547346, 1.835629921152314825 ) ) ;
#46277=EDGE_LOOP ( 'NONE', ( #11048, #35957, #13240, #33453 ) ) ;
#46278=CARTESIAN_POINT ( 'NONE',  ( -0.7185039370078739607, 1.928577636452523993E-17, 0.5413385826771653919 ) ) ;
#46279=CARTESIAN_POINT ( 'NONE',  ( -1.054774247047244096, 0.000000000000000000, 0.9325787401037164415 ) ) ;
#46280=( BOUNDED_CURVE ( )  B_SPLINE_CURVE ( 2, ( #15049, #861, #3993, #15519, #44241, #37788, #1105, #22447, #15996 ),
 .UNSPECIFIED., .F., .T. ) 
 B_SPLINE_CURVE_WITH_KNOTS ( ( 3, 2, 2, 2, 3 ),
 ( 0.5400000000000000355, 0.5424999999999999822, 0.5450000000000000400, 0.5474999999999999867, 0.5500000000000000444 ),
 .UNSPECIFIED. ) 
 CURVE ( )  GEOMETRIC_REPRESENTATION_ITEM ( )  RATIONAL_B_SPLINE_CURVE ( ( 1.000000000000000000, 0.9238795325112869605, 1.000000000000000000, 0.9238795325112869605, 1.000000000000000000, 0.9238795325112869605, 1.000000000000000000, 0.9238795325112869605, 1.000000000000000000 ) ) 
 REPRESENTATION_ITEM ( '' )  ) ;
#46284=EDGE_LOOP ( 'NONE', ( #5218, #22585, #11346, #18336 ) ) ;
#46285=CARTESIAN_POINT ( 'NONE',  ( 1.054774247047244096, 0.000000000000000000, 1.400098425143086800 ) ) ;
#46288=CARTESIAN_POINT ( 'NONE',  ( 0.8759842519685039353, 0.000000000000000000, 4.498031496062992574 ) ) ;
#46290=CARTESIAN_POINT ( 'NONE',  ( 0.6971942568897648851, -0.07405724077823297447, 1.658464566875369472 ) ) ;
#46294=AXIS2_PLACEMENT_3D ( 'NONE', #25652, #43596, #18211 ) ;
#46295=CARTESIAN_POINT ( 'NONE',  ( 0.6971942568897637749, 2.189545951927499583E-17, 0.4355314960092284138 ) ) ;
#46297=CARTESIAN_POINT ( 'NONE',  ( -1.054774247047244096, 0.000000000000000000, 0.7357283464029290565 ) ) ;
#46299=CARTESIAN_POINT ( 'NONE',  ( 0.8107537697050254399, 0.1574803149606300301, 0.9965551180027086842 ) ) ;
#46301=CARTESIAN_POINT ( 'NONE',  ( -0.7738239533278032933, -0.1371752372774997231, 1.986169549678695079 ) ) ;
#46305=CARTESIAN_POINT ( 'NONE',  ( 1.054774247047244096, 0.000000000000000000, 1.562499999946236118 ) ) ;
#46307=LINE ( 'NONE', #10378, #12449 ) ;
#46308=CARTESIAN_POINT ( 'NONE',  ( 0.6971942568897648851, 0.07405724077823318263, 0.3543307086076538659 ) ) ;
#46310=VERTEX_POINT ( 'NONE', #41022 ) ;
#46313=EDGE_CURVE ( 'NONE', #34404, #32938, #12070, .T. ) ;
#46315=CARTESIAN_POINT ( 'NONE',  ( -0.7185039370078739607, 0.000000000000000000, -2.869337061179095023E-17 ) ) ;
#46318=CARTESIAN_POINT ( 'NONE',  ( 0.8759842519685039353, -0.1787899950787401882, 0.5634842519147401640 ) ) ;
#46320=CARTESIAN_POINT ( 'NONE',  ( 0.7603450666732096686, -0.1189009846179017033, 0.03937015212195697778 ) ) ;
#46321=CARTESIAN_POINT ( 'NONE',  ( -0.7185039370078739607, 1.928577636452523993E-17, 1.515748031388535200 ) ) ;
#46322=CARTESIAN_POINT ( 'NONE',  ( -0.8019270111902717657, -0.1787899950787401604, 1.505905511757261284 ) ) ;
#46324=CARTESIAN_POINT ( 'NONE',  ( 0.7185039370078739607, 1.928577636452523993E-17, 0.4232283464566928832 ) ) ;
#46325=CARTESIAN_POINT ( 'NONE',  ( 0.7495606340400177148, 0.1264236179284866091, 0.9867125983714331028 ) ) ;
#46326=CARTESIAN_POINT ( 'NONE',  ( -0.7646288533564489232, 0.1113553986120547346, 0.7234251967428662056 ) ) ;
#46327=CARTESIAN_POINT ( 'NONE',  ( 1.002407869896990045, -0.1264236179284866091, 1.670767716481669440 ) ) ;
#46328=CARTESIAN_POINT ( 'NONE',  ( -0.7646288533564489232, 0.1113553986120547346, 1.363188976377952999 ) ) ;
#46329=CARTESIAN_POINT ( 'NONE',  ( -1.002407869896990045, -0.1264236179284866091, 0.8833661416785196785 ) ) ;
#46330=FACE_OUTER_BOUND ( 'NONE', #42961, .T. ) ;
#46331=CARTESIAN_POINT ( 'NONE',  ( 0.9500414927467377701, 0.1787899950787401604, 0.1525590550643468324 ) ) ;
#46332=CARTESIAN_POINT ( 'NONE',  ( -1.054774247047244096, 0.000000000000000000, 0.1008858267178899676 ) ) ;
#46333=CARTESIAN_POINT ( 'NONE',  ( 0.9412147342319837628, 0.1574803149606300301, 1.621555118002709683 ) ) ;
#46335=CARTESIAN_POINT ( 'NONE',  ( -1.054774247047244540, 0.07405724077823318263, 1.756889763725764553 ) ) ;
#46338=CARTESIAN_POINT ( 'NONE',  ( -1.033464566929133799, 0.000000000000000000, 0.7972440944881890035 ) ) ;
#46346=CARTESIAN_POINT ( 'NONE',  ( 0.7495606340400177148, 0.1264236179284866091, 1.060531496009228247 ) ) ;
#46347=CARTESIAN_POINT ( 'NONE',  ( -1.033464566929134687, -0.06523048226347956391, 1.218011810916094895 ) ) ;
#46348=CARTESIAN_POINT ( 'NONE',  ( -1.033464566929133799, 0.000000000000000000, 0.9055118109160944506 ) ) ;
#46349=CARTESIAN_POINT ( 'NONE',  ( 0.7185039370078746268, 0.06523048226347956391, 1.759350393700787940 ) ) ;
#46353=CARTESIAN_POINT ( 'NONE',  ( -0.9500414927467377701, -0.1787899950787401604, 0.4133858267178901480 ) ) ;
#46355=CARTESIAN_POINT ( 'NONE',  ( -0.7185039370078692977, 0.06523048226347515077, 1.946358267609008097 ) ) ;
#46356=CARTESIAN_POINT ( 'NONE',  ( 0.8759842519685039353, -0.1787899950787401882, 1.080216535379306952 ) ) ;
#46357=CARTESIAN_POINT ( 'NONE',  ( 0.9500414927467377701, 0.1787899950787401604, 1.486220472387181912 ) ) ;
#46358=CARTESIAN_POINT ( 'NONE',  ( 0.7495606340400177148, 0.1264236179284866091, 0.2337598424659216578 ) ) ;
#46362=CARTESIAN_POINT ( 'NONE',  ( 0.8107537697050253289, -0.1574803149606297803, 1.651082677165354839 ) ) ;
#46363=CARTESIAN_POINT ( 'NONE',  ( 0.7185039370078739607, 0.000000000000000000, 4.498031496062992574 ) ) ;
#46364=CARTESIAN_POINT ( 'NONE',  ( -0.8537172869947121656, 0.1566887183902881953, 1.978776088056980464 ) ) ;
#46365=LINE ( 'NONE', #46127, #18275 ) ;
#46366=CARTESIAN_POINT ( 'NONE',  ( -0.9412147342319837628, 0.1574803149606300301, 1.700295275483023172 ) ) ;
#46369=CARTESIAN_POINT ( 'NONE',  ( 0.7495606340400177148, -0.1264236179284866091, 1.070374015694267600 ) ) ;
#46370=DIRECTION ( 'NONE',  ( 0.000000000000000000, 0.000000000000000000, -1.000000000000000000 ) ) ;
#46371=CARTESIAN_POINT ( 'NONE',  ( 0.9500414927467377701, -0.1787899950787401604, 1.909448818843873186 ) ) ;
#46372=CARTESIAN_POINT ( 'NONE',  ( 1.033464566929133799, 0.000000000000000000, 0.5511811022546778682 ) ) ;
#46375=CARTESIAN_POINT ( 'NONE',  ( 1.031513553818225626, 0.03767821469943116036, 0.03937002695152881648 ) ) ;
#46376=AXIS2_PLACEMENT_3D ( 'NONE', #2832, #20591, #46931 ) ;
#46377=CARTESIAN_POINT ( 'NONE',  ( -0.8107537697050234415, -0.1574803149606297803, 0.1845472439869611236 ) ) ;
#46378=ORIENTED_EDGE ( 'NONE', *, *, #27582, .T. ) ;
#46379=CARTESIAN_POINT ( 'NONE',  ( 1.002407869896990045, -0.1264236179284866091, 1.237696850339937038 ) ) ;
#46380=CARTESIAN_POINT ( 'NONE',  ( 1.033464566929134687, 0.06523048226347956391, 1.222933070758614127 ) ) ;
#46383=CARTESIAN_POINT ( 'NONE',  ( 0.7185039370078739607, 1.928577636452523993E-17, 0.7381889763779527769 ) ) ;
#46386=CARTESIAN_POINT ( 'NONE',  ( 0.7185039370078746268, -0.06523048226347956391, 0.5044291338582675976 ) ) ;
#46389=CARTESIAN_POINT ( 'NONE',  ( -1.054774247047244096, 0.000000000000000000, 1.400098425143086800 ) ) ;
#46392=CARTESIAN_POINT ( 'NONE',  ( -0.7495606340400177148, -0.1264236179284866091, 0.9571850393163149340 ) ) ;
#46393=CARTESIAN_POINT ( 'NONE',  ( -0.8019270111902717657, 0.1787899950787401604, 1.963582677111591401 ) ) ;
#46394=EDGE_LOOP ( 'NONE', ( #5605, #30728, #17095, #18226 ) ) ;
#46395=CARTESIAN_POINT ( 'NONE',  ( -0.8759842519685039353, 0.1787899950787401882, 1.055610236166708793 ) ) ;
#46396=CARTESIAN_POINT ( 'NONE',  ( -1.002407869896990045, -0.1264236179284866091, 0.6914370078202519698 ) ) ;
#46397=ADVANCED_FACE ( 'NONE', ( #42906 ), #35528, .T. ) ;
#46400=CARTESIAN_POINT ( 'NONE',  ( -0.7185039370078739607, 1.928577636452523993E-17, 0.06889763779527559306 ) ) ;
#46403=CARTESIAN_POINT ( 'NONE',  ( -0.9873396505805591694, -0.1113553986120547346, 0.3494094487113705294 ) ) ;
#46404=CARTESIAN_POINT ( 'NONE',  ( -1.002407869896990045, 0.1264236179284866091, 0.6176181101824566033 ) ) ;
#46405=ORIENTED_EDGE ( 'NONE', *, *, #34779, .F. ) ;
#46406=CARTESIAN_POINT ( 'NONE',  ( -0.9500414927467377701, -0.1787899950787401604, 1.633858267662771091 ) ) ;
#46407=LINE ( 'NONE', #9537, #16502 ) ;
#46408=EDGE_CURVE ( 'NONE', #44045, #36569, #38161, .T. ) ;
#46409=CARTESIAN_POINT ( 'NONE',  ( -0.8759842519685039353, 0.1574803149606299191, 0.4921259842519685179 ) ) ;
#46410=ORIENTED_EDGE ( 'NONE', *, *, #36744, .T. ) ;
#46413=CARTESIAN_POINT ( 'NONE',  ( -0.7185039370078746268, 0.06523048226347956391, 1.395177165246804130 ) ) ;
#46414=CARTESIAN_POINT ( 'NONE',  ( 0.8019270111902717657, 0.1787899950787401604, 0.6692913385289144257 ) ) ;
#46416=DIRECTION ( 'NONE',  ( -1.000000000000000000, 0.000000000000000000, 0.000000000000000000 ) ) ;
#46417=ORIENTED_EDGE ( 'NONE', *, *, #42281, .T. ) ;
#46418=CARTESIAN_POINT ( 'NONE',  ( 0.8107537697050254399, 0.1574803149606300301, 0.1697834644594022058 ) ) ;
#46420=CARTESIAN_POINT ( 'NONE',  ( 0.9412147342319837628, 0.1574803149606300301, 1.316437007874015519 ) ) ;
#46422=CARTESIAN_POINT ( 'NONE',  ( -0.8759842519685039353, -0.1574803149606299191, 1.338582677165354395 ) ) ;
#46423=CARTESIAN_POINT ( 'NONE',  ( 0.9873396505805591694, -0.1113553986120547346, 1.855314960629921295 ) ) ;
#46425=CARTESIAN_POINT ( 'NONE',  ( 1.054774247047244540, 0.07405724077823318263, 0.6545275590013546196 ) ) ;
#46430=CARTESIAN_POINT ( 'NONE',  ( 0.9500414927467378812, 0.1787899950787401604, 0.7775590550643479704 ) ) ;
#46435=CARTESIAN_POINT ( 'NONE',  ( 0.7185039370078739607, 1.928577636452523993E-17, 1.240157480207432883 ) ) ;
#46439=CARTESIAN_POINT ( 'NONE',  ( -0.9500414927467378812, -0.1787899950787401604, 1.909448818843873186 ) ) ;
#46440=CYLINDRICAL_SURFACE ( 'NONE', #25227, 0.1574803149606299191 ) ;
#46441=ORIENTED_EDGE ( 'NONE', *, *, #20710, .T. ) ;
#46443=CARTESIAN_POINT ( 'NONE',  ( -0.8019270111902716547, 0.1787899950787401604, 1.889763779473794481 ) ) ;
#46444=CARTESIAN_POINT ( 'NONE',  ( -0.9500414927467378812, -0.1787899950787401604, 1.589566929080094448 ) ) ;
#46446=CARTESIAN_POINT ( 'NONE',  ( -1.054774247047244540, -0.07405724077823318263, 1.003937007820251193 ) ) ;
#46447=CARTESIAN_POINT ( 'NONE',  ( -0.8759842519685039353, 0.1787899950787401882, 0.1943897637257641919 ) ) ;
#46449=CARTESIAN_POINT ( 'NONE',  ( -0.8019270111902717657, 0.1787899950787401604, 1.929133858213952335 ) ) ;
#46450=CARTESIAN_POINT ( 'NONE',  ( -1.033464566929134687, -0.06523048226347956391, 1.936515748031494955 ) ) ;
#46454=CARTESIAN_POINT ( 'NONE',  ( -0.7185039370078739607, 1.928577636452523993E-17, 0.7283464565853858819 ) ) ;
#46457=CARTESIAN_POINT ( 'NONE',  ( -1.002407869896990045, 0.1264236179284866091, 0.2239173227808822775 ) ) ;
#46458=ORIENTED_EDGE ( 'NONE', *, *, #46956, .T. ) ;
#46460=CARTESIAN_POINT ( 'NONE',  ( -0.8759842519685039353, 0.1787899950787401882, 1.257381889710015743 ) ) ;
#46461=ORIENTED_EDGE ( 'NONE', *, *, #33087, .F. ) ;
#46467=CARTESIAN_POINT ( 'NONE',  ( -0.7185039370078746268, -0.06523048226347956391, 0.2288385826771655862 ) ) ;
#46468=CARTESIAN_POINT ( 'NONE',  ( -1.033464566929134687, 0.06523048226347956391, 0.9079724408373542888 ) ) ;
#46469=CARTESIAN_POINT ( 'NONE',  ( -0.9873396505805591694, -0.1113553986120547346, 0.7529527559055118058 ) ) ;
#46471=EDGE_LOOP ( 'NONE', ( #29096, #17028, #26210, #43281 ) ) ;
#46472=CARTESIAN_POINT ( 'NONE',  ( 0.8759842519685039353, 0.1574803149606299191, 1.860236220364913207 ) ) ;
#46474=CARTESIAN_POINT ( 'NONE',  ( 0.7646288533564489232, 0.1113553986120547346, 0.7726377952755906220 ) ) ;
#46480=CARTESIAN_POINT ( 'NONE',  ( 0.8107537697050254399, -0.1574803149606297803, 1.090059055010582423 ) ) ;
#46481=CARTESIAN_POINT ( 'NONE',  ( 0.7646288533564489232, -0.1113553986120547346, 0.1820866140657015630 ) ) ;
#46487=CARTESIAN_POINT ( 'NONE',  ( -1.054774247047244096, 0.000000000000000000, 1.911909448765133801 ) ) ;
#46488=VERTEX_POINT ( 'NONE', #34578 ) ;
#46489=ORIENTED_EDGE ( 'NONE', *, *, #37438, .F. ) ;
#46490=CARTESIAN_POINT ( 'NONE',  ( -0.8019270111902717657, 0.1787899950787401604, 1.456692913332062744 ) ) ;
#46491=ORIENTED_EDGE ( 'NONE', *, *, #5880, .T. ) ;
#46492=CARTESIAN_POINT ( 'NONE',  ( 0.8107537697050254399, -0.1574803149606297803, 0.9325787400499523372 ) ) ;
#46494=CARTESIAN_POINT ( 'NONE',  ( -1.002407869896990045, 0.1264236179284866091, 0.7012795275052913224 ) ) ;
#46495=CARTESIAN_POINT ( 'NONE',  ( 0.7495606340400177148, 0.1264236179284866091, 0.1993110235682838682 ) ) ;
#46497=CARTESIAN_POINT ( 'NONE',  ( -1.054774247047244096, 0.000000000000000000, 0.5339566928596221063 ) ) ;
#46499=CARTESIAN_POINT ( 'NONE',  ( -0.7646288533564489232, -0.1113553986120547346, 0.8612204724409449064 ) ) ;
#46500=ORIENTED_EDGE ( 'NONE', *, *, #7625, .F. ) ;
#46501=CARTESIAN_POINT ( 'NONE',  ( -0.6971942568897637749, 2.189545951927499583E-17, 1.424704724355685181 ) ) ;
#46504=CARTESIAN_POINT ( 'NONE',  ( -0.7646288533564489232, -0.1113553986120547346, 1.491141732283464583 ) ) ;
#46505=CARTESIAN_POINT ( 'NONE',  ( -0.7185039370078746268, -0.06523048226347956391, 0.4650590551181104093 ) ) ;
#46506=CARTESIAN_POINT ( 'NONE',  ( 0.7495606340400177148, -0.1264236179284866091, 1.311515747977732405 ) ) ;
#46511=CYLINDRICAL_SURFACE ( 'NONE', #45513, 0.1574803149606299191 ) ;
#46512=EDGE_CURVE ( 'NONE', #37122, #3623, #29254, .T. ) ;
#46518=VERTEX_POINT ( 'NONE', #43150 ) ;
#46519=CARTESIAN_POINT ( 'NONE',  ( 1.054774247047244540, 0.07405724077823318263, 1.441929133804504604 ) ) ;
#46524=CARTESIAN_POINT ( 'NONE',  ( 0.9500414927467378812, -0.1787899950787401604, 1.668307086560410157 ) ) ;
#46525=CARTESIAN_POINT ( 'NONE',  ( 1.054774247047244096, 0.000000000000000000, 0.3764763778989925203 ) ) ;
#46529=CARTESIAN_POINT ( 'NONE',  ( 1.054774247047244096, 0.000000000000000000, 0.5733267715997795166 ) ) ;
#46530=( BOUNDED_CURVE ( )  B_SPLINE_CURVE ( 2, ( #27219, #9209, #37496, #1295, #1058, #19754, #26974, #23592, #38205 ),
 .UNSPECIFIED., .F., .T. ) 
 B_SPLINE_CURVE_WITH_KNOTS ( ( 3, 2, 2, 2, 3 ),
 ( 0.9799999999999999822, 0.9825000000000000400, 0.9849999999999999867, 0.9875000000000000444, 0.9899999999999999911 ),
 .UNSPECIFIED. ) 
 CURVE ( )  GEOMETRIC_REPRESENTATION_ITEM ( )  RATIONAL_B_SPLINE_CURVE ( ( 1.000000000000000000, 0.9238795325112869605, 1.000000000000000000, 0.9238795325112869605, 1.000000000000000000, 0.9238795325112869605, 1.000000000000000000, 0.9238795325112869605, 1.000000000000000000 ) ) 
 REPRESENTATION_ITEM ( '' )  ) ;
#46531=CARTESIAN_POINT ( 'NONE',  ( -0.9500414927467377701, 0.1787899950787401604, 0.8612204723871810241 ) ) ;
#46533=CARTESIAN_POINT ( 'NONE',  ( 1.033464566929133799, 0.000000000000000000, 1.692913385719244213 ) ) ;
#46535=CARTESIAN_POINT ( 'NONE',  ( -0.8433719236205573511, -0.1704368056499333817, 1.987609075866120456 ) ) ;
#46536=CARTESIAN_POINT ( 'NONE',  ( -0.9412147342319837628, -0.1574803149606297803, 1.252460629813731519 ) ) ;
#46537=CARTESIAN_POINT ( 'NONE',  ( 0.8019270111902716547, 0.1787899950787401604, 1.924212598371433325 ) ) ;
#46539=CARTESIAN_POINT ( 'NONE',  ( 1.002407869896990045, -0.1264236179284866091, 0.4502952755367874427 ) ) ;
#46541=ORIENTED_EDGE ( 'NONE', *, *, #8331, .T. ) ;
#46544=CARTESIAN_POINT ( 'NONE',  ( 0.6971942568897637749, 2.189545951927499583E-17, 0.5930118109698583329 ) ) ;
#46546=CARTESIAN_POINT ( 'NONE',  ( 0.9500414927467378812, -0.1787899950787401604, 0.1377952755367876370 ) ) ;
#46547=CARTESIAN_POINT ( 'NONE',  ( -0.8759842519685039353, -0.1574803149606299191, 1.525590551073574774 ) ) ;
#46549=CARTESIAN_POINT ( 'NONE',  ( -0.9500414927467378812, -0.1787899950787401604, 1.392716535379308285 ) ) ;
#46552=CARTESIAN_POINT ( 'NONE',  ( 0.9500414927467378812, 0.1787899950787401604, 1.215551181048599272 ) ) ;
#46553=CARTESIAN_POINT ( 'NONE',  ( -0.7185039370078739607, 1.928577636452523993E-17, 0.7283464565853858819 ) ) ;
#46554=CARTESIAN_POINT ( 'NONE',  ( 0.7495606340400177148, 0.1264236179284866091, 1.808562992072220377 ) ) ;
#46555=CARTESIAN_POINT ( 'NONE',  ( -0.7646288533564489232, -0.1113553986120547346, 1.373031496062992352 ) ) ;
#46556=CARTESIAN_POINT ( 'NONE',  ( -0.8759842519685039353, -0.1787899950787401882, 0.9571850393163149340 ) ) ;
#46559=CARTESIAN_POINT ( 'NONE',  ( 0.9500414927467377701, -0.1787899950787401604, 0.1771653542769452416 ) ) ;
#46560=CARTESIAN_POINT ( 'NONE',  ( -0.6971942568897626646, 0.07405724077823318263, 0.07874015742655143812 ) ) ;
#46561=CARTESIAN_POINT ( 'NONE',  ( 0.8759842519685039353, -0.1574803149606299191, 1.643700787294047228 ) ) ;
#46563=VECTOR ( 'NONE', #25683, 39.37007874015748143 ) ;
#46564=( BOUNDED_CURVE ( )  B_SPLINE_CURVE ( 2, ( #29541, #11288, #40710, #22283, #7910, #4291, #32401, #46977, #14170 ),
 .UNSPECIFIED., .F., .T. ) 
 B_SPLINE_CURVE_WITH_KNOTS ( ( 3, 2, 2, 2, 3 ),
 ( 0.4400000000000000022, 0.4425000000000000044, 0.4450000000000000067, 0.4475000000000000089, 0.4500000000000000111 ),
 .UNSPECIFIED. ) 
 CURVE ( )  GEOMETRIC_REPRESENTATION_ITEM ( )  RATIONAL_B_SPLINE_CURVE ( ( 1.000000000000000000, 0.9238795325112869605, 1.000000000000000000, 0.9238795325112869605, 1.000000000000000000, 0.9238795325112869605, 1.000000000000000000, 0.9238795325112869605, 1.000000000000000000 ) ) 
 REPRESENTATION_ITEM ( '' )  ) ;
#46567=CARTESIAN_POINT ( 'NONE',  ( 1.054774247047244540, -0.07405724077823318263, 0.7726377952218265177 ) ) ;
#46568=CARTESIAN_POINT ( 'NONE',  ( -0.6971942568897648851, -0.07405724077823297447, 1.697834645615527771 ) ) ;
#46569=ADVANCED_FACE ( 'NONE', ( #10360 ), #3625, .T. ) ;
#46572=CYLINDRICAL_SURFACE ( 'NONE', #11549, 0.1574803149606299191 ) ;
#46579=CARTESIAN_POINT ( 'NONE',  ( 0.8019270111902717657, -0.1787899950787401604, 1.072834645615528659 ) ) ;
#46582=CARTESIAN_POINT ( 'NONE',  ( -0.7185039370078746268, -0.06523048226347956391, 0.4158464565853863260 ) ) ;
#46584=CARTESIAN_POINT ( 'NONE',  ( 0.6971942568897626646, -0.07405724077823297447, 0.04429133852891373180 ) ) ;
#46588=CARTESIAN_POINT ( 'NONE',  ( -0.9500414927467377701, 0.1787899950787401604, 0.3100393700249766682 ) ) ;
#46590=CARTESIAN_POINT ( 'NONE',  ( 0.8759842519685039353, -0.1787899950787401882, 1.158956692859621995 ) ) ;
#46591=VECTOR ( 'NONE', #22209, 39.37007874015748143 ) ;
#46592=CARTESIAN_POINT ( 'NONE',  ( 0.9500414927467377701, -0.1787899950787401604, 1.550196850339938148 ) ) ;
#46594=CARTESIAN_POINT ( 'NONE',  ( 0.7646288533564489232, -0.1113553986120547346, 0.8907480313885355327 ) ) ;
#46595=CARTESIAN_POINT ( 'NONE',  ( -0.7185039370078739607, 1.928577636452523993E-17, 1.240157480207432883 ) ) ;
#46598=CARTESIAN_POINT ( 'NONE',  ( -0.8759842519685039353, 0.1574803149606299191, 1.663385826664125933 ) ) ;
#46600=CARTESIAN_POINT ( 'NONE',  ( 0.7495606340400177148, -0.1264236179284866091, 0.2042322834108035723 ) ) ;
#46602=CARTESIAN_POINT ( 'NONE',  ( 0.9500414927467377701, 0.1787899950787401604, 1.092519684985606032 ) ) ;
#46603=FACE_OUTER_BOUND ( 'NONE', #37293, .T. ) ;
#46605=CARTESIAN_POINT ( 'NONE',  ( 0.9873396505805591694, -0.1113553986120547346, 0.4281496061916850726 ) ) ;
#46607=CARTESIAN_POINT ( 'NONE',  ( -0.9412147342319837628, 0.1574803149606300301, 1.119586614173229577 ) ) ;
#46608=CARTESIAN_POINT ( 'NONE',  ( 1.020804986503725420, 0.07407192766898883229, 0.03937343678672019370 ) ) ;
#46610=CARTESIAN_POINT ( 'NONE',  ( 1.002407869896990045, 0.1264236179284866091, 1.483759842465921075 ) ) ;
#46615=CARTESIAN_POINT ( 'NONE',  ( 0.7646288533564489232, 0.1113553986120547346, 0.7332677165354331006 ) ) ;
#46618=CARTESIAN_POINT ( 'NONE',  ( 0.9873396505805591694, -0.1113553986120547346, 0.5167322834645668994 ) ) ;
#46619=CARTESIAN_POINT ( 'NONE',  ( -1.033464566929133799, 1.928577636452524610E-17, 2.869337061179095023E-17 ) ) ;
#46620=CARTESIAN_POINT ( 'NONE',  ( 1.054774247047244096, 0.000000000000000000, 0.4995078739619842612 ) ) ;
#46621=ORIENTED_EDGE ( 'NONE', *, *, #17964, .F. ) ;
#46622=CARTESIAN_POINT ( 'NONE',  ( -0.6971942568897637749, 2.189545951927499583E-17, 1.419783464513165505 ) ) ;
#46624=CARTESIAN_POINT ( 'NONE',  ( -0.8759842519685039353, 0.1787899950787401882, 1.099901574749385880 ) ) ;
#46625=CARTESIAN_POINT ( 'NONE',  ( -0.7646288533564489232, -0.1113553986120547346, 0.03444881889763779653 ) ) ;
#46626=CARTESIAN_POINT ( 'NONE',  ( -1.054774247047244096, 0.000000000000000000, 1.045767716481669440 ) ) ;
#46628=CARTESIAN_POINT ( 'NONE',  ( -0.9500414927467378812, -0.1787899950787401604, 0.8464566928596233275 ) ) ;
#46629=EDGE_CURVE ( 'NONE', #33076, #36685, #13942, .T. ) ;
#46630=CYLINDRICAL_SURFACE ( 'NONE', #19817, 0.1574803149606299191 ) ;
#46632=ORIENTED_EDGE ( 'NONE', *, *, #35034, .T. ) ;
#46637=CARTESIAN_POINT ( 'NONE',  ( -1.033464566929133799, 0.000000000000000000, 1.692913385719244213 ) ) ;
#46638=CARTESIAN_POINT ( 'NONE',  ( -0.6971942568897626646, 0.07405724077823318263, 0.5905511810485987167 ) ) ;
#46640=ORIENTED_EDGE ( 'NONE', *, *, #31033, .F. ) ;
#46641=CARTESIAN_POINT ( 'NONE',  ( -0.9500414927467377701, 0.1787899950787401604, 1.609251968450173598 ) ) ;
#46647=CARTESIAN_POINT ( 'NONE',  ( -0.8107537697050253289, 0.1574803149606300301, 1.390255905404285119 ) ) ;
#46648=CARTESIAN_POINT ( 'NONE',  ( 0.8759842519685039353, -0.1787899950787401882, 0.6865157479777322935 ) ) ;
#46650=CARTESIAN_POINT ( 'NONE',  ( 0.7646288533564489232, 0.1113553986120547346, 1.628937007766488199 ) ) ;
#46653=CARTESIAN_POINT ( 'NONE',  ( 1.033464566929134687, 0.06523048226347956391, 1.311515748031496509 ) ) ;
#46655=CARTESIAN_POINT ( 'NONE',  ( -1.033464566929133799, 0.000000000000000000, 1.348425196850393748 ) ) ;
#46659=CARTESIAN_POINT ( 'NONE',  ( 1.054774247047244096, 0.000000000000000000, 0.7308070865604093802 ) ) ;
#46660=CARTESIAN_POINT ( 'NONE',  ( 0.7185039370078746268, -0.06523048226347956391, 0.2583661416247562959 ) ) ;
#46663=CARTESIAN_POINT ( 'NONE',  ( -0.7185039370078739607, 0.000000000000000000, -2.869337061179095023E-17 ) ) ;
#46665=CARTESIAN_POINT ( 'NONE',  ( 0.6971942568897626646, 0.07405724077823318263, 0.7874015747493863238 ) ) ;
#46671=CARTESIAN_POINT ( 'NONE',  ( 1.033464566929134687, 0.06523048226347956391, 1.232775590551180134 ) ) ;
#46672=CARTESIAN_POINT ( 'NONE',  ( -0.8019270111902717657, -0.1787899950787401604, 0.08858267711159097113 ) ) ;
#46673=ORIENTED_EDGE ( 'NONE', *, *, #26986, .T. ) ;
#46674=CARTESIAN_POINT ( 'NONE',  ( 0.6971942568897648851, 0.07405724077823318263, 1.973425196796630088 ) ) ;
#46676=CARTESIAN_POINT ( 'NONE',  ( 0.7495606340400177148, 0.1264236179284866091, 0.8292322834108031282 ) ) ;
#46678=CARTESIAN_POINT ( 'NONE',  ( -1.054774247047244096, 0.000000000000000000, 0.2632874015210397434 ) ) ;
#46682=CARTESIAN_POINT ( 'NONE',  ( -1.054774247047244540, 0.07405724077823318263, 1.840551181048599938 ) ) ;
#46683=CARTESIAN_POINT ( 'NONE',  ( 0.9412147342319837628, 0.1574803149606300301, 0.2928149606299214613 ) ) ;
#46684=CARTESIAN_POINT ( 'NONE',  ( -0.7185039370078746268, -0.06523048226347956391, 1.882381889763779181 ) ) ;
#46687=CARTESIAN_POINT ( 'NONE',  ( 0.7185039370078739607, 1.928577636452523993E-17, 1.358267716427907779 ) ) ;
#46688=CARTESIAN_POINT ( 'NONE',  ( -0.7185039370078739607, 1.928577636452523993E-17, 0.05905511800270921846 ) ) ;
#46691=CARTESIAN_POINT ( 'NONE',  ( -0.9500414927467378812, 0.1787899950787401604, 0.2263779527021421711 ) ) ;
#46693=CARTESIAN_POINT ( 'NONE',  ( -1.054774247047244540, 0.07405724077823318263, 1.210629921206079818 ) ) ;
#46694=EDGE_LOOP ( 'NONE', ( #45487, #5443, #14297, #23573 ) ) ;
#46700=CARTESIAN_POINT ( 'NONE',  ( -0.9412147342319837628, 0.1574803149606300301, 0.9128937006798734100 ) ) ;
#46701=CARTESIAN_POINT ( 'NONE',  ( -0.8759842519685039353, -0.1574803149606299191, 0.6692913385826771977 ) ) ;
#46703=CARTESIAN_POINT ( 'NONE',  ( 0.7646288533564489232, -0.1113553986120547346, 1.874999999892472458 ) ) ;
#46705=CARTESIAN_POINT ( 'NONE',  ( 1.033464566929134687, -0.06523048226347956391, 0.2337598424121580809 ) ) ;
#46706=CARTESIAN_POINT ( 'NONE',  ( 0.9412147342319837628, 0.1574803149606300301, 0.7652559055118115516 ) ) ;
#46710=CARTESIAN_POINT ( 'NONE',  ( 1.033464566929133799, 0.000000000000000000, 0.8267716534357796299 ) ) ;
#46712=CARTESIAN_POINT ( 'NONE',  ( 0.9873396505805591694, 0.1113553986120547346, 0.1230314959554651699 ) ) ;
#46717=FACE_OUTER_BOUND ( 'NONE', #31909, .T. ) ;
#46721=CARTESIAN_POINT ( 'NONE',  ( 0.8759842519685039353, -0.1574803149606299191, 0.8169291337507401662 ) ) ;
#46723=CARTESIAN_POINT ( 'NONE',  ( -1.054774247047244096, 0.000000000000000000, 0.4158464566391496531 ) ) ;
#46724=EDGE_LOOP ( 'NONE', ( #26276, #40016, #8077, #31791 ) ) ;
#46725=CARTESIAN_POINT ( 'NONE',  ( -0.8019270111902717657, 0.1787899950787401604, 1.496062992072220821 ) ) ;
#46728=CARTESIAN_POINT ( 'NONE',  ( 1.002407869896990045, 0.1264236179284866091, 1.567421259788755794 ) ) ;
#46730=CARTESIAN_POINT ( 'NONE',  ( 1.033464566929134687, -0.06523048226347956391, 0.9424212597349931331 ) ) ;
#46731=ADVANCED_FACE ( 'NONE', ( #33128 ), #10114, .T. ) ;
#46732=CARTESIAN_POINT ( 'NONE',  ( -0.8759842519685039353, -0.1787899950787401882, 0.6471456692375747721 ) ) ;
#46733=CARTESIAN_POINT ( 'NONE',  ( 0.8019270111902717657, -0.1787899950787401604, 0.1328740156942679607 ) ) ;
#46734=CARTESIAN_POINT ( 'NONE',  ( -1.033464566929133799, 0.000000000000000000, 1.072834645669291431 ) ) ;
#46735=CARTESIAN_POINT ( 'NONE',  ( -0.8019270111902716547, -0.1787899950787401604, 0.6791338582139527791 ) ) ;
#46737=EDGE_CURVE ( 'NONE', #10926, #16359, #30899, .T. ) ;
#46740=CARTESIAN_POINT ( 'NONE',  ( -0.8759842519685039353, 0.1787899950787401882, 1.375492125930488196 ) ) ;
#46741=CARTESIAN_POINT ( 'NONE',  ( -1.033464566929134687, -0.06523048226347956391, 0.4010826771653545619 ) ) ;
#46742=CARTESIAN_POINT ( 'NONE',  ( 0.6971942568897648851, -0.07405724077823297447, 1.269685039316314601 ) ) ;
#46745=EDGE_CURVE ( 'NONE', #20507, #40966, #34245, .T. ) ;
#46751=EDGE_LOOP ( 'NONE', ( #29531, #2939, #6917, #44307 ) ) ;
#46752=CARTESIAN_POINT ( 'NONE',  ( 0.8019270111902717657, 0.1787899950787401604, 1.373031496009229135 ) ) ;
#46760=CARTESIAN_POINT ( 'NONE',  ( 0.8759842519685039353, -0.1787899950787401882, 0.3272637794737956463 ) ) ;
#46765=DIRECTION ( 'NONE',  ( -1.000000000000000000, 0.000000000000000000, 0.000000000000000000 ) ) ;
#46766=CARTESIAN_POINT ( 'NONE',  ( 0.9500414927467378812, 0.1787899950787401604, 0.5413385826234012876 ) ) ;
#46767=CARTESIAN_POINT ( 'NONE',  ( -0.6971942568897648851, -0.07405724077823297447, 0.9940944881352130613 ) ) ;
#46772=CARTESIAN_POINT ( 'NONE',  ( 1.054774247047244540, -0.07405724077823318263, 1.678149606245448622 ) ) ;
#46777=EDGE_CURVE ( 'NONE', #3281, #18202, #4387, .T. ) ;
#46778=CARTESIAN_POINT ( 'NONE',  ( 0.7646288533564489232, -0.1113553986120547346, 0.03444881889763779653 ) ) ;
#46781=CARTESIAN_POINT ( 'NONE',  ( 0.7495606340400177148, -0.1264236179284866091, 0.6373031495525354195 ) ) ;
#46783=DIRECTION ( 'NONE',  ( -1.000000000000000000, 0.000000000000000000, 0.000000000000000000 ) ) ;
#46785=CARTESIAN_POINT ( 'NONE',  ( -0.9873396505805591694, -0.1113553986120547346, 0.9891732283464568232 ) ) ;
#46786=CARTESIAN_POINT ( 'NONE',  ( -1.002407869896990045, -0.1264236179284866091, 1.434547244040724534 ) ) ;
#46790=CARTESIAN_POINT ( 'NONE',  ( 0.7495606340400177148, -0.1264236179284866091, 1.232775590497417362 ) ) ;
#46791=CARTESIAN_POINT ( 'NONE',  ( -0.8107537697050253289, 0.1574803149606300301, 0.7209645668216065895 ) ) ;
#46794=CARTESIAN_POINT ( 'NONE',  ( 0.8107537697050254399, -0.1574803149606297803, 1.493602362204724754 ) ) ;
#46795=CARTESIAN_POINT ( 'NONE',  ( 0.7495606340400177148, 0.1264236179284866091, 1.847933070812378009 ) ) ;
#46796=CARTESIAN_POINT ( 'NONE',  ( -0.9412147342319837628, 0.1574803149606300301, 1.434547244094487972 ) ) ;
#46797=CARTESIAN_POINT ( 'NONE',  ( -0.6971942568897626646, 0.07405724077823318263, 0.9448818897100165204 ) ) ;
#46800=CARTESIAN_POINT ( 'NONE',  ( 0.6971942568897648851, 0.07405724077823318263, 0.3592519684501735422 ) ) ;
#46801=CARTESIAN_POINT ( 'NONE',  ( -1.054774247047244540, -0.07405724077823318263, 0.5708661416785201226 ) ) ;
#46803=CARTESIAN_POINT ( 'NONE',  ( 0.9412147342319837628, 0.1574803149606300301, 1.542814960522393308 ) ) ;
#46806=CARTESIAN_POINT ( 'NONE',  ( 0.9412147342319837628, 0.1574803149606300301, 1.779035432963339769 ) ) ;
#46807=CARTESIAN_POINT ( 'NONE',  ( 0.8019270111902717657, -0.1787899950787401604, 0.8415354330171019859 ) ) ;
#46808=CARTESIAN_POINT ( 'NONE',  ( -1.054774247047244096, 0.000000000000000000, 1.911909448765133801 ) ) ;
#46809=DIRECTION ( 'NONE',  ( 0.000000000000000000, 0.000000000000000000, -1.000000000000000000 ) ) ;
#46814=ORIENTED_EDGE ( 'NONE', *, *, #23177, .F. ) ;
#46817=( BOUNDED_CURVE ( )  B_SPLINE_CURVE ( 2, ( #34473, #45699, #41618, #46182, #27548, #35188, #27070, #42100, #9305 ),
 .UNSPECIFIED., .F., .T. ) 
 B_SPLINE_CURVE_WITH_KNOTS ( ( 3, 2, 2, 2, 3 ),
 ( 0.5799999999999999600, 0.5825000000000000178, 0.5849999999999999645, 0.5875000000000000222, 0.5899999999999999689 ),
 .UNSPECIFIED. ) 
 CURVE ( )  GEOMETRIC_REPRESENTATION_ITEM ( )  RATIONAL_B_SPLINE_CURVE ( ( 1.000000000000000000, 0.9238795325112869605, 1.000000000000000000, 0.9238795325112869605, 1.000000000000000000, 0.9238795325112869605, 1.000000000000000000, 0.9238795325112869605, 1.000000000000000000 ) ) 
 REPRESENTATION_ITEM ( '' )  ) ;
#46819=VECTOR ( 'NONE', #41963, 39.37007874015748143 ) ;
#46823=CARTESIAN_POINT ( 'NONE',  ( -0.8759842519685039353, 0.1787899950787401882, 0.4306102361667086820 ) ) ;
#46826=CARTESIAN_POINT ( 'NONE',  ( 0.7495606340400177148, 0.1264236179284866091, 1.222933070812378009 ) ) ;
#46827=CARTESIAN_POINT ( 'NONE',  ( 0.7495606340400177148, -0.1264236179284866091, 1.542814960576157413 ) ) ;
#46829=CARTESIAN_POINT ( 'NONE',  ( 0.7185039370078739607, 1.928577636452523993E-17, 1.683070866141732402 ) ) ;
#46831=CARTESIAN_POINT ( 'NONE',  ( 0.8759842519685039353, -0.1574803149606299191, 1.525590551073574774 ) ) ;
#46832=CARTESIAN_POINT ( 'NONE',  ( 0.9412147342319837628, 0.1574803149606300301, 0.6766732282389295028 ) ) ;
#46833=CARTESIAN_POINT ( 'NONE',  ( -0.7646288533564489232, 0.1113553986120547346, 1.786417322727117840 ) ) ;
#46834=CARTESIAN_POINT ( 'NONE',  ( 1.054774247047244540, 0.07405724077823318263, 0.1033464566391498751 ) ) ;
#46835=( BOUNDED_SURFACE ( )  B_SPLINE_SURFACE ( 1, 2, ( 
 ( #11707, #32817, #4014, #176, #33293, #47410, #33056, #416, #33524, #18865, #18407, #22709, #29715, #43802, #4235, #37315, #14823, #640, #11002, #25619, #40654, #22002, #36627, #44034, #7851, #3790, #22469, #37087, #43473, #36319, #32257, #6343, #28670, #46834, #17371, #14024, #43716, #40113, #32008, #43238, #47326, #25543, #10679, #3474, #14498, #7306, #28909, #6585, #21926, #18330, #21197, #10920, #25039, #32495, #3220, #18086, #24571, #13778, #32732, #25287, #39171, #13548, #35832, #42990, #35604, #9959, #20958, #21689, #2743, #29159, #17611, #2978, #39402, #32967, #46600, #10441, #28185, #6816, #28424, #36546, #7062, #42744, #3707, #10198, #24804, #39634, #21436, #39876, #36063, #17849, #47077, #14270, #15699, #36776, #44179, #29409, #18789, #33443, #11150, #11383, #4386, #44883, #40341, #8239, #559, #26720, #43953, #3934, #14985, #22383, #19264, #18555, #11855, #33212, #30108, #12096, #41274, #40575, #11624, #26481, #25771, #26243, #37480, #19502, #8473, #29638, #25995, #7531, #22630, #19017, #7767, #37007, #33680, #23108, #793, #22866, #15457, #37723, #41045, #33918, #1041, #4874, #38668, #8715, #31256, #37962, #16626, #45834, #30799, #13043, #23810, #27679, #31491, #5346, #41990, #19735, #42242, #9192, #9445, #46076, #20445, #38891, #1759, #45364, #19970, #24293, #5113, #12577, #24061, #5837, #34371, #35083, #34610, #6054, #20203, #2231, #1511, #16850, #13277, #27910, #41754, #42473, #9678, #41510, #38188, #34146, #38429, #16401, #1276, #15931, #31026, #26958, #45593, #12814, #16164, #27444, #30560, #45121, #27205, #5595, #12338, #23351, #8958, #23578, #34855, #2000, #36010, #13727, #32679, #26119, #28365, #18033, #32194, #39587, #10386, #25228, #31725, #20912, #10625, #17797, #46318, #20680, #42934, #2696, #42691, #17087, #28134, #28857, #13502, #21632, #24753, #10144, #46544, #40690, #9909, #2921, #35320, #13968, #24518, #7005, #14217, #2460, #39816, #47267, #39116, #6768, #14447, #29103, #24992, #36266, #46781, #39348, #6530, #11498, #6292, #35552, #21144, #35779, #28618, #17323, #44294, #43178, #21385, #3167, #32444, #47022, #43417, #19383, #23476, #41635, #23234, #8841, #4503, #45477, #677, #26604, #18903, #12704, #16286, #33559, #19140, #12214, #33805, #34037, #22986, #38078, #5234, #37597, #27329, #4757, #7885, #15819, #45001, #41397, #8596, #19623, #10023, #34742, #2116, #13608, #27807, #39238, #5719, #20334, #42585, #42113, #9327, #46430, #9566, #45716, #5481, #46665, #13850, #24643, #12932, #35208, #13396, #31851, #41876, #13171, #28249, #23946, #38553, #24407, #34972, #16746, #38787, #27566, #9081, #23700, #42812, #42367, #6412, #21028, #31387, #38309, #46198, #45957, #24185, #5944, #20565, #35674, #20096, #2346, #1883, #9798, #39009, #32076, #16979, #31617, #6176, #16518, #28026, #20799, #35440, #2811, #17442, #2577, #17216, #31146, #3770, #14339, #14569, #6886, #17676, #10757, #32326, #29470, #18392, #39946, #43064, #43543, #33035, #402, #44015, #46905, #25110, #10267, #32570, #28984, #39473, #39699, #32799, #11217, #21268, #36611, #47155, #7596, #24878, #3047, #28743, #3296, #161, #14095, #25604, #43307, #10987, #40178, #21505, #7378, #18159, #21989, #25830, #25364, #36392, #10511, #14809, #3547, #40408, #22210, #36840, #33277, #7136, #36142, #21757, #18616, #17916, #47394, #3996, #28496, #29237, #6651, #43788, #35893, #1108, #4945, #619, #12159, #1345, #41342, #22692, #26783, #19572, #22448, #19082, #15051, #4701, #15524, #44948, #37793, #33753, #7835, #30166, #864, #18850, #44706, #45188, #41581, #33507, #11929, #16000, #27030, #8543, #34216, #30623, #8783, #30399, #8069, #23419, #19802, #37296, #12410, #26548, #33981, #19332, #38022, #26064, #15278, #5181, #23176, #40633, #29700, #4447, #44474, #37068, #11447, #4222, #34434, #29929, #44243, #41108, #8300, #40871, #11690, #26314, #22931, #37541, #15767, #23643, #35383, #42534, #16231, #20741, #31795, #46379, #42060, #20272, #46143, #30866, #41820, #9265, #2528, #34920, #28195, #12875, #27509, #2290, #1824, #16460, #6116, #16695, #5418, #12645, #6354, #20969, #17154, #20037, #42313, #20512, #38951, #1581, #2064, #42753, #31096, #45657, #31560, #23882, #38494, #45901, #34678, #45427, #27271, #9972, #31324, #24584, #39181, #5664, #9021, #5900, #9506, #24128, #38732, #35148, #38255, #16920, #13339, #27968, #9737, #24353, #25781, #21447, #3233, #47340, #28437, #43486, #32267, #32744, #7320, #3719, #43728, #14513, #10693, #10931, #36076, #21700, #14037, #24815, #17863, #39414, #36559, #25552, #47088, #2758, #104, #6596, #7073, #32981, #14750, #25300, #21939, #32505, #39646, #43251, #40351, #7544, #35615, #6827, #14282, #28922, #32019, #40123, #17381, #18340, #36333, #46610, #28683, #29421, #39888, #43966, #29177, #3485, #11164, #21209, #13791, #43001, #18100, #10212, #35841, #2990, #17622, #46846, #10452, #25052, #807, #18570, #44896, #15713, #37024, #41287, #19030, #37735, #4175, #8015, #11394, #1291, #44652, #4891, #44421, #22396, #11869, #15946, #3944, #40590, #15001, #4649, #19275, #12350, #22646, #26494, #33932, #29652, #41056, #18800, #1054, #8487, #19513, #30348, #12109, #8254, #23122, #34161, #30572, #574, #26010, #45133, #7781, #26969, #22155, #33226, #352, #44194, #33457, #15232, #29878, #11637, #26257, #40820, #16640, #31270, #45849, #46327, #8728, #23364, #13056, #27694, #24074, #19750, #13289, #37972, #42484, #38683, #34385, #1772, #46086, #5850, #38903, #16860, #20459, #2471, #8970, #31739, #1524, #35093, #16178, #45378, #23589, #38201, #5363, #31503, #19983, #34622, #39128, #18043, #36277, #10156, #14456, #39598, #10877, #24765, #28629, #31970, #21884, #6777, #25497, #35564, #2930, #29114, #43187, #40064, #6543, #21154, #43427, #42948, #39363, #47278, #10399, #46554, #6299, #44, #14692, #7265, #13738, #36020, #14227, #32687, #42702, #13980, #43666, #35789, #17567, #25241, #32206, #46795, #21395, #28380, #9921, #24528, #36504, #3180, #3659, #18282, #17809, #20922, #47036, #32457, #28869, #2707, #10636, #39828, #32925, #7020, #21644, #3429, #17335, #4335, #25950, #26433, #989, #44835, #37421, #8184, #33630, #4576, #15173, #15405, #7718, #18513, #11569, #33166, #30284, #19211, #40762, #43906, #41218, #288, #30052, #26668, #8421, #44594, #15646, #26196, #33398, #36963, #1227, #29366, #11107, #514, #44362, #7957, #40299, #33871 ),
 ( #22577, #7482, #12046, #22808, #11338, #23050, #11810, #4822, #40529, #29817, #14935, #22101, #3888, #22335, #4117, #18740, #2178, #27392, #13232, #19918, #34550, #16579, #16116, #41936, #20390, #9143, #23760, #8658, #30505, #45066, #31440, #38370, #34803, #1949, #5785, #23294, #31208, #16801, #45781, #27630, #38608, #6006, #2643, #46733, #20862, #7203, #21825, #39767, #35735, #14404, #21578, #35503, #31680, #6717, #28311, #39302, #17277, #13917, #25434, #28085, #9859, #6958, #32139, #29053, #36221, #31912, #24470, #21332, #42879, #6477, #46495, #28564, #6235, #43132, #10336, #39544, #17748, #46973, #35963, #32396, #14166, #43372, #3372, #17981, #32634, #693, #8137, #19157, #11762, #15347, #44313, #26382, #22279, #22521, #14877, #25671, #18683, #40246, #33820, #22760, #466, #32868, #937, #7433, #7905, #15597, #30233, #26138, #44783, #33342, #40478, #44088, #38523, #14635, #29304, #7662, #4070, #15119, #11055, #11997, #22052, #36677, #37137, #3836, #29537, #18458, #29765, #33107, #231, #4287, #25896, #36915, #11515, #40706, #18918, #37614, #28446, #17391, #4773, #26854, #27346, #8611, #1657, #19401, #45733, #16534, #37866, #42130, #5254, #6363, #5020, #8858, #12231, #2767, #34503, #20978, #15838, #30695, #9980, #23492, #35625, #34283, #1409, #23718, #23250, #19639, #27579, #38092, #41414, #34052, #43012, #23002, #32029, #16070, #16303, #41889, #12946, #1177, #41654, #24591, #45259, #12480, #5497, #27105, #30931, #45492, #12719, #30460, #45018, #9097, #38324, #20109, #46620, #34757, #1897, #31163, #13803, #36343, #6606, #32992, #3728, #25062, #29431, #39899, #25792, #39653, #10706, #46858, #36801, #7086, #40363, #2999, #17872, #43975, #25311, #7553, #21457, #36088, #10942, #10462, #6837, #14761, #21711, #14045, #21221, #15010, #29663, #22162, #28692, #3497, #29191, #114, #10221, #28935, #11177, #3245, #32516, #40133, #47101, #14291, #18112, #43261, #24825, #39427, #3954, #32755, #18577, #33234, #47351, #17633, #14525, #43738, #25561, #7331, #21947, #361, #32277, #36568, #18347, #41298, #1303, #11647, #44663, #22887, #12362, #40832, #1063, #8025, #8739, #5135, #15479, #1782, #31050, #45617, #27466, #13069, #42013, #9220, #23838, #2023, #6556, #18294, #7276, #28881, #31979, #29377, #21166, #36289, #14702, #43917, #7030, #36516, #47047, #21406, #25013, #7495, #36740, #17347, #36033, #32468, #43442, #13749, #21894, #46567, #3671, #18053, #22115, #10411, #32935, #10647, #56, #10889, #32700, #11121, #35800, #40312, #10167, #39611, #25739, #3194, #28391, #28642, #43200, #47290, #17580, #32222, #42959, #14240, #2945, #24775, #39372, #46807, #13992, #6788, #25252, #3441, #17822, #39841, #21656, #14470, #29126, #43680, #25509, #40078, #4127, #44602, #22346, #8670, #33178, #41228, #37201, #1238, #23062, #18750, #299, #8197, #29828, #18978, #33408, #41006, #45077, #40540, #22820, #7730, #1001, #12055, #41467, #37435, #8433, #15892, #41762, #42250, #31034, #31500, #6060, #2467, #42481, #13285, #9454, #9684, #20212, #20454, #12820, #23585, #16634, #38196, #35328, #38900, #45844, #1519, #46325, #5357, #5845, #31732, #13508, #24068, #20688, #31265, #38437, #41996, #24525, #6297, #34380, #5604, #2008, #13052, #30806, #17094, #16172, #28142, #35089, #39126, #27453, #42699, #27688, #9917, #27916, #2237, #45373, #19978, #12587, #8966, #34862, #34617, #1766, #16408, #45601, #9200, #38677, #23818, #16856, #46082, #10874, #14455, #35788, #40062, #3176, #36503, #2927, #6776, #10154, #42, #17806, #3658, #24761, #7262, #39595, #11105, #7014, #25495, #6539, #18041, #21883, #47276, #28628, #32686, #18281, #28376, #24999, #20920, #10632, #21392, #3426, #32923, #36017, #13735, #32455, #47032, #39358, #14223, #14690, #29364, #17565, #28866, #25728, #40296, #29113, #35560, #2704, #17331, #36275, #13977, #31967, #46552, #43185, #42944, #43424, #39825, #25237, #32203, #46790, #10395, #44833, #4575, #18509, #36728, #29815, #36962, #29596, #286, #14932, #37667, #44138, #4821, #11568, #44360, #33397, #12281, #11337, #37190, #40528, #743, #7717, #19445, #986, #22332, #34097, #1225, #15879, #513, #26193, #33868, #18738, #22573, #45065, #26899, #15171, #7956, #4334, #33629, #15404, #30048, #37418, #38137, #45777, #9622, #34325, #2175, #12760, #20623, #8657, #16115, #41702, #30971, #46018, #30738, #38604, #12528, #5780, #20387, #5299, #35027, #31205, #16798, #38838, #27390, #1942, #27149, #31437, #16575, #13228, #6003, #42418, #46255, #9141, #19917, #41934, #31677, #8903, #34548, #24240, #35270, #1699, #2405, #20153, #17038, #13452, #9387, #41457, #23535, #23293, #1455, #23758, #37909, #5065, #45537, #38367, #34800, #12986, #27627, #42179, #24465, #3368, #21576, #42875, #47219, #10332, #43608, #10086, #13914, #17272, #7201, #24943, #25431, #20856, #35731, #40006, #28559, #21822, #39298, #6472, #28806, #28308, #24698, #32631, #43128, #31908, #39063, #32865, #43852, #36451, #13670, #21329, #14163, #17978, #28082, #46728, #3605, #2869, #17504, #10581, #32135, #39540, #6714, #35961, #42644, #9855, #18225, #3118, #6232, #35499, #17745, #2640, #32392, #43369, #25179, #39763, #6955, #36216, #43850, #33103, #7431, #15344, #11757, #4770, #463, #29762, #26380, #22049, #22518, #11281, #40938, #33818, #30231, #22758, #8134, #37133, #37363, #15116, #691, #40475, #3833, #44309, #18455, #15593, #4517, #26134, #29302, #26616, #225, #33574, #11995, #41169, #4284, #934, #11512, #18679, #22276, #19397, #34049, #14632, #33339, #40703, #7902, #11053, #19154, #25667, #44780, #29997, #40242, #18915, #8372, #36675, #22999, #14874, #25893, #29534, #44541, #37611, #44085, #7659, #36912, #4065, #41410, #9340, #34500, #42377, #15834, #23247, #1406, #23489, #5730, #37861, #45729, #5015, #31159, #12944, #45256, #27576, #38321, #42127, #45967, #1654, #9093, #34279, #23959, #23715, #38565, #13182, #2129, #5956, #16299, #12476, #30927, #38796, #19635, #27099, #16758, #31397, #16066, #9576, #45489, #20576, #16531, #24194, #30692, #1173, #45014, #12226, #8854, #8608, #41651, #38090, #5251, #12716, #5494, #27342, #41886, #20107, #6422, #28037, #2819, #21042, #39019, #35683, #17924, #14345, #6185, #17452, #21514, #47162, #17686, #10521, #36153, #28994, #3059, #28261, #43552, #39952, #42822, #32577, #46674, #6662, #24889, #39711, #46207, #35448, #25119, #32337, #13408, #35218 ) ),
 .UNSPECIFIED., .F., .F., .F. ) 
 B_SPLINE_SURFACE_WITH_KNOTS ( ( 2, 2 ),
 ( 3, 2, 2, 2, 2, 2, 2, 2, 2, 2, 2, 2, 2, 2, 2, 2, 2, 2, 2, 2, 2, 2, 2, 2, 2, 2, 2, 2, 2, 2, 2, 2, 2, 2, 2, 2, 2, 2, 2, 2, 2, 2, 2, 2, 2, 2, 2, 2, 2, 2, 2, 2, 2, 2, 2, 2, 2, 2, 2, 2, 2, 2, 2, 2, 2, 2, 2, 2, 2, 2, 2, 2, 2, 2, 2, 2, 2, 2, 2, 2, 2, 2, 2, 2, 2, 2, 2, 2, 2, 2, 2, 2, 2, 2, 2, 2, 2, 2, 2, 2, 2, 2, 2, 2, 2, 2, 2, 2, 2, 2, 2, 2, 2, 2, 2, 2, 2, 2, 2, 2, 2, 2, 2, 2, 2, 2, 2, 2, 2, 2, 2, 2, 2, 2, 2, 2, 2, 2, 2, 2, 2, 2, 2, 2, 2, 2, 2, 2, 2, 2, 2, 2, 2, 2, 2, 2, 2, 2, 2, 2, 2, 2, 2, 2, 2, 2, 2, 2, 2, 2, 2, 2, 2, 2, 2, 2, 2, 2, 2, 2, 2, 2, 2, 2, 2, 2, 2, 2, 2, 2, 2, 2, 2, 2, 2, 2, 2, 2, 2, 2, 2, 2, 2, 2, 2, 2, 2, 2, 2, 2, 2, 2, 2, 2, 2, 2, 2, 2, 2, 2, 2, 2, 2, 2, 2, 2, 2, 2, 2, 2, 2, 2, 2, 2, 2, 2, 2, 2, 2, 2, 2, 2, 2, 2, 2, 2, 2, 2, 2, 2, 2, 2, 2, 2, 2, 2, 2, 2, 2, 2, 2, 2, 2, 2, 2, 2, 2, 2, 2, 2, 2, 2, 2, 2, 2, 2, 2, 2, 2, 2, 2, 2, 2, 2, 2, 2, 2, 2, 2, 2, 2, 2, 2, 2, 2, 2, 2, 2, 2, 2, 2, 2, 2, 2, 2, 2, 2, 2, 2, 2, 2, 2, 2, 2, 2, 2, 2, 2, 2, 2, 2, 2, 2, 2, 2, 2, 2, 2, 2, 2, 2, 2, 2, 2, 2, 2, 2, 2, 2, 2, 2, 2, 2, 2, 2, 2, 2, 2, 2, 2, 2, 2, 2, 2, 2, 2, 2, 2, 2, 2, 2, 2, 2, 2, 2, 2, 2, 2, 2, 2, 2, 2, 2, 2, 2, 2, 2, 2, 2, 2, 2, 2, 2, 2, 2, 2, 2, 2, 2, 2, 2, 2, 2, 2, 2, 2, 2, 2, 2, 2, 3 ),
 ( 0.000000000000000000, 1.000000000000000000 ),
 ( 0.000000000000000000, 0.002500000000000000052, 0.005000000000000000104, 0.007499999999999999722, 0.01000000000000000021, 0.01250000000000000069, 0.01499999999999999944, 0.01750000000000000167, 0.02000000000000000042, 0.02249999999999999917, 0.02500000000000000139, 0.02750000000000000014, 0.02999999999999999889, 0.03250000000000000111, 0.03500000000000000333, 0.03749999999999999861, 0.04000000000000000083, 0.04250000000000000305, 0.04499999999999999833, 0.04750000000000000056, 0.05000000000000000278, 0.05249999999999999806, 0.05500000000000000028, 0.05750000000000000250, 0.05999999999999999778, 0.06250000000000000000, 0.06500000000000000222, 0.06750000000000000444, 0.07000000000000000666, 0.07249999999999999500, 0.07499999999999999722, 0.07749999999999999944, 0.08000000000000000167, 0.08250000000000000389, 0.08500000000000000611, 0.08749999999999999445, 0.08999999999999999667, 0.09249999999999999889, 0.09500000000000000111, 0.09750000000000000333, 0.1000000000000000056, 0.1024999999999999939, 0.1049999999999999961, 0.1074999999999999983, 0.1100000000000000006, 0.1125000000000000028, 0.1150000000000000050, 0.1174999999999999933, 0.1199999999999999956, 0.1224999999999999978, 0.1250000000000000000, 0.1275000000000000022, 0.1300000000000000044, 0.1325000000000000067, 0.1350000000000000089, 0.1375000000000000111, 0.1400000000000000133, 0.1424999999999999878, 0.1449999999999999900, 0.1474999999999999922, 0.1499999999999999944, 0.1524999999999999967, 0.1549999999999999989, 0.1575000000000000011, 0.1600000000000000033, 0.1625000000000000056, 0.1650000000000000078, 0.1675000000000000100, 0.1700000000000000122, 0.1724999999999999867, 0.1749999999999999889, 0.1774999999999999911, 0.1799999999999999933, 0.1824999999999999956, 0.1849999999999999978, 0.1875000000000000000, 0.1900000000000000022, 0.1925000000000000044, 0.1950000000000000067, 0.1975000000000000089, 0.2000000000000000111, 0.2025000000000000133, 0.2049999999999999878, 0.2074999999999999900, 0.2099999999999999922, 0.2124999999999999944, 0.2149999999999999967, 0.2174999999999999989, 0.2200000000000000011, 0.2225000000000000033, 0.2250000000000000056, 0.2275000000000000078, 0.2300000000000000100, 0.2325000000000000122, 0.2349999999999999867, 0.2374999999999999889, 0.2399999999999999911, 0.2424999999999999933, 0.2449999999999999956, 0.2474999999999999978, 0.2500000000000000000, 0.2525000000000000022, 0.2550000000000000044, 0.2575000000000000067, 0.2600000000000000089, 0.2625000000000000111, 0.2650000000000000133, 0.2675000000000000155, 0.2700000000000000178, 0.2725000000000000200, 0.2750000000000000222, 0.2775000000000000244, 0.2800000000000000266, 0.2824999999999999734, 0.2849999999999999756, 0.2874999999999999778, 0.2899999999999999800, 0.2924999999999999822, 0.2949999999999999845, 0.2974999999999999867, 0.2999999999999999889, 0.3024999999999999911, 0.3049999999999999933, 0.3074999999999999956, 0.3099999999999999978, 0.3125000000000000000, 0.3150000000000000022, 0.3175000000000000044, 0.3200000000000000067, 0.3225000000000000089, 0.3250000000000000111, 0.3275000000000000133, 0.3300000000000000155, 0.3325000000000000178, 0.3350000000000000200, 0.3375000000000000222, 0.3400000000000000244, 0.3425000000000000266, 0.3449999999999999734, 0.3474999999999999756, 0.3499999999999999778, 0.3524999999999999800, 0.3549999999999999822, 0.3574999999999999845, 0.3599999999999999867, 0.3624999999999999889, 0.3649999999999999911, 0.3674999999999999933, 0.3699999999999999956, 0.3724999999999999978, 0.3750000000000000000, 0.3775000000000000022, 0.3800000000000000044, 0.3825000000000000067, 0.3850000000000000089, 0.3875000000000000111, 0.3900000000000000133, 0.3925000000000000155, 0.3950000000000000178, 0.3975000000000000200, 0.4000000000000000222, 0.4025000000000000244, 0.4050000000000000266, 0.4074999999999999734, 0.4099999999999999756, 0.4124999999999999778, 0.4149999999999999800, 0.4174999999999999822, 0.4199999999999999845, 0.4224999999999999867, 0.4249999999999999889, 0.4274999999999999911, 0.4299999999999999933, 0.4324999999999999956, 0.4349999999999999978, 0.4375000000000000000, 0.4400000000000000022, 0.4425000000000000044, 0.4450000000000000067, 0.4475000000000000089, 0.4500000000000000111, 0.4525000000000000133, 0.4550000000000000155, 0.4575000000000000178, 0.4600000000000000200, 0.4625000000000000222, 0.4650000000000000244, 0.4675000000000000266, 0.4699999999999999734, 0.4724999999999999756, 0.4749999999999999778, 0.4774999999999999800, 0.4799999999999999822, 0.4824999999999999845, 0.4849999999999999867, 0.4874999999999999889, 0.4899999999999999911, 0.4924999999999999933, 0.4949999999999999956, 0.4974999999999999978, 0.5000000000000000000, 0.5024999999999999467, 0.5050000000000000044, 0.5074999999999999512, 0.5100000000000000089, 0.5124999999999999556, 0.5150000000000000133, 0.5174999999999999600, 0.5200000000000000178, 0.5224999999999999645, 0.5250000000000000222, 0.5274999999999999689, 0.5300000000000000266, 0.5324999999999999734, 0.5350000000000000311, 0.5374999999999999778, 0.5400000000000000355, 0.5424999999999999822, 0.5450000000000000400, 0.5474999999999999867, 0.5500000000000000444, 0.5524999999999999911, 0.5550000000000000488, 0.5574999999999999956, 0.5600000000000000533, 0.5625000000000000000, 0.5649999999999999467, 0.5675000000000000044, 0.5699999999999999512, 0.5725000000000000089, 0.5749999999999999556, 0.5775000000000000133, 0.5799999999999999600, 0.5825000000000000178, 0.5849999999999999645, 0.5875000000000000222, 0.5899999999999999689, 0.5925000000000000266, 0.5949999999999999734, 0.5975000000000000311, 0.5999999999999999778, 0.6025000000000000355, 0.6049999999999999822, 0.6075000000000000400, 0.6099999999999999867, 0.6125000000000000444, 0.6149999999999999911, 0.6175000000000000488, 0.6199999999999999956, 0.6225000000000000533, 0.6250000000000000000, 0.6274999999999999467, 0.6300000000000000044, 0.6324999999999999512, 0.6350000000000000089, 0.6374999999999999556, 0.6400000000000000133, 0.6424999999999999600, 0.6450000000000000178, 0.6474999999999999645, 0.6500000000000000222, 0.6524999999999999689, 0.6550000000000000266, 0.6574999999999999734, 0.6600000000000000311, 0.6624999999999999778, 0.6650000000000000355, 0.6674999999999999822, 0.6700000000000000400, 0.6724999999999999867, 0.6750000000000000444, 0.6774999999999999911, 0.6800000000000000488, 0.6824999999999999956, 0.6850000000000000533, 0.6875000000000000000, 0.6899999999999999467, 0.6925000000000000044, 0.6949999999999999512, 0.6975000000000000089, 0.6999999999999999556, 0.7025000000000000133, 0.7049999999999999600, 0.7075000000000000178, 0.7099999999999999645, 0.7125000000000000222, 0.7149999999999999689, 0.7175000000000000266, 0.7199999999999999734, 0.7225000000000000311, 0.7249999999999999778, 0.7275000000000000355, 0.7299999999999999822, 0.7325000000000000400, 0.7349999999999999867, 0.7375000000000000444, 0.7399999999999999911, 0.7425000000000000488, 0.7449999999999999956, 0.7475000000000000533, 0.7500000000000000000, 0.7524999999999999467, 0.7550000000000000044, 0.7574999999999999512, 0.7600000000000000089, 0.7624999999999999556, 0.7650000000000000133, 0.7674999999999999600, 0.7700000000000000178, 0.7724999999999999645, 0.7750000000000000222, 0.7774999999999999689, 0.7800000000000000266, 0.7824999999999999734, 0.7850000000000000311, 0.7874999999999999778, 0.7900000000000000355, 0.7924999999999999822, 0.7950000000000000400, 0.7974999999999999867, 0.8000000000000000444, 0.8024999999999999911, 0.8050000000000000488, 0.8074999999999999956, 0.8100000000000000533, 0.8125000000000000000, 0.8149999999999999467, 0.8175000000000000044, 0.8199999999999999512, 0.8225000000000000089, 0.8249999999999999556, 0.8275000000000000133, 0.8299999999999999600, 0.8325000000000000178, 0.8349999999999999645, 0.8375000000000000222, 0.8399999999999999689, 0.8425000000000000266, 0.8449999999999999734, 0.8475000000000000311, 0.8499999999999999778, 0.8525000000000000355, 0.8549999999999999822, 0.8575000000000000400, 0.8599999999999999867, 0.8625000000000000444, 0.8649999999999999911, 0.8675000000000000488, 0.8699999999999999956, 0.8725000000000000533, 0.8750000000000000000, 0.8774999999999999467, 0.8800000000000000044, 0.8824999999999999512, 0.8850000000000000089, 0.8874999999999999556, 0.8900000000000000133, 0.8924999999999999600, 0.8950000000000000178, 0.8974999999999999645, 0.9000000000000000222, 0.9024999999999999689, 0.9050000000000000266, 0.9074999999999999734, 0.9100000000000000311, 0.9124999999999999778, 0.9150000000000000355, 0.9174999999999999822, 0.9200000000000000400, 0.9224999999999999867, 0.9250000000000000444, 0.9274999999999999911, 0.9300000000000000488, 0.9324999999999999956, 0.9350000000000000533, 0.9375000000000000000, 0.9399999999999999467, 0.9425000000000000044, 0.9449999999999999512, 0.9475000000000000089, 0.9499999999999999556, 0.9525000000000000133, 0.9549999999999999600, 0.9575000000000000178, 0.9599999999999999645, 0.9625000000000000222, 0.9649999999999999689, 0.9675000000000000266, 0.9699999999999999734, 0.9725000000000000311, 0.9749999999999999778, 0.9775000000000000355, 0.9799999999999999822, 0.9825000000000000400, 0.9849999999999999867, 0.9875000000000000444, 0.9899999999999999911, 0.9925000000000000488, 0.9949999999999999956, 0.9975000000000000533, 1.000000000000000000 ),
 .UNSPECIFIED. ) 
 GEOMETRIC_REPRESENTATION_ITEM ( )  RATIONAL_B_SPLINE_SURFACE ( (
 ( 1.000000000000000000, 0.9238795325112869605, 1.000000000000000000, 0.9238795325112869605, 1.000000000000000000, 0.9238795325112869605, 1.000000000000000000, 0.9238795325112869605, 1.000000000000000000, 0.9238795325112869605, 1.000000000000000000, 0.9238795325112869605, 1.000000000000000000, 0.9238795325112869605, 1.000000000000000000, 0.9238795325112869605, 1.000000000000000000, 0.9238795325112869605, 1.000000000000000000, 0.9238795325112869605, 1.000000000000000000, 0.9238795325112869605, 1.000000000000000000, 0.9238795325112869605, 1.000000000000000000, 0.9238795325112869605, 1.000000000000000000, 0.9238795325112869605, 1.000000000000000000, 0.9238795325112869605, 1.000000000000000000, 0.9238795325112869605, 1.000000000000000000, 0.9238795325112869605, 1.000000000000000000, 0.9238795325112869605, 1.000000000000000000, 0.9238795325112869605, 1.000000000000000000, 0.9238795325112869605, 1.000000000000000000, 0.9238795325112869605, 1.000000000000000000, 0.9238795325112869605, 1.000000000000000000, 0.9238795325112869605, 1.000000000000000000, 0.9238795325112869605, 1.000000000000000000, 0.9238795325112869605, 1.000000000000000000, 0.9238795325112869605, 1.000000000000000000, 0.9238795325112869605, 1.000000000000000000, 0.9238795325112869605, 1.000000000000000000, 0.9238795325112869605, 1.000000000000000000, 0.9238795325112869605, 1.000000000000000000, 0.9238795325112869605, 1.000000000000000000, 0.9238795325112869605, 1.000000000000000000, 0.9238795325112869605, 1.000000000000000000, 0.9238795325112869605, 1.000000000000000000, 0.9238795325112869605, 1.000000000000000000, 0.9238795325112869605, 1.000000000000000000, 0.9238795325112869605, 1.000000000000000000, 0.9238795325112869605, 1.000000000000000000, 0.9238795325112869605, 1.000000000000000000, 0.9238795325112869605, 1.000000000000000000, 0.9238795325112869605, 1.000000000000000000, 0.9238795325112869605, 1.000000000000000000, 0.9238795325112869605, 1.000000000000000000, 0.9238795325112869605, 1.000000000000000000, 0.9238795325112869605, 1.000000000000000000, 0.9238795325112869605, 1.000000000000000000, 0.9238795325112869605, 1.000000000000000000, 0.9238795325112869605, 1.000000000000000000, 0.9238795325112869605, 1.000000000000000000, 0.9238795325112869605, 1.000000000000000000, 0.9238795325112869605, 1.000000000000000000, 0.9238795325112869605, 1.000000000000000000, 0.9238795325112869605, 1.000000000000000000, 0.9238795325112869605, 1.000000000000000000, 0.9238795325112869605, 1.000000000000000000, 0.9238795325112869605, 1.000000000000000000, 0.9238795325112869605, 1.000000000000000000, 0.9238795325112869605, 1.000000000000000000, 0.9238795325112869605, 1.000000000000000000, 0.9238795325112869605, 1.000000000000000000, 0.9238795325112869605, 1.000000000000000000, 0.9238795325112869605, 1.000000000000000000, 0.9238795325112869605, 1.000000000000000000, 0.9238795325112869605, 1.000000000000000000, 0.9238795325112869605, 1.000000000000000000, 0.9238795325112869605, 1.000000000000000000, 0.9238795325112869605, 1.000000000000000000, 0.9238795325112869605, 1.000000000000000000, 0.9238795325112869605, 1.000000000000000000, 0.9238795325112869605, 1.000000000000000000, 0.9238795325112869605, 1.000000000000000000, 0.9238795325112869605, 1.000000000000000000, 0.9238795325112869605, 1.000000000000000000, 0.9238795325112869605, 1.000000000000000000, 0.9238795325112869605, 1.000000000000000000, 0.9238795325112869605, 1.000000000000000000, 0.9238795325112869605, 1.000000000000000000, 0.9238795325112869605, 1.000000000000000000, 0.9238795325112869605, 1.000000000000000000, 0.9238795325112869605, 1.000000000000000000, 0.9238795325112869605, 1.000000000000000000, 0.9238795325112869605, 1.000000000000000000, 0.9238795325112869605, 1.000000000000000000, 0.9238795325112869605, 1.000000000000000000, 0.9238795325112869605, 1.000000000000000000, 0.9238795325112869605, 1.000000000000000000, 0.9238795325112869605, 1.000000000000000000, 0.9238795325112869605, 1.000000000000000000, 0.9238795325112869605, 1.000000000000000000, 0.9238795325112869605, 1.000000000000000000, 0.9238795325112869605, 1.000000000000000000, 0.9238795325112869605, 1.000000000000000000, 0.9238795325112869605, 1.000000000000000000, 0.9238795325112869605, 1.000000000000000000, 0.9238795325112869605, 1.000000000000000000, 0.9238795325112869605, 1.000000000000000000, 0.9238795325112869605, 1.000000000000000000, 0.9238795325112869605, 1.000000000000000000, 0.9238795325112869605, 1.000000000000000000, 0.9238795325112869605, 1.000000000000000000, 0.9238795325112869605, 1.000000000000000000, 0.9238795325112869605, 1.000000000000000000, 0.9238795325112869605, 1.000000000000000000, 0.9238795325112869605, 1.000000000000000000, 0.9238795325112869605, 1.000000000000000000, 0.9238795325112869605, 1.000000000000000000, 0.9238795325112869605, 1.000000000000000000, 0.9238795325112869605, 1.000000000000000000, 0.9238795325112869605, 1.000000000000000000, 0.9238795325112869605, 1.000000000000000000, 0.9238795325112869605, 1.000000000000000000, 0.9238795325112869605, 1.000000000000000000, 0.9238795325112869605, 1.000000000000000000, 0.9238795325112869605, 1.000000000000000000, 0.9238795325112869605, 1.000000000000000000, 0.9238795325112869605, 1.000000000000000000, 0.9238795325112869605, 1.000000000000000000, 0.9238795325112869605, 1.000000000000000000, 0.9238795325112869605, 1.000000000000000000, 0.9238795325112869605, 1.000000000000000000, 0.9238795325112869605, 1.000000000000000000, 0.9238795325112869605, 1.000000000000000000, 0.9238795325112869605, 1.000000000000000000, 0.9238795325112869605, 1.000000000000000000, 0.9238795325112869605, 1.000000000000000000, 0.9238795325112869605, 1.000000000000000000, 0.9238795325112869605, 1.000000000000000000, 0.9238795325112869605, 1.000000000000000000, 0.9238795325112869605, 1.000000000000000000, 0.9238795325112869605, 1.000000000000000000, 0.9238795325112869605, 1.000000000000000000, 0.9238795325112869605, 1.000000000000000000, 0.9238795325112869605, 1.000000000000000000, 0.9238795325112869605, 1.000000000000000000, 0.9238795325112869605, 1.000000000000000000, 0.9238795325112869605, 1.000000000000000000, 0.9238795325112869605, 1.000000000000000000, 0.9238795325112869605, 1.000000000000000000, 0.9238795325112869605, 1.000000000000000000, 0.9238795325112869605, 1.000000000000000000, 0.9238795325112869605, 1.000000000000000000, 0.9238795325112869605, 1.000000000000000000, 0.9238795325112869605, 1.000000000000000000, 0.9238795325112869605, 1.000000000000000000, 0.9238795325112869605, 1.000000000000000000, 0.9238795325112869605, 1.000000000000000000, 0.9238795325112869605, 1.000000000000000000, 0.9238795325112869605, 1.000000000000000000, 0.9238795325112869605, 1.000000000000000000, 0.9238795325112869605, 1.000000000000000000, 0.9238795325112869605, 1.000000000000000000, 0.9238795325112869605, 1.000000000000000000, 0.9238795325112869605, 1.000000000000000000, 0.9238795325112869605, 1.000000000000000000, 0.9238795325112869605, 1.000000000000000000, 0.9238795325112869605, 1.000000000000000000, 0.9238795325112869605, 1.000000000000000000, 0.9238795325112869605, 1.000000000000000000, 0.9238795325112869605, 1.000000000000000000, 0.9238795325112869605, 1.000000000000000000, 0.9238795325112869605, 1.000000000000000000, 0.9238795325112869605, 1.000000000000000000, 0.9238795325112869605, 1.000000000000000000, 0.9238795325112869605, 1.000000000000000000, 0.9238795325112869605, 1.000000000000000000, 0.9238795325112869605, 1.000000000000000000, 0.9238795325112869605, 1.000000000000000000, 0.9238795325112869605, 1.000000000000000000, 0.9238795325112869605, 1.000000000000000000, 0.9238795325112869605, 1.000000000000000000, 0.9238795325112869605, 1.000000000000000000, 0.9238795325112869605, 1.000000000000000000, 0.9238795325112869605, 1.000000000000000000, 0.9238795325112869605, 1.000000000000000000, 0.9238795325112869605, 1.000000000000000000, 0.9238795325112869605, 1.000000000000000000, 0.9238795325112869605, 1.000000000000000000, 0.9238795325112869605, 1.000000000000000000, 0.9238795325112869605, 1.000000000000000000, 0.9238795325112869605, 1.000000000000000000, 0.9238795325112869605, 1.000000000000000000, 0.9238795325112869605, 1.000000000000000000, 0.9238795325112869605, 1.000000000000000000, 0.9238795325112869605, 1.000000000000000000, 0.9238795325112869605, 1.000000000000000000, 0.9238795325112869605, 1.000000000000000000, 0.9238795325112869605, 1.000000000000000000, 0.9238795325112869605, 1.000000000000000000, 0.9238795325112869605, 1.000000000000000000, 0.9238795325112869605, 1.000000000000000000, 0.9238795325112869605, 1.000000000000000000, 0.9238795325112869605, 1.000000000000000000, 0.9238795325112869605, 1.000000000000000000, 0.9238795325112869605, 1.000000000000000000, 0.9238795325112869605, 1.000000000000000000, 0.9238795325112869605, 1.000000000000000000, 0.9238795325112869605, 1.000000000000000000, 0.9238795325112869605, 1.000000000000000000, 0.9238795325112869605, 1.000000000000000000, 0.9238795325112869605, 1.000000000000000000, 0.9238795325112869605, 1.000000000000000000, 0.9238795325112869605, 1.000000000000000000, 0.9238795325112869605, 1.000000000000000000, 0.9238795325112869605, 1.000000000000000000, 0.9238795325112869605, 1.000000000000000000, 0.9238795325112869605, 1.000000000000000000, 0.9238795325112869605, 1.000000000000000000, 0.9238795325112869605, 1.000000000000000000, 0.9238795325112869605, 1.000000000000000000, 0.9238795325112869605, 1.000000000000000000, 0.9238795325112869605, 1.000000000000000000, 0.9238795325112869605, 1.000000000000000000, 0.9238795325112869605, 1.000000000000000000, 0.9238795325112869605, 1.000000000000000000, 0.9238795325112869605, 1.000000000000000000, 0.9238795325112869605, 1.000000000000000000, 0.9238795325112869605, 1.000000000000000000, 0.9238795325112869605, 1.000000000000000000, 0.9238795325112869605, 1.000000000000000000, 0.9238795325112869605, 1.000000000000000000, 0.9238795325112869605, 1.000000000000000000, 0.9238795325112869605, 1.000000000000000000, 0.9238795325112869605, 1.000000000000000000, 0.9238795325112869605, 1.000000000000000000, 0.9238795325112869605, 1.000000000000000000, 0.9238795325112869605, 1.000000000000000000, 0.9238795325112869605, 1.000000000000000000, 0.9238795325112869605, 1.000000000000000000, 0.9238795325112869605, 1.000000000000000000, 0.9238795325112869605, 1.000000000000000000, 0.9238795325112869605, 1.000000000000000000, 0.9238795325112869605, 1.000000000000000000, 0.9238795325112869605, 1.000000000000000000, 0.9238795325112869605, 1.000000000000000000, 0.9238795325112869605, 1.000000000000000000, 0.9238795325112869605, 1.000000000000000000, 0.9238795325112869605, 1.000000000000000000, 0.9238795325112869605, 1.000000000000000000, 0.9238795325112869605, 1.000000000000000000, 0.9238795325112869605, 1.000000000000000000, 0.9238795325112869605, 1.000000000000000000, 0.9238795325112869605, 1.000000000000000000, 0.9238795325112869605, 1.000000000000000000, 0.9238795325112869605, 1.000000000000000000, 0.9238795325112869605, 1.000000000000000000, 0.9238795325112869605, 1.000000000000000000, 0.9238795325112869605, 1.000000000000000000, 0.9238795325112869605, 1.000000000000000000, 0.9238795325112869605, 1.000000000000000000, 0.9238795325112869605, 1.000000000000000000, 0.9238795325112869605, 1.000000000000000000, 0.9238795325112869605, 1.000000000000000000, 0.9238795325112869605, 1.000000000000000000, 0.9238795325112869605, 1.000000000000000000, 0.9238795325112869605, 1.000000000000000000, 0.9238795325112869605, 1.000000000000000000, 0.9238795325112869605, 1.000000000000000000, 0.9238795325112869605, 1.000000000000000000, 0.9238795325112869605, 1.000000000000000000, 0.9238795325112869605, 1.000000000000000000, 0.9238795325112869605, 1.000000000000000000, 0.9238795325112869605, 1.000000000000000000, 0.9238795325112869605, 1.000000000000000000, 0.9238795325112869605, 1.000000000000000000, 0.9238795325112869605, 1.000000000000000000, 0.9238795325112869605, 1.000000000000000000, 0.9238795325112869605, 1.000000000000000000, 0.9238795325112869605, 1.000000000000000000, 0.9238795325112869605, 1.000000000000000000, 0.9238795325112869605, 1.000000000000000000, 0.9238795325112869605, 1.000000000000000000, 0.9238795325112869605, 1.000000000000000000, 0.9238795325112869605, 1.000000000000000000, 0.9238795325112869605, 1.000000000000000000, 0.9238795325112869605, 1.000000000000000000, 0.9238795325112869605, 1.000000000000000000, 0.9238795325112869605, 1.000000000000000000, 0.9238795325112869605, 1.000000000000000000, 0.9238795325112869605, 1.000000000000000000, 0.9238795325112869605, 1.000000000000000000, 0.9238795325112869605, 1.000000000000000000, 0.9238795325112869605, 1.000000000000000000, 0.9238795325112869605, 1.000000000000000000, 0.9238795325112869605, 1.000000000000000000, 0.9238795325112869605, 1.000000000000000000, 0.9238795325112869605, 1.000000000000000000, 0.9238795325112869605, 1.000000000000000000, 0.9238795325112869605, 1.000000000000000000, 0.9238795325112869605, 1.000000000000000000, 0.9238795325112869605, 1.000000000000000000, 0.9238795325112869605, 1.000000000000000000, 0.9238795325112869605, 1.000000000000000000, 0.9238795325112869605, 1.000000000000000000, 0.9238795325112869605, 1.000000000000000000, 0.9238795325112869605, 1.000000000000000000, 0.9238795325112869605, 1.000000000000000000, 0.9238795325112869605, 1.000000000000000000, 0.9238795325112869605, 1.000000000000000000, 0.9238795325112869605, 1.000000000000000000, 0.9238795325112869605, 1.000000000000000000, 0.9238795325112869605, 1.000000000000000000, 0.9238795325112869605, 1.000000000000000000, 0.9238795325112869605, 1.000000000000000000, 0.9238795325112869605, 1.000000000000000000, 0.9238795325112869605, 1.000000000000000000, 0.9238795325112869605, 1.000000000000000000, 0.9238795325112869605, 1.000000000000000000, 0.9238795325112869605, 1.000000000000000000, 0.9238795325112869605, 1.000000000000000000, 0.9238795325112869605, 1.000000000000000000, 0.9238795325112869605, 1.000000000000000000, 0.9238795325112869605, 1.000000000000000000, 0.9238795325112869605, 1.000000000000000000, 0.9238795325112869605, 1.000000000000000000, 0.9238795325112869605, 1.000000000000000000, 0.9238795325112869605, 1.000000000000000000, 0.9238795325112869605, 1.000000000000000000, 0.9238795325112869605, 1.000000000000000000, 0.9238795325112869605, 1.000000000000000000, 0.9238795325112869605, 1.000000000000000000, 0.9238795325112869605, 1.000000000000000000, 0.9238795325112869605, 1.000000000000000000, 0.9238795325112869605, 1.000000000000000000, 0.9238795325112869605, 1.000000000000000000, 0.9238795325112869605, 1.000000000000000000, 0.9238795325112869605, 1.000000000000000000, 0.9238795325112869605, 1.000000000000000000, 0.9238795325112869605, 1.000000000000000000, 0.9238795325112869605, 1.000000000000000000, 0.9238795325112869605, 1.000000000000000000, 0.9238795325112869605, 1.000000000000000000, 0.9238795325112869605, 1.000000000000000000, 0.9238795325112869605, 1.000000000000000000, 0.9238795325112869605, 1.000000000000000000, 0.9238795325112869605, 1.000000000000000000, 0.9238795325112869605, 1.000000000000000000, 0.9238795325112869605, 1.000000000000000000, 0.9238795325112869605, 1.000000000000000000, 0.9238795325112869605, 1.000000000000000000, 0.9238795325112869605, 1.000000000000000000, 0.9238795325112869605, 1.000000000000000000, 0.9238795325112869605, 1.000000000000000000, 0.9238795325112869605, 1.000000000000000000, 0.9238795325112869605, 1.000000000000000000, 0.9238795325112869605, 1.000000000000000000, 0.9238795325112869605, 1.000000000000000000, 0.9238795325112869605, 1.000000000000000000, 0.9238795325112869605, 1.000000000000000000, 0.9238795325112869605, 1.000000000000000000, 0.9238795325112869605, 1.000000000000000000, 0.9238795325112869605, 1.000000000000000000, 0.9238795325112869605, 1.000000000000000000, 0.9238795325112869605, 1.000000000000000000, 0.9238795325112869605, 1.000000000000000000, 0.9238795325112869605, 1.000000000000000000, 0.9238795325112869605, 1.000000000000000000, 0.9238795325112869605, 1.000000000000000000, 0.9238795325112869605, 1.000000000000000000, 0.9238795325112869605, 1.000000000000000000, 0.9238795325112869605, 1.000000000000000000, 0.9238795325112869605, 1.000000000000000000, 0.9238795325112869605, 1.000000000000000000, 0.9238795325112869605, 1.000000000000000000, 0.9238795325112869605, 1.000000000000000000, 0.9238795325112869605, 1.000000000000000000, 0.9238795325112869605, 1.000000000000000000, 0.9238795325112869605, 1.000000000000000000, 0.9238795325112869605, 1.000000000000000000, 0.9238795325112869605, 1.000000000000000000, 0.9238795325112869605, 1.000000000000000000, 0.9238795325112869605, 1.000000000000000000, 0.9238795325112869605, 1.000000000000000000, 0.9238795325112869605, 1.000000000000000000, 0.9238795325112869605, 1.000000000000000000, 0.9238795325112869605, 1.000000000000000000, 0.9238795325112869605, 1.000000000000000000, 0.9238795325112869605, 1.000000000000000000, 0.9238795325112869605, 1.000000000000000000, 0.9238795325112869605, 1.000000000000000000, 0.9238795325112869605, 1.000000000000000000, 0.9238795325112869605, 1.000000000000000000, 0.9238795325112869605, 1.000000000000000000, 0.9238795325112869605, 1.000000000000000000, 0.9238795325112869605, 1.000000000000000000, 0.9238795325112869605, 1.000000000000000000, 0.9238795325112869605, 1.000000000000000000, 0.9238795325112869605, 1.000000000000000000, 0.9238795325112869605, 1.000000000000000000, 0.9238795325112869605, 1.000000000000000000, 0.9238795325112869605, 1.000000000000000000, 0.9238795325112869605, 1.000000000000000000, 0.9238795325112869605, 1.000000000000000000, 0.9238795325112869605, 1.000000000000000000, 0.9238795325112869605, 1.000000000000000000, 0.9238795325112869605, 1.000000000000000000, 0.9238795325112869605, 1.000000000000000000, 0.9238795325112869605, 1.000000000000000000, 0.9238795325112869605, 1.000000000000000000, 0.9238795325112869605, 1.000000000000000000, 0.9238795325112869605, 1.000000000000000000),
 ( 1.000000000000000000, 0.9238795325112869605, 1.000000000000000000, 0.9238795325112869605, 1.000000000000000000, 0.9238795325112869605, 1.000000000000000000, 0.9238795325112869605, 1.000000000000000000, 0.9238795325112869605, 1.000000000000000000, 0.9238795325112869605, 1.000000000000000000, 0.9238795325112869605, 1.000000000000000000, 0.9238795325112869605, 1.000000000000000000, 0.9238795325112869605, 1.000000000000000000, 0.9238795325112869605, 1.000000000000000000, 0.9238795325112869605, 1.000000000000000000, 0.9238795325112869605, 1.000000000000000000, 0.9238795325112869605, 1.000000000000000000, 0.9238795325112869605, 1.000000000000000000, 0.9238795325112869605, 1.000000000000000000, 0.9238795325112869605, 1.000000000000000000, 0.9238795325112869605, 1.000000000000000000, 0.9238795325112869605, 1.000000000000000000, 0.9238795325112869605, 1.000000000000000000, 0.9238795325112869605, 1.000000000000000000, 0.9238795325112869605, 1.000000000000000000, 0.9238795325112869605, 1.000000000000000000, 0.9238795325112869605, 1.000000000000000000, 0.9238795325112869605, 1.000000000000000000, 0.9238795325112869605, 1.000000000000000000, 0.9238795325112869605, 1.000000000000000000, 0.9238795325112869605, 1.000000000000000000, 0.9238795325112869605, 1.000000000000000000, 0.9238795325112869605, 1.000000000000000000, 0.9238795325112869605, 1.000000000000000000, 0.9238795325112869605, 1.000000000000000000, 0.9238795325112869605, 1.000000000000000000, 0.9238795325112869605, 1.000000000000000000, 0.9238795325112869605, 1.000000000000000000, 0.9238795325112869605, 1.000000000000000000, 0.9238795325112869605, 1.000000000000000000, 0.9238795325112869605, 1.000000000000000000, 0.9238795325112869605, 1.000000000000000000, 0.9238795325112869605, 1.000000000000000000, 0.9238795325112869605, 1.000000000000000000, 0.9238795325112869605, 1.000000000000000000, 0.9238795325112869605, 1.000000000000000000, 0.9238795325112869605, 1.000000000000000000, 0.9238795325112869605, 1.000000000000000000, 0.9238795325112869605, 1.000000000000000000, 0.9238795325112869605, 1.000000000000000000, 0.9238795325112869605, 1.000000000000000000, 0.9238795325112869605, 1.000000000000000000, 0.9238795325112869605, 1.000000000000000000, 0.9238795325112869605, 1.000000000000000000, 0.9238795325112869605, 1.000000000000000000, 0.9238795325112869605, 1.000000000000000000, 0.9238795325112869605, 1.000000000000000000, 0.9238795325112869605, 1.000000000000000000, 0.9238795325112869605, 1.000000000000000000, 0.9238795325112869605, 1.000000000000000000, 0.9238795325112869605, 1.000000000000000000, 0.9238795325112869605, 1.000000000000000000, 0.9238795325112869605, 1.000000000000000000, 0.9238795325112869605, 1.000000000000000000, 0.9238795325112869605, 1.000000000000000000, 0.9238795325112869605, 1.000000000000000000, 0.9238795325112869605, 1.000000000000000000, 0.9238795325112869605, 1.000000000000000000, 0.9238795325112869605, 1.000000000000000000, 0.9238795325112869605, 1.000000000000000000, 0.9238795325112869605, 1.000000000000000000, 0.9238795325112869605, 1.000000000000000000, 0.9238795325112869605, 1.000000000000000000, 0.9238795325112869605, 1.000000000000000000, 0.9238795325112869605, 1.000000000000000000, 0.9238795325112869605, 1.000000000000000000, 0.9238795325112869605, 1.000000000000000000, 0.9238795325112869605, 1.000000000000000000, 0.9238795325112869605, 1.000000000000000000, 0.9238795325112869605, 1.000000000000000000, 0.9238795325112869605, 1.000000000000000000, 0.9238795325112869605, 1.000000000000000000, 0.9238795325112869605, 1.000000000000000000, 0.9238795325112869605, 1.000000000000000000, 0.9238795325112869605, 1.000000000000000000, 0.9238795325112869605, 1.000000000000000000, 0.9238795325112869605, 1.000000000000000000, 0.9238795325112869605, 1.000000000000000000, 0.9238795325112869605, 1.000000000000000000, 0.9238795325112869605, 1.000000000000000000, 0.9238795325112869605, 1.000000000000000000, 0.9238795325112869605, 1.000000000000000000, 0.9238795325112869605, 1.000000000000000000, 0.9238795325112869605, 1.000000000000000000, 0.9238795325112869605, 1.000000000000000000, 0.9238795325112869605, 1.000000000000000000, 0.9238795325112869605, 1.000000000000000000, 0.9238795325112869605, 1.000000000000000000, 0.9238795325112869605, 1.000000000000000000, 0.9238795325112869605, 1.000000000000000000, 0.9238795325112869605, 1.000000000000000000, 0.9238795325112869605, 1.000000000000000000, 0.9238795325112869605, 1.000000000000000000, 0.9238795325112869605, 1.000000000000000000, 0.9238795325112869605, 1.000000000000000000, 0.9238795325112869605, 1.000000000000000000, 0.9238795325112869605, 1.000000000000000000, 0.9238795325112869605, 1.000000000000000000, 0.9238795325112869605, 1.000000000000000000, 0.9238795325112869605, 1.000000000000000000, 0.9238795325112869605, 1.000000000000000000, 0.9238795325112869605, 1.000000000000000000, 0.9238795325112869605, 1.000000000000000000, 0.9238795325112869605, 1.000000000000000000, 0.9238795325112869605, 1.000000000000000000, 0.9238795325112869605, 1.000000000000000000, 0.9238795325112869605, 1.000000000000000000, 0.9238795325112869605, 1.000000000000000000, 0.9238795325112869605, 1.000000000000000000, 0.9238795325112869605, 1.000000000000000000, 0.9238795325112869605, 1.000000000000000000, 0.9238795325112869605, 1.000000000000000000, 0.9238795325112869605, 1.000000000000000000, 0.9238795325112869605, 1.000000000000000000, 0.9238795325112869605, 1.000000000000000000, 0.9238795325112869605, 1.000000000000000000, 0.9238795325112869605, 1.000000000000000000, 0.9238795325112869605, 1.000000000000000000, 0.9238795325112869605, 1.000000000000000000, 0.9238795325112869605, 1.000000000000000000, 0.9238795325112869605, 1.000000000000000000, 0.9238795325112869605, 1.000000000000000000, 0.9238795325112869605, 1.000000000000000000, 0.9238795325112869605, 1.000000000000000000, 0.9238795325112869605, 1.000000000000000000, 0.9238795325112869605, 1.000000000000000000, 0.9238795325112869605, 1.000000000000000000, 0.9238795325112869605, 1.000000000000000000, 0.9238795325112869605, 1.000000000000000000, 0.9238795325112869605, 1.000000000000000000, 0.9238795325112869605, 1.000000000000000000, 0.9238795325112869605, 1.000000000000000000, 0.9238795325112869605, 1.000000000000000000, 0.9238795325112869605, 1.000000000000000000, 0.9238795325112869605, 1.000000000000000000, 0.9238795325112869605, 1.000000000000000000, 0.9238795325112869605, 1.000000000000000000, 0.9238795325112869605, 1.000000000000000000, 0.9238795325112869605, 1.000000000000000000, 0.9238795325112869605, 1.000000000000000000, 0.9238795325112869605, 1.000000000000000000, 0.9238795325112869605, 1.000000000000000000, 0.9238795325112869605, 1.000000000000000000, 0.9238795325112869605, 1.000000000000000000, 0.9238795325112869605, 1.000000000000000000, 0.9238795325112869605, 1.000000000000000000, 0.9238795325112869605, 1.000000000000000000, 0.9238795325112869605, 1.000000000000000000, 0.9238795325112869605, 1.000000000000000000, 0.9238795325112869605, 1.000000000000000000, 0.9238795325112869605, 1.000000000000000000, 0.9238795325112869605, 1.000000000000000000, 0.9238795325112869605, 1.000000000000000000, 0.9238795325112869605, 1.000000000000000000, 0.9238795325112869605, 1.000000000000000000, 0.9238795325112869605, 1.000000000000000000, 0.9238795325112869605, 1.000000000000000000, 0.9238795325112869605, 1.000000000000000000, 0.9238795325112869605, 1.000000000000000000, 0.9238795325112869605, 1.000000000000000000, 0.9238795325112869605, 1.000000000000000000, 0.9238795325112869605, 1.000000000000000000, 0.9238795325112869605, 1.000000000000000000, 0.9238795325112869605, 1.000000000000000000, 0.9238795325112869605, 1.000000000000000000, 0.9238795325112869605, 1.000000000000000000, 0.9238795325112869605, 1.000000000000000000, 0.9238795325112869605, 1.000000000000000000, 0.9238795325112869605, 1.000000000000000000, 0.9238795325112869605, 1.000000000000000000, 0.9238795325112869605, 1.000000000000000000, 0.9238795325112869605, 1.000000000000000000, 0.9238795325112869605, 1.000000000000000000, 0.9238795325112869605, 1.000000000000000000, 0.9238795325112869605, 1.000000000000000000, 0.9238795325112869605, 1.000000000000000000, 0.9238795325112869605, 1.000000000000000000, 0.9238795325112869605, 1.000000000000000000, 0.9238795325112869605, 1.000000000000000000, 0.9238795325112869605, 1.000000000000000000, 0.9238795325112869605, 1.000000000000000000, 0.9238795325112869605, 1.000000000000000000, 0.9238795325112869605, 1.000000000000000000, 0.9238795325112869605, 1.000000000000000000, 0.9238795325112869605, 1.000000000000000000, 0.9238795325112869605, 1.000000000000000000, 0.9238795325112869605, 1.000000000000000000, 0.9238795325112869605, 1.000000000000000000, 0.9238795325112869605, 1.000000000000000000, 0.9238795325112869605, 1.000000000000000000, 0.9238795325112869605, 1.000000000000000000, 0.9238795325112869605, 1.000000000000000000, 0.9238795325112869605, 1.000000000000000000, 0.9238795325112869605, 1.000000000000000000, 0.9238795325112869605, 1.000000000000000000, 0.9238795325112869605, 1.000000000000000000, 0.9238795325112869605, 1.000000000000000000, 0.9238795325112869605, 1.000000000000000000, 0.9238795325112869605, 1.000000000000000000, 0.9238795325112869605, 1.000000000000000000, 0.9238795325112869605, 1.000000000000000000, 0.9238795325112869605, 1.000000000000000000, 0.9238795325112869605, 1.000000000000000000, 0.9238795325112869605, 1.000000000000000000, 0.9238795325112869605, 1.000000000000000000, 0.9238795325112869605, 1.000000000000000000, 0.9238795325112869605, 1.000000000000000000, 0.9238795325112869605, 1.000000000000000000, 0.9238795325112869605, 1.000000000000000000, 0.9238795325112869605, 1.000000000000000000, 0.9238795325112869605, 1.000000000000000000, 0.9238795325112869605, 1.000000000000000000, 0.9238795325112869605, 1.000000000000000000, 0.9238795325112869605, 1.000000000000000000, 0.9238795325112869605, 1.000000000000000000, 0.9238795325112869605, 1.000000000000000000, 0.9238795325112869605, 1.000000000000000000, 0.9238795325112869605, 1.000000000000000000, 0.9238795325112869605, 1.000000000000000000, 0.9238795325112869605, 1.000000000000000000, 0.9238795325112869605, 1.000000000000000000, 0.9238795325112869605, 1.000000000000000000, 0.9238795325112869605, 1.000000000000000000, 0.9238795325112869605, 1.000000000000000000, 0.9238795325112869605, 1.000000000000000000, 0.9238795325112869605, 1.000000000000000000, 0.9238795325112869605, 1.000000000000000000, 0.9238795325112869605, 1.000000000000000000, 0.9238795325112869605, 1.000000000000000000, 0.9238795325112869605, 1.000000000000000000, 0.9238795325112869605, 1.000000000000000000, 0.9238795325112869605, 1.000000000000000000, 0.9238795325112869605, 1.000000000000000000, 0.9238795325112869605, 1.000000000000000000, 0.9238795325112869605, 1.000000000000000000, 0.9238795325112869605, 1.000000000000000000, 0.9238795325112869605, 1.000000000000000000, 0.9238795325112869605, 1.000000000000000000, 0.9238795325112869605, 1.000000000000000000, 0.9238795325112869605, 1.000000000000000000, 0.9238795325112869605, 1.000000000000000000, 0.9238795325112869605, 1.000000000000000000, 0.9238795325112869605, 1.000000000000000000, 0.9238795325112869605, 1.000000000000000000, 0.9238795325112869605, 1.000000000000000000, 0.9238795325112869605, 1.000000000000000000, 0.9238795325112869605, 1.000000000000000000, 0.9238795325112869605, 1.000000000000000000, 0.9238795325112869605, 1.000000000000000000, 0.9238795325112869605, 1.000000000000000000, 0.9238795325112869605, 1.000000000000000000, 0.9238795325112869605, 1.000000000000000000, 0.9238795325112869605, 1.000000000000000000, 0.9238795325112869605, 1.000000000000000000, 0.9238795325112869605, 1.000000000000000000, 0.9238795325112869605, 1.000000000000000000, 0.9238795325112869605, 1.000000000000000000, 0.9238795325112869605, 1.000000000000000000, 0.9238795325112869605, 1.000000000000000000, 0.9238795325112869605, 1.000000000000000000, 0.9238795325112869605, 1.000000000000000000, 0.9238795325112869605, 1.000000000000000000, 0.9238795325112869605, 1.000000000000000000, 0.9238795325112869605, 1.000000000000000000, 0.9238795325112869605, 1.000000000000000000, 0.9238795325112869605, 1.000000000000000000, 0.9238795325112869605, 1.000000000000000000, 0.9238795325112869605, 1.000000000000000000, 0.9238795325112869605, 1.000000000000000000, 0.9238795325112869605, 1.000000000000000000, 0.9238795325112869605, 1.000000000000000000, 0.9238795325112869605, 1.000000000000000000, 0.9238795325112869605, 1.000000000000000000, 0.9238795325112869605, 1.000000000000000000, 0.9238795325112869605, 1.000000000000000000, 0.9238795325112869605, 1.000000000000000000, 0.9238795325112869605, 1.000000000000000000, 0.9238795325112869605, 1.000000000000000000, 0.9238795325112869605, 1.000000000000000000, 0.9238795325112869605, 1.000000000000000000, 0.9238795325112869605, 1.000000000000000000, 0.9238795325112869605, 1.000000000000000000, 0.9238795325112869605, 1.000000000000000000, 0.9238795325112869605, 1.000000000000000000, 0.9238795325112869605, 1.000000000000000000, 0.9238795325112869605, 1.000000000000000000, 0.9238795325112869605, 1.000000000000000000, 0.9238795325112869605, 1.000000000000000000, 0.9238795325112869605, 1.000000000000000000, 0.9238795325112869605, 1.000000000000000000, 0.9238795325112869605, 1.000000000000000000, 0.9238795325112869605, 1.000000000000000000, 0.9238795325112869605, 1.000000000000000000, 0.9238795325112869605, 1.000000000000000000, 0.9238795325112869605, 1.000000000000000000, 0.9238795325112869605, 1.000000000000000000, 0.9238795325112869605, 1.000000000000000000, 0.9238795325112869605, 1.000000000000000000, 0.9238795325112869605, 1.000000000000000000, 0.9238795325112869605, 1.000000000000000000, 0.9238795325112869605, 1.000000000000000000, 0.9238795325112869605, 1.000000000000000000, 0.9238795325112869605, 1.000000000000000000, 0.9238795325112869605, 1.000000000000000000, 0.9238795325112869605, 1.000000000000000000, 0.9238795325112869605, 1.000000000000000000, 0.9238795325112869605, 1.000000000000000000, 0.9238795325112869605, 1.000000000000000000, 0.9238795325112869605, 1.000000000000000000, 0.9238795325112869605, 1.000000000000000000, 0.9238795325112869605, 1.000000000000000000, 0.9238795325112869605, 1.000000000000000000, 0.9238795325112869605, 1.000000000000000000, 0.9238795325112869605, 1.000000000000000000, 0.9238795325112869605, 1.000000000000000000, 0.9238795325112869605, 1.000000000000000000, 0.9238795325112869605, 1.000000000000000000, 0.9238795325112869605, 1.000000000000000000, 0.9238795325112869605, 1.000000000000000000, 0.9238795325112869605, 1.000000000000000000, 0.9238795325112869605, 1.000000000000000000, 0.9238795325112869605, 1.000000000000000000, 0.9238795325112869605, 1.000000000000000000, 0.9238795325112869605, 1.000000000000000000, 0.9238795325112869605, 1.000000000000000000, 0.9238795325112869605, 1.000000000000000000, 0.9238795325112869605, 1.000000000000000000, 0.9238795325112869605, 1.000000000000000000, 0.9238795325112869605, 1.000000000000000000, 0.9238795325112869605, 1.000000000000000000, 0.9238795325112869605, 1.000000000000000000, 0.9238795325112869605, 1.000000000000000000, 0.9238795325112869605, 1.000000000000000000, 0.9238795325112869605, 1.000000000000000000, 0.9238795325112869605, 1.000000000000000000, 0.9238795325112869605, 1.000000000000000000, 0.9238795325112869605, 1.000000000000000000, 0.9238795325112869605, 1.000000000000000000, 0.9238795325112869605, 1.000000000000000000, 0.9238795325112869605, 1.000000000000000000, 0.9238795325112869605, 1.000000000000000000, 0.9238795325112869605, 1.000000000000000000, 0.9238795325112869605, 1.000000000000000000, 0.9238795325112869605, 1.000000000000000000, 0.9238795325112869605, 1.000000000000000000, 0.9238795325112869605, 1.000000000000000000, 0.9238795325112869605, 1.000000000000000000, 0.9238795325112869605, 1.000000000000000000, 0.9238795325112869605, 1.000000000000000000, 0.9238795325112869605, 1.000000000000000000, 0.9238795325112869605, 1.000000000000000000, 0.9238795325112869605, 1.000000000000000000, 0.9238795325112869605, 1.000000000000000000, 0.9238795325112869605, 1.000000000000000000, 0.9238795325112869605, 1.000000000000000000, 0.9238795325112869605, 1.000000000000000000, 0.9238795325112869605, 1.000000000000000000, 0.9238795325112869605, 1.000000000000000000, 0.9238795325112869605, 1.000000000000000000, 0.9238795325112869605, 1.000000000000000000, 0.9238795325112869605, 1.000000000000000000, 0.9238795325112869605, 1.000000000000000000, 0.9238795325112869605, 1.000000000000000000, 0.9238795325112869605, 1.000000000000000000, 0.9238795325112869605, 1.000000000000000000, 0.9238795325112869605, 1.000000000000000000, 0.9238795325112869605, 1.000000000000000000, 0.9238795325112869605, 1.000000000000000000, 0.9238795325112869605, 1.000000000000000000, 0.9238795325112869605, 1.000000000000000000, 0.9238795325112869605, 1.000000000000000000, 0.9238795325112869605, 1.000000000000000000, 0.9238795325112869605, 1.000000000000000000, 0.9238795325112869605, 1.000000000000000000, 0.9238795325112869605, 1.000000000000000000, 0.9238795325112869605, 1.000000000000000000, 0.9238795325112869605, 1.000000000000000000, 0.9238795325112869605, 1.000000000000000000, 0.9238795325112869605, 1.000000000000000000, 0.9238795325112869605, 1.000000000000000000, 0.9238795325112869605, 1.000000000000000000, 0.9238795325112869605, 1.000000000000000000, 0.9238795325112869605, 1.000000000000000000, 0.9238795325112869605, 1.000000000000000000, 0.9238795325112869605, 1.000000000000000000, 0.9238795325112869605, 1.000000000000000000, 0.9238795325112869605, 1.000000000000000000, 0.9238795325112869605, 1.000000000000000000, 0.9238795325112869605, 1.000000000000000000, 0.9238795325112869605, 1.000000000000000000, 0.9238795325112869605, 1.000000000000000000, 0.9238795325112869605, 1.000000000000000000, 0.9238795325112869605, 1.000000000000000000, 0.9238795325112869605, 1.000000000000000000) ) ) 
 REPRESENTATION_ITEM ( '' )  SURFACE ( )  ) ;
#46837=CARTESIAN_POINT ( 'NONE',  ( 0.9500414927467377701, 0.1787899950787401604, 1.210629921206079818 ) ) ;
#46838=CARTESIAN_POINT ( 'NONE',  ( -0.8107537697050254399, 0.1574803149606300301, 1.951279527559056870 ) ) ;
#46839=CARTESIAN_POINT ( 'NONE',  ( 1.033464566929134687, -0.06523048226347956391, 0.4306102361129448552 ) ) ;
#46843=CARTESIAN_POINT ( 'NONE',  ( 0.8700650591850297433, 0.1747820667289631535, 0.03936860327882610311 ) ) ;
#46844=CARTESIAN_POINT ( 'NONE',  ( -0.8759842519685039353, -0.1574803149606299191, 0.3444881888688507976 ) ) ;
#46845=CARTESIAN_POINT ( 'NONE',  ( -0.7646288533564489232, -0.1113553986120547346, 1.530511811023621993 ) ) ;
#46846=CARTESIAN_POINT ( 'NONE',  ( 1.002407869896990045, 0.1264236179284866091, 1.523129921206078707 ) ) ;
#46848=CARTESIAN_POINT ( 'NONE',  ( -0.8107537697050254399, -0.1574803149606297803, 1.769192913385826404 ) ) ;
#46849=CARTESIAN_POINT ( 'NONE',  ( 0.9412147342319837628, -0.1574803149606297803, 1.183562992125983593 ) ) ;
#46851=VERTEX_POINT ( 'NONE', #9058 ) ;
#46854=ORIENTED_EDGE ( 'NONE', *, *, #20886, .T. ) ;
#46857=DIRECTION ( 'NONE',  ( 0.000000000000000000, 0.000000000000000000, 1.000000000000000000 ) ) ;
#46858=CARTESIAN_POINT ( 'NONE',  ( 1.054774247047244540, -0.07405724077823318263, 0.5364173227808821665 ) ) ;
#46861=CARTESIAN_POINT ( 'NONE',  ( -1.054774247047244096, 0.000000000000000000, 1.090059055064346527 ) ) ;
#46864=CARTESIAN_POINT ( 'NONE',  ( -0.9412147342319837628, -0.1574803149606297803, 0.1993110236220472509 ) ) ;
#46866=CARTESIAN_POINT ( 'NONE',  ( -0.7495606340400177148, 0.1264236179284866091, 0.8292322834108031282 ) ) ;
#46867=CARTESIAN_POINT ( 'NONE',  ( -0.6971942568897626646, 0.07405724077823318263, 0.2017716534895435399 ) ) ;
#46871=ORIENTED_EDGE ( 'NONE', *, *, #27399, .T. ) ;
#46872=CARTESIAN_POINT ( 'NONE',  ( -0.7185039370078746268, 0.06523048226347956391, 0.06643700787401589369 ) ) ;
#46874=ORIENTED_EDGE ( 'NONE', *, *, #36744, .F. ) ;
#46876=DIRECTION ( 'NONE',  ( 1.000000000000000000, 0.000000000000000000, -1.822029033848725275E-16 ) ) ;
#46877=CARTESIAN_POINT ( 'NONE',  ( -0.8019270111902717657, -0.1787899950787401604, 0.6003937007336380693 ) ) ;
#46878=DIRECTION ( 'NONE',  ( 0.000000000000000000, 0.000000000000000000, -1.000000000000000000 ) ) ;
#46880=CARTESIAN_POINT ( 'NONE',  ( -0.6971942568897637749, 2.189545951927499583E-17, 1.779035433017102319 ) ) ;
#46883=CARTESIAN_POINT ( 'NONE',  ( -0.9873396505805591694, 0.1113553986120547346, 0.4872047244094488416 ) ) ;
#46884=ORIENTED_EDGE ( 'NONE', *, *, #1721, .F. ) ;
#46885=CARTESIAN_POINT ( 'NONE',  ( 0.8759842519685039353, -0.1574803149606299191, 0.6299212598425196763 ) ) ;
#46887=CARTESIAN_POINT ( 'NONE',  ( -0.9412147342319837628, 0.1574803149606300301, 0.9621062992125994917 ) ) ;
#46888=CARTESIAN_POINT ( 'NONE',  ( -0.9873396505805591694, 0.1113553986120547346, 1.422244094380661572 ) ) ;
#46889=CARTESIAN_POINT ( 'NONE',  ( 1.002407869896990045, 0.1264236179284866091, 0.7800196849856062542 ) ) ;
#46893=CARTESIAN_POINT ( 'NONE',  ( 0.7185039370078746268, -0.06523048226347956391, 1.213090551181103427 ) ) ;
#46894=CARTESIAN_POINT ( 'NONE',  ( 0.9325001150361308389, -0.1669857002805301138, 1.989206133734520154 ) ) ;
#46897=ADVANCED_FACE ( 'NONE', ( #22727 ), #31126, .T. ) ;
#46898=CARTESIAN_POINT ( 'NONE',  ( 0.9500414927467377701, 0.1787899950787401604, 0.6594488188438737408 ) ) ;
#46900=DIRECTION ( 'NONE',  ( -4.336808689942014285E-16, 0.000000000000000000, -1.000000000000000000 ) ) ;
#46903=CARTESIAN_POINT ( 'NONE',  ( 0.9412147342319837628, -0.1574803149606297803, 1.734744094488190003 ) ) ;
#46904=CARTESIAN_POINT ( 'NONE',  ( 0.8107537697050254399, -0.1574803149606297803, 0.7062007874015745479 ) ) ;
#46905=CARTESIAN_POINT ( 'NONE',  ( 0.6971942568897626646, 0.07405724077823318263, 0.9448818897100165204 ) ) ;
#46908=CARTESIAN_POINT ( 'NONE',  ( 0.7185039370078746268, 0.06523048226347956391, 1.483759842519686067 ) ) ;
#46913=CARTESIAN_POINT ( 'NONE',  ( 1.033464566929133799, 0.000000000000000000, 1.230314960629921295 ) ) ;
#46915=CARTESIAN_POINT ( 'NONE',  ( -1.002407869896990045, -0.1264236179284866091, 0.1353346456155277433 ) ) ;
#46920=CARTESIAN_POINT ( 'NONE',  ( -1.002407869896990045, 0.1264236179284866091, 1.961122047190330786 ) ) ;
#46921=CARTESIAN_POINT ( 'NONE',  ( -0.7495606340400177148, -0.1264236179284866091, 1.582185039316315045 ) ) ;
#46922=CARTESIAN_POINT ( 'NONE',  ( 0.7495606340400177148, -0.1264236179284866091, 0.8784448818360000022 ) ) ;
#46923=CARTESIAN_POINT ( 'NONE',  ( -0.6971942568897637749, 2.189545951927499583E-17, 0.8292322834108031282 ) ) ;
#46924=CARTESIAN_POINT ( 'NONE',  ( -1.054774247047244540, -0.07405724077823318263, 0.3789370078202520253 ) ) ;
#46927=CARTESIAN_POINT ( 'NONE',  ( -1.002407869896990045, 0.1264236179284866091, 1.882381889710015743 ) ) ;
#46928=CARTESIAN_POINT ( 'NONE',  ( -0.7646288533564489232, 0.1113553986120547346, 1.914370078740157632 ) ) ;
#46931=DIRECTION ( 'NONE',  ( -1.000000000000000000, 0.000000000000000000, 0.000000000000000000 ) ) ;
#46935=CARTESIAN_POINT ( 'NONE',  ( -0.8759842519685039353, -0.1787899950787401882, 0.09104330703285078152 ) ) ;
#46938=CARTESIAN_POINT ( 'NONE',  ( -0.8019270111902716547, 0.1787899950787401604, 1.220472440891118504 ) ) ;
#46942=DIRECTION ( 'NONE',  ( 1.822029033848725028E-16, 0.000000000000000000, 1.000000000000000000 ) ) ;
#46943=CARTESIAN_POINT ( 'NONE',  ( 0.7646288533564489232, -0.1113553986120547346, 0.3494094488188976277 ) ) ;
#46944=DIRECTION ( 'NONE',  ( 1.000000000000000000, 0.000000000000000000, 0.000000000000000000 ) ) ;
#46945=CARTESIAN_POINT ( 'NONE',  ( -0.8759842519685039353, -0.1574803149606299191, 0.8956692912310552090 ) ) ;
#46946=CARTESIAN_POINT ( 'NONE',  ( -0.8759842519685039353, 0.1574803149606299191, 0.7677165354330708347 ) ) ;
#46948=CARTESIAN_POINT ( 'NONE',  ( 1.033464566929133799, 0.000000000000000000, 1.811023621939716444 ) ) ;
#46951=CARTESIAN_POINT ( 'NONE',  ( 0.7185039370078746268, -0.06523048226347956391, 0.8587598425196850682 ) ) ;
#46955=( BOUNDED_CURVE ( )  B_SPLINE_CURVE ( 2, ( #22604, #4605, #19712, #16142, #37216, #19238, #4849, #37696, #23323 ),
 .UNSPECIFIED., .F., .F. ) 
 B_SPLINE_CURVE_WITH_KNOTS ( ( 3, 2, 2, 2, 3 ),
 ( 0.3499999999999999778, 0.3524999999999999800, 0.3549999999999999822, 0.3574999999999999845, 0.3599999999999999867 ),
 .UNSPECIFIED. ) 
 CURVE ( )  GEOMETRIC_REPRESENTATION_ITEM ( )  RATIONAL_B_SPLINE_CURVE ( ( 1.000000000000000000, 0.9238795325112879597, 1.000000000000000000, 0.9238795325112869605, 1.000000000000000000, 0.9238795325112869605, 1.000000000000000000, 0.9238795325112869605, 1.000000000000000000 ) ) 
 REPRESENTATION_ITEM ( '' )  ) ;
#46956=EDGE_CURVE ( 'NONE', #23930, #19760, #5926, .T. ) ;
#46959=CARTESIAN_POINT ( 'NONE',  ( 0.7185039370078746268, -0.06523048226347956391, 0.1402559054042841202 ) ) ;
#46966=CARTESIAN_POINT ( 'NONE',  ( 0.7185039370078746268, -0.06523048226347956391, 0.9276574802074333270 ) ) ;
#46968=CARTESIAN_POINT ( 'NONE',  ( -0.6971942568897626646, -0.07405724077823297447, 0.4379921259304882519 ) ) ;
#46971=CARTESIAN_POINT ( 'NONE',  ( -0.8019270111902717657, -0.1787899950787401604, 1.628937007820252303 ) ) ;
#46972=CARTESIAN_POINT ( 'NONE',  ( -0.8019270111902717657, -0.1787899950787401604, 0.8021653542769460188 ) ) ;
#46973=CARTESIAN_POINT ( 'NONE',  ( 0.9500414927467378812, -0.1787899950787401604, 0.2165354330171024577 ) ) ;
#46974=CARTESIAN_POINT ( 'NONE',  ( -0.9873396505805591694, -0.1113553986120547346, 1.687992125876724536 ) ) ;
#46975=CARTESIAN_POINT ( 'NONE',  ( 0.6971942568897648851, -0.07405724077823297447, 0.7578740156942688211 ) ) ;
#46976=CARTESIAN_POINT ( 'NONE',  ( -1.002407869896990045, -0.1264236179284866091, 0.7652559054580472253 ) ) ;
#46977=CARTESIAN_POINT ( 'NONE',  ( 0.7185039370078746268, 0.06523048226347956391, 0.9227362203649142058 ) ) ;
#46978=CARTESIAN_POINT ( 'NONE',  ( 0.7185039370078739607, 1.928577636452523993E-17, 1.131889763779527547 ) ) ;
#46980=CARTESIAN_POINT ( 'NONE',  ( -0.7495606340400177148, 0.1264236179284866091, 1.419783464513165505 ) ) ;
#46982=CARTESIAN_POINT ( 'NONE',  ( -0.8759842519685039353, 0.1574803149606299191, 1.515748031496062964 ) ) ;
#46983=CARTESIAN_POINT ( 'NONE',  ( -0.9412147342319837628, 0.1574803149606300301, 0.4109251968503938590 ) ) ;
#46984=CARTESIAN_POINT ( 'NONE',  ( 1.054774247047244540, -0.07405724077823318263, 1.481299212544662902 ) ) ;
#46986=CARTESIAN_POINT ( 'NONE',  ( 0.7185039370078739607, 1.928577636452523993E-17, 1.958661417322834719 ) ) ;
#46991=VERTEX_POINT ( 'NONE', #24383 ) ;
#46992=CARTESIAN_POINT ( 'NONE',  ( 1.033464566929134687, -0.06523048226347956391, 0.4010826771653545619 ) ) ;
#47005=CARTESIAN_POINT ( 'NONE',  ( -0.9412147342319837628, -0.1574803149606297803, 1.695374015748031926 ) ) ;
#47006=CARTESIAN_POINT ( 'NONE',  ( 0.7495606340400177148, -0.1264236179284866091, 0.6766732282926929409 ) ) ;
#47007=CARTESIAN_POINT ( 'NONE',  ( -0.9500414927467377701, 0.1787899950787401604, 0.9793307086076531442 ) ) ;
#47008=EDGE_CURVE ( 'NONE', #27709, #44763, #6220, .T. ) ;
#47009=CARTESIAN_POINT ( 'NONE',  ( -0.8617263095615074198, 0.1748397955725940756, 0.03937007874015843734 ) ) ;
#47011=CYLINDRICAL_SURFACE ( 'NONE', #24599, 0.1574803149606299191 ) ;
#47012=CARTESIAN_POINT ( 'NONE',  ( 0.9500414927467378812, 0.1787899950787401604, 1.687992125930489307 ) ) ;
#47013=FACE_OUTER_BOUND ( 'NONE', #30578, .T. ) ;
#47018=EDGE_CURVE ( 'NONE', #32014, #31452, #27006, .T. ) ;
#47019=CARTESIAN_POINT ( 'NONE',  ( 1.033464566929133799, 0.000000000000000000, 1.338582677057826853 ) ) ;
#47021=CARTESIAN_POINT ( 'NONE',  ( -1.002407869896990045, -0.1264236179284866091, 0.4158464566391496531 ) ) ;
#47022=CARTESIAN_POINT ( 'NONE',  ( 0.6971942568897626646, -0.07405724077823297447, 0.6742125983714335469 ) ) ;
#47024=CARTESIAN_POINT ( 'NONE',  ( 0.9500414927467378812, 0.1787899950787401604, 0.07381889758403178958 ) ) ;
#47027=CARTESIAN_POINT ( 'NONE',  ( -0.9500414927467378812, 0.1787899950787401604, 1.564960629867495845 ) ) ;
#47028=ORIENTED_EDGE ( 'NONE', *, *, #45879, .T. ) ;
#47029=VECTOR ( 'NONE', #8750, 39.37007874015748143 ) ;
#47030=CARTESIAN_POINT ( 'NONE',  ( -0.8019270111902717657, -0.1787899950787401604, 1.117125984198206412 ) ) ;
#47032=CARTESIAN_POINT ( 'NONE',  ( 0.9500414927467378812, 0.1787899950787401604, 1.176181102308441417 ) ) ;
#47035=CARTESIAN_POINT ( 'NONE',  ( -0.7185039370078746268, 0.06523048226347956391, 0.6865157479239701876 ) ) ;
#47036=CARTESIAN_POINT ( 'NONE',  ( 1.054774247047244540, 0.07405724077823318263, 1.874999999946236784 ) ) ;
#47037=CARTESIAN_POINT ( 'NONE',  ( -0.8019270111902717657, -0.1787899950787401604, 0.8759842519147408302 ) ) ;
#47038=CARTESIAN_POINT ( 'NONE',  ( -0.9873396505805591694, -0.1113553986120547346, 1.619094488188976388 ) ) ;
#47040=CARTESIAN_POINT ( 'NONE',  ( 0.6971942568897626646, 0.07405724077823318263, 0.2805118109698587214 ) ) ;
#47041=CARTESIAN_POINT ( 'NONE',  ( -0.8759842519685039353, -0.1787899950787401882, 0.2485236219934806867 ) ) ;
#47042=CARTESIAN_POINT ( 'NONE',  ( -0.8019270111902717657, -0.1787899950787401604, 0.7185039369541108556 ) ) ;
#47043=CARTESIAN_POINT ( 'NONE',  ( 1.033464566929133799, 0.000000000000000000, 1.574803149498771537 ) ) ;
#47047=CARTESIAN_POINT ( 'NONE',  ( 0.8759842519685039353, 0.1787899950787401882, 0.7455708660879684091 ) ) ;
#47048=CARTESIAN_POINT ( 'NONE',  ( 1.054774247047244540, 0.07405724077823318263, 1.013779527505291878 ) ) ;
#47049=CARTESIAN_POINT ( 'NONE',  ( -0.8019270111902716547, -0.1787899950787401604, 1.860236220418677089 ) ) ;
#47050=FACE_OUTER_BOUND ( 'NONE', #8655, .T. ) ;
#47051=CARTESIAN_POINT ( 'NONE',  ( 0.9873396505805591694, 0.1113553986120547346, 1.313976377952756014 ) ) ;
#47055=ORIENTED_EDGE ( 'NONE', *, *, #34521, .F. ) ;
#47056=CARTESIAN_POINT ( 'NONE',  ( 1.002407869896990045, -0.1264236179284866091, 1.119586614119464585 ) ) ;
#47060=CARTESIAN_POINT ( 'NONE',  ( 0.7646288533564489232, -0.1113553986120547346, 1.963582677165354395 ) ) ;
#47067=CARTESIAN_POINT ( 'NONE',  ( -0.8759842519685039353, -0.1787899950787401882, 0.4896653542769449086 ) ) ;
#47070=CARTESIAN_POINT ( 'NONE',  ( 1.054774247047244540, 0.07405724077823318263, 1.210629921206079818 ) ) ;
#47071=CARTESIAN_POINT ( 'NONE',  ( 1.002407869896990045, 0.1264236179284866091, 1.562499999946236118 ) ) ;
#47072=DIRECTION ( 'NONE',  ( 0.000000000000000000, 1.000000000000000000, 0.000000000000000000 ) ) ;
#47073=CARTESIAN_POINT ( 'NONE',  ( 0.7185039370078746268, 0.06523048226347956391, 1.719980314960629864 ) ) ;
#47076=CARTESIAN_POINT ( 'NONE',  ( -0.8759842519685039353, 0.1574803149606299191, 1.742125984144440975 ) ) ;
#47077=CARTESIAN_POINT ( 'NONE',  ( 0.7495606340400177148, -0.1264236179284866091, 0.2436023621509610382 ) ) ;
#47078=CARTESIAN_POINT ( 'NONE',  ( 0.9500414927467377701, 0.1787899950787401604, 1.131889763725763887 ) ) ;
#47082=CARTESIAN_POINT ( 'NONE',  ( 1.033464566929133799, 0.000000000000000000, 0.4330708660342047489 ) ) ;
#47083=VERTEX_POINT ( 'NONE', #40320 ) ;
#47085=CARTESIAN_POINT ( 'NONE',  ( 0.8729137959494666088, 0.1746894649194470073, 0.03936731548249973456 ) ) ;
#47086=CARTESIAN_POINT ( 'NONE',  ( -0.9873396505805591694, -0.1113553986120547346, 0.4675196849318432601 ) ) ;
#47088=CARTESIAN_POINT ( 'NONE',  ( 0.8019270111902717657, -0.1787899950787401604, 1.427165354276944687 ) ) ;
#47089=CARTESIAN_POINT ( 'NONE',  ( -0.7185039370078739607, 1.928577636452523993E-17, 1.131889763779527547 ) ) ;
#47090=CARTESIAN_POINT ( 'NONE',  ( -0.8759842519685039353, 0.000000000000000000, 0.000000000000000000 ) ) ;
#47091=CARTESIAN_POINT ( 'NONE',  ( 0.9412147342319837628, -0.1574803149606297803, 0.07135826760900840227 ) ) ;
#47093=VERTEX_POINT ( 'NONE', #14711 ) ;
#47096=VECTOR ( 'NONE', #14123, 39.37007874015748143 ) ;
#47097=DIRECTION ( 'NONE',  ( 0.000000000000000000, 0.000000000000000000, -1.000000000000000000 ) ) ;
#47099=VERTEX_POINT ( 'NONE', #22357 ) ;
#47101=CARTESIAN_POINT ( 'NONE',  ( 1.002407869896990045, -0.1264236179284866091, 0.6126968503399370380 ) ) ;
#47103=CARTESIAN_POINT ( 'NONE',  ( -0.8759842519685039353, 0.1787899950787401882, 1.449311023568283341 ) ) ;
#47105=CARTESIAN_POINT ( 'NONE',  ( -0.6971942568897648851, 0.07405724077823318263, 1.146653543253323582 ) ) ;
#47108=CARTESIAN_POINT ( 'NONE',  ( -0.7185039370078746268, -0.06523048226347956391, 0.1894685039370080093 ) ) ;
#47109=CARTESIAN_POINT ( 'NONE',  ( -0.9500414927467377701, -0.1787899950787401604, 1.038385826717890259 ) ) ;
#47110=CARTESIAN_POINT ( 'NONE',  ( -0.6971942568897637749, 2.189545951927499583E-17, 0.7554133857730077617 ) ) ;
#47111=( BOUNDED_CURVE ( )  B_SPLINE_CURVE ( 2, ( #24456, #13664, #34790, #31430, #27381, #31668, #27852, #9846, #2632 ),
 .UNSPECIFIED., .F., .F. ) 
 B_SPLINE_CURVE_WITH_KNOTS ( ( 3, 2, 2, 2, 3 ),
 ( 0.1700000000000000122, 0.1724999999999999867, 0.1749999999999999889, 0.1774999999999999911, 0.1799999999999999933 ),
 .UNSPECIFIED. ) 
 CURVE ( )  GEOMETRIC_REPRESENTATION_ITEM ( )  RATIONAL_B_SPLINE_CURVE ( ( 1.000000000000000000, 0.9238795325112849621, 1.000000000000000000, 0.9238795325112869605, 1.000000000000000000, 0.9238795325112869605, 1.000000000000000000, 0.9238795325112869605, 1.000000000000000000 ) ) 
 REPRESENTATION_ITEM ( '' )  ) ;
#47115=CARTESIAN_POINT ( 'NONE',  ( 0.7554274433290401047, 0.1321208994424742933, 0.03937161865901335489 ) ) ;
#47117=CARTESIAN_POINT ( 'NONE',  ( -0.7185039370078746268, -0.06523048226347956391, 0.3371062991050715607 ) ) ;
#47120=CARTESIAN_POINT ( 'NONE',  ( -1.054774247047244096, 0.000000000000000000, 0.6126968503399370380 ) ) ;
#47125=CARTESIAN_POINT ( 'NONE',  ( -0.7495606340400177148, -0.1264236179284866091, 1.823326771599779406 ) ) ;
#47126=AXIS2_PLACEMENT_3D ( 'NONE', #40179, #39947, #18394 ) ;
#47130=( BOUNDED_CURVE ( )  B_SPLINE_CURVE ( 2, ( #16537, #15130, #44556, #7674, #29548, #33119, #15606, #44795, #25444 ),
 .UNSPECIFIED., .F., .F. ) 
 B_SPLINE_CURVE_WITH_KNOTS ( ( 3, 2, 2, 2, 3 ),
 ( 0.8199999999999999512, 0.8225000000000000089, 0.8249999999999999556, 0.8275000000000000133, 0.8299999999999999600 ),
 .UNSPECIFIED. ) 
 CURVE ( )  GEOMETRIC_REPRESENTATION_ITEM ( )  RATIONAL_B_SPLINE_CURVE ( ( 1.000000000000000000, 0.9238795325112899581, 1.000000000000000000, 0.9238795325112869605, 1.000000000000000000, 0.9238795325112869605, 1.000000000000000000, 0.9238795325112829637, 1.000000000000000000 ) ) 
 REPRESENTATION_ITEM ( '' )  ) ;
#47131=CARTESIAN_POINT ( 'NONE',  ( -1.002407869896990045, -0.1264236179284866091, 0.1008858267178899676 ) ) ;
#47132=ORIENTED_EDGE ( 'NONE', *, *, #5795, .T. ) ;
#47133=CARTESIAN_POINT ( 'NONE',  ( 0.7185039370078746268, 0.06523048226347956391, 0.6963582677165359724 ) ) ;
#47135=CARTESIAN_POINT ( 'NONE',  ( -1.033464566929133799, 0.000000000000000000, 0.3937007872940476716 ) ) ;
#47136=CARTESIAN_POINT ( 'NONE',  ( -0.9873396505805591694, 0.1113553986120547346, 1.343503936900346529 ) ) ;
#47137=CARTESIAN_POINT ( 'NONE',  ( 0.6971942568897626646, -0.07405724077823297447, 0.8366141731745828647 ) ) ;
#47139=VECTOR ( 'NONE', #9591, 39.37007874015748143 ) ;
#47141=VERTEX_POINT ( 'NONE', #25967 ) ;
#47143=CARTESIAN_POINT ( 'NONE',  ( 0.9873396505805591694, -0.1113553986120547346, 1.225393700787401619 ) ) ;
#47144=CARTESIAN_POINT ( 'NONE',  ( 0.8435002617486037080, -0.1706024796764649409, 1.987610845726340392 ) ) ;
#47146=CARTESIAN_POINT ( 'NONE',  ( 1.033464566929134687, -0.06523048226347956391, 1.975885826771653475 ) ) ;
#47148=CARTESIAN_POINT ( 'NONE',  ( 0.7495606340400177148, 0.1264236179284866091, 0.7062007873478109987 ) ) ;
#47152=EDGE_LOOP ( 'NONE', ( #45845, #9273, #10215, #35182 ) ) ;
#47155=CARTESIAN_POINT ( 'NONE',  ( 1.002407869896990045, 0.1264236179284866091, 0.9719488188438739629 ) ) ;
#47160=CARTESIAN_POINT ( 'NONE',  ( -1.054774247047244096, 0.000000000000000000, 0.06151574797773248782 ) ) ;
#47162=CARTESIAN_POINT ( 'NONE',  ( 0.8759842519685039353, -0.1787899950787401882, 1.946358267662771757 ) ) ;
#47163=ORIENTED_EDGE ( 'NONE', *, *, #16538, .T. ) ;
#47165=CARTESIAN_POINT ( 'NONE',  ( -0.9500414927467377701, 0.1787899950787401604, 1.924212598371433325 ) ) ;
#47166=CARTESIAN_POINT ( 'NONE',  ( -1.002407869896990045, 0.1264236179284866091, 1.601870078686393750 ) ) ;
#47168=CARTESIAN_POINT ( 'NONE',  ( -0.9500414927467378812, -0.1787899950787401604, 1.077755905458048113 ) ) ;
#47169=CARTESIAN_POINT ( 'NONE',  ( -1.054774247047244540, -0.07405724077823318263, 0.3395669290800945039 ) ) ;
#47171=CARTESIAN_POINT ( 'NONE',  ( -0.8759842519685039353, -0.1787899950787401882, 1.946358267662771757 ) ) ;
#47172=CARTESIAN_POINT ( 'NONE',  ( -0.7185039370078746268, 0.06523048226347956391, 1.483759842519686067 ) ) ;
#47173=CARTESIAN_POINT ( 'NONE',  ( -0.7185039370078746268, 0.06523048226347956391, 1.838090551181102539 ) ) ;
#47174=LINE ( 'NONE', #29946, #38187 ) ;
#47178=CARTESIAN_POINT ( 'NONE',  ( -0.8759842519685039353, 0.000000000000000000, 1.990649606245448844 ) ) ;
#47179=CARTESIAN_POINT ( 'NONE',  ( -1.002407869896990045, -0.1264236179284866091, 0.1353346456155277433 ) ) ;
#47180=EDGE_CURVE ( 'NONE', #6785, #42193, #38710, .T. ) ;
#47183=EDGE_LOOP ( 'NONE', ( #38450, #20736, #14848, #22745 ) ) ;
#47185=CARTESIAN_POINT ( 'NONE',  ( -0.8019270111902716547, 0.1787899950787401604, 1.456692913332062522 ) ) ;
#47191=CARTESIAN_POINT ( 'NONE',  ( 0.8107537697050253289, 0.1574803149606300301, 0.3371062992125987146 ) ) ;
#47193=CARTESIAN_POINT ( 'NONE',  ( -0.8107537697050234415, -0.1574803149606297803, 0.2337598425196851515 ) ) ;
#47194=CARTESIAN_POINT ( 'NONE',  ( -0.8759842519685039353, 0.1574803149606299191, 0.9940944880814488460 ) ) ;
#47195=CARTESIAN_POINT ( 'NONE',  ( 0.6971942568897626646, -0.07405724077823297447, 0.4429133857730075952 ) ) ;
#47197=CARTESIAN_POINT ( 'NONE',  ( 1.033464566929134687, 0.06523048226347956391, 1.892224409341292546 ) ) ;
#47200=CARTESIAN_POINT ( 'NONE',  ( 0.9873396505805591694, 0.1113553986120547346, 0.8021653543307086798 ) ) ;
#47202=CARTESIAN_POINT ( 'NONE',  ( -0.7185039370078746268, 0.06523048226347956391, 1.090059055118109965 ) ) ;
#47205=CARTESIAN_POINT ( 'NONE',  ( 1.033464566929134687, -0.06523048226347956391, 0.1156496061916856694 ) ) ;
#47207=DIRECTION ( 'NONE',  ( 1.000000000000000000, 0.000000000000000000, 0.000000000000000000 ) ) ;
#47212=CARTESIAN_POINT ( 'NONE',  ( 1.033464566929134687, 0.06523048226347956391, 0.9079724408373542888 ) ) ;
#47214=CARTESIAN_POINT ( 'NONE',  ( -0.9500414927467378812, 0.1787899950787401604, 0.3444881889226146243 ) ) ;
#47215=VERTEX_POINT ( 'NONE', #34123 ) ;
#47216=VERTEX_POINT ( 'NONE', #19235 ) ;
#47217=CARTESIAN_POINT ( 'NONE',  ( -0.8759842519685039353, -0.1787899950787401882, 1.670767716481669440 ) ) ;
#47219=CARTESIAN_POINT ( 'NONE',  ( 0.9500414927467378812, 0.1787899950787401604, 1.491141732229701367 ) ) ;
#47220=ORIENTED_EDGE ( 'NONE', *, *, #41846, .F. ) ;
#47221=CARTESIAN_POINT ( 'NONE',  ( -0.8759842519685039353, -0.1787899950787401882, 0.8439960629383622681 ) ) ;
#47222=CARTESIAN_POINT ( 'NONE',  ( -0.9873396505805591694, 0.1113553986120547346, 0.2509842519685039353 ) ) ;
#47223=CARTESIAN_POINT ( 'NONE',  ( 0.8019270111902716547, -0.1787899950787401604, 0.8021653542769462408 ) ) ;
#47224=CARTESIAN_POINT ( 'NONE',  ( -0.8019270111902716547, 0.1787899950787401604, 0.6643700786863951935 ) ) ;
#47226=CARTESIAN_POINT ( 'NONE',  ( 0.9873396505805591694, -0.1113553986120547346, 1.146653543307086798 ) ) ;
#47228=CARTESIAN_POINT ( 'NONE',  ( -1.033464566929133799, 0.000000000000000000, 1.850393700679873854 ) ) ;
#47229=VERTEX_POINT ( 'NONE', #1481 ) ;
#47230=CARTESIAN_POINT ( 'NONE',  ( -1.033464566929134687, 0.06523048226347956391, 0.4847440944881890590 ) ) ;
#47231=CARTESIAN_POINT ( 'NONE',  ( 0.6971942568897648851, -0.07405724077823297447, 1.427165354276944687 ) ) ;
#47233=CARTESIAN_POINT ( 'NONE',  ( -0.8107537697050254399, -0.1574803149606297803, 1.572342519685040907 ) ) ;
#47236=VERTEX_POINT ( 'NONE', #41479 ) ;
#47243=CARTESIAN_POINT ( 'NONE',  ( 0.9873396505805591694, 0.1113553986120547346, 1.038385826771653475 ) ) ;
#47245=CARTESIAN_POINT ( 'NONE',  ( 0.9500414927467378812, 0.1787899950787401604, 1.722440944828125930 ) ) ;
#47246=CARTESIAN_POINT ( 'NONE',  ( 0.6971942568897626646, 0.07405724077823318263, 0.2755905511273391006 ) ) ;
#47251=CARTESIAN_POINT ( 'NONE',  ( 0.7646288533564489232, -0.1113553986120547346, 0.1427165353255439029 ) ) ;
#47252=CARTESIAN_POINT ( 'NONE',  ( 0.8759842519685039353, -0.1787899950787401882, 0.6028543306548976854 ) ) ;
#47254=CARTESIAN_POINT ( 'NONE',  ( -1.002407869896990045, -0.1264236179284866091, 1.006397637741511808 ) ) ;
#47255=CARTESIAN_POINT ( 'NONE',  ( -0.8759842519685039353, 0.000000000000000000, 0.000000000000000000 ) ) ;
#47256=CARTESIAN_POINT ( 'NONE',  ( 0.9412147342319837628, 0.1574803149606300301, 1.700295275483023172 ) ) ;
#47259=CARTESIAN_POINT ( 'NONE',  ( 0.7495606340400177148, -0.1264236179284866091, 1.626476377898992132 ) ) ;
#47260=CARTESIAN_POINT ( 'NONE',  ( 0.7646288533564489232, 0.1113553986120547346, 0.1328740156405045225 ) ) ;
#47261=VERTEX_POINT ( 'NONE', #19471 ) ;
#47262=CARTESIAN_POINT ( 'NONE',  ( -0.7185039370078739607, 1.928577636452523993E-17, 1.407480314960629864 ) ) ;
#47265=CARTESIAN_POINT ( 'NONE',  ( -0.9500414927467378812, -0.1787899950787401604, 0.4527559054580477249 ) ) ;
#47267=CARTESIAN_POINT ( 'NONE',  ( 0.9500414927467378812, 0.1787899950787401604, 0.6200787401037165525 ) ) ;
#47268=EDGE_CURVE ( 'NONE', #29740, #18622, #2851, .T. ) ;
#47270=CARTESIAN_POINT ( 'NONE',  ( 0.8019270111902717657, 0.1787899950787401604, 0.1574803149068664809 ) ) ;
#47271=CARTESIAN_POINT ( 'NONE',  ( 0.9412147342319837628, 0.1574803149606300301, 1.109744094380661350 ) ) ;
#47272=CARTESIAN_POINT ( 'NONE',  ( -0.7495606340400177148, -0.1264236179284866091, 1.660925196796630088 ) ) ;
#47273=ORIENTED_EDGE ( 'NONE', *, *, #46745, .F. ) ;
#47274=CARTESIAN_POINT ( 'NONE',  ( -0.8759842519685039353, -0.1787899950787401882, 1.198326771599779628 ) ) ;
#47276=CARTESIAN_POINT ( 'NONE',  ( 0.8019270111902717657, 0.1787899950787401604, 1.141732283410804349 ) ) ;
#47278=CARTESIAN_POINT ( 'NONE',  ( 0.8759842519685039353, 0.1787899950787401882, 1.803641732229700700 ) ) ;
#47279=CARTESIAN_POINT ( 'NONE',  ( -0.7185039370078739607, 1.928577636452523993E-17, 0.6200787401574803237 ) ) ;
#47280=CARTESIAN_POINT ( 'NONE',  ( -0.9500414927467378812, -0.1787899950787401604, 0.8415354330171019859 ) ) ;
#47282=CARTESIAN_POINT ( 'NONE',  ( -1.033464566929133799, 0.000000000000000000, 1.338582677057826853 ) ) ;
#47283=CARTESIAN_POINT ( 'NONE',  ( 0.6971942568897637749, 2.189545951927499583E-17, 0.3617125983714334359 ) ) ;
#47284=CARTESIAN_POINT ( 'NONE',  ( -0.6971942568897637749, 2.189545951927499583E-17, 0.1599409448281264023 ) ) ;
#47285=CARTESIAN_POINT ( 'NONE',  ( -0.6971942568897626646, -0.07405724077823297447, 0.7923228345919055560 ) ) ;
#47286=CARTESIAN_POINT ( 'NONE',  ( 0.8107537697050253289, 0.1574803149606300301, 1.587106299105073060 ) ) ;
#47290=CARTESIAN_POINT ( 'NONE',  ( 0.9500414927467378812, 0.1787899950787401604, 0.8218503936470251681 ) ) ;
#47291=CARTESIAN_POINT ( 'NONE',  ( 0.7495606340400177148, 0.1264236179284866091, 1.104822834591905556 ) ) ;
#47292=CARTESIAN_POINT ( 'NONE',  ( -0.6971942568897637749, 2.189545951927499583E-17, 1.892224409395055096 ) ) ;
#47294=CARTESIAN_POINT ( 'NONE',  ( 0.8759842519685039353, 0.1787899950787401882, 1.961122047190330786 ) ) ;
#47297=EDGE_CURVE ( 'NONE', #1535, #5296, #30529, .T. ) ;
#47304=CARTESIAN_POINT ( 'NONE',  ( 0.6971942568897637749, 2.189545951927499583E-17, 1.144192913332062966 ) ) ;
#47305=ADVANCED_FACE ( 'NONE', ( #13251 ), #39084, .T. ) ;
#47307=CARTESIAN_POINT ( 'NONE',  ( 1.033464566929133799, 0.000000000000000000, 1.377952755797984263 ) ) ;
#47309=CARTESIAN_POINT ( 'NONE',  ( 0.7185039370078739607, 1.928577636452523993E-17, 1.919291338582677309 ) ) ;
#47312=CARTESIAN_POINT ( 'NONE',  ( -0.6971942568897637749, 2.189545951927499583E-17, 0.5191929133320630774 ) ) ;
#47316=CARTESIAN_POINT ( 'NONE',  ( 0.6971942568897637749, 2.189545951927502049E-17, 1.990649606245448844 ) ) ;
#47317=CARTESIAN_POINT ( 'NONE',  ( 1.054774247047244540, -0.07405724077823318263, 1.205708661363558365 ) ) ;
#47318=CARTESIAN_POINT ( 'NONE',  ( 1.054774247047244096, 0.000000000000000000, 1.675688976324189117 ) ) ;
#47319=CARTESIAN_POINT ( 'NONE',  ( -0.7185039370078746268, 0.06523048226347956391, 0.6077755904436539236 ) ) ;
#47321=CARTESIAN_POINT ( 'NONE',  ( -0.7579867284075441081, 0.1110391951864165283, 1.980897914036486407 ) ) ;
#47324=CARTESIAN_POINT ( 'NONE',  ( -0.9873396505805591694, -0.1113553986120547346, 1.766732283357039135 ) ) ;
#47326=CARTESIAN_POINT ( 'NONE',  ( 0.6971942568897637749, 2.189545951927499583E-17, 0.1205708660879689087 ) ) ;
#47328=CARTESIAN_POINT ( 'NONE',  ( 0.7027460018079232373, -0.01315211221934205719, 0.03936999329196508302 ) ) ;
#47329=CARTESIAN_POINT ( 'NONE',  ( 0.6971942568897648851, -0.07405724077823297447, 1.264763779473795813 ) ) ;
#47330=CARTESIAN_POINT ( 'NONE',  ( -0.7185039370078739607, 1.928577636452523993E-17, 0.5314960628845992741 ) ) ;
#47332=CARTESIAN_POINT ( 'NONE',  ( -0.7495606340400177148, -0.1264236179284866091, 1.188484251914740275 ) ) ;
#47333=CARTESIAN_POINT ( 'NONE',  ( 0.8759842519685039353, 0.1574803149606299191, 0.5216535431995598104 ) ) ;
#47335=CARTESIAN_POINT ( 'NONE',  ( -0.8759842519685039353, 0.1787899950787401882, 1.060531496009228247 ) ) ;
#47337=CARTESIAN_POINT ( 'NONE',  ( 0.8584509703022565885, 0.1747054016738197046, 0.03937131093437663820 ) ) ;
#47338=CARTESIAN_POINT ( 'NONE',  ( -0.8759842519685039353, -0.1574803149606299191, 0.4232283463491653963 ) ) ;
#47339=ORIENTED_EDGE ( 'NONE', *, *, #40067, .F. ) ;
#47340=CARTESIAN_POINT ( 'NONE',  ( 0.6971942568897637749, 2.189545951927499583E-17, 1.380413385773007873 ) ) ;
#47341=CARTESIAN_POINT ( 'NONE',  ( -0.7185039370078739607, 1.928577636452523993E-17, 1.082677165246803241 ) ) ;
#47343=CARTESIAN_POINT ( 'NONE',  ( -0.9873396505805591694, -0.1113553986120547346, 0.1230314960629921295 ) ) ;
#47344=CARTESIAN_POINT ( 'NONE',  ( 0.7185039370078739607, 1.928577636452523993E-17, 1.171259842519684957 ) ) ;
#47347=DIRECTION ( 'NONE',  ( 1.822029033848725028E-16, 0.000000000000000000, 1.000000000000000000 ) ) ;
#47351=CARTESIAN_POINT ( 'NONE',  ( 0.6971942568897637749, 2.189545951927499583E-17, 0.6373031495525354195 ) ) ;
#47352=EDGE_CURVE ( 'NONE', #9783, #740, #38978, .T. ) ;
#47355=CARTESIAN_POINT ( 'NONE',  ( -0.8759842519685039353, 0.1787899950787401882, 1.139271653489543290 ) ) ;
#47357=CARTESIAN_POINT ( 'NONE',  ( -1.054774247047244096, 0.000000000000000000, 1.085137795221826629 ) ) ;
#47360=CARTESIAN_POINT ( 'NONE',  ( -0.7495606340400177148, -0.1264236179284866091, 0.2091535432533232486 ) ) ;
#47361=CARTESIAN_POINT ( 'NONE',  ( 1.033464566929133799, 0.000000000000000000, 1.269685039370078705 ) ) ;
#47362=CARTESIAN_POINT ( 'NONE',  ( 0.9412147342319837628, -0.1574803149606297803, 1.646161417215307843 ) ) ;
#47367=ORIENTED_EDGE ( 'NONE', *, *, #30541, .F. ) ;
#47368=CARTESIAN_POINT ( 'NONE',  ( 1.002407869896990045, 0.1264236179284866091, 1.011318897584031484 ) ) ;
#47371=CARTESIAN_POINT ( 'NONE',  ( -1.054774247047244096, 0.000000000000000000, 0.7308070865604093802 ) ) ;
#47372=CARTESIAN_POINT ( 'NONE',  ( -0.8759842519685039353, 0.1787899950787401882, 1.769192913332062966 ) ) ;
#47373=CARTESIAN_POINT ( 'NONE',  ( -0.9500414927467377701, 0.1787899950787401604, 0.1131889763241892000 ) ) ;
#47374=CARTESIAN_POINT ( 'NONE',  ( 0.7185039370078746268, 0.06523048226347956391, 0.6569881889763781180 ) ) ;
#47377=CARTESIAN_POINT ( 'NONE',  ( -0.7646288533564489232, 0.1113553986120547346, 1.432086614065700925 ) ) ;
#47378=CARTESIAN_POINT ( 'NONE',  ( 0.9500414927467378812, -0.1787899950787401604, 0.7677165353793073965 ) ) ;
#47379=CARTESIAN_POINT ( 'NONE',  ( 0.9500414927467377701, 0.1787899950787401604, 1.368110236166710125 ) ) ;
#47381=FACE_OUTER_BOUND ( 'NONE', #46394, .T. ) ;
#47383=CARTESIAN_POINT ( 'NONE',  ( 0.7185039370078746268, -0.06523048226347956391, 1.449311023622047445 ) ) ;
#47384=CARTESIAN_POINT ( 'NONE',  ( 0.9537752801991592477, -0.1590467385219253571, 1.989622353916787878 ) ) ;
#47385=CARTESIAN_POINT ( 'NONE',  ( 1.033464566929134687, -0.06523048226347956391, 1.572342519577513142 ) ) ;
#47386=CARTESIAN_POINT ( 'NONE',  ( 0.9873396505805591694, -0.1113553986120547346, 1.727362204616881947 ) ) ;
#47387=CARTESIAN_POINT ( 'NONE',  ( 0.8759842519685039353, -0.1787899950787401882, 0.7209645668753701386 ) ) ;
#47392=CARTESIAN_POINT ( 'NONE',  ( 1.033464566929134687, -0.06523048226347956391, 0.6274606298137325178 ) ) ;
#47394=CARTESIAN_POINT ( 'NONE',  ( 1.054774247047244540, 0.07405724077823318263, 1.048228346402928723 ) ) ;
#47398=CARTESIAN_POINT ( 'NONE',  ( 0.7185039370078746268, 0.06523048226347956391, 1.247539370078740273 ) ) ;
#47399=( BOUNDED_CURVE ( )  B_SPLINE_CURVE ( 2, ( #33614, #25476, #40515, #18954, #728, #11322, #40745, #3876, #25711 ),
 .UNSPECIFIED., .F., .T. ) 
 B_SPLINE_CURVE_WITH_KNOTS ( ( 3, 2, 2, 2, 3 ),
 ( 0.9300000000000000488, 0.9324999999999999956, 0.9350000000000000533, 0.9375000000000000000, 0.9399999999999999467 ),
 .UNSPECIFIED. ) 
 CURVE ( )  GEOMETRIC_REPRESENTATION_ITEM ( )  RATIONAL_B_SPLINE_CURVE ( ( 1.000000000000000000, 0.9238795325112899581, 1.000000000000000000, 0.9238795325112869605, 1.000000000000000000, 0.9238795325112869605, 1.000000000000000000, 0.9238795325112829637, 1.000000000000000000 ) ) 
 REPRESENTATION_ITEM ( '' )  ) ;
#47400=CARTESIAN_POINT ( 'NONE',  ( -0.8759842519685039353, -0.1787899950787401882, 0.05167322829269314910 ) ) ;
#47405=CARTESIAN_POINT ( 'NONE',  ( -0.8019270111902716547, -0.1787899950787401604, 1.943897637741510254 ) ) ;
#47406=CARTESIAN_POINT ( 'NONE',  ( -0.8759842519685039353, -0.1787899950787401882, 1.744586614119464807 ) ) ;
#47407=CARTESIAN_POINT ( 'NONE',  ( -0.7495606340400177148, 0.1264236179284866091, 0.4355314960092284138 ) ) ;
#47408=CARTESIAN_POINT ( 'NONE',  ( -0.8759842519685039353, -0.1574803149606299191, 1.801181102254677091 ) ) ;
#47410=CARTESIAN_POINT ( 'NONE',  ( 0.8019270111902717657, 0.1787899950787401604, 0.03444881884387430981 ) ) ;
#47414=FACE_OUTER_BOUND ( 'NONE', #30406, .T. ) ;
#47416=( BOUNDED_CURVE ( )  B_SPLINE_CURVE ( 2, ( #22714, #4471, #30419, #11466, #11954 ),
 .UNSPECIFIED., .F., .T. ) 
 B_SPLINE_CURVE_WITH_KNOTS ( ( 3, 2, 3 ),
 ( 0.9799999999999999822, 0.9825000000000000400, 0.9850000000591240257 ),
 .UNSPECIFIED. ) 
 CURVE ( )  GEOMETRIC_REPRESENTATION_ITEM ( )  RATIONAL_B_SPLINE_CURVE ( ( 1.000000000000000000, 0.9238795325112869605, 1.000000000000000000, 0.9238795325112869605, 1.000000000000000000 ) ) 
 REPRESENTATION_ITEM ( '' )  ) ;
#47417=CARTESIAN_POINT ( 'NONE',  ( -0.8759842519685039353, -0.1787899950787401882, 0.3272637794737956463 ) ) ;
#47418=CARTESIAN_POINT ( 'NONE',  ( -0.7108038343253642033, 0.06841996760810098444, 0.03937007874015843040 ) ) ;
#47420=CARTESIAN_POINT ( 'NONE',  ( 0.7185039370078746268, -0.06523048226347956391, 1.606791338582677309 ) ) ;
#47423=CARTESIAN_POINT ( 'NONE',  ( -1.002407869896990045, 0.1264236179284866091, 1.370570866087968520 ) ) ;
#47426=AXIS2_PLACEMENT_3D ( 'NONE', #19454, #41005, #45075 ) ;
#47430=CARTESIAN_POINT ( 'NONE',  ( 0.9873396505805591694, -0.1113553986120547346, 0.3198818897637795700 ) ) ;
#47432=CARTESIAN_POINT ( 'NONE',  ( -0.8107537697050253289, -0.1574803149606297803, 0.9719488187901104137 ) ) ;
#47433=AXIS2_PLACEMENT_3D ( 'NONE', #11645, #11401, #26739 ) ;
#47434=CARTESIAN_POINT ( 'NONE',  ( 0.6971942568897637749, 2.189545951927499583E-17, 0.4798228345919055560 ) ) ;
#47437=CARTESIAN_POINT ( 'NONE',  ( 1.033464566929134687, -0.06523048226347956391, 1.808562992018457383 ) ) ;
#47440=CARTESIAN_POINT ( 'NONE',  ( 1.033464566929134687, -0.06523048226347956391, 0.8341535433070870198 ) ) ;
#47443=CARTESIAN_POINT ( 'NONE',  ( -1.033464566929134687, -0.06523048226347956391, 0.8341535433070870198 ) ) ;
#47445=ORIENTED_EDGE ( 'NONE', *, *, #25974, .T. ) ;
#47446=ADVANCED_FACE ( 'NONE', ( #39559 ), #6026, .T. ) ;
#47447=CARTESIAN_POINT ( 'NONE',  ( -0.9873396505805591694, -0.1113553986120547346, 0.6249999998924724576 ) ) ;
#47451=CARTESIAN_POINT ( 'NONE',  ( -1.033464566929134687, 0.06523048226347956391, 0.1205708660342053040 ) ) ;
#47453=CARTESIAN_POINT ( 'NONE',  ( 0.8759842519685039353, -0.1574803149606299191, 0.8956692912310552090 ) ) ;
#47454=EDGE_CURVE ( 'NONE', #2356, #47099, #34115, .T. ) ;
#47456=VECTOR ( 'NONE', #36148, 39.37007874015748143 ) ;
#47457=CARTESIAN_POINT ( 'NONE',  ( -1.054774247047244540, 0.07405724077823318263, 0.3789370078202520253 ) ) ;
#47459=CARTESIAN_POINT ( 'NONE',  ( -1.002407869896990045, -0.1264236179284866091, 1.675688976324189117 ) ) ;
#47460=ORIENTED_EDGE ( 'NONE', *, *, #23617, .F. ) ;
ENDSEC;
END-ISO-10303-21;
